ISO-10303-21;
HEADER;
FILE_DESCRIPTION (('STEP AP214'),
    '1' );
FILE_NAME ('coil.step',
    '2026-10-05T20:10:51',
    ( '' ),
    ( '' ),
    'SwSTEP 2.0',
    'SolidWorks 2020',
    '' );
FILE_SCHEMA (( 'AUTOMOTIVE_DESIGN' ));
ENDSEC;

DATA;
#2=( NAMED_UNIT ( * ) PLANE_ANGLE_UNIT ( ) SI_UNIT ( $, .RADIAN. ) );
#4=CARTESIAN_POINT ( 'NONE',  ( 5.963713532047742127, -0.4821895448718095945, 1.909345749545824367 ) ) ;
#5=CARTESIAN_POINT ( 'NONE',  ( 1.311946287462633309, 1.302956792059128066, -1.440285294924074311 ) ) ;
#6=CARTESIAN_POINT ( 'NONE',  ( 0.2454708137151571101, -1.954895187565863779, -0.4925657318226167591 ) ) ;
#8=CARTESIAN_POINT ( 'NONE',  ( 4.311269015108330827, -1.545260327404588852, -1.036625270625696205 ) ) ;
#15=CARTESIAN_POINT ( 'NONE',  ( 0.04676574305502099321, -1.756316032869180921, 1.310637071781264984 ) ) ;
#19=CARTESIAN_POINT ( 'NONE',  ( 1.260069262837599791, 0.7379878962356714034, 1.670071910705408946 ) ) ;
#22=CARTESIAN_POINT ( 'NONE',  ( 3.515997504735939305, -1.600726479906929844, 0.6675610986628178756 ) ) ;
#24=CARTESIAN_POINT ( 'NONE',  ( 6.609000000000019526, 4.695354556932705314, 2.562644781943986150 ) ) ;
#25=CARTESIAN_POINT ( 'NONE',  ( 0.1331565106231329398, 0.7299000548664087429, -2.029785554894456556 ) ) ;
#26=CARTESIAN_POINT ( 'NONE',  ( 6.445924739416000193, 0.6936395621829589686, -1.688995215704327313 ) ) ;
#27=CARTESIAN_POINT ( 'NONE',  ( 4.504711789546460565, 0.5192035298374733099, 1.891763301562799260 ) ) ;
#30=CARTESIAN_POINT ( 'NONE',  ( 4.389387035479824561, -0.001039498178659337352, -2.120667954306009406 ) ) ;
#34=CARTESIAN_POINT ( 'NONE',  ( 3.274343992483694787, -1.016290647400164282, -1.803532422793553636 ) ) ;
#38=CARTESIAN_POINT ( 'NONE',  ( 2.549810578889585067, -1.582449011024213981, 1.667500336659861748 ) ) ;
#46=CARTESIAN_POINT ( 'NONE',  ( 3.568532368641282648, 0.6928216322696268969, 1.782650395559831180 ) ) ;
#47=CARTESIAN_POINT ( 'NONE',  ( 4.928557879857294211, 1.651178231652555617, 0.4983569138605167814 ) ) ;
#48=CARTESIAN_POINT ( 'NONE',  ( 3.608611488583326032, 1.916353073142588403, 0.6279913346786819561 ) ) ;
#50=CARTESIAN_POINT ( 'NONE',  ( 5.063244923127927954, -1.278613472530117035, 1.910113253385301801 ) ) ;
#52=CARTESIAN_POINT ( 'NONE',  ( 0.8388348947251201837, 2.174866457552121268, 0.3736606161612308630 ) ) ;
#54=CARTESIAN_POINT ( 'NONE',  ( 6.362547694819080668, -1.249765848162401438, 1.253281529121505589 ) ) ;
#56=CARTESIAN_POINT ( 'NONE',  ( 1.851946410329910808, 2.285883199777267283, -0.1717553002464344836 ) ) ;
#57=CARTESIAN_POINT ( 'NONE',  ( 6.228435704027582176, 0.1854037366294820077, 1.831779187086844729 ) ) ;
#62=CARTESIAN_POINT ( 'NONE',  ( 0.3269468692386565678, -1.417551234153333395, 1.644607001386617418 ) ) ;
#63=CARTESIAN_POINT ( 'NONE',  ( 1.973842561262352469, -0.8578407463649927456, 1.825077436249371354 ) ) ;
#65=CARTESIAN_POINT ( 'NONE',  ( 5.479104952107777926, -0.04952074540257554031, -1.926025958231538882 ) ) ;
#67=CARTESIAN_POINT ( 'NONE',  ( 1.898975720090949837, -2.179683001098455808, -0.4277757613022105110 ) ) ;
#73=CARTESIAN_POINT ( 'NONE',  ( 5.706559709869656771, 1.539012945689299139, 0.8127616963746787659 ) ) ;
#74=CARTESIAN_POINT ( 'NONE',  ( 3.596105239937871456, 0.8843387906064968940, -1.751336483779348585 ) ) ;
#78=CARTESIAN_POINT ( 'NONE',  ( 4.763087504681410955, -2.017952330160921015, -1.023110994099560411 ) ) ;
#79=CARTESIAN_POINT ( 'NONE',  ( 1.135301032730736237, -0.04873925880971052838, -2.062252310772247910 ) ) ;
#82=CARTESIAN_POINT ( 'NONE',  ( 2.782378429719241986, -1.163933448739282062, 1.940043740367594305 ) ) ;
#85=CARTESIAN_POINT ( 'NONE',  ( 2.301827437220682171, -1.870247568056710774, 0.04138213060620592881 ) ) ;
#86=CARTESIAN_POINT ( 'NONE',  ( 1.441630353877725979, -1.487241779905050576, -0.8915045353455192112 ) ) ;
#87=CARTESIAN_POINT ( 'NONE',  ( 5.495707582769355781, -2.191739722525353429, -0.0009102486706394352645 ) ) ;
#88=CARTESIAN_POINT ( 'NONE',  ( 0.2533207856364183552, -1.770817270756098960, 1.316655756711228253 ) ) ;
#89=CARTESIAN_POINT ( 'NONE',  ( 1.534131747024346737, 1.016495879925772616, -1.792692027746685346 ) ) ;
#90=CARTESIAN_POINT ( 'NONE',  ( 4.013568362537369261, -0.9994162096361800529, -1.664904219174968114 ) ) ;
#93=CARTESIAN_POINT ( 'NONE',  ( 1.718750000000001554, -0.7852924748298989455, 1.895863743164124093 ) ) ;
#95=CARTESIAN_POINT ( 'NONE',  ( 0.2800716429562755683, -1.702078881456047688, 0.3292984779095942116 ) ) ;
#98=CARTESIAN_POINT ( 'NONE',  ( 4.483046177357690176, -2.016033783801042034, -0.04667830911464498911 ) ) ;
#102=CARTESIAN_POINT ( 'NONE',  ( 2.068725586703868746, -1.668841220716179130, -0.7407507213199536755 ) ) ;
#110=CARTESIAN_POINT ( 'NONE',  ( 0.01783989211246589379, -0.5346760324982450241, 1.947684760809722304 ) ) ;
#111=CARTESIAN_POINT ( 'NONE',  ( 6.551452540055466400, -1.985718062329771438, 0.9957849561875466993 ) ) ;
#115=MECHANICAL_DESIGN_GEOMETRIC_PRESENTATION_REPRESENTATION('',(#107520),#142122);
#116=CARTESIAN_POINT ( 'NONE',  ( 6.666874348205719336, -1.883165374045802087, -0.8376701409097894180 ) ) ;
#117=CARTESIAN_POINT ( 'NONE',  ( 4.869767617671093340, -0.2496050341583149201, -2.000857388266870984 ) ) ;
#126=CARTESIAN_POINT ( 'NONE',  ( 4.639999869408336863, 0.002810260262744306969, -2.016288307263448321 ) ) ;
#127=CARTESIAN_POINT ( 'NONE',  ( 4.294743845541324490, 1.480121740587354573, 1.094796260939827404 ) ) ;
#129=CARTESIAN_POINT ( 'NONE',  ( 3.317284684000018746, 2.086097511483188338, 0.9870085806921449212 ) ) ;
#131=CARTESIAN_POINT ( 'NONE',  ( 4.727887898869392203, -1.325758432718616042, -1.707240035374466114 ) ) ;
#133=CARTESIAN_POINT ( 'NONE',  ( 1.030689935155226555, -1.755017395645932066, 0.8318847510124205424 ) ) ;
#140=CARTESIAN_POINT ( 'NONE',  ( 3.783945140921864070, -0.9226758061156097313, 1.627204332209288395 ) ) ;
#141=CARTESIAN_POINT ( 'NONE',  ( 1.828231037913151447, -0.9045423626323212396, -1.684975973026317408 ) ) ;
#144=CARTESIAN_POINT ( 'NONE',  ( 3.018423772948013006, -1.088090592406821155, -1.919924466345590108 ) ) ;
#145=CARTESIAN_POINT ( 'NONE',  ( 6.883263157960402445, 0.001763689368145578400, 1.846037217754380011 ) ) ;
#150=CARTESIAN_POINT ( 'NONE',  ( 0.9484320465981105341, 0.5679970104440315026, 1.887783002132171539 ) ) ;
#151=CARTESIAN_POINT ( 'NONE',  ( 0.3414292828918061296, 0.3991051782518301727, 2.272663865251875581 ) ) ;
#152=CARTESIAN_POINT ( 'NONE',  ( 1.838261372102001800, -1.052240823716396267, 1.655630454418555830 ) ) ;
#153=CARTESIAN_POINT ( 'NONE',  ( 5.032111728107424575, 1.183179145130999643, 1.689302184701612086 ) ) ;
#160=CARTESIAN_POINT ( 'NONE',  ( 1.042111193480334430, 1.456518763772189695, 1.610191069602670000 ) ) ;
#162=CARTESIAN_POINT ( 'NONE',  ( 6.251489360189885325, 1.835807759842246423, -0.1425652098738516838 ) ) ;
#165=CARTESIAN_POINT ( 'NONE',  ( 1.915107840602244593, -0.2339084544023955492, 1.855816807740391150 ) ) ;
#166=CARTESIAN_POINT ( 'NONE',  ( 5.343121995983710626, -1.856993961526328007, 1.106124453333141577 ) ) ;
#168=CARTESIAN_POINT ( 'NONE',  ( -0.02244404828160087226, 0.2256878572204877031, -2.222431841814066278 ) ) ;
#171=CARTESIAN_POINT ( 'NONE',  ( 1.664566505720616929, 0.6010121217654046388, 1.815428919054395518 ) ) ;
#172=CARTESIAN_POINT ( 'NONE',  ( 2.623613022005319984, -1.017049183177589855, -1.448221827668960238 ) ) ;
#173=CARTESIAN_POINT ( 'NONE',  ( 0.2406774923011632261, 1.829974501424940891, 0.5550298453492612527 ) ) ;
#175=CARTESIAN_POINT ( 'NONE',  ( 4.991753579581297728, -1.905966813954384387, 0.1920618708746626713 ) ) ;
#176=CARTESIAN_POINT ( 'NONE',  ( 6.057084849134293236, 1.611049215779712940, -1.132701646639628246 ) ) ;
#178=CARTESIAN_POINT ( 'NONE',  ( 0.7035762090183244055, 1.867434778015097940, -1.004864118554361863 ) ) ;
#180=CARTESIAN_POINT ( 'NONE',  ( 3.959713429720784106, 1.856571849420919795, -0.2284545790810637578 ) ) ;
#181=CARTESIAN_POINT ( 'NONE',  ( 0.5569169099325711469, -1.540613122784354916, -0.9793164655157863274 ) ) ;
#183=CARTESIAN_POINT ( 'NONE',  ( 5.074942902252104204, -2.077123540546990110, -0.7459609299403434646 ) ) ;
#186=CARTESIAN_POINT ( 'NONE',  ( 2.189955769151647580, -1.345473201219016701, -1.563545076720110227 ) ) ;
#191=CARTESIAN_POINT ( 'NONE',  ( 6.521744167503259249, -0.4122283346772101509, 1.874327247564554266 ) ) ;
#193=CARTESIAN_POINT ( 'NONE',  ( 3.912603064140641074, 0.7423916865902054907, 1.932869565047180549 ) ) ;
#195=CARTESIAN_POINT ( 'NONE',  ( 2.003414267471514965, 1.795956895356983551, 1.202623776965026536 ) ) ;
#197=CARTESIAN_POINT ( 'NONE',  ( 1.647134723225437636, 0.2000593722277475561, 2.009751748981201569 ) ) ;
#203=CARTESIAN_POINT ( 'NONE',  ( -0.2234322562767385167, -0.4468160588090731022, -1.973564571300358228 ) ) ;
#204=CARTESIAN_POINT ( 'NONE',  ( 6.539320575229278454, 0.5749733277502915296, 2.156147827957733742 ) ) ;
#205=CARTESIAN_POINT ( 'NONE',  ( 4.704715985517350596, 1.906866092115505840, 1.080010033982371498 ) ) ;
#207=CARTESIAN_POINT ( 'NONE',  ( 3.287273477832891366, 0.04233216220104508987, -1.912079899511004433 ) ) ;
#211=CARTESIAN_POINT ( 'NONE',  ( 1.880482680076976720, -0.5405129038237622696, -1.942536604102131026 ) ) ;
#213=CARTESIAN_POINT ( 'NONE',  ( 0.5566822826340491748, -1.655162342056889502, 1.586242259447123493 ) ) ;
#215=CARTESIAN_POINT ( 'NONE',  ( 4.612129873793564094, -0.7390372460917455921, -1.558541145072767975 ) ) ;
#219=CARTESIAN_POINT ( 'NONE',  ( 0.8714495147512549833, -0.2914478312704605889, 1.939986204769503786 ) ) ;
#220=CARTESIAN_POINT ( 'NONE',  ( 0.3033014811697418711, -0.5033704626738467747, 1.801585485020948729 ) ) ;
#222=CARTESIAN_POINT ( 'NONE',  ( 0.1751657365761703222, 4.087554309226840488, -2.598743260590470783 ) ) ;
#226=CARTESIAN_POINT ( 'NONE',  ( 5.039644362999008642, -1.718302384056184851, 0.5736564087924463928 ) ) ;
#230=CARTESIAN_POINT ( 'NONE',  ( 5.514259914679787045, -1.811656974672648746, 0.006318095929410197376 ) ) ;
#235=CARTESIAN_POINT ( 'NONE',  ( 6.215283151739675382, -1.596727646711604942, -0.9557930639402379969 ) ) ;
#237=CARTESIAN_POINT ( 'NONE',  ( 3.480013654308728555, -1.913576260228011749, -0.09060460826773930609 ) ) ;
#245=CARTESIAN_POINT ( 'NONE',  ( 6.016841150788749815, 0.2099786098018930069, 2.106937748889408546 ) ) ;
#246=CARTESIAN_POINT ( 'NONE',  ( 0.3917762336288696523, 1.602822130585265015, 1.450656209987542855 ) ) ;
#249=CARTESIAN_POINT ( 'NONE',  ( 1.307329191252764922, -0.4475898743878243824, 1.769731943805815222 ) ) ;
#251=CARTESIAN_POINT ( 'NONE',  ( 3.680510133705969800, -1.759192178946006990, -0.4875382671739314500 ) ) ;
#253=CARTESIAN_POINT ( 'NONE',  ( 2.742330423940505302, 1.058908597569432120, -1.592262909973440888 ) ) ;
#255=CARTESIAN_POINT ( 'NONE',  ( 2.418351439525995961, 0.8393807748916733980, 1.781860320225916228 ) ) ;
#256=CARTESIAN_POINT ( 'NONE',  ( 5.108904621496645149, -0.2812511558281989288, 1.921465535368711786 ) ) ;
#259=CARTESIAN_POINT ( 'NONE',  ( 4.974906307097914926, -1.534222593358970821, 1.464151343314526121 ) ) ;
#262=CARTESIAN_POINT ( 'NONE',  ( 2.508343198132975349, -1.907285675847451234, -0.1387974571645037292 ) ) ;
#268=CARTESIAN_POINT ( 'NONE',  ( 4.600122369450095228, -1.825375079466069694, -0.04201004182294298950 ) ) ;
#269=CARTESIAN_POINT ( 'NONE',  ( 0.9243811426856913815, 1.018911950503737174, 1.802186752163869699 ) ) ;
#273=CARTESIAN_POINT ( 'NONE',  ( 5.172658500931742509, -1.761684834526537680, -0.6294727512598657926 ) ) ;
#283=CARTESIAN_POINT ( 'NONE',  ( 6.649308703871936288, 1.893188687436907047, -1.062577851937399620 ) ) ;
#285=CARTESIAN_POINT ( 'NONE',  ( 2.882529129721671080, -0.6171794022716176054, -2.025259201532733755 ) ) ;
#288=CARTESIAN_POINT ( 'NONE',  ( 5.981320602565292965, -0.05662044862421274777, 2.069665677200482445 ) ) ;
#293=CARTESIAN_POINT ( 'NONE',  ( 2.959215247630428536, 0.3357152255929369278, -2.267430770885081603 ) ) ;
#296=CARTESIAN_POINT ( 'NONE',  ( 2.548957913124219044, 0.2380835140640499836, 1.897471792728817386 ) ) ;
#298=CARTESIAN_POINT ( 'NONE',  ( 0.7033859027741823366, 1.773467923640878796, -0.9528479892364212223 ) ) ;
#299=CARTESIAN_POINT ( 'NONE',  ( 0.8835585337332927391, -1.864609544942645414, 0.6100022000963196689 ) ) ;
#303=CARTESIAN_POINT ( 'NONE',  ( 3.451197694293614671, 0.5077425806990677470, -2.027912974856157291 ) ) ;
#304=CARTESIAN_POINT ( 'NONE',  ( 2.500565701108145689, 1.422975883020457077, -1.052153950563482265 ) ) ;
#305=CARTESIAN_POINT ( 'NONE',  ( 6.827182134110199030, 7.629137130509070275, 2.410944104600701188 ) ) ;
#307=CARTESIAN_POINT ( 'NONE',  ( 5.789115795541526666, 1.732349586671273922, 1.501262892615047750 ) ) ;
#308=CARTESIAN_POINT ( 'NONE',  ( 3.943067085940495264, 0.5840054040482050013, -1.639550319303827219 ) ) ;
#311=CARTESIAN_POINT ( 'NONE',  ( 2.934579196337202323, 0.9245653808827180020, 1.466514439666162684 ) ) ;
#312=CARTESIAN_POINT ( 'NONE',  ( 1.559489335033688251, -1.894147805384650995, -1.132260830144316888 ) ) ;
#313=CARTESIAN_POINT ( 'NONE',  ( 5.248546085168739772, -2.154154806625402596, -0.2710006578958406576 ) ) ;
#315=CARTESIAN_POINT ( 'NONE',  ( 5.682827415814322158, 1.645762192317705486, -1.164983060713747909 ) ) ;
#316=CARTESIAN_POINT ( 'NONE',  ( 0.06249170576382599707, -1.450827213159947338, -1.451031289061120777 ) ) ;
#319=CARTESIAN_POINT ( 'NONE',  ( 2.221590912301483645, -1.869112302256823011, 0.4658275329730912628 ) ) ;
#321=CARTESIAN_POINT ( 'NONE',  ( 5.449557989901563815, -2.008192194917140849, 0.9499826718327757380 ) ) ;
#323=CARTESIAN_POINT ( 'NONE',  ( 6.883263157960367806, 0.5819222519044697783, 1.998722019247618276 ) ) ;
#327=CARTESIAN_POINT ( 'NONE',  ( 1.559560479473407701, -1.874198601735496794, 1.192037787016706485 ) ) ;
#328=CARTESIAN_POINT ( 'NONE',  ( 6.373494408814909917, -0.2414686440028299685, 1.946897059556201848 ) ) ;
#332=CARTESIAN_POINT ( 'NONE',  ( 4.211423687607918076, -1.713229066603161099, -1.148409633951211761 ) ) ;
#336=CARTESIAN_POINT ( 'NONE',  ( 6.151601556293980977, 0.5431611868166182910, -1.789914130245950696 ) ) ;
#337=CARTESIAN_POINT ( 'NONE',  ( 4.623498406067056088, 0.3027793956022621913, 1.707322668435699242 ) ) ;
#338=CARTESIAN_POINT ( 'NONE',  ( 4.071615416877820692, -0.9979366678331093032, 1.425717084491331832 ) ) ;
#340=CARTESIAN_POINT ( 'NONE',  ( 1.453083402393087642, -1.969018001514400540, -1.173635730923931808 ) ) ;
#342=CARTESIAN_POINT ( 'NONE',  ( 6.198786912940476235, 1.738631647849303130, 1.160874564816395615 ) ) ;
#343=CARTESIAN_POINT ( 'NONE',  ( 0.6382991350510487383, -1.580419255802448575, 0.9442637585924051891 ) ) ;
#346=CARTESIAN_POINT ( 'NONE',  ( 1.143204175302305670, 0.8197749522141674072, 1.842446510343001442 ) ) ;
#347=CARTESIAN_POINT ( 'NONE',  ( 0.4280004979528989617, 1.123059939108238314, -1.881669248891951085 ) ) ;
#352=CARTESIAN_POINT ( 'NONE',  ( 3.018346832952636394, -2.117961878424143407, 0.1061830045200745365 ) ) ;
#354=CARTESIAN_POINT ( 'NONE',  ( 5.707590141996651489, -0.4392596013848491521, 1.771934311310577659 ) ) ;
#361=CARTESIAN_POINT ( 'NONE',  ( 3.674085990935217261, 2.004049791156937044, -0.2512726544132165563 ) ) ;
#362=CARTESIAN_POINT ( 'NONE',  ( 6.458075443588827014, 2.201329523236052577, -0.1558686762383256763 ) ) ;
#365=CARTESIAN_POINT ( 'NONE',  ( 4.698021595848828724, 0.7982989760673472324, -1.681190670221676120 ) ) ;
#370=CARTESIAN_POINT ( 'NONE',  ( 0.3917762336288696523, 1.602822130585265015, 1.450656209987542855 ) ) ;
#374=CARTESIAN_POINT ( 'NONE',  ( 1.352469423652577607, -0.7852941029048329247, 1.545897522503926647 ) ) ;
#375=CARTESIAN_POINT ( 'NONE',  ( 0.9545595967530025039, 0.3431710391763979073, -1.705965249089304470 ) ) ;
#376=CARTESIAN_POINT ( 'NONE',  ( 0.2711454947614586608, -1.503558885491006247, 1.750568091222578282 ) ) ;
#379=CARTESIAN_POINT ( 'NONE',  ( 2.091158219120598183, 1.794587730539594972, -1.012862355382545765 ) ) ;
#382=CARTESIAN_POINT ( 'NONE',  ( 1.563827143785265328, 1.649830188709809686, -1.158509706484150970 ) ) ;
#386=CARTESIAN_POINT ( 'NONE',  ( 6.420764531294745225, 1.746252128813120086, 0.6712297951826234899 ) ) ;
#387=CARTESIAN_POINT ( 'NONE',  ( 5.220932206144772714, 1.444093599275039885, -1.253800916539760113 ) ) ;
#389=CARTESIAN_POINT ( 'NONE',  ( 6.656857027519620829, -1.708965229049699053, 1.396003577074665714 ) ) ;
#394=CARTESIAN_POINT ( 'NONE',  ( -0.09308815784560355022, -0.4424663830696302091, -1.977475021732390204 ) ) ;
#396=CARTESIAN_POINT ( 'NONE',  ( 4.085262347903253044, -0.2225469472450763153, -2.296823545465367822 ) ) ;
#397=CARTESIAN_POINT ( 'NONE',  ( 5.090269282739749102, 1.010147525469132557, -1.681691772506640481 ) ) ;
#398=CARTESIAN_POINT ( 'NONE',  ( 1.744895479173363517, -0.2825750800353257208, -1.941159045430330465 ) ) ;
#402=CARTESIAN_POINT ( 'NONE',  ( -0.01227199510028028316, -0.5578357038005901103, 2.042509832261687475 ) ) ;
#404=CARTESIAN_POINT ( 'NONE',  ( 0.6382991350510487383, -1.580419255802448575, 0.9442637585924050780 ) ) ;
#405=CARTESIAN_POINT ( 'NONE',  ( 4.399414683135016269, -1.891862197681973834, 1.064912953861403944 ) ) ;
#406=CARTESIAN_POINT ( 'NONE',  ( 3.063685658700274761, 1.282989771343697294, 1.555699169480361022 ) ) ;
#408=CARTESIAN_POINT ( 'NONE',  ( 1.494549364340029163, -1.129948290531690658, 1.794289463044356436 ) ) ;
#413=CARTESIAN_POINT ( 'NONE',  ( 2.407559617977403477, -0.4546984313768054342, 2.009812782922258734 ) ) ;
#418=CARTESIAN_POINT ( 'NONE',  ( 0.07755575628183572490, 2.860544851022389867, -2.677061994759164065 ) ) ;
#420=CARTESIAN_POINT ( 'NONE',  ( 4.406835678522929456, -0.4222698756407486931, -1.864907683101609370 ) ) ;
#422=CARTESIAN_POINT ( 'NONE',  ( 1.669569175971203023, 0.1671416771932125456, -2.256311322606067371 ) ) ;
#424=CARTESIAN_POINT ( 'NONE',  ( 1.898416112216103624, -1.777124406008349533, -0.3506645682890742743 ) ) ;
#426=CARTESIAN_POINT ( 'NONE',  ( 2.378032431427847371, -1.910899176573145342, -0.1362895805000780836 ) ) ;
#427=CARTESIAN_POINT ( 'NONE',  ( 3.156751980976373329, -0.5984545454679365273, -1.982000093670479135 ) ) ;
#430=CARTESIAN_POINT ( 'NONE',  ( 0.3386658216258168763, 0.3346604457750371187, 1.942702894000091662 ) ) ;
#431=CARTESIAN_POINT ( 'NONE',  ( 5.936148346467474468, 0.9475192508551170123, -1.677314091114836980 ) ) ;
#432=CARTESIAN_POINT ( 'NONE',  ( 0.6984242042700332664, -0.8252692633385866339, 2.155259511649917137 ) ) ;
#435=CARTESIAN_POINT ( 'NONE',  ( 5.810998785189021909, -1.628375694745004321, 1.266036720739783128 ) ) ;
#440=CARTESIAN_POINT ( 'NONE',  ( 5.139724016738759005, -1.487180916556319454, -1.491360876250556800 ) ) ;
#444=CARTESIAN_POINT ( 'NONE',  ( 5.044278900083454253, 2.155409826167026477, 0.1645634770654491874 ) ) ;
#445=CARTESIAN_POINT ( 'NONE',  ( 4.916668454303085412, -0.6825918349771132876, -1.900952964002266210 ) ) ;
#452=CARTESIAN_POINT ( 'NONE',  ( 3.274625289317079524, -0.3981104328964027994, -1.976669913042613747 ) ) ;
#457=CARTESIAN_POINT ( 'NONE',  ( 4.979442225389012933, 2.018306902694905425, -0.7746836383674888804 ) ) ;
#459=PRESENTATION_STYLE_ASSIGNMENT (( #53513 ) ) ;
#462=CARTESIAN_POINT ( 'NONE',  ( 5.360953910674266965, -0.05231296482399727665, -2.015913715532565043 ) ) ;
#464=CARTESIAN_POINT ( 'NONE',  ( 0.3633288501447570207, 1.706897997983588322, -0.2475752363529682698 ) ) ;
#469=CARTESIAN_POINT ( 'NONE',  ( 0.1921619543209041325, -0.3744425218715953796, -1.735604558297418443 ) ) ;
#471=CARTESIAN_POINT ( 'NONE',  ( 1.313140557769366890, 1.644527964066449632, -1.160800818697106163 ) ) ;
#477=CARTESIAN_POINT ( 'NONE',  ( 2.315225504062240702, 1.701464259299827919, -1.265282535349021575 ) ) ;
#478=CARTESIAN_POINT ( 'NONE',  ( 2.073842424929934314, -0.8596134062341630466, 1.824128527830502833 ) ) ;
#479=CARTESIAN_POINT ( 'NONE',  ( 2.724650786558381999, 1.309284593816659736, -1.252271045645783065 ) ) ;
#481=CARTESIAN_POINT ( 'NONE',  ( 6.754756207809571755, -1.674487575904315406, 1.366813541845832924 ) ) ;
#485=CARTESIAN_POINT ( 'NONE',  ( 0.6025738811294746311, 1.771267034891465642, 0.7302799438476501592 ) ) ;
#492=CARTESIAN_POINT ( 'NONE',  ( 4.100566281481184738, -0.6756360485904688851, -2.053482476349233643 ) ) ;
#495=CARTESIAN_POINT ( 'NONE',  ( 1.617596980227502756, 1.765956010477184535, 1.173731981927571555 ) ) ;
#496=CARTESIAN_POINT ( 'NONE',  ( 6.422862827026682098, 1.704596635199370880, 0.6539724957527744964 ) ) ;
#497=CARTESIAN_POINT ( 'NONE',  ( 3.339098322719173062, -1.740117145613935268, 0.9263661929081908886 ) ) ;
#498=CARTESIAN_POINT ( 'NONE',  ( 5.642805672956042962, 1.844803604357934779, 0.5037821151940986564 ) ) ;
#501=CARTESIAN_POINT ( 'NONE',  ( 6.215292997425397203, -1.688482396400727170, -1.013753615619580106 ) ) ;
#502=CARTESIAN_POINT ( 'NONE',  ( 1.201004818612857017, -0.4721336787944198643, 1.883569333377318245 ) ) ;
#506=CARTESIAN_POINT ( 'NONE',  ( 2.449268230884271702, 0.5568478702235891697, -2.015041263885499756 ) ) ;
#511=CARTESIAN_POINT ( 'NONE',  ( 6.305323439471717251, 1.661359358424657318, -0.9468341723649562613 ) ) ;
#513=CARTESIAN_POINT ( 'NONE',  ( 4.459734715955371520, 0.4851516707722826061, -2.152740496749529608 ) ) ;
#514=CARTESIAN_POINT ( 'NONE',  ( 1.431021430919703574, 2.126993092707793132, 0.5877070120439558121 ) ) ;
#515=CARTESIAN_POINT ( 'NONE',  ( 0.9614044138335111622, -1.507904615609249488, -1.175938229252027956 ) ) ;
#518=CARTESIAN_POINT ( 'NONE',  ( 4.703616579153604427, -1.598285800263723688, -1.315984976451072708 ) ) ;
#521=CARTESIAN_POINT ( 'NONE',  ( 2.254944280175336324, -1.671361177491991201, 1.370965666894090385 ) ) ;
#522=CARTESIAN_POINT ( 'NONE',  ( 3.966501855323391723, -2.045284974426237579, -0.7877190255709336508 ) ) ;
#528=CARTESIAN_POINT ( 'NONE',  ( 5.994686951402704800, -1.719894441074249158, 0.2214109503040090354 ) ) ;
#531=CARTESIAN_POINT ( 'NONE',  ( 3.731357587288412159, 0.05568397596692271218, -2.069689236595618542 ) ) ;
#532=CARTESIAN_POINT ( 'NONE',  ( 5.343409318383084639, 0.4121200312635669993, -2.076573192147526115 ) ) ;
#535=CARTESIAN_POINT ( 'NONE',  ( 2.852355409199380798, -1.963852837454314271, -0.1495663577412101042 ) ) ;
#536=CARTESIAN_POINT ( 'NONE',  ( 5.455124386806871506, 0.4517125544712205509, -2.247162937307800590 ) ) ;
#537=CARTESIAN_POINT ( 'NONE',  ( 2.490611698265518648, -0.3118145247060916114, -1.798701865878708839 ) ) ;
#544=CARTESIAN_POINT ( 'NONE',  ( 4.183843882646627321, 1.951733592454238497, -0.4931575689418183917 ) ) ;
#545=CARTESIAN_POINT ( 'NONE',  ( 4.223457129239616137, 0.2443821477370981265, -1.946437379933690481 ) ) ;
#548=CARTESIAN_POINT ( 'NONE',  ( 0.1755611466353786954, 2.859968053823423784, -2.732108412375580109 ) ) ;
#549=CARTESIAN_POINT ( 'NONE',  ( 0.3278234441896179518, 1.071198113070050972, -1.795324408978350439 ) ) ;
#550=CARTESIAN_POINT ( 'NONE',  ( 5.858207189965921380, 0.7206212418228461480, 1.616676333947133504 ) ) ;
#552=CARTESIAN_POINT ( 'NONE',  ( 2.343918204863020271, 2.190988169473460090, 0.05230688499441307066 ) ) ;
#553=CARTESIAN_POINT ( 'NONE',  ( 0.6259951400321401849, 0.1256764613348868298, 1.735981902797034238 ) ) ;
#556=CARTESIAN_POINT ( 'NONE',  ( 0.2335667940003048615, 2.868049447791064743, -2.641685461849890171 ) ) ;
#557=CARTESIAN_POINT ( 'NONE',  ( 0.7676545703292583234, 0.8460830606174443158, 1.503042688352700829 ) ) ;
#558=CARTESIAN_POINT ( 'NONE',  ( 0.6151802255017734256, 0.7180209600621060284, -2.183386540618210692 ) ) ;
#559=CARTESIAN_POINT ( 'NONE',  ( 0.06437606466144081552, -1.426665095847098330, 1.663708609037084951 ) ) ;
#560=CARTESIAN_POINT ( 'NONE',  ( 3.053566222061272040, -1.804402116661915967, -1.270350324234905903 ) ) ;
#561=CARTESIAN_POINT ( 'NONE',  ( 1.112457285868488910, 2.168641027238225938, -0.1045176843600063021 ) ) ;
#562=CARTESIAN_POINT ( 'NONE',  ( 0.3986991128735201673, 1.519733473351183362, -1.011397189243423700 ) ) ;
#563=CARTESIAN_POINT ( 'NONE',  ( 2.694651208505644213, 1.530237149716510370, -1.463602791221560118 ) ) ;
#564=CARTESIAN_POINT ( 'NONE',  ( 6.727182134110196721, 6.033756510516266935, 2.783943001041962795 ) ) ;
#565=CARTESIAN_POINT ( 'NONE',  ( 5.913098435216375570, 1.699041482274340265, 0.9079036414736068039 ) ) ;
#567=CARTESIAN_POINT ( 'NONE',  ( 2.824086921994493071, 1.271197760638997254, -1.907441589200240983 ) ) ;
#572=CARTESIAN_POINT ( 'NONE',  ( 4.987093027905733500, -2.091254775410257061, -0.7492775906185499268 ) ) ;
#580=CARTESIAN_POINT ( 'NONE',  ( 2.672500184003968382, 1.427937546361924381, 1.423961308954827754 ) ) ;
#582=CARTESIAN_POINT ( 'NONE',  ( 1.358340336993546726, -2.062741126468564890, -0.004002619933256982773 ) ) ;
#587=CARTESIAN_POINT ( 'NONE',  ( 3.925867417771063739, 1.172880473742785812, -1.850976771919823793 ) ) ;
#588=CARTESIAN_POINT ( 'NONE',  ( 1.020157974382044364, -1.821741137083273010, 0.8647263380179845971 ) ) ;
#589=CARTESIAN_POINT ( 'NONE',  ( 0.7844012160764175512, 1.623964078452419857, -0.8677550623670119423 ) ) ;
#590=CARTESIAN_POINT ( 'NONE',  ( 4.417794048288587128, 1.130693009273657124, -1.452954439256304520 ) ) ;
#593=CARTESIAN_POINT ( 'NONE',  ( 5.508770632382115728, 1.381118045931900573, -1.193960910464037850 ) ) ;
#594=CARTESIAN_POINT ( 'NONE',  ( 5.906875006520014182, -1.122496024291631755, -1.674889250513518446 ) ) ;
#596=CARTESIAN_POINT ( 'NONE',  ( 4.153392199625399073, -1.879142691831453105, -1.259808711832038464 ) ) ;
#598=CARTESIAN_POINT ( 'NONE',  ( 6.739294440770141392, -1.883009798889522024, 0.9431707147840006078 ) ) ;
#600=CARTESIAN_POINT ( 'NONE',  ( 5.090316257491098284, 1.067296284200716983, -1.773933887923849984 ) ) ;
#605=CARTESIAN_POINT ( 'NONE',  ( 3.703666587441448943, -0.5581696590808477021, 1.843871709287647764 ) ) ;
#609=CARTESIAN_POINT ( 'NONE',  ( 0.8969213510382867405, -2.070190491330957006, -0.4589741369691033857 ) ) ;
#610=CARTESIAN_POINT ( 'NONE',  ( 1.231071286002645815, 1.486838745870424860, -1.650645422243676164 ) ) ;
#611=CARTESIAN_POINT ( 'NONE',  ( 3.399542317941701253, 1.658995184361473196, 1.297097526815289115 ) ) ;
#614=CARTESIAN_POINT ( 'NONE',  ( 2.822649888979886335, -1.354935067541668259, 1.419045635080482093 ) ) ;
#621=CARTESIAN_POINT ( 'NONE',  ( 2.215225606797793567, 1.700350911433265555, -1.266953333846132512 ) ) ;
#623=CARTESIAN_POINT ( 'NONE',  ( 3.894932841003693191, 0.2855096342280309396, 1.940843471192068570 ) ) ;
#624=CARTESIAN_POINT ( 'NONE',  ( 2.993221558690632556, 1.854768100113469265, -1.110066390340218367 ) ) ;
#625=CARTESIAN_POINT ( 'NONE',  ( 3.034521004542716227, -1.622529355458858236, 0.8704296449140033198 ) ) ;
#631=CARTESIAN_POINT ( 'NONE',  ( 5.050617384047394687, -1.472844127453584839, -0.9267575401476387809 ) ) ;
#635=CARTESIAN_POINT ( 'NONE',  ( 2.377987466095924152, 1.329388817951412394, 1.704534938537699995 ) ) ;
#636=CARTESIAN_POINT ( 'NONE',  ( 4.042342166264912606, 1.899327733865597168, -0.6766104081444989093 ) ) ;
#638=CARTESIAN_POINT ( 'NONE',  ( 0.9717996764858798375, 2.083101276202529384, -0.5774176476955604764 ) ) ;
#639=CARTESIAN_POINT ( 'NONE',  ( 3.098462860235187133, -0.5706901479570201108, -1.887068881103808327 ) ) ;
#640=CARTESIAN_POINT ( 'NONE',  ( 2.354701247847644119, -1.526412939949482128, 1.247560610424301109 ) ) ;
#642=CARTESIAN_POINT ( 'NONE',  ( 3.843253449720198667, 0.6512379428032251116, -1.829756300597375596 ) ) ;
#651=CARTESIAN_POINT ( 'NONE',  ( 0.9915960798324228165, 1.945464911009102460, -1.041603813667857370 ) ) ;
#653=CARTESIAN_POINT ( 'NONE',  ( 4.961744919065853132, -0.5270168765720646409, 1.889542207339139024 ) ) ;
#656=CARTESIAN_POINT ( 'NONE',  ( 3.151669946411875589, 2.064753251683769442, -0.4682690128248386818 ) ) ;
#658=CARTESIAN_POINT ( 'NONE',  ( 0.07479286986305544449, 2.046156589154801253, -2.272744413733415403 ) ) ;
#660=CARTESIAN_POINT ( 'NONE',  ( 4.118977087773854961, -1.761250088754966692, 0.5364436722887636622 ) ) ;
#665=CARTESIAN_POINT ( 'NONE',  ( 5.519825572852568030, -0.5132647233585425628, 2.057443900658859182 ) ) ;
#669=CARTESIAN_POINT ( 'NONE',  ( 5.554002131806472065, 2.058623415865985518, -0.09669752385456369115 ) ) ;
#672=CARTESIAN_POINT ( 'NONE',  ( 1.275590745840638363, -1.816738662498600165, 0.4029602180237248366 ) ) ;
#673=CARTESIAN_POINT ( 'NONE',  ( 2.876309626556411203, -0.1380247437976732383, -1.836149222064882514 ) ) ;
#678=CARTESIAN_POINT ( 'NONE',  ( 2.051678093609669240, -1.773579625386853875, -1.313098587465796774 ) ) ;
#679=CARTESIAN_POINT ( 'NONE',  ( 5.448581927027607463, 0.6492139302081233465, 2.167288725150788409 ) ) ;
#681=CARTESIAN_POINT ( 'NONE',  ( 5.220911918456066836, 1.366450397884883428, -1.189473885788590035 ) ) ;
#682=CARTESIAN_POINT ( 'NONE',  ( 5.612480213242726279, 1.848112342440700440, 0.5042863886801035589 ) ) ;
#684=CARTESIAN_POINT ( 'NONE',  ( 5.172658500931742509, -1.761684834526537680, -0.6294727512598657926 ) ) ;
#685=CARTESIAN_POINT ( 'NONE',  ( 4.527703488433511225, 1.805393378231552326, -0.4512502670087223944 ) ) ;
#688=CARTESIAN_POINT ( 'NONE',  ( 6.561408083364261401, 0.2975169865880605835, -1.744492507556465011 ) ) ;
#689=CARTESIAN_POINT ( 'NONE',  ( -0.1706859984542466180, -1.561801110730935971, -1.275320528755889526 ) ) ;
#691=CARTESIAN_POINT ( 'NONE',  ( 2.649164382713434573, -1.750592827090621917, 1.170555837024005008 ) ) ;
#697=CARTESIAN_POINT ( 'NONE',  ( 1.722921806169195547, 1.493705621373665915, -1.359711205623759023 ) ) ;
#699=CARTESIAN_POINT ( 'NONE',  ( 6.620655732516645742, 3.706282450693794139, 2.340867613974298767 ) ) ;
#703=CARTESIAN_POINT ( 'NONE',  ( 1.827627302340195437, -2.036028831988645926, 0.7264203155534704193 ) ) ;
#704=CARTESIAN_POINT ( 'NONE',  ( 6.889999999999967706, 3.707772630975701311, 2.234475054783117809 ) ) ;
#711=CARTESIAN_POINT ( 'NONE',  ( 1.083813775577105565, -0.9808430935620198188, 1.959877696171570927 ) ) ;
#713=CARTESIAN_POINT ( 'NONE',  ( 1.042281785820580176, 0.9147803334835495903, -2.069518175336809929 ) ) ;
#721=CARTESIAN_POINT ( 'NONE',  ( 2.811481186154769496, -1.751065702721636308, 0.2553572387639922447 ) ) ;
#722=CARTESIAN_POINT ( 'NONE',  ( 5.965903178300210108, 2.175115270774199416, -0.3715683035191638117 ) ) ;
#726=CARTESIAN_POINT ( 'NONE',  ( 5.114861317887108072, 0.1511565883688982259, 2.010826320608386730 ) ) ;
#728=CARTESIAN_POINT ( 'NONE',  ( 2.219420098953532428, -1.815089452277141691, 0.4520615115926190919 ) ) ;
#729=CARTESIAN_POINT ( 'NONE',  ( 3.854399998794607374, -2.067664388167046674, -0.1065051105964970740 ) ) ;
#731=CARTESIAN_POINT ( 'NONE',  ( 2.109489925670060551, 1.480643174185194200, 1.210387159491378650 ) ) ;
#736=CARTESIAN_POINT ( 'NONE',  ( 0.7559434568639654684, 0.7726834774516875282, -1.749509110286852742 ) ) ;
#738=CARTESIAN_POINT ( 'NONE',  ( 2.752341281506097470, -1.956419249932477955, -0.1471676765215298721 ) ) ;
#741=CARTESIAN_POINT ( 'NONE',  ( 5.185831674374465905, 2.043064739972153543, -0.5678235988075125418 ) ) ;
#744=CARTESIAN_POINT ( 'NONE',  ( 6.292255012522757873, -1.961630990407544406, -0.1958228842163112771 ) ) ;
#746=CARTESIAN_POINT ( 'NONE',  ( 1.775641216270260170, 0.3400756789797795832, -1.984116031292797677 ) ) ;
#748=CARTESIAN_POINT ( 'NONE',  ( 0.7204975843347528608, 2.086673352822054461, 0.3575386888887230885 ) ) ;
#750=CARTESIAN_POINT ( 'NONE',  ( 2.225130849662222410, -1.891980959128433781, -0.8411517639917851508 ) ) ;
#753=ORIENTED_EDGE ( 'NONE', *, *, #46793, .F. ) ;
#754=CARTESIAN_POINT ( 'NONE',  ( 6.298786922650962516, 1.737427944715240091, 1.162477542130130548 ) ) ;
#756=CARTESIAN_POINT ( 'NONE',  ( 3.873894609034499670, 1.013791609252197690, 1.518000939925366000 ) ) ;
#757=CARTESIAN_POINT ( 'NONE',  ( 2.789504176380937395, 1.719411750852325449, -0.5702826837221984801 ) ) ;
#761=CARTESIAN_POINT ( 'NONE',  ( 5.438574045396407541, 2.173287242562565780, 0.3821286992964008089 ) ) ;
#764=CARTESIAN_POINT ( 'NONE',  ( 3.615784255950851289, -0.5524401208748200842, 1.830756043982272097 ) ) ;
#772=CARTESIAN_POINT ( 'NONE',  ( -0.1121326479804653220, -0.4008509640632436088, -1.803546454093779561 ) ) ;
#775=CARTESIAN_POINT ( 'NONE',  ( 4.885944009213345929, -0.8832235454491498272, 1.648918812636574804 ) ) ;
#780=CARTESIAN_POINT ( 'NONE',  ( 1.252720943002823883, -0.4733663544725670302, -1.911600023467324716 ) ) ;
#781=CARTESIAN_POINT ( 'NONE',  ( 2.530875249677287719, -1.674875632724934338, 1.122518345125958383 ) ) ;
#785=CARTESIAN_POINT ( 'NONE',  ( 2.273600812266802773, 1.349468827467028120, 1.726581335083368085 ) ) ;
#786=CARTESIAN_POINT ( 'NONE',  ( 6.024025069106937913, -1.018266858664597763, -1.515143308444939274 ) ) ;
#795=CARTESIAN_POINT ( 'NONE',  ( 4.036529152626888717, -1.599951230533543267, 0.9111318136766360931 ) ) ;
#796=CARTESIAN_POINT ( 'NONE',  ( 0.9264321329857813092, -0.9072109017984790746, -1.797169606962043309 ) ) ;
#797=CARTESIAN_POINT ( 'NONE',  ( 2.724286267170890952, -1.998689782195923081, -1.134749220811093418 ) ) ;
#799=CARTESIAN_POINT ( 'NONE',  ( 0.7603355536747276044, -0.6198598984368717257, -1.754846704163029125 ) ) ;
#803=CARTESIAN_POINT ( 'NONE',  ( 4.218947473185084007, 1.474887410857337100, -1.217315437338606365 ) ) ;
#806=CARTESIAN_POINT ( 'NONE',  ( 4.159774813393120496, 0.9870934738810345221, 1.843074783240926884 ) ) ;
#807=CARTESIAN_POINT ( 'NONE',  ( 2.553401164250346245, 0.5009360343536627402, -1.802255699741683870 ) ) ;
#810=CARTESIAN_POINT ( 'NONE',  ( 5.601068772352080671, -0.4412860211496574814, 1.787476196608045464 ) ) ;
#814=CARTESIAN_POINT ( 'NONE',  ( 5.127475435434773132, -1.636205250265274191, 0.5461684234016728201 ) ) ;
#816=CARTESIAN_POINT ( 'NONE',  ( 0.2637851986186890429, 1.619078963417280859, -0.6216347861247341067 ) ) ;
#817=CARTESIAN_POINT ( 'NONE',  ( 6.340462157465731607, 2.182225300935904055, 0.3281612982340698093 ) ) ;
#820=CARTESIAN_POINT ( 'NONE',  ( 4.979425714853139340, -0.1133551455631234828, 2.168255935233906584 ) ) ;
#821=CARTESIAN_POINT ( 'NONE',  ( 3.387140609607977026, 1.650079954178599539, -0.7815607168924765258 ) ) ;
#822=CARTESIAN_POINT ( 'NONE',  ( 0.9538670997781794059, -0.7113550649951918547, 1.828410001767373450 ) ) ;
#823=CARTESIAN_POINT ( 'NONE',  ( 5.278551870535488355, -0.5171574069430958653, -2.053072726559619365 ) ) ;
#826=CARTESIAN_POINT ( 'NONE',  ( 5.566080547264319556, -1.456586111465259403, 1.770153815000871989 ) ) ;
#829=CARTESIAN_POINT ( 'NONE',  ( 1.576976220782677185, -1.497206391897941913, 1.501870991332490135 ) ) ;
#837=CARTESIAN_POINT ( 'NONE',  ( 6.561400879130542485, 1.800260439488234443, 1.213256210689506176 ) ) ;
#838=CARTESIAN_POINT ( 'NONE',  ( 6.983263157960362122, 6.035089925019382129, 2.648702789725385198 ) ) ;
#841=CARTESIAN_POINT ( 'NONE',  ( 2.051734446849303506, -1.982521776546506853, 1.002060208660388474 ) ) ;
#843=CARTESIAN_POINT ( 'NONE',  ( 6.135388727473008785, 0.6351960432287793168, 1.913804721665197883 ) ) ;
#845=CARTESIAN_POINT ( 'NONE',  ( 4.012594160722949610, 0.7376926799337081286, 1.926325278971857236 ) ) ;
#851=CARTESIAN_POINT ( 'NONE',  ( 0.7793769126323678575, 1.405529721366456597, 1.547827308177295746 ) ) ;
#852=CARTESIAN_POINT ( 'NONE',  ( 4.219375079941334761, 1.978050461189932552, 0.3905991720301109082 ) ) ;
#853=CARTESIAN_POINT ( 'NONE',  ( 4.528748383445759806, -1.681502307688139908, 0.7506017836093890061 ) ) ;
#855=ORIENTED_EDGE ( 'NONE', *, *, #55426, .T. ) ;
#856=CARTESIAN_POINT ( 'NONE',  ( 1.834533585138716782, 0.1645414454686990324, 1.716894335133994698 ) ) ;
#857=CARTESIAN_POINT ( 'NONE',  ( 0.04025042243083893495, 0.7762349914572730381, 1.861342399428978389 ) ) ;
#858=CARTESIAN_POINT ( 'NONE',  ( 1.424907242902058613, -1.669187457468356950, -1.580674740522235888 ) ) ;
#860=CARTESIAN_POINT ( 'NONE',  ( 1.230147817042701375, -1.435374304221140651, -1.748800500726248153 ) ) ;
#861=CARTESIAN_POINT ( 'NONE',  ( 3.774133669461790852, 1.169908569812891264, 1.751025317131530423 ) ) ;
#865=CARTESIAN_POINT ( 'NONE',  ( 6.687508294236179651, -1.450827213159664675, 1.451031289061379681 ) ) ;
#871=CARTESIAN_POINT ( 'NONE',  ( 5.607756438734910809, 1.682095628590657643, 1.451081198120441229 ) ) ;
#872=CARTESIAN_POINT ( 'NONE',  ( 3.398540877415173966, 1.727514402264049620, -1.348270469230819391 ) ) ;
#875=CARTESIAN_POINT ( 'NONE',  ( 6.111998723603361938, -0.7147493727725148238, 1.996541221815250733 ) ) ;
#877=CARTESIAN_POINT ( 'NONE',  ( 6.610000000000006537, 0.002781820520842553934, 2.000159646111852929 ) ) ;
#879=CARTESIAN_POINT ( 'NONE',  ( 5.590118541908202232, 1.264772504208915072, 1.701965355810124203 ) ) ;
#883=CARTESIAN_POINT ( 'NONE',  ( 6.438358464623771482, 2.137424745569570295, 0.3223339197731683869 ) ) ;
#888=CARTESIAN_POINT ( 'NONE',  ( 1.628031597684251208, 0.1703553616784689029, 1.732092769550299227 ) ) ;
#893=CARTESIAN_POINT ( 'NONE',  ( 4.891577088959510711, 1.599438101461609918, 1.454397306527709155 ) ) ;
#896=CARTESIAN_POINT ( 'NONE',  ( 5.084929678302336775, -0.2608814864752464491, -2.145832476913120068 ) ) ;
#899=CARTESIAN_POINT ( 'NONE',  ( 6.292255012522757873, -1.961630990407544406, -0.1958228842163112771 ) ) ;
#900=CARTESIAN_POINT ( 'NONE',  ( 4.956219290344169970, 1.285291309562084816, 1.163873732738918587 ) ) ;
#902=CARTESIAN_POINT ( 'NONE',  ( 1.558417602779540889, -1.546676288433556756, 1.552911753681482487 ) ) ;
#903=CARTESIAN_POINT ( 'NONE',  ( 2.151827808644761308, -1.853761708218491178, -1.374033529217959515 ) ) ;
#904=CARTESIAN_POINT ( 'NONE',  ( 4.780574613336814771, -1.997868641178605298, -0.5047315492533087644 ) ) ;
#905=CARTESIAN_POINT ( 'NONE',  ( 6.515186996419942034, -1.882659881547473546, 0.4762376372081030262 ) ) ;
#910=EDGE_CURVE ( 'NONE', #102469, #190223, #25470, .T. ) ;
#911=CARTESIAN_POINT ( 'NONE',  ( 3.287459871768631636, 0.04819156399121089784, -2.120204644799832394 ) ) ;
#913=CARTESIAN_POINT ( 'NONE',  ( 1.547500230860882287, -1.423960469535384465, 1.427938386157491246 ) ) ;
#915=CARTESIAN_POINT ( 'NONE',  ( 4.735508036034060453, -2.019198892066270457, 0.8907332283012432406 ) ) ;
#917=CARTESIAN_POINT ( 'NONE',  ( 2.307254945994464457, -1.491077236629720248, -1.113220461199310618 ) ) ;
#921=CARTESIAN_POINT ( 'NONE',  ( 6.825078400183582694, 7.051583320515966591, 2.842498375355909435 ) ) ;
#923=ORIENTED_EDGE ( 'NONE', *, *, #66878, .F. ) ;
#924=CARTESIAN_POINT ( 'NONE',  ( 3.080987681966301572, -0.1499786273361273514, -2.055480798767507444 ) ) ;
#928=CARTESIAN_POINT ( 'NONE',  ( 3.158857784513937617, 0.4929582698031101939, 1.958447305144744410 ) ) ;
#931=CARTESIAN_POINT ( 'NONE',  ( 1.692332502075646783, -2.050886281836623581, -0.2028688129896583647 ) ) ;
#937=CARTESIAN_POINT ( 'NONE',  ( -0.1409997244345879974, 2.021982482314553131, -2.415666835770650778 ) ) ;
#938=CARTESIAN_POINT ( 'NONE',  ( 1.394213304513430174, 1.506067903837378097, -1.058747118707924262 ) ) ;
#940=CARTESIAN_POINT ( 'NONE',  ( 6.270183524512255246, 1.130759168108757873, 1.895055401287759178 ) ) ;
#942=CARTESIAN_POINT ( 'NONE',  ( 1.845224345143604561, -1.827161268409679407, 1.154667503900350445 ) ) ;
#944=CARTESIAN_POINT ( 'NONE',  ( 2.307827663788959871, -1.164988201124015577, -1.645758576239789051 ) ) ;
#948=CARTESIAN_POINT ( 'NONE',  ( 4.205908039233514195, -1.966248567454803364, 0.1440612947745979200 ) ) ;
#949=CARTESIAN_POINT ( 'NONE',  ( 3.010954138651841916, 0.05432569772663429358, 2.015980714967258614 ) ) ;
#953=CARTESIAN_POINT ( 'NONE',  ( -0.02244404828157658613, -0.004869073801674199918, -2.189079685368473527 ) ) ;
#955=CARTESIAN_POINT ( 'NONE',  ( 5.512195382060368409, 2.068158883198469855, -0.09793725168850964113 ) ) ;
#958=CARTESIAN_POINT ( 'NONE',  ( 6.539320575229233157, 0.001224430076711413356, 2.103502572931112091 ) ) ;
#959=CARTESIAN_POINT ( 'NONE',  ( 4.851822172175670467, -1.431287984025449100, -1.425384875499214443 ) ) ;
#962=CARTESIAN_POINT ( 'NONE',  ( 0.8310137546357538874, -1.940837517380919808, -0.6983779148895614686 ) ) ;
#970=CARTESIAN_POINT ( 'NONE',  ( 3.367796644333774569, -0.4264072692300807099, 2.128736309618290079 ) ) ;
#973=CARTESIAN_POINT ( 'NONE',  ( 2.823586671956069605, 1.020774559177588081, -1.532180179759069283 ) ) ;
#975=CARTESIAN_POINT ( 'NONE',  ( 3.896163805485418852, -0.6886730243073329039, -2.080591098665984795 ) ) ;
#977=CARTESIAN_POINT ( 'NONE',  ( 4.768612610038791111, -1.481304060603398032, 1.710260256980479898 ) ) ;
#983=CARTESIAN_POINT ( 'NONE',  ( 6.678955280633751102, -0.08981333502068940267, -1.767555964166868998 ) ) ;
#984=CARTESIAN_POINT ( 'NONE',  ( 4.266274873615797603, 2.012593780953766842, -0.05172614775082911426 ) ) ;
#986=CARTESIAN_POINT ( 'NONE',  ( 2.714012760861806317, -2.083235677042583944, 0.3076118897425133003 ) ) ;
#987=CARTESIAN_POINT ( 'NONE',  ( 1.300237133077002394, 1.285435684207901774, -1.420472988465313557 ) ) ;
#991=CARTESIAN_POINT ( 'NONE',  ( 1.803111746996020948, -1.665554870236161333, 1.050892442246372349 ) ) ;
#992=CARTESIAN_POINT ( 'NONE',  ( 0.4087956859853311142, 1.625333209436867321, 0.9259686016569528277 ) ) ;
#993=CARTESIAN_POINT ( 'NONE',  ( 0.5550359226569913096, 1.633180182981083028, -1.086726831054436682 ) ) ;
#994=CARTESIAN_POINT ( 'NONE',  ( -0.1054227091227821350, -1.855472971956134920, -0.4628026090111520552 ) ) ;
#998=CARTESIAN_POINT ( 'NONE',  ( 6.350466393003619814, 0.5888352225367661230, 1.775644890098279749 ) ) ;
#1003=CARTESIAN_POINT ( 'NONE',  ( 0.4146172280090759665, 0.7909515328246279342, 1.913518691844050323 ) ) ;
#1011=CARTESIAN_POINT ( 'NONE',  ( 5.793401095800717826, -1.774274828963496198, 0.8374297333502839225 ) ) ;
#1013=CARTESIAN_POINT ( 'NONE',  ( 2.741564358335503382, -1.928455994415989139, -0.5879317209081732498 ) ) ;
#1014=CARTESIAN_POINT ( 'NONE',  ( 3.116317603207694464, 1.870113986138211670, 0.4147879586954768549 ) ) ;
#1017=CARTESIAN_POINT ( 'NONE',  ( 2.103317784989285677, -0.4765762082987561321, 2.138964651187735821 ) ) ;
#1018=CARTESIAN_POINT ( 'NONE',  ( 0.2335667940002320309, 7.629137130509054288, -2.753349444758381281 ) ) ;
#1019=CARTESIAN_POINT ( 'NONE',  ( 3.004993591039197831, 1.578202713744047303, 1.003818400984110681 ) ) ;
#1023=CARTESIAN_POINT ( 'NONE',  ( 4.341493734318905950, 0.4621530863439751724, -2.066033417628045932 ) ) ;
#1025=CARTESIAN_POINT ( 'NONE',  ( 6.180147188013234150, -1.146869210499700920, -1.723488058659912392 ) ) ;
#1026=CARTESIAN_POINT ( 'NONE',  ( 2.454727380131729753, -1.820530515947630379, -1.027877103350574250 ) ) ;
#1028=CARTESIAN_POINT ( 'NONE',  ( 1.061059408578250318, 0.3424711756105159877, -1.690240703899626107 ) ) ;
#1039=CARTESIAN_POINT ( 'NONE',  ( 1.066738840199648042, -1.428349636637029407, 1.113955053652333493 ) ) ;
#1050=CARTESIAN_POINT ( 'NONE',  ( 2.576407586095734725, 1.218277932339612901, -1.406949740073556887 ) ) ;
#1051=CARTESIAN_POINT ( 'NONE',  ( 0.3334082175802362547, 0.6002418569295930872, -1.819223357073847636 ) ) ;
#1052=CARTESIAN_POINT ( 'NONE',  ( 0.4695848928168535608, -1.793611485386744420, -1.130822890709509254 ) ) ;
#1059=CARTESIAN_POINT ( 'NONE',  ( 4.698083300297758669, 0.8457734583860087030, -1.778757171186759134 ) ) ;
#1060=CARTESIAN_POINT ( 'NONE',  ( 1.067215373428985092, -1.669322716927954753, 1.307481345630675529 ) ) ;
#1064=CARTESIAN_POINT ( 'NONE',  ( 6.035146784841348477, -1.584849238314169240, -1.513754250258770639 ) ) ;
#1066=CARTESIAN_POINT ( 'NONE',  ( 3.803666480526507687, -0.5600534170543782775, 1.843171563392527856 ) ) ;
#1069=CARTESIAN_POINT ( 'NONE',  ( 0.9442952520863318044, 0.8911936224933308948, -2.019119535841918278 ) ) ;
#1072=( BOUNDED_SURFACE ( )  B_SPLINE_SURFACE ( 3, 3, ( 
 ( #98633, #161515, #128031, #95467, #162577, #66087, #46700, #14151, #212356, #17347, #180936 ),
 ( #13097, #131196, #197184, #132230, #163643, #16279, #15224, #195062, #81314, #83429, #112817 ),
 ( #177756, #63996, #147390, #61866, #193985, #48821, #130148, #164693, #213417, #82365, #79177 ),
 ( #148454, #145293, #181989, #24, #80245, #198239, #211298, #49877, #33621, #146343, #62922 ),
 ( #47778, #99692, #129090, #178830, #30444, #113891, #54142, #20550, #137536, #171077, #168948 ),
 ( #103965, #38957, #120278, #170007, #117067, #2151, #186252, #187328, #153773, #37887, #183065 ),
 ( #203554, #68228, #85563, #34679, #201424, #102889, #67156, #71425, #3222, #21595, #118138 ) ),
 .UNSPECIFIED., .T., .F., .F. ) 
 B_SPLINE_SURFACE_WITH_KNOTS ( ( 4, 3, 4 ),
 ( 4, 1, 1, 1, 1, 1, 1, 1, 4 ),
 ( 0.000000000000000000, 0.5000000000000000000, 1.000000000000000000 ),
 ( 0.000000000000000000, 0.2256085737580844630, 0.3975982043691296264, 0.5251069566405043298, 0.6172860083021659561, 0.6832860984239963464, 0.7321959383537668398, 0.7728624839797392232, 1.000000000000000000 ),
 .UNSPECIFIED. ) 
 GEOMETRIC_REPRESENTATION_ITEM ( )  RATIONAL_B_SPLINE_SURFACE ( (
 ( 1.000000000000000222, 1.000000000000000222, 1.000000000000000444, 0.9999999999999996669, 1.000000000000000444, 0.9999999999999997780, 1.000000000000000222, 1.000000000000000222, 0.9999999999999996669, 1.000000000000000000, 1.000000000000000000),
 ( 0.3333333333333334259, 0.3333333333333334259, 0.3333333333333334259, 0.3333333333333333703, 0.3333333333333334259, 0.3333333333333333148, 0.3333333333333334814, 0.3333333333333334259, 0.3333333333333331483, 0.3333333333333334259, 0.3333333333333333703),
 ( 0.3333333333333334259, 0.3333333333333334259, 0.3333333333333334259, 0.3333333333333333703, 0.3333333333333334259, 0.3333333333333333148, 0.3333333333333334814, 0.3333333333333334259, 0.3333333333333331483, 0.3333333333333334259, 0.3333333333333333703),
 ( 1.000000000000000222, 1.000000000000000222, 1.000000000000000444, 0.9999999999999996669, 1.000000000000000444, 0.9999999999999997780, 1.000000000000000222, 1.000000000000000222, 0.9999999999999996669, 1.000000000000000000, 1.000000000000000000),
 ( 0.3333333333333334259, 0.3333333333333334259, 0.3333333333333334259, 0.3333333333333333703, 0.3333333333333334259, 0.3333333333333333148, 0.3333333333333334814, 0.3333333333333334259, 0.3333333333333331483, 0.3333333333333334259, 0.3333333333333333703),
 ( 0.3333333333333334259, 0.3333333333333334259, 0.3333333333333334259, 0.3333333333333333703, 0.3333333333333334259, 0.3333333333333333148, 0.3333333333333334814, 0.3333333333333334259, 0.3333333333333331483, 0.3333333333333334259, 0.3333333333333333703),
 ( 1.000000000000000222, 1.000000000000000222, 1.000000000000000444, 0.9999999999999996669, 1.000000000000000444, 0.9999999999999997780, 1.000000000000000222, 1.000000000000000222, 0.9999999999999996669, 1.000000000000000000, 1.000000000000000000) ) ) 
 REPRESENTATION_ITEM ( '' )  SURFACE ( )  );
#1074=CARTESIAN_POINT ( 'NONE',  ( 6.543809977506837683, 1.355650292293397507, 1.428865145875155340 ) ) ;
#1075=CARTESIAN_POINT ( 'NONE',  ( 1.505311199525250831, -1.927169978453403321, 0.2396651170105366657 ) ) ;
#1076=CARTESIAN_POINT ( 'NONE',  ( 6.766976407292540685, -2.298085592349991213, 0.04593636341931536110 ) ) ;
#1078=CARTESIAN_POINT ( 'NONE',  ( 4.381604285809827637, -1.781765127997904763, 0.5371461504297748712 ) ) ;
#1084=CARTESIAN_POINT ( 'NONE',  ( 0.6092356648998223934, -0.3158941238240610128, 2.168550393043596536 ) ) ;
#1089=( BOUNDED_CURVE ( )  B_SPLINE_CURVE ( 3, ( #195966, #64881, #99529, #165589 ),
 .UNSPECIFIED., .F., .T. ) 
 B_SPLINE_CURVE_WITH_KNOTS ( ( 4, 4 ),
 ( 0.4999999999999963918, 1.000000000000000000 ),
 .UNSPECIFIED. ) 
 CURVE ( )  GEOMETRIC_REPRESENTATION_ITEM ( )  RATIONAL_B_SPLINE_CURVE ( ( 1.000000000000004663, 0.3333333333333333703, 0.3333333333333285409, 1.000000000000000000 ) ) 
 REPRESENTATION_ITEM ( '' )  );
#1090=CARTESIAN_POINT ( 'NONE',  ( 1.717148762710469789, -0.2249250470785572054, 1.811706739299999924 ) ) ;
#1093=CARTESIAN_POINT ( 'NONE',  ( 4.113671241589770489, 0.09026135180613574505, 1.731944212183807341 ) ) ;
#1096=CARTESIAN_POINT ( 'NONE',  ( 0.1331565106231571705, 2.881392620029461504, -2.434650611646618223 ) ) ;
#1098=CARTESIAN_POINT ( 'NONE',  ( 0.2934164811014350893, 1.426665091747752356, 1.294802382297273180 ) ) ;
#1099=CARTESIAN_POINT ( 'NONE',  ( 4.135565103414404753, 1.848670044762780407, -0.6568835154602686854 ) ) ;
#1103=CARTESIAN_POINT ( 'NONE',  ( 5.180389117862056914, 1.045492054797515946, 1.844774357600783121 ) ) ;
#1107=CARTESIAN_POINT ( 'NONE',  ( 3.397389602098393802, -1.828008730618407851, 0.9717071122367711977 ) ) ;
#1111=CARTESIAN_POINT ( 'NONE',  ( 3.446149177467156655, -2.027825264502993718, -1.082511230532481106 ) ) ;
#1119=CARTESIAN_POINT ( 'NONE',  ( 3.761887187967042134, 0.6396200178584460216, -1.802413552503052463 ) ) ;
#1121=CARTESIAN_POINT ( 'NONE',  ( 5.297747862459361912, -0.6177129893134482019, 1.610538751920454592 ) ) ;
#1122=CARTESIAN_POINT ( 'NONE',  ( 3.362517798112668821, -1.944730434982215650, -0.5331690889110105580 ) ) ;
#1123=CARTESIAN_POINT ( 'NONE',  ( 5.537770794106480210, -1.814135573521371780, 1.411581493584870728 ) ) ;
#1125=CARTESIAN_POINT ( 'NONE',  ( 1.260703874955213744, 0.8971468365699288849, 2.016480257658866737 ) ) ;
#1127=CARTESIAN_POINT ( 'NONE',  ( 5.852768638770064591, -1.394116391329143667, 1.090054309861036241 ) ) ;
#1129=CARTESIAN_POINT ( 'NONE',  ( 1.728911070687192186, 0.2280534122649588435, 2.280891765651926750 ) ) ;
#1130=CARTESIAN_POINT ( 'NONE',  ( 0.04040834310030903126, -1.341606091951352164, -1.108378290077848494 ) ) ;
#1135=CARTESIAN_POINT ( 'NONE',  ( 6.707487347292075519, -1.660346423639452951, -1.236579608897829363 ) ) ;
#1136=CARTESIAN_POINT ( 'NONE',  ( 1.305875433988498813, -1.124247956386617009, -1.673852571057245830 ) ) ;
#1139=CARTESIAN_POINT ( 'NONE',  ( 5.197847267195914611, -0.6914886683457229788, 1.798296804713859220 ) ) ;
#1141=CARTESIAN_POINT ( 'NONE',  ( 1.863841412593499003, -1.787636906239049805, -1.318573911375673369 ) ) ;
#1148=CARTESIAN_POINT ( 'NONE',  ( 3.948569229637605815, -1.449640539659799776, -0.9628182713226125511 ) ) ;
#1149=CARTESIAN_POINT ( 'NONE',  ( 2.611707774152134842, 0.5260268489151799232, -1.889944157703125072 ) ) ;
#1155=CARTESIAN_POINT ( 'NONE',  ( 0.6255240776356413290, 0.2040786869749251498, -2.052575575099666150 ) ) ;
#1158=CARTESIAN_POINT ( 'NONE',  ( 1.516897200560879178, 1.518302048914378588, -1.677564506150258206 ) ) ;
#1161=CARTESIAN_POINT ( 'NONE',  ( 2.442468673064964957, 0.4055347385497136137, 1.825902681341363021 ) ) ;
#1162=CARTESIAN_POINT ( 'NONE',  ( 1.177864744846460754, 1.312336027064511690, 1.133722492108141244 ) ) ;
#1163=CARTESIAN_POINT ( 'NONE',  ( 5.214472588068230330, 2.024700573814151028, 0.8392323156421463981 ) ) ;
#1164=CARTESIAN_POINT ( 'NONE',  ( 5.438606028847273066, 2.272309368472532398, 0.4011960609803484901 ) ) ;
#1165=CARTESIAN_POINT ( 'NONE',  ( 0.9013288230189763217, 1.684346374898238352, 1.187240197102001904 ) ) ;
#1166=CARTESIAN_POINT ( 'NONE',  ( 3.503789773231671845, -0.7878879028691202491, -1.775113385239434072 ) ) ;
#1168=CARTESIAN_POINT ( 'NONE',  ( 6.169203917683822702, 0.1378038699498609632, -1.865550841118966297 ) ) ;
#1169=CARTESIAN_POINT ( 'NONE',  ( 1.468750000000000888, 0.7852924748299092705, -1.895863743164120097 ) ) ;
#1171=CARTESIAN_POINT ( 'NONE',  ( 0.4734851067992265627, 1.504414441068102404, 0.8618086654073161545 ) ) ;
#1175=CARTESIAN_POINT ( 'NONE',  ( 4.729138786257041538, 2.011204126674607462, 0.1455352507326590494 ) ) ;
#1179=CARTESIAN_POINT ( 'NONE',  ( 2.156629195875509719, -1.411784796728832392, 1.157573153174975111 ) ) ;
#1187=CARTESIAN_POINT ( 'NONE',  ( 6.481118763745143063, -1.847444428138062422, -0.8165197575118980922 ) ) ;
#1188=CARTESIAN_POINT ( 'NONE',  ( 6.621772978582266767, -0.4938884631311352691, 2.173981893038397839 ) ) ;
#1191=CARTESIAN_POINT ( 'NONE',  ( 5.858293207932864455, 0.8329246649354884457, 1.885258002110825615 ) ) ;
#1192=CARTESIAN_POINT ( 'NONE',  ( 5.502577337681268332, -1.966645332631598908, 0.4444998760482973821 ) ) ;
#1196=CARTESIAN_POINT ( 'NONE',  ( -0.2108831679770946654, 7.629137130509072939, -2.497154329497498715 ) ) ;
#1201=CARTESIAN_POINT ( 'NONE',  ( 5.448592227559037049, 1.351948914259465173, 1.495821383734573073 ) ) ;
#1202=CARTESIAN_POINT ( 'NONE',  ( 4.663899394030392997, -1.200468288914667614, 1.396033019000951336 ) ) ;
#1203=CARTESIAN_POINT ( 'NONE',  ( -0.02319159430947541692, 2.051704324979522820, -2.228571760951563618 ) ) ;
#1204=CARTESIAN_POINT ( 'NONE',  ( 3.405163318333865874, 1.819529416799025912, -1.419322092190724138 ) ) ;
#1206=CARTESIAN_POINT ( 'NONE',  ( 5.237646302014136168, -1.524508687941978469, -1.532700278705993790 ) ) ;
#1208=CARTESIAN_POINT ( 'NONE',  ( 0.1693407553623625106, 1.118952433510589817, 1.587118285914286941 ) ) ;
#1210=CARTESIAN_POINT ( 'NONE',  ( 4.025041230705061146, 2.281562605710918845, -0.2770438755856743929 ) ) ;
#1213=CARTESIAN_POINT ( 'NONE',  ( 3.432352559540859271, 1.824792983844251371, 0.4109263881779609551 ) ) ;
#1214=CARTESIAN_POINT ( 'NONE',  ( 0.9844543725016400293, -1.211084316286781037, 1.480072698922259455 ) ) ;
#1217=CARTESIAN_POINT ( 'NONE',  ( 2.912931060594741162, 1.598032330669514778, -1.522282275181946032 ) ) ;
#1218=EDGE_CURVE ( 'NONE', #40908, #89432, #43359, .T. ) ;
#1224=CARTESIAN_POINT ( 'NONE',  ( 0.3331948752925878998, -1.804169345717737238, 0.7948754592718260126 ) ) ;
#1225=CARTESIAN_POINT ( 'NONE',  ( 0.08353690965077953390, -0.1615750995121113531, -2.271551823106517709 ) ) ;
#1226=CARTESIAN_POINT ( 'NONE',  ( 1.662477996687723669, -0.7030478115006146833, -1.831755296705489977 ) ) ;
#1227=CARTESIAN_POINT ( 'NONE',  ( 4.487212223095434105, 0.09620561770018636050, 2.060423205476647812 ) ) ;
#1235=CARTESIAN_POINT ( 'NONE',  ( 6.877413710614480813, -0.1567828624706164298, 2.136824976188213654 ) ) ;
#1237=CARTESIAN_POINT ( 'NONE',  ( 6.567912610837368881, -1.126952994821692533, 1.456688911285822119 ) ) ;
#1241=CARTESIAN_POINT ( 'NONE',  ( 1.475632603725419267, 1.109822327618605442, 1.505604422130282449 ) ) ;
#1245=CARTESIAN_POINT ( 'NONE',  ( 0.6977377480232997975, 1.284608138224270002, 1.416691289136004395 ) ) ;
#1247=CARTESIAN_POINT ( 'NONE',  ( 2.957584522866180343, 1.761491525812574510, -0.1715649573520404425 ) ) ;
#1248=CARTESIAN_POINT ( 'NONE',  ( 1.031728963041964153, -1.865498905729731316, 0.4196304693004496156 ) ) ;
#1251=CARTESIAN_POINT ( 'NONE',  ( 4.235878408818731344, 1.915113449751761010, -0.05082400106456300831 ) ) ;
#1253=CARTESIAN_POINT ( 'NONE',  ( 5.107841235723004303, 0.6198312778436664283, -1.869525964861347589 ) ) ;
#1254=CARTESIAN_POINT ( 'NONE',  ( 1.002369745560643510, -0.9483682245385971488, 1.896766750748935415 ) ) ;
#1256=CARTESIAN_POINT ( 'NONE',  ( 3.449935675575486638, 1.870836310073907827, 0.001118452434160921221 ) ) ;
#1257=CARTESIAN_POINT ( 'NONE',  ( 1.101864800459760207, -1.825872481749410525, -0.002338443969775172437 ) ) ;
#1259=CARTESIAN_POINT ( 'NONE',  ( 3.985166894971280183, -0.2153072539897090687, -2.196357064762343825 ) ) ;
#1262=CARTESIAN_POINT ( 'NONE',  ( 2.383324636069758640, -0.002395321609373335381, 2.062851379284504461 ) ) ;
#1271=CARTESIAN_POINT ( 'NONE',  ( 4.738769824615551407, -2.007376682328159134, -0.5062664373569197851 ) ) ;
#1273=CARTESIAN_POINT ( 'NONE',  ( 1.563986776035675819, 2.129895014553784272, -0.3678597298803277793 ) ) ;
#1275=CARTESIAN_POINT ( 'NONE',  ( 2.033858944562048965, -1.958440182618191416, 0.4929867953931149627 ) ) ;
#1279=CARTESIAN_POINT ( 'NONE',  ( 6.380232485702068246, -0.2495653932444163448, 2.000551205290925783 ) ) ;
#1280=CARTESIAN_POINT ( 'NONE',  ( -0.04763828917917976857, -1.313539345393003321, 1.530161206715647149 ) ) ;
#1281=CARTESIAN_POINT ( 'NONE',  ( 6.639320575229256782, 2.033582276073117701, 2.408309898857839304 ) ) ;
#1282=CARTESIAN_POINT ( 'NONE',  ( 4.792620198997869174, 1.822056328612733145, -1.217503271791681163 ) ) ;
#1284=CARTESIAN_POINT ( 'NONE',  ( 3.902528505893249733, -1.892296425594198750, -0.2755589300712790735 ) ) ;
#1288=CARTESIAN_POINT ( 'NONE',  ( 1.722280025409760329, 1.994874335020242695, 0.2930476355553628953 ) ) ;
#1290=CARTESIAN_POINT ( 'NONE',  ( 0.2227793574855509162, 2.196107815404338748, 0.6574155683778097892 ) ) ;
#1292=CARTESIAN_POINT ( 'NONE',  ( 4.401177694619070380, 1.385992036768167068, 1.026327495003590551 ) ) ;
#1293=CARTESIAN_POINT ( 'NONE',  ( 0.1399997263886038068, 0.2431072571701595186, -2.034387401959360187 ) ) ;
#1296=CARTESIAN_POINT ( 'NONE',  ( 1.310910670669521272, -1.548711629584406113, 1.204245502051364936 ) ) ;
#1298=CARTESIAN_POINT ( 'NONE',  ( 0.1755611466353447780, 1.308645672766622914, -2.493865953706751792 ) ) ;
#1302=CARTESIAN_POINT ( 'NONE',  ( 3.773895570499671503, 1.797357569013877887, -0.2251608728849313346 ) ) ;
#1306=CARTESIAN_POINT ( 'NONE',  ( 4.406777823604307365, -0.4013596350818599556, -1.766266891646672166 ) ) ;
#1308=FILL_AREA_STYLE ('',( #117284 ) ) ;
#1310=CARTESIAN_POINT ( 'NONE',  ( 6.039480578167179203, 1.719269793624801590, -0.7129749698730929452 ) ) ;
#1312=CARTESIAN_POINT ( 'NONE',  ( 3.550306043379815257, -1.284141074626928392, 1.421643848488469031 ) ) ;
#1321=CARTESIAN_POINT ( 'NONE',  ( 5.260995011843273339, -0.05493784808423751720, -2.116803055475650730 ) ) ;
#1322=CARTESIAN_POINT ( 'NONE',  ( 0.9894095316701528864, 1.906041449620498707, -1.019753361306941386 ) ) ;
#1325=CARTESIAN_POINT ( 'NONE',  ( 0.7799652524137989928, -1.018268764971082430, 1.515009401286564694 ) ) ;
#1327=CARTESIAN_POINT ( 'NONE',  ( 3.258640109524315154, -1.383274205585843797, 1.191454006006509303 ) ) ;
#1329=CARTESIAN_POINT ( 'NONE',  ( 1.757924209179074770, 0.7287868685415777037, -1.768279316124596878 ) ) ;
#1331=CARTESIAN_POINT ( 'NONE',  ( 2.963290904843593587, 1.662405373943407261, 1.055889934586044188 ) ) ;
#1332=CARTESIAN_POINT ( 'NONE',  ( 4.739756017840593749, 1.937102985688110568, 0.1393878014490906314 ) ) ;
#1335=CARTESIAN_POINT ( 'NONE',  ( 4.096021571020786567, 1.387573888390711385, 1.603661410755026440 ) ) ;
#1337=CARTESIAN_POINT ( 'NONE',  ( 2.789602095257078584, 1.815147277589121533, -0.6018686165152677958 ) ) ;
#1343=CARTESIAN_POINT ( 'NONE',  ( 5.268108045213575785, 0.9031548532531764595, 1.586571422427636824 ) ) ;
#1348=CARTESIAN_POINT ( 'NONE',  ( 5.787941465827733722, -0.8397648285632768328, 1.671655200917811168 ) ) ;
#1357=CARTESIAN_POINT ( 'NONE',  ( 6.877770952621925282, -2.108145516380425910, 0.5186976372570563099 ) ) ;
#1358=CARTESIAN_POINT ( 'NONE',  ( 0.8259615556985228091, 0.8540520341687988237, -1.937501654548081875 ) ) ;
#1361=CARTESIAN_POINT ( 'NONE',  ( 6.807487347360918761, -1.659057770219806160, -1.238116672595261480 ) ) ;
#1362=CARTESIAN_POINT ( 'NONE',  ( 1.733694375844633706, 1.821329977863223926, 0.2691589665217360983 ) ) ;
#1367=CARTESIAN_POINT ( 'NONE',  ( 1.939794425703120995, 0.8746495868690505882, -2.119022276272637839 ) ) ;
#1370=CARTESIAN_POINT ( 'NONE',  ( 2.197387184563174944, 1.746976956643018442, -0.7784620831182070821 ) ) ;
#1374=CARTESIAN_POINT ( 'NONE',  ( 0.6330651387380836770, 1.861715503769780566, 0.7666268175344230773 ) ) ;
#1375=CARTESIAN_POINT ( 'NONE',  ( 0.9187138386215136787, -1.424830647414500051, 1.348730089142296418 ) ) ;
#1380=CARTESIAN_POINT ( 'NONE',  ( 4.312501488504257630, 1.911392599577836693, 0.8473735431044140398 ) ) ;
#1381=CARTESIAN_POINT ( 'NONE',  ( 2.693947877954734338, -1.764960265255947736, -0.1323486908471616652 ) ) ;
#1384=CARTESIAN_POINT ( 'NONE',  ( 5.736350775408121550, 0.4420370857395071740, 2.249087507758650517 ) ) ;
#1385=CARTESIAN_POINT ( 'NONE',  ( 3.327794560494615084, 1.698141246764593770, 0.3800555388253792355 ) ) ;
#1387=CARTESIAN_POINT ( 'NONE',  ( 2.864235035935404738, -0.5475380835847867278, 1.645162456946830831 ) ) ;
#1388=CARTESIAN_POINT ( 'NONE',  ( 3.772083221923136609, -2.139637338432040181, 0.3678540365955537128 ) ) ;
#1390=CARTESIAN_POINT ( 'NONE',  ( 5.753138727196851043, 0.1435251449807967150, -2.011451301405759118 ) ) ;
#1391=CARTESIAN_POINT ( 'NONE',  ( 0.6250000000000001110, -2.052068128417942283, 3.751950811937565850E-14 ) ) ;
#1393=CARTESIAN_POINT ( 'NONE',  ( 2.010648722831087198, 1.429088002864507212, -1.291968487218410511 ) ) ;
#1395=CARTESIAN_POINT ( 'NONE',  ( 5.414381242519362480, -2.221583670654456721, 0.0001252536179462138133 ) ) ;
#1397=CARTESIAN_POINT ( 'NONE',  ( -0.1106856583841242386, 7.629137130509040965, -2.596956429031356262 ) ) ;
#1402=CARTESIAN_POINT ( 'NONE',  ( 1.418920233055203761, -0.8037200727962053870, -2.070967414838392084 ) ) ;
#1406=CARTESIAN_POINT ( 'NONE',  ( 6.802048716365778347, -2.262122309816359422, 0.04523717395405778968 ) ) ;
#1410=CARTESIAN_POINT ( 'NONE',  ( 4.018078825213769356, 2.047437054436978876, -0.2496575186523365686 ) ) ;
#1414=CARTESIAN_POINT ( 'NONE',  ( 5.413307058180727438, -0.2754873708227522644, 1.850039175317084617 ) ) ;
#1415=CARTESIAN_POINT ( 'NONE',  ( 4.729033670188855787, 1.730023327335796113, 0.1204123811070593880 ) ) ;
#1416=CARTESIAN_POINT ( 'NONE',  ( 4.247407853763897734, 1.739958666061100390, -0.04810691789801542495 ) ) ;
#1418=CARTESIAN_POINT ( 'NONE',  ( 1.664052950329899971, 1.182993008014191938, 1.963431667052175422 ) ) ;
#1420=CARTESIAN_POINT ( 'NONE',  ( 5.847236579984706140, 0.6061975457797988964, -2.000951093856804253 ) ) ;
#1421=CARTESIAN_POINT ( 'NONE',  ( 6.456980378258257325, 0.3295113258894696862, -1.913641714292084073 ) ) ;
#1423=CARTESIAN_POINT ( 'NONE',  ( 1.090470458312575053, -0.4872005951904456733, 1.956561897242928172 ) ) ;
#1429=CARTESIAN_POINT ( 'NONE',  ( 3.405043383231837417, -0.4154483767263848493, -2.079220720149973278 ) ) ;
#1431=CARTESIAN_POINT ( 'NONE',  ( 5.654876981934024549, -1.436564326775534806, 1.126588154728463742 ) ) ;
#1437=CARTESIAN_POINT ( 'NONE',  ( 3.744402900219420793, 1.076886947916893211, -1.708549110318995368 ) ) ;
#1438=CARTESIAN_POINT ( 'NONE',  ( 0.5343771797220103759, 1.082321145649869587, -1.806417116151628477 ) ) ;
#1440=CARTESIAN_POINT ( 'NONE',  ( 3.572968443166994579, 1.680613686130405515, 0.7995154651666557255 ) ) ;
#1445=CARTESIAN_POINT ( 'NONE',  ( 6.332896556214961947, 0.1992470125839322093, 2.051223679500746133 ) ) ;
#1449=CARTESIAN_POINT ( 'NONE',  ( 2.073226780758777643, 1.288078611216292302, -1.160843940205048774 ) ) ;
#1450=CARTESIAN_POINT ( 'NONE',  ( 1.481926975991064710, -0.2526488567047910361, -1.721760536436983680 ) ) ;
#1451=CARTESIAN_POINT ( 'NONE',  ( 0.3941752559601471306, 1.712991706939146486, 1.546321376980333007 ) ) ;
#1454=CARTESIAN_POINT ( 'NONE',  ( 1.774756598535260466, -1.955815263226182932, -0.6494449766335576024 ) ) ;
#1456=CARTESIAN_POINT ( 'NONE',  ( 6.309976275596433481, -1.946771231211348319, 1.221538734657970693 ) ) ;
#1460=CARTESIAN_POINT ( 'NONE',  ( 0.6023365795125863453, -0.6618663087945526602, -1.857178468014776263 ) ) ;
#1462=CARTESIAN_POINT ( 'NONE',  ( 4.359561026920276916, -1.481784043772149229, -1.208992945495937610 ) ) ;
#1464=CARTESIAN_POINT ( 'NONE',  ( 6.375609195709820654, 2.113139023092651225, -0.6363509056886568205 ) ) ;
#1468=CARTESIAN_POINT ( 'NONE',  ( -0.02277885239688070759, -1.805142470748948513, -0.9059449988992168690 ) ) ;
#1469=CARTESIAN_POINT ( 'NONE',  ( 3.329449612262088021, 0.05463889213834548231, 2.307092628889866326 ) ) ;
#1470=CARTESIAN_POINT ( 'NONE',  ( 5.195737816846159873, -1.386088135442983260, -1.388664821390848347 ) ) ;
#1471=CARTESIAN_POINT ( 'NONE',  ( 1.235121763443976395, -0.04261391538399812023, -1.961451400788959631 ) ) ;
#1475=CARTESIAN_POINT ( 'NONE',  ( -0.2349522205629230309, -0.1529240981989663239, -2.083514258294770105 ) ) ;
#1479=CARTESIAN_POINT ( 'NONE',  ( 3.924824802941798030, -1.462044496099848212, 1.605114832664520153 ) ) ;
#1481=CARTESIAN_POINT ( 'NONE',  ( 1.652743449602233072, 2.098267697663995790, 0.3060111223712052020 ) ) ;
#1487=CARTESIAN_POINT ( 'NONE',  ( 2.179047869568909945, -0.09785464545388269930, -2.058565441667548068 ) ) ;
#1491=CARTESIAN_POINT ( 'NONE',  ( -0.02244404828157658613, 5.719765766439059540, -2.783169749654360814 ) ) ;
#1494=CARTESIAN_POINT ( 'NONE',  ( 4.512308969215598431, -1.911949174345693336, -0.04343532550177275214 ) ) ;
#1496=CARTESIAN_POINT ( 'NONE',  ( 1.616897013105462522, 1.519709519468028791, -1.676125853178417113 ) ) ;
#1498=CARTESIAN_POINT ( 'NONE',  ( 1.265540092975623088, 0.5243090560775253151, -1.734071359953066382 ) ) ;
#1499=CARTESIAN_POINT ( 'NONE',  ( 2.290125521308879808, -0.7372973962519657753, -1.768360312244516841 ) ) ;
#1500=CARTESIAN_POINT ( 'NONE',  ( 2.734898984476673789, -1.980466496001157317, -0.6033880717724803278 ) ) ;
#1502=CARTESIAN_POINT ( 'NONE',  ( 0.3210827503922530357, -0.09932373348091848297, 1.969089571372897085 ) ) ;
#1503=CARTESIAN_POINT ( 'NONE',  ( 5.672470344399177300, -1.220246509433765558, 1.490775554449337070 ) ) ;
#1504=CARTESIAN_POINT ( 'NONE',  ( 6.586557750117827403, -2.163372447211810989, -0.4352210726449382006 ) ) ;
#1507=CARTESIAN_POINT ( 'NONE',  ( 5.318824396150737321, -1.496427615725079097, 1.419873077484270496 ) ) ;
#1513=CARTESIAN_POINT ( 'NONE',  ( 4.735441112814092079, -1.926550399551892001, 0.8509862954892956077 ) ) ;
#1515=CARTESIAN_POINT ( 'NONE',  ( 1.346384888165049754, -0.9767783691352300846, 1.939140577548441380 ) ) ;
#1517=CARTESIAN_POINT ( 'NONE',  ( 5.237646302014136168, -1.524508687941978469, -1.532700278705993790 ) ) ;
#1518=CARTESIAN_POINT ( 'NONE',  ( 5.074870355641393438, -1.461326316769593348, 1.394373881654621394 ) ) ;
#1525=CARTESIAN_POINT ( 'NONE',  ( 3.749232653202066778, 0.2420323627391370025, -2.001857840249580800 ) ) ;
#1530=CARTESIAN_POINT ( 'NONE',  ( 5.401312781148373432, 1.764888628567516049, 1.247983453017486699 ) ) ;
#1535=CARTESIAN_POINT ( 'NONE',  ( 5.132435489663482286, 0.5880379476735001498, 1.928747580961232444 ) ) ;
#1537=CARTESIAN_POINT ( 'NONE',  ( 0.08204731311520391257, -1.671590265245853413, -0.4250796685295650246 ) ) ;
#1542=CARTESIAN_POINT ( 'NONE',  ( 5.606678975738343951, 1.416997745663551633, -1.221222563005261774 ) ) ;
#1543=CARTESIAN_POINT ( 'NONE',  ( 0.1881394758670457412, 1.160778376788082378, 1.644543748126830796 ) ) ;
#1544=CARTESIAN_POINT ( 'NONE',  ( 6.539320575229254473, 0.5926322452488984593, 1.950287522085321301 ) ) ;
#1549=CARTESIAN_POINT ( 'NONE',  ( 1.770341816056511863, 2.114587264445011883, -0.1591180397043714667 ) ) ;
#1550=CARTESIAN_POINT ( 'NONE',  ( 1.247672978039487734, 1.986097573956084439, -0.3474914183895366215 ) ) ;
#1551=CARTESIAN_POINT ( 'NONE',  ( 2.355456482938292240, -1.344675202547132464, -1.214172642412311598 ) ) ;
#1553=CARTESIAN_POINT ( 'NONE',  ( 5.981359018292747187, 1.999130597612966964, -0.8229454869796914984 ) ) ;
#1556=CLOSED_SHELL ( 'NONE', ( #107918, #9042, #10227, #38719, #9976, #149647, #133397, #214326 ) ) ;
#1558=CARTESIAN_POINT ( 'NONE',  ( -0.01269188720853537365, -0.5084903737302053361, 1.846954624685708923 ) ) ;
#1564=CARTESIAN_POINT ( 'NONE',  ( 4.540002997438313592, 0.9271085556134452954, -1.952944755896801610 ) ) ;
#1567=CARTESIAN_POINT ( 'NONE',  ( 1.793382672576701919, -0.1090974814243403090, -2.117938670719583527 ) ) ;
#1568=CARTESIAN_POINT ( 'NONE',  ( 6.809597967592865508, -0.3964169337347979161, 1.788522171948719874 ) ) ;
#1569=CARTESIAN_POINT ( 'NONE',  ( 2.776590643643538581, -1.885432240069355503, -0.5755950866291289492 ) ) ;
#1570=CARTESIAN_POINT ( 'NONE',  ( 5.414289803398987466, -1.912571729023364364, 0.006307610287324683096 ) ) ;
#1573=CARTESIAN_POINT ( 'NONE',  ( 6.373500198570408060, -0.2424619166165129514, 1.954513512140013676 ) ) ;
#1574=CARTESIAN_POINT ( 'NONE',  ( 1.728360517318433542, 0.1903740514868361433, 1.932600189055997619 ) ) ;
#1575=ORIENTED_EDGE ( 'NONE', *, *, #16285, .F. ) ;
#1582=CARTESIAN_POINT ( 'NONE',  ( 5.602191078447533279, -0.8559053986842229955, 1.710104642658970997 ) ) ;
#1584=CARTESIAN_POINT ( 'NONE',  ( 2.842613246588860942, 2.190307313262893185, 0.2694104812042824038 ) ) ;
#1585=CARTESIAN_POINT ( 'NONE',  ( 2.292262453775519404, -0.9438808975747980945, 1.994871701834355804 ) ) ;
#1587=CARTESIAN_POINT ( 'NONE',  ( 0.4516295384478058450, -1.352486712789633172, -1.352142238705160704 ) ) ;
#1590=CARTESIAN_POINT ( 'NONE',  ( 3.385274849524767316, 0.04804411014160993310, 2.069964801482151895 ) ) ;
#1594=CARTESIAN_POINT ( 'NONE',  ( 2.219795081190904629, -2.096929600374438429, 0.5247480557022954351 ) ) ;
#1595=CARTESIAN_POINT ( 'NONE',  ( 3.720431430916489646, 2.081484170424623859, 0.6860852429351402826 ) ) ;
#1603=CARTESIAN_POINT ( 'NONE',  ( 5.660742353926829118, 1.040242247344788762, 1.387327330804826619 ) ) ;
#1605=CARTESIAN_POINT ( 'NONE',  ( 3.784089331405198209, -1.229265877060268242, -1.665672133652921660 ) ) ;
#1606=CARTESIAN_POINT ( 'NONE',  ( 5.484029812627264633, -2.117403151077674739, 0.0008096548943584136460 ) ) ;
#1610=CARTESIAN_POINT ( 'NONE',  ( 2.799605281554286229, -1.456005023894543893, -1.326338995474019011 ) ) ;
#1611=CARTESIAN_POINT ( 'NONE',  ( 1.037202349414727109, -0.04413313863061394532, 1.912034500058952036 ) ) ;
#1612=CARTESIAN_POINT ( 'NONE',  ( 6.035170563425642953, -1.656272789430097703, -1.584931405618497990 ) ) ;
#1613=CARTESIAN_POINT ( 'NONE',  ( 3.351995281737112364, 1.825872481133209657, -0.0009662468829912955644 ) ) ;
#1619=CARTESIAN_POINT ( 'NONE',  ( 3.656497369231588745, 2.003880934342232578, 0.1932520657266077191 ) ) ;
#1621=CARTESIAN_POINT ( 'NONE',  ( 4.750807836863311095, -0.4258335417525476729, -1.914832529679215023 ) ) ;
#1625=CARTESIAN_POINT ( 'NONE',  ( 0.8727377898805768197, -0.05501089605610678251, -2.090203850258448792 ) ) ;
#1626=CARTESIAN_POINT ( 'NONE',  ( 6.262547730648324595, -1.248425448203832611, 1.254777848270997254 ) ) ;
#1628=CARTESIAN_POINT ( 'NONE',  ( 1.588088344156918907, -2.181139600106785092, -0.2122876309011075546 ) ) ;
#1629=CARTESIAN_POINT ( 'NONE',  ( 0.02830193721903468546, -1.592744100209501967, 0.7021035195741828216 ) ) ;
#1631=CARTESIAN_POINT ( 'NONE',  ( 0.1333692844072559003, 2.872395615372814515, -2.542035612928101873 ) ) ;
#1632=CARTESIAN_POINT ( 'NONE',  ( 0.2051046121598932848, -0.4657588872633237065, 1.660747436093058083 ) ) ;
#1633=CARTESIAN_POINT ( 'NONE',  ( 0.8085102987360716087, -1.969961327451934086, 1.183767188307288221 ) ) ;
#1634=CARTESIAN_POINT ( 'NONE',  ( 0.4861908890553789941, -2.175720422541329580, -0.2624175912114696252 ) ) ;
#1635=CARTESIAN_POINT ( 'NONE',  ( 3.106307083854151774, -2.204334110825040494, 0.1085914373066959593 ) ) ;
#1636=CARTESIAN_POINT ( 'NONE',  ( 0.3214382364499007161, -1.938747691508705184, -0.9774007134471692781 ) ) ;
#1638=CARTESIAN_POINT ( 'NONE',  ( 2.659486872612493613, 2.008994876937011398, -0.6687478447182227947 ) ) ;
#1640=CARTESIAN_POINT ( 'NONE',  ( 6.827182134110199030, 1.215541611938670608, 2.400477883804314150 ) ) ;
#1641=CARTESIAN_POINT ( 'NONE',  ( 5.245112492223927170, -1.652184091924509879, 0.9903546681122497031 ) ) ;
#1643=CARTESIAN_POINT ( 'NONE',  ( 2.033172958078794501, -2.045629734292064850, 1.034765616053961557 ) ) ;
#1647=CARTESIAN_POINT ( 'NONE',  ( 4.424628119981884211, -0.9497243516023866627, -2.008178830631357492 ) ) ;
#1655=CARTESIAN_POINT ( 'NONE',  ( 3.094375128876575065, -0.3905979561782264575, 1.978050703236901686 ) ) ;
#1657=CARTESIAN_POINT ( 'NONE',  ( 0.5497677191402570163, 1.525909772416549126, 1.387868932477815065 ) ) ;
#1663=CARTESIAN_POINT ( 'NONE',  ( 4.418054252288761141, 1.349281245414082342, -1.726737887558588591 ) ) ;
#1664=CARTESIAN_POINT ( 'NONE',  ( 1.002577532868035526, -1.966644254196001196, 0.4445047019146358691 ) ) ;
#1665=CARTESIAN_POINT ( 'NONE',  ( 1.311775528174640604, 1.236260529797410301, -1.364685630449238740 ) ) ;
#1666=CARTESIAN_POINT ( 'NONE',  ( 5.513300880735551246, -2.237181406077014323, 0.4993042908148867531 ) ) ;
#1667=CARTESIAN_POINT ( 'NONE',  ( 3.960763856159645879, 0.2235175650571289141, -1.827449369368571386 ) ) ;
#1671=CARTESIAN_POINT ( 'NONE',  ( 3.996943106591983597, 1.542326501817241180, -0.9764022233923685956 ) ) ;
#1672=CARTESIAN_POINT ( 'NONE',  ( 5.256482491209823138, 1.942542154241846397, -0.5404887192124520068 ) ) ;
#1674=CARTESIAN_POINT ( 'NONE',  ( 4.997079013686112958, 1.883918014071528146, -1.252661935414706162 ) ) ;
#1676=CARTESIAN_POINT ( 'NONE',  ( 6.282269041519704444, -1.129704631681987204, 1.777121156631493726 ) ) ;
#1678=CARTESIAN_POINT ( 'NONE',  ( 4.650872726564402981, -0.4503784926754761386, -2.020631409805350387 ) ) ;
#1683=CARTESIAN_POINT ( 'NONE',  ( 2.191906549581578822, -0.8239416835312768361, 1.741544141456285555 ) ) ;
#1686=CARTESIAN_POINT ( 'NONE',  ( 6.455907338579963017, -0.6669464233056993097, 1.853184144328771543 ) ) ;
#1690=CARTESIAN_POINT ( 'NONE',  ( 0.4398875993102538962, -2.011672884243600024, 0.6710486789910232730 ) ) ;
#1691=CARTESIAN_POINT ( 'NONE',  ( 2.268119307372215676, 0.5874642799142595351, -2.142291314107084954 ) ) ;
#1692=CARTESIAN_POINT ( 'NONE',  ( 3.715936783694527179, -2.075135040979354528, 0.3580079364009710052 ) ) ;
#1695=CARTESIAN_POINT ( 'NONE',  ( 0.6075646283644918766, 0.5893627863808469369, -1.765331146162614662 ) ) ;
#1701=CARTESIAN_POINT ( 'NONE',  ( 0.8441712343106638761, -1.349783269286155774, -1.635521010841307410 ) ) ;
#1704=CARTESIAN_POINT ( 'NONE',  ( 4.949637131784443866, 1.452432516441283905, 1.319008059494260143 ) ) ;
#1705=CARTESIAN_POINT ( 'NONE',  ( 3.204151765443470357, -2.159293047372488950, 0.1044485798024074874 ) ) ;
#1706=CARTESIAN_POINT ( 'NONE',  ( 1.311775528174640604, 1.236260529797410301, -1.364685630449238740 ) ) ;
#1709=CARTESIAN_POINT ( 'NONE',  ( 4.277133665768851678, 1.139379310349198260, 1.315593229251702523 ) ) ;
#1713=CARTESIAN_POINT ( 'NONE',  ( 1.463986924769441478, 2.129665692569195024, -0.3698555562515608020 ) ) ;
#1714=CARTESIAN_POINT ( 'NONE',  ( 3.796249832574852601, -1.863883295361246084, 0.7690029265580224926 ) ) ;
#1716=CARTESIAN_POINT ( 'NONE',  ( 1.305796196612364124, -0.5247483525172502716, 2.096912610238470975 ) ) ;
#1717=CARTESIAN_POINT ( 'NONE',  ( 3.660970522598467891, -1.737989841360635834, -0.9306492429120606369 ) ) ;
#1718=CARTESIAN_POINT ( 'NONE',  ( 6.609000000000047947, 7.629137130509099585, 2.699999999999993516 ) ) ;
#1719=CARTESIAN_POINT ( 'NONE',  ( 3.069799403425711226, -1.154559939549955949, 1.561474065217777207 ) ) ;
#1728=CARTESIAN_POINT ( 'NONE',  ( 6.299901696735699552, -0.7855725015378700604, 2.169893659913350259 ) ) ;
#1730=CARTESIAN_POINT ( 'NONE',  ( 4.873855640358407904, -1.924671727690111966, 0.3787619532854279436 ) ) ;
#1731=CARTESIAN_POINT ( 'NONE',  ( 1.828750219146151323, 0.7691198443132395424, -1.864169014999479623 ) ) ;
#1733=CARTESIAN_POINT ( 'NONE',  ( 3.415340404243884187, -1.954662906411578804, 0.8143554997327147049 ) ) ;
#1737=CARTESIAN_POINT ( 'NONE',  ( 3.908013947242465314, 1.300727540704300633, -1.303293010247716488 ) ) ;
#1741=CARTESIAN_POINT ( 'NONE',  ( 4.974906307097914926, -1.534222593358970821, 1.464151343314526121 ) ) ;
#1745=CARTESIAN_POINT ( 'NONE',  ( 5.589157960464589792, 1.819533713976368094, -0.9674792931896135650 ) ) ;
#1747=CARTESIAN_POINT ( 'NONE',  ( 1.047037934171668905, 1.643801913826014482, -0.8725737860223039544 ) ) ;
#1748=CARTESIAN_POINT ( 'NONE',  ( 2.718100415690410721, 1.734538518968967935, 0.6181264464550640936 ) ) ;
#1751=( BOUNDED_CURVE ( )  B_SPLINE_CURVE ( 3, ( #164109, #28773, #94855, #113290 ),
 .UNSPECIFIED., .F., .T. ) 
 B_SPLINE_CURVE_WITH_KNOTS ( ( 4, 4 ),
 ( 0.4999999999999988898, 1.000000000000000000 ),
 .UNSPECIFIED. ) 
 CURVE ( )  GEOMETRIC_REPRESENTATION_ITEM ( )  RATIONAL_B_SPLINE_CURVE ( ( 1.000000000000001998, 0.3333333333333334814, 0.3333333333333319826, 1.000000000000000444 ) ) 
 REPRESENTATION_ITEM ( '' )  );
#1754=CARTESIAN_POINT ( 'NONE',  ( 2.649284799151204073, -1.834272514977531632, 1.226802785254533568 ) ) ;
#1755=CARTESIAN_POINT ( 'NONE',  ( 4.640055761359395348, 0.9730784542925293712, -2.042606338686814738 ) ) ;
#1757=CARTESIAN_POINT ( 'NONE',  ( 4.658376882426285448, 1.807244876408566681, 0.1260263862136162261 ) ) ;
#1758=CARTESIAN_POINT ( 'NONE',  ( 5.032410968829077014, 0.5625187028349203366, 1.831241071522809127 ) ) ;
#1760=CARTESIAN_POINT ( 'NONE',  ( 3.696128747971284323, -1.969148060776576337, -0.09815990810512796594 ) ) ;
#1761=CARTESIAN_POINT ( 'NONE',  ( 5.330866702616011921, 0.1386157390740362649, 1.865562100978317206 ) ) ;
#1762=CARTESIAN_POINT ( 'NONE',  ( 4.844130899818556379, -0.8777628995196519179, 1.641066814073613767 ) ) ;
#1765=CARTESIAN_POINT ( 'NONE',  ( 4.891328792415849058, 1.312644105602623457, 1.187316208720709421 ) ) ;
#1766=CARTESIAN_POINT ( 'NONE',  ( 0.05782782957228919940, 1.164991625563294386, 1.645756161228327130 ) ) ;
#1768=CARTESIAN_POINT ( 'NONE',  ( 1.489043601129129701, -0.3103829872296200443, -2.082944856911663312 ) ) ;
#1773=CARTESIAN_POINT ( 'NONE',  ( 3.181995841446764839, 2.068044944583770306, -0.4684364081647199307 ) ) ;
#1775=CARTESIAN_POINT ( 'NONE',  ( 1.511979465466501527, -0.6765842426028411127, 1.903255196800458071 ) ) ;
#1777=CARTESIAN_POINT ( 'NONE',  ( 6.720655732516641834, 2.102516797890502165, 2.037305422295607293 ) ) ;
#1780=CARTESIAN_POINT ( 'NONE',  ( 2.548304106926166490, 2.161049004374314464, 0.05582717182670697553 ) ) ;
#1781=CARTESIAN_POINT ( 'NONE',  ( 6.620655732516649294, 0.5971256128398574337, 1.879834161342401666 ) ) ;
#1788=CARTESIAN_POINT ( 'NONE',  ( 0.6795420635867071013, 1.475991390215245058, 1.620154534501851096 ) ) ;
#1790=CARTESIAN_POINT ( 'NONE',  ( 1.692605830730309791, -2.251738780704269249, -0.2206997258237669290 ) ) ;
#1797=CARTESIAN_POINT ( 'NONE',  ( 4.125434265850294047, -1.649698657028845883, 0.5036723037128154612 ) ) ;
#1799=CARTESIAN_POINT ( 'NONE',  ( 2.706023412207391843, -0.6731984680253579878, -1.636901589742848051 ) ) ;
#1800=CARTESIAN_POINT ( 'NONE',  ( 5.579209114504255496, -0.04897750150410771358, -2.206396493298476980 ) ) ;
#1803=CARTESIAN_POINT ( 'NONE',  ( 5.554314605481814660, -1.277030258849481736, 1.560512323070535112 ) ) ;
#1805=CARTESIAN_POINT ( 'NONE',  ( 2.412791964582483129, 1.669947582624079274, 0.8431454209596804805 ) ) ;
#1806=CARTESIAN_POINT ( 'NONE',  ( 2.166927730644189420, 1.536898783757352005, -1.387270004372019416 ) ) ;
#1808=CARTESIAN_POINT ( 'NONE',  ( 1.951281838316549777, -1.706683157587106425, 0.8630329916254894096 ) ) ;
#1813=CARTESIAN_POINT ( 'NONE',  ( 6.411931881972196610E-05, -0.8997486769052507327, 1.687471195204979457 ) ) ;
#1816=CARTESIAN_POINT ( 'NONE',  ( 1.398799877119625501, 0.3793605821263335565, 1.924665094374561791 ) ) ;
#1817=CARTESIAN_POINT ( 'NONE',  ( 0.3333609138582178111, -1.319029705771988858, 1.524807370920200356 ) ) ;
#1819=CARTESIAN_POINT ( 'NONE',  ( 5.783468009189684622, 0.1541500780414573613, -2.115021274163720211 ) ) ;
#1822=CARTESIAN_POINT ( 'NONE',  ( 6.134049847598044281, 0.9739642658876453973, -1.713909437456696105 ) ) ;
#1824=CARTESIAN_POINT ( 'NONE',  ( 1.459241111239812705, -1.698469834904120290, 1.080578982646386743 ) ) ;
#1827=CARTESIAN_POINT ( 'NONE',  ( 1.318125747981816698, 1.040119728068724880, -1.844044674895953806 ) ) ;
#1829=CARTESIAN_POINT ( 'NONE',  ( 2.137250951388528275, -0.09934309608320915363, -2.068088366144354318 ) ) ;
#1833=CARTESIAN_POINT ( 'NONE',  ( 4.189459526602421491, -0.8002100119003925371, 1.931633446273020693 ) ) ;
#1835=CARTESIAN_POINT ( 'NONE',  ( 3.786012796616508247, -0.9002957760516903107, 1.588078298607284111 ) ) ;
#1836=CARTESIAN_POINT ( 'NONE',  ( 2.314858244453772862, 1.454059926310177220, -1.080092325806664144 ) ) ;
#1841=CARTESIAN_POINT ( 'NONE',  ( 5.614374367772542840, -0.9875226594672005254, -1.973556357105679337 ) ) ;
#1844=CARTESIAN_POINT ( 'NONE',  ( 3.633378786761193968, -0.1378984027537045187, 1.907353237798288470 ) ) ;
#1850=CARTESIAN_POINT ( 'NONE',  ( 0.8371598888798935656, 0.7463826720714298313, -1.683355135116318069 ) ) ;
#1853=CARTESIAN_POINT ( 'NONE',  ( 3.954256261376987602, 0.6707706173689140794, 1.746330409709492937 ) ) ;
#1859=CARTESIAN_POINT ( 'NONE',  ( 6.385608392048681026, -1.951384585020640383, 0.6918703269920488674 ) ) ;
#1860=CARTESIAN_POINT ( 'NONE',  ( 2.583611426500437069, -0.6298568260672477992, 1.915607262459443794 ) ) ;
#1863=CARTESIAN_POINT ( 'NONE',  ( 2.343918204863020271, 2.190988169473460090, 0.05230688499441307066 ) ) ;
#1864=CARTESIAN_POINT ( 'NONE',  ( 6.094357461763900474, -1.817385979143220087, -0.1739998769475573914 ) ) ;
#1872=CARTESIAN_POINT ( 'NONE',  ( 3.579498943475650563, -0.9044721095569520086, 1.603693017070174864 ) ) ;
#1873=CARTESIAN_POINT ( 'NONE',  ( 1.172521868268823875, 0.8179054604866965450, 1.839630344048637678 ) ) ;
#1874=CARTESIAN_POINT ( 'NONE',  ( 2.618911895557019420, 0.6142130902007210125, -2.214721005821191024 ) ) ;
#1876=CARTESIAN_POINT ( 'NONE',  ( 1.481066496106745234, -0.05241980694788496431, 1.860401082089859770 ) ) ;
#1880=CARTESIAN_POINT ( 'NONE',  ( 4.552931727387078631, 0.3324577288378940954, 1.883125075537089854 ) ) ;
#1884=CARTESIAN_POINT ( 'NONE',  ( 3.667594231577479658, 1.163246697351211223, 1.737046641446901463 ) ) ;
#1885=CARTESIAN_POINT ( 'NONE',  ( 2.201827603038747139, -1.870314503716500099, 0.04339327950253490246 ) ) ;
#1888=CARTESIAN_POINT ( 'NONE',  ( 3.069568678616676927, -1.034394858748697743, 1.399543075413912430 ) ) ;
#1892=CARTESIAN_POINT ( 'NONE',  ( 4.142953665201137170, -1.499297852604332348, 0.8526725997853346062 ) ) ;
#1894=CARTESIAN_POINT ( 'NONE',  ( 6.498651167236064730, -0.5841124237929047336, -2.128106146270396071 ) ) ;
#1897=CARTESIAN_POINT ( 'NONE',  ( 3.116274269780743733, 2.161009848182334991, -0.2084346501036362376 ) ) ;
#1898=CARTESIAN_POINT ( 'NONE',  ( 3.773894676421325478, 1.015518775504126614, 1.516979517045339509 ) ) ;
#1899=CARTESIAN_POINT ( 'NONE',  ( 0.2682999959267086676, -0.8333247372044672030, -1.774235371720728649 ) ) ;
#1900=CARTESIAN_POINT ( 'NONE',  ( 5.665271214873143890, 1.955333520279872506, -0.8127364881663766694 ) ) ;
#1903=CARTESIAN_POINT ( 'NONE',  ( 5.671479170183292950, 1.362789248821870025, 1.843150307845689229 ) ) ;
#1906=CARTESIAN_POINT ( 'NONE',  ( 1.084817099560590803, -1.342388549496125627, 1.641497191572589776 ) ) ;
#1911=CARTESIAN_POINT ( 'NONE',  ( 6.174718801439761151, 1.464035886807094844, -1.603313688547292726 ) ) ;
#1915=CARTESIAN_POINT ( 'NONE',  ( 1.155278206730834256, 0.4382352071879510036, 2.177490050429623736 ) ) ;
#1917=CARTESIAN_POINT ( 'NONE',  ( 5.924453975591452703, -1.462443569488897754, -1.388487997949397368 ) ) ;
#1919=CARTESIAN_POINT ( 'NONE',  ( 3.995030872118944032, 0.2978362323166737213, 2.040820773513659425 ) ) ;
#1925=CARTESIAN_POINT ( 'NONE',  ( 0.5157159539815784344, -1.120044586405210207, -1.765097889335610404 ) ) ;
#1926=CARTESIAN_POINT ( 'NONE',  ( 4.342422763466713853, 0.4390309838058319425, -1.967887491402267486 ) ) ;
#1927=CARTESIAN_POINT ( 'NONE',  ( 3.931074656914943954, -1.272613488525012659, -1.330884258478791438 ) ) ;
#1930=CARTESIAN_POINT ( 'NONE',  ( 0.3930057192131968802, 1.272852841813755687, 1.164116782529129868 ) ) ;
#1934=CARTESIAN_POINT ( 'NONE',  ( 0.8610526709191126393, -1.638059776709074322, 1.560773681941391100 ) ) ;
#1935=CARTESIAN_POINT ( 'NONE',  ( 3.141344390434357869, -1.857286833677756599, 0.9929794709265575836 ) ) ;
#1939=CARTESIAN_POINT ( 'NONE',  ( 6.093750000000004441, -1.895863743164213355, -0.7852924748296624680 ) ) ;
#1943=CARTESIAN_POINT ( 'NONE',  ( 5.221006152755099272, 1.681885564164938840, -1.451226649161361015 ) ) ;
#1944=CARTESIAN_POINT ( 'NONE',  ( 3.732539452256115275, 0.3211115598316104935, 2.167677955659273348 ) ) ;
#1948=CARTESIAN_POINT ( 'NONE',  ( 6.609999999999985221, 3.681232580627872952, 2.794007784547379192 ) ) ;
#1951=CARTESIAN_POINT ( 'NONE',  ( 4.887034483293543730, -1.997634423138573867, -0.7120497732875651353 ) ) ;
#1955=CARTESIAN_POINT ( 'NONE',  ( 6.121977807712331909, -1.196819783530624015, -1.799967629666970881 ) ) ;
#1957=CARTESIAN_POINT ( 'NONE',  ( 6.321814700078944860, 1.054209175812788502, -1.509406368332133930 ) ) ;
#1959=CARTESIAN_POINT ( 'NONE',  ( 1.030331162470259354, -1.574104619921200765, 0.7428470239391560259 ) ) ;
#1963=CARTESIAN_POINT ( 'NONE',  ( 5.049776242366147194, 0.6816224847111511664, -2.051488706027407183 ) ) ;
#1966=CARTESIAN_POINT ( 'NONE',  ( 4.557600102482579629, 0.4766696971462945909, -2.108333899287537339 ) ) ;
#1968=CARTESIAN_POINT ( 'NONE',  ( 6.485619883616900339, 1.357675630217811014, 1.429558606944077326 ) ) ;
#1969=CARTESIAN_POINT ( 'NONE',  ( 4.604694260812782325, 0.7408162341489711311, -1.567766963475358599 ) ) ;
#1971=CARTESIAN_POINT ( 'NONE',  ( 1.575987392057216940, -1.168677030305173004, 1.853764812240476623 ) ) ;
#1972=CARTESIAN_POINT ( 'NONE',  ( 2.345130104517737291, 0.5056967325399002178, 2.251352274652190122 ) ) ;
#1973=CARTESIAN_POINT ( 'NONE',  ( 4.323548078123999439, -1.973147536489193499, 0.5946332991794788247 ) ) ;
#1974=CARTESIAN_POINT ( 'NONE',  ( 6.480031042553710208, -1.905489079494159910, -0.3742900760800580984 ) ) ;
#1980=CARTESIAN_POINT ( 'NONE',  ( 1.776017750421728270, 1.753029812786778940, -0.9963028777105964462 ) ) ;
#1982=CARTESIAN_POINT ( 'NONE',  ( 3.926972183325681875, 2.094573593246536802, 0.6948772193901550098 ) ) ;
#1984=CARTESIAN_POINT ( 'NONE',  ( 1.815070623055618615, -1.592837743320011601, -0.9620759905232498799 ) ) ;
#1985=FACE_OUTER_BOUND ( 'NONE', #56986, .T. ) ;
#1989=CARTESIAN_POINT ( 'NONE',  ( 6.925078400183531713, 7.629137130509035636, 2.644348168701659674 ) ) ;
#1992=CARTESIAN_POINT ( 'NONE',  ( 3.836836124264888959, 0.3005266716369097701, 2.038723765318616099 ) ) ;
#1995=CARTESIAN_POINT ( 'NONE',  ( 2.244791279253912197, 1.959548689066059168, 0.4886446307589187854 ) ) ;
#1998=CARTESIAN_POINT ( 'NONE',  ( 1.991158371866567967, 1.793705239296649045, -1.014668517943543513 ) ) ;
#2002=CARTESIAN_POINT ( 'NONE',  ( -0.1409997244345879974, 6.947781918643359589, -2.595319453918026653 ) ) ;
#2003=CARTESIAN_POINT ( 'NONE',  ( 0.3218710511002781383, 1.760991339961643920, 0.5373333866721883290 ) ) ;
#2004=CARTESIAN_POINT ( 'NONE',  ( 5.725267921653402148, -0.05769419298589681389, 2.206291853148376170 ) ) ;
#2006=CARTESIAN_POINT ( 'NONE',  ( 1.616726252867954683, 1.452999108549270169, -1.600537328674697779 ) ) ;
#2008=CARTESIAN_POINT ( 'NONE',  ( 2.272673044126482189, -0.3494851828299732621, -1.985868527484459634 ) ) ;
#2009=CARTESIAN_POINT ( 'NONE',  ( 2.302535375473542700, -2.053259096611260937, 1.032894330136547856 ) ) ;
#2011=CARTESIAN_POINT ( 'NONE',  ( 0.4966798268824790252, 1.557709316500059726, -1.035497600327957235 ) ) ;
#2012=CARTESIAN_POINT ( 'NONE',  ( 4.715676653857135747, -1.933614719187324082, 0.3836508851736331605 ) ) ;
#2013=CARTESIAN_POINT ( 'NONE',  ( 3.837125247982266174, -1.679222704393277921, -1.116210984008485507 ) ) ;
#2017=CARTESIAN_POINT ( 'NONE',  ( 4.723321587070372196, -0.1039652108096918437, 2.103624988570974352 ) ) ;
#2018=CARTESIAN_POINT ( 'NONE',  ( 5.846161131210033446, -0.9342735719010831774, 1.847668428805064655 ) ) ;
#2022=CARTESIAN_POINT ( 'NONE',  ( 5.273696820376614802, 0.3899264243738297941, -1.981607871481812833 ) ) ;
#2024=CARTESIAN_POINT ( 'NONE',  ( 0.7431262955939599291, -0.2488486719821168813, -2.047412193126110225 ) ) ;
#2030=( LENGTH_UNIT ( ) NAMED_UNIT ( * ) SI_UNIT ( .MILLI., .METRE. ) );
#2032=CARTESIAN_POINT ( 'NONE',  ( 3.192005314569335894, -1.456082124923337995, -1.610717807342199048 ) ) ;
#2034=CARTESIAN_POINT ( 'NONE',  ( 3.491602800004707241, -1.839307750763185645, -0.08696504193297231733 ) ) ;
#2036=CARTESIAN_POINT ( 'NONE',  ( 4.159861740090546434, 1.033864333764370702, 1.932389678422803181 ) ) ;
#2038=CARTESIAN_POINT ( 'NONE',  ( 4.750980993940300046, -1.819980134924009452, 1.343945550547174239 ) ) ;
#2044=CARTESIAN_POINT ( 'NONE',  ( 6.415310830085463323, -0.2139434178000785558, 1.756706237510232915 ) ) ;
#2045=CARTESIAN_POINT ( 'NONE',  ( 4.424480750451430744, -0.8629065238535367222, -1.818916818396177026 ) ) ;
#2047=CARTESIAN_POINT ( 'NONE',  ( 3.012826026228847098, 1.526343371991075948, -1.451234828553144673 ) ) ;
#2048=CARTESIAN_POINT ( 'NONE',  ( 0.9135317552573400945, -1.216341065326152160, -1.479849217926126004 ) ) ;
#2051=CARTESIAN_POINT ( 'NONE',  ( 2.594150448275188481, 0.9308562254837976502, -1.735710503097695145 ) ) ;
#2052=CARTESIAN_POINT ( 'NONE',  ( 0.4263524580605422276, 1.788790299270696993, 0.5473224044415525569 ) ) ;
#2053=CARTESIAN_POINT ( 'NONE',  ( 1.117545225965112188, 0.3861695934333775337, -1.923310697798483293 ) ) ;
#2054=CARTESIAN_POINT ( 'NONE',  ( 0.1231139863388103495, 1.664874722635242277, 0.9407772870168448209 ) ) ;
#2060=CARTESIAN_POINT ( 'NONE',  ( 5.752782329262379868, -1.473788443143897453, 1.151991621687727507 ) ) ;
#2063=CARTESIAN_POINT ( 'NONE',  ( 5.735237735067807208, -0.04509738862551111033, -2.069921269439451539 ) ) ;
#2066=CARTESIAN_POINT ( 'NONE',  ( 0.3267351109269465148, -1.353470794461093973, 1.566751113397255812 ) ) ;
#2074=CARTESIAN_POINT ( 'NONE',  ( 5.635196431686764207, -0.04651148872366302894, -1.961470878453225763 ) ) ;
#2076=CARTESIAN_POINT ( 'NONE',  ( 2.794295885581669747, -1.882186412485300719, 0.7230279869864173481 ) ) ;
#2077=CARTESIAN_POINT ( 'NONE',  ( 2.114329361022151854, 1.859220375642420819, 0.4613663794279678765 ) ) ;
#2079=CARTESIAN_POINT ( 'NONE',  ( 0.1170720436180875679, -0.1011795954627830590, 2.189343785608413917 ) ) ;
#2080=CARTESIAN_POINT ( 'NONE',  ( 0.2331713839410576583, 0.005725554726919174046, -1.953566683266183102 ) ) ;
#2081=CARTESIAN_POINT ( 'NONE',  ( 2.794054307841778328, -1.865266697571520194, -0.1415833504254116748 ) ) ;
#2085=CARTESIAN_POINT ( 'NONE',  ( 4.780926590999498238, 1.759528625808198354, -1.177310133890494548 ) ) ;
#2087=CARTESIAN_POINT ( 'NONE',  ( 6.039524589772497620, 1.914416561877980261, -0.7887839105886890190 ) ) ;
#2088=CARTESIAN_POINT ( 'NONE',  ( 1.997712292880989837, -2.090220067774691159, 0.05436529341687650757 ) ) ;
#2089=CARTESIAN_POINT ( 'NONE',  ( 6.620655732516651071, 4.689394895873098434, 2.736297475404291024 ) ) ;
#2090=CARTESIAN_POINT ( 'NONE',  ( 0.7797844759148920835, -0.9637546898726162548, 1.430169641563599159 ) ) ;
#2100=CARTESIAN_POINT ( 'NONE',  ( 0.2932429122153769052, 1.690905606409907058, -0.6502662643994570058 ) ) ;
#2110=CARTESIAN_POINT ( 'NONE',  ( 0.7025736824820059123, 1.770395976773591284, 0.7320947492839694482 ) ) ;
#2111=CARTESIAN_POINT ( 'NONE',  ( 0.2410938523699951708, 2.030451451530786766, 0.6113826261911478044 ) ) ;
#2113=CARTESIAN_POINT ( 'NONE',  ( -0.1399997263889594112, -0.002789056014654289761, -2.000146600338557956 ) ) ;
#2117=CARTESIAN_POINT ( 'NONE',  ( 3.045709290742618425, 1.389371873615535602, 1.396104611999344769 ) ) ;
#2118=CARTESIAN_POINT ( 'NONE',  ( 0.9969211937387794098, -2.069638562867767373, -0.4609060192823294932 ) ) ;
#2122=CARTESIAN_POINT ( 'NONE',  ( 6.421842908546859796, 1.265077015623069512, -1.789241164368003290 ) ) ;
#2124=CARTESIAN_POINT ( 'NONE',  ( 3.768508550381458821, -1.294476758928708060, 1.426794059921440594 ) ) ;
#2126=CARTESIAN_POINT ( 'NONE',  ( -0.2411972340275866378, -0.002466136893032525382, -1.900252416837118874 ) ) ;
#2127=CARTESIAN_POINT ( 'NONE',  ( 0.7157882511714327434, -0.3199875008889854766, 2.183444778895065941 ) ) ;
#2132=CARTESIAN_POINT ( 'NONE',  ( 6.332857179708399009, -1.868906791504289844, -0.6213115537570863545 ) ) ;
#2133=CARTESIAN_POINT ( 'NONE',  ( 6.614805131849967879, -0.1256686391097518729, 1.812046779126045726 ) ) ;
#2134=CARTESIAN_POINT ( 'NONE',  ( 6.257181701683109942, -2.286357481388684221, -0.2351346485395827413 ) ) ;
#2136=CARTESIAN_POINT ( 'NONE',  ( 4.416758307032777608, -1.381121683685157642, 1.247472197611438016 ) ) ;
#2142=CARTESIAN_POINT ( 'NONE',  ( -0.1232117409455633916, -0.1621322592461546530, -2.156395338765437764 ) ) ;
#2147=CARTESIAN_POINT ( 'NONE',  ( 0.2932112110246976044, 1.350478442433366677, 1.228755397233910696 ) ) ;
#2150=CARTESIAN_POINT ( 'NONE',  ( 2.865509578329272777, -0.1299577181766899403, -1.729349861900606022 ) ) ;
#2151=CARTESIAN_POINT ( 'NONE',  ( 6.508999999999982577, 2.977730662443831111, 2.353651457310241835 ) ) ;
#2153=CARTESIAN_POINT ( 'NONE',  ( 0.01214912391013078102, -0.8215866570660257384, -1.740624652096602221 ) ) ;
#2154=CARTESIAN_POINT ( 'NONE',  ( 3.994932754639446859, 0.2835094185691371393, 1.941019531709553103 ) ) ;
#2157=CARTESIAN_POINT ( 'NONE',  ( 5.285831659486547984, 2.043504495962459977, -0.5658664308652374686 ) ) ;
#2161=CARTESIAN_POINT ( 'NONE',  ( 3.239188805615275335, -0.1476314317495740769, -2.065021578984991724 ) ) ;
#2163=CARTESIAN_POINT ( 'NONE',  ( 5.145291483242067088, 0.1622298597842904699, 2.215448774714718461 ) ) ;
#2165=CARTESIAN_POINT ( 'NONE',  ( 2.954051123917677213, -2.124883583899921824, -0.8772644825643919342 ) ) ;
#2175=CARTESIAN_POINT ( 'NONE',  ( 4.429883728109570207, -1.874397765517330061, 0.3784635845696313061 ) ) ;
#2177=CARTESIAN_POINT ( 'NONE',  ( 4.875862107049974803, 0.9950566627994448243, 1.408581599115072747 ) ) ;
#2178=CARTESIAN_POINT ( 'NONE',  ( 3.925017756809038527, -1.752140073516525565, 0.9981236898717813499 ) ) ;
#2179=CARTESIAN_POINT ( 'NONE',  ( 5.485083606918717436, -2.298851034700015727, -0.002838145216723860897 ) ) ;
#2181=CARTESIAN_POINT ( 'NONE',  ( 6.375619162920919791, 2.015872221316476143, -0.6097100970045774559 ) ) ;
#2183=CARTESIAN_POINT ( 'NONE',  ( 6.327411112729964593, -1.665570200489007169, 0.5986406977509810545 ) ) ;
#2186=CARTESIAN_POINT ( 'NONE',  ( 2.062813984423640612, -2.096776522422974409, -0.9266714075790563054 ) ) ;
#2187=CARTESIAN_POINT ( 'NONE',  ( 6.597600327481837112, -1.840612352326329804, 0.05063316525460298534 ) ) ;
#2193=CARTESIAN_POINT ( 'NONE',  ( 6.865700769154306826, -0.4580177224273937475, 2.026514595051785772 ) ) ;
#2194=CARTESIAN_POINT ( 'NONE',  ( 1.762908039156896978, -0.1037823317905466058, -2.014007988105172231 ) ) ;
#2196=CARTESIAN_POINT ( 'NONE',  ( 5.004483369110711344, -0.6506757832731756563, -1.813419023564779353 ) ) ;
#2198=CARTESIAN_POINT ( 'NONE',  ( 1.951734608585634190, -1.981729029064113856, 1.003908989668365948 ) ) ;
#2206=CARTESIAN_POINT ( 'NONE',  ( 4.036439982160089812, -1.511860617216064684, 0.8620873645008280128 ) ) ;
#2207=CARTESIAN_POINT ( 'NONE',  ( 2.541395235131336694, 1.794889867694851260, -0.7924082849640816661 ) ) ;
#2213=CARTESIAN_POINT ( 'NONE',  ( 1.469262158920743966, 1.818092299969736425, 0.9742969159239748267 ) ) ;
#2217=CARTESIAN_POINT ( 'NONE',  ( 1.481717434351536244, 2.089849803356018221, -0.8673477522002839279 ) ) ;
#2220=CARTESIAN_POINT ( 'NONE',  ( 3.022558680773678397, 1.760047114015901526, 0.6337009143728977723 ) ) ;
#2221=CARTESIAN_POINT ( 'NONE',  ( 0.8790820841908916217, -0.4200629052855206491, -1.682323782590444461 ) ) ;
#2222=CARTESIAN_POINT ( 'NONE',  ( 5.741772062182810998, 2.188963553168365994, 0.1087695542012837302 ) ) ;
#2223=CARTESIAN_POINT ( 'NONE',  ( 5.772612788190349953, -1.469667252935745960, 1.779063562929294129 ) ) ;
#2224=CARTESIAN_POINT ( 'NONE',  ( 1.780222679459046997, -1.103320402871512673, 1.740482491890801287 ) ) ;
#2225=CARTESIAN_POINT ( 'NONE',  ( 3.697155016903285407, -0.5626119583077812125, 1.858668453590556213 ) ) ;
#2227=CARTESIAN_POINT ( 'NONE',  ( 5.782452155351484713, -1.824793809246130438, -0.4103911052399379367 ) ) ;
#2228=CARTESIAN_POINT ( 'NONE',  ( 1.937500000000002220, 1.451031289061040841, -1.451031289061198049 ) ) ;
#2230=CARTESIAN_POINT ( 'NONE',  ( 0.2625146791020065984, -1.733275965524210482, -0.05152637578398518159 ) ) ;
#2233=CARTESIAN_POINT ( 'NONE',  ( 4.500625067706437221, -1.976956227568788638, 0.3961002554062897918 ) ) ;
#2237=CARTESIAN_POINT ( 'NONE',  ( 1.769861954154128725, 0.9373860217288846330, 1.566528536362868707 ) ) ;
#2247=CARTESIAN_POINT ( 'NONE',  ( 5.303380940763749329, 1.780254367526274972, -0.9538449857209270188 ) ) ;
#2248=CARTESIAN_POINT ( 'NONE',  ( 0.3465379015402513252, 1.086389676674501148, -1.820904993421072371 ) ) ;
#2252=CARTESIAN_POINT ( 'NONE',  ( 4.873930702218094879, 1.184903577025652188, 1.686001177547257424 ) ) ;
#2253=CARTESIAN_POINT ( 'NONE',  ( 5.027970288326707227, -1.728003250605243180, 1.038991650911202713 ) ) ;
#2261=CARTESIAN_POINT ( 'NONE',  ( 4.833361152654930493, -1.319026006086077230, 1.524810761284051575 ) ) ;
#2262=CARTESIAN_POINT ( 'NONE',  ( 4.329911453333429527, 1.806054511993939515, 0.3568155486674411958 ) ) ;
#2264=CARTESIAN_POINT ( 'NONE',  ( 1.823324434984688214, 2.154351390505971686, 0.8276274939288345012 ) ) ;
#2266=CARTESIAN_POINT ( 'NONE',  ( 5.307972821619873827, -2.151738229465068653, 0.2060058040841972193 ) ) ;
#2268=CARTESIAN_POINT ( 'NONE',  ( 0.3802858058059845336, -0.2390265653847540028, -1.927249604900363122 ) ) ;
#2273=CARTESIAN_POINT ( 'NONE',  ( 3.590566789841375339, -0.3639703897368729568, -1.834726254853453087 ) ) ;
#2274=CARTESIAN_POINT ( 'NONE',  ( 0.08795244648929222142, 1.102731429460445334, 1.562230693318837238 ) ) ;
#2277=CARTESIAN_POINT ( 'NONE',  ( 2.403190426070573871, 1.771669130372434564, -1.315670724662293178 ) ) ;
#2278=CARTESIAN_POINT ( 'NONE',  ( 6.720655732516647163, -0.001531948155462499201, 2.073773125298985054 ) ) ;
#2283=CARTESIAN_POINT ( 'NONE',  ( 0.3683541893860732275, -1.290952873633111953, 1.489922359098810878 ) ) ;
#2284=CARTESIAN_POINT ( 'NONE',  ( 0.1129635547038260190, -0.9897495874401724958, -2.082026327295583012 ) ) ;
#2285=CARTESIAN_POINT ( 'NONE',  ( 1.961309178647975715, 1.629323162926434199, 1.092499269706406428 ) ) ;
#2286=CARTESIAN_POINT ( 'NONE',  ( 3.801677422522796945, -1.558724286948458548, -1.350822056805228266 ) ) ;
#2294=CARTESIAN_POINT ( 'NONE',  ( 0.2511275705787468504, -0.4786951167374750571, -2.125832126681607370 ) ) ;
#2296=CARTESIAN_POINT ( 'NONE',  ( 6.497600353373155002, -1.840680978339729545, 0.05264081064878384231 ) ) ;
#2300=CARTESIAN_POINT ( 'NONE',  ( 0.9482695043977107385, 0.5371953702461745861, 1.791772314883005146 ) ) ;
#2306=CARTESIAN_POINT ( 'NONE',  ( 0.7504700684401002242, 1.884043224930329385, 0.3264296256808990049 ) ) ;
#2307=CARTESIAN_POINT ( 'NONE',  ( 2.817004693338585941, -0.1753839976894235320, 1.761133515796961868 ) ) ;
#2308=CARTESIAN_POINT ( 'NONE',  ( 0.2055213853429035953, 1.417038256915002181, 1.284265443176696442 ) ) ;
#2310=CARTESIAN_POINT ( 'NONE',  ( 4.710494965788769584, 1.834319554003289721, 0.5521488281355608763 ) ) ;
#2311=CARTESIAN_POINT ( 'NONE',  ( -0.1409997244346075651, 7.629137130509101361, -2.600278764091648487 ) ) ;
#2312=CARTESIAN_POINT ( 'NONE',  ( 5.371531009330141160, -0.2907324665500017891, 1.947856185699713638 ) ) ;
#2313=CARTESIAN_POINT ( 'NONE',  ( 0.5277791401020451856, -0.3051165123582540994, 2.098401203810342786 ) ) ;
#2316=CARTESIAN_POINT ( 'NONE',  ( 4.223419137798128276, -1.790188510885984297, 0.5427707113358354318 ) ) ;
#2317=CARTESIAN_POINT ( 'NONE',  ( 0.7151340513122245168, -0.2707656271505008982, 1.805370379145049275 ) ) ;
#2319=CARTESIAN_POINT ( 'NONE',  ( 3.053566222061272040, -1.804402116661915967, -1.270350324234905903 ) ) ;
#2322=CARTESIAN_POINT ( 'NONE',  ( 1.100133984900531825, 0.8377775336174065890, -1.885062252648894265 ) ) ;
#2330=CARTESIAN_POINT ( 'NONE',  ( 3.578635096964689843, 1.315621898185691974, -1.598582974826658010 ) ) ;
#2332=CARTESIAN_POINT ( 'NONE',  ( 1.388190569347878212, -0.9732202972718406730, 1.930209198840258100 ) ) ;
#2334=CARTESIAN_POINT ( 'NONE',  ( 1.049479869930733944, -1.824965358647975489, 0.8655331567536515003 ) ) ;
#2339=CARTESIAN_POINT ( 'NONE',  ( 6.749375321999433908, -1.976647572034227140, -0.3960365597561604778 ) ) ;
#2340=CARTESIAN_POINT ( 'NONE',  ( 0.3918150239524306189, -2.006371095615328226, 0.2024682584410575914 ) ) ;
#2341=CARTESIAN_POINT ( 'NONE',  ( 6.539320575229230492, 2.428701779328062749, 2.485127258459709054 ) ) ;
#2342=CARTESIAN_POINT ( 'NONE',  ( 4.669572502782517454, 1.262004115398765780, 1.791526714441132873 ) ) ;
#2345=CARTESIAN_POINT ( 'NONE',  ( 3.146637304467227558, 1.866760668956708447, 0.4145885930168375921 ) ) ;
#2349=CARTESIAN_POINT ( 'NONE',  ( 1.528922965942226986, -1.701935853630029083, 1.081086586856384590 ) ) ;
#2351=CARTESIAN_POINT ( 'NONE',  ( 0.5391474206018737059, -1.962199071191613964, 1.185045521927590162 ) ) ;
#2353=CARTESIAN_POINT ( 'NONE',  ( 3.627714610788032701, -1.027129601966117134, -1.385419451709940519 ) ) ;
#2354=CARTESIAN_POINT ( 'NONE',  ( 0.1399997263885795207, 2.876830203203218694, -2.488333633689450597 ) ) ;
#2357=CARTESIAN_POINT ( 'NONE',  ( 1.767943819387544968, -1.947426213878332035, 0.2369139692007388165 ) ) ;
#2361=CARTESIAN_POINT ( 'NONE',  ( 0.1753634416057498202, 0.7014533214223102053, -2.226873008360684913 ) ) ;
#2365=CARTESIAN_POINT ( 'NONE',  ( 3.457467740999135231, -1.373635607365558453, -1.181027286383716124 ) ) ;
#2369=CARTESIAN_POINT ( 'NONE',  ( 4.986864056229866726, -1.707513420791425540, -0.6052512474536574372 ) ) ;
#2373=CARTESIAN_POINT ( 'NONE',  ( 5.810971417242416948, -1.466730511752023958, 1.145431029696217573 ) ) ;
#2375=CARTESIAN_POINT ( 'NONE',  ( 4.306187113567048641, 1.175507255964372222, -1.512451795395561405 ) ) ;
#2383=CARTESIAN_POINT ( 'NONE',  ( 0.4620835240300471547, 2.137967531602209981, -0.3185850937674692407 ) ) ;
#2386=CARTESIAN_POINT ( 'NONE',  ( 0.3053143536290473525, -0.4923201697357786344, 1.757875871163572024 ) ) ;
#2388=CARTESIAN_POINT ( 'NONE',  ( 3.241029684393876842, -1.610631872634618933, 0.8593927405577477252 ) ) ;
#2391=CARTESIAN_POINT ( 'NONE',  ( 2.523828315609038864, 1.932092998399935091, -0.3813574256018251729 ) ) ;
#2392=CARTESIAN_POINT ( 'NONE',  ( 4.019036194231017767, -1.857530068489420705, 0.5666795103562488611 ) ) ;
#2395=CARTESIAN_POINT ( 'NONE',  ( 4.430007776716601953, -2.079114408633813582, 0.4165480963118637914 ) ) ;
#2403=CARTESIAN_POINT ( 'NONE',  ( 5.391160240453525709, 1.608232483172780558, -0.8641324296934371763 ) ) ;
#2411=CARTESIAN_POINT ( 'NONE',  ( 6.086763352761943580, -0.2763008855245497331, -1.850001521387992565 ) ) ;
#2413=CARTESIAN_POINT ( 'NONE',  ( 3.563037003841040828, -1.699336121007990918, -0.9075540061579747686 ) ) ;
#2420=CARTESIAN_POINT ( 'NONE',  ( 0.7556430218940900501, 2.039295976802601995, -0.5688827987148316057 ) ) ;
#2423=CARTESIAN_POINT ( 'NONE',  ( 6.420769920452011448, -1.468259139554881409, 1.459777494992514857 ) ) ;
#2424=CARTESIAN_POINT ( 'NONE',  ( 1.593040506729075823, -0.6195558395927207584, 1.734028948791266345 ) ) ;
#2429=CARTESIAN_POINT ( 'NONE',  ( 1.553083273963658639, -1.967900166212281476, -1.175304309182874096 ) ) ;
#2433=CARTESIAN_POINT ( 'NONE',  ( 5.806574285656749268, 1.713600856677459205, 0.9136399477176879724 ) ) ;
#2437=CARTESIAN_POINT ( 'NONE',  ( 0.4045417950784445105, -1.998468379361338698, -0.2424310749817460697 ) ) ;
#2442=CARTESIAN_POINT ( 'NONE',  ( 3.978531085967525360, -0.2047937889433377179, -2.080580830362771305 ) ) ;
#2443=CARTESIAN_POINT ( 'NONE',  ( 2.535733614153494742, 0.8364609567749015095, -1.559706200981937352 ) ) ;
#2446=CARTESIAN_POINT ( 'NONE',  ( 5.648434673080700463, -1.810194131346474222, 1.406188067625735449 ) ) ;
#2447=CARTESIAN_POINT ( 'NONE',  ( 3.380519863291716387, 1.572804015177066805, -0.7453022471971497698 ) ) ;
#2449=CARTESIAN_POINT ( 'NONE',  ( 3.514723022282209897, 1.734034291474368494, 0.002059465714070173124 ) ) ;
#2450=CARTESIAN_POINT ( 'NONE',  ( 3.842362351650536301, -1.073271228610745309, 1.887301499758537116 ) ) ;
#2452=CARTESIAN_POINT ( 'NONE',  ( 4.610564714392807240, 1.931124171932835809, 0.5807562064495259690 ) ) ;
#2453=CARTESIAN_POINT ( 'NONE',  ( 1.250000000000001110, 7.216295638291068821E-14, 2.052068128417951609 ) ) ;
#2455=CARTESIAN_POINT ( 'NONE',  ( 1.764547866544708521, -1.364041108321904616, 1.360535031132574568 ) ) ;
#2457=CARTESIAN_POINT ( 'NONE',  ( 5.238630872344578471, 1.322862460432130849, -1.784462157271723859 ) ) ;
#2459=CARTESIAN_POINT ( 'NONE',  ( -0.2110808730067273986, 0.0005491059566040295322, -1.796958327270286704 ) ) ;
#2464=CARTESIAN_POINT ( 'NONE',  ( 0.5576789645300848086, -1.902086909048054331, 1.147088156025797057 ) ) ;
#2465=CARTESIAN_POINT ( 'NONE',  ( 5.687936657224680559, -1.243353266631580523, -1.517579924814119074 ) ) ;
#2468=CARTESIAN_POINT ( 'NONE',  ( 6.837213258907510749, -2.025504081721161143, 1.008097451810068268 ) ) ;
#2472=CARTESIAN_POINT ( 'NONE',  ( 3.912594259961211574, 0.7396031425229695477, 1.925699983396757409 ) ) ;
#2476=CARTESIAN_POINT ( 'NONE',  ( 6.169203917683822702, 0.1378038699498609632, -1.865550841118966297 ) ) ;
#2478=CARTESIAN_POINT ( 'NONE',  ( 4.324694450628805420, 0.7358571774197277815, -1.570421820497726051 ) ) ;
#2479=CARTESIAN_POINT ( 'NONE',  ( 4.739680933654325301, 1.736262504677583474, 0.1214163294094624396 ) ) ;
#2481=CARTESIAN_POINT ( 'NONE',  ( 2.279227788079383643, 2.094250403060330168, -0.9326617097511098464 ) ) ;
#2483=CARTESIAN_POINT ( 'NONE',  ( 5.513254163946260000, -2.039523011555996579, 0.4591751592910776614 ) ) ;
#2484=CARTESIAN_POINT ( 'NONE',  ( 0.09336763325077861164, -1.840659761701424646, -0.04852334659839750014 ) ) ;
#2487=CARTESIAN_POINT ( 'NONE',  ( 2.162732623366144136, 1.242727809108796322, 1.587836805404294171 ) ) ;
#2492=CARTESIAN_POINT ( 'NONE',  ( 2.895306150831237879, -0.1582170333116576511, -2.114654843180157950 ) ) ;
#2495=CARTESIAN_POINT ( 'NONE',  ( 5.127504350819418910, -1.732488751877172772, 0.5760870007271366999 ) ) ;
#2503=CARTESIAN_POINT ( 'NONE',  ( 2.812765223479243737, -0.5904890161391795900, -1.931511402468567340 ) ) ;
#2504=CARTESIAN_POINT ( 'NONE',  ( 6.774453055690137226, -1.363307072557031985, 1.735998097611628932 ) ) ;
#2506=CARTESIAN_POINT ( 'NONE',  ( 4.504654980070036174, 0.4933668235826896287, 1.794306199697106363 ) ) ;
#2509=EDGE_LOOP ( 'NONE', ( #47711, #94882 ) ) ;
#2515=CARTESIAN_POINT ( 'NONE',  ( 1.704000572024838123, -1.251590786289292101, -1.200144391261132482 ) ) ;
#2516=CARTESIAN_POINT ( 'NONE',  ( 1.411604581429444893, 1.170971978790593448, -1.287647580301202410 ) ) ;
#2517=CARTESIAN_POINT ( 'NONE',  ( 6.270204019816865149, 1.180490267363063062, 1.982795515311958079 ) ) ;
#2520=CARTESIAN_POINT ( 'NONE',  ( 1.862644954548669185, -1.459483730259679257, 1.455164547919563844 ) ) ;
#2522=CARTESIAN_POINT ( 'NONE',  ( 6.731773689652298387, -2.096994807688298934, -0.9412720059410217832 ) ) ;
#2525=CARTESIAN_POINT ( 'NONE',  ( 0.3914019522827461017, 1.459281966464224256, 1.325753552615087871 ) ) ;
#2527=CARTESIAN_POINT ( 'NONE',  ( 5.203337695038355193, 1.683698669361912259, -0.9069238330124268499 ) ) ;
#2529=CARTESIAN_POINT ( 'NONE',  ( 6.252570086353132162, 0.6882034672392455255, 2.096894461246688213 ) ) ;
#2533=CARTESIAN_POINT ( 'NONE',  ( 0.5748750247985534578, -1.461244816878112029, 1.394459567027491076 ) ) ;
#2535=CARTESIAN_POINT ( 'NONE',  ( 3.856711057068095805, 0.8274802039119494301, 2.154294293310366371 ) ) ;
#2536=CARTESIAN_POINT ( 'NONE',  ( 4.562918044398325712, 1.517878595006398212, -1.242988302126393441 ) ) ;
#2537=CARTESIAN_POINT ( 'NONE',  ( 0.9890223832832998330, 0.1386981244183866091, 1.956888703154149312 ) ) ;
#2541=CARTESIAN_POINT ( 'NONE',  ( 0.07561343334091479018, 1.573685453729951833, 1.416787448489342127 ) ) ;
#2544=CARTESIAN_POINT ( 'NONE',  ( 0.02305342982030639948, -1.130023889514218505, -1.454075609423427728 ) ) ;
#2545=CARTESIAN_POINT ( 'NONE',  ( 2.799877792657178066, -1.606015216909290277, -1.461049007858437054 ) ) ;
#2547=CARTESIAN_POINT ( 'NONE',  ( 0.1410940620840978044, 2.031152781523197337, 0.6094965309384676733 ) ) ;
#2553=CARTESIAN_POINT ( 'NONE',  ( 2.319669497725483254, -1.999663683883694532, 0.4976976026799494468 ) ) ;
#2560=CARTESIAN_POINT ( 'NONE',  ( 4.037688526304391345, -1.829018870347882242, 0.5580751363460645376 ) ) ;
#2565=CARTESIAN_POINT ( 'NONE',  ( 1.247787707462020723, -1.783668181329477465, -1.391623327695093115 ) ) ;
#2567=CARTESIAN_POINT ( 'NONE',  ( 1.142488074861398140, 1.746299531065167221, 0.4817477467682490522 ) ) ;
#2568=CARTESIAN_POINT ( 'NONE',  ( 1.305720528479116682, -1.067273574023764438, -1.590657944389769707 ) ) ;
#2569=CARTESIAN_POINT ( 'NONE',  ( 1.785682506433339478, -1.950172559450613852, 0.6955597780969878796 ) ) ;
#2573=CARTESIAN_POINT ( 'NONE',  ( 6.825078400183573812, 0.002648415797040087893, 1.855566311045192540 ) ) ;
#2574=CARTESIAN_POINT ( 'NONE',  ( 5.848256421918945236, 1.924412893870678820, 0.09223618542448899782 ) ) ;
#2575=CARTESIAN_POINT ( 'NONE',  ( 6.358075476802443227, 2.201304964888863402, -0.1578768562689457922 ) ) ;
#2578=CARTESIAN_POINT ( 'NONE',  ( 3.947761307511790552, 1.492003129663575622, 1.424497906600069363 ) ) ;
#2583=CARTESIAN_POINT ( 'NONE',  ( 5.333084004640892495, 0.1517067650670254342, 2.100546829335631749 ) ) ;
#2585=CARTESIAN_POINT ( 'NONE',  ( 0.5554291532160166023, 1.804893407318912901, -1.206520995182088329 ) ) ;
#2587=CARTESIAN_POINT ( 'NONE',  ( 4.604844690042745547, 1.674155836469687575, -1.367402732809947397 ) ) ;
#2588=CARTESIAN_POINT ( 'NONE',  ( 5.567059059060062154, -1.590727130084067964, 1.244318111769521229 ) ) ;
#2596=CARTESIAN_POINT ( 'NONE',  ( 3.046111529846948329, 0.9110102549910354952, 1.799122713138465279 ) ) ;
#2600=CARTESIAN_POINT ( 'NONE',  ( 5.049776242366147194, 0.6816224847111511664, -2.051488706027407183 ) ) ;
#2605=CARTESIAN_POINT ( 'NONE',  ( 4.569935513796226978, -0.9480243344661150040, 1.779636403143824985 ) ) ;
#2607=CARTESIAN_POINT ( 'NONE',  ( 0.4160739966224377140, 1.193427498895651029, -1.245624518738875697 ) ) ;
#2612=CARTESIAN_POINT ( 'NONE',  ( 5.026551685794930613, 1.789549103570491573, 0.5443708928771497924 ) ) ;
#2613=CARTESIAN_POINT ( 'NONE',  ( 0.04752084976851479736, -1.839644132637440865, 0.8178810061007844023 ) ) ;
#2617=CARTESIAN_POINT ( 'NONE',  ( 2.420699464796825850, -0.8139657014685426351, -1.958238820914718792 ) ) ;
#2618=CARTESIAN_POINT ( 'NONE',  ( 0.2105648349144396136, 1.930425396462841725, 0.5826343419270894053 ) ) ;
#2619=CARTESIAN_POINT ( 'NONE',  ( 1.142488074861398140, 1.746299531065167221, 0.4817477467682490522 ) ) ;
#2621=CARTESIAN_POINT ( 'NONE',  ( 5.963787895669663719, 2.130530397400759668, -0.3648857593604309391 ) ) ;
#2624=CARTESIAN_POINT ( 'NONE',  ( 0.8135319083415553099, -1.217954555017298324, -1.478650609923468195 ) ) ;
#2630=CARTESIAN_POINT ( 'NONE',  ( 3.854492016355787420, 0.7758605394001509836, 2.017853709245204463 ) ) ;
#2633=CARTESIAN_POINT ( 'NONE',  ( 1.090261293813089560, 1.267680250814690934, 1.699812782343253170 ) ) ;
#2634=CARTESIAN_POINT ( 'NONE',  ( 6.370122744524995717, 0.9412729668686821149, 1.564051812004362940 ) ) ;
#2636=CARTESIAN_POINT ( 'NONE',  ( 1.721884408201577399, -1.091793429770457458, -1.641225607529321229 ) ) ;
#2637=CARTESIAN_POINT ( 'NONE',  ( 4.939673314881130040, -1.814047719456039154, 0.6055163330952323397 ) ) ;
#2638=VERTEX_POINT ( 'NONE', #191324 ) ;
#2640=CARTESIAN_POINT ( 'NONE',  ( 6.602011381505620946, 0.7551138498248446407, -1.819252348156335852 ) ) ;
#2641=CARTESIAN_POINT ( 'NONE',  ( 2.027192386733965179, -1.268372964689370663, -1.470586975900304516 ) ) ;
#2648=CARTESIAN_POINT ( 'NONE',  ( 4.951771945676144426, -1.355037094400749487, -1.349591858340569717 ) ) ;
#2650=CARTESIAN_POINT ( 'NONE',  ( 3.668774463136436736, -1.482526648764719734, 1.634931011441637771 ) ) ;
#2651=CARTESIAN_POINT ( 'NONE',  ( 1.589210545419886378, -0.3244246349418925535, -2.182665228674217861 ) ) ;
#2653=CARTESIAN_POINT ( 'NONE',  ( 0.3813228709106940006, 0.1872568833237615027, -1.903067810102520241 ) ) ;
#2654=CARTESIAN_POINT ( 'NONE',  ( 0.07661050522431848975, 5.726661425590173771, -2.304854160881860903 ) ) ;
#2657=CARTESIAN_POINT ( 'NONE',  ( 3.508316276398337319, 2.070544812355082254, 0.002818362966339192730 ) ) ;
#2662=CARTESIAN_POINT ( 'NONE',  ( 1.112450467520700537, -0.9725818059473789745, -1.930612204972524282 ) ) ;
#2663=CARTESIAN_POINT ( 'NONE',  ( 3.755584314896889264, 2.174856280799509545, -0.2696606696684644700 ) ) ;
#2670=CARTESIAN_POINT ( 'NONE',  ( 6.135404405475363809, 0.5537102809010217008, 1.643457313873160741 ) ) ;
#2673=CARTESIAN_POINT ( 'NONE',  ( 3.502843950909264592, 0.4983820457637299639, 2.009271733256080772 ) ) ;
#2674=CARTESIAN_POINT ( 'NONE',  ( 4.359064374566766986, -0.001685027751544953406, -2.117403152337670846 ) ) ;
#2677=CARTESIAN_POINT ( 'NONE',  ( 3.116014175596728109, 1.960399024780419275, -0.1881816519722582237 ) ) ;
#2678=CARTESIAN_POINT ( 'NONE',  ( 1.160255710619631397, 1.910328232974867868, 0.09094507755665059978 ) ) ;
#2679=CARTESIAN_POINT ( 'NONE',  ( 4.980587577705724911, -0.2770739538935252932, -2.275404589957805701 ) ) ;
#2680=CARTESIAN_POINT ( 'NONE',  ( 3.000428103051573814, -0.5303778429210231904, -1.746945217264872507 ) ) ;
#2685=CARTESIAN_POINT ( 'NONE',  ( 4.394793396725252599, -1.953840400094335905, -0.4849018877997012256 ) ) ;
#2686=CARTESIAN_POINT ( 'NONE',  ( 4.276187414114787089, -1.004825795036960567, -1.684713053385626269 ) ) ;
#2689=CARTESIAN_POINT ( 'NONE',  ( 0.1755611466353629579, -0.002217706044341584935, -2.244164702216360219 ) ) ;
#2691=CARTESIAN_POINT ( 'NONE',  ( 0.7672655991019157184, 2.013871065616902989, -0.5614242917610365868 ) ) ;
#2692=CARTESIAN_POINT ( 'NONE',  ( 6.104346055523492964, -0.6409971714030155976, -1.649885601521252410 ) ) ;
#2694=CARTESIAN_POINT ( 'NONE',  ( 2.133021248740565756, -1.956732443736847182, 0.9868821405488172882 ) ) ;
#2695=CARTESIAN_POINT ( 'NONE',  ( 6.597592293924691376, -1.739768381213904647, 0.05089061930978015791 ) ) ;
#2697=CARTESIAN_POINT ( 'NONE',  ( 0.2333690889706925564, 0.2409277441041447754, -2.087868073146467829 ) ) ;
#2698=CARTESIAN_POINT ( 'NONE',  ( 0.1172359533097135365, -1.692718506494130359, 0.3305547394890032686 ) ) ;
#2699=CARTESIAN_POINT ( 'NONE',  ( 0.6503308509665306492, -0.2843267121918050533, -2.280655268134044622 ) ) ;
#2700=CARTESIAN_POINT ( 'NONE',  ( 0.9256184737543894370, -1.394389637717853514, -1.690728713229103342 ) ) ;
#2701=CARTESIAN_POINT ( 'NONE',  ( 2.596532132193625664, -2.201043451360765957, -0.1612727490639675743 ) ) ;
#2702=CARTESIAN_POINT ( 'NONE',  ( 6.496539221175353873, 2.146586416477539672, 0.3252249059467678394 ) ) ;
#2704=CARTESIAN_POINT ( 'NONE',  ( 0.9017390913304748068, -2.064370131783893392, 0.4699791444322827250 ) ) ;
#2705=CARTESIAN_POINT ( 'NONE',  ( 6.727182134110196721, 7.051813866762763006, 2.787205683092201181 ) ) ;
#2706=CARTESIAN_POINT ( 'NONE',  ( 5.579104889113781773, -0.04751220352695872257, -1.925958990430853612 ) ) ;
#2707=ORIENTED_EDGE ( 'NONE', *, *, #46793, .T. ) ;
#2708=CARTESIAN_POINT ( 'NONE',  ( 1.259778491951433654, 2.257442302724984806, -0.3979086512072607107 ) ) ;
#2713=CARTESIAN_POINT ( 'NONE',  ( 5.321006124507968060, 1.683121437214535554, -1.449644825538060733 ) ) ;
#2720=CARTESIAN_POINT ( 'NONE',  ( 2.303361484738715159, 1.314996338066702242, -1.528741580717301263 ) ) ;
#2722=CARTESIAN_POINT ( 'NONE',  ( 0.7255239074139888666, 0.2060675592777498066, -2.052282084198739920 ) ) ;
#2727=CARTESIAN_POINT ( 'NONE',  ( 3.996163734398257894, -0.6867376513691285655, -2.081127982183433645 ) ) ;
#2728=CARTESIAN_POINT ( 'NONE',  ( 1.178361531996233280, 1.528742360773158282, 1.314995429398260196 ) ) ;
#2729=CARTESIAN_POINT ( 'NONE',  ( 0.9777802892061361328, -1.796362506263927017, -0.4033719513514141264 ) ) ;
#2731=CARTESIAN_POINT ( 'NONE',  ( 5.407889476941767803, -1.028354611087534787, -2.048866343328694661 ) ) ;
#2732=CARTESIAN_POINT ( 'NONE',  ( 2.853255899669316697, 1.832232481769331844, -0.1808706098178694266 ) ) ;
#2735=CARTESIAN_POINT ( 'NONE',  ( 4.471595891589618788, 1.770651423122941548, -0.4439726157009425411 ) ) ;
#2736=CARTESIAN_POINT ( 'NONE',  ( 4.869767617671093340, -0.2496050341583149201, -2.000857388266870984 ) ) ;
#2738=CARTESIAN_POINT ( 'NONE',  ( 4.504895162230450723, 1.751659092587343869, -1.432031112679124085 ) ) ;
#2740=CARTESIAN_POINT ( 'NONE',  ( 6.422895033429510292, 1.963595603779586973, 0.7616278367365038049 ) ) ;
#2742=CARTESIAN_POINT ( 'NONE',  ( 3.156751980976373329, -0.5984545454679365273, -1.982000093670479135 ) ) ;
#2747=CARTESIAN_POINT ( 'NONE',  ( 1.611812915071403784, -1.911997954552616008, 0.2354761707349817823 ) ) ;
#2749=CARTESIAN_POINT ( 'NONE',  ( 6.930521655090660538, -1.214226768402311363, 1.551031149239000761 ) ) ;
#2755=CARTESIAN_POINT ( 'NONE',  ( 1.811064542976594360, -0.5979718353220222493, -2.139333889645285147 ) ) ;
#2756=CARTESIAN_POINT ( 'NONE',  ( 3.786240212431398966, -1.039621666623831597, 1.831390154885542243 ) ) ;
#2759=CARTESIAN_POINT ( 'NONE',  ( 6.895359103435129811, -1.662453150013998515, 0.8363214020891978073 ) ) ;
#2764=CARTESIAN_POINT ( 'NONE',  ( 0.9672155168029163974, -1.668165459610539081, 1.309123814877902969 ) ) ;
#2767=CARTESIAN_POINT ( 'NONE',  ( 4.070719198475009293, 1.388998261151509039, -1.385754695631277844 ) ) ;
#2768=CARTESIAN_POINT ( 'NONE',  ( 3.415052781332720055, 1.953485055394106107, 0.9259690932504063277 ) ) ;
#2769=CARTESIAN_POINT ( 'NONE',  ( 1.628196140939692338, 0.1813696128579282696, 1.832309401408799276 ) ) ;
#2772=CARTESIAN_POINT ( 'NONE',  ( 4.681465254972009049, -0.8165918992961908041, 1.536851246062352905 ) ) ;
#2777=CARTESIAN_POINT ( 'NONE',  ( 1.850665834824256173, 0.6780317805383448970, 2.052694239800388676 ) ) ;
#2778=CARTESIAN_POINT ( 'NONE',  ( 3.304064382408095302, -1.779354530013575131, 0.9478943420064069869 ) ) ;
#2780=CARTESIAN_POINT ( 'NONE',  ( 1.745224485312408813, -1.826185749030174499, 1.156423465944363294 ) ) ;
#2781=CARTESIAN_POINT ( 'NONE',  ( 3.063307058708428787, 0.2908816738307045680, -1.949781715572605600 ) ) ;
#2782=CARTESIAN_POINT ( 'NONE',  ( 6.609000000000011532, 3.695567819995113634, 2.514302272609474809 ) ) ;
#2783=CARTESIAN_POINT ( 'NONE',  ( 3.526839302598220982, -1.793260235690095072, 0.7459913709994684394 ) ) ;
#2793=CARTESIAN_POINT ( 'NONE',  ( 0.3060867131535297547, -0.5861141839358529060, 2.127432003918772629 ) ) ;
#2795=CARTESIAN_POINT ( 'NONE',  ( 4.469553177461598636, -0.3394721387663233170, 1.932013773527320843 ) ) ;
#2796=CARTESIAN_POINT ( 'NONE',  ( 1.178361531996233280, 1.528742360773158060, 1.314995429398259974 ) ) ;
#2798=CARTESIAN_POINT ( 'NONE',  ( 3.380171168471556520, -2.115091482053657934, -0.09962960183704583361 ) ) ;
#2800=CARTESIAN_POINT ( 'NONE',  ( 0.07479286986305544449, 6.948552162806721277, -2.450557996216149892 ) ) ;
#2802=CARTESIAN_POINT ( 'NONE',  ( 2.624749632297512569, -1.717891791495285592, 0.6627527109525217508 ) ) ;
#2806=CARTESIAN_POINT ( 'NONE',  ( 5.308877466510794285, -0.5174029350529658622, -2.056363676157816123 ) ) ;
#2807=CARTESIAN_POINT ( 'NONE',  ( 6.925078400183548588, 0.0006614011395407459748, 1.855452278108092656 ) ) ;
#2809=CARTESIAN_POINT ( 'NONE',  ( 5.571578285044489043, 1.987195396197571462, -0.5455906853745869922 ) ) ;
#2810=CARTESIAN_POINT ( 'NONE',  ( 1.064655064206044166, 1.412561167129450457, -1.211817338188374782 ) ) ;
#2811=CARTESIAN_POINT ( 'NONE',  ( 2.946635061770470632, -1.506786691049965432, -1.057933238436038925 ) ) ;
#2816=CARTESIAN_POINT ( 'NONE',  ( 1.946200625105892312, 0.8427435547867198062, -2.039832142532324255 ) ) ;
#2817=CARTESIAN_POINT ( 'NONE',  ( 4.868612525405347391, -1.482742447731852709, 1.708856814797095725 ) ) ;
#2820=CARTESIAN_POINT ( 'NONE',  ( 4.886864132303106345, -1.708302746381512804, -0.6034029335190493892 ) ) ;
#2821=CARTESIAN_POINT ( 'NONE',  ( 4.258935762849770157, -0.005977556496831581273, -1.915903398800692159 ) ) ;
#2824=CARTESIAN_POINT ( 'NONE',  ( 3.994965595081632959, 1.666078911148192843, -1.053691615683423510 ) ) ;
#2825=CARTESIAN_POINT ( 'NONE',  ( 5.541831131927607679, 0.7570117910807551143, -1.710825945835430462 ) ) ;
#2826=CARTESIAN_POINT ( 'NONE',  ( 5.248444859377932481, -1.846993913715170077, -0.2278608691909170259 ) ) ;
#2830=CARTESIAN_POINT ( 'NONE',  ( 0.4972802279516430612, -0.2910764605805628014, 1.995268990643041640 ) ) ;
#2832=CARTESIAN_POINT ( 'NONE',  ( 1.207801281821162975, -0.5101631384078918474, 2.043215687033891559 ) ) ;
#2836=CARTESIAN_POINT ( 'NONE',  ( 2.865608904542978674, -1.736054085904148669, -1.217558864107195715 ) ) ;
#2838=CARTESIAN_POINT ( 'NONE',  ( 1.371359653073561891, -1.734546099648653472, -1.034550878434212784 ) ) ;
#2843=CARTESIAN_POINT ( 'NONE',  ( 2.460438939752377152, 0.9218109643280818499, 1.955300211207489758 ) ) ;
#2844=CARTESIAN_POINT ( 'NONE',  ( 6.890000000000047642, 4.686644152421160392, 2.842524626796953946 ) ) ;
#2851=CARTESIAN_POINT ( 'NONE',  ( 0.8377433530848135135, 0.8832496248250313320, -2.005872107257236969 ) ) ;
#2853=CARTESIAN_POINT ( 'NONE',  ( 1.147787885906520033, -1.784999543274916611, -1.390116309797536864 ) ) ;
#2860=CARTESIAN_POINT ( 'NONE',  ( 4.072648179469573471, -1.610461668677556801, -0.6182406629154230115 ) ) ;
#2862=CARTESIAN_POINT ( 'NONE',  ( 2.143481220494340533, 0.6824282661134513095, -1.633078482676100007 ) ) ;
#2863=CARTESIAN_POINT ( 'NONE',  ( 2.965492324039080252, -1.647071928310759326, -1.157207142784054010 ) ) ;
#2864=CARTESIAN_POINT ( 'NONE',  ( 5.772568991252683190, -1.404203161598962968, 1.702366421003978392 ) ) ;
#2866=CARTESIAN_POINT ( 'NONE',  ( 4.605726162909654420, 1.499404818428259345, 1.353488595782571524 ) ) ;
#2868=CARTESIAN_POINT ( 'NONE',  ( 5.712517600013327979, 1.944077172375497264, 0.5350714256760412679 ) ) ;
#2869=CARTESIAN_POINT ( 'NONE',  ( 4.763805435907580765, 0.5614848394812530508, -1.722472548925155778 ) ) ;
#2871=CARTESIAN_POINT ( 'NONE',  ( 2.817106861211693847, -0.1851908181382568019, 1.861470920997858380 ) ) ;
#2873=CARTESIAN_POINT ( 'NONE',  ( 2.056764645581514728, 0.4224895836346024280, 1.864965418913032913 ) ) ;
#2878=CARTESIAN_POINT ( 'NONE',  ( 0.01762790050853849447, -0.5081247445114078776, 1.843608005305336528 ) ) ;
#2880=CARTESIAN_POINT ( 'NONE',  ( 1.240593047436115759, -1.913272810121857237, -0.4332019784048374289 ) ) ;
#2883=CARTESIAN_POINT ( 'NONE',  ( 5.273731010124149243, 0.4114677744767555878, -2.080124947408354963 ) ) ;
#2886=CARTESIAN_POINT ( 'NONE',  ( 5.694591516259816188, -0.4762896487527890632, -1.912855984147985744 ) ) ;
#2888=CARTESIAN_POINT ( 'NONE',  ( 0.3342400628787962624, -1.080556536492575770, -1.698484060877824886 ) ) ;
#2890=CARTESIAN_POINT ( 'NONE',  ( 1.335737955381975928, 0.6106153762303926369, -2.027287256620951439 ) ) ;
#2892=CARTESIAN_POINT ( 'NONE',  ( 2.963400493335893948, 1.747644659881589568, 1.109742091278065113 ) ) ;
#2896=CARTESIAN_POINT ( 'NONE',  ( 4.628904841183094199, -1.911603206638176511, 0.8469096376574613005 ) ) ;
#2898=CARTESIAN_POINT ( 'NONE',  ( 3.610199614654508338, -0.7391254383575728282, -1.669438027971142047 ) ) ;
#2899=CARTESIAN_POINT ( 'NONE',  ( 2.508236654460756387, -1.806733793710820324, -0.1315605372460958433 ) ) ;
#2905=CARTESIAN_POINT ( 'NONE',  ( 4.981566806912655743, 2.060606067865732527, -0.7902562557115796471 ) ) ;
#2908=CARTESIAN_POINT ( 'NONE',  ( 3.580628178849315280, -1.282259035790348722, 1.418852674340838060 ) ) ;
#2911=CARTESIAN_POINT ( 'NONE',  ( 6.602015318333181781, 0.7961593463888805289, -1.911361562896146671 ) ) ;
#2919=CARTESIAN_POINT ( 'NONE',  ( 3.831198023013999698, -1.729401117988647707, 0.7132991360168300377 ) ) ;
#2922=( BOUNDED_CURVE ( )  B_SPLINE_CURVE ( 3, ( #143401, #28547, #44819, #156418 ),
 .UNSPECIFIED., .F., .T. ) 
 B_SPLINE_CURVE_WITH_KNOTS ( ( 4, 4 ),
 ( 0.000000000000000000, 0.4999999999999970579 ),
 .UNSPECIFIED. ) 
 CURVE ( )  GEOMETRIC_REPRESENTATION_ITEM ( )  RATIONAL_B_SPLINE_CURVE ( ( 1.000000000000000222, 0.3333333333333373671, 0.3333333333333334259, 0.9999999999999963363 ) ) 
 REPRESENTATION_ITEM ( '' )  );
#2926=CARTESIAN_POINT ( 'NONE',  ( 6.930528400284448054, -1.278709912597691511, 1.628784411136071197 ) ) ;
#2928=CARTESIAN_POINT ( 'NONE',  ( 1.159780049612362030, 1.203373692603469935, 1.617804775344060308 ) ) ;
#2932=CARTESIAN_POINT ( 'NONE',  ( 0.9729166594223404019, -0.05710519180573449260, -2.190871861337650994 ) ) ;
#2933=CARTESIAN_POINT ( 'NONE',  ( 6.234959169399230561, 0.1841439077357870380, 1.816378869960999509 ) ) ;
#2940=CARTESIAN_POINT ( 'NONE',  ( 3.720104550828434942, 1.749555917645674530, 0.5740644926693627692 ) ) ;
#2941=CARTESIAN_POINT ( 'NONE',  ( 0.1529896150729666005, 0.3463191217260193633, 1.982936507005612414 ) ) ;
#2942=CARTESIAN_POINT ( 'NONE',  ( 2.513387927098627905, 2.297807174607501057, 0.05796762653747893068 ) ) ;
#2944=CARTESIAN_POINT ( 'NONE',  ( 0.4790722831046652641, -0.09921120595577682943, 1.858460205838560864 ) ) ;
#2948=CARTESIAN_POINT ( 'NONE',  ( 4.324404969281474109, -0.8226261416362996570, -1.726585468271451651 ) ) ;
#2951=ADVANCED_FACE ( 'NONE', ( #43763 ), #141285, .T. ) ;
#2953=CARTESIAN_POINT ( 'NONE',  ( 3.773056988009905410, 1.967892522216899476, -0.7064651350525589235 ) ) ;
#2954=CARTESIAN_POINT ( 'NONE',  ( 2.184254540302111636, -1.834043650784190405, -0.3674020703766100460 ) ) ;
#2957=CARTESIAN_POINT ( 'NONE',  ( 3.632115859802576008, 0.2593814109021801984, 1.720877339435398667 ) ) ;
#2961=CARTESIAN_POINT ( 'NONE',  ( 3.914446297384760243, 1.218041307117226690, -1.221573883832317575 ) ) ;
#2963=CARTESIAN_POINT ( 'NONE',  ( 3.650093349144762023, 0.7902683543556283663, 2.044282924279612779 ) ) ;
#2964=CARTESIAN_POINT ( 'NONE',  ( 6.674453038267287752, -1.361800985140369402, 1.737325302230605883 ) ) ;
#2967=CARTESIAN_POINT ( 'NONE',  ( 3.625983508040203862, 2.119313185944927902, -0.4706255054970372997 ) ) ;
#2968=CARTESIAN_POINT ( 'NONE',  ( 2.490611698265518648, -0.3118145247060916114, -1.798701865878708839 ) ) ;
#2971=CARTESIAN_POINT ( 'NONE',  ( 6.051990796818580876, 1.090527953092842894, 1.814802726937503330 ) ) ;
#2973=CARTESIAN_POINT ( 'NONE',  ( 5.407889476941767803, -1.028354611087534787, -2.048866343328694661 ) ) ;
#2975=CARTESIAN_POINT ( 'NONE',  ( 6.720655732516650716, 1.307757891114844417, 1.844004982043083940 ) ) ;
#2977=CARTESIAN_POINT ( 'NONE',  ( 1.893382502257603850, -0.1070854039621378373, -2.117916637519041689 ) ) ;
#2983=CARTESIAN_POINT ( 'NONE',  ( 6.883263157960362477, 2.445608615952394871, 2.336423753955836791 ) ) ;
#2986=CARTESIAN_POINT ( 'NONE',  ( 6.065077313367789102, -1.076319894221990259, 1.704936797084610101 ) ) ;
#2988=CARTESIAN_POINT ( 'NONE',  ( 4.891499300893256574, -1.887858789894794054, 0.8311416006015391877 ) ) ;
#2990=CARTESIAN_POINT ( 'NONE',  ( -0.2409995289980246258, 7.629137130509076492, -2.600476469121239198 ) ) ;
#2993=CARTESIAN_POINT ( 'NONE',  ( 0.3047781727255130524, 1.820093451774043691, 1.028452505696121344 ) ) ;
#2994=CARTESIAN_POINT ( 'NONE',  ( 5.027970288326706338, -1.728003250605243180, 1.038991650911202713 ) ) ;
#2995=CARTESIAN_POINT ( 'NONE',  ( 4.423293856316495187, -1.136390847421838490, -1.448631019334602144 ) ) ;
#2997=CARTESIAN_POINT ( 'NONE',  ( 0.8852880119799062530, 1.153610147808200370, 1.282378885572494465 ) ) ;
#2998=CARTESIAN_POINT ( 'NONE',  ( 0.1281391398850126040, 2.011452084832816123, 0.1435147193784985509 ) ) ;
#2999=CARTESIAN_POINT ( 'NONE',  ( 1.178858319146030009, 1.745148694481736484, 1.496268366688303653 ) ) ;
#3001=CARTESIAN_POINT ( 'NONE',  ( 1.054439146255849780, 2.259743442402757818, -0.1116689827955052033 ) ) ;
#3002=CARTESIAN_POINT ( 'NONE',  ( 3.053452221204506323, -1.721964003836244039, -1.212301904834027333 ) ) ;
#3010=CARTESIAN_POINT ( 'NONE',  ( 4.974942202162922378, -1.608427002576447995, 1.532403895573146491 ) ) ;
#3011=CARTESIAN_POINT ( 'NONE',  ( 2.994263412949604852, -0.6367403190770392074, -2.096898073876966251 ) ) ;
#3015=CARTESIAN_POINT ( 'NONE',  ( 5.072687121480487171, 1.354251660176824856, -1.419695456575476689 ) ) ;
#3018=CARTESIAN_POINT ( 'NONE',  ( 6.609999999999973674, -0.005249217919313375023, 2.280159464062641916 ) ) ;
#3020=CARTESIAN_POINT ( 'NONE',  ( 4.535463010148616192, -0.1012041512906610846, 2.118281909017679432 ) ) ;
#3024=CARTESIAN_POINT ( 'NONE',  ( 6.754756207809571755, -1.674487575904315406, 1.366813541845832924 ) ) ;
#3026=CARTESIAN_POINT ( 'NONE',  ( 5.425302022954732628, -1.172690680311109901, -1.419496581506813904 ) ) ;
#3029=CARTESIAN_POINT ( 'NONE',  ( 1.012787145881738793, -1.698268246007793802, 0.3799501884491280901 ) ) ;
#3033=CARTESIAN_POINT ( 'NONE',  ( 5.647404790089923132, -1.701416311724871067, -1.333359258283283166 ) ) ;
#3037=CARTESIAN_POINT ( 'NONE',  ( 4.241217004700631676, -1.882188537963986219, 1.063020064016991117 ) ) ;
#3039=CARTESIAN_POINT ( 'NONE',  ( 4.323478126428228485, -1.887445700180546915, 0.5691147572158322676 ) ) ;
#3040=CARTESIAN_POINT ( 'NONE',  ( 4.463993690379265189, 1.392342236284923152, 1.032948281618131903 ) ) ;
#3041=CARTESIAN_POINT ( 'NONE',  ( 0.8025787753177977546, 1.655945718051672566, -1.435626523826734280 ) ) ;
#3042=CARTESIAN_POINT ( 'NONE',  ( 2.081525663035548757, -0.1140690627178981842, -2.304871973535598251 ) ) ;
#3043=CARTESIAN_POINT ( 'NONE',  ( 5.202442474109128412, -0.6904536177961515531, -1.941828258638809368 ) ) ;
#3044=CARTESIAN_POINT ( 'NONE',  ( 0.4099697989727095204, 1.339763683568921504, -1.405998798013205819 ) ) ;
#3049=CARTESIAN_POINT ( 'NONE',  ( 0.9850002542920628379, -2.016597020373378513, 0.002813405579435435122 ) ) ;
#3051=CARTESIAN_POINT ( 'NONE',  ( 3.839080194659278966, 0.3211572903306300075, 2.183152695405643051 ) ) ;
#3053=CARTESIAN_POINT ( 'NONE',  ( 0.9536794021071954841, -0.6768100219149524310, 1.733691362649824264 ) ) ;
#3057=CARTESIAN_POINT ( 'NONE',  ( 6.925078400183569904, 6.033938712579569597, 2.739235483740619426 ) ) ;
#3058=CARTESIAN_POINT ( 'NONE',  ( 6.087831982560696353, -1.832735460234231617, -0.1757473516527594259 ) ) ;
#3060=CARTESIAN_POINT ( 'NONE',  ( 3.555589940775650604, 0.5024415226424256975, -1.998565159594118068 ) ) ;
#3063=CARTESIAN_POINT ( 'NONE',  ( 2.139325021376851765, 0.002241307429765720949, 2.019862492052142855 ) ) ;
#3066=CARTESIAN_POINT ( 'NONE',  ( 2.008734545381769543, 1.527802914727709016, -1.383344190003793495 ) ) ;
#3067=CARTESIAN_POINT ( 'NONE',  ( 6.883263157960362477, -0.004191378316371896506, 2.053658919477070910 ) ) ;
#3070=CARTESIAN_POINT ( 'NONE',  ( -0.1411974294641838990, 5.723166529328228336, -2.494358352568406545 ) ) ;
#3071=CARTESIAN_POINT ( 'NONE',  ( 5.496761087669068679, -0.5331231007881258588, -2.141394884921154151 ) ) ;
#3072=CARTESIAN_POINT ( 'NONE',  ( 1.546389740860309781, 2.159050155192781872, 0.1077149563947499555 ) ) ;
#3075=CARTESIAN_POINT ( 'NONE',  ( 1.780482797753998092, -0.5424726148271253878, -1.942096288550937411 ) ) ;
#3076=CARTESIAN_POINT ( 'NONE',  ( 2.179500908114082591, -1.083194949601238521, -2.027108130913716444 ) ) ;
#3081=CARTESIAN_POINT ( 'NONE',  ( 1.832664747978371533, 0.1804508633567840359, 1.861920966532565336 ) ) ;
#3082=CARTESIAN_POINT ( 'NONE',  ( 3.063685658700274761, 1.282989771343697294, 1.555699169480361022 ) ) ;
#3084=CARTESIAN_POINT ( 'NONE',  ( 6.639320575229257670, 2.957073754255258535, 2.555924021811271540 ) ) ;
#3086=CARTESIAN_POINT ( 'NONE',  ( 5.162764661449575243, -1.526107291725445236, 1.451632374922463553 ) ) ;
#3090=CARTESIAN_POINT ( 'NONE',  ( 5.238538122511118722, 1.199862898965612823, -1.624631798562142793 ) ) ;
#3093=CARTESIAN_POINT ( 'NONE',  ( 1.270463096138880088, -0.9239429406890822261, -1.844087381150324001 ) ) ;
#3100=CARTESIAN_POINT ( 'NONE',  ( 3.104148162264197985, 0.7838245717375692534, -2.024915708489416044 ) ) ;
#3103=CARTESIAN_POINT ( 'NONE',  ( 1.874305484616908934, -0.09156810461483089192, -1.839108553062768214 ) ) ;
#3105=CARTESIAN_POINT ( 'NONE',  ( 4.441096743985088580, -1.694418930461354611, -1.389946530008886905 ) ) ;
#3106=CARTESIAN_POINT ( 'NONE',  ( 6.883263157960369583, 7.629137130509070275, 2.653810918356712900 ) ) ;
#3107=CARTESIAN_POINT ( 'NONE',  ( 4.909165057579100377, 1.966063467186284663, 1.119528758242648525 ) ) ;
#3114=CARTESIAN_POINT ( 'NONE',  ( 5.747242073547443653, -1.395821259116083013, -1.087781934379092874 ) ) ;
#3116=CARTESIAN_POINT ( 'NONE',  ( 3.229155175764964802, 1.820814436659716096, 0.8588418517583608081 ) ) ;
#3118=CARTESIAN_POINT ( 'NONE',  ( 2.256984296129550760, -1.628445616851754263, 1.335386477757320778 ) ) ;
#3122=CARTESIAN_POINT ( 'NONE',  ( 1.486696478045932635, 1.897211281248304848, 0.5285659569534242319 ) ) ;
#3123=CARTESIAN_POINT ( 'NONE',  ( 0.6373110600932235803, -1.319858442276698129, -1.325903642019378381 ) ) ;
#3124=CARTESIAN_POINT ( 'NONE',  ( 0.7835587076311965049, -1.864072139945194717, 0.6119401183290391621 ) ) ;
#3125=CARTESIAN_POINT ( 'NONE',  ( 5.713115418873079498, 1.475880075617709730, -1.050242514106846992 ) ) ;
#3129=CARTESIAN_POINT ( 'NONE',  ( 5.647288160985431738, -1.475499438119257878, -1.149758287351684949 ) ) ;
#3132=CARTESIAN_POINT ( 'NONE',  ( 5.032118066406459533, 1.187563481491529682, 1.695602288408842417 ) ) ;
#3135=CARTESIAN_POINT ( 'NONE',  ( 0.3091450132529197647, -1.663722454078466306, 1.232067777400827069 ) ) ;
#3142=EDGE_CURVE ( 'NONE', #106915, #35846, #25835, .T. ) ;
#3144=CARTESIAN_POINT ( 'NONE',  ( 5.107842384611220865, 0.6171798735227496113, -1.862306164846748491 ) ) ;
#3146=CARTESIAN_POINT ( 'NONE',  ( 3.128279665134887644, 0.2985813455266342342, -1.993766061640166232 ) ) ;
#3147=CARTESIAN_POINT ( 'NONE',  ( 2.624132809847005365, 1.901796678110598382, 0.2296932149444090299 ) ) ;
#3148=CARTESIAN_POINT ( 'NONE',  ( 0.8201894534925309177, 1.301127354658284663, -1.763390660798454634 ) ) ;
#3150=CARTESIAN_POINT ( 'NONE',  ( 3.708139779478221598, -0.7553879706188313392, -1.711406342686023541 ) ) ;
#3154=CARTESIAN_POINT ( 'NONE',  ( 4.130539392780770314, 0.5663510459464686786, 2.039993263092474418 ) ) ;
#3156=CARTESIAN_POINT ( 'NONE',  ( 5.881320641815353412, -0.05461762546566179682, 2.069818975884097689 ) ) ;
#3157=CARTESIAN_POINT ( 'NONE',  ( 0.6969597590469852610, 1.711416582936477804, 1.200673393543179479 ) ) ;
#3158=CARTESIAN_POINT ( 'NONE',  ( 6.620655732516679493, 7.051632961313193171, 2.871890384929445261 ) ) ;
#3159=CARTESIAN_POINT ( 'NONE',  ( 6.633835642106551411, -1.195214757176918496, -1.380038946949893486 ) ) ;
#3168=CARTESIAN_POINT ( 'NONE',  ( 0.01197859805690624189, -1.811022649853447630, -0.04676520365421397291 ) ) ;
#3177=CARTESIAN_POINT ( 'NONE',  ( 6.573846656420020196, -0.8593871168269312522, 1.822298249534954673 ) ) ;
#3178=CARTESIAN_POINT ( 'NONE',  ( 0.9090200710941964690, -0.5189423241485704441, -2.055877189782874481 ) ) ;
#3180=CARTESIAN_POINT ( 'NONE',  ( 0.1405533004714799583, 1.991423289015941345, -2.694406653617386294 ) ) ;
#3184=CARTESIAN_POINT ( 'NONE',  ( 3.748844217038479698, -0.3797678475170936929, -1.932296744971262692 ) ) ;
#3185=CARTESIAN_POINT ( 'NONE',  ( 4.974232547167513729, -2.001514726140873890, -0.2440111082952014510 ) ) ;
#3189=CARTESIAN_POINT ( 'NONE',  ( 4.857479518068650748, 2.167902099161696849, -0.3196092617779102696 ) ) ;
#3191=CARTESIAN_POINT ( 'NONE',  ( 4.278288924157873652, -1.109688035731031475, 1.574481611047764851 ) ) ;
#3193=CARTESIAN_POINT ( 'NONE',  ( -0.1296875068448125057, 1.390030859318210688, -2.083197486262199138 ) ) ;
#3194=CARTESIAN_POINT ( 'NONE',  ( 0.1331565106231606399, 5.723858289613107608, -2.539976893513963052 ) ) ;
#3200=CARTESIAN_POINT ( 'NONE',  ( 5.594576842560746499, 1.939643975919752572, 0.3403973628498639936 ) ) ;
#3201=CARTESIAN_POINT ( 'NONE',  ( 0.3099700162084629285, 1.338387961458173070, -1.407469107711552425 ) ) ;
#3202=CARTESIAN_POINT ( 'NONE',  ( 4.160795161724285762, 0.5389290103979550439, 1.939535095694967959 ) ) ;
#3203=CARTESIAN_POINT ( 'NONE',  ( 6.011119390975155241, 2.295276066174879670, 0.1220560631845988148 ) ) ;
#3205=CARTESIAN_POINT ( 'NONE',  ( 4.698021595848828724, 0.7982989760673472324, -1.681190670221676120 ) ) ;
#3212=CARTESIAN_POINT ( 'NONE',  ( 0.7322823680011962821, 2.160084099745246178, 0.3691886501416344335 ) ) ;
#3218=CARTESIAN_POINT ( 'NONE',  ( 0.5744775230259161480, -1.718042477583326066, -0.6180270036199516648 ) ) ;
#3220=CARTESIAN_POINT ( 'NONE',  ( 2.777623227853244003, 1.486122661887591123, -0.8934276201044144550 ) ) ;
#3222=CARTESIAN_POINT ( 'NONE',  ( 6.509000000000021657, 1.267728212239338959, 2.115804336118334295 ) ) ;
#3224=CARTESIAN_POINT ( 'NONE',  ( 5.250558533952181861, 0.5335417292645014964, 1.745990657226546894 ) ) ;
#3225=CARTESIAN_POINT ( 'NONE',  ( 3.590630163336411051, 1.912927474663427496, 0.4342120235502828218 ) ) ;
#3230=MECHANICAL_DESIGN_GEOMETRIC_PRESENTATION_REPRESENTATION('',(#89724),#203779);
#3231=CARTESIAN_POINT ( 'NONE',  ( 4.635462950926918957, -0.1032030737609032217, 2.118083805499561656 ) ) ;
#3235=CARTESIAN_POINT ( 'NONE',  ( 3.291909242638372923, -1.386922682245657734, -1.537212927083357217 ) ) ;
#3238=CARTESIAN_POINT ( 'NONE',  ( 4.301594116137519741, 1.984124119141786657, -0.9988866673766303439 ) ) ;
#3240=CARTESIAN_POINT ( 'NONE',  ( 3.006738235175490548, -2.214768494356106121, 0.6152039052057678425 ) ) ;
#3246=CARTESIAN_POINT ( 'NONE',  ( 3.357576282340120066, -1.451192137084562628, -1.245647637661301044 ) ) ;
#3248=CARTESIAN_POINT ( 'NONE',  ( 4.383650571098846704, 1.127723038421009738, 1.305118705121767420 ) ) ;
#3249=CARTESIAN_POINT ( 'NONE',  ( 3.134000194803722383, 2.016708403948695771, -0.004836970814638129855 ) ) ;
#3250=CARTESIAN_POINT ( 'NONE',  ( 4.483195000112350392, -2.298113444969139607, -0.05724751674645797012 ) ) ;
#3252=CARTESIAN_POINT ( 'NONE',  ( 6.586557477600968546, -2.065026496990796101, -0.4128237726619687353 ) ) ;
#3255=CARTESIAN_POINT ( 'NONE',  ( 4.393649985211129483, -0.6784793013954493190, 1.634714195790587077 ) ) ;
#3257=CARTESIAN_POINT ( 'NONE',  ( 0.7973255588549054140, 1.877056169618742443, 1.315483550797888812 ) ) ;
#3258=CARTESIAN_POINT ( 'NONE',  ( 6.369096972855497363, 1.760372669148374758, -0.5393517311068628528 ) ) ;
#3260=CARTESIAN_POINT ( 'NONE',  ( 6.544889499999918314, -1.757580744090202041, -1.308772488114395616 ) ) ;
#3264=CARTESIAN_POINT ( 'NONE',  ( 0.6433370543819162402, -0.2662039958584628829, -2.154713702345659510 ) ) ;
#3265=CARTESIAN_POINT ( 'NONE',  ( 1.130092623156966347, 2.014433208573155110, 0.09411304420373775570 ) ) ;
#3268=CARTESIAN_POINT ( 'NONE',  ( 5.549420396211061757, -1.520166291496179323, -1.183330462961203589 ) ) ;
#3270=CARTESIAN_POINT ( 'NONE',  ( 1.600152846412273844, 1.536270192620782238, 1.604750372702767214 ) ) ;
#3279=CARTESIAN_POINT ( 'NONE',  ( 4.212277857634297185, 1.593487861523819271, 0.7003764074154511521 ) ) ;
#3280=CARTESIAN_POINT ( 'NONE',  ( 2.822649888979886335, -1.354935067541668259, 1.419045635080482093 ) ) ;
#3286=CARTESIAN_POINT ( 'NONE',  ( 0.1685210592646404493, -0.8794871949406095624, -1.863628177300826305 ) ) ;
#3289=CARTESIAN_POINT ( 'NONE',  ( 5.401577436481666439, -1.966305606708594667, 0.4464985920552416720 ) ) ;
#3290=CARTESIAN_POINT ( 'NONE',  ( 1.130147970125170431, -1.436987675322987101, -1.747601730595295333 ) ) ;
#3294=CARTESIAN_POINT ( 'NONE',  ( 1.792056902697708454, -1.861051795492570049, -0.1884349046137670514 ) ) ;
#3295=CARTESIAN_POINT ( 'NONE',  ( 1.635018144205732771, 0.5444147220468772419, 1.646514679669469849 ) ) ;
#3296=CARTESIAN_POINT ( 'NONE',  ( 4.441096743985088580, -1.694418930461354611, -1.389946530008886905 ) ) ;
#3297=CARTESIAN_POINT ( 'NONE',  ( 5.104635005266920267, -0.7716809915320420599, -2.174869537816104703 ) ) ;
#3298=CARTESIAN_POINT ( 'NONE',  ( 1.041951191326966342, 0.8359002368949167705, -1.883948988615320896 ) ) ;
#3299=CARTESIAN_POINT ( 'NONE',  ( 3.310425057758420664, 1.755882755489517999, 0.8297573096471222431 ) ) ;
#3301=CARTESIAN_POINT ( 'NONE',  ( 5.712129104542990277, -0.8404194184173617854, -1.671158263034502767 ) ) ;
#3303=CARTESIAN_POINT ( 'NONE',  ( 6.573592277014387086, 1.495820547097842068, -1.351949839681469090 ) ) ;
#3305=CARTESIAN_POINT ( 'NONE',  ( 4.975232503164924935, -2.001511053420693020, -0.2440319332882301961 ) ) ;
#3308=CARTESIAN_POINT ( 'NONE',  ( 1.699542765152612711, -0.6164703606487754728, 1.718597393154073671 ) ) ;
#3316=CARTESIAN_POINT ( 'NONE',  ( 6.610000000000006537, 0.002781820520842553934, 2.000159646111852929 ) ) ;
#3318=CARTESIAN_POINT ( 'NONE',  ( 6.076820933934619084, -1.426746821240878704, 1.429770112406039795 ) ) ;
#3319=CARTESIAN_POINT ( 'NONE',  ( 0.2234921222181683598, 1.847112181986635626, 1.041312259928407702 ) ) ;
#3323=CARTESIAN_POINT ( 'NONE',  ( 5.805559403952022635, -0.5031923959765474130, 1.998377753082048347 ) ) ;
#3324=CARTESIAN_POINT ( 'NONE',  ( 4.676407821165474488, 1.496050514612049742, 1.352155788975975437 ) ) ;
#3332=CARTESIAN_POINT ( 'NONE',  ( 4.587267430073429963, 1.242536178122002344, -1.587594670648798445 ) ) ;
#3333=CARTESIAN_POINT ( 'NONE',  ( 3.626748959588219634, -1.700609458330613055, 0.7059681596332522124 ) ) ;
#3335=CARTESIAN_POINT ( 'NONE',  ( 1.735461890456877487, 0.2295834678119219041, 2.296248630371207966 ) ) ;
#3338=CARTESIAN_POINT ( 'NONE',  ( 4.481803774187195444, 1.408218611193782221, 1.640057829624480101 ) ) ;
#3340=CARTESIAN_POINT ( 'NONE',  ( 0.5384922876028491734, -1.664970009179422616, 0.9995421319052009146 ) ) ;
#3341=CARTESIAN_POINT ( 'NONE',  ( 2.782435679340321766, -0.5899881929209308540, -1.928257399728677601 ) ) ;
#3344=CARTESIAN_POINT ( 'NONE',  ( 4.060169364306280393, 1.944150891614861543, -1.225672094199470985 ) ) ;
#3346=CARTESIAN_POINT ( 'NONE',  ( 3.098369316282158614, -0.5415621961667067552, -1.790553177708480215 ) ) ;
#3347=CARTESIAN_POINT ( 'NONE',  ( 6.297732458894883756, -0.6644727202288897017, 1.856229495857963263 ) ) ;
#3350=CARTESIAN_POINT ( 'NONE',  ( 2.034064749695370100, -1.442962035976073309, -1.669870808145665020 ) ) ;
#3356=CARTESIAN_POINT ( 'NONE',  ( 0.4035112227387879225, -0.5299352985012796280, 1.898712856893035816 ) ) ;
#3357=CARTESIAN_POINT ( 'NONE',  ( 0.5698726823011552867, 0.2221484770595567870, -2.296888066578778087 ) ) ;
#3358=CARTESIAN_POINT ( 'NONE',  ( 0.5726126529861442771, 1.355618539282506640, -1.418395753018865113 ) ) ;
#3360=CARTESIAN_POINT ( 'NONE',  ( 3.819230306994053858, -1.816680642618787145, -0.9767294869839551197 ) ) ;
#3368=CARTESIAN_POINT ( 'NONE',  ( 6.848074921520021618, -0.9335981340678388696, 1.958013476854936652 ) ) ;
#3369=B_SPLINE_CURVE_WITH_KNOTS ( 'NONE', 3,
 ( #163944, #67452, #212656, #15519, #199603, #168192 ),
 .UNSPECIFIED., .F., .F.,
 ( 4, 1, 1, 4 ),
 ( 0.000000000000000000, 0.3720156466326168809, 0.4720156466326168587, 1.000000000000000000 ),
 .UNSPECIFIED. ) ;
#3371=CARTESIAN_POINT ( 'NONE',  ( 5.478019777291557979, -1.797689181224306321, -0.3974485807837144224 ) ) ;
#3374=CARTESIAN_POINT ( 'NONE',  ( 0.5966796567213605851, 1.558732183387041781, -1.033768272189788950 ) ) ;
#3379=CARTESIAN_POINT ( 'NONE',  ( 1.400873256076972329, -0.2815782128867699852, -1.891321520182134508 ) ) ;
#3380=CARTESIAN_POINT ( 'NONE',  ( 2.799370285489965138, -0.5572909556486020932, 1.679871745949900408 ) ) ;
#3381=CARTESIAN_POINT ( 'NONE',  ( 0.01216826571975513152, -1.911853497171299265, -0.04704278909201110859 ) ) ;
#3383=CARTESIAN_POINT ( 'NONE',  ( 4.411684386003834391, -1.181747345438967312, -1.507543049613221386 ) ) ;
#3384=CARTESIAN_POINT ( 'NONE',  ( -0.1409997244346122836, 0.7174646053854060179, -2.082770303449644977 ) ) ;
#3385=CARTESIAN_POINT ( 'NONE',  ( 5.213322861785598228, -1.662839039401903696, -1.055205849181278799 ) ) ;
#3386=CARTESIAN_POINT ( 'NONE',  ( 0.5453776912951785460, 0.1620316879334358084, 2.114494688702214020 ) ) ;
#3388=CARTESIAN_POINT ( 'NONE',  ( 4.258574955689950592, -1.386304660245713860, 1.256184814050688603 ) ) ;
#3389=CARTESIAN_POINT ( 'NONE',  ( 5.760297821273290708, 0.7050700890500715134, 1.574392225784694066 ) ) ;
#3391=CARTESIAN_POINT ( 'NONE',  ( 2.912931060594741162, 1.598032330669514778, -1.522282275181946032 ) ) ;
#3395=CARTESIAN_POINT ( 'NONE',  ( 1.152864133210535824, -0.4991712053786099279, -2.001264041248071113 ) ) ;
#3402=CARTESIAN_POINT ( 'NONE',  ( 3.086448098943677998, 1.152334561581969785, -1.719836228861029603 ) ) ;
#3406=CARTESIAN_POINT ( 'NONE',  ( 1.190109814708179670, 1.204940744830071075, 1.620691797242173937 ) ) ;
#3411=CARTESIAN_POINT ( 'NONE',  ( 0.07499057489260704812, 2.034159190454051913, -2.372362849262329210 ) ) ;
#3413=CARTESIAN_POINT ( 'NONE',  ( 6.257185446134499784, -2.006139278912861368, -0.2004013049526700285 ) ) ;
#3414=CARTESIAN_POINT ( 'NONE',  ( 5.946487413881851758, -1.349596479577100272, 1.359900094196204279 ) ) ;
#3415=CARTESIAN_POINT ( 'NONE',  ( 6.539320575229258914, 2.958022083381315337, 2.556018433155104574 ) ) ;
#3416=CARTESIAN_POINT ( 'NONE',  ( 4.107102485094754840, -0.3736803571842537974, 2.159302612355806339 ) ) ;
#3418=CARTESIAN_POINT ( 'NONE',  ( 3.568532368641282648, 0.6928216322696268969, 1.782650395559831180 ) ) ;
#3422=CARTESIAN_POINT ( 'NONE',  ( 1.212517793387542842, 1.944078472882956987, 0.5350667013180390175 ) ) ;
#3424=CARTESIAN_POINT ( 'NONE',  ( -0.1112335732281382050, -0.5161050057324081397, -2.242239947022279356 ) ) ;
#3426=CARTESIAN_POINT ( 'NONE',  ( 4.717633463169556229, -1.691034389814783712, 0.3384810450017295969 ) ) ;
#3428=CARTESIAN_POINT ( 'NONE',  ( -0.1405533004718676759, 7.629137130509054288, -2.320277334263821434 ) ) ;
#3432=CARTESIAN_POINT ( 'NONE',  ( 1.451531895509536874, 1.483362660712842063, 1.284035263222626844 ) ) ;
#3435=CARTESIAN_POINT ( 'NONE',  ( 0.07556134207195497332, 5.719716873484223640, -2.838244455430352087 ) ) ;
#3439=CARTESIAN_POINT ( 'NONE',  ( 3.738735263490736926, 1.721172062854194218, 0.5650376532472713986 ) ) ;
#3442=CARTESIAN_POINT ( 'NONE',  ( 4.934136933359813071, -0.9735637292621384109, -1.527415209752202019 ) ) ;
#3446=CARTESIAN_POINT ( 'NONE',  ( 4.615577964900333008, 0.4086796715298928184, -1.815441397462829398 ) ) ;
#3448=CARTESIAN_POINT ( 'NONE',  ( 2.478032317504985649, -1.910654254087537307, -0.1382841363062360662 ) ) ;
#3455=CARTESIAN_POINT ( 'NONE',  ( 0.4972265960483426284, 1.796464302094663346, -1.202062886709959422 ) ) ;
#3458=CARTESIAN_POINT ( 'NONE',  ( 1.219449367515994309, -1.782015241123528826, 0.3957228718986585680 ) ) ;
#3460=CARTESIAN_POINT ( 'NONE',  ( 1.869861807837460921, 0.9356042063937074493, 1.567457579366556386 ) ) ;
#3462=CARTESIAN_POINT ( 'NONE',  ( 2.390748813209525814, -1.831196095803063528, -0.5514187292172747501 ) ) ;
#3463=CARTESIAN_POINT ( 'NONE',  ( 3.209381719453743287, -1.608569549925453313, -1.136198915559688105 ) ) ;
#3464=CARTESIAN_POINT ( 'NONE',  ( 3.737779845645439636, 1.932976868219363764, 0.1874624384631869700 ) ) ;
#3468=CARTESIAN_POINT ( 'NONE',  ( 4.640951271726033056, 2.030106984047326701, 0.6129599860185754867 ) ) ;
#3476=CARTESIAN_POINT ( 'NONE',  ( 3.703562413045482060, -0.5285312144065814621, 1.747510042522756990 ) ) ;
#3481=CARTESIAN_POINT ( 'NONE',  ( 4.504681594071535677, 1.446009304718363087, -1.186774495104812699 ) ) ;
#3483=CARTESIAN_POINT ( 'NONE',  ( 3.053258290938072772, -1.575281680543440643, -1.108752609043755832 ) ) ;
#3484=CARTESIAN_POINT ( 'NONE',  ( 6.578960362708798471, 1.829258725439562916, 0.7091506158454219388 ) ) ;
#3489=CARTESIAN_POINT ( 'NONE',  ( 1.370887597065591823, -0.3147031148599331307, -2.093612404753260492 ) ) ;
#3492=CARTESIAN_POINT ( 'NONE',  ( 6.121949425127414024, 2.040613181561203859, -0.3481179853092666865 ) ) ;
#3493=CARTESIAN_POINT ( 'NONE',  ( 0.09881949811249221560, -0.4921898920670075839, 1.774194203830472993 ) ) ;
#3495=CARTESIAN_POINT ( 'NONE',  ( 5.871801794802778751, -0.3338885390306855494, -2.274238935559732333 ) ) ;
#3499=CARTESIAN_POINT ( 'NONE',  ( 1.641004737452517626, -1.934627630680013199, 1.229243952562808939 ) ) ;
#3500=CARTESIAN_POINT ( 'NONE',  ( -0.005637892868452093476, -0.3948761927005627337, -1.788892068844874395 ) ) ;
#3502=CARTESIAN_POINT ( 'NONE',  ( 5.947205882781483766, 0.5613781043299302942, -1.859040749089553524 ) ) ;
#3505=CARTESIAN_POINT ( 'NONE',  ( 0.6857920578585029459, 1.939116618559855842, -0.5408100507186993644 ) ) ;
#3506=CARTESIAN_POINT ( 'NONE',  ( 6.315638730379727228, -1.320822524126588515, -1.523799118890494020 ) ) ;
#3510=CARTESIAN_POINT ( 'NONE',  ( 2.712926231669846810, -0.2040156676378352685, 2.080649193556554533 ) ) ;
#3511=CARTESIAN_POINT ( 'NONE',  ( 1.709447022217532641, -1.756973726300320449, 0.2123998563456699906 ) ) ;
#3514=CARTESIAN_POINT ( 'NONE',  ( 4.470831859796895458, 0.002540009476469616122, -2.292435214262526166 ) ) ;
#3515=CARTESIAN_POINT ( 'NONE',  ( 3.257457426684560620, 0.7833967258410595713, 1.554110229252920528 ) ) ;
#3517=CARTESIAN_POINT ( 'NONE',  ( 3.444447550215405052, 1.098527548611628601, 1.341433071544478217 ) ) ;
#3518=CARTESIAN_POINT ( 'NONE',  ( 3.104148162264197985, 0.7838245717375692534, -2.024915708489416044 ) ) ;
#3520=CARTESIAN_POINT ( 'NONE',  ( 5.014861385384292269, 0.1531656238677771009, 2.010801456750747285 ) ) ;
#3521=CARTESIAN_POINT ( 'NONE',  ( 2.468750000000001776, 0.7852924748298570901, -1.895863743164139859 ) ) ;
#3523=CARTESIAN_POINT ( 'NONE',  ( 1.641497204607924809, -1.393575563620005786, -1.330239063421148948 ) ) ;
#3525=CARTESIAN_POINT ( 'NONE',  ( 4.517978939158282969, -0.5908935252547321548, 2.141346583060988351 ) ) ;
#3533=CARTESIAN_POINT ( 'NONE',  ( 0.9619568641448449364, -1.754440713604523916, -1.362318395052774633 ) ) ;
#3535=CARTESIAN_POINT ( 'NONE',  ( 6.021922112293466967, 1.933069186966931863, -0.3339256516061983038 ) ) ;
#3539=CARTESIAN_POINT ( 'NONE',  ( 0.4741787938652639034, 1.244221353789766837, 1.767418780601250017 ) ) ;
#3543=CARTESIAN_POINT ( 'NONE',  ( 3.631348232279749233, 0.05352869315983609100, -2.062151203995182147 ) ) ;
#3548=CARTESIAN_POINT ( 'NONE',  ( 6.432864026670258362, 0.1834693771665257822, 1.861492386831371748 ) ) ;
#3549=CARTESIAN_POINT ( 'NONE',  ( 4.693871744853702843, 1.512258256419211078, 0.8485452647231973566 ) ) ;
#3550=CARTESIAN_POINT ( 'NONE',  ( 3.333312927339195930, 0.7792813341828198626, -1.556285420506423600 ) ) ;
#3551=CARTESIAN_POINT ( 'NONE',  ( 2.191363998320290385, 1.774703082125920428, 1.451028844865470901 ) ) ;
#3553=CARTESIAN_POINT ( 'NONE',  ( 5.829650940335100451, 1.029561424092540589, -1.819573902328343484 ) ) ;
#3554=CARTESIAN_POINT ( 'NONE',  ( 0.2691533882960769897, 1.057504993221158873, 1.506941669042777265 ) ) ;
#3556=CARTESIAN_POINT ( 'NONE',  ( 1.582657950916711131, -0.6767122143778031562, 1.899619169727875700 ) ) ;
#3561=CARTESIAN_POINT ( 'NONE',  ( 2.912858673564645784, -0.6176872867308530468, -2.028511212565413224 ) ) ;
#3563=CARTESIAN_POINT ( 'NONE',  ( 5.057177669875371429, -1.544152220135000420, -0.9737345633797565014 ) ) ;
#3568=CARTESIAN_POINT ( 'NONE',  ( 1.617450697425420802, 1.681603173096592796, 1.118491831857356456 ) ) ;
#3569=CARTESIAN_POINT ( 'NONE',  ( 6.791986947960565679, -0.9495855537378705691, 1.990061496475347802 ) ) ;
#3572=CARTESIAN_POINT ( 'NONE',  ( 3.889374201350876525, -1.720966249256241865, 0.7085912657165122086 ) ) ;
#3577=CARTESIAN_POINT ( 'NONE',  ( 5.250558533952181861, 0.5335417292645014964, 1.745990657226546894 ) ) ;
#3581=CARTESIAN_POINT ( 'NONE',  ( 1.950155486560195772, 1.191851295230661467, 1.259505011191792923 ) ) ;
#3582=CARTESIAN_POINT ( 'NONE',  ( 0.3920123891120600446, 1.449622948667350641, -0.9626461102210502885 ) ) ;
#3583=CARTESIAN_POINT ( 'NONE',  ( 5.285860113471884780, 1.546311580504238670, 1.713158476844111933 ) ) ;
#3586=CARTESIAN_POINT ( 'NONE',  ( 1.669287087933446490, 0.1544451976582127406, -2.055073672515697059 ) ) ;
#3587=CARTESIAN_POINT ( 'NONE',  ( 6.837282040791485827, -1.423258038995322661, 1.805902563099166080 ) ) ;
#3590=CARTESIAN_POINT ( 'NONE',  ( 0.08089089327990153788, -0.1352431037574420292, -1.940231264204687722 ) ) ;
#3591=CARTESIAN_POINT ( 'NONE',  ( 3.093911922779784440, 1.216618333484908998, 1.475457842794763996 ) ) ;
#3593=CARTESIAN_POINT ( 'NONE',  ( 4.705825944637973990, -0.5905853116198942487, 2.126329296355852883 ) ) ;
#3595=B_SPLINE_CURVE_WITH_KNOTS ( 'NONE', 3,
 ( #166565, #52809, #5093, #18154, #84241, #20297, #86383, #182800, #150328, #4029, #67954 ),
 .UNSPECIFIED., .F., .F.,
 ( 4, 1, 1, 1, 1, 1, 1, 1, 4 ),
 ( 0.000000000000000000, 0.2255509035172358623, 0.3975895543896152406, 0.5252637114030099807, 0.6177357421269481508, 0.6841390318922365710, 0.7334310489036851566, 0.7741974304450970346, 1.000000000000000000 ),
 .UNSPECIFIED. ) ;
#3599=CARTESIAN_POINT ( 'NONE',  ( 6.076833508651091620, -1.499762292660647311, 1.499315088411487640 ) ) ;
#3601=CARTESIAN_POINT ( 'NONE',  ( 3.874305460179793048, 1.279221729648010175, 1.920377363040247420 ) ) ;
#3602=CARTESIAN_POINT ( 'NONE',  ( 4.299235682465595509, -1.708000122724560477, 0.9650500775852040025 ) ) ;
#3604=CARTESIAN_POINT ( 'NONE',  ( 1.270277045833507312, -0.8771146801004360283, -1.754798696806989078 ) ) ;
#3608=CARTESIAN_POINT ( 'NONE',  ( 5.735564631760892595, 0.5807582108038509272, -1.931123567068816493 ) ) ;
#3610=CARTESIAN_POINT ( 'NONE',  ( 2.958077724197702096, -0.6850214551260015439, 2.060201288156039645 ) ) ;
#3612=CARTESIAN_POINT ( 'NONE',  ( 0.6859744409541921328, 2.042103856186634925, -0.5713114342573709648 ) ) ;
#3617=CARTESIAN_POINT ( 'NONE',  ( 1.862644954548669185, -1.459483730259679257, 1.455164547919563844 ) ) ;
#3625=CARTESIAN_POINT ( 'NONE',  ( 4.969353466749234727, -1.617520173792227567, -1.019718193788564209 ) ) ;
#3628=CARTESIAN_POINT ( 'NONE',  ( 0.2635251908490592876, 0.5682291949154983923, -1.720254828205844966 ) ) ;
#3630=CARTESIAN_POINT ( 'NONE',  ( 0.8310839537030527691, -1.512174478060366534, -1.176066492228915017 ) ) ;
#3631=CARTESIAN_POINT ( 'NONE',  ( 2.154816067267216084, -0.5500195584662926906, -1.995915215819036748 ) ) ;
#3633=CARTESIAN_POINT ( 'NONE',  ( 0.7429697149608678330, -1.692012040804885098, 1.011587418319284781 ) ) ;
#3634=CARTESIAN_POINT ( 'NONE',  ( 2.297230901563730665, 1.410920830412419003, 1.158640757216542028 ) ) ;
#3635=CARTESIAN_POINT ( 'NONE',  ( 0.01296380302724577452, -0.9916191462571806170, -2.081274906121612034 ) ) ;
#3638=CARTESIAN_POINT ( 'NONE',  ( 4.633292856664962933, 0.003200217577232782832, -2.062851381006901352 ) ) ;
#3643=CARTESIAN_POINT ( 'NONE',  ( 5.157299734135989411, -1.777537633589726163, -1.129047594716176217 ) ) ;
#3645=CARTESIAN_POINT ( 'NONE',  ( 6.004363041306050697, 2.067815565686380364, 0.1054426792976848049 ) ) ;
#3647=CARTESIAN_POINT ( 'NONE',  ( 4.956408742875526130, 0.8222144862577386304, 1.999314050312686275 ) ) ;
#3648=CARTESIAN_POINT ( 'NONE',  ( 4.512370939326771691, -2.019285345247460839, -0.04732774261236893931 ) ) ;
#3650=CARTESIAN_POINT ( 'NONE',  ( 6.720655732516648051, 1.999557737031621540, 2.575425662770465252 ) ) ;
#3655=CARTESIAN_POINT ( 'NONE',  ( 2.096888995370162156, 1.803417055948232761, 0.9023429676050932491 ) ) ;
#3658=CARTESIAN_POINT ( 'NONE',  ( 6.614806895146394972, -0.1608752592793839531, 2.155998228907447523 ) ) ;
#3661=CARTESIAN_POINT ( 'NONE',  ( 6.720655732516665815, 6.034026441762381232, 2.768628153821062199 ) ) ;
#3663=CARTESIAN_POINT ( 'NONE',  ( 4.692982559244565088, 1.755779632255444422, 0.9913831279167032440 ) ) ;
#3665=CARTESIAN_POINT ( 'NONE',  ( 0.8907089605301542479, 1.523294409195220966, -0.8092020298176191284 ) ) ;
#3671=CARTESIAN_POINT ( 'NONE',  ( 5.887941446147332947, -0.8415115861447747259, 1.670666529855535654 ) ) ;
#3672=CARTESIAN_POINT ( 'NONE',  ( -0.02280469861281903335, -1.799075986276091887, -0.9034098368623093567 ) ) ;
#3676=CARTESIAN_POINT ( 'NONE',  ( 0.1226730236999207246, 0.3474926252081366185, 1.986097365194151809 ) ) ;
#3677=CARTESIAN_POINT ( 'NONE',  ( 1.054613590283080660, 0.3547985653672180439, 1.776302104178028252 ) ) ;
#3685=CARTESIAN_POINT ( 'NONE',  ( 0.3213152726999657927, -1.356817153130492004, -1.352679412961822925 ) ) ;
#3692=CARTESIAN_POINT ( 'NONE',  ( 3.889662759143839299, 1.564074849111227516, 1.492423382767386508 ) ) ;
#3695=CARTESIAN_POINT ( 'NONE',  ( 0.4398875993102538962, -2.011672884243600024, 0.6710486789910232730 ) ) ;
#3697=CARTESIAN_POINT ( 'NONE',  ( 2.091034261367350933, 1.717025232345986252, -0.9683794122406997884 ) ) ;
#3698=CARTESIAN_POINT ( 'NONE',  ( 4.974826827724895928, -1.381046924789817831, 1.323090558688621909 ) ) ;
#3701=CARTESIAN_POINT ( 'NONE',  ( 6.443809999611881167, 1.357174585993505378, 1.427557633841854967 ) ) ;
#3702=CARTESIAN_POINT ( 'NONE',  ( 0.8494333778440340543, 1.939759575794866242, -0.09477157414044742878 ) ) ;
#3708=CARTESIAN_POINT ( 'NONE',  ( 5.145129553670328981, 0.1446803459003667691, 1.906877450533929874 ) ) ;
#3710=CARTESIAN_POINT ( 'NONE',  ( 2.221956617217385244, -2.140583525707707935, 0.5359638216213060691 ) ) ;
#3712=CARTESIAN_POINT ( 'NONE',  ( 0.6274217273865910771, -0.2802014979648696502, 1.891502685196179812 ) ) ;
#3713=CARTESIAN_POINT ( 'NONE',  ( -0.02338929933909470252, 5.726375320706490690, -2.305055744220934066 ) ) ;
#3717=CARTESIAN_POINT ( 'NONE',  ( 3.191909353267761151, -1.388477207968623839, -1.535938721777901472 ) ) ;
#3722=CARTESIAN_POINT ( 'NONE',  ( 0.2159880523044250267, -2.119658899406823505, 0.4233941889316418239 ) ) ;
#3723=CARTESIAN_POINT ( 'NONE',  ( 2.999763140970078901, -2.188934734890151113, 0.1099877568606702771 ) ) ;
#3730=CARTESIAN_POINT ( 'NONE',  ( 5.854130254062820171, 0.1179724184225266898, -1.730206517700397795 ) ) ;
#3732=CARTESIAN_POINT ( 'NONE',  ( 3.239188805615275335, -0.1476314317495740769, -2.065021578984991724 ) ) ;
#3733=CARTESIAN_POINT ( 'NONE',  ( 4.148151592129151410, 0.9998098737230370903, 1.866312969332243998 ) ) ;
#3736=CARTESIAN_POINT ( 'NONE',  ( 3.133609412646401360, 1.871568317120005265, -0.6134489921753321084 ) ) ;
#3737=CARTESIAN_POINT ( 'NONE',  ( 0.7383556378116812313, 1.137082172773289379, -1.537495029474859276 ) ) ;
#3738=CARTESIAN_POINT ( 'NONE',  ( 4.839906306838932970, 2.285852466752227752, 0.1720476854494106811 ) ) ;
#3739=CARTESIAN_POINT ( 'NONE',  ( 3.475057130574196407, 0.04366187338752242769, -1.825333387291371512 ) ) ;
#3743=CARTESIAN_POINT ( 'NONE',  ( 4.095951438411546519, 1.318107682886668242, 1.521754241968393373 ) ) ;
#3744=CARTESIAN_POINT ( 'NONE',  ( 2.817183829107517745, -1.704460984269993817, -0.9711623693852902139 ) ) ;
#3747=CARTESIAN_POINT ( 'NONE',  ( 0.1751657365761547791, 2.016170943927285908, -2.458682602970231112 ) ) ;
#3749=CARTESIAN_POINT ( 'NONE',  ( 6.650343161644081569, -1.616936162011050948, 1.324992778059615128 ) ) ;
#3750=CARTESIAN_POINT ( 'NONE',  ( 5.629715507205930614, -1.125428185119830005, -1.365942169508828741 ) ) ;
#3752=CARTESIAN_POINT ( 'NONE',  ( 1.658417429842372393, -1.548019161032044844, 1.551412955586493947 ) ) ;
#3753=CARTESIAN_POINT ( 'NONE',  ( 6.158121301954061266, -1.225565299391921936, 1.235896697784558906 ) ) ;
#3755=CARTESIAN_POINT ( 'NONE',  ( 0.08204731311520391257, -1.671590265245853413, -0.4250796685295650246 ) ) ;
#3756=CARTESIAN_POINT ( 'NONE',  ( 0.5096300131263042932, 2.292432092913086361, 0.1664806320332279099 ) ) ;
#3757=CARTESIAN_POINT ( 'NONE',  ( 0.7147126110796617748, 2.027027023440019171, 0.8336157706642086662 ) ) ;
#3758=CARTESIAN_POINT ( 'NONE',  ( 2.948105999307056635, 0.7938017206191756436, -2.059354589195587337 ) ) ;
#3759=CARTESIAN_POINT ( 'NONE',  ( 6.456263137377813877, -1.236968576560824040, 1.593241027169020052 ) ) ;
#3760=CARTESIAN_POINT ( 'NONE',  ( 0.3390589225593713674, -2.105617620008819468, -0.5285623031292383533 ) ) ;
#3762=CARTESIAN_POINT ( 'NONE',  ( 1.306030339497979531, -1.181222338749428280, -1.757047197724722620 ) ) ;
#3763=CARTESIAN_POINT ( 'NONE',  ( 6.620655732516645742, 7.051964633898824886, 2.771890290588132189 ) ) ;
#3764=CARTESIAN_POINT ( 'NONE',  ( 5.420897863522853299, 1.779935589243306859, 0.7372156234431108679 ) ) ;
#3766=CARTESIAN_POINT ( 'NONE',  ( 1.822231264363738834, 1.315867814366477484, -1.876927872033665956 ) ) ;
#3771=CARTESIAN_POINT ( 'NONE',  ( 3.317226741293349157, 1.750174726733638497, -1.367746370967915626 ) ) ;
#3778=CARTESIAN_POINT ( 'NONE',  ( 1.582657950916711131, -0.6767122143778031562, 1.899619169727875700 ) ) ;
#3780=CARTESIAN_POINT ( 'NONE',  ( 1.569262014403381755, 1.817060349070098724, 0.9760215062899217919 ) ) ;
#3783=CARTESIAN_POINT ( 'NONE',  ( 6.603062865972897377, -0.3679811349713958957, 1.707173594542527040 ) ) ;
#3785=CARTESIAN_POINT ( 'NONE',  ( 2.319294515261476342, -1.717818424975267932, 0.4250260156472511208 ) ) ;
#3786=CARTESIAN_POINT ( 'NONE',  ( 1.406875202279284753, -1.122500148236497575, -1.674886495921081631 ) ) ;
#3787=CARTESIAN_POINT ( 'NONE',  ( 0.02850758872123548837, -1.683968158181762043, 0.7450552726024004535 ) ) ;
#3788=CARTESIAN_POINT ( 'NONE',  ( 4.880587636231574322, -0.2790779774165750293, -2.275280792031343147 ) ) ;
#3789=CARTESIAN_POINT ( 'NONE',  ( 3.538839456958355889, -1.395042877683351890, -1.201619466480362108 ) ) ;
#3793=CARTESIAN_POINT ( 'NONE',  ( 4.260648785556298890, -1.352668379831567069, 1.226179085325199258 ) ) ;
#3794=CARTESIAN_POINT ( 'NONE',  ( 4.658827374183164949, 1.163267680695536876, 1.646840100852072997 ) ) ;
#3796=CARTESIAN_POINT ( 'NONE',  ( 3.749113412367131914, -1.851274732041636950, 1.300436299091920045 ) ) ;
#3798=CARTESIAN_POINT ( 'NONE',  ( 6.053767517140953736, 0.6149031373867475114, -2.014179596626505919 ) ) ;
#3800=CARTESIAN_POINT ( 'NONE',  ( 3.895033709675084221, 0.3008086390649654662, 2.048262060622765279 ) ) ;
#3805=CARTESIAN_POINT ( 'NONE',  ( 2.525899207762692722, -1.109253551102797664, -1.574925972939792418 ) ) ;
#3808=CARTESIAN_POINT ( 'NONE',  ( 0.2737963954951051493, -1.932246063674218473, 0.3805649573235761474 ) ) ;
#3813=CARTESIAN_POINT ( 'NONE',  ( 0.3697636260225238836, -1.880949819439242443, -1.181558314010826116 ) ) ;
#3814=CARTESIAN_POINT ( 'NONE',  ( 3.434694453818935678, 2.054221006159732354, 0.4631738978765443382 ) ) ;
#3818=CARTESIAN_POINT ( 'NONE',  ( 0.4318009167844725771, 1.066696818439222039, 1.524822319796947934 ) ) ;
#3823=CARTESIAN_POINT ( 'NONE',  ( 1.353939357992512305, -1.539690173578952770, -1.458446627980537480 ) ) ;
#3826=CARTESIAN_POINT ( 'NONE',  ( 4.685966490639408732, -1.205361723144786845, -1.547842780461285761 ) ) ;
#3827=CARTESIAN_POINT ( 'NONE',  ( 3.661132068870280420, -1.905464569931826446, -1.020879743040298271 ) ) ;
#3828=CARTESIAN_POINT ( 'NONE',  ( 1.364538772237647413, 0.1349417713633893900, -1.836341338755695718 ) ) ;
#3831=CARTESIAN_POINT ( 'NONE',  ( 4.980260712887213614, -0.2176769249225460612, -1.726585916463187376 ) ) ;
#3836=CARTESIAN_POINT ( 'NONE',  ( 1.393688021309073433, 1.637156065531343740, 1.411701162175371893 ) ) ;
#3837=CARTESIAN_POINT ( 'NONE',  ( 2.952499795743710020, 1.423742661936340470, 1.427719607385954381 ) ) ;
#3839=CARTESIAN_POINT ( 'NONE',  ( 1.200320640528436789, -2.161883444890321915, 0.0006282887012112879947 ) ) ;
#3840=CARTESIAN_POINT ( 'NONE',  ( 3.590661340855735961, -0.3832702008734929500, -1.933690442540521470 ) ) ;
#3841=CARTESIAN_POINT ( 'NONE',  ( 6.509000000000034092, 7.052765612591089806, 2.598154238703707541 ) ) ;
#3842=CARTESIAN_POINT ( 'NONE',  ( 2.894010800797857108, -0.5660635412718226789, -1.857715926975093135 ) ) ;
#3847=CARTESIAN_POINT ( 'NONE',  ( -0.2106854629475244378, 7.629137130509075604, -2.597154134060948749 ) ) ;
#3852=CARTESIAN_POINT ( 'NONE',  ( 0.4994150495197279271, 1.833458848295946186, -1.227822027206025179 ) ) ;
#3855=CARTESIAN_POINT ( 'NONE',  ( 3.713678095275750657, 0.4809820416172749802, -1.901733992618503066 ) ) ;
#3857=CARTESIAN_POINT ( 'NONE',  ( 1.195935645703485761, 1.779627574718087635, 0.9480385367472211611 ) ) ;
#3859=CARTESIAN_POINT ( 'NONE',  ( 3.872345094350841510, -2.094861191690357227, -0.3068023397686749920 ) ) ;
#3863=CARTESIAN_POINT ( 'NONE',  ( 3.503688343963582863, -0.7473321665184138318, -1.682825604429179833 ) ) ;
#3867=CARTESIAN_POINT ( 'NONE',  ( 3.779626292077961747, 0.2561244552635975058, -2.104982076983111572 ) ) ;
#3870=CARTESIAN_POINT ( 'NONE',  ( 5.255176862235733992, -1.738700696582769378, -1.105936373271217521 ) ) ;
#3872=CARTESIAN_POINT ( 'NONE',  ( 2.313779677144182312, 1.201330555204615180, -1.395457044143719072 ) ) ;
#3880=CARTESIAN_POINT ( 'NONE',  ( 1.875870136999336246, 2.111227540014638304, -0.6426800678154330759 ) ) ;
#3881=CARTESIAN_POINT ( 'NONE',  ( 4.147957446309138874, 0.7671257181886274035, -2.128492778801443830 ) ) ;
#3884=CARTESIAN_POINT ( 'NONE',  ( 4.798965708296219823, -0.2289270959113845205, -1.797013726050479709 ) ) ;
#3885=CARTESIAN_POINT ( 'NONE',  ( 4.680823747822191017, 1.589204433792507087, -1.069448900409355030 ) ) ;
#3887=CARTESIAN_POINT ( 'NONE',  ( 3.379716691394366368, 1.249474069150168454, 1.524969178572218809 ) ) ;
#3888=CARTESIAN_POINT ( 'NONE',  ( 4.768341783539651324, -1.221614081569386334, 1.416756073533788518 ) ) ;
#3889=CARTESIAN_POINT ( 'NONE',  ( 3.862222655691281759, 2.290455142492770602, -0.2811034502991411888 ) ) ;
#3890=CARTESIAN_POINT ( 'NONE',  ( 4.773795620589037725, -1.825254877749547866, 0.3623055857514579370 ) ) ;
#3892=CARTESIAN_POINT ( 'NONE',  ( 0.6203277878081385754, 1.987498645412737908, 0.3399528957561820386 ) ) ;
#3894=CARTESIAN_POINT ( 'NONE',  ( 1.840588936376737372, 2.083348874589638466, 0.3076409294043966902 ) ) ;
#3898=CARTESIAN_POINT ( 'NONE',  ( 2.812858766682566181, -0.6196351552101020399, -2.028021595557969015 ) ) ;
#3900=CARTESIAN_POINT ( 'NONE',  ( 0.8615889817988997557, -1.594800366461980756, -1.239340803694780835 ) ) ;
#3906=CARTESIAN_POINT ( 'NONE',  ( 2.372553944209778720, -1.331880425775422205, 1.702409713178254069 ) ) ;
#3907=CARTESIAN_POINT ( 'NONE',  ( 6.610000000000026077, 2.442988107647511509, 2.382821027452782570 ) ) ;
#3915=CARTESIAN_POINT ( 'NONE',  ( 6.550343146927733784, -1.615745695573450824, 1.326605865911892002 ) ) ;
#3917=CARTESIAN_POINT ( 'NONE',  ( 2.008995473212730865, 1.676182761729711590, -1.519857458481475909 ) ) ;
#3924=CARTESIAN_POINT ( 'NONE',  ( 3.756244407761480275, 0.6229016427463770489, 1.608663766957881824 ) ) ;
#3926=CARTESIAN_POINT ( 'NONE',  ( 1.598528592787134883, 1.450519685958560512, -1.013601284844565908 ) ) ;
#3927=CARTESIAN_POINT ( 'NONE',  ( 2.631496214491501728, -0.1952657482040425496, 2.003584891602292473 ) ) ;
#3928=CARTESIAN_POINT ( 'NONE',  ( 5.508869005905306260, 1.674340917344345536, -1.437622030140395912 ) ) ;
#3929=ORIENTED_EDGE ( 'NONE', *, *, #161141, .F. ) ;
#3931=CARTESIAN_POINT ( 'NONE',  ( 4.969442291489525765, -1.791676405564743169, -1.133875526122554156 ) ) ;
#3932=CARTESIAN_POINT ( 'NONE',  ( 4.165638788432171502, 1.319243065725501429, 1.525032742243138228 ) ) ;
#3933=CARTESIAN_POINT ( 'NONE',  ( 4.623216614435611937, 1.579690555364177351, 0.8866180403494609008 ) ) ;
#3936=CARTESIAN_POINT ( 'NONE',  ( 1.867826558377215118, 0.9591755677602132879, 1.605880698980370225 ) ) ;
#3940=CARTESIAN_POINT ( 'NONE',  ( 1.476665317443916603, -1.350161712199383413, 1.354623164920423450 ) ) ;
#3948=CARTESIAN_POINT ( 'NONE',  ( 2.084357000244409175, 1.132115006494602394, -1.602057852124554316 ) ) ;
#3951=CARTESIAN_POINT ( 'NONE',  ( 4.728832233812888752, 1.460412846248357210, -1.537820402542383169 ) ) ;
#3954=CARTESIAN_POINT ( 'NONE',  ( 5.272717044759430927, -1.855309747074182836, -0.6666870051924634888 ) ) ;
#3956=CARTESIAN_POINT ( 'NONE',  ( 0.9846361663228007099, -1.273826410524713459, 1.558997777263083417 ) ) ;
#3958=CARTESIAN_POINT ( 'NONE',  ( 1.107202915679715405, -0.04781017987004822223, 2.116844178444466706 ) ) ;
#3960=CARTESIAN_POINT ( 'NONE',  ( 3.068866956829822801, 1.501395149897828851, -1.425812640530661479 ) ) ;
#3964=CARTESIAN_POINT ( 'NONE',  ( 5.103505634659632584, -2.080644823048905412, 0.2041521072984452956 ) ) ;
#3966=CARTESIAN_POINT ( 'NONE',  ( 2.871877888313049354, 0.9750061419492547232, 1.543211660213184899 ) ) ;
#3967=CARTESIAN_POINT ( 'NONE',  ( 1.031567638852897373, -1.767431343716918013, 0.3961611186833951526 ) ) ;
#3969=CARTESIAN_POINT ( 'NONE',  ( 6.463508838306311510, 0.3818026259072569983, -2.173449913608488160 ) ) ;
#3973=CARTESIAN_POINT ( 'NONE',  ( 4.911249081476435130, 1.917979745144289261, 1.091307337132418454 ) ) ;
#3976=CARTESIAN_POINT ( 'NONE',  ( 4.441997247558228779, -1.179148908705367482, -1.505365500079666852 ) ) ;
#3979=CARTESIAN_POINT ( 'NONE',  ( 6.338344951546218908, -1.110931056888088353, 1.746890944850579830 ) ) ;
#3982=CARTESIAN_POINT ( 'NONE',  ( 6.304242050522723240, 1.625252681175231029, -1.470355468214133543 ) ) ;
#3988=CARTESIAN_POINT ( 'NONE',  ( 4.094877388769967652, 1.581529129216452390, -0.9985332613470514485 ) ) ;
#3994=CARTESIAN_POINT ( 'NONE',  ( 0.2390023523631857882, -0.1431304410692470219, -1.937466148627289719 ) ) ;
#3995=CARTESIAN_POINT ( 'NONE',  ( 0.9136856707930467447, -1.281379520587552889, -1.556895127150646374 ) ) ;
#3999=CARTESIAN_POINT ( 'NONE',  ( 1.236564921189796662, 0.4304113295856801247, 2.148598399174222351 ) ) ;
#4000=CARTESIAN_POINT ( 'NONE',  ( 5.848246728868278232, 1.823843535133644389, 0.08496628090458313576 ) ) ;
#4007=CARTESIAN_POINT ( 'NONE',  ( 3.632213977189250098, 0.2737156317273430894, 1.820677940640710979 ) ) ;
#4008=CARTESIAN_POINT ( 'NONE',  ( 0.7682272020711936600, 2.010684543107125410, -0.1010625827991030873 ) ) ;
#4009=CARTESIAN_POINT ( 'NONE',  ( 1.599382804601066743, 1.132622197759477478, -1.999898178936350357 ) ) ;
#4011=CARTESIAN_POINT ( 'NONE',  ( 0.9536794021071954841, -0.6768100219149524310, 1.733691362649824264 ) ) ;
#4015=CARTESIAN_POINT ( 'NONE',  ( 4.007995338699682719, -0.7271224857151190601, 1.768968726348684406 ) ) ;
#4019=CARTESIAN_POINT ( 'NONE',  ( 3.351197789220595080, 0.5058271172731694243, -2.028516034726547623 ) ) ;
#4020=CARTESIAN_POINT ( 'NONE',  ( 2.324885834233282544, -0.002380789299309681549, 1.870836310375329381 ) ) ;
#4023=CARTESIAN_POINT ( 'NONE',  ( 2.911345607792231949, -0.8600081332746039031, -1.513042209403854699 ) ) ;
#4026=CARTESIAN_POINT ( 'NONE',  ( 3.562884411436726850, -1.522066076379503974, -0.8114761229951471533 ) ) ;
#4027=CARTESIAN_POINT ( 'NONE',  ( 4.370767597569780172, -0.0006098066561242150270, -2.191739723162715592 ) ) ;
#4028=CARTESIAN_POINT ( 'NONE',  ( 5.918643953348324160, 1.484978324971843566, -1.632713241052483832 ) ) ;
#4029=CARTESIAN_POINT ( 'NONE',  ( 6.983263157960349687, 0.5706719223780298833, 2.105707282093812083 ) ) ;
#4031=CARTESIAN_POINT ( 'NONE',  ( 3.274467656630496659, -1.066080149914239161, -1.891199154716957098 ) ) ;
#4032=CARTESIAN_POINT ( 'NONE',  ( 2.736711336054332921, 0.2235625380298221498, 1.811883384933578256 ) ) ;
#4034=CARTESIAN_POINT ( 'NONE',  ( 4.610634390349757084, 2.027228601534016406, 0.6112464051817678712 ) ) ;
#4037=CARTESIAN_POINT ( 'NONE',  ( 5.091491514903929705, -0.8269519956315901643, 2.138199492833972482 ) ) ;
#4039=CARTESIAN_POINT ( 'NONE',  ( 6.620655732516648406, 2.482285041548700111, 2.111775279032622521 ) ) ;
#4042=CARTESIAN_POINT ( 'NONE',  ( 0.5398874254142792539, -2.012210497580559476, 0.6691108114003360141 ) ) ;
#4049=CARTESIAN_POINT ( 'NONE',  ( 5.502577337681268332, -1.966645332631598908, 0.4444998760482973821 ) ) ;
#4051=CARTESIAN_POINT ( 'NONE',  ( 4.539923930118438200, 1.343280314546798637, 1.565306332949261803 ) ) ;
#4053=CARTESIAN_POINT ( 'NONE',  ( -0.2411972340276022364, 0.7381021182278154624, -1.984382818515282532 ) ) ;
#4056=CARTESIAN_POINT ( 'NONE',  ( 0.1329588055935760349, 4.094961471249922269, -2.400852151441670745 ) ) ;
#4057=CARTESIAN_POINT ( 'NONE',  ( 0.9551577523512165824, 0.4061005957273036704, -2.050632492140195939 ) ) ;
#4058=CARTESIAN_POINT ( 'NONE',  ( 5.010388774477189777, -1.913804350592800629, 0.6351971752796632398 ) ) ;
#4059=CARTESIAN_POINT ( 'NONE',  ( 4.212339636135824961, 1.685202893791247769, 0.7422218904534692019 ) ) ;
#4061=CARTESIAN_POINT ( 'NONE',  ( 2.187500000000001332, -1.451031289061030849, 1.451031289061208041 ) ) ;
#4063=CARTESIAN_POINT ( 'NONE',  ( 0.3402809042804251227, 0.2871511109263942818, 1.700534619074739906 ) ) ;
#4065=CARTESIAN_POINT ( 'NONE',  ( 1.126083094664981799, 0.4549445381971609637, 2.253098081826758303 ) ) ;
#4067=CARTESIAN_POINT ( 'NONE',  ( 0.7204656808509112276, -1.211343046821738101, -1.910610397963452112 ) ) ;
#4068=CARTESIAN_POINT ( 'NONE',  ( 3.088603512095712045, -2.074978072712420296, -0.3595722787458465186 ) ) ;
#4072=CARTESIAN_POINT ( 'NONE',  ( 5.875000000000001776, 2.052068128417940951, -3.214650538869141380E-13 ) ) ;
#4077=CARTESIAN_POINT ( 'NONE',  ( 5.097972104635399404, 1.492264293747805226, 1.645667271412653898 ) ) ;
#4078=CARTESIAN_POINT ( 'NONE',  ( 1.886939110189549185, 1.905679594745551819, -1.081921739459410059 ) ) ;
#4081=CARTESIAN_POINT ( 'NONE',  ( 5.916451087343006954, 0.7937011933104149985, 1.794315766958521241 ) ) ;
#4083=CARTESIAN_POINT ( 'NONE',  ( 6.890000000000012115, 1.205492346117660762, 2.388860368086835884 ) ) ;
#4086=CARTESIAN_POINT ( 'NONE',  ( 5.027636390373714903, -0.3086946445357250379, 2.097867224209007730 ) ) ;
#4090=CARTESIAN_POINT ( 'NONE',  ( 6.772347375734490527, -1.334533509509854943, 1.701269717329929820 ) ) ;
#4092=CARTESIAN_POINT ( 'NONE',  ( 5.161589042655139181, 0.9124512986629171873, 1.599201395118980740 ) ) ;
#4096=CARTESIAN_POINT ( 'NONE',  ( 1.047962540061377679, -1.372746097444921043, 1.069743175550162295 ) ) ;
#4100=CARTESIAN_POINT ( 'NONE',  ( 5.014612968065254250, 1.493337269798940881, -1.563205770552501761 ) ) ;
#4104=CARTESIAN_POINT ( 'NONE',  ( 4.118171802502921253, -1.108985364570359566, -1.855417305202881506 ) ) ;
#4106=CARTESIAN_POINT ( 'NONE',  ( 5.061777102197771327, 1.950294035894485356, -0.2865203566276338654 ) ) ;
#4107=CARTESIAN_POINT ( 'NONE',  ( 4.481622980438174864, 1.585354267084694957, 0.7024943803609559057 ) ) ;
#4108=CARTESIAN_POINT ( 'NONE',  ( 0.3983070667218471805, -0.7439898890007863308, -2.061537379893277677 ) ) ;
#4109=CARTESIAN_POINT ( 'NONE',  ( 2.573609363736366618, 0.1136701668994527237, -2.304911326000145699 ) ) ;
#4110=CARTESIAN_POINT ( 'NONE',  ( 4.200502791967850591, -0.6429285697095908914, -1.958015678616845445 ) ) ;
#4111=CARTESIAN_POINT ( 'NONE',  ( 0.005655660794708254786, -0.8285957215397036224, -1.754384556632330838 ) ) ;
#4117=CARTESIAN_POINT ( 'NONE',  ( 3.382038520680182181, 1.398480293485371284, 1.707083182650385389 ) ) ;
#4120=CARTESIAN_POINT ( 'NONE',  ( 0.9009385260731802569, -1.599958946562014539, 0.9501217156336287939 ) ) ;
#4121=CARTESIAN_POINT ( 'NONE',  ( -0.1290005225502432740, 4.081813041011835175, -2.728655865233818201 ) ) ;
#4125=CARTESIAN_POINT ( 'NONE',  ( 6.825078400183550720, 7.629137130509051623, 2.644348168701659674 ) ) ;
#4126=CARTESIAN_POINT ( 'NONE',  ( 6.404252597826388893, 1.360807738692754176, -1.240355271200761056 ) ) ;
#4128=CARTESIAN_POINT ( 'NONE',  ( 2.870052109166462362, 1.101224123558439905, 1.741800865840010593 ) ) ;
#4131=CARTESIAN_POINT ( 'NONE',  ( 2.332681060731033540, 1.317659697769531624, -1.530744237074317171 ) ) ;
#4135=CARTESIAN_POINT ( 'NONE',  ( 1.850533416564412725, 0.6455992098736047513, 1.957236905219070566 ) ) ;
#4139=CARTESIAN_POINT ( 'NONE',  ( -0.2409995289980038091, 6.947781193150415646, -2.595509233728268583 ) ) ;
#4140=CARTESIAN_POINT ( 'NONE',  ( 6.006501602161061548, -0.7906231143557163055, -2.060575041408031272 ) ) ;
#4141=CARTESIAN_POINT ( 'NONE',  ( 1.792469030454997059, -2.151019407201111289, -0.2137723215496489249 ) ) ;
#4143=CARTESIAN_POINT ( 'NONE',  ( 1.270720652900014791, -0.3006520276036573902, -1.993892820393451615 ) ) ;
#4144=CARTESIAN_POINT ( 'NONE',  ( 2.214639623771569088, -1.845710301178200119, -1.369457037089250484 ) ) ;
#4146=CARTESIAN_POINT ( 'NONE',  ( 6.639320575229252341, 0.005161017367553630275, 1.896863882003448021 ) ) ;
#4149=CARTESIAN_POINT ( 'NONE',  ( 1.551402291579254022, 0.5461136009352780540, -1.789155053659279071 ) ) ;
#4150=CARTESIAN_POINT ( 'NONE',  ( 3.538296236868877731, 0.7303062672313584969, 1.879804216660937666 ) ) ;
#4154=CARTESIAN_POINT ( 'NONE',  ( 4.688165273298999125, -0.9932770932522380081, 1.857119049063939320 ) ) ;
#4159=CARTESIAN_POINT ( 'NONE',  ( 4.992447118679333329, -1.118567257517719460, 1.681552772592603384 ) ) ;
#4161=CARTESIAN_POINT ( 'NONE',  ( 0.9188877648007650611, -1.496628706349166338, 1.419512306474308261 ) ) ;
#4163=CARTESIAN_POINT ( 'NONE',  ( 5.571600594950134600, 2.084881007647599205, -0.5705972643132785072 ) ) ;
#4168=CARTESIAN_POINT ( 'NONE',  ( 3.279888855285200577, -2.093262694144955027, 0.5762538248230695270 ) ) ;
#4171=CARTESIAN_POINT ( 'NONE',  ( 1.891909123491273492, -0.4922293657834125313, -1.774144672653771293 ) ) ;
#4174=CARTESIAN_POINT ( 'NONE',  ( 4.353197867323560288, 0.4795420089713005041, -2.138300074133951068 ) ) ;
#4175=CARTESIAN_POINT ( 'NONE',  ( 6.883263157960341161, 7.051904271082326758, 2.751962465287846271 ) ) ;
#4176=CARTESIAN_POINT ( 'NONE',  ( 4.680719170653036443, -2.193521624435289752, -0.5540208151394544478 ) ) ;
#4183=CARTESIAN_POINT ( 'NONE',  ( 5.589024195967314590, 1.560314836579352438, -0.8350092274562578298 ) ) ;
#4185=CARTESIAN_POINT ( 'NONE',  ( 2.116374960856721277, -0.9918371849380368532, -1.857756019195427877 ) ) ;
#4189=CARTESIAN_POINT ( 'NONE',  ( 2.348051406654600104, -0.8447338538565999366, 1.779358369178071886 ) ) ;
#4192=CARTESIAN_POINT ( 'NONE',  ( 5.730666697864316816, 1.210223194361861543, -1.348246716841319692 ) ) ;
#4196=CARTESIAN_POINT ( 'NONE',  ( 5.981297838379463272, 1.727768277425823396, -0.7175292643646775659 ) ) ;
#4198=CARTESIAN_POINT ( 'NONE',  ( 5.348515126027269417, -2.053966340784090239, -0.2589089449258550890 ) ) ;
#4210=CARTESIAN_POINT ( 'NONE',  ( 5.336364984333265227, -1.091323163865608459, 1.630109012322231266 ) ) ;
#4212=CARTESIAN_POINT ( 'NONE',  ( 3.497422563753574298, 1.966343570655813666, 0.4444343670074250574 ) ) ;
#4213=CARTESIAN_POINT ( 'NONE',  ( 2.835059001918965649, -1.568902116443865236, -1.099054045514812117 ) ) ;
#4214=CARTESIAN_POINT ( 'NONE',  ( -0.1108833634136975610, 0.7331455517814323697, -1.980187714524218823 ) ) ;
#4215=CARTESIAN_POINT ( 'NONE',  ( 0.2752733618501881363, 2.042644424557562122, -0.7945232813236638991 ) ) ;
#4216=CARTESIAN_POINT ( 'NONE',  ( 0.1331715793776600265, 2.877549198462618474, -2.442236402435117526 ) ) ;
#4217=CARTESIAN_POINT ( 'NONE',  ( 2.547943918863291302, 1.870051909910470878, 0.05015897750767356333 ) ) ;
#4219=CARTESIAN_POINT ( 'NONE',  ( 4.148693527746351251, 1.975194156771160170, 0.3885511358477158894 ) ) ;
#4222=CARTESIAN_POINT ( 'NONE',  ( 4.974263482967073990, -2.101360013415910721, -0.2580830166784564006 ) ) ;
#4223=CARTESIAN_POINT ( 'NONE',  ( 6.531696417657103737, 1.982406992490031383, -0.5971068152322634992 ) ) ;
#4224=CARTESIAN_POINT ( 'NONE',  ( 0.7672655991019157184, 2.013871065616902989, -0.5614242917610365868 ) ) ;
#4226=CARTESIAN_POINT ( 'NONE',  ( 6.247073575888860475, -1.540555741078741825, 0.9791950884799265342 ) ) ;
#4235=CARTESIAN_POINT ( 'NONE',  ( 0.5393639851597960000, -1.720521155456521400, 0.5669088471357224268 ) ) ;
#4242=CARTESIAN_POINT ( 'NONE',  ( 6.151970292378349470, 1.039009440890667824, 1.727993850779283802 ) ) ;
#4243=CARTESIAN_POINT ( 'NONE',  ( 0.6805317496583452863, 1.048634805427307359, 1.842989218901350812 ) ) ;
#4247=CARTESIAN_POINT ( 'NONE',  ( 0.1405533004714175083, 0.2365636613079393491, -2.314604644119310439 ) ) ;
#4251=CARTESIAN_POINT ( 'NONE',  ( 3.080859285270169057, 1.852775266960526412, 0.6680929264101590492 ) ) ;
#4252=CARTESIAN_POINT ( 'NONE',  ( 4.341422844945469706, 0.4390097190783425196, -1.967893369681630311 ) ) ;
#4255=CARTESIAN_POINT ( 'NONE',  ( 5.314472526525434226, 2.023830839259177949, 0.8410439265160507549 ) ) ;
#4257=CARTESIAN_POINT ( 'NONE',  ( 3.575144680771982220, 0.04857402364528973226, -1.925943534667476476 ) ) ;
#4259=CARTESIAN_POINT ( 'NONE',  ( -0.02968770228137587730, 6.948707269782667062, -2.421356871654921417 ) ) ;
#4260=CARTESIAN_POINT ( 'NONE',  ( 0.1333542156527140476, 0.7077123155428012291, -2.127987941987404596 ) ) ;
#4264=CARTESIAN_POINT ( 'NONE',  ( 5.049637312653283416, 1.456549282395647849, 1.325737238711437893 ) ) ;
#4265=CARTESIAN_POINT ( 'NONE',  ( 0.1341856092403709844, 0.3330598185416616119, 1.913145364980510799 ) ) ;
#4266=CARTESIAN_POINT ( 'NONE',  ( 3.563142721848435279, -1.644496397275853505, 1.160845683069864798 ) ) ;
#4267=CARTESIAN_POINT ( 'NONE',  ( 4.921405902946369260, 0.8734970824106644827, 2.126109943308290617 ) ) ;
#4269=CARTESIAN_POINT ( 'NONE',  ( 3.871788065385643574, -1.834046284760854961, 0.3141801383321814467 ) ) ;
#4273=CARTESIAN_POINT ( 'NONE',  ( 6.720655732516671144, 1.288224904612661925, 1.942155157606942240 ) ) ;
#4274=CARTESIAN_POINT ( 'NONE',  ( 0.8377433530848135135, 0.8832496248250313320, -2.005872107257236969 ) ) ;
#4279=CARTESIAN_POINT ( 'NONE',  ( 0.1174333910212103232, -1.791171220025630895, 0.3524246893974944395 ) ) ;
#4282=CARTESIAN_POINT ( 'NONE',  ( 2.918323747256291956, -1.167012588333454781, -1.282868673017246941 ) ) ;
#4286=CARTESIAN_POINT ( 'NONE',  ( 5.215394836314163562, -0.2642288504575221464, 1.806346989861665087 ) ) ;
#4287=CARTESIAN_POINT ( 'NONE',  ( 2.975390029205773779, -0.1970676810524821521, 1.951864085487287959 ) ) ;
#4292=CARTESIAN_POINT ( 'NONE',  ( 5.092489908381383934, -1.177591669451777179, 1.763244422785560150 ) ) ;
#4295=CARTESIAN_POINT ( 'NONE',  ( 2.254815949590884827, -0.5480598642870064818, -1.996355599893632649 ) ) ;
#4298=CARTESIAN_POINT ( 'NONE',  ( 4.512477240926440203, -2.220771887297602110, -0.05487108470654011860 ) ) ;
#4300=CARTESIAN_POINT ( 'NONE',  ( 1.952162490553134955, -2.103507816325803415, -0.9273050526804761384 ) ) ;
#4306=CARTESIAN_POINT ( 'NONE',  ( 3.463059065379545221, -1.560675823418774533, 1.104941681961457256 ) ) ;
#4308=CARTESIAN_POINT ( 'NONE',  ( 3.803458131734431813, -0.5007765277059565978, 1.650448229862747196 ) ) ;
#4310=CARTESIAN_POINT ( 'NONE',  ( 2.149625371984189126, 1.976669504256656218, -0.3981124878784659815 ) ) ;
#4311=CARTESIAN_POINT ( 'NONE',  ( 4.008600857689972763, -2.199693827605917917, 0.6672659128543911855 ) ) ;
#4313=CARTESIAN_POINT ( 'NONE',  ( 6.516252164726425100, -0.9909202252585481707, -1.858390699035996407 ) ) ;
#4316=CARTESIAN_POINT ( 'NONE',  ( 5.184699891622216228, -0.2167559868061739725, -1.756304918635148704 ) ) ;
#4318=CARTESIAN_POINT ( 'NONE',  ( 0.4633194693007875453, 0.2188196410306940398, -2.281803551658576179 ) ) ;
#4319=CARTESIAN_POINT ( 'NONE',  ( 6.714805130922314014, -0.1276373473727103192, 1.811824464382847832 ) ) ;
#4321=CARTESIAN_POINT ( 'NONE',  ( 5.191441776010861986, -0.7909675746368142191, 2.043907961996515699 ) ) ;
#4324=CARTESIAN_POINT ( 'NONE',  ( -0.1296875068448159751, 0.001480089298542403009, -1.826395826379861864 ) ) ;
#4325=CARTESIAN_POINT ( 'NONE',  ( 0.2038950025188591975, -1.678810847859620869, -1.376375048264495859 ) ) ;
#4326=CARTESIAN_POINT ( 'NONE',  ( 1.587125413319636635, 1.679225032509903404, 1.116207499648947943 ) ) ;
#4329=CARTESIAN_POINT ( 'NONE',  ( 4.617753627809100259, -1.889021752119159459, 0.3773520080231194673 ) ) ;
#4331=CARTESIAN_POINT ( 'NONE',  ( 1.459560619642571000, -1.873223059428649639, 1.193793739728800762 ) ) ;
#4341=CARTESIAN_POINT ( 'NONE',  ( 3.878220372009810291, -0.1751146298830832670, -1.731616844506628006 ) ) ;
#4342=CARTESIAN_POINT ( 'NONE',  ( 2.312880826517309085, -1.518475810973318074, 1.242258525517292433 ) ) ;
#4347=CARTESIAN_POINT ( 'NONE',  ( 0.3091261446717024630, -1.657722840873154135, 1.227268292441574538 ) ) ;
#4350=CARTESIAN_POINT ( 'NONE',  ( 5.278529876733943915, -0.4946281652532491524, -1.954780475499573900 ) ) ;
#4351=CARTESIAN_POINT ( 'NONE',  ( 0.8665589547518313118, 1.117614298721156585, 1.967126077831014896 ) ) ;
#4355=EDGE_CURVE ( 'NONE', #77820, #55444, #175748, .T. ) ;
#4356=CARTESIAN_POINT ( 'NONE',  ( 1.686563950722594685, -0.2693046698774223535, -1.850923959389898288 ) ) ;
#4357=CARTESIAN_POINT ( 'NONE',  ( -0.01748474828899664046, -1.733701077801694579, -0.04590633323625636919 ) ) ;
#4358=CARTESIAN_POINT ( 'NONE',  ( 4.634432875810733599, 0.3748786239917039631, 2.159109584303263940 ) ) ;
#4359=CARTESIAN_POINT ( 'NONE',  ( 5.948310197725324322, 2.304532173486303570, 0.1212388396696506970 ) ) ;
#4360=CARTESIAN_POINT ( 'NONE',  ( 0.7431281084272289839, -1.767980789219452342, 1.058748425497215262 ) ) ;
#4361=CARTESIAN_POINT ( 'NONE',  ( 3.820204237656314561, 1.844379349147889480, 0.6080220579995837538 ) ) ;
#4363=CARTESIAN_POINT ( 'NONE',  ( 5.624238404463478780, 1.114819804898508515, -1.501858222471161408 ) ) ;
#4365=CARTESIAN_POINT ( 'NONE',  ( 4.096327398540238640, -0.3419367296172080017, 1.987046374476949095 ) ) ;
#4369=CARTESIAN_POINT ( 'NONE',  ( 2.473051018021198200, 0.08991741065280876855, -1.823594477012622228 ) ) ;
#4378=CARTESIAN_POINT ( 'NONE',  ( 6.094400524283400067, -1.078572965507901715, 1.707356775630589851 ) ) ;
#4379=CARTESIAN_POINT ( 'NONE',  ( 6.358078514681034576, 0.8530912398192547208, -2.051143523256500067 ) ) ;
#4383=CARTESIAN_POINT ( 'NONE',  ( 5.823136237661057812, -0.05295972098229295016, 2.060385759621866431 ) ) ;
#4384=CARTESIAN_POINT ( 'NONE',  ( 3.428361437285933455, -1.528740797599713153, -1.314997250469025936 ) ) ;
#4386=ORIENTED_EDGE ( 'NONE', *, *, #83840, .T. ) ;
#4392=CARTESIAN_POINT ( 'NONE',  ( 3.954453749441131816, 1.458333106491338960, 1.392332789497241263 ) ) ;
#4393=CARTESIAN_POINT ( 'NONE',  ( 3.890429890068654917, 1.554390554365025379, -0.9864425779082321988 ) ) ;
#4395=CARTESIAN_POINT ( 'NONE',  ( 2.579137097422959712, -2.208767019342866345, -0.6684429575241066512 ) ) ;
#4397=CARTESIAN_POINT ( 'NONE',  ( 4.798204600472657511, -2.160985683756014630, -0.05834674948757002932 ) ) ;
#4399=CARTESIAN_POINT ( 'NONE',  ( 6.567912610837368881, -1.126952994821692533, 1.456688911285822119 ) ) ;
#4404=CARTESIAN_POINT ( 'NONE',  ( 2.641296366799699147, -1.384790685969448099, -1.257831364775918503 ) ) ;
#4406=CARTESIAN_POINT ( 'NONE',  ( 0.4386656386161046917, 0.3326637607320662160, 1.942932543480476726 ) ) ;
#4408=CARTESIAN_POINT ( 'NONE',  ( 1.172829962703396456, -1.397616723802884708, 1.707921395779465890 ) ) ;
#4414=CARTESIAN_POINT ( 'NONE',  ( 6.649300054797159909, -1.583302550941813491, -1.174460211130315512 ) ) ;
#4415=CARTESIAN_POINT ( 'NONE',  ( 6.516287943725491694, -1.081378002916585368, -2.038673766938512877 ) ) ;
#4416=CARTESIAN_POINT ( 'NONE',  ( 6.725070007137362360, -1.702231675683645973, -0.7527390810756880990 ) ) ;
#4417=CARTESIAN_POINT ( 'NONE',  ( 4.276276908810595856, -1.056066993903046924, -1.771547272865436673 ) ) ;
#4426=CARTESIAN_POINT ( 'NONE',  ( 6.268071979561871565, -2.155543878041016992, 0.2595383615264702515 ) ) ;
#4428=CARTESIAN_POINT ( 'NONE',  ( 5.196754805642953556, 1.508532920973480795, 1.055450849767838317 ) ) ;
#4432=CARTESIAN_POINT ( 'NONE',  ( 0.3681424317822541425, -1.226883886190757611, 1.412057460252094554 ) ) ;
#4436=CARTESIAN_POINT ( 'NONE',  ( 0.8207898099904624711, 1.447681275506585541, -1.249484660484905030 ) ) ;
#4437=CARTESIAN_POINT ( 'NONE',  ( 2.377515701973518691, 1.086635889927405341, 1.396898309679272865 ) ) ;
#4438=CARTESIAN_POINT ( 'NONE',  ( -0.05814382529654647802, -1.176414490726215734, -1.508152472379259867 ) ) ;
#4440=CARTESIAN_POINT ( 'NONE',  ( 4.640194291141960470, 0.7370120463812566136, 1.768359169405645304 ) ) ;
#4442=CARTESIAN_POINT ( 'NONE',  ( 5.476995390384709061, 1.819097369218507732, 0.7554879866787550524 ) ) ;
#4443=CARTESIAN_POINT ( 'NONE',  ( 6.099869210120771434, 1.395876734396967356, 1.460039163664628159 ) ) ;
#4445=CARTESIAN_POINT ( 'NONE',  ( 3.889402362484274622, 1.354500474538382626, 1.290456140434749654 ) ) ;
#4446=CARTESIAN_POINT ( 'NONE',  ( 6.164645834669005175, -1.214467819493704415, 1.225147371335724156 ) ) ;
#4448=CARTESIAN_POINT ( 'NONE',  ( 3.616033620774202983, -2.174319932014677548, 0.3768175846284789743 ) ) ;
#4451=CARTESIAN_POINT ( 'NONE',  ( 0.2915633711191143451, -1.886499572934543956, 0.8344948317597818965 ) ) ;
#4458=CARTESIAN_POINT ( 'NONE',  ( 3.051297593704501043, 1.777051743073382761, -1.062048545217339823 ) ) ;
#4462=CARTESIAN_POINT ( 'NONE',  ( 1.313155450441779726, 1.649776782055782709, -1.164742093282441937 ) ) ;
#4464=CARTESIAN_POINT ( 'NONE',  ( 0.07499057489264347731, 7.629137130509110243, -2.555503484197537922 ) ) ;
#4466=CARTESIAN_POINT ( 'NONE',  ( 6.116564501996816894, 0.5879282371138266905, -1.928457050679150298 ) ) ;
#4467=CARTESIAN_POINT ( 'NONE',  ( 5.700375016119385130, 1.281441245451527600, -1.424251128553160273 ) ) ;
#4469=CARTESIAN_POINT ( 'NONE',  ( 3.544632465004614374, -1.790652189326558563, 1.263247045326251872 ) ) ;
#4472=CARTESIAN_POINT ( 'NONE',  ( 2.935702856749935918, -1.841876368404654629, 0.5141854427313449216 ) ) ;
#4476=CARTESIAN_POINT ( 'NONE',  ( 0.9136856707930467447, -1.281379520587552889, -1.556895127150646374 ) ) ;
#4478=CARTESIAN_POINT ( 'NONE',  ( 6.480031355044912900, -2.148842909532014289, -0.4297212958329286736 ) ) ;
#4480=CARTESIAN_POINT ( 'NONE',  ( 3.434305118180380756, 1.682496158873967529, 0.3786907865064632062 ) ) ;
#4482=CARTESIAN_POINT ( 'NONE',  ( 0.1394461523057500818, 4.098109337479769465, -2.274588453029251500 ) ) ;
#4486=CARTESIAN_POINT ( 'NONE',  ( 1.064813361795993618, 1.487921858168140377, -1.278797858372302088 ) ) ;
#4494=CARTESIAN_POINT ( 'NONE',  ( 4.459482644723921752, -1.403152132390030449, -1.145693287117461656 ) ) ;
#4499=CARTESIAN_POINT ( 'NONE',  ( 5.109926359719781708, -0.6467658019376655298, 1.692270648455761917 ) ) ;
#4502=CARTESIAN_POINT ( 'NONE',  ( 5.195690723081275664, -1.315925274417349522, -1.316268238436297144 ) ) ;
#4504=CARTESIAN_POINT ( 'NONE',  ( 2.460426067449926535, -1.833815074015308300, -0.5538200352182551800 ) ) ;
#4513=CARTESIAN_POINT ( 'NONE',  ( 1.324293675337850695, 2.015212547500934814, 0.5562262626958893730 ) ) ;
#4515=CARTESIAN_POINT ( 'NONE',  ( 6.282248997152713343, -1.030047846951231971, 1.627708832905690350 ) ) ;
#4517=CARTESIAN_POINT ( 'NONE',  ( 2.203868028057700990, -1.825262823911228072, 0.04193083753635528516 ) ) ;
#4519=CARTESIAN_POINT ( 'NONE',  ( 2.373185085050379506, -1.665764800640230803, -0.9392108107411781814 ) ) ;
#4520=CARTESIAN_POINT ( 'NONE',  ( 1.803111746996020948, -1.665554870236161333, 1.050892442246372349 ) ) ;
#4521=CARTESIAN_POINT ( 'NONE',  ( 3.491681510897004959, -1.939965067831977530, -0.09248793024771610749 ) ) ;
#4525=CARTESIAN_POINT ( 'NONE',  ( 4.183913158364858553, 2.056144659531285779, -0.5182805708664262045 ) ) ;
#4533=CARTESIAN_POINT ( 'NONE',  ( 3.932112477472641920, 0.9751300899686901058, -1.543267412809447681 ) ) ;
#4534=CARTESIAN_POINT ( 'NONE',  ( 0.2036857628631080219, -1.599406074100502506, -1.314310892166506317 ) ) ;
#4538=CARTESIAN_POINT ( 'NONE',  ( 4.610133579271312954, -0.8000244862099057386, -1.691074300901610261 ) ) ;
#4540=CARTESIAN_POINT ( 'NONE',  ( 2.648949911425259263, -1.601578617359520340, 1.070393023584510050 ) ) ;
#4541=CARTESIAN_POINT ( 'NONE',  ( 6.965691013979927959, -0.4331334938386353084, 1.920344510276908112 ) ) ;
#4550=CARTESIAN_POINT ( 'NONE',  ( 0.8084048693777341477, 1.257526981011043654, -1.703196666993979536 ) ) ;
#4553=CARTESIAN_POINT ( 'NONE',  ( 6.684440181240522527, 1.196966437107028547, -1.688953195037292243 ) ) ;
#4554=CARTESIAN_POINT ( 'NONE',  ( 0.8195642880178370948, 1.096917009463085790, -1.478703137254427924 ) ) ;
#4556=CARTESIAN_POINT ( 'NONE',  ( 6.557281991921043662, -1.419039031320767474, 1.809608378690949149 ) ) ;
#4559=CARTESIAN_POINT ( 'NONE',  ( 0.9906304909971673789, -0.5616109214932778482, -2.222291424677411698 ) ) ;
#4562=CARTESIAN_POINT ( 'NONE',  ( 6.544875487120448199, -1.561333999131156780, -1.154546517916557269 ) ) ;
#4568=CARTESIAN_POINT ( 'NONE',  ( 6.187759705938407073, 1.828009178079874841, -0.5617473972939349691 ) ) ;
#4572=CARTESIAN_POINT ( 'NONE',  ( 3.134800171978794125, -1.843606372480216082, 0.9858348089602610997 ) ) ;
#4573=CARTESIAN_POINT ( 'NONE',  ( 1.182078593147641632, -1.725526258793514067, -0.3928099155053321745 ) ) ;
#4574=CARTESIAN_POINT ( 'NONE',  ( 6.592432824109000222, -0.4393352932590722792, 1.975308225066509049 ) ) ;
#4576=CARTESIAN_POINT ( 'NONE',  ( 4.172042307184393728, -1.321354948109268346, 1.872925066384116377 ) ) ;
#4577=CARTESIAN_POINT ( 'NONE',  ( 3.433312839113885850, 0.7810296162102482453, -1.555295924109141303 ) ) ;
#4581=CARTESIAN_POINT ( 'NONE',  ( 3.760871765136180933, -1.731833850012770126, -0.08630056690941270703 ) ) ;
#4582=CARTESIAN_POINT ( 'NONE',  ( 3.455704523497793001, 1.709784277118444162, 1.338028058695311273 ) ) ;
#4584=CARTESIAN_POINT ( 'NONE',  ( 4.399625206644591557, -1.976670321813909892, 0.3981083777728141038 ) ) ;
#4585=CARTESIAN_POINT ( 'NONE',  ( 2.125000000000001332, -2.052068128417950277, 1.216660472349556312E-13 ) ) ;
#4587=CARTESIAN_POINT ( 'NONE',  ( 1.448133341116746964, 1.924057924963176180, 0.09734726817032554602 ) ) ;
#4589=CARTESIAN_POINT ( 'NONE',  ( 4.939773707303276140, -2.109081064246129067, 0.6975513078685476875 ) ) ;
#4591=CARTESIAN_POINT ( 'NONE',  ( -0.2108831679770960255, 0.2438762813419328990, -1.931650693707862132 ) ) ;
#4596=CARTESIAN_POINT ( 'NONE',  ( 1.014661930782149168, -2.221473418436111125, 0.005229513783167742333 ) ) ;
#4597=CARTESIAN_POINT ( 'NONE',  ( 5.863715402168387492, -0.4781514528688200483, 1.902565108626977031 ) ) ;
#4600=CARTESIAN_POINT ( 'NONE',  ( 6.538354595224527444, 2.236366790538524718, 0.3417416818044561877 ) ) ;
#4602=CARTESIAN_POINT ( 'NONE',  ( 3.701677541426426910, -1.560128098810292130, -1.349382831327667454 ) ) ;
#4605=EDGE_CURVE ( 'NONE', #57181, #111140, #15100, .T. ) ;
#4607=CARTESIAN_POINT ( 'NONE',  ( 4.657402308249613654, 0.4116239899518738810, -1.824517662812553009 ) ) ;
#4608=CARTESIAN_POINT ( 'NONE',  ( 3.498401880895495086, -1.707742140280370746, 0.3003691301488361498 ) ) ;
#4609=CARTESIAN_POINT ( 'NONE',  ( 3.632115859802576008, 0.2593814109021801984, 1.720877339435398667 ) ) ;
#4610=CARTESIAN_POINT ( 'NONE',  ( 1.189493828671518427, 1.739998485882883861, 1.492566873345043010 ) ) ;
#4612=CARTESIAN_POINT ( 'NONE',  ( 4.071883345936186060, -1.202257327942996445, 1.710302118368298707 ) ) ;
#4613=CARTESIAN_POINT ( 'NONE',  ( 0.3394786764520755784, 1.835982197492795898, 0.1384515631646099088 ) ) ;
#4617=CARTESIAN_POINT ( 'NONE',  ( 1.248672897702383988, 1.986100274556975354, -0.3474695496914689818 ) ) ;
#4618=CARTESIAN_POINT ( 'NONE',  ( 0.5686479265839607944, -2.064760635122906418, -0.7346842419702694915 ) ) ;
#4622=CARTESIAN_POINT ( 'NONE',  ( 2.403126630736720948, -0.3650820022202577730, -2.088671427859823293 ) ) ;
#4624=CARTESIAN_POINT ( 'NONE',  ( 5.918537399722813674, 1.222626809077583587, -1.356019982345892050 ) ) ;
#4630=CARTESIAN_POINT ( 'NONE',  ( 1.775654988352931563, 0.3410282263864356511, -1.990609417402624537 ) ) ;
#4631=CARTESIAN_POINT ( 'NONE',  ( 6.668967514498191029, -2.014860697535350020, -0.9005387006749266954 ) ) ;
#4633=CARTESIAN_POINT ( 'NONE',  ( 4.627703445648046809, 1.805782058207167529, -0.4492820238155226797 ) ) ;
#4641=CARTESIAN_POINT ( 'NONE',  ( 4.811078068098579408, 1.589968679568127596, 0.8971634079883783475 ) ) ;
#4646=CARTESIAN_POINT ( 'NONE',  ( 1.264529683829066498, -1.734034291683920426, -0.006956266631255938158 ) ) ;
#4647=CARTESIAN_POINT ( 'NONE',  ( 0.07555271646370392835, -1.686692104669092807, -0.4283695578703243245 ) ) ;
#4648=CARTESIAN_POINT ( 'NONE',  ( 5.690114378391165850, -1.042650834883801947, 2.058788517775663962 ) ) ;
#4650=CARTESIAN_POINT ( 'NONE',  ( 1.405620310220422109, -0.5036079032930698141, 1.998149085168912986 ) ) ;
#4652=CARTESIAN_POINT ( 'NONE',  ( 0.1458495181914116201, -0.1430550213798176262, -1.983920851313693223 ) ) ;
#4655=CARTESIAN_POINT ( 'NONE',  ( 0.2683544108190681898, -1.289511475198481305, 1.491327623740832387 ) ) ;
#4656=CARTESIAN_POINT ( 'NONE',  ( 3.744317949583543470, 1.018843395500759197, -1.618198357137661469 ) ) ;
#4658=CARTESIAN_POINT ( 'NONE',  ( 5.426482453889071245, 1.317083479513626587, -1.770629405693980640 ) ) ;
#4663=CARTESIAN_POINT ( 'NONE',  ( 6.182307711929101224, 1.089732742074623006, 1.818925385317768928 ) ) ;
#4665=CARTESIAN_POINT ( 'NONE',  ( 3.839178312322106823, 0.3354718084071331430, 2.282954970297036201 ) ) ;
#4666=CARTESIAN_POINT ( 'NONE',  ( 3.807043925254738781, -1.605251362286563177, 1.127602784832412386 ) ) ;
#4668=CARTESIAN_POINT ( 'NONE',  ( 1.199968502355329703, 0.8001272530510427083, -1.791371145023381128 ) ) ;
#4672=CARTESIAN_POINT ( 'NONE',  ( 6.245327377194020535, 0.3399632236478037917, -1.987496870419297013 ) ) ;
#4675=CARTESIAN_POINT ( 'NONE',  ( 2.940461416894753377, -1.119856305176626821, 1.859859765203975890 ) ) ;
#4677=CARTESIAN_POINT ( 'NONE',  ( 0.4047333657465709278, -2.105317319661216047, -0.2534319464195868843 ) ) ;
#4682=CARTESIAN_POINT ( 'NONE',  ( 0.6146155864290882009, 1.423047967033652883, -1.490775708471054006 ) ) ;
#4684=CARTESIAN_POINT ( 'NONE',  ( 6.727182134110202050, 7.629137130509070275, 2.410944104600750038 ) ) ;
#4687=CARTESIAN_POINT ( 'NONE',  ( 4.160738352132353768, 0.5130957772990808463, 1.842076966104645663 ) ) ;
#4690=CARTESIAN_POINT ( 'NONE',  ( -0.0001156980946178872989, -0.8540272384012604912, 1.597593110781750925 ) ) ;
#4692=CARTESIAN_POINT ( 'NONE',  ( 1.182675045768744271, 1.564012596108365072, -1.105954659444969401 ) ) ;
#4693=CARTESIAN_POINT ( 'NONE',  ( 1.574760213118006735, 1.391939136705011348, -1.532762857463897843 ) ) ;
#4695=CARTESIAN_POINT ( 'NONE',  ( 6.807498166657679484, -0.4075194142965676836, 1.832415718333743282 ) ) ;
#4696=CARTESIAN_POINT ( 'NONE',  ( 2.982817717652554101, -0.1347461720548545627, -1.820777111243766733 ) ) ;
#4697=CARTESIAN_POINT ( 'NONE',  ( 6.287735281038357549, 1.518688880046001444, 1.601449620450722700 ) ) ;
#4700=CARTESIAN_POINT ( 'NONE',  ( 4.334473715658632820, -1.190102281996632261, 1.684540188307581010 ) ) ;
#4705=CARTESIAN_POINT ( 'NONE',  ( 6.933263157960373846, 7.629137130509066722, 2.546189081643289942 ) ) ;
#4707=CARTESIAN_POINT ( 'NONE',  ( 5.719784389160836646, -2.055351168476500234, 0.4581721925015455610 ) ) ;
#4709=CARTESIAN_POINT ( 'NONE',  ( 6.074686117427479992, 1.393331124738606652, -1.531503843499823381 ) ) ;
#4710=AXIS2_PLACEMENT_3D ( 'NONE', #23898, #119350, #90004 ) ;
#4712=CARTESIAN_POINT ( 'NONE',  ( 3.550220938608072085, 2.161773192003491495, 0.003901938047633223515 ) ) ;
#4713=CARTESIAN_POINT ( 'NONE',  ( 4.301429021398018193, 1.803172560858562701, -0.9099306128727399079 ) ) ;
#4719=CARTESIAN_POINT ( 'NONE',  ( 2.360564879530482330, -1.931125380751706810, -0.5807522007576990664 ) ) ;
#4724=CARTESIAN_POINT ( 'NONE',  ( 5.379139070037473935, -1.731557697741787916, -0.8120211572784155063 ) ) ;
#4727=CARTESIAN_POINT ( 'NONE',  ( 4.235953958900400274, 2.015913684659226490, -0.05231418598541925924 ) ) ;
#4730=CARTESIAN_POINT ( 'NONE',  ( 6.071300242175304618, 0.1216566699881876934, -1.720563304769450630 ) ) ;
#4735=CARTESIAN_POINT ( 'NONE',  ( 5.237510374101456812, -1.321932271818569093, -1.323673891312632245 ) ) ;
#4736=CARTESIAN_POINT ( 'NONE',  ( 6.433844876963536130, -1.951739824409718160, 0.4931976252120565118 ) ) ;
#4740=CARTESIAN_POINT ( 'NONE',  ( 1.001577623981730891, -1.966640429010723112, 0.4445266750975271353 ) ) ;
#4741=CARTESIAN_POINT ( 'NONE',  ( 0.8963918696095014571, -1.767652434117328308, -0.3957652751337119024 ) ) ;
#4748=CARTESIAN_POINT ( 'NONE',  ( 5.835529424904522422, 0.5513129833306378291, -1.834571867064521022 ) ) ;
#4755=CARTESIAN_POINT ( 'NONE',  ( 3.415052781332720055, 1.953485055394106107, 0.9259690932504063277 ) ) ;
#4758=CARTESIAN_POINT ( 'NONE',  ( 0.8969213510382867405, -2.070190491330957006, -0.4589741369691033857 ) ) ;
#4759=CARTESIAN_POINT ( 'NONE',  ( 5.438443955714742373, 1.798867289239113987, 0.3102399082220568816 ) ) ;
#4760=CARTESIAN_POINT ( 'NONE',  ( 1.880087831454971603, -1.058004756265405799, 1.663231189906771990 ) ) ;
#4761=CARTESIAN_POINT ( 'NONE',  ( 4.675980034926481288, 1.890745994642643479, -0.2862527531290667837 ) ) ;
#4763=CARTESIAN_POINT ( 'NONE',  ( 4.844182406995376944, -0.9301426015250592316, 1.736093160643120914 ) ) ;
#4764=CARTESIAN_POINT ( 'NONE',  ( 0.02324440041187331510, -1.194077796415137449, -1.532174088482601837 ) ) ;
#4770=CARTESIAN_POINT ( 'NONE',  ( 5.391234928627540945, -0.05113397888981999206, -1.911771334517261778 ) ) ;
#4773=CARTESIAN_POINT ( 'NONE',  ( 0.9388347430083656686, 2.174419798330699649, 0.3756190385216377492 ) ) ;
#4775=CARTESIAN_POINT ( 'NONE',  ( 6.481113961022470171, -1.841437297342415791, -0.8137991234780891370 ) ) ;
#4779=CARTESIAN_POINT ( 'NONE',  ( 2.559107912120599071, 1.664280205102614429, -1.231313097332722872 ) ) ;
#4783=CARTESIAN_POINT ( 'NONE',  ( 0.4972265960483426284, 1.796464302094663346, -1.202062886709959422 ) ) ;
#4790=CARTESIAN_POINT ( 'NONE',  ( 5.889268099914369614, -0.6330491082502353040, -1.614684210577774115 ) ) ;
#4792=CARTESIAN_POINT ( 'NONE',  ( 3.590741003927795827, 2.018730135711533258, 0.4582614309688318177 ) ) ;
#4793=CARTESIAN_POINT ( 'NONE',  ( 4.745783977240443541, 2.094000167431044446, -0.3121058131653231538 ) ) ;
#4796=CARTESIAN_POINT ( 'NONE',  ( 2.342574202377019521, -1.930441307185966515, -0.3890957575964202886 ) ) ;
#4797=CARTESIAN_POINT ( 'NONE',  ( 0.9492982845318720386, -1.727743609841876360, 0.8201845251225792222 ) ) ;
#4798=CARTESIAN_POINT ( 'NONE',  ( 4.435649837374885607, 0.9824219174630977047, -2.071190651000577976 ) ) ;
#4799=CARTESIAN_POINT ( 'NONE',  ( 2.086296903703276140, -1.790263230197926436, -0.3570169370194844483 ) ) ;
#4804=CARTESIAN_POINT ( 'NONE',  ( 2.742442218595582570, 1.114876114576800248, -1.676130933394081923 ) ) ;
#4805=CARTESIAN_POINT ( 'NONE',  ( 3.783995958019512607, -1.164969938643352299, -1.578273546942794647 ) ) ;
#4808=CARTESIAN_POINT ( 'NONE',  ( 0.07536363704233049743, 0.2309889609098912111, -2.177957698420322163 ) ) ;
#4809=CARTESIAN_POINT ( 'NONE',  ( 6.386679164125504293, 1.819714881846513199, -1.029135884875460372 ) ) ;
#4810=CARTESIAN_POINT ( 'NONE',  ( 4.574921169738827231, -0.001286399002502561879, -1.770032026507301515 ) ) ;
#4813=CARTESIAN_POINT ( 'NONE',  ( 1.254151665356119549, 0.8908215700371600043, 2.002402562943622844 ) ) ;
#4814=CARTESIAN_POINT ( 'NONE',  ( 6.492160993672303704, -0.4719841783793111145, -1.675048763955745645 ) ) ;
#4817=CARTESIAN_POINT ( 'NONE',  ( 0.5624050986996537160, 1.909334820886617656, -1.279222687617764809 ) ) ;
#4818=CARTESIAN_POINT ( 'NONE',  ( 0.4510473619779230003, -1.854578567552306767, -1.167393260480112493 ) ) ;
#4820=CARTESIAN_POINT ( 'NONE',  ( 6.520799197568460492, 1.728869810328565793, -0.1316537485448170952 ) ) ;
#4821=CARTESIAN_POINT ( 'NONE',  ( 3.035963658818414235, -1.482449291622448095, -1.634993338104336891 ) ) ;
#4823=CARTESIAN_POINT ( 'NONE',  ( 6.619587810436369679, 0.3779085275587866777, -2.137903583376862038 ) ) ;
#4825=CARTESIAN_POINT ( 'NONE',  ( 1.024788983299034451, 0.4191291695722613730, 2.075291419971446061 ) ) ;
#4826=CARTESIAN_POINT ( 'NONE',  ( 2.906250000000002220, 1.895863743164021509, -0.7852924748301391977 ) ) ;
#4827=CARTESIAN_POINT ( 'NONE',  ( 6.827182134110222123, -0.006956174471953178659, 2.188967759425272330 ) ) ;
#4828=CARTESIAN_POINT ( 'NONE',  ( 5.965835030274156736, 1.897794126051439045, -0.3298099971670089281 ) ) ;
#4830=CARTESIAN_POINT ( 'NONE',  ( 1.119135019589584834, -0.04993059730015738523, 2.291989107133483028 ) ) ;
#4834=CARTESIAN_POINT ( 'NONE',  ( 3.211816561499138523, 1.752256602034316213, 1.365123760953767418 ) ) ;
#4841=CARTESIAN_POINT ( 'NONE',  ( 2.356092462967720458, 0.09613450340887133572, -2.014232768679749430 ) ) ;
#4843=CARTESIAN_POINT ( 'NONE',  ( 6.320769014966518107, -1.461346085113580440, 1.455966316998691168 ) ) ;
#4846=CARTESIAN_POINT ( 'NONE',  ( 6.058121337783492599, -1.224224903413055010, 1.237393016278231617 ) ) ;
#4850=CARTESIAN_POINT ( 'NONE',  ( 0.8250501123308005003, -1.682963436248402056, 0.5476568922856797084 ) ) ;
#4851=CARTESIAN_POINT ( 'NONE',  ( 0.3697678102792775756, -0.2496098759999023087, -2.000856779379902139 ) ) ;
#4852=CARTESIAN_POINT ( 'NONE',  ( 0.3097736896383457839, 1.270387085892955792, -1.333027339516623888 ) ) ;
#4853=CARTESIAN_POINT ( 'NONE',  ( 3.825942575589100780, 1.225831451615842393, -1.936910307245596652 ) ) ;
#4854=CARTESIAN_POINT ( 'NONE',  ( 3.890429890068654917, 1.554390554365025379, -0.9864425779082321988 ) ) ;
#4857=CARTESIAN_POINT ( 'NONE',  ( 4.629811725094972630, -1.123643258228578024, -1.438734611599351565 ) ) ;
#4858=CARTESIAN_POINT ( 'NONE',  ( 4.834611377684539413, 0.6298767044488963185, -1.915599524792414465 ) ) ;
#4860=CARTESIAN_POINT ( 'NONE',  ( 3.960077240414155764, 2.245805352194740756, -0.2739276486512822184 ) ) ;
#4862=CARTESIAN_POINT ( 'NONE',  ( 6.756868576547260474, -1.630415217921374671, 1.332730856581629375 ) ) ;
#4864=CARTESIAN_POINT ( 'NONE',  ( 3.596198176508007105, 0.9334358170956689182, -1.848091447891623051 ) ) ;
#4867=CARTESIAN_POINT ( 'NONE',  ( 6.041668349913133618, -1.996727924239691587, 0.7141442534656232688 ) ) ;
#4870=CARTESIAN_POINT ( 'NONE',  ( 1.752441099931791868, 0.6037874858934308975, 1.829501483119711169 ) ) ;
#4872=CARTESIAN_POINT ( 'NONE',  ( 0.1507525579465497367, -0.4251589684514142653, -1.929747299214799483 ) ) ;
#4877=CARTESIAN_POINT ( 'NONE',  ( 1.143189493912871280, 2.142763695547444058, 0.5857495978145771387 ) ) ;
#4878=CARTESIAN_POINT ( 'NONE',  ( 3.469845758843297823, 2.055011051013386769, -0.4596899858253248872 ) ) ;
#4881=CARTESIAN_POINT ( 'NONE',  ( 0.2560159283585193846, -1.860519322180047785, -0.05176575080893807551 ) ) ;
#4887=CARTESIAN_POINT ( 'NONE',  ( 0.7211286721200690364, 1.601891702520108485, -1.389630591760198541 ) ) ;
#4890=CARTESIAN_POINT ( 'NONE',  ( 4.404711838702720428, 0.5211615849865286476, 1.891323523724611766 ) ) ;
#4891=CARTESIAN_POINT ( 'NONE',  ( 2.167066695894452888, -1.976221826324360498, -0.8764929760368763700 ) ) ;
#4892=CARTESIAN_POINT ( 'NONE',  ( 1.716098596715152746, 1.718394358364897068, 0.6617865747741287219 ) ) ;
#4895=CARTESIAN_POINT ( 'NONE',  ( 3.837644434229481316, 1.732183052659850286, 0.1680905250187741673 ) ) ;
#4899=CARTESIAN_POINT ( 'NONE',  ( 0.8136072859011161951, -0.3160970183575459447, 2.138355382504661506 ) ) ;
#4900=CARTESIAN_POINT ( 'NONE',  ( 3.884138610457484653, -0.1511163893381066714, 2.010518618204664154 ) ) ;
#4903=CARTESIAN_POINT ( 'NONE',  ( 3.678557393866654923, -1.899675168901427513, -0.5269097987367215019 ) ) ;
#4905=CARTESIAN_POINT ( 'NONE',  ( 6.609000000000010644, 6.035875036286768136, 2.694900582964809388 ) ) ;
#4906=CARTESIAN_POINT ( 'NONE',  ( 2.806119653986011819, 1.404935138194723265, -1.341025529631818980 ) ) ;
#4907=CARTESIAN_POINT ( 'NONE',  ( 6.827182134110198142, 0.003888933837258023996, 1.810856214465889069 ) ) ;
#4915=CARTESIAN_POINT ( 'NONE',  ( 0.5345543961663907773, 1.132513062451316221, -1.893880525681296723 ) ) ;
#4917=CARTESIAN_POINT ( 'NONE',  ( 3.889464431383614862, -1.814284039448841979, 0.7467176931179178023 ) ) ;
#4919=CARTESIAN_POINT ( 'NONE',  ( 2.233046271152541618, 2.016033844848092560, 0.04667593304989729047 ) ) ;
#4921=CARTESIAN_POINT ( 'NONE',  ( 2.606785607150950757, 1.995414689559615207, 0.7085744572869844271 ) ) ;
#4925=CARTESIAN_POINT ( 'NONE',  ( 3.345483972246702020, 1.841320589717788447, -0.001054884335952021917 ) ) ;
#4930=CARTESIAN_POINT ( 'NONE',  ( 4.412424163657523657, -2.120181911468725033, -0.04909571644767100895 ) ) ;
#4933=CARTESIAN_POINT ( 'NONE',  ( 4.745419391729821967, -1.590323190411299770, -1.310567541734160457 ) ) ;
#4935=CARTESIAN_POINT ( 'NONE',  ( 2.788419073117563762, 1.577926727847511312, -0.9486480243563880643 ) ) ;
#4940=( BOUNDED_SURFACE ( )  B_SPLINE_SURFACE ( 3, 3, ( 
 ( #108628, #203899, #90197, #26230, #158386, #9982, #156261, #7842, #73930, #76060, #140023, #142159, #208175, #59808, #125963, #191919, #121699, #187663, #105387, #171426, #178909, #28375, #30524, #128106, #144313, #97663, #145378, #15301, #211376, #130222, #32637, #63002, #164773, #146423, #127033, #115020, #98714, #163721, #160510, #14227, #77117, #80322, #129173, #181017, #192992, #48900, #44646, #110760, #194064, #196216, #195150, #143240, #64079, #45717, #162656, #96604, #46784, #176759, #111836, #13183, #47857, #212437, #113969, #79261, #60874, #112898, #94469, #61947, #78187, #179966, #213494, #31588, #12113, #209229, #210311, #177839, #81389, #29453, #95543, #161594, #147473, #131272, #65116, #197260, #104045, #151735, #70435, #69375, #201505, #16363, #148531, #166912, #66164, #184203, #3305, #52090, #51025, #86716, #186337, #82441, #118217, #117146, #100827, #165839, #85648, #17425, #83508, #54224, #1175, #37972, #67239, #183150, #134441, #135483, #19575, #101904, #33697, #102972, #149591, #34753, #167969, #2233, #98, #136551, #68310, #53152, #119281, #152785, #185267, #133373, #132309, #199378, #99774, #36890, #49956, #18506, #202572, #198316, #120362, #169030, #116075, #182065, #20627, #84585, #4365, #150672, #200444, #35826, #106221, #5430, #123581, #157069, #205789, #204704, #25971, #125701, #21677, #57419, #56354, #40110, #105124, #24901, #171164, #22753, #207920, #154925, #191660, #6510, #122517, #73664, #8658, #173323, #41192, #187408, #42257, #88871, #188480, #107299, #155992, #43324, #75800, #7579, #74737, #91007, #140842, #206854, #59540, #72586, #58486, #124642, #190599, #138687, #55289, #172247, #139763, #23834, #189544, #108370, #174393, #92077, #158134, #89941, #170091, #87787, #9725, #141908, #121439, #153861, #71509, #137621, #203638, #39039, #47592, #29188, #162397, #64873, #95278, #197011, #178645, #159178, #147218, #131019, #195958, #192727, #46513, #109442, #112636, #161326, #213243, #10779, #81132, #76854, #142973, #160249, #13973, #12910, #175449, #96342, #11850, #194877, #62736, #177575, #208974, #77928, #45451, #80060, #30256, #146161, #111567, #93141, #78990, #60610, #94209, #110503, #145106, #128896, #126769, #212176, #27033, #144048, #63811, #113707, #44381, #211112, #176503, #28115, #129971, #179711, #210044, #31328, #61683, #127852, #193802, #97405, #163460, #15040, #1980, #180761, #98453, #117962, #49697, #183956, #132059, #51843, #149333, #35566, #17174, #65912, #68044, #913, #199117, #18243, #48647, #148280, #66980, #101647, #133118, #198069, #83248, #34506, #100579, #50760, #166652, #116890, #151479, #165580, #115825, #134181, #167714, #182889, #19317, #84327, #181812, #82187, #33444, #214279, #99521, #150413, #135239, #200190, #85393, #3049, #69118, #201253, #52893, #114764, #164518, #119027, #32388, #16103, #77556, #49338, #112266, #45089, #47221, #28817, #15738, #180395, #162027, #159879, #212879, #144742, #209671, #79691, #210752, #29889, #130655, #94902, #193446, #32017, #12543, #194505, #11484, #143678, #62375, #147906, #98101, #27745, #14674, #128537, #178279, #177203, #111198, #127475, #160952, #131690, #78617, #80769, #164152, #163093, #113338, #115457, #93840, #145803, #46153, #63447, #95974, #179344, #211810, #61314, #13618, #129601, #97041, #195586, #81824, #30966, #146858 ),
 ( #64511, #196646, #65545, #48286, #213922, #114398, #197694, #17858, #20000, #101260, #54650, #168404, #83942, #52516, #134865, #35184, #66596, #150033, #117586, #86085, #184635, #118649, #183577, #165206, #151105, #148957, #166267, #182501, #2670, #103406, #36252, #116511, #99153, #100201, #50391, #102331, #528, #67663, #153220, #33076, #21051, #152160, #4790, #181447, #3730, #87148, #69804, #135911, #16796, #82880, #167344, #132741, #200872, #201929, #68742, #1603, #37331, #136983, #198744, #53585, #133807, #51462, #34132, #119718, #199819, #18930, #70868, #85016, #203010, #185699, #169467, #24262, #107746, #124013, #206226, #138051, #207299, #55716, #6939, #57853, #106658, #76238, #26413, #172685, #173770, #189980, #41632, #25347, #158564, #187840, #91446, #157508, #9103, #39467, #5868, #121869, #90368, #73020, #156435, #75179, #141290, #58922, #125081, #40554, #10164, #142347, #8020, #74111, #71940, #140205, #171596, #105565, #191037, #23190, #42704, #174835, #89305, #139117, #155354, #120800, #104482, #188916, #205145, #56787, #170528, #208355, #122956, #204064, #108811, #92525, #186776, #38403, #22112, #88224, #154293, #176946, #27485, #112017, #28561, #62131, #165760, #127217, #11223, #1093, #44834, #12287, #43768, #109881, #94650, #183063, #133290, #59987, #49875, #160694, #144488, #209412, #77305, #159629, #61058, #166828, #143417, #115999, #67154, #198237, #82363, #150587, #126140, #178017, #193185, #95721, #78368, #148452, #29636, #93585, #110940, #84497, #132228, #22, #175893, #66085, #34677, #210495, #99690, #149509, #128291, #161773, #192102, #194253, #181987, #13366, #100746, #33619, #45897, #18423, #17345, #83427, #199296, #50941, #117066, #134357, #118136, #171075, #201422, #22671, #69288, #38955, #152700, #88783, #20549, #151650, #55205, #4282, #54140, #153772, #2150, #167885, #70353, #105038, #136469, #3220, #86634, #37885, #103963, #202488, #170005, #120276, #204621, #36805, #135399, #121351, #154840, #168947, #6425, #5340, #85561, #35743, #53061, #19486, #119195, #186250, #40025, #185181, #102888, #101817, #21593, #106137, #87698, #203552, #72499, #137534, #71423, #89857, #68226, #187326, #138599, #56273, #122432, #188389, #172160, #184122, #23753, #200362, #52010, #175368, #205701, #93058, #127765, #124558, #192644, #28029, #139679, #125618, #7493, #8573, #60521, #207833, #193720, #142890, #74653, #45363, #156985, #59460, #110419, #94127, #208890, #73577, #57336, #176422, #140758, #160165, #206769, #44297, #91993, #11765, #174309, #90920, #126682, #158053, #191577, #159096, #155908, #107216, #9638, #77839, #75716, #58403, #25883, #43240, #109357, #141830, #26950, #10697, #143961, #190516, #42173, #209956, #61593, #108289, #111480, #76767, #24818, #189464, #177487, #173240, #29101, #123500, #41107, #79969, #16012, #149241, #146072, #14947, #96251, #95185, #78895, #196920, #162304, #13889, #145018, #116800, #114678, #112542, #180671, #212085, #83161, #33352, #32297, #46424, #65819, #129881, #178553, #82098, #47505, #148190, #197978, #214192, #30163, #99434, #131966, #181722, #165487, #17084, #816, #66885, #182798, #183869, #104782, #8323, #125363, #10450, #142634, #176181, #77592, #93879, #39770, #105875, #189213, #205451, #197726, #99184, #112301, #178316, #29925, #96008, #79723, #211844, #63482 ),
 ( #196680, #179378, #47258, #14709, #52548, #185727, #69833, #201959, #135942, #104513, #133840, #37360, #103435, #169496, #117616, #166299, #183609, #184664, #85046, #36283, #21078, #87180, #4820, #70900, #102361, #22140, #88254, #20029, #137011, #83975, #203038, #101292, #151134, #120828, #134893, #186804, #154323, #66624, #198774, #50423, #182533, #34161, #100232, #150063, #68774, #92555, #89335, #157538, #27515, #9134, #206258, #43799, #121901, #192134, #55745, #187868, #56817, #58952, #140236, #93614, #207333, #122987, #91478, #173800, #74143, #105595, #188945, #156467, #125110, #75209, #141320, #8054, #204092, #190012, #39497, #205175, #6967, #41662, #142377, #191068, #155383, #138079, #139147, #73048, #42732, #171628, #106690, #109912, #71969, #60018, #108840, #175923, #5897, #174866, #126171, #26445, #158595, #23223, #40585, #172715, #24291, #90397, #57883, #124046, #107775, #10194, #25377, #76268, #208386, #210529, #30739, #113111, #13395, #44866, #128322, #95752, #146636, #162869, #96820, #161804, #143448, #129383, #127249, #144520, #160726, #195362, #81600, #14449, #94683, #77335, #78400, #28596, #80540, #193220, #45930, #131473, #11257, #213702, #212652, #197475, #32856, #64293, #65326, #130439, #196426, #159658, #209445, #79471, #61090, #179116, #48071, #46994, #194286, #15515, #115238, #110971, #114182, #112049, #29668, #12319, #180177, #62164, #178050, #49120, #145588, #181228, #211585, #63221, #31803, #97879, #163939, #147685, #176978, #185486, #33912, #199598, #36039, #84799, #54443, #4581, #150887, #151946, #102119, #19787, #168188, #136765, #166054, #69588, #135699, #85869, #17639, #198528, #99988, #2449, #51241, #68524, #201725, #3517, #53366, #119500, #18715, #202793, #120585, #134652, #200656, #50175, #52305, #149815, #83725, #37112, #167130, #103190, #118435, #169253, #186563, #184422, #98931, #20839, #148743, #164985, #16576, #86938, #182286, #153004, #82659, #70655, #311, #66383, #132531, #116295, #1387, #67448, #133593, #117367, #183364, #34968, #101040, #124855, #121658, #189762, #59767, #41414, #24054, #76021, #154078, #9945, #88007, #5645, #89092, #91228, #172466, #125926, #25125, #155146, #123802, #206007, #106443, #137838, #6728, #188701, #157288, #107521, #173551, #40337, #21897, #7800, #71726, #22974, #39253, #73892, #174617, #8878, #187626, #170309, #171383, #105346, #74957, #203860, #138908, #142124, #104262, #92308, #141067, #208137, #38191, #207074, #158352, #58705, #190819, #55505, #72807, #90157, #204928, #57642, #42480, #139986, #56579, #108589, #122738, #156223, #26193, #12078, #61907, #126996, #46742, #192955, #44607, #15262, #176723, #147429, #28335, #144276, #95505, #178871, #195106, #62960, #209195, #64037, #110723, #78145, #129130, #177797, #213453, #97622, #29414, #30482, #112855, #96566, #162613, #81349, #94432, #14190, #80282, #146381, #160471, #77077, #210269, #161552, #128069, #13140, #212394, #130182, #196175, #47816, #111792, #65076, #191884, #79216, #145335, #143205, #211336, #194025, #45675, #113928, #179924, #31547, #163680, #43545, #109667, #175669, #27257, #93365, #159401, #60835, #11000, #34751, #1171, #100824, #19572, #52087, #85646, #69372, #183147, #155726, #7310, #166909, #150669, #95, #2230, #99771, #116073, #135480, #18502, #201502, #84581, #101901, #73387 ),
 ( #68307, #89676, #164770, #23566, #98711, #16361, #165837, #167965, #134438, #139492, #35824, #17422, #200441, #118214, #184201, #148529, #83505, #199376, #151732, #3303, #53148, #51022, #32635, #119279, #82439, #33695, #49953, #185263, #39845, #105952, #198313, #181013, #182063, #132305, #171976, #66160, #149587, #48896, #115017, #67237, #133370, #28925, #78723, #126504, #45194, #44120, #176251, #205520, #123319, #141648, #40922, #158925, #192468, #26776, #25707, #61419, #161059, #57154, #92879, #91815, #75537, #140580, #60343, #206591, #58219, #95010, #190336, #12652, #41998, #157873, #109178, #110241, #208717, #76595, #8391, #77665, #124378, #9466, #142707, #191399, #189282, #111308, #43065, #27852, #93949, #159990, #11591, #143785, #107028, #108105, #209780, #127583, #193552, #174133, #90742, #207659, #175190, #59278, #10521, #177311, #173054, #24634, #156804, #125437, #74473, #34236, #130757, #32120, #96079, #98203, #195692, #211918, #165309, #212978, #82984, #64618, #197801, #100310, #196752, #17968, #214023, #194611, #182614, #166376, #16903, #13721, #81927, #144850, #148013, #48393, #210856, #46254, #116621, #112372, #178383, #47327, #49436, #114506, #62482, #131795, #113442, #15841, #164253, #180502, #29994, #179447, #80873, #115555, #65648, #181552, #146963, #128646, #33180, #162132, #129709, #145907, #99261, #66700, #149059, #79794, #63553, #31069, #97145, #636, #163198, #14781, #132847, #198851, #50499, #87261, #121980, #171705, #4900, #138160, #137089, #54759, #84055, #1714, #20106, #133920, #37438, #70978, #119826, #118752, #154399, #39574, #150142, #185805, #184736, #168507, #19042, #153326, #85121, #151207, #187946, #68849, #105677, #134969, #36364, #202033, #203117, #120908, #169574, #101372, #170636, #2778, #102439, #21157, #69910, #67769, #204168, #136020, #186880, #167448, #38513, #199927, #104591, #53695, #51572, #117698, #55824, #183689, #35295, #200977, #22221, #3837, #52624, #88334, #86193, #5978, #103515, #152264, #72049, #206334, #173877, #10268, #26521, #174939, #25451, #7046, #207406, #205253, #8136, #24367, #59025, #159733, #92630, #172796, #155463, #156544, #106767, #158671, #56895, #124125, #209522, #89414, #77410, #76343, #61163, #111047, #142451, #127325, #208459, #60092, #23303, #73122, #91558, #139222, #191144, #126251, #125183, #57960, #93690, #193295, #123070, #42810, #190087, #107851, #90479, #192210, #74220, #140316, #44940, #41740, #189024, #157614, #9211, #141396, #43872, #176000, #108917, #40665, #27592, #75282, #11331, #114257, #162945, #132596, #82738, #14525, #15586, #180253, #97955, #31877, #382, #29743, #147759, #213776, #164011, #95826, #62236, #178127, #80622, #129458, #146712, #65399, #81673, #131546, #197547, #96896, #66455, #198599, #212729, #64367, #128395, #130513, #13470, #161883, #49191, #30817, #115311, #196502, #181301, #50246, #48144, #177054, #32929, #12396, #28671, #94756, #99004, #165059, #16652, #148811, #160805, #78475, #144594, #210608, #194362, #46004, #195441, #112123, #79546, #145664, #211662, #63298, #47071, #113188, #179194, #53434, #88076, #84869, #153075, #202862, #100060, #85944, #182356, #183435, #20909, #168258, #154150, #103262, #35038, #5718, #117440, #19857, #70722, #54509, #169324, #33985, #17708, #136836, #101110, #120654, #167197, #4652, #52378 ),
 ( #184489, #18784, #134721, #152019, #3587, #118506, #69663, #36107, #104335, #150957, #2522, #87003, #186632, #68598, #38259, #119572, #199669, #149890, #200727, #133666, #51313, #135771, #71795, #102191, #185558, #170380, #201794, #37186, #21968, #116368, #166124, #137908, #203928, #83797, #1456, #67521, #140055, #72873, #75028, #56648, #43616, #208208, #189836, #187697, #26261, #172538, #23046, #107595, #24123, #57712, #158414, #122810, #6797, #59840, #40409, #7873, #39324, #105419, #90225, #175742, #125992, #55576, #42556, #156289, #206078, #205002, #138979, #155216, #188769, #159476, #106511, #73961, #207152, #41484, #11074, #27335, #173626, #108659, #58776, #190891, #124929, #93437, #123869, #92380, #10016, #174686, #25197, #91301, #157359, #8951, #141141, #76091, #142194, #191950, #109734, #77152, #143274, #121730, #171457, #89162, #96641, #160544, #162696, #45751, #61986, #15338, #63042, #147509, #129210, #47896, #164809, #46820, #82479, #64118, #44685, #98752, #16401, #81427, #78223, #146459, #209263, #212474, #112935, #60909, #110794, #181056, #176796, #28412, #111870, #114008, #178948, #127067, #196251, #177875, #80362, #14268, #30561, #94506, #29486, #145412, #180003, #130261, #97700, #211413, #193029, #163760, #12151, #194103, #210345, #213529, #197300, #48940, #144345, #128142, #95579, #161628, #13221, #79295, #100865, #38010, #116114, #170131, #3344, #182104, #1210, #69413, #67273, #201541, #185304, #133411, #51061, #150708, #18542, #168006, #135520, #184238, #35865, #103010, #43356, #153897, #123619, #122554, #7616, #22790, #157102, #88908, #154962, #125735, #72625, #109477, #138724, #40145, #205826, #74774, #91042, #24939, #105161, #26004, #6546, #8693, #206889, #73700, #203676, #57457, #55326, #204741, #56391, #189581, #9761, #42293, #188515, #5466, #106259, #171200, #108405, #121477, #139798, #59580, #187448, #191697, #92115, #175487, #87827, #75835, #39075, #107336, #63845, #114793, #159213, #177612, #143010, #112669, #146194, #162429, #61719, #97436, #197040, #93180, #195992, #111603, #95315, #11887, #47627, #77962, #144083, #131052, #161363, #48676, #12947, #145142, #113737, #31360, #163491, #15072, #81164, #213274, #27073, #60644, #35598, #150447, #136326, #86493, #2009, #19344, #167745, #85423, #151509, #4144, #33474, #3076, #69147, #52923, #165612, #49725, #17201, #68076, #50791, #134211, #119055, #185039, #102750, #168806, #200221, #70215, #53996, #51872, #20411, #83276, #152557, #180792, #32416, #98481, #164547, #82217, #204481, #173100, #58269, #122293, #124425, #155772, #21459, #120135, #186113, #24681, #55067, #7356, #37746, #87567, #71281, #121217, #154704, #187186, #72359, #188250, #106001, #38813, #104899, #39891, #23615, #89723, #184662, #52545, #167372, #198772, #67692, #35215, #152187, #153244, #83972, #117614, #100229, #99181, #82910, #18960, #166297, #17888, #148983, #120826, #183606, #116541, #102359, #150061, #87178, #37358, #85044, #16826, #69831, #1633, #66622, #151132, #133838, #101290, #201957, #199849, #50421, #103433, #2699, #68771, #558, #132769, #134891, #4817, #169494, #165233, #3756, #200898, #168431, #20027, #182531, #135939, #119747, #203036, #185725, #21076, #70898, #137009, #54677, #186802, #38431, #156465, #138077, #74141, #56815, #57881, #8051, #5895, #171626 ),
 ( #170555, #188943, #88251, #206256, #25375, #140234, #73046, #108838, #208385, #104511, #124043, #139145, #122985, #187866, #107773, #39495, #105593, #76266, #23220, #60016, #89333, #205173, #190010, #91476, #41660, #173798, #55743, #125108, #155381, #40582, #157537, #24289, #126169, #158593, #90395, #9132, #75207, #141318, #207330, #142375, #6965, #58950, #191066, #42730, #106688, #204090, #172713, #174864, #26443, #92553, #10192, #22138, #154321, #71967, #121899, #84529, #180964, #147418, #32586, #165790, #198263, #17373, #1123, #114964, #150618, #2179, #98663, #82392, #146369, #148481, #31537, #47805, #67185, #48850, #133322, #164718, #33644, #68255, #16307, #195094, #49906, #30471, #18452, #46731, #199325, #64026, #132256, #112843, #116028, #50, #178859, #96555, #166856, #162602, #14178, #97612, #99718, #66113, #80271, #182013, #163669, #83457, #149537, #50971, #212384, #15253, #131222, #117093, #183093, #34705, #197210, #130172, #100774, #196164, #179914, #113918, #81339, #213443, #65066, #69318, #52039, #53093, #3250, #137568, #167918, #20578, #106168, #200391, #188423, #203585, #172195, #7527, #55237, #40059, #187357, #105072, #134388, #118165, #70382, #184151, #87731, #121384, #170037, #168978, #204654, #89890, #35774, #21623, #86662, #4311, #135428, #38987, #201450, #119226, #23784, #185210, #155941, #36834, #152729, #37919, #171110, #22703, #5376, #151680, #6456, #102917, #136498, #71455, #120307, #101848, #19515, #186282, #88816, #154873, #72533, #138631, #85592, #202519, #56303, #122465, #54169, #103993, #153804, #74686, #191609, #60555, #76800, #159129, #90951, #160196, #8602, #174340, #10730, #59490, #95219, #193750, #125647, #126715, #142921, #208921, #192675, #111513, #140787, #44329, #110451, #176452, #206801, #173270, #58434, #43271, #25918, #109391, #28064, #94157, #11798, #77873, #207866, #177519, #161269, #175396, #93088, #24850, #143995, #124587, #190547, #209987, #61629, #127795, #45396, #73610, #139709, #205732, #189495, #41139, #107249, #108320, #92026, #9671, #75747, #164463, #34454, #16049, #213191, #50710, #128839, #199064, #62680, #46456, #63756, #65855, #147164, #100526, #214227, #129916, #82133, #180707, #64818, #112578, #195902, #163407, #132005, #148225, #198015, #14982, #211055, #196956, #178590, #212118, #13922, #48594, #149277, #49643, #162339, #30198, #47538, #96287, #115766, #80002, #113651, #116836, #78930, #66924, #181755, #182837, #12855, #33389, #133066, #99467, #165526, #179655, #31275, #130964, #97350, #17118, #83195, #114712, #858, #22454, #122210, #18190, #202267, #201204, #36583, #101594, #21382, #167662, #19263, #204400, #151426, #188172, #2999, #118978, #85345, #4065, #121139, #38736, #153556, #84275, #67992, #187102, #69068, #104818, #135188, #203334, #168728, #170864, #184957, #52843, #5127, #20330, #70135, #103742, #166601, #183906, #86416, #54987, #152483, #136247, #53918, #120055, #186030, #37666, #169793, #87491, #154624, #71202, #137318, #88566, #6204, #72273, #138382, #56053, #35517, #51795, #39806, #150362, #134134, #9429, #143747, #90706, #175152, #77625, #8354, #190298, #106991, #105912, #73348, #25668, #173016, #24597, #139451, #127543, #91775, #140540, #125395, #206554, #209742, #176211, #75499, #57117, #27813, #58182, #59236, #43027, #109139, #92841, #193514 ),
 ( #32079, #13684, #129671, #194573, #62443, #144811, #46219, #149019, #210818, #98167, #49397, #180463, #64579, #132807, #45155, #163158, #128606, #80835, #63519, #130720, #14743, #12613, #178348, #66660, #114463, #196711, #94972, #48352, #16865, #79754, #81888, #131754, #28888, #146925, #111269, #112336, #164215, #97106, #82945, #15802, #29956, #594, #177272, #99220, #147974, #161018, #78686, #213984, #165270, #65604, #197759, #96042, #162095, #195656, #145870, #212942, #115516, #181511, #211878, #33140, #47290, #113405, #179411, #31032, #68807, #133877, #53650, #199884, #51529, #22179, #183647, #154356, #35251, #151165, #102397, #185763, #201992, #69868, #1672, #70937, #117654, #85081, #135977, #184698, #5935, #104549, #36319, #37395, #119782, #103470, #169532, #88295, #101327, #21112, #87218, #153282, #167408, #84009, #19000, #168465, #2736, #20063, #4858, #137047, #203073, #54717, #118710, #72006, #198811, #86152, #152223, #150100, #3794, #134929, #200934, #120866, #52582, #186840, #38472, #170593, #50457, #116576, #182571, #34193, #100268, #166333, #17925, #67726, #7004, #75243, #159692, #141355, #124084, #175958, #39534, #109948, #187904, #105635, #188979, #191103, #57919, #11291, #125146, #40623, #9168, #91516, #206294, #23259, #106726, #74182, #42771, #207369, #58989, #140275, #121938, #107809, #171663, #123028, #139182, #173834, #60054, #108878, #73081, #55781, #56854, #205212, #174902, #89371, #24328, #27553, #190047, #155420, #25411, #172753, #90436, #156504, #157575, #126209, #26481, #8093, #41699, #92591, #158633, #10230, #76305, #142412, #93649, #204128, #192171, #208420, #138119, #43832, #212689, #131508, #130472, #48105, #165020, #209482, #13431, #127283, #30777, #64331, #113147, #112086, #147721, #32890, #143485, #179153, #178087, #161843, #12355, #146674, #78434, #210565, #115271, #62199, #98968, #128355, #29705, #195402, #196463, #80576, #162904, #94718, #163973, #194323, #95786, #14486, #63257, #61123, #197511, #129419, #114217, #180216, #31838, #97914, #181264, #45965, #15549, #81636, #213738, #79507, #177014, #211622, #47032, #96856, #65361, #49155, #193254, #44901, #111009, #28631, #160761, #120621, #2487, #118472, #182321, #184457, #67486, #83762, #37147, #84836, #169288, #150926, #69628, #186598, #68562, #104299, #85908, #66419, #54476, #38225, #103228, #100025, #168225, #16614, #19823, #134689, #82695, #132562, #202828, #198563, #50212, #133632, #135737, #200693, #148776, #3556, #199634, #102158, #36075, #52344, #116331, #51280, #167165, #201759, #151983, #53400, #119538, #17676, #35005, #185523, #20873, #18752, #86972, #153042, #4617, #117405, #149855, #70689, #136802, #183401, #346, #33950, #166088, #1423, #101077, #187661, #105384, #73928, #208172, #155183, #25164, #9979, #6766, #188737, #171424, #170347, #154113, #24090, #23011, #89128, #5683, #191916, #40376, #39289, #189800, #72840, #158384, #108624, #90195, #88042, #141105, #138945, #137876, #7838, #204966, #172505, #58742, #56613, #121696, #174653, #122777, #106478, #71760, #203896, #156258, #76057, #26227, #21932, #157323, #140020, #206046, #57682, #123839, #55542, #41451, #59804, #107559, #8915, #92344, #91266, #173594, #43582, #74996, #207116, #124894, #190857, #42518, #142156, #125960, #77113, #28372, #131270, #178906, #129169, #159437 ) ),
 .UNSPECIFIED., .T., .F., .T. ) 
 B_SPLINE_SURFACE_WITH_KNOTS ( ( 4, 3, 4 ),
 ( 4, 1, 1, 1, 1, 1, 1, 1, 1, 1, 1, 1, 1, 1, 1, 1, 1, 1, 1, 1, 1, 1, 1, 1, 1, 1, 1, 1, 1, 1, 1, 1, 1, 1, 1, 1, 1, 1, 1, 1, 1, 1, 1, 1, 1, 1, 1, 1, 1, 1, 1, 1, 1, 1, 1, 1, 1, 1, 1, 1, 1, 1, 1, 1, 1, 1, 1, 1, 1, 1, 1, 1, 1, 1, 1, 1, 1, 1, 1, 1, 1, 1, 1, 1, 1, 1, 1, 1, 1, 1, 1, 1, 1, 1, 1, 1, 1, 1, 1, 1, 1, 1, 1, 1, 1, 1, 1, 1, 1, 1, 1, 1, 1, 1, 1, 1, 1, 1, 1, 1, 1, 1, 1, 1, 1, 1, 1, 1, 1, 1, 1, 1, 1, 1, 1, 1, 1, 1, 1, 1, 1, 1, 1, 1, 1, 1, 1, 1, 1, 1, 1, 1, 1, 1, 1, 1, 1, 1, 1, 1, 1, 1, 1, 1, 1, 1, 1, 1, 1, 1, 1, 1, 1, 1, 1, 1, 1, 1, 1, 1, 1, 1, 1, 1, 1, 1, 1, 1, 1, 1, 1, 1, 1, 1, 1, 1, 1, 1, 1, 1, 1, 1, 1, 1, 1, 1, 1, 1, 1, 1, 1, 1, 1, 1, 1, 1, 1, 1, 1, 1, 1, 1, 1, 1, 1, 1, 1, 1, 1, 1, 1, 1, 1, 1, 1, 1, 1, 1, 1, 1, 1, 1, 1, 1, 1, 1, 1, 1, 1, 1, 1, 1, 1, 1, 1, 1, 1, 1, 1, 1, 1, 1, 1, 1, 1, 1, 1, 1, 1, 1, 1, 1, 1, 1, 1, 1, 1, 1, 1, 1, 1, 1, 1, 1, 1, 1, 1, 1, 1, 1, 1, 1, 1, 1, 1, 1, 1, 1, 1, 1, 1, 1, 1, 1, 1, 1, 1, 1, 1, 1, 1, 1, 1, 1, 1, 1, 1, 1, 1, 1, 1, 1, 1, 1, 1, 1, 1, 1, 1, 1, 1, 1, 1, 1, 1, 1, 1, 1, 1, 1, 1, 1, 1, 1, 1, 1, 1, 1, 1, 1, 1, 1, 1, 1, 1, 1, 1, 1, 1, 1, 1, 1, 1, 1, 1, 1, 1, 1, 1, 1, 1, 1, 1, 1, 1, 1, 1, 1, 1, 1, 1, 1, 1, 1, 4 ),
 ( 0.000000000000000000, 0.5000000000000000000, 1.000000000000000000 ),
 ( 0.000000000000000000, 0.002600033395298661284, 0.005208813367820810773, 0.007813200023264601363, 0.01041635779573905213, 0.01302082523971277370, 0.01562491580351430334, 0.01822918961192645723, 0.02083333155136493989, 0.02343746137460561707, 0.02604174567981391505, 0.02864576082122225614, 0.03125012338981237453, 0.03385410379569547823, 0.03645843966640821554, 0.03906250599122108869, 0.04166672065998115043, 0.04427093656960304907, 0.04687500111868234121, 0.04947933663890847350, 0.05208331727515622817, 0.05468767913406928638, 0.05729168951085979872, 0.05989597295159828499, 0.06250011041458469752, 0.06510424634142775169, 0.06770853038940542745, 0.07031253939703428768, 0.07291690072920921362, 0.07552088074063932621, 0.07812521459448035221, 0.08072927904253822395, 0.08333349217322323643, 0.08593770650149938628, 0.08854176936806532061, 0.09114610329512429221, 0.09375008230893774885, 0.09635444258075796797, 0.09895845137230636912, 0.1015627332241899466, 0.1041668691376404637, 0.1067710034717011397, 0.1093752859901425123, 0.1119792934252105548, 0.1145836532378000650, 0.1171876317139315254, 0.1197919640503514460, 0.1223960270027875247, 0.1250002386107842423, 0.1276044514713231270, 0.1302085128224930721, 0.1328128452953424854, 0.1354168228245230532, 0.1380211816480703679, 0.1406251889951717071, 0.1432294693974442978, 0.1458336039016293884, 0.1484377367829480265, 0.1510420179109137340, 0.1536460239143070949, 0.1562503823458506746, 0.1588543594276481397, 0.1614586903853630351, 0.1640627519827278502, 0.1666669622076225599, 0.1692711737400035832, 0.1718752337163205746, 0.1744795648736557347, 0.1770835410591554138, 0.1796878985729436218, 0.1822919046164021839, 0.1848961837081005144, 0.1875003169431251615, 0.1901044485118078553, 0.1927087283883223978, 0.1953127331008320255, 0.1979170902898210183, 0.2005210661182068033, 0.2031253958358791578, 0.2057294562186703923, 0.2083336651999991573, 0.2109378755437518183, 0.2135419342857080849, 0.2161462642661750033, 0.2187502392488957503, 0.2213545955913898966, 0.2239586004719608947, 0.2265628783920732026, 0.2291670104979939837, 0.2317711408940984485, 0.2343754196581391558, 0.2369794232205082452, 0.2395837793053874898, 0.2421877540212369617, 0.2447920826374832270, 0.2473961419461526701, 0.2500003498234057431, 0.2526045591180144934, 0.2552086167660569949, 0.2578129457082574683, 0.2604169196290564980, 0.2630212749386780513, 0.2656252787970727613, 0.2682295556845439854, 0.2708336868013750398, 0.2734378161649161920, 0.2760420939554183439, 0.2786460965083475960, 0.2812504516275206035, 0.2838544253716674404, 0.2864587530250631842, 0.2890628114000217685, 0.2916670183126490179, 0.2942712266975582858, 0.2968752833920936807, 0.2994796114345903981, 0.3020835844342854570, 0.3046879388494173613, 0.3072919418263086455, 0.3098962178200457829, 0.3125003480877632800, 0.3151044765587182606, 0.3177087535145803887, 0.3203127551987332566, 0.3229171094905676220, 0.3255210824038090589, 0.3281254092328941829, 0.3307294668145174810, 0.3333336729019333866, 0.3359378805165532667, 0.3385419363979534357, 0.3411462636792753078, 0.3437502358986498918, 0.3463545895576419231, 0.3489585917936692261, 0.3515628670325462446, 0.3541669965910940188, 0.3567711243094072171, 0.3593754005694961839, 0.3619794015255044517, 0.3645837551283364619, 0.3671877273514386752, 0.3697920534947228832, 0.3723961104233561858, 0.3750003158249449187, 0.3776045228086560845, 0.3802085780172632101, 0.3828129046759103926, 0.3854168762557192984, 0.3880212292968930887, 0.3906252309326675998, 0.3932295055555311003, 0.3958336345448258409, 0.3984377616504144459, 0.4010420373535708016, 0.4036460377220391638, 0.4062503907741795706, 0.4088543624478828686, 0.4114586880438503846, 0.4140627444598136697, 0.4166669493149349202, 0.4192711558070936761, 0.4218752104832254046, 0.4244795366576747386, 0.4270835077386489487, 0.4296878603003031483, 0.4322918614764136302, 0.4348961356220873986, 0.4375002641820237570, 0.4401043908147829753, 0.4427086660998260093, 0.4453126660213379551, 0.4479170186610768045, 0.4505209899261007900, 0.4531253151132156320, 0.4557293711568096706, 0.4583335756048029785, 0.4609377817447468106, 0.4635418360287018591, 0.4661461618574116450, 0.4687501325802634344, 0.4713544848006788190, 0.4739584856576960492, 0.4765627594649867738, 0.4791668877354426925, 0.4817710140352507997, 0.4843752890409837031, 0.4869792886561065681, 0.4895836410217184742, 0.4921876120187673176, 0.4947919369354787933, 0.4973959927469893683, 0.5000001969271801183, 0.5026044028542325792, 0.5052084568862954539, 0.5078127825077110025, 0.5104167530131399344, 0.5130211050305848453, 0.5156251057090676104, 0.5182293793167697116, 0.5208335074376115870, 0.5234376335443351458, 0.5260419084095501185, 0.5286459078588399141, 0.5312502600885893322, 0.5338542309583571566, 0.5364585557431046370, 0.5390626114628084276, 0.5416668155145124564, 0.5442710213679887721, 0.5468750752884355970, 0.5494794008409938924, 0.5520833712696913143, 0.5546877232224267651, 0.5572917238629264691, 0.5598959974098275394, 0.5625001255209155504, 0.5651042515744146844, 0.5677085264378984863, 0.5703125258619060611, 0.5729168780940517847, 0.5755208489772277725, 0.5781251737684461878, 0.5807292295366155432, 0.5833334335991446906, 0.5859376395183565345, 0.5885416934674594369, 0.5911460190895951872, 0.5937499895822500040, 0.5963543416085342885, 0.5989583423516006144, 0.6015626159764864145, 0.6041667442176794633, 0.6067708703578130747, 0.6093751453583519107, 0.6119791448976270587, 0.6145834972704286026, 0.6171874683077025470, 0.6197917932438269384, 0.6223958492007358734, 0.6250000534134032559, 0.6276042595376638555, 0.6302083136556971832, 0.6328126394858472059, 0.6354166101831504321, 0.6380209624212449526, 0.6406249634074311361, 0.6432292372490908683, 0.6458333657602520761, 0.6484374921268833969, 0.6510417674032679125, 0.6536457671983656459, 0.6562501198500874100, 0.6588540911821543222, 0.6614584164016259482, 0.6640624726875546946, 0.6666666771896793131, 0.6692708836583093346, 0.6718749380855545406, 0.6744792642621626477, 0.6770832353048136243, 0.6796875878929879988, 0.6822915892628557133, 0.6848958634600870177, 0.6874999923810890534, 0.6901041191140900866, 0.6927083948051209195, 0.6953123949966061312, 0.6979167480655225075, 0.7005207198330885010, 0.7031250454743595002, 0.7057291022295995031, 0.7083333071605121267, 0.7109375141128444486, 0.7135415689895947544, 0.7161458956511181917, 0.7187498671798290273, 0.7213542202563657524, 0.7239582221504904380, 0.7265624968421051655, 0.7291666263128349090, 0.7317707535520923123, 0.7343750297965853102, 0.7369790305250381035, 0.7395833841494394711, 0.7421873564932268685, 0.7447916826947649227, 0.7473957400596251688, 0.7499999455586733310, 0.7526041531340577073, 0.7552082086006238759, 0.7578125358855373195, 0.7604165080410384414, 0.7630208617442386654, 0.7656248643032155243, 0.7682291396280439555, 0.7708332697884082707, 0.7734373976738285750, 0.7760416746106194585, 0.7786456760166404756, 0.7812500303348380859, 0.7838540033955903041, 0.7864583302958847444, 0.7890623884106959807, 0.7916665946172487534, 0.7942708029550582527, 0.7968748591517740287, 0.7994791871985751364, 0.8020831601216208417, 0.8046875145898089166, 0.8072915179542569097, 0.8098957940511537501, 0.8124999250410844809, 0.8151040537125986418, 0.8177083314805486669, 0.8203123337047645292, 0.8229166888550945025, 0.8255206627735817149, 0.8281249905111484066, 0.8307290495162685806, 0.8333332565697225691, 0.8359374658093579047, 0.8385415228765847884, 0.8411458518237998616, 0.8437498256551729803, 0.8463541810267020127, 0.8489581853372698550, 0.8515624623451190089, 0.8541665943045783083, 0.8567707239021479237, 0.8593750026401490993, 0.8619790058232168484, 0.8645833619440471685, 0.8671873368610717447, 0.8697916655744575287, 0.8723957256102774505, 0.8749999336500613456, 0.8776041439309557601, 0.8802082020090884473, 0.8828125319952765393, 0.8854165068757942070, 0.8880208632890512765, 0.8906248686864229880, 0.8932291467441429988, 0.8958332798131283248, 0.8984374104767501867, 0.9010416903237299380, 0.9036456946063434748, 0.9062500518360779855, 0.9088540278924787108, 0.9114583577202677311, 0.9140624189272162914, 0.9166666280927961985, 0.9192708395544209043, 0.9218748987838942810, 0.9244792299476556341, 0.9270832060181642964, 0.9296875636115721209, 0.9322915702365133228, 0.9348958494830461596, 0.9374999838014769216, 0.9401041156712998115, 0.9427083967663798525, 0.9453124022892170908, 0.9479167607665550666, 0.9505207380999710631, 0.9531250691809918241, 0.9557291317261836783, 0.9583333421310490374, 0.9609375547886240820, 0.9635416155522130710, 0.9661459483928183101, 0.9687499245033458495, 0.9713542829945021051, 0.9739582954330652242, 0.9765625745907361432, 0.9791667024412501474, 0.9817708385604039245, 0.9843751096149007118, 0.9869791944699233266, 0.9895836584107432499, 0.9921868132917668337, 0.9947911946869415489, 0.9973999724172807335, 1.000000000000000000 ),
 .UNSPECIFIED. ) 
 GEOMETRIC_REPRESENTATION_ITEM ( )  RATIONAL_B_SPLINE_SURFACE ( (
 ( 1.000000000000000000, 1.000000000000000000, 1.000000000000000000, 0.9999999999999997780, 1.000000000000000000, 1.000000000000000000, 1.000000000000000000, 1.000000000000000222, 1.000000000000000000, 1.000000000000000000, 1.000000000000000222, 0.9999999999999997780, 1.000000000000000222, 1.000000000000000222, 1.000000000000000000, 1.000000000000000000, 1.000000000000000000, 0.9999999999999997780, 1.000000000000000222, 0.9999999999999996669, 1.000000000000000222, 1.000000000000000000, 1.000000000000000000, 0.9999999999999996669, 1.000000000000000444, 0.9999999999999996669, 1.000000000000000444, 1.000000000000000000, 1.000000000000000000, 0.9999999999999997780, 1.000000000000000222, 0.9999999999999994449, 1.000000000000000444, 1.000000000000000000, 1.000000000000000000, 1.000000000000000000, 1.000000000000000000, 1.000000000000000444, 0.9999999999999997780, 1.000000000000000000, 1.000000000000000000, 1.000000000000000000, 1.000000000000000000, 1.000000000000000000, 1.000000000000000000, 0.9999999999999997780, 1.000000000000000000, 1.000000000000000444, 0.9999999999999997780, 1.000000000000000444, 0.9999999999999997780, 0.9999999999999997780, 1.000000000000000000, 1.000000000000000222, 1.000000000000000000, 1.000000000000000000, 1.000000000000000000, 1.000000000000000000, 0.9999999999999997780, 1.000000000000000444, 0.9999999999999997780, 1.000000000000000000, 1.000000000000000222, 0.9999999999999997780, 1.000000000000000000, 1.000000000000000222, 0.9999999999999997780, 1.000000000000000222, 1.000000000000000000, 1.000000000000000222, 1.000000000000000000, 1.000000000000000222, 0.9999999999999997780, 1.000000000000000000, 1.000000000000000222, 1.000000000000000000, 1.000000000000000222, 0.9999999999999997780, 1.000000000000000222, 0.9999999999999997780, 1.000000000000000222, 0.9999999999999997780, 1.000000000000000222, 1.000000000000000222, 0.9999999999999997780, 1.000000000000000222, 1.000000000000000222, 0.9999999999999997780, 1.000000000000000222, 1.000000000000000000, 1.000000000000000000, 1.000000000000000222, 0.9999999999999996669, 1.000000000000000444, 0.9999999999999997780, 0.9999999999999997780, 1.000000000000000000, 1.000000000000000000, 1.000000000000000000, 0.9999999999999996669, 1.000000000000000444, 1.000000000000000000, 1.000000000000000222, 1.000000000000000000, 0.9999999999999997780, 1.000000000000000222, 0.9999999999999997780, 1.000000000000000222, 1.000000000000000000, 1.000000000000000000, 1.000000000000000222, 1.000000000000000000, 1.000000000000000222, 0.9999999999999994449, 1.000000000000000444, 1.000000000000000000, 0.9999999999999996669, 1.000000000000000222, 0.9999999999999997780, 1.000000000000000222, 0.9999999999999997780, 1.000000000000000000, 1.000000000000000000, 1.000000000000000000, 1.000000000000000000, 1.000000000000000000, 1.000000000000000444, 1.000000000000000000, 1.000000000000000000, 1.000000000000000222, 1.000000000000000000, 1.000000000000000000, 0.9999999999999997780, 1.000000000000000000, 1.000000000000000222, 1.000000000000000000, 1.000000000000000222, 0.9999999999999997780, 1.000000000000000000, 0.9999999999999997780, 0.9999999999999997780, 1.000000000000000222, 0.9999999999999997780, 1.000000000000000444, 0.9999999999999997780, 1.000000000000000000, 1.000000000000000222, 1.000000000000000000, 1.000000000000000000, 0.9999999999999997780, 1.000000000000000222, 1.000000000000000000, 1.000000000000000000, 1.000000000000000000, 1.000000000000000222, 0.9999999999999996669, 1.000000000000000222, 1.000000000000000222, 0.9999999999999996669, 1.000000000000000444, 0.9999999999999996669, 1.000000000000000000, 1.000000000000000222, 0.9999999999999996669, 1.000000000000000222, 1.000000000000000000, 1.000000000000000222, 1.000000000000000000, 1.000000000000000222, 0.9999999999999997780, 1.000000000000000444, 0.9999999999999997780, 0.9999999999999997780, 1.000000000000000222, 0.9999999999999996669, 1.000000000000000222, 1.000000000000000000, 1.000000000000000000, 1.000000000000000000, 0.9999999999999997780, 1.000000000000000222, 1.000000000000000222, 0.9999999999999997780, 1.000000000000000222, 0.9999999999999997780, 1.000000000000000222, 1.000000000000000000, 1.000000000000000444, 1.000000000000000000, 1.000000000000000222, 0.9999999999999996669, 1.000000000000000444, 0.9999999999999993339, 1.000000000000000444, 0.9999999999999997780, 1.000000000000000444, 0.9999999999999997780, 1.000000000000000000, 1.000000000000000000, 0.9999999999999997780, 1.000000000000000222, 0.9999999999999997780, 0.9999999999999996669, 1.000000000000000444, 1.000000000000000222, 1.000000000000000000, 0.9999999999999997780, 1.000000000000000222, 0.9999999999999996669, 1.000000000000000222, 0.9999999999999997780, 1.000000000000000222, 1.000000000000000000, 1.000000000000000000, 1.000000000000000000, 1.000000000000000000, 0.9999999999999997780, 1.000000000000000000, 1.000000000000000000, 0.9999999999999997780, 1.000000000000000000, 1.000000000000000000, 1.000000000000000000, 1.000000000000000222, 1.000000000000000000, 1.000000000000000444, 1.000000000000000222, 1.000000000000000000, 1.000000000000000000, 0.9999999999999997780, 1.000000000000000222, 1.000000000000000000, 1.000000000000000000, 1.000000000000000000, 0.9999999999999997780, 1.000000000000000222, 0.9999999999999997780, 1.000000000000000222, 1.000000000000000444, 0.9999999999999997780, 1.000000000000000222, 1.000000000000000000, 1.000000000000000000, 1.000000000000000000, 0.9999999999999997780, 1.000000000000000444, 0.9999999999999997780, 1.000000000000000222, 0.9999999999999997780, 1.000000000000000222, 0.9999999999999994449, 1.000000000000000222, 1.000000000000000000, 1.000000000000000222, 1.000000000000000000, 0.9999999999999997780, 1.000000000000000222, 1.000000000000000000, 0.9999999999999997780, 1.000000000000000444, 0.9999999999999996669, 1.000000000000000222, 1.000000000000000000, 1.000000000000000000, 1.000000000000000222, 0.9999999999999997780, 0.9999999999999997780, 1.000000000000000444, 1.000000000000000222, 1.000000000000000000, 0.9999999999999997780, 0.9999999999999997780, 1.000000000000000222, 1.000000000000000000, 1.000000000000000222, 1.000000000000000000, 0.9999999999999997780, 1.000000000000000000, 1.000000000000000000, 1.000000000000000000, 1.000000000000000222, 0.9999999999999997780, 1.000000000000000222, 1.000000000000000000, 1.000000000000000000, 1.000000000000000000, 0.9999999999999997780, 1.000000000000000000, 1.000000000000000222, 1.000000000000000222, 0.9999999999999996669, 1.000000000000000444, 0.9999999999999996669, 1.000000000000000222, 1.000000000000000000, 1.000000000000000222, 0.9999999999999997780, 1.000000000000000444, 1.000000000000000000, 1.000000000000000444, 0.9999999999999994449, 1.000000000000000222, 0.9999999999999997780, 0.9999999999999997780, 1.000000000000000000, 1.000000000000000222, 1.000000000000000000, 1.000000000000000000, 1.000000000000000000, 1.000000000000000222, 0.9999999999999996669, 1.000000000000000222, 1.000000000000000000, 0.9999999999999996669, 1.000000000000000444, 1.000000000000000000, 1.000000000000000000, 1.000000000000000000, 0.9999999999999996669, 1.000000000000000222, 1.000000000000000000, 1.000000000000000000, 1.000000000000000222, 0.9999999999999997780, 0.9999999999999997780, 1.000000000000000000, 1.000000000000000000, 1.000000000000000222, 0.9999999999999997780, 1.000000000000000222, 1.000000000000000000, 1.000000000000000000, 0.9999999999999996669, 1.000000000000000222, 1.000000000000000000, 1.000000000000000222, 1.000000000000000000, 1.000000000000000000, 1.000000000000000000, 0.9999999999999997780, 1.000000000000000222, 0.9999999999999996669, 1.000000000000000444, 1.000000000000000000, 0.9999999999999997780, 1.000000000000000000, 1.000000000000000222, 1.000000000000000222, 0.9999999999999996669, 1.000000000000000000, 1.000000000000000000, 0.9999999999999997780, 1.000000000000000222, 1.000000000000000000, 1.000000000000000222, 0.9999999999999996669, 1.000000000000000444, 1.000000000000000000, 1.000000000000000000, 1.000000000000000000, 1.000000000000000222, 1.000000000000000000, 0.9999999999999997780, 1.000000000000000444, 1.000000000000000000, 1.000000000000000444, 0.9999999999999997780, 1.000000000000000444, 1.000000000000000000, 1.000000000000000222, 1.000000000000000222, 1.000000000000000000, 0.9999999999999996669, 1.000000000000000000, 1.000000000000000000, 1.000000000000000000, 1.000000000000000000, 1.000000000000000222, 0.9999999999999996669, 1.000000000000000000, 1.000000000000000222, 0.9999999999999997780, 0.9999999999999997780, 1.000000000000000000, 1.000000000000000000, 1.000000000000000000, 1.000000000000000000),
 ( 0.3333333333333333703, 0.3333333333333333703, 0.3333333333333333703, 0.3333333333333333148, 0.3333333333333333703, 0.3333333333333333148, 0.3333333333333333703, 0.3333333333333334259, 0.3333333333333333703, 0.3333333333333333148, 0.3333333333333334259, 0.3333333333333332593, 0.3333333333333334259, 0.3333333333333333703, 0.3333333333333333703, 0.3333333333333332593, 0.3333333333333334259, 0.3333333333333333148, 0.3333333333333334259, 0.3333333333333333148, 0.3333333333333334259, 0.3333333333333334259, 0.3333333333333333148, 0.3333333333333333148, 0.3333333333333334814, 0.3333333333333332593, 0.3333333333333334259, 0.3333333333333334259, 0.3333333333333333703, 0.3333333333333333703, 0.3333333333333334814, 0.3333333333333332038, 0.3333333333333334814, 0.3333333333333333703, 0.3333333333333334259, 0.3333333333333333148, 0.3333333333333334259, 0.3333333333333334814, 0.3333333333333333703, 0.3333333333333332593, 0.3333333333333334259, 0.3333333333333333148, 0.3333333333333333148, 0.3333333333333333703, 0.3333333333333333703, 0.3333333333333334259, 0.3333333333333333148, 0.3333333333333335369, 0.3333333333333333148, 0.3333333333333334259, 0.3333333333333333703, 0.3333333333333332038, 0.3333333333333334259, 0.3333333333333334259, 0.3333333333333333148, 0.3333333333333334259, 0.3333333333333333703, 0.3333333333333333703, 0.3333333333333334259, 0.3333333333333334259, 0.3333333333333333703, 0.3333333333333334259, 0.3333333333333334259, 0.3333333333333333148, 0.3333333333333333703, 0.3333333333333333703, 0.3333333333333333148, 0.3333333333333334259, 0.3333333333333333148, 0.3333333333333334814, 0.3333333333333333703, 0.3333333333333334259, 0.3333333333333333148, 0.3333333333333333703, 0.3333333333333334259, 0.3333333333333333703, 0.3333333333333333703, 0.3333333333333333148, 0.3333333333333334259, 0.3333333333333333148, 0.3333333333333334259, 0.3333333333333333703, 0.3333333333333334259, 0.3333333333333334814, 0.3333333333333333148, 0.3333333333333334259, 0.3333333333333334259, 0.3333333333333333148, 0.3333333333333333703, 0.3333333333333333703, 0.3333333333333333148, 0.3333333333333334814, 0.3333333333333332593, 0.3333333333333334259, 0.3333333333333333703, 0.3333333333333333148, 0.3333333333333333703, 0.3333333333333333703, 0.3333333333333334259, 0.3333333333333333148, 0.3333333333333334259, 0.3333333333333333148, 0.3333333333333334814, 0.3333333333333333148, 0.3333333333333333148, 0.3333333333333334259, 0.3333333333333333148, 0.3333333333333333703, 0.3333333333333333703, 0.3333333333333334259, 0.3333333333333333703, 0.3333333333333334259, 0.3333333333333333703, 0.3333333333333332593, 0.3333333333333334259, 0.3333333333333333703, 0.3333333333333333148, 0.3333333333333334814, 0.3333333333333333148, 0.3333333333333334259, 0.3333333333333334259, 0.3333333333333333148, 0.3333333333333333703, 0.3333333333333334259, 0.3333333333333333703, 0.3333333333333333703, 0.3333333333333334259, 0.3333333333333333703, 0.3333333333333334259, 0.3333333333333333703, 0.3333333333333334259, 0.3333333333333333148, 0.3333333333333333703, 0.3333333333333333703, 0.3333333333333333703, 0.3333333333333333703, 0.3333333333333335369, 0.3333333333333332593, 0.3333333333333333703, 0.3333333333333333703, 0.3333333333333332593, 0.3333333333333333703, 0.3333333333333333703, 0.3333333333333334259, 0.3333333333333332593, 0.3333333333333333703, 0.3333333333333333703, 0.3333333333333333703, 0.3333333333333333703, 0.3333333333333333703, 0.3333333333333334259, 0.3333333333333333148, 0.3333333333333334259, 0.3333333333333333703, 0.3333333333333334814, 0.3333333333333332593, 0.3333333333333333703, 0.3333333333333334814, 0.3333333333333332038, 0.3333333333333334259, 0.3333333333333333148, 0.3333333333333333703, 0.3333333333333334814, 0.3333333333333332038, 0.3333333333333334259, 0.3333333333333333703, 0.3333333333333333703, 0.3333333333333333703, 0.3333333333333334259, 0.3333333333333333703, 0.3333333333333335369, 0.3333333333333333148, 0.3333333333333333148, 0.3333333333333334259, 0.3333333333333333148, 0.3333333333333333703, 0.3333333333333333703, 0.3333333333333334259, 0.3333333333333333148, 0.3333333333333334259, 0.3333333333333332593, 0.3333333333333334814, 0.3333333333333333703, 0.3333333333333333703, 0.3333333333333333703, 0.3333333333333333703, 0.3333333333333333703, 0.3333333333333334259, 0.3333333333333333703, 0.3333333333333334259, 0.3333333333333333148, 0.3333333333333335369, 0.3333333333333332038, 0.3333333333333335369, 0.3333333333333333148, 0.3333333333333334259, 0.3333333333333333703, 0.3333333333333333148, 0.3333333333333334259, 0.3333333333333333148, 0.3333333333333334259, 0.3333333333333332593, 0.3333333333333333148, 0.3333333333333334259, 0.3333333333333334814, 0.3333333333333333703, 0.3333333333333333703, 0.3333333333333334259, 0.3333333333333333148, 0.3333333333333333703, 0.3333333333333333148, 0.3333333333333334259, 0.3333333333333333148, 0.3333333333333333703, 0.3333333333333333703, 0.3333333333333334259, 0.3333333333333333148, 0.3333333333333334259, 0.3333333333333333703, 0.3333333333333333148, 0.3333333333333332593, 0.3333333333333334259, 0.3333333333333333148, 0.3333333333333334259, 0.3333333333333334259, 0.3333333333333334814, 0.3333333333333334259, 0.3333333333333333703, 0.3333333333333333703, 0.3333333333333333148, 0.3333333333333334259, 0.3333333333333333703, 0.3333333333333334259, 0.3333333333333333148, 0.3333333333333333703, 0.3333333333333333703, 0.3333333333333332593, 0.3333333333333334259, 0.3333333333333335369, 0.3333333333333333148, 0.3333333333333334814, 0.3333333333333333703, 0.3333333333333333148, 0.3333333333333334259, 0.3333333333333332593, 0.3333333333333334814, 0.3333333333333333148, 0.3333333333333333703, 0.3333333333333333148, 0.3333333333333334259, 0.3333333333333333148, 0.3333333333333334259, 0.3333333333333333148, 0.3333333333333333703, 0.3333333333333333703, 0.3333333333333333148, 0.3333333333333334259, 0.3333333333333333703, 0.3333333333333333703, 0.3333333333333335369, 0.3333333333333332038, 0.3333333333333334814, 0.3333333333333333148, 0.3333333333333334259, 0.3333333333333334259, 0.3333333333333333703, 0.3333333333333333148, 0.3333333333333334814, 0.3333333333333333703, 0.3333333333333333703, 0.3333333333333333703, 0.3333333333333333703, 0.3333333333333333703, 0.3333333333333334259, 0.3333333333333333703, 0.3333333333333334259, 0.3333333333333333148, 0.3333333333333333703, 0.3333333333333334259, 0.3333333333333334259, 0.3333333333333333703, 0.3333333333333333703, 0.3333333333333334259, 0.3333333333333333703, 0.3333333333333333148, 0.3333333333333333148, 0.3333333333333333703, 0.3333333333333333703, 0.3333333333333334259, 0.3333333333333334259, 0.3333333333333333703, 0.3333333333333333703, 0.3333333333333333703, 0.3333333333333333703, 0.3333333333333333703, 0.3333333333333333148, 0.3333333333333334259, 0.3333333333333334259, 0.3333333333333333703, 0.3333333333333335369, 0.3333333333333332038, 0.3333333333333334814, 0.3333333333333332593, 0.3333333333333333703, 0.3333333333333332593, 0.3333333333333334814, 0.3333333333333333148, 0.3333333333333333703, 0.3333333333333334259, 0.3333333333333334259, 0.3333333333333332593, 0.3333333333333334259, 0.3333333333333333148, 0.3333333333333333703, 0.3333333333333334259, 0.3333333333333334814, 0.3333333333333333148, 0.3333333333333334259, 0.3333333333333333148, 0.3333333333333334814, 0.3333333333333334259, 0.3333333333333333703, 0.3333333333333334259, 0.3333333333333332593, 0.3333333333333333148, 0.3333333333333333703, 0.3333333333333333703, 0.3333333333333334259, 0.3333333333333333703, 0.3333333333333334259, 0.3333333333333333703, 0.3333333333333334259, 0.3333333333333333148, 0.3333333333333333703, 0.3333333333333334259, 0.3333333333333334259, 0.3333333333333333703, 0.3333333333333333703, 0.3333333333333333703, 0.3333333333333333148, 0.3333333333333333703, 0.3333333333333333148, 0.3333333333333334259, 0.3333333333333334259, 0.3333333333333333148, 0.3333333333333333703, 0.3333333333333334259, 0.3333333333333333703, 0.3333333333333333148, 0.3333333333333333703, 0.3333333333333333148, 0.3333333333333333703, 0.3333333333333334259, 0.3333333333333333148, 0.3333333333333334259, 0.3333333333333332593, 0.3333333333333334814, 0.3333333333333334814, 0.3333333333333333148, 0.3333333333333333703, 0.3333333333333334814, 0.3333333333333333148, 0.3333333333333333703, 0.3333333333333334814, 0.3333333333333333703, 0.3333333333333334259, 0.3333333333333334259, 0.3333333333333334814, 0.3333333333333333703, 0.3333333333333333703, 0.3333333333333333703, 0.3333333333333333148, 0.3333333333333333148, 0.3333333333333333703, 0.3333333333333333703, 0.3333333333333333703, 0.3333333333333334259, 0.3333333333333334259, 0.3333333333333333148, 0.3333333333333333148, 0.3333333333333334814, 0.3333333333333333148, 0.3333333333333333148, 0.3333333333333333703, 0.3333333333333333703, 0.3333333333333333703, 0.3333333333333333703),
 ( 0.3333333333333333703, 0.3333333333333333703, 0.3333333333333333703, 0.3333333333333333148, 0.3333333333333333703, 0.3333333333333333148, 0.3333333333333333703, 0.3333333333333334259, 0.3333333333333333703, 0.3333333333333333148, 0.3333333333333334259, 0.3333333333333332593, 0.3333333333333334259, 0.3333333333333333703, 0.3333333333333333703, 0.3333333333333332593, 0.3333333333333334259, 0.3333333333333333148, 0.3333333333333334259, 0.3333333333333333148, 0.3333333333333334259, 0.3333333333333334259, 0.3333333333333333148, 0.3333333333333333148, 0.3333333333333334814, 0.3333333333333332593, 0.3333333333333334259, 0.3333333333333334259, 0.3333333333333333703, 0.3333333333333333703, 0.3333333333333334814, 0.3333333333333332038, 0.3333333333333334814, 0.3333333333333333703, 0.3333333333333334259, 0.3333333333333333148, 0.3333333333333334259, 0.3333333333333334814, 0.3333333333333333703, 0.3333333333333332593, 0.3333333333333334259, 0.3333333333333333148, 0.3333333333333333148, 0.3333333333333333703, 0.3333333333333333703, 0.3333333333333334259, 0.3333333333333333148, 0.3333333333333335369, 0.3333333333333333148, 0.3333333333333334259, 0.3333333333333333703, 0.3333333333333332038, 0.3333333333333334259, 0.3333333333333334259, 0.3333333333333333148, 0.3333333333333334259, 0.3333333333333333703, 0.3333333333333333703, 0.3333333333333334259, 0.3333333333333334259, 0.3333333333333333703, 0.3333333333333334259, 0.3333333333333334259, 0.3333333333333333148, 0.3333333333333333703, 0.3333333333333333703, 0.3333333333333333148, 0.3333333333333334259, 0.3333333333333333148, 0.3333333333333334814, 0.3333333333333333703, 0.3333333333333334259, 0.3333333333333333148, 0.3333333333333333703, 0.3333333333333334259, 0.3333333333333333703, 0.3333333333333333703, 0.3333333333333333148, 0.3333333333333334259, 0.3333333333333333148, 0.3333333333333334259, 0.3333333333333333703, 0.3333333333333334259, 0.3333333333333334814, 0.3333333333333333148, 0.3333333333333334259, 0.3333333333333334259, 0.3333333333333333148, 0.3333333333333333703, 0.3333333333333333703, 0.3333333333333333148, 0.3333333333333334814, 0.3333333333333332593, 0.3333333333333334259, 0.3333333333333333703, 0.3333333333333333148, 0.3333333333333333703, 0.3333333333333333703, 0.3333333333333334259, 0.3333333333333333148, 0.3333333333333334259, 0.3333333333333333148, 0.3333333333333334814, 0.3333333333333333148, 0.3333333333333333148, 0.3333333333333334259, 0.3333333333333333148, 0.3333333333333333703, 0.3333333333333333703, 0.3333333333333334259, 0.3333333333333333703, 0.3333333333333334259, 0.3333333333333333703, 0.3333333333333332593, 0.3333333333333334259, 0.3333333333333333703, 0.3333333333333333148, 0.3333333333333334814, 0.3333333333333333148, 0.3333333333333334259, 0.3333333333333334259, 0.3333333333333333148, 0.3333333333333333703, 0.3333333333333334259, 0.3333333333333333703, 0.3333333333333333703, 0.3333333333333334259, 0.3333333333333333703, 0.3333333333333334259, 0.3333333333333333703, 0.3333333333333334259, 0.3333333333333333148, 0.3333333333333333703, 0.3333333333333333703, 0.3333333333333333703, 0.3333333333333333703, 0.3333333333333335369, 0.3333333333333332593, 0.3333333333333333703, 0.3333333333333333703, 0.3333333333333332593, 0.3333333333333333703, 0.3333333333333333703, 0.3333333333333334259, 0.3333333333333332593, 0.3333333333333333703, 0.3333333333333333703, 0.3333333333333333703, 0.3333333333333333703, 0.3333333333333333703, 0.3333333333333334259, 0.3333333333333333148, 0.3333333333333334259, 0.3333333333333333703, 0.3333333333333334814, 0.3333333333333332593, 0.3333333333333333703, 0.3333333333333334814, 0.3333333333333332038, 0.3333333333333334259, 0.3333333333333333148, 0.3333333333333333703, 0.3333333333333334814, 0.3333333333333332038, 0.3333333333333334259, 0.3333333333333333703, 0.3333333333333333703, 0.3333333333333333703, 0.3333333333333334259, 0.3333333333333333703, 0.3333333333333335369, 0.3333333333333333148, 0.3333333333333333148, 0.3333333333333334259, 0.3333333333333333148, 0.3333333333333333703, 0.3333333333333333703, 0.3333333333333334259, 0.3333333333333333148, 0.3333333333333334259, 0.3333333333333332593, 0.3333333333333334814, 0.3333333333333333703, 0.3333333333333333703, 0.3333333333333333703, 0.3333333333333333703, 0.3333333333333333703, 0.3333333333333334259, 0.3333333333333333703, 0.3333333333333334259, 0.3333333333333333148, 0.3333333333333335369, 0.3333333333333332038, 0.3333333333333335369, 0.3333333333333333148, 0.3333333333333334259, 0.3333333333333333703, 0.3333333333333333148, 0.3333333333333334259, 0.3333333333333333148, 0.3333333333333334259, 0.3333333333333332593, 0.3333333333333333148, 0.3333333333333334259, 0.3333333333333334814, 0.3333333333333333703, 0.3333333333333333703, 0.3333333333333334259, 0.3333333333333333148, 0.3333333333333333703, 0.3333333333333333148, 0.3333333333333334259, 0.3333333333333333148, 0.3333333333333333703, 0.3333333333333333703, 0.3333333333333334259, 0.3333333333333333148, 0.3333333333333334259, 0.3333333333333333703, 0.3333333333333333148, 0.3333333333333332593, 0.3333333333333334259, 0.3333333333333333148, 0.3333333333333334259, 0.3333333333333334259, 0.3333333333333334814, 0.3333333333333334259, 0.3333333333333333703, 0.3333333333333333703, 0.3333333333333333148, 0.3333333333333334259, 0.3333333333333333703, 0.3333333333333334259, 0.3333333333333333148, 0.3333333333333333703, 0.3333333333333333703, 0.3333333333333332593, 0.3333333333333334259, 0.3333333333333335369, 0.3333333333333333148, 0.3333333333333334814, 0.3333333333333333703, 0.3333333333333333148, 0.3333333333333334259, 0.3333333333333332593, 0.3333333333333334814, 0.3333333333333333148, 0.3333333333333333703, 0.3333333333333333148, 0.3333333333333334259, 0.3333333333333333148, 0.3333333333333334259, 0.3333333333333333148, 0.3333333333333333703, 0.3333333333333333703, 0.3333333333333333148, 0.3333333333333334259, 0.3333333333333333703, 0.3333333333333333703, 0.3333333333333335369, 0.3333333333333332038, 0.3333333333333334814, 0.3333333333333333148, 0.3333333333333334259, 0.3333333333333334259, 0.3333333333333333703, 0.3333333333333333148, 0.3333333333333334814, 0.3333333333333333703, 0.3333333333333333703, 0.3333333333333333703, 0.3333333333333333703, 0.3333333333333333703, 0.3333333333333334259, 0.3333333333333333703, 0.3333333333333334259, 0.3333333333333333148, 0.3333333333333333703, 0.3333333333333334259, 0.3333333333333334259, 0.3333333333333333703, 0.3333333333333333703, 0.3333333333333334259, 0.3333333333333333703, 0.3333333333333333148, 0.3333333333333333148, 0.3333333333333333703, 0.3333333333333333703, 0.3333333333333334259, 0.3333333333333334259, 0.3333333333333333703, 0.3333333333333333703, 0.3333333333333333703, 0.3333333333333333703, 0.3333333333333333703, 0.3333333333333333148, 0.3333333333333334259, 0.3333333333333334259, 0.3333333333333333703, 0.3333333333333335369, 0.3333333333333332038, 0.3333333333333334814, 0.3333333333333332593, 0.3333333333333333703, 0.3333333333333332593, 0.3333333333333334814, 0.3333333333333333148, 0.3333333333333333703, 0.3333333333333334259, 0.3333333333333334259, 0.3333333333333332593, 0.3333333333333334259, 0.3333333333333333148, 0.3333333333333333703, 0.3333333333333334259, 0.3333333333333334814, 0.3333333333333333148, 0.3333333333333334259, 0.3333333333333333148, 0.3333333333333334814, 0.3333333333333334259, 0.3333333333333333703, 0.3333333333333334259, 0.3333333333333332593, 0.3333333333333333148, 0.3333333333333333703, 0.3333333333333333703, 0.3333333333333334259, 0.3333333333333333703, 0.3333333333333334259, 0.3333333333333333703, 0.3333333333333334259, 0.3333333333333333148, 0.3333333333333333703, 0.3333333333333334259, 0.3333333333333334259, 0.3333333333333333703, 0.3333333333333333703, 0.3333333333333333703, 0.3333333333333333148, 0.3333333333333333703, 0.3333333333333333148, 0.3333333333333334259, 0.3333333333333334259, 0.3333333333333333148, 0.3333333333333333703, 0.3333333333333334259, 0.3333333333333333703, 0.3333333333333333148, 0.3333333333333333703, 0.3333333333333333148, 0.3333333333333333703, 0.3333333333333334259, 0.3333333333333333148, 0.3333333333333334259, 0.3333333333333332593, 0.3333333333333334814, 0.3333333333333334814, 0.3333333333333333148, 0.3333333333333333703, 0.3333333333333334814, 0.3333333333333333148, 0.3333333333333333703, 0.3333333333333334814, 0.3333333333333333703, 0.3333333333333334259, 0.3333333333333334259, 0.3333333333333334814, 0.3333333333333333703, 0.3333333333333333703, 0.3333333333333333703, 0.3333333333333333148, 0.3333333333333333148, 0.3333333333333333703, 0.3333333333333333703, 0.3333333333333333703, 0.3333333333333334259, 0.3333333333333334259, 0.3333333333333333148, 0.3333333333333333148, 0.3333333333333334814, 0.3333333333333333148, 0.3333333333333333148, 0.3333333333333333703, 0.3333333333333333703, 0.3333333333333333703, 0.3333333333333333703),
 ( 1.000000000000000000, 1.000000000000000000, 1.000000000000000000, 0.9999999999999997780, 1.000000000000000000, 1.000000000000000000, 1.000000000000000000, 1.000000000000000222, 1.000000000000000000, 1.000000000000000000, 1.000000000000000222, 0.9999999999999997780, 1.000000000000000222, 1.000000000000000222, 1.000000000000000000, 1.000000000000000000, 1.000000000000000000, 0.9999999999999997780, 1.000000000000000222, 0.9999999999999996669, 1.000000000000000222, 1.000000000000000000, 1.000000000000000000, 0.9999999999999996669, 1.000000000000000444, 0.9999999999999996669, 1.000000000000000444, 1.000000000000000000, 1.000000000000000000, 0.9999999999999997780, 1.000000000000000222, 0.9999999999999994449, 1.000000000000000444, 1.000000000000000000, 1.000000000000000000, 1.000000000000000000, 1.000000000000000000, 1.000000000000000444, 0.9999999999999997780, 1.000000000000000000, 1.000000000000000000, 1.000000000000000000, 1.000000000000000000, 1.000000000000000000, 1.000000000000000000, 0.9999999999999997780, 1.000000000000000000, 1.000000000000000444, 0.9999999999999997780, 1.000000000000000444, 0.9999999999999997780, 0.9999999999999997780, 1.000000000000000000, 1.000000000000000222, 1.000000000000000000, 1.000000000000000000, 1.000000000000000000, 1.000000000000000000, 0.9999999999999997780, 1.000000000000000444, 0.9999999999999997780, 1.000000000000000000, 1.000000000000000222, 0.9999999999999997780, 1.000000000000000000, 1.000000000000000222, 0.9999999999999997780, 1.000000000000000222, 1.000000000000000000, 1.000000000000000222, 1.000000000000000000, 1.000000000000000222, 0.9999999999999997780, 1.000000000000000000, 1.000000000000000222, 1.000000000000000000, 1.000000000000000222, 0.9999999999999997780, 1.000000000000000222, 0.9999999999999997780, 1.000000000000000222, 0.9999999999999997780, 1.000000000000000222, 1.000000000000000222, 0.9999999999999997780, 1.000000000000000222, 1.000000000000000222, 0.9999999999999997780, 1.000000000000000222, 1.000000000000000000, 1.000000000000000000, 1.000000000000000222, 0.9999999999999996669, 1.000000000000000444, 0.9999999999999997780, 0.9999999999999997780, 1.000000000000000000, 1.000000000000000000, 1.000000000000000000, 0.9999999999999996669, 1.000000000000000444, 1.000000000000000000, 1.000000000000000222, 1.000000000000000000, 0.9999999999999997780, 1.000000000000000222, 0.9999999999999997780, 1.000000000000000222, 1.000000000000000000, 1.000000000000000000, 1.000000000000000222, 1.000000000000000000, 1.000000000000000222, 0.9999999999999994449, 1.000000000000000444, 1.000000000000000000, 0.9999999999999996669, 1.000000000000000222, 0.9999999999999997780, 1.000000000000000222, 0.9999999999999997780, 1.000000000000000000, 1.000000000000000000, 1.000000000000000000, 1.000000000000000000, 1.000000000000000000, 1.000000000000000444, 1.000000000000000000, 1.000000000000000000, 1.000000000000000222, 1.000000000000000000, 1.000000000000000000, 0.9999999999999997780, 1.000000000000000000, 1.000000000000000222, 1.000000000000000000, 1.000000000000000222, 0.9999999999999997780, 1.000000000000000000, 0.9999999999999997780, 0.9999999999999997780, 1.000000000000000222, 0.9999999999999997780, 1.000000000000000444, 0.9999999999999997780, 1.000000000000000000, 1.000000000000000222, 1.000000000000000000, 1.000000000000000000, 0.9999999999999997780, 1.000000000000000222, 1.000000000000000000, 1.000000000000000000, 1.000000000000000000, 1.000000000000000222, 0.9999999999999996669, 1.000000000000000222, 1.000000000000000222, 0.9999999999999996669, 1.000000000000000444, 0.9999999999999996669, 1.000000000000000000, 1.000000000000000222, 0.9999999999999996669, 1.000000000000000222, 1.000000000000000000, 1.000000000000000222, 1.000000000000000000, 1.000000000000000222, 0.9999999999999997780, 1.000000000000000444, 0.9999999999999997780, 0.9999999999999997780, 1.000000000000000222, 0.9999999999999996669, 1.000000000000000222, 1.000000000000000000, 1.000000000000000000, 1.000000000000000000, 0.9999999999999997780, 1.000000000000000222, 1.000000000000000222, 0.9999999999999997780, 1.000000000000000222, 0.9999999999999997780, 1.000000000000000222, 1.000000000000000000, 1.000000000000000444, 1.000000000000000000, 1.000000000000000222, 0.9999999999999996669, 1.000000000000000444, 0.9999999999999993339, 1.000000000000000444, 0.9999999999999997780, 1.000000000000000444, 0.9999999999999997780, 1.000000000000000000, 1.000000000000000000, 0.9999999999999997780, 1.000000000000000222, 0.9999999999999997780, 0.9999999999999996669, 1.000000000000000444, 1.000000000000000222, 1.000000000000000000, 0.9999999999999997780, 1.000000000000000222, 0.9999999999999996669, 1.000000000000000222, 0.9999999999999997780, 1.000000000000000222, 1.000000000000000000, 1.000000000000000000, 1.000000000000000000, 1.000000000000000000, 0.9999999999999997780, 1.000000000000000000, 1.000000000000000000, 0.9999999999999997780, 1.000000000000000000, 1.000000000000000000, 1.000000000000000000, 1.000000000000000222, 1.000000000000000000, 1.000000000000000444, 1.000000000000000222, 1.000000000000000000, 1.000000000000000000, 0.9999999999999997780, 1.000000000000000222, 1.000000000000000000, 1.000000000000000000, 1.000000000000000000, 0.9999999999999997780, 1.000000000000000222, 0.9999999999999997780, 1.000000000000000222, 1.000000000000000444, 0.9999999999999997780, 1.000000000000000222, 1.000000000000000000, 1.000000000000000000, 1.000000000000000000, 0.9999999999999997780, 1.000000000000000444, 0.9999999999999997780, 1.000000000000000222, 0.9999999999999997780, 1.000000000000000222, 0.9999999999999994449, 1.000000000000000222, 1.000000000000000000, 1.000000000000000222, 1.000000000000000000, 0.9999999999999997780, 1.000000000000000222, 1.000000000000000000, 0.9999999999999997780, 1.000000000000000444, 0.9999999999999996669, 1.000000000000000222, 1.000000000000000000, 1.000000000000000000, 1.000000000000000222, 0.9999999999999997780, 0.9999999999999997780, 1.000000000000000444, 1.000000000000000222, 1.000000000000000000, 0.9999999999999997780, 0.9999999999999997780, 1.000000000000000222, 1.000000000000000000, 1.000000000000000222, 1.000000000000000000, 0.9999999999999997780, 1.000000000000000000, 1.000000000000000000, 1.000000000000000000, 1.000000000000000222, 0.9999999999999997780, 1.000000000000000222, 1.000000000000000000, 1.000000000000000000, 1.000000000000000000, 0.9999999999999997780, 1.000000000000000000, 1.000000000000000222, 1.000000000000000222, 0.9999999999999996669, 1.000000000000000444, 0.9999999999999996669, 1.000000000000000222, 1.000000000000000000, 1.000000000000000222, 0.9999999999999997780, 1.000000000000000444, 1.000000000000000000, 1.000000000000000444, 0.9999999999999994449, 1.000000000000000222, 0.9999999999999997780, 0.9999999999999997780, 1.000000000000000000, 1.000000000000000222, 1.000000000000000000, 1.000000000000000000, 1.000000000000000000, 1.000000000000000222, 0.9999999999999996669, 1.000000000000000222, 1.000000000000000000, 0.9999999999999996669, 1.000000000000000444, 1.000000000000000000, 1.000000000000000000, 1.000000000000000000, 0.9999999999999996669, 1.000000000000000222, 1.000000000000000000, 1.000000000000000000, 1.000000000000000222, 0.9999999999999997780, 0.9999999999999997780, 1.000000000000000000, 1.000000000000000000, 1.000000000000000222, 0.9999999999999997780, 1.000000000000000222, 1.000000000000000000, 1.000000000000000000, 0.9999999999999996669, 1.000000000000000222, 1.000000000000000000, 1.000000000000000222, 1.000000000000000000, 1.000000000000000000, 1.000000000000000000, 0.9999999999999997780, 1.000000000000000222, 0.9999999999999996669, 1.000000000000000444, 1.000000000000000000, 0.9999999999999997780, 1.000000000000000000, 1.000000000000000222, 1.000000000000000222, 0.9999999999999996669, 1.000000000000000000, 1.000000000000000000, 0.9999999999999997780, 1.000000000000000222, 1.000000000000000000, 1.000000000000000222, 0.9999999999999996669, 1.000000000000000444, 1.000000000000000000, 1.000000000000000000, 1.000000000000000000, 1.000000000000000222, 1.000000000000000000, 0.9999999999999997780, 1.000000000000000444, 1.000000000000000000, 1.000000000000000444, 0.9999999999999997780, 1.000000000000000444, 1.000000000000000000, 1.000000000000000222, 1.000000000000000222, 1.000000000000000000, 0.9999999999999996669, 1.000000000000000000, 1.000000000000000000, 1.000000000000000000, 1.000000000000000000, 1.000000000000000222, 0.9999999999999996669, 1.000000000000000000, 1.000000000000000222, 0.9999999999999997780, 0.9999999999999997780, 1.000000000000000000, 1.000000000000000000, 1.000000000000000000, 1.000000000000000000),
 ( 0.3333333333333333703, 0.3333333333333333703, 0.3333333333333333703, 0.3333333333333333148, 0.3333333333333333703, 0.3333333333333333148, 0.3333333333333333703, 0.3333333333333334259, 0.3333333333333333703, 0.3333333333333333148, 0.3333333333333334259, 0.3333333333333332593, 0.3333333333333334259, 0.3333333333333333703, 0.3333333333333333703, 0.3333333333333332593, 0.3333333333333334259, 0.3333333333333333148, 0.3333333333333334259, 0.3333333333333333148, 0.3333333333333334259, 0.3333333333333334259, 0.3333333333333333148, 0.3333333333333333148, 0.3333333333333334814, 0.3333333333333332593, 0.3333333333333334259, 0.3333333333333334259, 0.3333333333333333703, 0.3333333333333333703, 0.3333333333333334814, 0.3333333333333332038, 0.3333333333333334814, 0.3333333333333333703, 0.3333333333333334259, 0.3333333333333333148, 0.3333333333333334259, 0.3333333333333334814, 0.3333333333333333703, 0.3333333333333332593, 0.3333333333333334259, 0.3333333333333333148, 0.3333333333333333148, 0.3333333333333333703, 0.3333333333333333703, 0.3333333333333334259, 0.3333333333333333148, 0.3333333333333335369, 0.3333333333333333148, 0.3333333333333334259, 0.3333333333333333703, 0.3333333333333332038, 0.3333333333333334259, 0.3333333333333334259, 0.3333333333333333148, 0.3333333333333334259, 0.3333333333333333703, 0.3333333333333333703, 0.3333333333333334259, 0.3333333333333334259, 0.3333333333333333703, 0.3333333333333334259, 0.3333333333333334259, 0.3333333333333333148, 0.3333333333333333703, 0.3333333333333333703, 0.3333333333333333148, 0.3333333333333334259, 0.3333333333333333148, 0.3333333333333334814, 0.3333333333333333703, 0.3333333333333334259, 0.3333333333333333148, 0.3333333333333333703, 0.3333333333333334259, 0.3333333333333333703, 0.3333333333333333703, 0.3333333333333333148, 0.3333333333333334259, 0.3333333333333333148, 0.3333333333333334259, 0.3333333333333333703, 0.3333333333333334259, 0.3333333333333334814, 0.3333333333333333148, 0.3333333333333334259, 0.3333333333333334259, 0.3333333333333333148, 0.3333333333333333703, 0.3333333333333333703, 0.3333333333333333148, 0.3333333333333334814, 0.3333333333333332593, 0.3333333333333334259, 0.3333333333333333703, 0.3333333333333333148, 0.3333333333333333703, 0.3333333333333333703, 0.3333333333333334259, 0.3333333333333333148, 0.3333333333333334259, 0.3333333333333333148, 0.3333333333333334814, 0.3333333333333333148, 0.3333333333333333148, 0.3333333333333334259, 0.3333333333333333148, 0.3333333333333333703, 0.3333333333333333703, 0.3333333333333334259, 0.3333333333333333703, 0.3333333333333334259, 0.3333333333333333703, 0.3333333333333332593, 0.3333333333333334259, 0.3333333333333333703, 0.3333333333333333148, 0.3333333333333334814, 0.3333333333333333148, 0.3333333333333334259, 0.3333333333333334259, 0.3333333333333333148, 0.3333333333333333703, 0.3333333333333334259, 0.3333333333333333703, 0.3333333333333333703, 0.3333333333333334259, 0.3333333333333333703, 0.3333333333333334259, 0.3333333333333333703, 0.3333333333333334259, 0.3333333333333333148, 0.3333333333333333703, 0.3333333333333333703, 0.3333333333333333703, 0.3333333333333333703, 0.3333333333333335369, 0.3333333333333332593, 0.3333333333333333703, 0.3333333333333333703, 0.3333333333333332593, 0.3333333333333333703, 0.3333333333333333703, 0.3333333333333334259, 0.3333333333333332593, 0.3333333333333333703, 0.3333333333333333703, 0.3333333333333333703, 0.3333333333333333703, 0.3333333333333333703, 0.3333333333333334259, 0.3333333333333333148, 0.3333333333333334259, 0.3333333333333333703, 0.3333333333333334814, 0.3333333333333332593, 0.3333333333333333703, 0.3333333333333334814, 0.3333333333333332038, 0.3333333333333334259, 0.3333333333333333148, 0.3333333333333333703, 0.3333333333333334814, 0.3333333333333332038, 0.3333333333333334259, 0.3333333333333333703, 0.3333333333333333703, 0.3333333333333333703, 0.3333333333333334259, 0.3333333333333333703, 0.3333333333333335369, 0.3333333333333333148, 0.3333333333333333148, 0.3333333333333334259, 0.3333333333333333148, 0.3333333333333333703, 0.3333333333333333703, 0.3333333333333334259, 0.3333333333333333148, 0.3333333333333334259, 0.3333333333333332593, 0.3333333333333334814, 0.3333333333333333703, 0.3333333333333333703, 0.3333333333333333703, 0.3333333333333333703, 0.3333333333333333703, 0.3333333333333334259, 0.3333333333333333703, 0.3333333333333334259, 0.3333333333333333148, 0.3333333333333335369, 0.3333333333333332038, 0.3333333333333335369, 0.3333333333333333148, 0.3333333333333334259, 0.3333333333333333703, 0.3333333333333333148, 0.3333333333333334259, 0.3333333333333333148, 0.3333333333333334259, 0.3333333333333332593, 0.3333333333333333148, 0.3333333333333334259, 0.3333333333333334814, 0.3333333333333333703, 0.3333333333333333703, 0.3333333333333334259, 0.3333333333333333148, 0.3333333333333333703, 0.3333333333333333148, 0.3333333333333334259, 0.3333333333333333148, 0.3333333333333333703, 0.3333333333333333703, 0.3333333333333334259, 0.3333333333333333148, 0.3333333333333334259, 0.3333333333333333703, 0.3333333333333333148, 0.3333333333333332593, 0.3333333333333334259, 0.3333333333333333148, 0.3333333333333334259, 0.3333333333333334259, 0.3333333333333334814, 0.3333333333333334259, 0.3333333333333333703, 0.3333333333333333703, 0.3333333333333333148, 0.3333333333333334259, 0.3333333333333333703, 0.3333333333333334259, 0.3333333333333333148, 0.3333333333333333703, 0.3333333333333333703, 0.3333333333333332593, 0.3333333333333334259, 0.3333333333333335369, 0.3333333333333333148, 0.3333333333333334814, 0.3333333333333333703, 0.3333333333333333148, 0.3333333333333334259, 0.3333333333333332593, 0.3333333333333334814, 0.3333333333333333148, 0.3333333333333333703, 0.3333333333333333148, 0.3333333333333334259, 0.3333333333333333148, 0.3333333333333334259, 0.3333333333333333148, 0.3333333333333333703, 0.3333333333333333703, 0.3333333333333333148, 0.3333333333333334259, 0.3333333333333333703, 0.3333333333333333703, 0.3333333333333335369, 0.3333333333333332038, 0.3333333333333334814, 0.3333333333333333148, 0.3333333333333334259, 0.3333333333333334259, 0.3333333333333333703, 0.3333333333333333148, 0.3333333333333334814, 0.3333333333333333703, 0.3333333333333333703, 0.3333333333333333703, 0.3333333333333333703, 0.3333333333333333703, 0.3333333333333334259, 0.3333333333333333703, 0.3333333333333334259, 0.3333333333333333148, 0.3333333333333333703, 0.3333333333333334259, 0.3333333333333334259, 0.3333333333333333703, 0.3333333333333333703, 0.3333333333333334259, 0.3333333333333333703, 0.3333333333333333148, 0.3333333333333333148, 0.3333333333333333703, 0.3333333333333333703, 0.3333333333333334259, 0.3333333333333334259, 0.3333333333333333703, 0.3333333333333333703, 0.3333333333333333703, 0.3333333333333333703, 0.3333333333333333703, 0.3333333333333333148, 0.3333333333333334259, 0.3333333333333334259, 0.3333333333333333703, 0.3333333333333335369, 0.3333333333333332038, 0.3333333333333334814, 0.3333333333333332593, 0.3333333333333333703, 0.3333333333333332593, 0.3333333333333334814, 0.3333333333333333148, 0.3333333333333333703, 0.3333333333333334259, 0.3333333333333334259, 0.3333333333333332593, 0.3333333333333334259, 0.3333333333333333148, 0.3333333333333333703, 0.3333333333333334259, 0.3333333333333334814, 0.3333333333333333148, 0.3333333333333334259, 0.3333333333333333148, 0.3333333333333334814, 0.3333333333333334259, 0.3333333333333333703, 0.3333333333333334259, 0.3333333333333332593, 0.3333333333333333148, 0.3333333333333333703, 0.3333333333333333703, 0.3333333333333334259, 0.3333333333333333703, 0.3333333333333334259, 0.3333333333333333703, 0.3333333333333334259, 0.3333333333333333148, 0.3333333333333333703, 0.3333333333333334259, 0.3333333333333334259, 0.3333333333333333703, 0.3333333333333333703, 0.3333333333333333703, 0.3333333333333333148, 0.3333333333333333703, 0.3333333333333333148, 0.3333333333333334259, 0.3333333333333334259, 0.3333333333333333148, 0.3333333333333333703, 0.3333333333333334259, 0.3333333333333333703, 0.3333333333333333148, 0.3333333333333333703, 0.3333333333333333148, 0.3333333333333333703, 0.3333333333333334259, 0.3333333333333333148, 0.3333333333333334259, 0.3333333333333332593, 0.3333333333333334814, 0.3333333333333334814, 0.3333333333333333148, 0.3333333333333333703, 0.3333333333333334814, 0.3333333333333333148, 0.3333333333333333703, 0.3333333333333334814, 0.3333333333333333703, 0.3333333333333334259, 0.3333333333333334259, 0.3333333333333334814, 0.3333333333333333703, 0.3333333333333333703, 0.3333333333333333703, 0.3333333333333333148, 0.3333333333333333148, 0.3333333333333333703, 0.3333333333333333703, 0.3333333333333333703, 0.3333333333333334259, 0.3333333333333334259, 0.3333333333333333148, 0.3333333333333333148, 0.3333333333333334814, 0.3333333333333333148, 0.3333333333333333148, 0.3333333333333333703, 0.3333333333333333703, 0.3333333333333333703, 0.3333333333333333703),
 ( 0.3333333333333333703, 0.3333333333333333703, 0.3333333333333333703, 0.3333333333333333148, 0.3333333333333333703, 0.3333333333333333148, 0.3333333333333333703, 0.3333333333333334259, 0.3333333333333333703, 0.3333333333333333148, 0.3333333333333334259, 0.3333333333333332593, 0.3333333333333334259, 0.3333333333333333703, 0.3333333333333333703, 0.3333333333333332593, 0.3333333333333334259, 0.3333333333333333148, 0.3333333333333334259, 0.3333333333333333148, 0.3333333333333334259, 0.3333333333333334259, 0.3333333333333333148, 0.3333333333333333148, 0.3333333333333334814, 0.3333333333333332593, 0.3333333333333334259, 0.3333333333333334259, 0.3333333333333333703, 0.3333333333333333703, 0.3333333333333334814, 0.3333333333333332038, 0.3333333333333334814, 0.3333333333333333703, 0.3333333333333334259, 0.3333333333333333148, 0.3333333333333334259, 0.3333333333333334814, 0.3333333333333333703, 0.3333333333333332593, 0.3333333333333334259, 0.3333333333333333148, 0.3333333333333333148, 0.3333333333333333703, 0.3333333333333333703, 0.3333333333333334259, 0.3333333333333333148, 0.3333333333333335369, 0.3333333333333333148, 0.3333333333333334259, 0.3333333333333333703, 0.3333333333333332038, 0.3333333333333334259, 0.3333333333333334259, 0.3333333333333333148, 0.3333333333333334259, 0.3333333333333333703, 0.3333333333333333703, 0.3333333333333334259, 0.3333333333333334259, 0.3333333333333333703, 0.3333333333333334259, 0.3333333333333334259, 0.3333333333333333148, 0.3333333333333333703, 0.3333333333333333703, 0.3333333333333333148, 0.3333333333333334259, 0.3333333333333333148, 0.3333333333333334814, 0.3333333333333333703, 0.3333333333333334259, 0.3333333333333333148, 0.3333333333333333703, 0.3333333333333334259, 0.3333333333333333703, 0.3333333333333333703, 0.3333333333333333148, 0.3333333333333334259, 0.3333333333333333148, 0.3333333333333334259, 0.3333333333333333703, 0.3333333333333334259, 0.3333333333333334814, 0.3333333333333333148, 0.3333333333333334259, 0.3333333333333334259, 0.3333333333333333148, 0.3333333333333333703, 0.3333333333333333703, 0.3333333333333333148, 0.3333333333333334814, 0.3333333333333332593, 0.3333333333333334259, 0.3333333333333333703, 0.3333333333333333148, 0.3333333333333333703, 0.3333333333333333703, 0.3333333333333334259, 0.3333333333333333148, 0.3333333333333334259, 0.3333333333333333148, 0.3333333333333334814, 0.3333333333333333148, 0.3333333333333333148, 0.3333333333333334259, 0.3333333333333333148, 0.3333333333333333703, 0.3333333333333333703, 0.3333333333333334259, 0.3333333333333333703, 0.3333333333333334259, 0.3333333333333333703, 0.3333333333333332593, 0.3333333333333334259, 0.3333333333333333703, 0.3333333333333333148, 0.3333333333333334814, 0.3333333333333333148, 0.3333333333333334259, 0.3333333333333334259, 0.3333333333333333148, 0.3333333333333333703, 0.3333333333333334259, 0.3333333333333333703, 0.3333333333333333703, 0.3333333333333334259, 0.3333333333333333703, 0.3333333333333334259, 0.3333333333333333703, 0.3333333333333334259, 0.3333333333333333148, 0.3333333333333333703, 0.3333333333333333703, 0.3333333333333333703, 0.3333333333333333703, 0.3333333333333335369, 0.3333333333333332593, 0.3333333333333333703, 0.3333333333333333703, 0.3333333333333332593, 0.3333333333333333703, 0.3333333333333333703, 0.3333333333333334259, 0.3333333333333332593, 0.3333333333333333703, 0.3333333333333333703, 0.3333333333333333703, 0.3333333333333333703, 0.3333333333333333703, 0.3333333333333334259, 0.3333333333333333148, 0.3333333333333334259, 0.3333333333333333703, 0.3333333333333334814, 0.3333333333333332593, 0.3333333333333333703, 0.3333333333333334814, 0.3333333333333332038, 0.3333333333333334259, 0.3333333333333333148, 0.3333333333333333703, 0.3333333333333334814, 0.3333333333333332038, 0.3333333333333334259, 0.3333333333333333703, 0.3333333333333333703, 0.3333333333333333703, 0.3333333333333334259, 0.3333333333333333703, 0.3333333333333335369, 0.3333333333333333148, 0.3333333333333333148, 0.3333333333333334259, 0.3333333333333333148, 0.3333333333333333703, 0.3333333333333333703, 0.3333333333333334259, 0.3333333333333333148, 0.3333333333333334259, 0.3333333333333332593, 0.3333333333333334814, 0.3333333333333333703, 0.3333333333333333703, 0.3333333333333333703, 0.3333333333333333703, 0.3333333333333333703, 0.3333333333333334259, 0.3333333333333333703, 0.3333333333333334259, 0.3333333333333333148, 0.3333333333333335369, 0.3333333333333332038, 0.3333333333333335369, 0.3333333333333333148, 0.3333333333333334259, 0.3333333333333333703, 0.3333333333333333148, 0.3333333333333334259, 0.3333333333333333148, 0.3333333333333334259, 0.3333333333333332593, 0.3333333333333333148, 0.3333333333333334259, 0.3333333333333334814, 0.3333333333333333703, 0.3333333333333333703, 0.3333333333333334259, 0.3333333333333333148, 0.3333333333333333703, 0.3333333333333333148, 0.3333333333333334259, 0.3333333333333333148, 0.3333333333333333703, 0.3333333333333333703, 0.3333333333333334259, 0.3333333333333333148, 0.3333333333333334259, 0.3333333333333333703, 0.3333333333333333148, 0.3333333333333332593, 0.3333333333333334259, 0.3333333333333333148, 0.3333333333333334259, 0.3333333333333334259, 0.3333333333333334814, 0.3333333333333334259, 0.3333333333333333703, 0.3333333333333333703, 0.3333333333333333148, 0.3333333333333334259, 0.3333333333333333703, 0.3333333333333334259, 0.3333333333333333148, 0.3333333333333333703, 0.3333333333333333703, 0.3333333333333332593, 0.3333333333333334259, 0.3333333333333335369, 0.3333333333333333148, 0.3333333333333334814, 0.3333333333333333703, 0.3333333333333333148, 0.3333333333333334259, 0.3333333333333332593, 0.3333333333333334814, 0.3333333333333333148, 0.3333333333333333703, 0.3333333333333333148, 0.3333333333333334259, 0.3333333333333333148, 0.3333333333333334259, 0.3333333333333333148, 0.3333333333333333703, 0.3333333333333333703, 0.3333333333333333148, 0.3333333333333334259, 0.3333333333333333703, 0.3333333333333333703, 0.3333333333333335369, 0.3333333333333332038, 0.3333333333333334814, 0.3333333333333333148, 0.3333333333333334259, 0.3333333333333334259, 0.3333333333333333703, 0.3333333333333333148, 0.3333333333333334814, 0.3333333333333333703, 0.3333333333333333703, 0.3333333333333333703, 0.3333333333333333703, 0.3333333333333333703, 0.3333333333333334259, 0.3333333333333333703, 0.3333333333333334259, 0.3333333333333333148, 0.3333333333333333703, 0.3333333333333334259, 0.3333333333333334259, 0.3333333333333333703, 0.3333333333333333703, 0.3333333333333334259, 0.3333333333333333703, 0.3333333333333333148, 0.3333333333333333148, 0.3333333333333333703, 0.3333333333333333703, 0.3333333333333334259, 0.3333333333333334259, 0.3333333333333333703, 0.3333333333333333703, 0.3333333333333333703, 0.3333333333333333703, 0.3333333333333333703, 0.3333333333333333148, 0.3333333333333334259, 0.3333333333333334259, 0.3333333333333333703, 0.3333333333333335369, 0.3333333333333332038, 0.3333333333333334814, 0.3333333333333332593, 0.3333333333333333703, 0.3333333333333332593, 0.3333333333333334814, 0.3333333333333333148, 0.3333333333333333703, 0.3333333333333334259, 0.3333333333333334259, 0.3333333333333332593, 0.3333333333333334259, 0.3333333333333333148, 0.3333333333333333703, 0.3333333333333334259, 0.3333333333333334814, 0.3333333333333333148, 0.3333333333333334259, 0.3333333333333333148, 0.3333333333333334814, 0.3333333333333334259, 0.3333333333333333703, 0.3333333333333334259, 0.3333333333333332593, 0.3333333333333333148, 0.3333333333333333703, 0.3333333333333333703, 0.3333333333333334259, 0.3333333333333333703, 0.3333333333333334259, 0.3333333333333333703, 0.3333333333333334259, 0.3333333333333333148, 0.3333333333333333703, 0.3333333333333334259, 0.3333333333333334259, 0.3333333333333333703, 0.3333333333333333703, 0.3333333333333333703, 0.3333333333333333148, 0.3333333333333333703, 0.3333333333333333148, 0.3333333333333334259, 0.3333333333333334259, 0.3333333333333333148, 0.3333333333333333703, 0.3333333333333334259, 0.3333333333333333703, 0.3333333333333333148, 0.3333333333333333703, 0.3333333333333333148, 0.3333333333333333703, 0.3333333333333334259, 0.3333333333333333148, 0.3333333333333334259, 0.3333333333333332593, 0.3333333333333334814, 0.3333333333333334814, 0.3333333333333333148, 0.3333333333333333703, 0.3333333333333334814, 0.3333333333333333148, 0.3333333333333333703, 0.3333333333333334814, 0.3333333333333333703, 0.3333333333333334259, 0.3333333333333334259, 0.3333333333333334814, 0.3333333333333333703, 0.3333333333333333703, 0.3333333333333333703, 0.3333333333333333148, 0.3333333333333333148, 0.3333333333333333703, 0.3333333333333333703, 0.3333333333333333703, 0.3333333333333334259, 0.3333333333333334259, 0.3333333333333333148, 0.3333333333333333148, 0.3333333333333334814, 0.3333333333333333148, 0.3333333333333333148, 0.3333333333333333703, 0.3333333333333333703, 0.3333333333333333703, 0.3333333333333333703),
 ( 1.000000000000000000, 1.000000000000000000, 1.000000000000000000, 0.9999999999999997780, 1.000000000000000000, 1.000000000000000000, 1.000000000000000000, 1.000000000000000222, 1.000000000000000000, 1.000000000000000000, 1.000000000000000222, 0.9999999999999997780, 1.000000000000000222, 1.000000000000000222, 1.000000000000000000, 1.000000000000000000, 1.000000000000000000, 0.9999999999999997780, 1.000000000000000222, 0.9999999999999996669, 1.000000000000000222, 1.000000000000000000, 1.000000000000000000, 0.9999999999999996669, 1.000000000000000444, 0.9999999999999996669, 1.000000000000000444, 1.000000000000000000, 1.000000000000000000, 0.9999999999999997780, 1.000000000000000222, 0.9999999999999994449, 1.000000000000000444, 1.000000000000000000, 1.000000000000000000, 1.000000000000000000, 1.000000000000000000, 1.000000000000000444, 0.9999999999999997780, 1.000000000000000000, 1.000000000000000000, 1.000000000000000000, 1.000000000000000000, 1.000000000000000000, 1.000000000000000000, 0.9999999999999997780, 1.000000000000000000, 1.000000000000000444, 0.9999999999999997780, 1.000000000000000444, 0.9999999999999997780, 0.9999999999999997780, 1.000000000000000000, 1.000000000000000222, 1.000000000000000000, 1.000000000000000000, 1.000000000000000000, 1.000000000000000000, 0.9999999999999997780, 1.000000000000000444, 0.9999999999999997780, 1.000000000000000000, 1.000000000000000222, 0.9999999999999997780, 1.000000000000000000, 1.000000000000000222, 0.9999999999999997780, 1.000000000000000222, 1.000000000000000000, 1.000000000000000222, 1.000000000000000000, 1.000000000000000222, 0.9999999999999997780, 1.000000000000000000, 1.000000000000000222, 1.000000000000000000, 1.000000000000000222, 0.9999999999999997780, 1.000000000000000222, 0.9999999999999997780, 1.000000000000000222, 0.9999999999999997780, 1.000000000000000222, 1.000000000000000222, 0.9999999999999997780, 1.000000000000000222, 1.000000000000000222, 0.9999999999999997780, 1.000000000000000222, 1.000000000000000000, 1.000000000000000000, 1.000000000000000222, 0.9999999999999996669, 1.000000000000000444, 0.9999999999999997780, 0.9999999999999997780, 1.000000000000000000, 1.000000000000000000, 1.000000000000000000, 0.9999999999999996669, 1.000000000000000444, 1.000000000000000000, 1.000000000000000222, 1.000000000000000000, 0.9999999999999997780, 1.000000000000000222, 0.9999999999999997780, 1.000000000000000222, 1.000000000000000000, 1.000000000000000000, 1.000000000000000222, 1.000000000000000000, 1.000000000000000222, 0.9999999999999994449, 1.000000000000000444, 1.000000000000000000, 0.9999999999999996669, 1.000000000000000222, 0.9999999999999997780, 1.000000000000000222, 0.9999999999999997780, 1.000000000000000000, 1.000000000000000000, 1.000000000000000000, 1.000000000000000000, 1.000000000000000000, 1.000000000000000444, 1.000000000000000000, 1.000000000000000000, 1.000000000000000222, 1.000000000000000000, 1.000000000000000000, 0.9999999999999997780, 1.000000000000000000, 1.000000000000000222, 1.000000000000000000, 1.000000000000000222, 0.9999999999999997780, 1.000000000000000000, 0.9999999999999997780, 0.9999999999999997780, 1.000000000000000222, 0.9999999999999997780, 1.000000000000000444, 0.9999999999999997780, 1.000000000000000000, 1.000000000000000222, 1.000000000000000000, 1.000000000000000000, 0.9999999999999997780, 1.000000000000000222, 1.000000000000000000, 1.000000000000000000, 1.000000000000000000, 1.000000000000000222, 0.9999999999999996669, 1.000000000000000222, 1.000000000000000222, 0.9999999999999996669, 1.000000000000000444, 0.9999999999999996669, 1.000000000000000000, 1.000000000000000222, 0.9999999999999996669, 1.000000000000000222, 1.000000000000000000, 1.000000000000000222, 1.000000000000000000, 1.000000000000000222, 0.9999999999999997780, 1.000000000000000444, 0.9999999999999997780, 0.9999999999999997780, 1.000000000000000222, 0.9999999999999996669, 1.000000000000000222, 1.000000000000000000, 1.000000000000000000, 1.000000000000000000, 0.9999999999999997780, 1.000000000000000222, 1.000000000000000222, 0.9999999999999997780, 1.000000000000000222, 0.9999999999999997780, 1.000000000000000222, 1.000000000000000000, 1.000000000000000444, 1.000000000000000000, 1.000000000000000222, 0.9999999999999996669, 1.000000000000000444, 0.9999999999999993339, 1.000000000000000444, 0.9999999999999997780, 1.000000000000000444, 0.9999999999999997780, 1.000000000000000000, 1.000000000000000000, 0.9999999999999997780, 1.000000000000000222, 0.9999999999999997780, 0.9999999999999996669, 1.000000000000000444, 1.000000000000000222, 1.000000000000000000, 0.9999999999999997780, 1.000000000000000222, 0.9999999999999996669, 1.000000000000000222, 0.9999999999999997780, 1.000000000000000222, 1.000000000000000000, 1.000000000000000000, 1.000000000000000000, 1.000000000000000000, 0.9999999999999997780, 1.000000000000000000, 1.000000000000000000, 0.9999999999999997780, 1.000000000000000000, 1.000000000000000000, 1.000000000000000000, 1.000000000000000222, 1.000000000000000000, 1.000000000000000444, 1.000000000000000222, 1.000000000000000000, 1.000000000000000000, 0.9999999999999997780, 1.000000000000000222, 1.000000000000000000, 1.000000000000000000, 1.000000000000000000, 0.9999999999999997780, 1.000000000000000222, 0.9999999999999997780, 1.000000000000000222, 1.000000000000000444, 0.9999999999999997780, 1.000000000000000222, 1.000000000000000000, 1.000000000000000000, 1.000000000000000000, 0.9999999999999997780, 1.000000000000000444, 0.9999999999999997780, 1.000000000000000222, 0.9999999999999997780, 1.000000000000000222, 0.9999999999999994449, 1.000000000000000222, 1.000000000000000000, 1.000000000000000222, 1.000000000000000000, 0.9999999999999997780, 1.000000000000000222, 1.000000000000000000, 0.9999999999999997780, 1.000000000000000444, 0.9999999999999996669, 1.000000000000000222, 1.000000000000000000, 1.000000000000000000, 1.000000000000000222, 0.9999999999999997780, 0.9999999999999997780, 1.000000000000000444, 1.000000000000000222, 1.000000000000000000, 0.9999999999999997780, 0.9999999999999997780, 1.000000000000000222, 1.000000000000000000, 1.000000000000000222, 1.000000000000000000, 0.9999999999999997780, 1.000000000000000000, 1.000000000000000000, 1.000000000000000000, 1.000000000000000222, 0.9999999999999997780, 1.000000000000000222, 1.000000000000000000, 1.000000000000000000, 1.000000000000000000, 0.9999999999999997780, 1.000000000000000000, 1.000000000000000222, 1.000000000000000222, 0.9999999999999996669, 1.000000000000000444, 0.9999999999999996669, 1.000000000000000222, 1.000000000000000000, 1.000000000000000222, 0.9999999999999997780, 1.000000000000000444, 1.000000000000000000, 1.000000000000000444, 0.9999999999999994449, 1.000000000000000222, 0.9999999999999997780, 0.9999999999999997780, 1.000000000000000000, 1.000000000000000222, 1.000000000000000000, 1.000000000000000000, 1.000000000000000000, 1.000000000000000222, 0.9999999999999996669, 1.000000000000000222, 1.000000000000000000, 0.9999999999999996669, 1.000000000000000444, 1.000000000000000000, 1.000000000000000000, 1.000000000000000000, 0.9999999999999996669, 1.000000000000000222, 1.000000000000000000, 1.000000000000000000, 1.000000000000000222, 0.9999999999999997780, 0.9999999999999997780, 1.000000000000000000, 1.000000000000000000, 1.000000000000000222, 0.9999999999999997780, 1.000000000000000222, 1.000000000000000000, 1.000000000000000000, 0.9999999999999996669, 1.000000000000000222, 1.000000000000000000, 1.000000000000000222, 1.000000000000000000, 1.000000000000000000, 1.000000000000000000, 0.9999999999999997780, 1.000000000000000222, 0.9999999999999996669, 1.000000000000000444, 1.000000000000000000, 0.9999999999999997780, 1.000000000000000000, 1.000000000000000222, 1.000000000000000222, 0.9999999999999996669, 1.000000000000000000, 1.000000000000000000, 0.9999999999999997780, 1.000000000000000222, 1.000000000000000000, 1.000000000000000222, 0.9999999999999996669, 1.000000000000000444, 1.000000000000000000, 1.000000000000000000, 1.000000000000000000, 1.000000000000000222, 1.000000000000000000, 0.9999999999999997780, 1.000000000000000444, 1.000000000000000000, 1.000000000000000444, 0.9999999999999997780, 1.000000000000000444, 1.000000000000000000, 1.000000000000000222, 1.000000000000000222, 1.000000000000000000, 0.9999999999999996669, 1.000000000000000000, 1.000000000000000000, 1.000000000000000000, 1.000000000000000000, 1.000000000000000222, 0.9999999999999996669, 1.000000000000000000, 1.000000000000000222, 0.9999999999999997780, 0.9999999999999997780, 1.000000000000000000, 1.000000000000000000, 1.000000000000000000, 1.000000000000000000) ) ) 
 REPRESENTATION_ITEM ( '' )  SURFACE ( )  );
#4941=CARTESIAN_POINT ( 'NONE',  ( 2.192262590105994668, -0.9421081357594159877, 1.995820444975453745 ) ) ;
#4942=CARTESIAN_POINT ( 'NONE',  ( 4.235799883310053637, -1.556133899351975103, -1.642472060615452589 ) ) ;
#4944=CARTESIAN_POINT ( 'NONE',  ( 3.796947700133224135, -0.1831754980210500150, -1.802320314001674806 ) ) ;
#4945=CARTESIAN_POINT ( 'NONE',  ( 4.030425823177123057, 0.5166280748541264289, 1.844641390986961671 ) ) ;
#4947=CARTESIAN_POINT ( 'NONE',  ( 3.819176294577591779, -0.1464417209034867828, 1.966092509880690065 ) ) ;
#4948=CARTESIAN_POINT ( 'NONE',  ( 0.6219390430294257088, -1.027834010343916749, -1.629101698904901863 ) ) ;
#4949=CARTESIAN_POINT ( 'NONE',  ( 5.207814216083940018, -1.861544245658670604, 0.1842191830812092979 ) ) ;
#4950=CARTESIAN_POINT ( 'NONE',  ( 3.159088808783340419, -1.747439373373047333, 1.507377025801335702 ) ) ;
#4951=CARTESIAN_POINT ( 'NONE',  ( 4.351900876113290018, -0.7134228844126557778, 1.719084262507431182 ) ) ;
#4956=CARTESIAN_POINT ( 'NONE',  ( 1.823018060162405085, 1.965545597939293954, 0.7568914254860066304 ) ) ;
#4960=CARTESIAN_POINT ( 'NONE',  ( 3.234745892528373634, 1.342314639517484087, -1.641720766639111817 ) ) ;
#4962=CARTESIAN_POINT ( 'NONE',  ( 0.8088602503539430444, -0.4949860548154049189, -1.958043583812353550 ) ) ;
#4967=CARTESIAN_POINT ( 'NONE',  ( 2.495597164219889308, 1.669172397749154380, 1.373402732410613725 ) ) ;
#4970=CARTESIAN_POINT ( 'NONE',  ( 6.825078400183592464, 1.263193418084729958, 2.069194724180785538 ) ) ;
#4973=CARTESIAN_POINT ( 'NONE',  ( 6.069546051295945155, 1.394081536189460069, 1.457239770841619597 ) ) ;
#4975=CARTESIAN_POINT ( 'NONE',  ( 0.1170720436180875679, -0.1011795954627830590, 2.189343785608413917 ) ) ;
#4977=CARTESIAN_POINT ( 'NONE',  ( 6.772347375734490527, -1.334533509509854943, 1.701269717329929820 ) ) ;
#4986=CARTESIAN_POINT ( 'NONE',  ( 2.596001052779199014, -1.720239769356088688, -0.1272231981628013098 ) ) ;
#4988=CARTESIAN_POINT ( 'NONE',  ( 1.932500037753889455, 0.1674293521093522530, 1.761778154814014119 ) ) ;
#4989=CARTESIAN_POINT ( 'NONE',  ( 2.842442125518374496, 1.116481279481882805, -1.674925767759533723 ) ) ;
#4990=CARTESIAN_POINT ( 'NONE',  ( 5.403435775159438847, 1.801252639416499379, 1.274624607731331905 ) ) ;
#4992=CARTESIAN_POINT ( 'NONE',  ( 4.676038720085195166, 1.997217120926295442, -0.3003719491122060492 ) ) ;
#4994=CARTESIAN_POINT ( 'NONE',  ( 4.758503674095369007, 2.114844282287762667, 0.1552407789479764433 ) ) ;
#4995=CARTESIAN_POINT ( 'NONE',  ( 3.497672881252233967, -1.986097994744703721, 0.3474890017408845955 ) ) ;
#4996=CARTESIAN_POINT ( 'NONE',  ( 4.552869461240817373, 0.3164949366275445208, 1.783561479213832346 ) ) ;
#5001=CARTESIAN_POINT ( 'NONE',  ( 0.9537216069140028729, 1.868711056098860235, -0.08788249432020722729 ) ) ;
#5005=CARTESIAN_POINT ( 'NONE',  ( 5.936161223257452768, -1.012099431654609472, -1.502142840615662944 ) ) ;
#5014=CARTESIAN_POINT ( 'NONE',  ( 1.557006721180295150, 1.605793932651664813, -1.126831546849601740 ) ) ;
#5017=CARTESIAN_POINT ( 'NONE',  ( 4.113620189327307664, 1.705085180707970771, 1.260635662952174663 ) ) ;
#5020=CARTESIAN_POINT ( 'NONE',  ( 5.870382883074816149, -1.252475921811508019, 1.522319303672705848 ) ) ;
#5022=CARTESIAN_POINT ( 'NONE',  ( 0.9318904303841836212, -1.963229875443720074, 0.4450799344311164862 ) ) ;
#5024=CARTESIAN_POINT ( 'NONE',  ( 0.7732552308061869661, 1.865071980587120315, -1.002124039132473055 ) ) ;
#5026=CARTESIAN_POINT ( 'NONE',  ( 2.365759603224312446, -0.4558734232973959966, 2.019384234097781228 ) ) ;
#5030=CARTESIAN_POINT ( 'NONE',  ( 5.261704619121490900, 1.029696775897260830, 1.819396322279245304 ) ) ;
#5032=CARTESIAN_POINT ( 'NONE',  ( 3.451995160207482538, 1.825762228170943136, 0.001041782061617091849 ) ) ;
#5033=CARTESIAN_POINT ( 'NONE',  ( 1.471055694106305101, -1.553634009935511484, -0.9311844293155254748 ) ) ;
#5034=ORIENTED_EDGE ( 'NONE', *, *, #97813, .T. ) ;
#5035=CARTESIAN_POINT ( 'NONE',  ( 6.287735281038357549, 1.518688880046001444, 1.601449620450722700 ) ) ;
#5036=CARTESIAN_POINT ( 'NONE',  ( 6.827182134110222123, -0.006956174471953178659, 2.188967759425272330 ) ) ;
#5037=CARTESIAN_POINT ( 'NONE',  ( 4.331241739176756589, 0.1049304944579672605, 2.204394592675275710 ) ) ;
#5040=CARTESIAN_POINT ( 'NONE',  ( 3.176317266091326807, 0.8619891151622931513, 1.707069686517001195 ) ) ;
#5043=CARTESIAN_POINT ( 'NONE',  ( 6.039524589772497620, 1.914416561877980261, -0.7887839105886890190 ) ) ;
#5046=CARTESIAN_POINT ( 'NONE',  ( 5.759372899636661991, 2.159370146098410714, -0.3733810082120898044 ) ) ;
#5050=CARTESIAN_POINT ( 'NONE',  ( 3.848780967690919930, -1.530814235938406709, 1.074699354247290017 ) ) ;
#5056=CARTESIAN_POINT ( 'NONE',  ( 0.5495732465782035003, 1.455460699200894270, 1.326940832280040450 ) ) ;
#5057=CARTESIAN_POINT ( 'NONE',  ( 0.7379079170338509464, 2.013986002441462198, -0.1017714793793283723 ) ) ;
#5061=CARTESIAN_POINT ( 'NONE',  ( 1.605704095283020605, -2.174604996184846595, 0.2706701637196773369 ) ) ;
#5062=CARTESIAN_POINT ( 'NONE',  ( 5.760330229460346452, 0.7440287100829170441, 1.667389206893993725 ) ) ;
#5070=CARTESIAN_POINT ( 'NONE',  ( 4.054132754448328768, -1.361571661076573792, 1.239656203754435193 ) ) ;
#5071=CARTESIAN_POINT ( 'NONE',  ( 0.2232913631893228001, 1.752491241892171647, 0.9904617665423065542 ) ) ;
#5072=CARTESIAN_POINT ( 'NONE',  ( 1.704906730629534684, -1.665072001576539007, -1.584524786048894240 ) ) ;
#5074=CARTESIAN_POINT ( 'NONE',  ( 0.3735836145450521228, -1.826584228078181660, 0.3550381321636967846 ) ) ;
#5077=CARTESIAN_POINT ( 'NONE',  ( 4.078302138561982204, 0.9061299177482335931, 1.684124486321957104 ) ) ;
#5081=CARTESIAN_POINT ( 'NONE',  ( 2.437156881564545685, -1.551092155746801815, -1.402114238623404896 ) ) ;
#5082=CARTESIAN_POINT ( 'NONE',  ( 0.9713206009373563932, 1.803875226702996049, -0.4951341686536685494 ) ) ;
#5083=CARTESIAN_POINT ( 'NONE',  ( 2.425157474508771838, 0.8594973679685766754, 1.823840639232063854 ) ) ;
#5086=CARTESIAN_POINT ( 'NONE',  ( 2.753125985903591477, 1.731854804227653366, -0.1727350219371779905 ) ) ;
#5090=CARTESIAN_POINT ( 'NONE',  ( 3.685938805993322909, -0.8483273805379875077, 1.501759545097125059 ) ) ;
#5091=CARTESIAN_POINT ( 'NONE',  ( 3.439196427729715566, -1.660734982795486481, -1.430121640581414111 ) ) ;
#5092=CARTESIAN_POINT ( 'NONE',  ( 6.481111342790009999, -0.1036386110354891726, -2.204582208980155222 ) ) ;
#5093=CARTESIAN_POINT ( 'NONE',  ( 6.983263157960362122, 6.035089925019382129, 2.648702789725385198 ) ) ;
#5094=CARTESIAN_POINT ( 'NONE',  ( 3.766621525425926098, -0.8750874339106663458, -1.987059052243181689 ) ) ;
#5095=CARTESIAN_POINT ( 'NONE',  ( 1.734698295210383767, 0.1775668987445792879, 1.817036636966688823 ) ) ;
#5097=CARTESIAN_POINT ( 'NONE',  ( 4.364542673910889015, -2.054697287276555873, -0.5108639600793271063 ) ) ;
#5099=CARTESIAN_POINT ( 'NONE',  ( 5.302359097629713247, 1.737542498810572322, -1.495360377712177113 ) ) ;
#5101=CARTESIAN_POINT ( 'NONE',  ( 6.620655732516672387, 6.040129668214249570, 2.321170174800915031 ) ) ;
#5103=CARTESIAN_POINT ( 'NONE',  ( 0.5926325054007793858, -1.174586488569592690, 1.765252418913294319 ) ) ;
#5110=CARTESIAN_POINT ( 'NONE',  ( 4.922500090287251773, -1.427935867408920645, -1.423962988533589158 ) ) ;
#5112=CARTESIAN_POINT ( 'NONE',  ( 3.239185349552040183, -0.1472093337855179818, -2.057344904835652688 ) ) ;
#5114=CARTESIAN_POINT ( 'NONE',  ( -0.1411974294641837879, -0.0004739540254219963859, -1.900147702309516795 ) ) ;
#5119=CARTESIAN_POINT ( 'NONE',  ( 6.615165563918417924, -2.126712762998611783, 0.5283135293715838232 ) ) ;
#5120=CARTESIAN_POINT ( 'NONE',  ( 4.166638809851969327, 1.319227567334404494, 1.525044649537968589 ) ) ;
#5121=CARTESIAN_POINT ( 'NONE',  ( 3.790429961727882713, 1.553415782126759792, -0.9881970032953185656 ) ) ;
#5125=CARTESIAN_POINT ( 'NONE',  ( 1.078623681775535914, -0.03615993657634165859, -1.724571457899269911 ) ) ;
#5127=CARTESIAN_POINT ( 'NONE',  ( 0.8624555810839064085, -0.06381188527813246025, -2.297968782114163222 ) ) ;
#5129=CARTESIAN_POINT ( 'NONE',  ( 0.4041009963523278237, -0.6015683965250936405, 2.180870993196832419 ) ) ;
#5130=CARTESIAN_POINT ( 'NONE',  ( 2.649164382713434573, -1.750592827090621917, 1.170555837024005008 ) ) ;
#5138=CARTESIAN_POINT ( 'NONE',  ( 3.709420277874009297, 1.875127481890274561, -1.190789481685197604 ) ) ;
#5139=CARTESIAN_POINT ( 'NONE',  ( 2.379091696419192381, 2.003018898301941686, -0.8894332929959417600 ) ) ;
#5143=CARTESIAN_POINT ( 'NONE',  ( 5.547302793442128177, 1.730978599593002043, -0.9233319674036490898 ) ) ;
#5145=CARTESIAN_POINT ( 'NONE',  ( 6.610000000000006537, 7.629137130509094256, 2.600000000000001421 ) ) ;
#5147=CARTESIAN_POINT ( 'NONE',  ( 4.957343421279006179, -1.817532610912236724, 1.092287347377165485 ) ) ;
#5151=CARTESIAN_POINT ( 'NONE',  ( 5.331013795412237855, 0.1550192300789655642, 2.156197635354038411 ) ) ;
#5153=CARTESIAN_POINT ( 'NONE',  ( 5.284640796330933199, 1.621094592300664106, -0.8731043043393661440 ) ) ;
#5157=CARTESIAN_POINT ( 'NONE',  ( 6.369106938980155341, 1.663098657370492672, -0.5127371055620026929 ) ) ;
#5162=CARTESIAN_POINT ( 'NONE',  ( 3.731458613173586514, -1.998165266068991253, 0.8252760040215676440 ) ) ;
#5167=CARTESIAN_POINT ( 'NONE',  ( 3.520547545725543515, 1.372905562624787024, -1.669742455111824286 ) ) ;
#5168=CARTESIAN_POINT ( 'NONE',  ( 4.798096821016461178, -1.970857504970180862, -0.05141287852120436652 ) ) ;
#5169=CARTESIAN_POINT ( 'NONE',  ( 3.848775019297555389, -0.8554209813324518130, 1.508043379464953260 ) ) ;
#5171=CARTESIAN_POINT ( 'NONE',  ( 0.3631484714031462668, 0.2087870660046411420, -2.181583536649676525 ) ) ;
#5172=CARTESIAN_POINT ( 'NONE',  ( 2.661487998672926292, -2.007448288467659214, -1.137923995292255741 ) ) ;
#5173=CARTESIAN_POINT ( 'NONE',  ( 3.286453515990275243, -2.029689310919643219, -0.3557144749045982879 ) ) ;
#5174=CARTESIAN_POINT ( 'NONE',  ( 5.917518263527802524, -1.082453682572570797, -1.612232301441741233 ) ) ;
#5180=CARTESIAN_POINT ( 'NONE',  ( 3.575398329460587554, 0.05639400328332971890, -2.206221599391814170 ) ) ;
#5183=CARTESIAN_POINT ( 'NONE',  ( 0.9712807694385624524, -0.2802886605943204490, 1.839611564956656453 ) ) ;
#5184=CARTESIAN_POINT ( 'NONE',  ( -0.1290005225502675879, 2.860092606084875033, -2.662085506130333457 ) ) ;
#5188=CARTESIAN_POINT ( 'NONE',  ( 6.825078400183574701, 2.043583509370741069, 2.350167621585138367 ) ) ;
#5189=CARTESIAN_POINT ( 'NONE',  ( 6.580030785786400216, -1.806642183828395920, -0.3538341520857649081 ) ) ;
#5191=CARTESIAN_POINT ( 'NONE',  ( 3.362233863015654300, 0.9250742651227459312, 1.841665905919416035 ) ) ;
#5197=CARTESIAN_POINT ( 'NONE',  ( 1.428666007085793277, 1.985871523383303749, 0.5506756191897729247 ) ) ;
#5204=CARTESIAN_POINT ( 'NONE',  ( 5.479209177496175087, -0.05098606815037013545, -2.206463706674952618 ) ) ;
#5205=CARTESIAN_POINT ( 'NONE',  ( 0.6323695665565836066, 1.111747700424435159, -1.853661729306683936 ) ) ;
#5207=CARTESIAN_POINT ( 'NONE',  ( 0.2511858651975951151, 0.1928294586405615574, -2.007256720055437871 ) ) ;
#5210=CARTESIAN_POINT ( 'NONE',  ( 2.360033908006432757, 0.7977434165707707470, 1.692156362554583460 ) ) ;
#5212=CARTESIAN_POINT ( 'NONE',  ( 3.134000194803722383, 2.016708403948695771, -0.004836970814638129855 ) ) ;
#5216=CARTESIAN_POINT ( 'NONE',  ( 5.092451870646586443, -2.090052423365583500, -0.2586305528886819194 ) ) ;
#5221=CARTESIAN_POINT ( 'NONE',  ( 4.043226763451240657, 0.1031935428237283348, 2.017299519520795670 ) ) ;
#5224=CARTESIAN_POINT ( 'NONE',  ( 6.760222218534770455, -2.062298699534569124, 0.04672293413533928907 ) ) ;
#5226=CARTESIAN_POINT ( 'NONE',  ( 5.255217470067075070, -1.823004960263453489, -1.161262906855420329 ) ) ;
#5231=CARTESIAN_POINT ( 'NONE',  ( 2.928372970691155430, 1.159507463759208878, 1.835456099276617570 ) ) ;
#5234=CARTESIAN_POINT ( 'NONE',  ( 2.032514702046281485, -1.644074058028240692, 0.8291662819630771786 ) ) ;
#5236=CARTESIAN_POINT ( 'NONE',  ( 3.157961424266928052, 0.9873743524775533409, 1.956624655947765357 ) ) ;
#5237=CARTESIAN_POINT ( 'NONE',  ( 6.983263157960363010, -0.009046620988246899253, 2.153544821522495489 ) ) ;
#5238=CARTESIAN_POINT ( 'NONE',  ( 3.696369045748033155, -2.259781416529721643, -0.1137371904085457408 ) ) ;
#5244=CARTESIAN_POINT ( 'NONE',  ( 5.624192029756354572, 1.053330351427090639, -1.421934073773284180 ) ) ;
#5246=CARTESIAN_POINT ( 'NONE',  ( 3.404942666290892817, -0.3948933297331903014, -1.973820178108119272 ) ) ;
#5248=CARTESIAN_POINT ( 'NONE',  ( 1.729655969393493642, -1.983145177596838948, 0.7090631796887718608 ) ) ;
#5250=CARTESIAN_POINT ( 'NONE',  ( 1.855843448759408210, -0.6666243292093411155, 1.853429361541816700 ) ) ;
#5252=CARTESIAN_POINT ( 'NONE',  ( 5.642768253578701376, 1.748184277621564808, 0.4749025624241067223 ) ) ;
#5257=CARTESIAN_POINT ( 'NONE',  ( 5.348468966913380029, 0.5439794105128460400, 1.789823788735760646 ) ) ;
#5259=CARTESIAN_POINT ( 'NONE',  ( 5.137584473783054051, 1.933663220787355419, -0.7400441640052904946 ) ) ;
#5269=CARTESIAN_POINT ( 'NONE',  ( 4.685966490639408732, -1.205361723144786845, -1.547842780461285761 ) ) ;
#5271=CARTESIAN_POINT ( 'NONE',  ( 2.179064334209149578, -0.9478932651061505732, -1.779355105811925020 ) ) ;
#5272=CARTESIAN_POINT ( 'NONE',  ( 2.448326871961825191, -1.317826014703428639, 1.390694818219958107 ) ) ;
#5273=EDGE_CURVE ( 'NONE', #36822, #70481, #131023, .T. ) ;
#5275=CARTESIAN_POINT ( 'NONE',  ( 0.5565083568685527116, -1.583368386835169783, 1.515454571103365344 ) ) ;
#5276=CARTESIAN_POINT ( 'NONE',  ( 6.639320575229251453, 0.008029245381881157731, 1.796863947021019925 ) ) ;
#5277=CARTESIAN_POINT ( 'NONE',  ( 2.565516880305099612, 1.835255434019352094, -0.3607447438512822457 ) ) ;
#5279=CARTESIAN_POINT ( 'NONE',  ( 4.043230579294037952, 0.1031557717955585846, 2.010702285795034072 ) ) ;
#5282=CARTESIAN_POINT ( 'NONE',  ( 4.200857891667449273, 1.936436120981197773, 0.8564517604346032487 ) ) ;
#5283=CARTESIAN_POINT ( 'NONE',  ( 5.898901817742318698, 0.4001337562283372451, 2.031160294743330486 ) ) ;
#5284=CARTESIAN_POINT ( 'NONE',  ( 1.259447021655529797, 2.059213905598542116, -0.3608319165549890295 ) ) ;
#5286=CARTESIAN_POINT ( 'NONE',  ( 5.913091143547532624, 1.611232972626057247, 0.8583240166551919792 ) ) ;
#5294=CARTESIAN_POINT ( 'NONE',  ( 0.9612203838427415548, -1.427409828940959136, -1.115214234437786223 ) ) ;
#5301=CARTESIAN_POINT ( 'NONE',  ( -0.1411974294642202310, -0.0004739540254597266757, -1.900147702309512132 ) ) ;
#5302=CARTESIAN_POINT ( 'NONE',  ( 0.4168467196605326053, -0.7183999135813923242, -1.995210048009891102 ) ) ;
#5304=CARTESIAN_POINT ( 'NONE',  ( -0.1394461523061326647, 2.860155921427895542, -2.768185420354400073 ) ) ;
#5308=CARTESIAN_POINT ( 'NONE',  ( 3.537912347765668208, 1.245987026601946157, 1.525231921242198307 ) ) ;
#5309=CARTESIAN_POINT ( 'NONE',  ( 4.323842328482737862, 0.8596156136044874607, -1.824127480631778653 ) ) ;
#5312=CARTESIAN_POINT ( 'NONE',  ( 4.839868765920234850, 2.185429510258177110, 0.1630863781024796955 ) ) ;
#5314=CARTESIAN_POINT ( 'NONE',  ( 2.590742828618552984, -0.3275076452619613554, -1.898194946008352035 ) ) ;
#5316=CARTESIAN_POINT ( 'NONE',  ( -0.1298852118744256712, 0.2531197755418754247, -1.761387242530809250 ) ) ;
#5317=CARTESIAN_POINT ( 'NONE',  ( 0.3818278861203865393, 2.057605126571937060, -0.7983354260262252033 ) ) ;
#5323=CARTESIAN_POINT ( 'NONE',  ( 5.207841159657320418, 0.6216970817616838119, -1.868779976745947202 ) ) ;
#5325=CARTESIAN_POINT ( 'NONE',  ( 0.01113493735188827126, -1.904398801838134148, 0.3797647843634504583 ) ) ;
#5326=CARTESIAN_POINT ( 'NONE',  ( 3.686192936682455734, 1.120187844794858556, 1.672449120617898410 ) ) ;
#5327=CARTESIAN_POINT ( 'NONE',  ( 5.378365493435281586, -0.3450152841970657858, 2.272265683862843666 ) ) ;
#5328=CARTESIAN_POINT ( 'NONE',  ( 3.414761196407948063, -1.412042937968212231, 1.212274210779472394 ) ) ;
#5333=CARTESIAN_POINT ( 'NONE',  ( 5.530836773642837656, -1.889722758269284375, 0.8948517497979097124 ) ) ;
#5338=CARTESIAN_POINT ( 'NONE',  ( 0.5920835508136900183, -1.811502216344462735, -0.2265648652611390590 ) ) ;
#5340=CARTESIAN_POINT ( 'NONE',  ( 2.531537987306311965, -1.440582175967281886, 0.9650062983845784093 ) ) ;
#5346=CARTESIAN_POINT ( 'NONE',  ( 0.6376584384039893916, 1.932990051301992418, -0.7417924570976216492 ) ) ;
#5347=CARTESIAN_POINT ( 'NONE',  ( 5.971303284387838417, 0.1295235881030691594, -1.821162830480331563 ) ) ;
#5348=CARTESIAN_POINT ( 'NONE',  ( 3.045700443693433179, 1.383923128670875746, 1.390673908496591782 ) ) ;
#5352=CARTESIAN_POINT ( 'NONE',  ( 3.721430941620011534, 1.819509361161365524, 1.088713516244857571 ) ) ;
#5353=CARTESIAN_POINT ( 'NONE',  ( 6.827182134110199918, 2.946470958711099541, 2.641117900019366527 ) ) ;
#5356=CARTESIAN_POINT ( 'NONE',  ( 1.305626334525695986, -1.629615561912756805, -1.276682400165381148 ) ) ;
#5357=CARTESIAN_POINT ( 'NONE',  ( 6.827182134110200806, 1.288579688585177685, 1.926502426867699347 ) ) ;
#5359=CARTESIAN_POINT ( 'NONE',  ( 4.494933454782477078, -2.154585855983886411, -0.5399016382821394400 ) ) ;
#5361=CARTESIAN_POINT ( 'NONE',  ( 1.495234749544295250, -2.280609600776092094, 0.2875172478875551163 ) ) ;
#5363=CARTESIAN_POINT ( 'NONE',  ( 0.5144084716053355377, 0.7454083195421266073, 1.814826383214888983 ) ) ;
#5372=CARTESIAN_POINT ( 'NONE',  ( 3.480628297764537304, -1.280852673386581264, 1.420289963180096260 ) ) ;
#5374=CARTESIAN_POINT ( 'NONE',  ( 3.715580044805122384, -1.699234090967314259, 0.2946211727567394911 ) ) ;
#5375=CARTESIAN_POINT ( 'NONE',  ( 2.395720570290179374, -1.993893129684479293, 0.3006499569925198956 ) ) ;
#5376=CARTESIAN_POINT ( 'NONE',  ( 3.780169564947546856, 1.941421826978003251, -1.230584599089700637 ) ) ;
#5377=CARTESIAN_POINT ( 'NONE',  ( 3.392113076582465858, -0.9204767452889413004, 2.066876591271109120 ) ) ;
#5378=CARTESIAN_POINT ( 'NONE',  ( 0.1357705729100426029, -2.015811560716780360, 0.8986578214904348272 ) ) ;
#5381=CARTESIAN_POINT ( 'NONE',  ( 4.657331418887999064, 0.3884847549131437705, -1.726375946583807774 ) ) ;
#5384=CARTESIAN_POINT ( 'NONE',  ( 0.9555020568867471642, 0.4423240407584581035, -2.249030425913514541 ) ) ;
#5385=CARTESIAN_POINT ( 'NONE',  ( 5.753808258465379133, 0.7501079416377672837, 1.681592913607635964 ) ) ;
#5387=CARTESIAN_POINT ( 'NONE',  ( 5.648420989521034663, -1.729380818958951460, 1.345873388983606533 ) ) ;
#5391=CARTESIAN_POINT ( 'NONE',  ( 5.564915762860970894, 1.570151797963925455, -1.349580972669261580 ) ) ;
#5392=CARTESIAN_POINT ( 'NONE',  ( 1.464077725791514517, -1.074659653367866952, 1.706114136832518779 ) ) ;
#5394=CARTESIAN_POINT ( 'NONE',  ( 4.740804336882096237, 0.3310356755545171836, 1.897698676112127725 ) ) ;
#5396=CARTESIAN_POINT ( 'NONE',  ( 1.072868727471010253, 0.9067168766181363804, 2.028134479351159314 ) ) ;
#5405=CARTESIAN_POINT ( 'NONE',  ( 4.352889007613729433, 0.3757914745146764823, -1.699215345876355476 ) ) ;
#5406=CARTESIAN_POINT ( 'NONE',  ( 2.330453122711079850, -1.209328770571056921, 1.544706564130463811 ) ) ;
#5411=CARTESIAN_POINT ( 'NONE',  ( 6.619590441841329387, 0.3365870006281460047, -1.932621868259084330 ) ) ;
#5415=CARTESIAN_POINT ( 'NONE',  ( 5.032435514249763209, 0.5899841883351600869, 1.928258608204669766 ) ) ;
#5416=CARTESIAN_POINT ( 'NONE',  ( 0.7786449305766733886, -1.254482527970951056, 1.882701536962180677 ) ) ;
#5420=CARTESIAN_POINT ( 'NONE',  ( 1.739302498465819191, -1.351291084634953066, -1.293660915597586003 ) ) ;
#5421=CARTESIAN_POINT ( 'NONE',  ( -0.1405533004718754753, 0.003749010675345095921, -1.720146753850458010 ) ) ;
#5423=CARTESIAN_POINT ( 'NONE',  ( 4.370767597569780172, -0.0006098066561242150270, -2.191739723162715592 ) ) ;
#5424=CARTESIAN_POINT ( 'NONE',  ( 5.579250153011313884, -0.04958841179729735205, -2.307219497322360535 ) ) ;
#5425=CARTESIAN_POINT ( 'NONE',  ( 0.6728171419645075924, -1.940266777691628919, -0.6950667680841491336 ) ) ;
#5426=CARTESIAN_POINT ( 'NONE',  ( 2.888542945859973177, 1.665235949713929076, -0.9988640340363763581 ) ) ;
#5430=CARTESIAN_POINT ( 'NONE',  ( 4.008435526009396455, -1.928752077057366732, 0.5880193435906443389 ) ) ;
#5434=CARTESIAN_POINT ( 'NONE',  ( 0.9612317138737861422, 0.3586375672061762887, -1.789940867121169843 ) ) ;
#5440=CARTESIAN_POINT ( 'NONE',  ( 6.543830163797104582, 0.7912256320986108538, -1.903158165889913045 ) ) ;
#5445=CARTESIAN_POINT ( 'NONE',  ( 5.338538087541965460, 1.201400599988803108, -1.623342581396812090 ) ) ;
#5446=CARTESIAN_POINT ( 'NONE',  ( 5.953820247260992460, -1.607154219335062528, -1.533616513404257198 ) ) ;
#5450=CARTESIAN_POINT ( 'NONE',  ( 5.207911835226475716, -2.051185258288893198, 0.1996322284415520676 ) ) ;
#5451=CARTESIAN_POINT ( 'NONE',  ( 4.254529844270301453, 1.955172953530256219, -0.4926405443339901269 ) ) ;
#5458=CARTESIAN_POINT ( 'NONE',  ( 4.446638634790680555, 1.314796391739967207, 1.528506369862133285 ) ) ;
#5459=CARTESIAN_POINT ( 'NONE',  ( 3.749809578975582536, 0.6641696684822319119, 1.717346325712478583 ) ) ;
#5461=CARTESIAN_POINT ( 'NONE',  ( 2.069360784497351613, -2.110879405061675929, -0.9329422106417961658 ) ) ;
#5463=CARTESIAN_POINT ( 'NONE',  ( 3.972077263441410100, 1.197190051160206936, 1.799587594625361220 ) ) ;
#5466=CARTESIAN_POINT ( 'NONE',  ( 3.198860821731682513, -1.541234334381531568, -1.705209785003541700 ) ) ;
#5469=CARTESIAN_POINT ( 'NONE',  ( 2.571000202304725590, 0.09389976206976291540, -1.868427151830873267 ) ) ;
#5470=( BOUNDED_CURVE ( )  B_SPLINE_CURVE ( 3, ( #69422, #100873, #2278, #134487 ),
 .UNSPECIFIED., .F., .T. ) 
 B_SPLINE_CURVE_WITH_KNOTS ( ( 4, 4 ),
 ( 0.000000000000000000, 0.5000000000000018874 ),
 .UNSPECIFIED. ) 
 CURVE ( )  GEOMETRIC_REPRESENTATION_ITEM ( )  RATIONAL_B_SPLINE_CURVE ( ( 1.000000000000000000, 0.3333333333333308723, 0.3333333333333333703, 1.000000000000002442 ) ) 
 REPRESENTATION_ITEM ( '' )  );
#5471=CARTESIAN_POINT ( 'NONE',  ( 6.543826718160733691, 0.7548084958455666404, -1.821436488709103019 ) ) ;
#5475=CARTESIAN_POINT ( 'NONE',  ( 2.104404934925046877, -2.206339196854599116, 0.05594281105186085790 ) ) ;
#5481=CARTESIAN_POINT ( 'NONE',  ( 6.332890595682218127, 0.1930081403669886009, 1.961983401381848457 ) ) ;
#5482=CARTESIAN_POINT ( 'NONE',  ( 5.162836451262333703, -1.674513216643868985, 1.588141549981958001 ) ) ;
#5483=CARTESIAN_POINT ( 'NONE',  ( 0.7659737006216191801, -1.952758744216346765, 0.1886366088557633325 ) ) ;
#5484=CARTESIAN_POINT ( 'NONE',  ( 3.643474114467046387, 1.866637444603681528, -0.8776443792693452428 ) ) ;
#5491=CARTESIAN_POINT ( 'NONE',  ( 6.127409529368080143, 0.1660417618732710210, -2.164901972331951363 ) ) ;
#5493=CARTESIAN_POINT ( 'NONE',  ( 4.739718475747470627, 1.836682745182907972, 0.1304020654292817605 ) ) ;
#5495=CARTESIAN_POINT ( 'NONE',  ( 6.251546423958431298, 2.185849743821382862, -0.1592787069685035195 ) ) ;
#5501=CARTESIAN_POINT ( 'NONE',  ( 2.043481384864866524, 0.6806142739823103360, -1.633949198972502570 ) ) ;
#5503=CARTESIAN_POINT ( 'NONE',  ( 6.516276865632868898, -2.012592099345715813, 0.05177761937730576691 ) ) ;
#5505=CARTESIAN_POINT ( 'NONE',  ( 3.937047882288559286, -1.594636078160330150, -1.061121380078999143 ) ) ;
#5507=CARTESIAN_POINT ( 'NONE',  ( 5.547300264688804994, 1.737891114709901208, -0.9267001309954668864 ) ) ;
#5508=CARTESIAN_POINT ( 'NONE',  ( 0.1762450972803019933, 2.096614079038420897, -0.3174041833761130360 ) ) ;
#5509=CARTESIAN_POINT ( 'NONE',  ( 3.344469905398727239, 0.4532862802011444758, 1.814783984445811127 ) ) ;
#5510=CARTESIAN_POINT ( 'NONE',  ( 6.516207646108923335, -0.8203346053292108753, -1.517322292280029350 ) ) ;
#5512=CARTESIAN_POINT ( 'NONE',  ( 3.158999515626020216, -1.670948785577108797, 1.441709373268922123 ) ) ;
#5516=CARTESIAN_POINT ( 'NONE',  ( 1.082570677935968062, 1.230128212588364356, -1.655568962787755005 ) ) ;
#5522=CARTESIAN_POINT ( 'NONE',  ( 3.490741092712910998, 2.019281663078629219, 0.4563312328872348722 ) ) ;
#5526=CARTESIAN_POINT ( 'NONE',  ( 1.383469627199322538, 0.1461868815116218467, -2.014428406654201531 ) ) ;
#5530=CARTESIAN_POINT ( 'NONE',  ( 0.1745949693968693039, 6.948552162806741705, -2.350360486623141121 ) ) ;
#5532=CARTESIAN_POINT ( 'NONE',  ( 6.046249930811113060, 1.863882344683247094, -0.7690052245405626374 ) ) ;
#5533=CARTESIAN_POINT ( 'NONE',  ( 6.174997428096934193, 1.663181612469267101, -0.9506077395253130780 ) ) ;
#5535=CARTESIAN_POINT ( 'NONE',  ( 3.825867475279482566, 1.171244075711602051, -1.852137614134836907 ) ) ;
#5537=CARTESIAN_POINT ( 'NONE',  ( 2.601700882821424976, 1.355260107747566334, 1.349524769375435973 ) ) ;
#5541=CARTESIAN_POINT ( 'NONE',  ( 0.8961114988408731552, -0.9091644883451601711, -1.799914091915676639 ) ) ;
#5543=CARTESIAN_POINT ( 'NONE',  ( 6.304242050522723240, 1.625252681175231029, -1.470355468214133543 ) ) ;
#5545=CARTESIAN_POINT ( 'NONE',  ( 3.223388876545678183, -1.662537434388009938, 0.4588695312727729125 ) ) ;
#5550=CARTESIAN_POINT ( 'NONE',  ( 0.6077679335219284829, 0.6189715888181289705, -1.861716921216026055 ) ) ;
#5558=CARTESIAN_POINT ( 'NONE',  ( 3.721195823539941827, 1.555462818066039254, 0.9281401003491447366 ) ) ;
#5563=CARTESIAN_POINT ( 'NONE',  ( 4.600164522386200439, -0.8494929878282222457, 1.599918020626096782 ) ) ;
#5567=CARTESIAN_POINT ( 'NONE',  ( 4.879284944527097601, -0.09183316818502919310, 1.858928597182760711 ) ) ;
#5569=CARTESIAN_POINT ( 'NONE',  ( 2.759290930233889494, 1.818065234828979637, -0.6036251144310407213 ) ) ;
#5573=CARTESIAN_POINT ( 'NONE',  ( 6.925078400183569904, 6.033938712579569597, 2.739235483740619426 ) ) ;
#5576=CARTESIAN_POINT ( 'NONE',  ( 0.07536363704235826688, -0.001874865094115066300, -2.144269471569634877 ) ) ;
#5577=CARTESIAN_POINT ( 'NONE',  ( 1.183663948672460942, -0.9384196385337481017, 1.868258235111931898 ) ) ;
#5579=CARTESIAN_POINT ( 'NONE',  ( 6.247092716751994068, -1.627016005604764670, 1.031123616215999794 ) ) ;
#5581=CARTESIAN_POINT ( 'NONE',  ( 2.555444900642935391, 0.4891320457309326075, -1.758753460580727790 ) ) ;
#5583=CARTESIAN_POINT ( 'NONE',  ( 1.740342883905017013, 1.098329146349947827, -1.565357986077076990 ) ) ;
#5584=CARTESIAN_POINT ( 'NONE',  ( 2.137097444212227693, -0.09349721708603592196, -1.967446466973846952 ) ) ;
#5585=CARTESIAN_POINT ( 'NONE',  ( 3.966302600639686204, -1.813262256789631266, -0.6959421042645166366 ) ) ;
#5591=CARTESIAN_POINT ( 'NONE',  ( 4.359710196644346780, -1.641147893522959089, -1.343014508298406628 ) ) ;
#5595=ORIENTED_EDGE ( 'NONE', *, *, #99713, .F. ) ;
#5598=CARTESIAN_POINT ( 'NONE',  ( 4.213378774425760476, -0.3099129147984269195, 1.799030153321119263 ) ) ;
#5603=CARTESIAN_POINT ( 'NONE',  ( 4.188257260935820625, -1.850246793840780279, -0.2747695030091561463 ) ) ;
#5605=CARTESIAN_POINT ( 'NONE',  ( 2.543477943364984117, -1.427709268621931260, -1.293647605089723429 ) ) ;
#5606=CARTESIAN_POINT ( 'NONE',  ( 6.491066726104213203, 0.1889763263339637456, 1.952597990788194959 ) ) ;
#5612=CARTESIAN_POINT ( 'NONE',  ( 1.159931391799984279, 1.264437666799199889, 1.698043086552150749 ) ) ;
#5617=CARTESIAN_POINT ( 'NONE',  ( 4.786024367859083029, -1.269482053145968514, -1.635305934682528717 ) ) ;
#5618=CARTESIAN_POINT ( 'NONE',  ( 0.2218712608162629052, 1.761692264604281633, 0.5354471447000588302 ) ) ;
#5621=CARTESIAN_POINT ( 'NONE',  ( 5.485083606918717436, -2.298851034700015727, -0.002838145216723860897 ) ) ;
#5624=CARTESIAN_POINT ( 'NONE',  ( 0.9379084653730703769, 0.9244841788896654977, -2.097747560502453812 ) ) ;
#5627=CARTESIAN_POINT ( 'NONE',  ( 4.628815217244971691, -1.774851831708891714, 0.7884768782448601243 ) ) ;
#5628=VERTEX_POINT ( 'NONE', #45808 ) ;
#5631=CARTESIAN_POINT ( 'NONE',  ( 6.433860211133586304, -1.853236450885078712, 0.4715264990977630077 ) ) ;
#5632=CARTESIAN_POINT ( 'NONE',  ( 5.665250009225348826, 1.861346387706263261, -0.7762253298396750711 ) ) ;
#5636=CARTESIAN_POINT ( 'NONE',  ( 3.205106881211945868, -0.4073652088906943858, 2.050380944992454602 ) ) ;
#5637=CARTESIAN_POINT ( 'NONE',  ( 1.234804682044550850, -1.602240143502192238, 0.7520855130052228610 ) ) ;
#5641=CARTESIAN_POINT ( 'NONE',  ( 3.679849949768813744, -1.130634651955428671, 1.993948080406320766 ) ) ;
#5642=CARTESIAN_POINT ( 'NONE',  ( 2.659766076405935653, -1.200293992427956757, 1.260412480424155435 ) ) ;
#5645=CARTESIAN_POINT ( 'NONE',  ( 2.565452462605917638, 1.394811117528846900, -1.029664540377094761 ) ) ;
#5646=CARTESIAN_POINT ( 'NONE',  ( 2.735037655519993560, -2.077075009683257090, -0.6322084445426826571 ) ) ;
#5648=CARTESIAN_POINT ( 'NONE',  ( 5.120327457147888950, 1.987497208294352280, 0.3399611521368098854 ) ) ;
#5649=CARTESIAN_POINT ( 'NONE',  ( 2.687500000000001332, -1.451031289061010421, 1.451031289061227136 ) ) ;
#5652=CARTESIAN_POINT ( 'NONE',  ( 0.7098319175448050133, -1.917404841279496397, 0.1857973779731073583 ) ) ;
#5654=CARTESIAN_POINT ( 'NONE',  ( 4.342156631555553759, -1.367984123109561301, -1.750111109629876260 ) ) ;
#5656=CARTESIAN_POINT ( 'NONE',  ( -0.1110810684432960160, 0.2482034880273851774, -1.831546034005934853 ) ) ;
#5661=CARTESIAN_POINT ( 'NONE',  ( 1.084998894000373637, -1.405142754555653628, 1.720412613360406295 ) ) ;
#5663=CARTESIAN_POINT ( 'NONE',  ( 5.951606347324344348, 1.484592722905058171, 1.282605414028796353 ) ) ;
#5666=CARTESIAN_POINT ( 'NONE',  ( 0.3687372981288695728, -1.412185959430117821, 1.636573055046482983 ) ) ;
#5668=CARTESIAN_POINT ( 'NONE',  ( 3.385269252200762580, 0.04793456357342047724, 2.062272590435239028 ) ) ;
#5673=CARTESIAN_POINT ( 'NONE',  ( 5.079306140367803479, 1.745876537259077432, -0.6719496041647440299 ) ) ;
#5674=CARTESIAN_POINT ( 'NONE',  ( 3.726996057929339745, 1.726255173046949309, 0.1649803145151728934 ) ) ;
#5675=CARTESIAN_POINT ( 'NONE',  ( 3.772797691900576567, 1.637269354731695881, -0.5906731273508105673 ) ) ;
#5676=CARTESIAN_POINT ( 'NONE',  ( 1.259778491951433654, 2.257442302724984806, -0.3979086512072607107 ) ) ;
#5678=CARTESIAN_POINT ( 'NONE',  ( 4.933190498422773018, -1.479524406611672394, -1.477502780037798447 ) ) ;
#5679=CARTESIAN_POINT ( 'NONE',  ( 6.667919370488161412, -1.192936252400189190, 1.533121312111614065 ) ) ;
#5683=CARTESIAN_POINT ( 'NONE',  ( 0.7916389524552720491, 1.525042296397002284, -1.319230309296010928 ) ) ;
#5684=CARTESIAN_POINT ( 'NONE',  ( 0.7562902151678205787, 0.8540304730459827853, -1.941197329821432227 ) ) ;
#5689=CARTESIAN_POINT ( 'NONE',  ( 2.139458383197485603, 0.002846582261652879763, 2.120667954922689002 ) ) ;
#5691=CARTESIAN_POINT ( 'NONE',  ( 4.353998665852670591, 1.825246345946249571, -0.04724550102237072557 ) ) ;
#5698=CARTESIAN_POINT ( 'NONE',  ( 1.881123716185427286, -1.848401041775033171, -0.8146170886813360879 ) ) ;
#5699=CARTESIAN_POINT ( 'NONE',  ( 5.104599427727727345, -0.7392731805347593221, -2.079399364341961487 ) ) ;
#5701=CARTESIAN_POINT ( 'NONE',  ( 4.047575586610673071, 1.345269348194571668, 1.286062638920927537 ) ) ;
#5707=CARTESIAN_POINT ( 'NONE',  ( 4.600122369450095228, -1.825375079466069694, -0.04201004182294298950 ) ) ;
#5711=CARTESIAN_POINT ( 'NONE',  ( 0.5437846328400409712, 1.620832503561630666, -0.6162787013818531445 ) ) ;
#5712=CARTESIAN_POINT ( 'NONE',  ( 0.6557207866510657013, -1.263530833501663952, 1.197007909421362370 ) ) ;
#5713=CARTESIAN_POINT ( 'NONE',  ( 5.918676688095830585, 1.554283316268306292, -1.705954940095489203 ) ) ;
#5715=CARTESIAN_POINT ( 'NONE',  ( 1.827488212121135769, -1.941439008138484246, 0.6915448510415463934 ) ) ;
#5718=CARTESIAN_POINT ( 'NONE',  ( 0.3509351863830567075, -0.9528684895154272416, 1.776737725368633614 ) ) ;
#5721=CARTESIAN_POINT ( 'NONE',  ( 5.647288160985431738, -1.475499438119257878, -1.149758287351684949 ) ) ;
#5722=CARTESIAN_POINT ( 'NONE',  ( 3.269685606991072468, 0.4601866041431811327, -1.856093204100267124 ) ) ;
#5724=CARTESIAN_POINT ( 'NONE',  ( 5.268293329372571776, 1.085216321637239023, 1.921556908365213312 ) ) ;
#5729=CARTESIAN_POINT ( 'NONE',  ( 5.813165546740090228, 1.733599321496303691, -1.220823391460408303 ) ) ;
#5730=CARTESIAN_POINT ( 'NONE',  ( 1.993646994336109257, 2.007229749184535450, -1.138263614794749801 ) ) ;
#5731=CARTESIAN_POINT ( 'NONE',  ( 3.683996026499200660, -1.166640140252427793, -1.577160851978461009 ) ) ;
#5733=CARTESIAN_POINT ( 'NONE',  ( 0.7956631384608278124, -1.383255022760669251, -1.391342014947573924 ) ) ;
#5737=CARTESIAN_POINT ( 'NONE',  ( 6.262907710099243630, -0.1037740067610822270, -2.014008436551452785 ) ) ;
#5740=CARTESIAN_POINT ( 'NONE',  ( 0.3043191165176574176, 1.600368420507289668, 0.9101283655772866021 ) ) ;
#5741=CARTESIAN_POINT ( 'NONE',  ( 3.432658224824499893, -1.297079494776206543, 1.740850151316934991 ) ) ;
#5744=CARTESIAN_POINT ( 'NONE',  ( 0.8793290508635929204, -1.919567575575848339, -0.9014759086384205311 ) ) ;
#5749=CARTESIAN_POINT ( 'NONE',  ( 0.5267265402719328860, 1.971218143044730420, 0.6008300406652696823 ) ) ;
#5755=CARTESIAN_POINT ( 'NONE',  ( 3.352119889487484183, 0.8575151890419380196, -1.709291564166728783 ) ) ;
#5756=CARTESIAN_POINT ( 'NONE',  ( 5.770295338139614927, -1.120113875738535825, 1.370259874377998788 ) ) ;
#5759=CARTESIAN_POINT ( 'NONE',  ( 0.7206316775285178666, 1.371080193274256676, -1.184091668402836639 ) ) ;
#5761=CARTESIAN_POINT ( 'NONE',  ( 0.6201578395632812990, 1.887877179178775400, 0.3243255173654129297 ) ) ;
#5762=CARTESIAN_POINT ( 'NONE',  ( 1.996617168637443429, 2.047528291220417351, 0.3059219562495316125 ) ) ;
#5764=CARTESIAN_POINT ( 'NONE',  ( 6.420764531294745225, 1.746252128813120086, 0.6712297951826234899 ) ) ;
#5765=CARTESIAN_POINT ( 'NONE',  ( 3.193790821891542731, -0.7392406677243367197, 1.669511829839696260 ) ) ;
#5766=CARTESIAN_POINT ( 'NONE',  ( 0.5929126122562259349, -2.290994082922478636, -0.2767204673215419852 ) ) ;
#5771=CARTESIAN_POINT ( 'NONE',  ( 4.668458352237446540, -0.8791470107305986437, -1.866060610730088332 ) ) ;
#5775=CARTESIAN_POINT ( 'NONE',  ( 0.1753634416057497925, 0.0001173177735149660839, -2.144164757042037017 ) ) ;
#5777=CARTESIAN_POINT ( 'NONE',  ( 6.355931484454268698, -0.7012994977402075003, 1.948090369817329526 ) ) ;
#5779=CARTESIAN_POINT ( 'NONE',  ( 3.602937629199114422, 1.706465849011789881, -1.326752773236601124 ) ) ;
#5780=CARTESIAN_POINT ( 'NONE',  ( 4.143226661672769318, 0.1011831993794048007, 2.017277399227022094 ) ) ;
#5781=CARTESIAN_POINT ( 'NONE',  ( 6.620655732516651071, 4.689394895873098434, 2.736297475404291024 ) ) ;
#5787=CARTESIAN_POINT ( 'NONE',  ( 2.325407997918966796, -1.497503195670712328, -1.350734289967000512 ) ) ;
#5792=CARTESIAN_POINT ( 'NONE',  ( 5.906500813101931868, -1.903809282439900219, -0.1807861040028224398 ) ) ;
#5796=CARTESIAN_POINT ( 'NONE',  ( 4.007435537932837910, -1.928747227692016564, 0.5880391185724976877 ) ) ;
#5799=CARTESIAN_POINT ( 'NONE',  ( 6.510786919798099426, 1.273903079158642981, -1.162983891536113479 ) ) ;
#5804=CARTESIAN_POINT ( 'NONE',  ( 4.956247902659736582, 0.7144662795386286236, 1.728917671469521800 ) ) ;
#5805=CARTESIAN_POINT ( 'NONE',  ( 0.06508986333318785011, -1.615617207129100397, 1.200762793324720690 ) ) ;
#5808=CARTESIAN_POINT ( 'NONE',  ( 2.623957243734816647, 2.031168598393529034, -0.3995267358143372860 ) ) ;
#5810=ORIENTED_EDGE ( 'NONE', *, *, #123967, .T. ) ;
#5812=CARTESIAN_POINT ( 'NONE',  ( 0.5621253344089729431, -1.117812357707391069, 1.678020072846800659 ) ) ;
#5814=CARTESIAN_POINT ( 'NONE',  ( 1.564434226245875026, 0.5705330181091838870, 1.719429346978663897 ) ) ;
#5821=CARTESIAN_POINT ( 'NONE',  ( 6.099236069963973605, -0.2290726985337887822, 1.901777391499546166 ) ) ;
#5832=CARTESIAN_POINT ( 'NONE',  ( 2.958072429731005926, 2.151414462573512765, -0.2105227563667099733 ) ) ;
#5836=CARTESIAN_POINT ( 'NONE',  ( 0.5453776912951785460, 0.1620316879334358084, 2.114494688702214020 ) ) ;
#5837=CARTESIAN_POINT ( 'NONE',  ( 5.579063851370913873, -0.04688903583028104782, -1.825137680102270288 ) ) ;
#5838=CARTESIAN_POINT ( 'NONE',  ( 1.704304553464238703, -0.7057161435466070554, -1.840894384558971808 ) ) ;
#5839=CARTESIAN_POINT ( 'NONE',  ( 4.465046277278037934, -1.532637281380120564, 1.143568071694904598 ) ) ;
#5842=CARTESIAN_POINT ( 'NONE',  ( 4.492606276566666779, 1.931098607525572497, 0.3863565733641035616 ) ) ;
#5843=CARTESIAN_POINT ( 'NONE',  ( 0.2693405865131668353, 1.117251289913205881, 1.588187351064213715 ) ) ;
#5850=CARTESIAN_POINT ( 'NONE',  ( 5.039673278062164918, -1.814583965733532978, 0.6035816954967700987 ) ) ;
#5852=CARTESIAN_POINT ( 'NONE',  ( 0.7103623821160671703, -2.195938746145317477, 0.2182302698266261887 ) ) ;
#5853=CARTESIAN_POINT ( 'NONE',  ( 5.830732115328919996, 1.350214353519451960, -1.493314199452821178 ) ) ;
#5854=CARTESIAN_POINT ( 'NONE',  ( 0.07680821025394035662, 2.052785608010514018, -2.228496998325917744 ) ) ;
#5857=CARTESIAN_POINT ( 'NONE',  ( 3.525891238081062085, 2.020528833579691597, -0.4508363271973143127 ) ) ;
#5861=CARTESIAN_POINT ( 'NONE',  ( 0.4620835240300471547, 2.137967531602209981, -0.3185850937674692407 ) ) ;
#5866=CARTESIAN_POINT ( 'NONE',  ( 6.825078400183548055, 2.475450427997231362, 2.140471860334830279 ) ) ;
#5868=CARTESIAN_POINT ( 'NONE',  ( 4.975145882941295561, -1.721944285756441984, -0.2046304421847028043 ) ) ;
#5870=CARTESIAN_POINT ( 'NONE',  ( 2.079047829753433163, 1.930162853665925216, 0.7490395704240898622 ) ) ;
#5871=CARTESIAN_POINT ( 'NONE',  ( 4.376635333690025220, -0.4654363970535125294, -2.065280895323940324 ) ) ;
#5874=CARTESIAN_POINT ( 'NONE',  ( 1.920693274676561924, -1.396391452584997417, 1.389085034315578060 ) ) ;
#5875=CARTESIAN_POINT ( 'NONE',  ( 0.4043728756845180183, -1.898191424145349471, -0.2318213773434482650 ) ) ;
#5876=CARTESIAN_POINT ( 'NONE',  ( 5.349693066923443041, 2.289838395228523282, -0.1081633463214677210 ) ) ;
#5877=CARTESIAN_POINT ( 'NONE',  ( 2.209345402013741300, -0.4006574107652469130, 1.781019818369505847 ) ) ;
#5881=CARTESIAN_POINT ( 'NONE',  ( 3.199479786217104493, 1.818179288054132536, -0.8647478076822049387 ) ) ;
#5882=CARTESIAN_POINT ( 'NONE',  ( 3.520314338623427020, 0.8779579967637550775, 1.754372790864023646 ) ) ;
#5887=CARTESIAN_POINT ( 'NONE',  ( 5.736299646367586824, 0.4068676293152873602, 2.050479918790772960 ) ) ;
#5888=CARTESIAN_POINT ( 'NONE',  ( 4.311239457809501907, -0.3017279273445966914, 1.743759454612598070 ) ) ;
#5891=CARTESIAN_POINT ( 'NONE',  ( 0.2698121887318750689, 1.265274936352598134, 1.789097752032620114 ) ) ;
#5892=CARTESIAN_POINT ( 'NONE',  ( 0.2393033055489251493, 1.735545043620636996, 0.1309560527960016429 ) ) ;
#5894=CARTESIAN_POINT ( 'NONE',  ( 0.1333692844072559003, 2.872395615372814515, -2.542035612928101873 ) ) ;
#5895=CARTESIAN_POINT ( 'NONE',  ( 0.1464030204712711281, -0.1495716826577230818, -2.263613701224455710 ) ) ;
#5897=CARTESIAN_POINT ( 'NONE',  ( 5.290307710256559659, -1.645723771949607173, 0.5459688634881465497 ) ) ;
#5898=CARTESIAN_POINT ( 'NONE',  ( 1.998912159191484905, -0.5904864226158462737, -2.126349760018491963 ) ) ;
#5899=CARTESIAN_POINT ( 'NONE',  ( 0.4269466478069834925, -1.418992435970769739, 1.643201522047117669 ) ) ;
#5901=CARTESIAN_POINT ( 'NONE',  ( 0.8489989883206483512, -1.916807839401615476, -0.8996751459469201073 ) ) ;
#5902=CARTESIAN_POINT ( 'NONE',  ( 4.437500000000002665, 1.451031289060936480, -1.451031289061293528 ) ) ;
#5904=CARTESIAN_POINT ( 'NONE',  ( 4.190394698586521471, -1.905300493120251515, -0.2835615876582204820 ) ) ;
#5905=CARTESIAN_POINT ( 'NONE',  ( 0.9794852244889130644, -2.010350447809361896, -0.9450808295136583492 ) ) ;
#5907=CARTESIAN_POINT ( 'NONE',  ( 1.347684858569838440, 0.6597076516901092536, -2.195415608770342253 ) ) ;
#5911=CARTESIAN_POINT ( 'NONE',  ( 3.809420206217276395, 1.876102094647231988, -1.189034995700769981 ) ) ;
#5919=CARTESIAN_POINT ( 'NONE',  ( 1.494767762416524093, -2.000856930885573259, 0.2496086726550551249 ) ) ;
#5921=CARTESIAN_POINT ( 'NONE',  ( 6.689892334039674537, -1.344252178338888992, -1.564594595144116695 ) ) ;
#5924=CARTESIAN_POINT ( 'NONE',  ( 6.374529642495492254, -0.09526421964337064563, -1.737987611564382862 ) ) ;
#5927=CARTESIAN_POINT ( 'NONE',  ( 1.334804486018669856, -1.602990312956679597, 0.7502176981645010123 ) ) ;
#5928=CARTESIAN_POINT ( 'NONE',  ( 6.592404480832670721, -0.3601991968599608795, 1.702173051257379832 ) ) ;
#5929=CARTESIAN_POINT ( 'NONE',  ( 6.251467208264422482, 1.735085017428819931, -0.1376019381845137446 ) ) ;
#5930=CARTESIAN_POINT ( 'NONE',  ( 3.878722286802076535, -0.2252994024176681598, -2.281293266731793778 ) ) ;
#5931=CARTESIAN_POINT ( 'NONE',  ( 3.310337721246572773, 1.664907390794263531, 0.7863323413084821745 ) ) ;
#5934=CARTESIAN_POINT ( 'NONE',  ( 4.700122295916242088, -1.825221593135372578, -0.04401369772454033491 ) ) ;
#5935=CARTESIAN_POINT ( 'NONE',  ( 5.151017605526480025, 0.9962996879465220168, 1.753031629501592192 ) ) ;
#5937=CARTESIAN_POINT ( 'NONE',  ( 3.010884265427976825, 1.639692042162781194, -1.559206548184206564 ) ) ;
#5939=CARTESIAN_POINT ( 'NONE',  ( 5.544006925699364707, 0.8563935509715396854, -1.924162301928746821 ) ) ;
#5941=CARTESIAN_POINT ( 'NONE',  ( 3.771986465066007099, -2.040223509676724500, 0.3510349978646867264 ) ) ;
#5944=CARTESIAN_POINT ( 'NONE',  ( 5.373730994130428762, 0.4134100146411868737, -2.079626175754036410 ) ) ;
#5947=CARTESIAN_POINT ( 'NONE',  ( 0.9086680563264810662, 1.459560178543020559, -1.257504221390127519 ) ) ;
#5949=CARTESIAN_POINT ( 'NONE',  ( 0.3792734414799744380, -0.1002090192285705339, 1.967142940827655284 ) ) ;
#5954=CARTESIAN_POINT ( 'NONE',  ( 0.9849990780092006126, -1.403669121040777457, 1.721781922543249799 ) ) ;
#5955=CARTESIAN_POINT ( 'NONE',  ( 2.784315802839703036, -1.083654668052931536, 1.805616322045165312 ) ) ;
#5958=CARTESIAN_POINT ( 'NONE',  ( 1.047037934171668905, 1.643801913826014482, -0.8725737860223039544 ) ) ;
#5964=CARTESIAN_POINT ( 'NONE',  ( 0.7914572142167939361, -0.05789999323873443182, -2.119991495365561640 ) ) ;
#5967=CARTESIAN_POINT ( 'NONE',  ( 3.262109210011232108, -1.959739898415867154, 0.09363895518171151677 ) ) ;
#5968=CARTESIAN_POINT ( 'NONE',  ( 1.745224485312408813, -1.826185749030174499, 1.156423465944363294 ) ) ;
#5969=CARTESIAN_POINT ( 'NONE',  ( 1.927068723821170559, -1.203646435588998198, -1.393412863611859454 ) ) ;
#5972=CARTESIAN_POINT ( 'NONE',  ( 3.661793474361102252, -1.167423004587186952, 1.290856655984705670 ) ) ;
#5976=CARTESIAN_POINT ( 'NONE',  ( 0.6905621207787122628, -2.145541755201633372, -0.2633910710312590275 ) ) ;
#5978=CARTESIAN_POINT ( 'NONE',  ( 2.882185300971401798, -0.2004049647258976941, 2.006138917898095730 ) ) ;
#5979=CARTESIAN_POINT ( 'NONE',  ( 6.825078400183577365, 2.023440267519378999, 2.448151054272352578 ) ) ;
#5980=CARTESIAN_POINT ( 'NONE',  ( 0.6554165194554737450, -1.826866057147133349, -1.155366728873077342 ) ) ;
#5981=CARTESIAN_POINT ( 'NONE',  ( 1.744934968351062210, -1.666494570726485991, 1.053036000364399483 ) ) ;
#5982=CARTESIAN_POINT ( 'NONE',  ( 6.609000000000034625, 7.052688111495289291, 2.598153854230552895 ) ) ;
#5983=CARTESIAN_POINT ( 'NONE',  ( 2.015084816950295732, -1.883260942463622856, 0.4737542896416384597 ) ) ;
#5984=FACE_OUTER_BOUND ( 'NONE', #161098, .T. ) ;
#5988=CARTESIAN_POINT ( 'NONE',  ( -0.1108833634137010027, 2.037774818562386514, -2.313487243312782216 ) ) ;
#5993=CARTESIAN_POINT ( 'NONE',  ( 6.405331179067034419, 1.913585160600343782, 1.289386977092843889 ) ) ;
#5994=CARTESIAN_POINT ( 'NONE',  ( 6.812952578306354035, -1.517200236233799071, 1.243500037895750143 ) ) ;
#5995=CARTESIAN_POINT ( 'NONE',  ( 4.205873059901494848, 0.6649649114027419428, -1.845726756006949909 ) ) ;
#5997=CARTESIAN_POINT ( 'NONE',  ( 1.934220422044399035, -1.621183349045727473, -1.198859219795316955 ) ) ;
#5999=CARTESIAN_POINT ( 'NONE',  ( 2.237658791021436056, 0.5595254372263277487, -2.042044324946710621 ) ) ;
#6004=CARTESIAN_POINT ( 'NONE',  ( 3.029072736150268952, -1.236975958831527445, -1.363863411116640334 ) ) ;
#6005=ORIENTED_EDGE ( 'NONE', *, *, #94249, .T. ) ;
#6008=CARTESIAN_POINT ( 'NONE',  ( 4.553055379497691568, 0.3652949536288411791, 2.088752307168060707 ) ) ;
#6009=CARTESIAN_POINT ( 'NONE',  ( 0.07576575995338691305, -1.785066692240460551, -0.4505573523648154222 ) ) ;
#6014=CARTESIAN_POINT ( 'NONE',  ( 3.901680821178232339, -0.6019389665811913925, 1.970883251864594454 ) ) ;
#6016=CARTESIAN_POINT ( 'NONE',  ( 1.944624168438695566, -1.479605912621816621, -1.095697124569312564 ) ) ;
#6021=CARTESIAN_POINT ( 'NONE',  ( 0.7157882511714327434, -0.3199875008889854766, 2.183444778895065941 ) ) ;
#6022=CARTESIAN_POINT ( 'NONE',  ( 4.007294123747324299, 1.937827550919896336, 1.167430888521280963 ) ) ;
#6024=CARTESIAN_POINT ( 'NONE',  ( 3.955163173390123799, -1.573275279051716158, 0.8980309717551668847 ) ) ;
#6025=EDGE_CURVE ( 'NONE', #137219, #194636, #141360, .T. ) ;
#6026=CARTESIAN_POINT ( 'NONE',  ( 4.153473468168114913, 1.856699357379907989, -0.4712526737844865976 ) ) ;
#6027=CARTESIAN_POINT ( 'NONE',  ( 5.582505937350194181, 1.236201877336528643, -1.660625051266072960 ) ) ;
#6029=CARTESIAN_POINT ( 'NONE',  ( 4.205908039233514195, -1.966248567454803364, 0.1440612947745979200 ) ) ;
#6030=CARTESIAN_POINT ( 'NONE',  ( 1.114139429068806919, -0.8636777455973219109, -1.721994443286285259 ) ) ;
#6031=CARTESIAN_POINT ( 'NONE',  ( 3.625732356982212412, -1.113523340526129335, -1.502988901547596567 ) ) ;
#6032=CARTESIAN_POINT ( 'NONE',  ( 3.967613463194498813, 0.2842429903056520324, -2.290057832888813483 ) ) ;
#6033=CARTESIAN_POINT ( 'NONE',  ( 3.261990205869094162, -1.859054838292145240, 0.08865997893938745711 ) ) ;
#6036=CARTESIAN_POINT ( 'NONE',  ( 2.209725257209711469, -0.4604840958662699268, 2.054942820982478935 ) ) ;
#6041=CARTESIAN_POINT ( 'NONE',  ( 3.568700945156903614, 0.7666329941097769218, 1.977337035738421900 ) ) ;
#6043=CARTESIAN_POINT ( 'NONE',  ( 1.177996693904998615, 1.989173073321507612, -0.3494277517126374577 ) ) ;
#6049=CARTESIAN_POINT ( 'NONE',  ( 1.036653925908154639, 2.129443126370239803, 0.3705773954724436159 ) ) ;
#6052=CARTESIAN_POINT ( 'NONE',  ( 6.825078400183510752, 3.697836898538444217, 2.470016017273040543 ) ) ;
#6055=CARTESIAN_POINT ( 'NONE',  ( 5.647672796105281279, 1.985869605424210649, -0.3494789899042491932 ) ) ;
#6057=CARTESIAN_POINT ( 'NONE',  ( 6.304249618663324561, 1.548718018665395713, -1.404690827926929453 ) ) ;
#6059=CARTESIAN_POINT ( 'NONE',  ( 0.8840797711214362087, 1.521441056815290516, 1.674750314396955542 ) ) ;
#6062=CARTESIAN_POINT ( 'NONE',  ( 4.311732611912100666, -1.244383703160652610, -1.586670621409623116 ) ) ;
#6064=CARTESIAN_POINT ( 'NONE',  ( 1.440887319015681012, -1.643870157486097217, -0.9831960898977005758 ) ) ;
#6068=CARTESIAN_POINT ( 'NONE',  ( 3.351896425306086336, 1.725068445106912707, -0.001234800371389954687 ) ) ;
#6070=CARTESIAN_POINT ( 'NONE',  ( 1.791920237496129609, -1.760627435414298558, -0.1794978127376868071 ) ) ;
#6071=CARTESIAN_POINT ( 'NONE',  ( 5.051906976816819217, 0.6964463896041681590, -2.094057263239030853 ) ) ;
#6075=CARTESIAN_POINT ( 'NONE',  ( 4.354221869268804390, 0.9056986662851629344, -1.917456963280274040 ) ) ;
#6076=CARTESIAN_POINT ( 'NONE',  ( 4.323842328482737862, 0.8596156136044875717, -1.824127480631778875 ) ) ;
#6080=CARTESIAN_POINT ( 'NONE',  ( 1.920565142479381038, 1.744437793965779582, 0.6759427408406930571 ) ) ;
#6082=CARTESIAN_POINT ( 'NONE',  ( -0.1935108285373255133, -0.3924519521045151671, -1.774502223569380144 ) ) ;
#6088=CARTESIAN_POINT ( 'NONE',  ( 0.4395310841842985927, -1.815173276516974799, 0.6020934215927519206 ) ) ;
#6094=CARTESIAN_POINT ( 'NONE',  ( 4.658503719480325600, 2.115088938745744329, 0.1532479335744420801 ) ) ;
#6095=CARTESIAN_POINT ( 'NONE',  ( -0.1294898018151836583, 2.884012836773319766, -2.415168928093185396 ) ) ;
#6097=CARTESIAN_POINT ( 'NONE',  ( 5.219980872528355853, -1.052265754357907701, -1.666845346888909729 ) ) ;
#6099=CARTESIAN_POINT ( 'NONE',  ( 0.5275904727545431827, -0.2913634075805496271, 1.991877199276798516 ) ) ;
#6101=CARTESIAN_POINT ( 'NONE',  ( 0.2459221440733790898, 2.093483123843339122, -0.3155690596675052584 ) ) ;
#6102=CARTESIAN_POINT ( 'NONE',  ( 1.662640112210824306, -0.7432673875312334477, -1.932532381715674097 ) ) ;
#6106=CARTESIAN_POINT ( 'NONE',  ( 4.330081446525359645, 2.050255175485806269, 0.4079974934644239326 ) ) ;
#6108=CARTESIAN_POINT ( 'NONE',  ( 3.117977517195897441, -0.8984765085307615529, -1.589086709143338272 ) ) ;
#6109=CARTESIAN_POINT ( 'NONE',  ( 1.277659230087615727, 1.784704083969153920, -0.3092532468622013475 ) ) ;
#6113=CARTESIAN_POINT ( 'NONE',  ( 4.454274341225270994, 2.206355006892012138, -0.05062909709598743119 ) ) ;
#6117=CARTESIAN_POINT ( 'NONE',  ( 2.402860538037488780, -0.3286879766849961082, -1.883663324302800035 ) ) ;
#6120=CARTESIAN_POINT ( 'NONE',  ( 6.619590326553026038, 0.3579758704960536719, -2.039031579972025554 ) ) ;
#6122=CARTESIAN_POINT ( 'NONE',  ( 5.794512526436308875, 1.792401445336734733, -1.260760892635464980 ) ) ;
#6128=CARTESIAN_POINT ( 'NONE',  ( 3.215925951850879816, -0.9189154559356220719, -1.629173103855706906 ) ) ;
#6133=CARTESIAN_POINT ( 'NONE',  ( 6.737176827083626307, -0.09545985418329960837, -2.068160202195384656 ) ) ;
#6134=CARTESIAN_POINT ( 'NONE',  ( 0.6324356828835416833, 0.5880426346329314935, 1.928746166857209676 ) ) ;
#6137=CARTESIAN_POINT ( 'NONE',  ( 1.939652437182255662, 0.8368340126228106524, -2.025574644071465258 ) ) ;
#6138=CARTESIAN_POINT ( 'NONE',  ( 5.496661139185262002, -0.4475443406098400523, -1.769863040007889410 ) ) ;
#6146=CARTESIAN_POINT ( 'NONE',  ( 3.087279721815265443, -0.7436087841871074078, 1.684586988852328160 ) ) ;
#6147=CARTESIAN_POINT ( 'NONE',  ( 6.275645410888611941, 0.3399709936107355168, -1.984134265935801000 ) ) ;
#6148=CARTESIAN_POINT ( 'NONE',  ( 1.476342052747819045, 2.027250371889641301, 1.083024425860839690 ) ) ;
#6150=CARTESIAN_POINT ( 'NONE',  ( 0.3911518402437937358, -1.704754640775848928, 0.7467128926999586636 ) ) ;
#6153=CARTESIAN_POINT ( 'NONE',  ( 3.093911922779784440, 1.216618333484908998, 1.475457842794763996 ) ) ;
#6158=CARTESIAN_POINT ( 'NONE',  ( 2.454727380131729753, -1.820530515947630379, -1.027877103350574250 ) ) ;
#6159=CARTESIAN_POINT ( 'NONE',  ( 1.639302681421180852, -1.352760811461351187, -1.292285834730775074 ) ) ;
#6160=CARTESIAN_POINT ( 'NONE',  ( 1.581407437776818581, 1.356094323556347181, -1.492024998029889638 ) ) ;
#6163=CARTESIAN_POINT ( 'NONE',  ( 3.403587037673636129, -0.7086591031593177936, -1.589830453666951415 ) ) ;
#6167=CARTESIAN_POINT ( 'NONE',  ( 3.808989599770518097, 1.480563749658039052, 0.8846867361136273589 ) ) ;
#6169=CARTESIAN_POINT ( 'NONE',  ( 2.243918346939121733, 2.191141468336772036, 0.05030144379260945153 ) ) ;
#6170=CARTESIAN_POINT ( 'NONE',  ( 5.356176587289051660, 2.204499490778097481, -0.1052899746726426722 ) ) ;
#6172=CARTESIAN_POINT ( 'NONE',  ( 3.889651762418313119, -2.008042162167834377, 0.8258804214429303903 ) ) ;
#6173=CARTESIAN_POINT ( 'NONE',  ( 2.613660848560446226, -1.805822647967849193, 0.2677728182119283318 ) ) ;
#6175=CARTESIAN_POINT ( 'NONE',  ( 4.839118085652931001, -1.790413437384326789, -1.129994989630648261 ) ) ;
#6176=CARTESIAN_POINT ( 'NONE',  ( 6.639320575229259447, 2.969246179279591225, 2.450030562065998119 ) ) ;
#6179=CARTESIAN_POINT ( 'NONE',  ( 4.546573649138107243, -1.841725595444974939, 1.364713657601625885 ) ) ;
#6183=CARTESIAN_POINT ( 'NONE',  ( 0.06529689308308950224, -1.700389599856198863, 1.266735544122286283 ) ) ;
#6189=CARTESIAN_POINT ( 'NONE',  ( 5.309220276109914316, 1.198862193007979471, -1.621181151826488254 ) ) ;
#6191=CARTESIAN_POINT ( 'NONE',  ( 3.713784835328519218, 0.5057260441109856508, -1.999473844451674642 ) ) ;
#6193=CARTESIAN_POINT ( 'NONE',  ( -0.2411972340276204718, 2.032951786628557134, -2.316127775276015655 ) ) ;
#6197=CARTESIAN_POINT ( 'NONE',  ( 6.017560223340764125, -1.214513600917455083, -1.823921334435735231 ) ) ;
#6198=CARTESIAN_POINT ( 'NONE',  ( 3.850232551101365086, 0.2440307281281335616, -2.001511205109906655 ) ) ;
#6199=CARTESIAN_POINT ( 'NONE',  ( 3.298233973420101606, 1.449563003725433896, -1.135193286699177628 ) ) ;
#6202=CARTESIAN_POINT ( 'NONE',  ( 0.4281588809218932479, 1.648258183568848789, 0.5080355103465240552 ) ) ;
#6203=DIRECTION ( 'NONE',  ( -3.451266460341926649E-31, -5.200009205990155575E-32, 1.000000000000000000 ) ) ;
#6204=CARTESIAN_POINT ( 'NONE',  ( 0.5108563537194388271, -2.180326652049785707, 0.7283127579034570642 ) ) ;
#6206=CARTESIAN_POINT ( 'NONE',  ( 6.666858444607468570, -2.065188582200903955, -0.9245386165244884324 ) ) ;
#6207=CARTESIAN_POINT ( 'NONE',  ( 2.578859754595532294, -2.015555182639038101, -0.6107849380157669428 ) ) ;
#6216=CARTESIAN_POINT ( 'NONE',  ( 2.180079139336263516, 2.078761533942363737, -0.4183221158333137457 ) ) ;
#6217=CARTESIAN_POINT ( 'NONE',  ( 4.377308812845062569, -1.984989629755340435, -0.9973083610524589027 ) ) ;
#6218=CARTESIAN_POINT ( 'NONE',  ( 2.150558370509841666, -1.692889690492072718, 1.391600924549152296 ) ) ;
#6221=CARTESIAN_POINT ( 'NONE',  ( 5.740667459973674447, -1.913685094937540132, -0.4313615418530327150 ) ) ;
#6226=CARTESIAN_POINT ( 'NONE',  ( 4.183913158364858553, 2.056144659531285779, -0.5182805708664262045 ) ) ;
#6229=CARTESIAN_POINT ( 'NONE',  ( 5.067319851952804655, 0.2155487944876262052, -2.150937003660175595 ) ) ;
#6231=CARTESIAN_POINT ( 'NONE',  ( 4.669393045487420402, 1.064170941109745305, 1.502380130741477693 ) ) ;
#6234=CARTESIAN_POINT ( 'NONE',  ( 0.3271923042600047848, 0.8970799620377118977, -1.491255180049656071 ) ) ;
#6235=CARTESIAN_POINT ( 'NONE',  ( 6.727182134110257117, 2.064761932694148872, 2.218145506119094890 ) ) ;
#6239=CARTESIAN_POINT ( 'NONE',  ( 4.188458007013862172, -2.137797052781073237, -0.3198388112101158143 ) ) ;
#6245=CARTESIAN_POINT ( 'NONE',  ( 3.063507763784904192, 0.3185916186679502715, -2.137983152197140413 ) ) ;
#6246=CARTESIAN_POINT ( 'NONE',  ( 4.956303624527079066, 0.7517850369052423432, 1.822569506419220220 ) ) ;
#6247=CARTESIAN_POINT ( 'NONE',  ( 3.479597601185040912, 1.566717760139114901, 0.7430284921127163766 ) ) ;
#6248=CARTESIAN_POINT ( 'NONE',  ( 0.8553300576445364012, 0.4222666777726029608, -2.150330908352434012 ) ) ;
#6249=CARTESIAN_POINT ( 'NONE',  ( 0.8159566880532771460, -0.3350741789154148553, 2.283031499596111402 ) ) ;
#6250=CARTESIAN_POINT ( 'NONE',  ( 4.077457721052785367, 1.941698500476006117, -0.6908173846359686454 ) ) ;
#6251=CARTESIAN_POINT ( 'NONE',  ( 5.829623785595809515, 0.9536246560681378437, -1.691722214391349732 ) ) ;
#6257=CARTESIAN_POINT ( 'NONE',  ( 3.557846488308267663, 0.5383450771202847873, -2.139971664446515653 ) ) ;
#6260=CARTESIAN_POINT ( 'NONE',  ( 1.094327318609791710, 1.832149372150039479, 0.3252389950085340375 ) ) ;
#6261=CARTESIAN_POINT ( 'NONE',  ( -0.02900071798684483726, 7.629137130509101361, -2.773797386654376584 ) ) ;
#6265=CARTESIAN_POINT ( 'NONE',  ( 0.1253635393240644380, 7.629137130509072051, -2.744100600304347104 ) ) ;
#6266=CARTESIAN_POINT ( 'NONE',  ( 6.562460610575872266, -1.685528226061007162, -0.7412392050258274079 ) ) ;
#6268=CARTESIAN_POINT ( 'NONE',  ( 1.991158371866567967, 1.793705239296649045, -1.014668517943543513 ) ) ;
#6274=CARTESIAN_POINT ( 'NONE',  ( 1.024374290915401442, 1.228313541842564138, -1.654675390109799693 ) ) ;
#6276=CARTESIAN_POINT ( 'NONE',  ( 4.212339636135824961, 1.685202893791247769, 0.7422218904534692019 ) ) ;
#6280=CARTESIAN_POINT ( 'NONE',  ( 5.760442859251142522, 0.8911043219209063837, 2.019162844794204048 ) ) ;
#6281=CARTESIAN_POINT ( 'NONE',  ( 0.4741787938652639034, 1.244221353789766837, 1.767418780601250017 ) ) ;
#6283=CARTESIAN_POINT ( 'NONE',  ( 0.5449873876890098945, 0.1430962203496731200, 1.907122450762772647 ) ) ;
#6284=CARTESIAN_POINT ( 'NONE',  ( 1.235564962061060257, 0.5807501988173838781, -1.931125984888550473 ) ) ;
#6288=CARTESIAN_POINT ( 'NONE',  ( 6.463533315534490065, -1.538886664202097965, -1.134999244291827747 ) ) ;
#6290=CARTESIAN_POINT ( 'NONE',  ( 1.393192293617943944, 1.414286473764417185, 1.224485199485196629 ) ) ;
#6291=CARTESIAN_POINT ( 'NONE',  ( 2.448454179885679149, -1.387098808145654560, 1.463928423225707931 ) ) ;
#6293=CARTESIAN_POINT ( 'NONE',  ( 6.639320575229282539, 7.629137130509070275, 2.703262396134015866 ) ) ;
#6295=CARTESIAN_POINT ( 'NONE',  ( 5.672525241255916839, -1.337268198843853506, 1.627036470456619810 ) ) ;
#6300=CARTESIAN_POINT ( 'NONE',  ( 4.025652601906283046, -0.3410878217046057204, 1.990599050954243054 ) ) ;
#6303=CARTESIAN_POINT ( 'NONE',  ( 6.742638559370645268, -2.022111636011727498, -0.4062529910623476903 ) ) ;
#6306=CARTESIAN_POINT ( 'NONE',  ( 4.973979902034267653, 1.240098594129716458, 1.770319513135506062 ) ) ;
#6312=CARTESIAN_POINT ( 'NONE',  ( 2.031898538270035637, 2.078123050159206286, -0.6288832818364347155 ) ) ;
#6315=CARTESIAN_POINT ( 'NONE',  ( 1.909461114401575843, -0.8690924446688346183, -1.623246667998109682 ) ) ;
#6317=CARTESIAN_POINT ( 'NONE',  ( 2.771223791512751333, 2.080116120148074010, -0.6901165687889164735 ) ) ;
#6318=CARTESIAN_POINT ( 'NONE',  ( 6.883263157960364254, 2.431740398616466070, 2.435552827938294751 ) ) ;
#6319=CARTESIAN_POINT ( 'NONE',  ( 3.942437297418455611, 2.251314906739984245, 0.2249487974115715883 ) ) ;
#6326=CARTESIAN_POINT ( 'NONE',  ( 5.061649853805494814, 1.750434175623495348, -0.2595850195740417310 ) ) ;
#6328=CARTESIAN_POINT ( 'NONE',  ( 2.432770431885710405, 2.042423857386191255, 0.5128348284264750978 ) ) ;
#6331=CARTESIAN_POINT ( 'NONE',  ( 1.223035424556912387, -1.779184897175438707, -0.8450996447877844320 ) ) ;
#6334=CARTESIAN_POINT ( 'NONE',  ( 0.2913577194270203785, -1.795273245208812485, 0.7915465721433642132 ) ) ;
#6335=CARTESIAN_POINT ( 'NONE',  ( 5.449399174529797385, -1.634242350402253852, 0.7820841365046418137 ) ) ;
#6339=CARTESIAN_POINT ( 'NONE',  ( 5.295714669793899709, -0.6724083694377264164, 1.745798414713333413 ) ) ;
#6341=CARTESIAN_POINT ( 'NONE',  ( 5.084861876562203342, 1.979495018489594305, 0.6061691862097525751 ) ) ;
#6351=CARTESIAN_POINT ( 'NONE',  ( 4.562918044398325712, 1.517878595006398212, -1.242988302126393441 ) ) ;
#6354=CARTESIAN_POINT ( 'NONE',  ( 2.425157474508771838, 0.8594973679685766754, 1.823840639232063632 ) ) ;
#6356=CARTESIAN_POINT ( 'NONE',  ( 0.9256184737543894370, -1.394389637717853514, -1.690728713229103342 ) ) ;
#6359=CARTESIAN_POINT ( 'NONE',  ( 2.196370303256788503, -0.4943915968025693330, -1.803980227719769847 ) ) ;
#6361=CARTESIAN_POINT ( 'NONE',  ( 3.867443265902783534, -1.676145683993632618, -1.114854040202686969 ) ) ;
#6364=CARTESIAN_POINT ( 'NONE',  ( 3.146228450019908252, 0.9544266383219732752, 1.889993806685738464 ) ) ;
#6366=CARTESIAN_POINT ( 'NONE',  ( 4.650872726564402981, -0.4503784926754761386, -2.020631409805350387 ) ) ;
#6368=CARTESIAN_POINT ( 'NONE',  ( 1.048509228467583876, -1.645825662996244443, 1.289236127856315139 ) ) ;
#6369=CARTESIAN_POINT ( 'NONE',  ( 6.620655732516611103, 6.035157181942712334, 2.668628960472289702 ) ) ;
#6370=CARTESIAN_POINT ( 'NONE',  ( 6.229513028222847026, -1.717969363144413952, 0.6179237509907066217 ) ) ;
#6378=CARTESIAN_POINT ( 'NONE',  ( -0.05833479489262324152, -1.112358503097829576, -1.430056051773327841 ) ) ;
#6386=CARTESIAN_POINT ( 'NONE',  ( 6.521112179100128969, -1.799899466697444383, 0.9092066555835758290 ) ) ;
#6389=CARTESIAN_POINT ( 'NONE',  ( -0.1399997263889611598, 2.874570648431204578, -2.488748559936367233 ) ) ;
#6392=CARTESIAN_POINT ( 'NONE',  ( 3.942214172571806508, -0.9744538365985645489, 1.711425102584500202 ) ) ;
#6393=CARTESIAN_POINT ( 'NONE',  ( 4.552361342037492875, -1.314984614574012944, 1.528753174698034067 ) ) ;
#6396=CARTESIAN_POINT ( 'NONE',  ( 4.470767510317084970, 0.001397387737574890204, -2.191629466793604930 ) ) ;
#6398=CARTESIAN_POINT ( 'NONE',  ( 2.696214026845968448, -1.921097006559132625, -0.1437054574915888616 ) ) ;
#6400=CARTESIAN_POINT ( 'NONE',  ( -0.02988540731099428513, 1.418068428043406382, -1.986943242881351601 ) ) ;
#6408=CARTESIAN_POINT ( 'NONE',  ( -0.1235792489666731608, -0.1369701924231395973, -1.910945132828122395 ) ) ;
#6409=CARTESIAN_POINT ( 'NONE',  ( 2.543610208494262892, -1.877569574052952328, 0.7265587727790027150 ) ) ;
#6410=CARTESIAN_POINT ( 'NONE',  ( 5.606872354539667036, 0.9390355927846851802, -2.097984029676060125 ) ) ;
#6412=CARTESIAN_POINT ( 'NONE',  ( 3.537814430808595922, 1.177328839734363308, 1.441218929277183536 ) ) ;
#6418=CARTESIAN_POINT ( 'NONE',  ( 5.601146835291897830, -0.5070800215070477845, 2.028203315493964709 ) ) ;
#6423=CARTESIAN_POINT ( 'NONE',  ( 0.2404813148422607627, 0.3085585699703840556, 1.799268721412583316 ) ) ;
#6425=CARTESIAN_POINT ( 'NONE',  ( 2.549097654585132045, -1.194521797001405927, 1.257391726941985421 ) ) ;
#6430=CARTESIAN_POINT ( 'NONE',  ( 0.2861044793709514589, -1.271156181823060560, -1.634742764404630844 ) ) ;
#6431=CARTESIAN_POINT ( 'NONE',  ( 5.461492464141177727, 0.3521552718798379722, -1.791230276788812414 ) ) ;
#6432=CARTESIAN_POINT ( 'NONE',  ( 3.836726278109466204, -1.889416792123297162, -0.5274722977551549175 ) ) ;
#6436=CARTESIAN_POINT ( 'NONE',  ( 3.844477943020713440, 1.133112341739877849, -1.792160191984671691 ) ) ;
#6439=CARTESIAN_POINT ( 'NONE',  ( 1.938418878558012315, -1.110983660290700170, 1.746734030103759938 ) ) ;
#6441=CARTESIAN_POINT ( 'NONE',  ( 4.073042245396302441, -1.645747789204109468, 1.492029542161198430 ) ) ;
#6443=CARTESIAN_POINT ( 'NONE',  ( 1.916985526034093335, -1.504927692415005014, -1.737642283433957768 ) ) ;
#6445=CARTESIAN_POINT ( 'NONE',  ( 6.227400143195995774, 0.1575970216860186346, -2.056636196940288652 ) ) ;
#6449=CARTESIAN_POINT ( 'NONE',  ( 6.286648950733226826, 1.598451336667701339, -0.9137711784916457969 ) ) ;
#6452=CARTESIAN_POINT ( 'NONE',  ( 3.216961742616857745, 1.504763323797538410, -1.180078671740567131 ) ) ;
#6453=CARTESIAN_POINT ( 'NONE',  ( -0.2106725631050099246, 1.363266585364702577, -2.259529575671606505 ) ) ;
#6454=CARTESIAN_POINT ( 'NONE',  ( 3.926516724862822993, 1.637815149125703584, 0.5408920155725772672 ) ) ;
#6455=CARTESIAN_POINT ( 'NONE',  ( 2.501185699981960830, -0.1928336239410358699, 2.007256303757164240 ) ) ;
#6456=CARTESIAN_POINT ( 'NONE',  ( 3.745041490520171212, 2.281215052333289250, -0.2826575254791847680 ) ) ;
#6457=CARTESIAN_POINT ( 'NONE',  ( 3.444836229973327946, 0.5457880569446837971, 2.195490905318697283 ) ) ;
#6458=CARTESIAN_POINT ( 'NONE',  ( 6.182269030498733997, -1.128069697684991546, 1.778281062836915449 ) ) ;
#6461=CARTESIAN_POINT ( 'NONE',  ( 5.026482010321593030, 1.693441115147217291, 0.5138918105389718161 ) ) ;
#6463=CARTESIAN_POINT ( 'NONE',  ( 1.236728449817244835, 0.4514257060114800213, 2.247219992417306411 ) ) ;
#6464=CARTESIAN_POINT ( 'NONE',  ( 5.525302006934727395, -1.171079710934025186, -1.420692760577553226 ) ) ;
#6467=CARTESIAN_POINT ( 'NONE',  ( 6.210891007176935652, -0.2719346519345893776, 2.174439262769362280 ) ) ;
#6471=CARTESIAN_POINT ( 'NONE',  ( 6.127406499145813257, 0.1562011534181114436, -2.064545280851529885 ) ) ;
#6474=CARTESIAN_POINT ( 'NONE',  ( 4.688067719671657585, -0.9068681981775075229, 1.699704011162524120 ) ) ;
#6477=CARTESIAN_POINT ( 'NONE',  ( 0.6334296782557496952, 2.055416226174343386, 0.8430641771750585489 ) ) ;
#6488=CARTESIAN_POINT ( 'NONE',  ( 1.398799877119625501, 0.3793605821263335565, 1.924665094374561791 ) ) ;
#6489=EDGE_CURVE ( 'NONE', #76973, #99811, #113005, .T. ) ;
#6492=CARTESIAN_POINT ( 'NONE',  ( 6.689906388054261299, -1.280585065398877731, -1.486383542710856043 ) ) ;
#6495=CARTESIAN_POINT ( 'NONE',  ( 0.1810634928296238622, -2.195609808662852824, -0.5457317257893978812 ) ) ;
#6499=CARTESIAN_POINT ( 'NONE',  ( 1.000990332655056436, 1.525750722454706443, 1.081861512215509524 ) ) ;
#6500=CARTESIAN_POINT ( 'NONE',  ( 0.1231123065759693186, 0.2931380485183229800, 1.709000606096510166 ) ) ;
#6502=CARTESIAN_POINT ( 'NONE',  ( 4.757479570170550787, 2.167726397749652367, -0.3216086267831194112 ) ) ;
#6503=CARTESIAN_POINT ( 'NONE',  ( 4.911288641948820199, 2.004953420984519674, 1.142316731622401882 ) ) ;
#6504=CARTESIAN_POINT ( 'NONE',  ( 0.1103218441215253337, -0.8811044119183660817, -1.861458889230242164 ) ) ;
#6505=CARTESIAN_POINT ( 'NONE',  ( 1.992034801999421623, -0.5177828490160235608, -1.871580480717034645 ) ) ;
#6510=CARTESIAN_POINT ( 'NONE',  ( 3.692029868468839737, 1.730865839653324079, 1.034166058993556181 ) ) ;
#6514=CARTESIAN_POINT ( 'NONE',  ( 0.9964003531478006215, -0.4411313887022934033, -1.771462291394958255 ) ) ;
#6519=CARTESIAN_POINT ( 'NONE',  ( 5.084866380259029484, -0.2499542577577648639, -2.045595823183245621 ) ) ;
#6524=CARTESIAN_POINT ( 'NONE',  ( 5.584630649692731375, -1.279725605644935760, 1.562507038963067973 ) ) ;
#6525=CARTESIAN_POINT ( 'NONE',  ( 5.690131909746282801, 1.321361375537116967, 1.785392519086197671 ) ) ;
#6529=CARTESIAN_POINT ( 'NONE',  ( 4.170816135027268778, -1.922254079802641069, -0.7435701193346122562 ) ) ;
#6530=CARTESIAN_POINT ( 'NONE',  ( 3.762342404062004597, 1.897698010425369564, -0.6819954029829020659 ) ) ;
#6531=ORIENTED_EDGE ( 'NONE', *, *, #98433, .T. ) ;
#6538=CARTESIAN_POINT ( 'NONE',  ( 4.481795959180916888, 1.842165523724150544, 0.8196470798618460396 ) ) ;
#6539=CARTESIAN_POINT ( 'NONE',  ( 3.398233898566359823, 1.450718870894672330, -1.133551952132209717 ) ) ;
#6541=CARTESIAN_POINT ( 'NONE',  ( 2.104549495715298590, -2.307096348898482585, 0.05917499873058817972 ) ) ;
#6543=CARTESIAN_POINT ( 'NONE',  ( 3.339309863714147397, -1.908069850993234340, 1.015702806061814734 ) ) ;
#6546=CARTESIAN_POINT ( 'NONE',  ( 3.427438825619326668, 1.030710970775401414, 2.054361689694866211 ) ) ;
#6548=CARTESIAN_POINT ( 'NONE',  ( 2.201827603038747139, -1.870314503716500099, 0.04339327950253490246 ) ) ;
#6550=CARTESIAN_POINT ( 'NONE',  ( 0.4738186427182951577, 1.131346554974651086, 1.614239802345132757 ) ) ;
#6554=CARTESIAN_POINT ( 'NONE',  ( 2.174722684859807575, -1.356406721008751814, 1.740749382485320407 ) ) ;
#6559=CARTESIAN_POINT ( 'NONE',  ( 6.069206959712960980, 0.1456670527590266107, -1.966150735595481258 ) ) ;
#6560=CARTESIAN_POINT ( 'NONE',  ( 5.514422467339478828, -1.033062203415137992, -2.063637023464809594 ) ) ;
#6561=CARTESIAN_POINT ( 'NONE',  ( 0.1683002474503410839, -0.8351952195557797998, -1.773497582445908938 ) ) ;
#6562=CARTESIAN_POINT ( 'NONE',  ( 2.746997431529357492, -0.3482204723163102034, -2.032804898803519222 ) ) ;
#6570=CARTESIAN_POINT ( 'NONE',  ( 5.143125006682406131, -0.2608717942136177248, -2.155377805267975067 ) ) ;
#6572=CARTESIAN_POINT ( 'NONE',  ( 5.706567001488551227, 1.626822141722890303, 0.8623401093873286349 ) ) ;
#6575=CARTESIAN_POINT ( 'NONE',  ( 0.3329892237508432218, -1.712944741146246841, 0.7519245212838021608 ) ) ;
#6576=CARTESIAN_POINT ( 'NONE',  ( 0.7907308791721240349, -2.245476950237018432, -0.2759641350603259657 ) ) ;
#6581=CARTESIAN_POINT ( 'NONE',  ( -0.1108833634136767443, 0.0002062650063822807356, -1.896853557917008271 ) ) ;
#6582=CARTESIAN_POINT ( 'NONE',  ( 1.375481398426938284, 1.050436561215197351, 1.424246879149461797 ) ) ;
#6583=CARTESIAN_POINT ( 'NONE',  ( -0.04057498839846879202, -1.478066481919372510, -1.213044814162365981 ) ) ;
#6585=CARTESIAN_POINT ( 'NONE',  ( 2.917496427270527715, -1.288711974188415654, -1.417462588220135933 ) ) ;
#6586=CARTESIAN_POINT ( 'NONE',  ( -0.1409997244346088419, 5.722143553014046979, -2.594341442600463843 ) ) ;
#6587=CARTESIAN_POINT ( 'NONE',  ( 4.633233401965040521, 0.002145104102065781716, -1.969739563307022712 ) ) ;
#6588=CARTESIAN_POINT ( 'NONE',  ( -0.05226516427493665962, -1.936187138999283297, 0.8653993394739032397 ) ) ;
#6590=CARTESIAN_POINT ( 'NONE',  ( 2.676452114398766291, -1.789519730395791486, -0.5449050523786898026 ) ) ;
#6591=CARTESIAN_POINT ( 'NONE',  ( 6.656889574143706412, -1.327764893807031221, 1.100862838992909598 ) ) ;
#6593=CARTESIAN_POINT ( 'NONE',  ( 2.789901687333019797, 1.561178712900921584, 1.560079944692857046 ) ) ;
#6596=CARTESIAN_POINT ( 'NONE',  ( 0.9243725180730785196, 1.015136377070953388, 1.795498427122848017 ) ) ;
#6601=CARTESIAN_POINT ( 'NONE',  ( 0.1747926744264712562, 2.889263262932476817, -2.344248796821886138 ) ) ;
#6604=CARTESIAN_POINT ( 'NONE',  ( 2.893098739488662030, 0.2508700648995808025, 2.055025655848155886 ) ) ;
#6608=CARTESIAN_POINT ( 'NONE',  ( 1.067063705314938771, -1.590654782179411031, 1.244411004956039291 ) ) ;
#6612=CARTESIAN_POINT ( 'NONE',  ( 0.1745949693968692484, 0.009193469831055355729, -1.755468632744116242 ) ) ;
#6614=CARTESIAN_POINT ( 'NONE',  ( 4.921249881687196570, 0.7690040753521176775, 1.863882819927860313 ) ) ;
#6615=CARTESIAN_POINT ( 'NONE',  ( 6.438697963858233564, -1.475898738386885123, 1.221124472464208743 ) ) ;
#6616=CARTESIAN_POINT ( 'NONE',  ( 6.639320575229244348, 1.270172395628932360, 2.119701008677194132 ) ) ;
#6617=CARTESIAN_POINT ( 'NONE',  ( 3.650093349144762023, 0.7902683543556283663, 2.044282924279612779 ) ) ;
#6619=CARTESIAN_POINT ( 'NONE',  ( 2.847809051801777791, -1.287500320553297994, -1.414207669007704116 ) ) ;
#6624=CARTESIAN_POINT ( 'NONE',  ( 0.5093889453341126083, -1.913797760093600919, 0.6352206787166372326 ) ) ;
#6626=CARTESIAN_POINT ( 'NONE',  ( 5.847271748948593029, 0.6375361197438635941, -2.096799129279611762 ) ) ;
#6628=CARTESIAN_POINT ( 'NONE',  ( 2.766273355629506714, -1.191139867243676598, 1.247637197061921555 ) ) ;
#6630=CARTESIAN_POINT ( 'NONE',  ( 6.047156637250688860, 0.2094617991648151656, 2.110256208591613003 ) ) ;
#6642=CARTESIAN_POINT ( 'NONE',  ( 2.314858244453772862, 1.454059926310177220, -1.080092325806664144 ) ) ;
#6646=CARTESIAN_POINT ( 'NONE',  ( 3.650846288169238729, 0.2690317868887618369, 1.791254203397556477 ) ) ;
#6652=CARTESIAN_POINT ( 'NONE',  ( 5.635155393647417910, -0.04589315835645593061, -1.860648885492953486 ) ) ;
#6654=CARTESIAN_POINT ( 'NONE',  ( 2.214329231836575040, 1.858617268789555466, 0.4632827458446056035 ) ) ;
#6660=CARTESIAN_POINT ( 'NONE',  ( 6.925078400183578786, 0.5640289027524867382, 2.196098379985710114 ) ) ;
#6664=CARTESIAN_POINT ( 'NONE',  ( 1.781308773403101231, 1.442672104170627190, 1.513329462076596243 ) ) ;
#6665=CARTESIAN_POINT ( 'NONE',  ( 6.194356126197313017, -1.917168722191398000, -0.1884046653951119699 ) ) ;
#6667=CARTESIAN_POINT ( 'NONE',  ( 2.713660727937648787, -1.805999004224107196, 0.2657717501357085843 ) ) ;
#6668=CARTESIAN_POINT ( 'NONE',  ( 3.141465813989018141, -1.946189201368169641, 1.040519825639886431 ) ) ;
#6670=CARTESIAN_POINT ( 'NONE',  ( 0.7383556378116812313, 1.137082172773289379, -1.537495029474859276 ) ) ;
#6671=CARTESIAN_POINT ( 'NONE',  ( 1.275766937089892750, -1.922257851437941811, 0.4282784019480969651 ) ) ;
#6672=CARTESIAN_POINT ( 'NONE',  ( 3.720204347993858462, 1.845125290474887159, 0.6061553137183937068 ) ) ;
#6676=CARTESIAN_POINT ( 'NONE',  ( 0.1329588055935396196, 0.006246367379872731426, -1.846049620084761367 ) ) ;
#6685=CARTESIAN_POINT ( 'NONE',  ( 3.351995281737112364, 1.825872481133209879, -0.0009662468829912954560 ) ) ;
#6686=CARTESIAN_POINT ( 'NONE',  ( 5.928922775424462444, -1.700964743930567513, 1.082835439959836776 ) ) ;
#6692=CARTESIAN_POINT ( 'NONE',  ( 4.135518821028766112, -1.289757458839156934, -1.355179912160727085 ) ) ;
#6694=CARTESIAN_POINT ( 'NONE',  ( 2.086434564137104264, -1.889293373815591481, -0.3759864732829041878 ) ) ;
#6695=CARTESIAN_POINT ( 'NONE',  ( 6.420756404446520627, -1.389671697431221542, 1.384925340169262054 ) ) ;
#6700=CARTESIAN_POINT ( 'NONE',  ( 0.5974486649760869517, -0.3061723685214760016, 2.094854868064464970 ) ) ;
#6702=CARTESIAN_POINT ( 'NONE',  ( 4.680570891794395116, 1.277791010243028991, -1.628752506732597638 ) ) ;
#6703=CARTESIAN_POINT ( 'NONE',  ( 0.04610459085982108324, -1.479553692838073475, 1.095721268101347734 ) ) ;
#6705=CARTESIAN_POINT ( 'NONE',  ( 4.887441975664971849, -0.7727101442582262614, -2.165022144963870243 ) ) ;
#6709=CARTESIAN_POINT ( 'NONE',  ( 0.6566820891428931661, -1.656472902050255991, 1.584714856167362074 ) ) ;
#6712=CARTESIAN_POINT ( 'NONE',  ( 5.226486033959851341, 0.1448775283907685063, 1.936603901228886926 ) ) ;
#6716=CARTESIAN_POINT ( 'NONE',  ( -0.1755273284492936958, -0.8636782348834280976, -1.816524446017355743 ) ) ;
#6717=CARTESIAN_POINT ( 'NONE',  ( 5.981657729715995409, -0.6748525008196132324, 1.900413905137773529 ) ) ;
#6720=CARTESIAN_POINT ( 'NONE',  ( 2.677772397998368081, -1.073972967945693080, 1.793542233829773291 ) ) ;
#6721=CARTESIAN_POINT ( 'NONE',  ( 1.463349669262783870, 1.744408624272808073, -0.2979475530153224416 ) ) ;
#6722=CARTESIAN_POINT ( 'NONE',  ( 6.434220164165640021, -1.621181005584397372, -1.198863592720422977 ) ) ;
#6724=CARTESIAN_POINT ( 'NONE',  ( 4.734495095973747070, 0.3888400998970488187, 2.258902165976091059 ) ) ;
#6725=CARTESIAN_POINT ( 'NONE',  ( 2.677380959318215847, -0.8946470780417746793, 1.492600998661142375 ) ) ;
#6728=CARTESIAN_POINT ( 'NONE',  ( 2.372030889105484430, -0.3844106184479143540, 1.690481094739235912 ) ) ;
#6730=CARTESIAN_POINT ( 'NONE',  ( 1.750234856725553900, -1.851685525784763975, -0.1866200871585097509 ) ) ;
#6731=CARTESIAN_POINT ( 'NONE',  ( 2.998652106967353514, 2.154486853421373027, 0.2683346083656880099 ) ) ;
#6733=CARTESIAN_POINT ( 'NONE',  ( 4.926970384345759513, -1.727065721694167832, 1.040790168839386798 ) ) ;
#6734=CARTESIAN_POINT ( 'NONE',  ( 1.687500000000001110, -1.451031289061048835, 1.451031289061190055 ) ) ;
#6736=CARTESIAN_POINT ( 'NONE',  ( 1.553604983729965472, 0.5615451523532221101, -1.842721482554928514 ) ) ;
#6738=CARTESIAN_POINT ( 'NONE',  ( 4.851916359752673991, -1.571614379473328160, -1.570179378767898370 ) ) ;
#6740=CARTESIAN_POINT ( 'NONE',  ( -0.2108831679770960255, -0.001785917861228669690, -1.896958272444612792 ) ) ;
#6744=CARTESIAN_POINT ( 'NONE',  ( 0.08310686162707729696, -1.445780664108237801, 1.686489957186103839 ) ) ;
#6745=CARTESIAN_POINT ( 'NONE',  ( 6.320756440275017596, -1.388331291134708767, 1.386421665916007795 ) ) ;
#6750=CARTESIAN_POINT ( 'NONE',  ( 5.712299329104530088, -1.009927678917849736, -2.024548151048012556 ) ) ;
#6752=CARTESIAN_POINT ( 'NONE',  ( 2.980982186342299833, 1.941357688518682290, 0.6972846330933372139 ) ) ;
#6757=CARTESIAN_POINT ( 'NONE',  ( 4.411305886619627081, -0.3218996851035611506, 1.842484647571709822 ) ) ;
#6758=CARTESIAN_POINT ( 'NONE',  ( 3.533592999799278989, -1.415137147236225079, 1.001973916141611687 ) ) ;
#6759=CARTESIAN_POINT ( 'NONE',  ( 3.386022052710332186, -0.3430625053944387770, -1.706099273433875130 ) ) ;
#6760=CARTESIAN_POINT ( 'NONE',  ( 1.119135019589584834, -0.04993059730015738523, 2.291989107133483028 ) ) ;
#6762=CARTESIAN_POINT ( 'NONE',  ( 4.757415945720180339, 2.067795187486476394, -0.3081579728113920669 ) ) ;
#6763=CARTESIAN_POINT ( 'NONE',  ( 6.175724022258248347, -1.036883830621424307, 1.641789595683869729 ) ) ;
#6766=CARTESIAN_POINT ( 'NONE',  ( 0.9322677863709986079, -1.591319861332978425, -1.238319039483272599 ) ) ;
#6767=CARTESIAN_POINT ( 'NONE',  ( 0.4750491441844888474, -1.531729482103380224, 1.466773057065169361 ) ) ;
#6771=CARTESIAN_POINT ( 'NONE',  ( 4.811078068098579408, 1.589968679568127596, 0.8971634079883783475 ) ) ;
#6777=CARTESIAN_POINT ( 'NONE',  ( 2.162373415809074828, 2.019440163517810749, 0.04526320522070524655 ) ) ;
#6778=CARTESIAN_POINT ( 'NONE',  ( 6.124089168553260798, -1.220954261165616783, -1.838047742986161026 ) ) ;
#6780=CARTESIAN_POINT ( 'NONE',  ( 3.063170293922971243, 1.569483505267080359, 0.9996245905467721071 ) ) ;
#6786=CARTESIAN_POINT ( 'NONE',  ( 5.268108045213575785, 0.9031548532531764595, 1.586571422427636824 ) ) ;
#6790=CARTESIAN_POINT ( 'NONE',  ( 0.3504316985127345907, -0.8248687954017698276, 1.525068808560197109 ) ) ;
#6791=CARTESIAN_POINT ( 'NONE',  ( 6.632757984263843554, -1.642112545546599023, 0.8327811610863435909 ) ) ;
#6792=CARTESIAN_POINT ( 'NONE',  ( 5.549573066657292664, -1.816037693736268333, -1.423817124750816232 ) ) ;
#6794=CARTESIAN_POINT ( 'NONE',  ( 0.2279051764371925748, -1.265926261136205211, -1.626655886597817124 ) ) ;
#6797=CARTESIAN_POINT ( 'NONE',  ( 5.993622264137510314, 2.212772176713458716, 0.6212890515704305727 ) ) ;
#6800=CARTESIAN_POINT ( 'NONE',  ( 5.752782329262380756, -1.473788443143897675, 1.151991621687727507 ) ) ;
#6801=CARTESIAN_POINT ( 'NONE',  ( 3.990413957267644474, -1.096855775730350757, 1.566394476586838724 ) ) ;
#6803=CARTESIAN_POINT ( 'NONE',  ( 5.004599478379411437, -0.7411955310945415043, -2.078817424605138964 ) ) ;
#6804=CARTESIAN_POINT ( 'NONE',  ( 4.698512310153400762, 1.457641359173178275, -1.535954635999142948 ) ) ;
#6806=CARTESIAN_POINT ( 'NONE',  ( 6.883263157960367806, 0.5819222519044697783, 1.998722019247618276 ) ) ;
#6809=CARTESIAN_POINT ( 'NONE',  ( 5.444028431581452665, -1.345373016635186714, -1.639009079359869725 ) ) ;
#6810=CARTESIAN_POINT ( 'NONE',  ( 2.222082089356589130, -2.238238103340572049, 0.5610464132631690637 ) ) ;
#6811=CARTESIAN_POINT ( 'NONE',  ( 3.332423539472821439, -1.170687260143790320, 1.574129132985650825 ) ) ;
#6813=CARTESIAN_POINT ( 'NONE',  ( 6.368047018367568590, -2.047660648193879496, 0.2468551644246498589 ) ) ;
#6816=ORIENTED_EDGE ( 'NONE', *, *, #25165, .T. ) ;
#6817=CARTESIAN_POINT ( 'NONE',  ( 5.454314652423888354, -1.275559214091715354, 1.561879324423600668 ) ) ;
#6821=CARTESIAN_POINT ( 'NONE',  ( 3.309609623814670165, -1.772202297075220256, -1.253863066769088874 ) ) ;
#6823=CARTESIAN_POINT ( 'NONE',  ( 0.7387272492362946252, 1.258454933865692293, -1.706699550108881080 ) ) ;
#6828=CARTESIAN_POINT ( 'NONE',  ( 0.5970370245043071789, 1.714778692204623312, -1.142632759096851913 ) ) ;
#6834=CARTESIAN_POINT ( 'NONE',  ( 3.369685512061989741, 0.4621021693036463374, -1.855490417808261183 ) ) ;
#6836=CARTESIAN_POINT ( 'NONE',  ( 5.664868940362820737, -1.601528614980719967, -0.7536287887903775351 ) ) ;
#6839=CARTESIAN_POINT ( 'NONE',  ( 0.6678513782990652681, 1.809512280066556400, -0.08962025572057349954 ) ) ;
#6841=CARTESIAN_POINT ( 'NONE',  ( 1.059628844421168559, 1.143981278108822108, 1.536452684808758962 ) ) ;
#6842=CARTESIAN_POINT ( 'NONE',  ( 1.820844063133007396, -1.465591517063179028, 1.462601037713284535 ) ) ;
#6844=CARTESIAN_POINT ( 'NONE',  ( 6.086763352761943580, -0.2763008855245497331, -1.850001521387992565 ) ) ;
#6845=CARTESIAN_POINT ( 'NONE',  ( 2.789462663364688844, 1.291185895303394116, 1.290987730777813702 ) ) ;
#6846=CARTESIAN_POINT ( 'NONE',  ( 5.197975494389605267, -0.7968864405506062010, 2.058166701804148957 ) ) ;
#6849=CARTESIAN_POINT ( 'NONE',  ( 4.211423687607918076, -1.713229066603161099, -1.148409633951211761 ) ) ;
#6853=CARTESIAN_POINT ( 'NONE',  ( 0.8433209000573947955, -1.854398715148808385, 1.110445933987347367 ) ) ;
#6854=CARTESIAN_POINT ( 'NONE',  ( 6.496543107701719499, 2.047251205643263017, 0.3077783505985449142 ) ) ;
#6856=CARTESIAN_POINT ( 'NONE',  ( 3.778741785029844369, -2.082091666206013159, -0.5805316298483630399 ) ) ;
#6857=CARTESIAN_POINT ( 'NONE',  ( 3.721357204503534355, 1.733397938510993885, 1.036269837853747378 ) ) ;
#6858=CARTESIAN_POINT ( 'NONE',  ( 2.435929278166943490, 1.204617592564939166, 1.548422000036096202 ) ) ;
#6859=CARTESIAN_POINT ( 'NONE',  ( 6.620655732516620873, 2.403464043289889496, 2.653833411862613012 ) ) ;
#6865=CARTESIAN_POINT ( 'NONE',  ( 2.026577684455236561, 0.4465047249504557891, 1.966304233017155845 ) ) ;
#6869=CARTESIAN_POINT ( 'NONE',  ( 5.976807594091998688, -1.347613670528555740, 1.357171208065083512 ) ) ;
#6874=CARTESIAN_POINT ( 'NONE',  ( 4.394157760337158436, -0.8647400765994193161, -1.821735888681835558 ) ) ;
#6877=CARTESIAN_POINT ( 'NONE',  ( 6.704117942027653321, -1.724248281341285827, 0.04880198193529976941 ) ) ;
#6881=CARTESIAN_POINT ( 'NONE',  ( 4.745289220334846902, -1.444806058459674691, -1.188008360142885245 ) ) ;
#6882=CARTESIAN_POINT ( 'NONE',  ( -0.02880301295727832195, -0.006976478922920550246, -2.273770288744045409 ) ) ;
#6883=CARTESIAN_POINT ( 'NONE',  ( 2.325130699016836555, -1.891071737562113997, -0.8429460452448678254 ) ) ;
#6887=CARTESIAN_POINT ( 'NONE',  ( 0.8082205221912192039, 1.198841770460257194, -1.621197638953228548 ) ) ;
#6888=CARTESIAN_POINT ( 'NONE',  ( 0.1053163366912619470, 1.342294115999270510, 1.216805694454982767 ) ) ;
#6895=CARTESIAN_POINT ( 'NONE',  ( 5.712480180419416520, 1.847460191615752700, 0.5061846876120765781 ) ) ;
#6896=CARTESIAN_POINT ( 'NONE',  ( 6.727182134110194944, 0.008744176509076190262, 1.710970312420515338 ) ) ;
#6903=CARTESIAN_POINT ( 'NONE',  ( 3.186554565756247737, -2.129457467500107004, -0.3711038070777840647 ) ) ;
#6906=CARTESIAN_POINT ( 'NONE',  ( 0.9848172835694012361, -1.340914915981223476, 1.642866500755429948 ) ) ;
#6907=CARTESIAN_POINT ( 'NONE',  ( 6.000976577881287355, 1.490888274384492895, -1.053294804101670090 ) ) ;
#6908=CARTESIAN_POINT ( 'NONE',  ( 2.495336804025758859, 1.521579944813663099, 1.253379492226768477 ) ) ;
#6909=CARTESIAN_POINT ( 'NONE',  ( 4.781465250580236415, 0.1816826923375300662, -1.903719681147630016 ) ) ;
#6912=CARTESIAN_POINT ( 'NONE',  ( 5.406690398188211510, 0.5700869393594419909, 1.885254869494409791 ) ) ;
#6913=CARTESIAN_POINT ( 'NONE',  ( 0.05839466612742905127, -1.734069842965625385, -0.8743347890363247776 ) ) ;
#6919=CARTESIAN_POINT ( 'NONE',  ( 4.670513044250029999, 0.7352163052343118066, 1.765496816765201427 ) ) ;
#6921=CARTESIAN_POINT ( 'NONE',  ( 0.9915960798324228165, 1.945464911009102460, -1.041603813667857370 ) ) ;
#6923=CARTESIAN_POINT ( 'NONE',  ( -0.09332341176954485340, -0.4182270256129701491, -1.872751671355552983 ) ) ;
#6924=CARTESIAN_POINT ( 'NONE',  ( -0.02319159430947542386, 0.2540490248266329965, -1.846305437520213477 ) ) ;
#6926=CARTESIAN_POINT ( 'NONE',  ( 5.542203953035277131, 0.8216685229280199509, 1.841735684200429990 ) ) ;
#6927=CARTESIAN_POINT ( 'NONE',  ( 6.727182134110222478, 0.005875948494733079785, 1.810970247402940547 ) ) ;
#6928=CARTESIAN_POINT ( 'NONE',  ( 2.225130849662221966, -1.891980959128433559, -0.8411517639917851508 ) ) ;
#6931=CARTESIAN_POINT ( 'NONE',  ( 1.094844843509492183, -0.5259716649698794599, -2.096624219460433647 ) ) ;
#6937=CARTESIAN_POINT ( 'NONE',  ( 6.925078400183523719, 3.697131557392329348, 2.469975972695995559 ) ) ;
#6939=CARTESIAN_POINT ( 'NONE',  ( 5.256420022722958052, 1.669015333217665820, -0.4704954288548191532 ) ) ;
#6941=CARTESIAN_POINT ( 'NONE',  ( 2.641538584800803502, 1.894577224340647792, -0.8349662684224223863 ) ) ;
#6942=CARTESIAN_POINT ( 'NONE',  ( 3.831750911750389399, 0.7112487137725398423, -1.994330698664834589 ) ) ;
#6945=CARTESIAN_POINT ( 'NONE',  ( 1.850388327615314799, -1.959487253598888312, -0.1980615517182797158 ) ) ;
#6948=CARTESIAN_POINT ( 'NONE',  ( 3.170184779232795957, -1.365206436085873776, 1.841245074435297502 ) ) ;
#6949=CARTESIAN_POINT ( 'NONE',  ( 1.576486190600217663, -1.733098801405801304, -0.5742540608338757568 ) ) ;
#6953=CARTESIAN_POINT ( 'NONE',  ( 3.287361135653954491, 0.04523670859641867187, -2.012844072734306433 ) ) ;
#6954=CARTESIAN_POINT ( 'NONE',  ( 3.660947809037872425, 1.549288415169544963, -1.203348422379519667 ) ) ;
#6958=CARTESIAN_POINT ( 'NONE',  ( 6.369093512601681439, 2.000948562089053695, -0.6057377149290378293 ) ) ;
#6959=CARTESIAN_POINT ( 'NONE',  ( 4.891328792415849058, 1.312644105602623457, 1.187316208720709421 ) ) ;
#6961=CARTESIAN_POINT ( 'NONE',  ( 1.043234067691005684, -1.729537258485489115, -1.345685951901639532 ) ) ;
#6962=CARTESIAN_POINT ( 'NONE',  ( 5.226372699876832506, 0.1332071266631333351, 1.735289576922446786 ) ) ;
#6965=CARTESIAN_POINT ( 'NONE',  ( 5.924520554715382303, -1.662438412150448963, -1.587772413480701639 ) ) ;
#6966=CARTESIAN_POINT ( 'NONE',  ( -0.05867695357848409787, -1.698172713885632401, -1.384993232510664640 ) ) ;
#6967=CARTESIAN_POINT ( 'NONE',  ( 5.571581879130038217, 1.311117947217877555, -1.134664832369073117 ) ) ;
#6968=CARTESIAN_POINT ( 'NONE',  ( 1.629795212970772456, -2.077151576879713080, 0.7458654493318407352 ) ) ;
#6969=CARTESIAN_POINT ( 'NONE',  ( 5.301315566676442437, -1.864821911710778490, 1.111730659606048111 ) ) ;
#6971=CARTESIAN_POINT ( 'NONE',  ( 1.464221803445309167, -1.127774752583620366, 1.791820951956924812 ) ) ;
#6972=CARTESIAN_POINT ( 'NONE',  ( 4.218750000000001776, -0.7852924748297752666, 1.895863743164170057 ) ) ;
#6974=CARTESIAN_POINT ( 'NONE',  ( 4.577124784165859772, 0.0005310917307651402686, -1.926566264685470875 ) ) ;
#6975=CARTESIAN_POINT ( 'NONE',  ( 0.9268046190927975436, -1.003647134691580289, -1.981720526202688015 ) ) ;
#6980=CARTESIAN_POINT ( 'NONE',  ( 4.213700991847090016, 1.784230803775087137, 1.322971166850190450 ) ) ;
#6987=CARTESIAN_POINT ( 'NONE',  ( 2.268204128460939550, 1.842446992372799963, -0.8197738674571022344 ) ) ;
#6989=CARTESIAN_POINT ( 'NONE',  ( 6.144999177589818729, -0.2990398410713848154, -2.040763669801145319 ) ) ;
#6992=CARTESIAN_POINT ( 'NONE',  ( 6.409682876116948869, -0.8291888958818021127, -1.530247525868874581 ) ) ;
#6995=CARTESIAN_POINT ( 'NONE',  ( 1.809446860903692444, -1.757098282301880365, 0.2103932681993408993 ) ) ;
#6996=CARTESIAN_POINT ( 'NONE',  ( 0.6510177983308338412, 0.9963039324867200008, 1.753029211773032392 ) ) ;
#6997=CARTESIAN_POINT ( 'NONE',  ( 0.3625324912872701089, 0.1813134127766780901, -1.832273687604975665 ) ) ;
#6998=CARTESIAN_POINT ( 'NONE',  ( 4.581715332782612116, -1.081557967857611935, 2.021163373060499424 ) ) ;
#6999=CARTESIAN_POINT ( 'NONE',  ( 3.169683937527142170, -1.096016708463069422, 1.479218548343118389 ) ) ;
#7003=CARTESIAN_POINT ( 'NONE',  ( 3.539906422930443775, 0.8216601389946125433, -1.630302437610211541 ) ) ;
#7004=CARTESIAN_POINT ( 'NONE',  ( 4.377577386359387646, -0.4445010797573499817, -1.966645064109616481 ) ) ;
#7006=CARTESIAN_POINT ( 'NONE',  ( 3.397619368019880959, 1.782376118940771637, 1.393485768503288202 ) ) ;
#7008=CARTESIAN_POINT ( 'NONE',  ( 5.754936497916005145, -1.662164095216655202, 1.293063917272518015 ) ) ;
#7012=CARTESIAN_POINT ( 'NONE',  ( 3.508316276398337319, 2.070544812355082254, 0.002818362966339192730 ) ) ;
#7015=CARTESIAN_POINT ( 'NONE',  ( 6.252600707356171128, 2.097339953035493476, 0.3115551810550785672 ) ) ;
#7017=CARTESIAN_POINT ( 'NONE',  ( 0.6625679566808447829, -1.396226752684716521, 1.327616383781888176 ) ) ;
#7024=CARTESIAN_POINT ( 'NONE',  ( 0.5455723692351510667, 0.1713331888719657747, 2.214891930232844253 ) ) ;
#7025=CARTESIAN_POINT ( 'NONE',  ( 2.397617287051221791, 1.627147360716905800, 1.336933552532795222 ) ) ;
#7028=CARTESIAN_POINT ( 'NONE',  ( 6.227394082031683986, 0.1379007965640146050, -1.855924616290964169 ) ) ;
#7032=CARTESIAN_POINT ( 'NONE',  ( 0.5453776912951785460, 0.1620316879334358084, 2.114494688702214020 ) ) ;
#7035=CARTESIAN_POINT ( 'NONE',  ( 2.998438581075290710, 1.946722116546204306, 0.2428724957088539971 ) ) ;
#7036=CARTESIAN_POINT ( 'NONE',  ( 2.061604318190731533, 0.3698614785779800185, -2.129673623264888960 ) ) ;
#7037=CARTESIAN_POINT ( 'NONE',  ( 1.030510548812729965, -1.664561007783531332, 0.7873658874757857307 ) ) ;
#7041=CARTESIAN_POINT ( 'NONE',  ( 3.503586914695429488, -0.7067764301678289840, -1.590537823618918711 ) ) ;
#7045=CARTESIAN_POINT ( 'NONE',  ( 0.3390366800232989530, 0.3710982241871863541, 2.129449491308422537 ) ) ;
#7046=CARTESIAN_POINT ( 'NONE',  ( 2.706407486732204770, -1.492025830231600070, -1.356093404896424826 ) ) ;
#7049=CARTESIAN_POINT ( 'NONE',  ( 2.360178788647437464, 0.8414710005770206225, 1.782988266942896693 ) ) ;
#7052=B_SPLINE_CURVE_WITH_KNOTS ( 'NONE', 3,
 ( #178064, #207349, #175937, #27532, #61104, #58969, #107790, #173815, #193234, #128337 ),
 .UNSPECIFIED., .F., .F.,
 ( 4, 1, 1, 1, 1, 1, 1, 4 ),
 ( 0.000000000000000000, 0.09123828766142533242, 0.1830323254715014447, 0.2554767746403809325, 0.3605042187413262100, 0.5206858269973231312, 0.7335850107976985557, 1.000000000000000000 ),
 .UNSPECIFIED. ) ;
#7061=CARTESIAN_POINT ( 'NONE',  ( 5.403480793235289070, 1.882684667239397758, 1.334102933689439663 ) ) ;
#7062=CARTESIAN_POINT ( 'NONE',  ( 6.877413162628407406, -0.1429737755889188000, 1.930079329684093237 ) ) ;
#7063=CARTESIAN_POINT ( 'NONE',  ( 3.590630163336411051, 1.912927474663427496, 0.4342120235502828773 ) ) ;
#7065=CARTESIAN_POINT ( 'NONE',  ( 0.1939827082095748889, 1.755770691208278889, 0.9913967135185000057 ) ) ;
#7067=CARTESIAN_POINT ( 'NONE',  ( 1.938805156862877022, -1.633297379596149845, 1.347353381010838458 ) ) ;
#7071=CARTESIAN_POINT ( 'NONE',  ( 3.556447125109524876, -1.624355972047783148, -0.8667379164201680641 ) ) ;
#7075=CARTESIAN_POINT ( 'NONE',  ( 4.008146050417991546, -0.8085630067716749192, 1.960596031080278356 ) ) ;
#7076=CARTESIAN_POINT ( 'NONE',  ( 0.4800843290509413386, -0.2225996465644273503, -1.827572303103291551 ) ) ;
#7080=CARTESIAN_POINT ( 'NONE',  ( 4.780574613336814771, -1.997868641178605298, -0.5047315492533087644 ) ) ;
#7083=CARTESIAN_POINT ( 'NONE',  ( 1.030510548812729965, -1.664561007783531332, 0.7873658874757857307 ) ) ;
#7088=CARTESIAN_POINT ( 'NONE',  ( 0.6806489137391663613, -1.222764829241920648, 1.836970590647703627 ) ) ;
#7089=CARTESIAN_POINT ( 'NONE',  ( 3.356942810317259163, -1.715728140842260441, 1.474839417774987060 ) ) ;
#7091=CARTESIAN_POINT ( 'NONE',  ( 3.726654843667742689, 1.277109331127034952, -1.285116454894990268 ) ) ;
#7092=CARTESIAN_POINT ( 'NONE',  ( 4.434732071067119641, -1.534896228733380052, 1.146084025706934684 ) ) ;
#7093=CARTESIAN_POINT ( 'NONE',  ( 4.879381568908511824, -0.1049739508458477355, 2.067839077007492143 ) ) ;
#7096=CARTESIAN_POINT ( 'NONE',  ( 2.641432621735483544, -1.459803026827242611, -1.325177341282377741 ) ) ;
#7097=CARTESIAN_POINT ( 'NONE',  ( 0.8153024884889724655, -0.2858729149923607826, 1.904955193227176879 ) ) ;
#7098=CARTESIAN_POINT ( 'NONE',  ( 3.783945140921864070, -0.9226758061156097313, 1.627204332209288395 ) ) ;
#7099=CARTESIAN_POINT ( 'NONE',  ( 3.827072092044791596, 2.190881801378454785, 0.7251257774964211533 ) ) ;
#7100=CARTESIAN_POINT ( 'NONE',  ( 3.156551239342288095, -0.5378050974185369926, -1.781664776597549293 ) ) ;
#7105=CARTESIAN_POINT ( 'NONE',  ( 0.6980488080095709202, -0.7561646473010454894, 1.965825473679798652 ) ) ;
#7109=CARTESIAN_POINT ( 'NONE',  ( 6.907524304660562109, -0.4813806915026208055, 2.115094849305596103 ) ) ;
#7110=CARTESIAN_POINT ( 'NONE',  ( 1.740644586495963431, 1.216819214799185866, -1.736574482785017359 ) ) ;
#7112=CARTESIAN_POINT ( 'NONE',  ( 0.5276105490271070231, -0.2919958673943868765, 1.998420469645475483 ) ) ;
#7117=CARTESIAN_POINT ( 'NONE',  ( 1.546389740860309781, 2.159050155192781872, 0.1077149563947499555 ) ) ;
#7120=CARTESIAN_POINT ( 'NONE',  ( 6.925078400183559246, 1.280611897634201357, 1.970548662192173284 ) ) ;
#7123=CARTESIAN_POINT ( 'NONE',  ( 6.368375356916068597, -1.978549699825098429, -0.3886382054163611821 ) ) ;
#7125=CARTESIAN_POINT ( 'NONE',  ( 6.620655732516666170, 0.0004550665020433551948, 2.073887158236031425 ) ) ;
#7127=CARTESIAN_POINT ( 'NONE',  ( 0.3216218905449366172, -0.1073394912241855820, 2.260102045549317928 ) ) ;
#7132=CARTESIAN_POINT ( 'NONE',  ( 1.001416299785270247, -1.868574072159228994, 0.4210543004025939506 ) ) ;
#7136=CARTESIAN_POINT ( 'NONE',  ( 2.736579049320194468, 0.2108767276123752754, 1.711865116355310246 ) ) ;
#7138=CARTESIAN_POINT ( 'NONE',  ( 1.774285776001020221, -1.678457933910833644, -0.5611888468203419800 ) ) ;
#7139=MECHANICAL_DESIGN_GEOMETRIC_PRESENTATION_REPRESENTATION('',(#121350),#69448);
#7140=CARTESIAN_POINT ( 'NONE',  ( 1.805339258485965992, 1.750370858315702272, -0.9942575048343755828 ) ) ;
#7143=CARTESIAN_POINT ( 'NONE',  ( 4.419099417909471583, 2.016199240759775524, 0.8975180220924662278 ) ) ;
#7146=CARTESIAN_POINT ( 'NONE',  ( 3.967525559752110631, -1.763746451813380967, -1.176840329774282212 ) ) ;
#7147=CARTESIAN_POINT ( 'NONE',  ( 4.042592340535226647, -1.492244431823461337, 1.356313616978216618 ) ) ;
#7148=CARTESIAN_POINT ( 'NONE',  ( 4.640750240102114788, 1.735609681454729492, 0.5192115853321179753 ) ) ;
#7152=CARTESIAN_POINT ( 'NONE',  ( 1.779943879855113709, -1.003247456797161652, 1.578688272967261996 ) ) ;
#7153=EDGE_CURVE ( 'NONE', #110107, #90194, #68756, .T. ) ;
#7165=CARTESIAN_POINT ( 'NONE',  ( 3.937823072884456099, -2.028283017459261650, 0.6187693826033290323 ) ) ;
#7168=CARTESIAN_POINT ( 'NONE',  ( 5.360604507329317592, -1.429826957936894960, 1.357393395290319660 ) ) ;
#7170=CARTESIAN_POINT ( 'NONE',  ( 0.5979028997950117663, 1.355058449971069834, 1.489028425022032698 ) ) ;
#7172=CARTESIAN_POINT ( 'NONE',  ( 0.4392562211190715882, -1.791127875450468920, -1.128673114062600957 ) ) ;
#7173=CARTESIAN_POINT ( 'NONE',  ( 1.363825363374836286, -0.5049007678423790280, 2.007717453658082629 ) ) ;
#7177=CARTESIAN_POINT ( 'NONE',  ( 3.785173937466048244, 1.514314676582936947, 1.441642292586094110 ) ) ;
#7180=CARTESIAN_POINT ( 'NONE',  ( 3.416849837094409370, 1.649954109374281996, 0.7815844185870900462 ) ) ;
#7181=CARTESIAN_POINT ( 'NONE',  ( 1.910541399130718743, -0.4838386274770510864, -1.745561575705076862 ) ) ;
#7183=CARTESIAN_POINT ( 'NONE',  ( 5.690102719724574598, -0.9953569382129350274, 1.969734210959340093 ) ) ;
#7185=CARTESIAN_POINT ( 'NONE',  ( 4.682781310676605635, -2.139571651222616833, -0.5399477217277389718 ) ) ;
#7188=CARTESIAN_POINT ( 'NONE',  ( 3.211475575234080004, 1.509012206799903666, 1.174515185244667581 ) ) ;
#7190=CARTESIAN_POINT ( 'NONE',  ( 6.355931484454268698, -0.7012994977402075003, 1.948090369817329526 ) ) ;
#7192=CARTESIAN_POINT ( 'NONE',  ( 5.566036750361066154, -1.391122746885119499, 1.693456055751572986 ) ) ;
#7203=CARTESIAN_POINT ( 'NONE',  ( 6.034052368894809781, 1.228512962337786396, 1.666229478724051027 ) ) ;
#7204=CARTESIAN_POINT ( 'NONE',  ( 3.949766350991973596, 0.6478974803514454539, -1.814415559773856490 ) ) ;
#7205=CARTESIAN_POINT ( 'NONE',  ( 1.441030037510174777, -1.730879250949714843, -1.034145807338890277 ) ) ;
#7209=CARTESIAN_POINT ( 'NONE',  ( 1.008081207548201741, -0.9882381260516819310, -1.956047874660173047 ) ) ;
#7210=CARTESIAN_POINT ( 'NONE',  ( 5.074738461036464088, -1.720261882950037124, -0.6118011564382742629 ) ) ;
#7217=CARTESIAN_POINT ( 'NONE',  ( 3.052128622409277181, -1.392423357299840792, 1.204796875372941667 ) ) ;
#7218=CARTESIAN_POINT ( 'NONE',  ( 6.328391183068679204, -0.9529656412403487709, -1.773404795463069838 ) ) ;
#7219=CARTESIAN_POINT ( 'NONE',  ( 1.898275044819753621, 0.2256094754716081452, 2.287263704067198145 ) ) ;
#7220=CARTESIAN_POINT ( 'NONE',  ( 6.649272889308863732, 1.708415183241231983, -0.9640671636572254455 ) ) ;
#7222=CARTESIAN_POINT ( 'NONE',  ( 3.726736447152957599, 1.348887845406310682, -1.355897031963343213 ) ) ;
#7224=CARTESIAN_POINT ( 'NONE',  ( 0.3267351109269465148, -1.353470794461093973, 1.566751113397255812 ) ) ;
#7226=CARTESIAN_POINT ( 'NONE',  ( 2.068024735862358021, -1.283949768261948288, 1.649988806608338798 ) ) ;
#7227=CARTESIAN_POINT ( 'NONE',  ( 1.533845512228737551, 0.9248708299973290581, -1.625957014461040906 ) ) ;
#7228=CARTESIAN_POINT ( 'NONE',  ( 1.915388525686153143, 0.6297767875703685903, 1.915307412907449436 ) ) ;
#7231=CARTESIAN_POINT ( 'NONE',  ( 2.067524827727816650, -1.070173352442949311, 1.372458522238986234 ) ) ;
#7235=CARTESIAN_POINT ( 'NONE',  ( 2.472937804810691809, 0.08526638500995675773, -1.722893361390212874 ) ) ;
#7236=CARTESIAN_POINT ( 'NONE',  ( 2.613028500285840661, -0.2118117899099076218, 2.181281865515646068 ) ) ;
#7237=CARTESIAN_POINT ( 'NONE',  ( 4.828867971087246858, 2.111205472107956282, 0.6427781511747706622 ) ) ;
#7239=CARTESIAN_POINT ( 'NONE',  ( 2.729531698892784242, 0.1106738598409856555, -2.168390435917330716 ) ) ;
#7240=CARTESIAN_POINT ( 'NONE',  ( 2.033574986395149775, -1.191784744093337123, -1.383114941912518159 ) ) ;
#7241=FILL_AREA_STYLE_COLOUR ( '', #142140 ) ;
#7242=CARTESIAN_POINT ( 'NONE',  ( 4.593022152086825294, 1.843820828628543129, 1.040707789177892861 ) ) ;
#7243=CARTESIAN_POINT ( 'NONE',  ( 6.639320575229259447, 0.002292789353198348111, 1.996863816985874118 ) ) ;
#7246=CARTESIAN_POINT ( 'NONE',  ( 5.284854174503876401, 2.022835781599085614, -1.078525118384612735 ) ) ;
#7251=CARTESIAN_POINT ( 'NONE',  ( 6.633471381225481522, -0.1569934505771773126, 2.186332552071496682 ) ) ;
#7257=CARTESIAN_POINT ( 'NONE',  ( 5.063125043234593115, -1.117834493326537393, 1.678003986596336761 ) ) ;
#7259=CARTESIAN_POINT ( 'NONE',  ( 3.537984270275731369, 1.304693584366970249, 1.597530370294945046 ) ) ;
#7261=CARTESIAN_POINT ( 'NONE',  ( -0.2409995289980037536, -0.004801160710915518791, -2.000252362011435192 ) ) ;
#7265=CARTESIAN_POINT ( 'NONE',  ( 6.544889499999918314, -1.757580744090202041, -1.308772488114395616 ) ) ;
#7266=CARTESIAN_POINT ( 'NONE',  ( 3.006482587178582300, -1.942541511447487990, 0.5404910644229294903 ) ) ;
#7267=CARTESIAN_POINT ( 'NONE',  ( 2.876309626556411203, -0.1380247437976732383, -1.836149222064882514 ) ) ;
#7271=CARTESIAN_POINT ( 'NONE',  ( 6.088856429251793934, -0.2706771573857471580, -1.805266125362497531 ) ) ;
#7273=CARTESIAN_POINT ( 'NONE',  ( 6.385631343721732911, 1.554564302923328700, 1.644106664497286596 ) ) ;
#7274=CARTESIAN_POINT ( 'NONE',  ( 2.227300950330353579, 0.0009978793536376256035, 2.106257355060832115 ) ) ;
#7283=CARTESIAN_POINT ( 'NONE',  ( 3.744553100839841608, 1.186064971860462114, -1.878093021827110354 ) ) ;
#7284=CARTESIAN_POINT ( 'NONE',  ( 2.097856687836355150, -2.190910012095201420, 0.05558666267656967030 ) ) ;
#7286=CARTESIAN_POINT ( 'NONE',  ( 0.1884680354247054990, -1.036234488384666586, 1.948478269905975946 ) ) ;
#7288=CARTESIAN_POINT ( 'NONE',  ( 5.002378505967388200, 1.956489882415031190, 0.1462272935644214900 ) ) ;
#7289=CARTESIAN_POINT ( 'NONE',  ( 0.4635302585514287088, 1.806487598472360956, -0.2625014351145052438 ) ) ;
#7295=CARTESIAN_POINT ( 'NONE',  ( 3.832379111121624327, -1.093062754469842579, -1.817066923117337751 ) ) ;
#7297=CARTESIAN_POINT ( 'NONE',  ( 5.454052192070485638, 2.159419290912270029, -0.1019294599445344784 ) ) ;
#7299=CARTESIAN_POINT ( 'NONE',  ( 5.530750200611445067, -1.661959182355336795, 0.7928504710919548337 ) ) ;
#7304=CARTESIAN_POINT ( 'NONE',  ( -0.1239745564502250652, -0.1323307239476738673, -1.711383809018538038 ) ) ;
#7305=CARTESIAN_POINT ( 'NONE',  ( 6.827182134110196365, 2.083530588508203607, 2.119847806254702594 ) ) ;
#7308=CARTESIAN_POINT ( 'NONE',  ( 4.452137864729129646, 2.161286467946467837, -0.05003489268536746859 ) ) ;
#7310=CARTESIAN_POINT ( 'NONE',  ( 0.3327679910518215878, -1.139612444193355278, 1.306804640533586026 ) ) ;
#7312=CARTESIAN_POINT ( 'NONE',  ( 3.098656953246520906, -0.6260995091542166380, -2.069055637940686143 ) ) ;
#7313=CARTESIAN_POINT ( 'NONE',  ( 5.343030940550726804, -1.692140053440434277, 1.011138898101251016 ) ) ;
#7314=CARTESIAN_POINT ( 'NONE',  ( 4.288270029534011485, -1.659180151977168283, 0.5033209731903751649 ) ) ;
#7316=CARTESIAN_POINT ( 'NONE',  ( 0.6795420635867071013, 1.475991390215245058, 1.620154534501851096 ) ) ;
#7317=CARTESIAN_POINT ( 'NONE',  ( 1.519075522400476830, 1.548194965108589782, -1.711296875134951545 ) ) ;
#7318=CARTESIAN_POINT ( 'NONE',  ( 3.145831276397454079, 0.7450406991881215468, -1.921561753228885783 ) ) ;
#7319=CARTESIAN_POINT ( 'NONE',  ( 6.093304272135602773, -0.6500253571345508963, 1.830188593850643697 ) ) ;
#7327=CARTESIAN_POINT ( 'NONE',  ( 2.239569982544288518, -1.971322999760493300, 0.9919465654871155724 ) ) ;
#7330=CARTESIAN_POINT ( 'NONE',  ( 0.6372766190945264864, 1.739209566756502845, -0.6625725129940361890 ) ) ;
#7331=CARTESIAN_POINT ( 'NONE',  ( -0.1291982275798261026, 4.084732128465967449, -2.628654587324832814 ) ) ;
#7336=CARTESIAN_POINT ( 'NONE',  ( 6.228435704027582176, 0.1854037366294820077, 1.831779187086844729 ) ) ;
#7338=CARTESIAN_POINT ( 'NONE',  ( 2.641540400197890825, -1.526127808488053628, -1.385168266076434174 ) ) ;
#7344=CARTESIAN_POINT ( 'NONE',  ( 0.8310182365124726411, 0.1507505247145359273, 2.055422933874837099 ) ) ;
#7346=CARTESIAN_POINT ( 'NONE',  ( 4.757273854911123756, 1.820453720981948242, -0.2752165127944474210 ) ) ;
#7349=CARTESIAN_POINT ( 'NONE',  ( -0.2409995289980037536, -0.004801160710915518791, -2.000252362011435192 ) ) ;
#7350=CARTESIAN_POINT ( 'NONE',  ( 4.477303810882872881, 0.001702072213635372200, -2.207063162522747479 ) ) ;
#7351=CARTESIAN_POINT ( 'NONE',  ( 6.872354139354274416, -1.400524804419982727, 1.777693731722047588 ) ) ;
#7353=CARTESIAN_POINT ( 'NONE',  ( 0.6328886395040033142, 1.767934563615305432, 0.7296191750566642931 ) ) ;
#7354=CARTESIAN_POINT ( 'NONE',  ( 0.8312679839070147292, -1.592664559859976237, -1.236796411087807801 ) ) ;
#7356=CARTESIAN_POINT ( 'NONE',  ( 1.546695614565428922, 2.123301925303363369, -0.8802762395820094010 ) ) ;
#7361=CARTESIAN_POINT ( 'NONE',  ( 0.8131078318618142342, -0.2785150557334699073, 1.849687307983488571 ) ) ;
#7362=CARTESIAN_POINT ( 'NONE',  ( 2.026577684455236561, 0.4465047249504557891, 1.966304233017155845 ) ) ;
#7366=CARTESIAN_POINT ( 'NONE',  ( 3.563196004013529983, -1.857486927118640718, -0.9925908497740908443 ) ) ;
#7371=CARTESIAN_POINT ( 'NONE',  ( 3.867448311701796371, -1.681569574351711838, -1.118542113429069396 ) ) ;
#7373=CARTESIAN_POINT ( 'NONE',  ( 6.637180544258393766, -0.09741176211745629365, -2.060485520500746848 ) ) ;
#7375=CARTESIAN_POINT ( 'NONE',  ( 4.183022562662654487, -0.2072598778708051315, -2.151613130492259440 ) ) ;
#7381=CARTESIAN_POINT ( 'NONE',  ( 2.365899470183946640, -0.4773124685180894500, 2.117905883517334775 ) ) ;
#7384=CARTESIAN_POINT ( 'NONE',  ( 1.276629239279066574, 1.701104413791530767, -0.7050613402737049284 ) ) ;
#7386=CARTESIAN_POINT ( 'NONE',  ( 3.087623348389135547, -0.8860277256741244667, 2.004638750299721828 ) ) ;
#7388=CARTESIAN_POINT ( 'NONE',  ( 4.047957556655322087, 0.7652766760943878754, -2.129282649148962925 ) ) ;
#7395=CARTESIAN_POINT ( 'NONE',  ( 5.641803817319237524, 0.7161603046910887116, -1.618556768665664114 ) ) ;
#7397=CARTESIAN_POINT ( 'NONE',  ( 1.975741970143765736, 2.015461639870301358, -0.6107432106882881850 ) ) ;
#7400=CARTESIAN_POINT ( 'NONE',  ( 1.029674291210751269, 1.899031994249468225, -0.5220998716058099509 ) ) ;
#7403=CARTESIAN_POINT ( 'NONE',  ( 6.011934222899888880, -0.6017306232493442320, 1.708898994858050191 ) ) ;
#7407=CARTESIAN_POINT ( 'NONE',  ( 5.190257414508706368, -1.856628772771324210, -0.2281712211116558864 ) ) ;
#7409=CARTESIAN_POINT ( 'NONE',  ( 4.645415698524104187, 1.851598927129452177, -0.9261206523473937136 ) ) ;
#7419=CARTESIAN_POINT ( 'NONE',  ( 4.316819842036943911, -1.455217238560998272, 1.315978175897666080 ) ) ;
#7422=CARTESIAN_POINT ( 'NONE',  ( 1.634138513624566080, 0.1511188354343559193, -2.010518437453466589 ) ) ;
#7426=CARTESIAN_POINT ( 'NONE',  ( 2.407302635362520427, -0.4140892318466664057, 1.823965488845371796 ) ) ;
#7428=CARTESIAN_POINT ( 'NONE',  ( 4.570568844821727872, 0.7744313447282255014, 1.858482759491510095 ) ) ;
#7431=CARTESIAN_POINT ( 'NONE',  ( 3.480171074976373013, -2.114893226951024108, -0.1016293738061168905 ) ) ;
#7433=CARTESIAN_POINT ( 'NONE',  ( 5.072747062355987602, 1.430223858385268665, -1.497173470029027120 ) ) ;
#7435=CARTESIAN_POINT ( 'NONE',  ( 1.435225040761441972, -1.516673362169782990, -1.439332739067126443 ) ) ;
#7436=CARTESIAN_POINT ( 'NONE',  ( 6.620655732516647518, 3.684600858287550906, 2.687722323901103660 ) ) ;
#7437=CARTESIAN_POINT ( 'NONE',  ( 0.09417432218480553674, -0.3651332853754212238, -1.691417143215419028 ) ) ;
#7446=CARTESIAN_POINT ( 'NONE',  ( 5.883449979803576646, 0.1360998956825946737, -1.907488392096804874 ) ) ;
#7453=FACE_OUTER_BOUND ( 'NONE', #22740, .T. ) ;
#7457=CARTESIAN_POINT ( 'NONE',  ( 6.503528962204017994, -1.955192063461574259, 0.4926555484118036454 ) ) ;
#7460=CARTESIAN_POINT ( 'NONE',  ( -0.1399997263889663501, 0.2375346743129815030, -2.034463206964792548 ) ) ;
#7463=CARTESIAN_POINT ( 'NONE',  ( 2.658990959838656742, 1.584636853462956685, -1.169278883008363135 ) ) ;
#7464=CARTESIAN_POINT ( 'NONE',  ( 4.851185501729457172, 0.1948232160459452411, -2.006962824030594561 ) ) ;
#7466=CARTESIAN_POINT ( 'NONE',  ( 6.727182134110181622, 6.034673098952469950, 2.683942742083842425 ) ) ;
#7467=CARTESIAN_POINT ( 'NONE',  ( 5.296902861200166512, 1.790115547914197247, 1.263834295783084150 ) ) ;
#7469=CARTESIAN_POINT ( 'NONE',  ( 3.452094016638465490, 1.926566264197142830, 0.001310335549949831480 ) ) ;
#7471=CARTESIAN_POINT ( 'NONE',  ( -0.02968770228139669398, 7.629137130509076492, -2.426318643530885222 ) ) ;
#7478=CARTESIAN_POINT ( 'NONE',  ( 5.671403949121008203, 1.101820082107987098, 1.475039313902235305 ) ) ;
#7479=CARTESIAN_POINT ( 'NONE',  ( 2.807291710112637340, 1.725400251052783052, -1.036881053028392508 ) ) ;
#7480=CARTESIAN_POINT ( 'NONE',  ( 5.800273438847154850, -2.081326394616866970, 0.9752826944557994038 ) ) ;
#7482=CARTESIAN_POINT ( 'NONE',  ( 2.887382943596613849, -1.738241981009930992, 0.6650857031204291392 ) ) ;
#7487=CARTESIAN_POINT ( 'NONE',  ( 6.251524270843968445, 2.085125267542327965, -0.1543399900023248728 ) ) ;
#7491=CARTESIAN_POINT ( 'NONE',  ( 6.340463942928090901, 1.707257656261139234, 0.2451334271395839426 ) ) ;
#7493=CARTESIAN_POINT ( 'NONE',  ( 1.845948222207854483, 0.2957656664513158007, -1.708526460754287157 ) ) ;
#7498=CARTESIAN_POINT ( 'NONE',  ( 6.614155491087242211, 2.165850671381476023, -0.1511765098734293433 ) ) ;
#7499=CARTESIAN_POINT ( 'NONE',  ( 5.936143289257818978, 0.8957264799932495025, -1.590785280889392528 ) ) ;
#7500=CARTESIAN_POINT ( 'NONE',  ( 2.272246806564695021, -0.9202570425024100276, -1.732484491337261456 ) ) ;
#7504=CARTESIAN_POINT ( 'NONE',  ( 3.545663791850160784, -1.958584582392399742, 0.8131309587096480218 ) ) ;
#7509=CARTESIAN_POINT ( 'NONE',  ( 1.657173498210939622, 1.694793865239911712, -1.188712540599102141 ) ) ;
#7512=CARTESIAN_POINT ( 'NONE',  ( 3.071146466883535098, -1.680802468121232573, 1.452339882875167021 ) ) ;
#7514=CARTESIAN_POINT ( 'NONE',  ( 1.442429577410338615, -1.974492438002553918, -1.176823363874231587 ) ) ;
#7516=CARTESIAN_POINT ( 'NONE',  ( 6.543808478091840186, 1.418056970388498206, 1.498012503012560170 ) ) ;
#7523=CARTESIAN_POINT ( 'NONE',  ( 2.812653035604309348, -0.5591599321941118639, -1.828790038765286452 ) ) ;
#7524=CARTESIAN_POINT ( 'NONE',  ( -0.1102773484823885153, 6.947233595868168798, -2.798541112319170576 ) ) ;
#7525=CARTESIAN_POINT ( 'NONE',  ( 4.014446192991796281, 1.219382930577699309, -1.220076339321971570 ) ) ;
#7526=CARTESIAN_POINT ( 'NONE',  ( 1.885954221117658092, -2.015980662343511032, 0.05432778586660082232 ) ) ;
#7527=CARTESIAN_POINT ( 'NONE',  ( 4.324990310505356206, 0.9834070133523404866, -2.077815080336536280 ) ) ;
#7528=CARTESIAN_POINT ( 'NONE',  ( 3.919400689748584465, -0.1713981403653370705, 2.255992170122776308 ) ) ;
#7529=CARTESIAN_POINT ( 'NONE',  ( 5.197925827040419833, -0.7590715138193807610, 1.964706065220876541 ) ) ;
#7531=CARTESIAN_POINT ( 'NONE',  ( 5.096827573163183800, 1.471272477087566699, -0.9831756853606200552 ) ) ;
#7533=CARTESIAN_POINT ( 'NONE',  ( 1.271856881794002136, 1.368814058113819732, 1.838566387026792093 ) ) ;
#7534=CARTESIAN_POINT ( 'NONE',  ( 5.648353745280480176, -1.448853643138726000, 1.135948691490688667 ) ) ;
#7537=CARTESIAN_POINT ( 'NONE',  ( 5.789076383285488347, 1.657349226701849476, 1.433863557930945110 ) ) ;
#7541=CARTESIAN_POINT ( 'NONE',  ( 5.617656447048144486, 0.4075009240860455462, -2.029694874052537568 ) ) ;
#7542=CARTESIAN_POINT ( 'NONE',  ( 0.1808755166769344669, 1.673851406602990366, -1.124249698880399162 ) ) ;
#7544=CARTESIAN_POINT ( 'NONE',  ( 4.248602273900093707, 0.5149172349826669493, 1.856347322705960146 ) ) ;
#7547=CARTESIAN_POINT ( 'NONE',  ( 1.371645089906252446, -1.908569115047893394, -1.136440837462453723 ) ) ;
#7557=CARTESIAN_POINT ( 'NONE',  ( 1.486689167417578616, 1.889818972856545987, 0.5264814339432167811 ) ) ;
#7560=CARTESIAN_POINT ( 'NONE',  ( 6.566857081534598350, 1.454584517406570132, -1.316677807353151097 ) ) ;
#7563=CARTESIAN_POINT ( 'NONE',  ( 0.1985910703563107393, -2.262096406685298877, -0.05156929113746439725 ) ) ;
#7567=CARTESIAN_POINT ( 'NONE',  ( 0.9131076777311696313, -0.2804849920042574718, 1.849292663789033009 ) ) ;
#7568=CARTESIAN_POINT ( 'NONE',  ( 0.3517064098005295292, 0.1722828621854489983, -1.725525930370126249 ) ) ;
#7571=CARTESIAN_POINT ( 'NONE',  ( 3.913774547416096095, -1.127657808996849198, -1.879056921112078893 ) ) ;
#7572=CARTESIAN_POINT ( 'NONE',  ( 4.489522129203258771, 2.063289974401757654, -1.033470928033096037 ) ) ;
#7573=CARTESIAN_POINT ( 'NONE',  ( 6.854767756753092023, -1.595935894175725123, 1.303543064889536751 ) ) ;
#7574=CARTESIAN_POINT ( 'NONE',  ( 2.800647771853786772, 1.640754720439155268, 1.038516083699735582 ) ) ;
#7577=CARTESIAN_POINT ( 'NONE',  ( 5.115537534566190203, 1.735013203181461350, 1.219038288318145646 ) ) ;
#7579=CARTESIAN_POINT ( 'NONE',  ( 3.445935549842124690, -1.779626424299302956, -0.9480406757386842242 ) ) ;
#7583=CARTESIAN_POINT ( 'NONE',  ( 0.4865809202317071813, -0.2202831055867389420, -1.812292406919484344 ) ) ;
#7588=CARTESIAN_POINT ( 'NONE',  ( 6.034070662188514511, 1.017841854155163706, -1.791927558475673754 ) ) ;
#7593=CARTESIAN_POINT ( 'NONE',  ( 4.723309930327257433, 1.758355855194023487, 0.9934411112178792580 ) ) ;
#7594=CARTESIAN_POINT ( 'NONE',  ( 5.356174596383207032, 0.9017655805138939940, -2.030186355573161627 ) ) ;
#7599=CARTESIAN_POINT ( 'NONE',  ( 4.205972405791720270, -2.055509729078345948, 0.1495927064073861168 ) ) ;
#7600=CARTESIAN_POINT ( 'NONE',  ( 3.463517678199812266, -1.944071305346905643, -0.5350885120067663259 ) ) ;
#7608=CARTESIAN_POINT ( 'NONE',  ( 3.638045922354939954, 0.05228986736816390590, -2.015604357568132166 ) ) ;
#7609=CARTESIAN_POINT ( 'NONE',  ( 3.275182144284936925, 1.168729223632531733, 1.422615900182722992 ) ) ;
#7612=CARTESIAN_POINT ( 'NONE',  ( 0.5050340691590156084, -0.7831231796689057667, -2.170891709475693876 ) ) ;
#7614=CARTESIAN_POINT ( 'NONE',  ( 4.218171724704827596, -1.107204882465680607, -1.856345114869990320 ) ) ;
#7616=CARTESIAN_POINT ( 'NONE',  ( 3.708664688178139102, -1.738024148615105569, -1.504010254680566483 ) ) ;
#7618=CARTESIAN_POINT ( 'NONE',  ( 2.729206520949432946, -1.746158693253213379, 0.6715030345267187784 ) ) ;
#7619=CARTESIAN_POINT ( 'NONE',  ( 0.3859243437699639845, -0.9334011365476569955, 1.736406649063494623 ) ) ;
#7623=CARTESIAN_POINT ( 'NONE',  ( 1.366164030173490973, 2.173753390890633685, -0.3800739277931909355 ) ) ;
#7628=CARTESIAN_POINT ( 'NONE',  ( 5.612177202991157188, -0.8859793764278474093, -1.761228054870385806 ) ) ;
#7629=CARTESIAN_POINT ( 'NONE',  ( 5.707753894846095299, -0.5660891107236701858, 2.237086922978877457 ) ) ;
#7630=CARTESIAN_POINT ( 'NONE',  ( 0.3089402658475807195, -1.578002999302514642, 1.165503548361209063 ) ) ;
#7631=CARTESIAN_POINT ( 'NONE',  ( 2.975492196776472031, -0.2068670369150918398, 2.052202205628439913 ) ) ;
#7639=CARTESIAN_POINT ( 'NONE',  ( 4.932167329841075976, 1.246153044254302289, 1.777787927081382779 ) ) ;
#7642=CARTESIAN_POINT ( 'NONE',  ( 4.827609030688454261, 0.9420861819694618111, -1.581835861328761528 ) ) ;
#7644=CARTESIAN_POINT ( 'NONE',  ( 6.620655732516645742, 3.706282450693794139, 2.340867613974298767 ) ) ;
#7646=CARTESIAN_POINT ( 'NONE',  ( 0.6318452133688509109, 0.9670987946563678328, -1.601024004909731513 ) ) ;
#7647=CARTESIAN_POINT ( 'NONE',  ( 0.3513179634891601677, -1.816012830335328232, 1.349138783986586931 ) ) ;
#7654=CARTESIAN_POINT ( 'NONE',  ( 1.516075769870619316, 1.192070010050453099, -1.308345436402546191 ) ) ;
#7655=CARTESIAN_POINT ( 'NONE',  ( 0.04731519813723152057, -1.748418646119804576, 0.7749314921376224685 ) ) ;
#7657=CARTESIAN_POINT ( 'NONE',  ( 3.444859266486454352, -1.690994526066817105, -0.8999980677824627184 ) ) ;
#7659=CARTESIAN_POINT ( 'NONE',  ( 3.842214238857721842, -0.9727578572899638898, 1.712498773813153408 ) ) ;
#7660=CARTESIAN_POINT ( 'NONE',  ( -0.08743476694611679312, -2.120266877281291595, -0.04547849331201780226 ) ) ;
#7662=CARTESIAN_POINT ( 'NONE',  ( 2.483090063216564669, 1.711211315118581711, -0.7561169667836544761 ) ) ;
#7663=CARTESIAN_POINT ( 'NONE',  ( 6.721331452548120922, -0.1233026559786208343, 1.696394328608492819 ) ) ;
#7665=CARTESIAN_POINT ( 'NONE',  ( 2.315298440750997777, 1.971968782506158924, 0.9909306302095726160 ) ) ;
#7668=CARTESIAN_POINT ( 'NONE',  ( 6.144970055084349347, -0.2864424343173576082, -1.940704187532462210 ) ) ;
#7676=CARTESIAN_POINT ( 'NONE',  ( 2.102089431743926706, 0.7944251937819692966, -1.912079865474418439 ) ) ;
#7680=CARTESIAN_POINT ( 'NONE',  ( 6.041668349913133618, -1.996727924239691587, 0.7141442534656232688 ) ) ;
#7683=CARTESIAN_POINT ( 'NONE',  ( 0.1747926744264920174, 4.095712681614646300, -2.410328719303979739 ) ) ;
#7686=CARTESIAN_POINT ( 'NONE',  ( 5.905624997962407363, 0.3905408587613137805, 1.977747231101577352 ) ) ;
#7687=CARTESIAN_POINT ( 'NONE',  ( 6.122283701245728516, 1.895932525083013465, 0.2736375990538899572 ) ) ;
#7688=CARTESIAN_POINT ( 'NONE',  ( 6.539320575229292665, 4.694805244051019066, 2.565894911293948422 ) ) ;
#7689=CARTESIAN_POINT ( 'NONE',  ( 3.773127072069931032, 2.063069237518061705, -0.7396954945804237180 ) ) ;
#7691=CARTESIAN_POINT ( 'NONE',  ( 2.478646075381494285, -1.315928518397539548, 1.387899491812602637 ) ) ;
#7694=CARTESIAN_POINT ( 'NONE',  ( 6.204719021523306566, 1.975628225290576356, 0.7617523325972180848 ) ) ;
#7696=CARTESIAN_POINT ( 'NONE',  ( 6.005464345382193869, -2.175231771021503668, 0.2666438670960933344 ) ) ;
#7698=CARTESIAN_POINT ( 'NONE',  ( 3.205755162861756435, -1.722880287277430478, 0.08319854473674663520 ) ) ;
#7700=CARTESIAN_POINT ( 'NONE',  ( 6.152600690169603759, 2.097733681304454034, 0.3095894981632039689 ) ) ;
#7703=AXIS2_PLACEMENT_3D ( 'NONE', #151708, #57391, #86688 ) ;
#7705=CARTESIAN_POINT ( 'NONE',  ( 0.5550359226569913096, 1.633180182981083028, -1.086726831054436682 ) ) ;
#7712=CARTESIAN_POINT ( 'NONE',  ( 2.771877521378500742, 1.802570752484193184, -0.1794005705246705940 ) ) ;
#7716=CARTESIAN_POINT ( 'NONE',  ( 4.195841788199461853, 1.186545534222239962, 1.368844175430401933 ) ) ;
#7721=CARTESIAN_POINT ( 'NONE',  ( 4.861673063681271501, -0.4970775243713953517, 1.793344219904927206 ) ) ;
#7724=CARTESIAN_POINT ( 'NONE',  ( 3.163600654563469838, 1.217692022474494262, 1.478743580268084390 ) ) ;
#7725=CARTESIAN_POINT ( 'NONE',  ( 0.9205982885796895054, 1.684962172289593996, 0.7030880920091547859 ) ) ;
#7733=CARTESIAN_POINT ( 'NONE',  ( 1.886780952650327636, 1.818441039422484806, -1.031378756152110610 ) ) ;
#7734=CARTESIAN_POINT ( 'NONE',  ( 6.493193421754636319, 1.675589973874438643, -0.9503142578028888066 ) ) ;
#7736=CARTESIAN_POINT ( 'NONE',  ( 2.854317205943053271, 0.6132515345431619469, 1.719634925709014439 ) ) ;
#7737=CARTESIAN_POINT ( 'NONE',  ( 3.000804911251079510, -0.6410980074830170405, -2.111705341948390657 ) ) ;
#7739=CARTESIAN_POINT ( 'NONE',  ( 1.388764059443419407, -1.816923020173771830, -0.5969786173363604842 ) ) ;
#7741=CARTESIAN_POINT ( 'NONE',  ( 1.557020932125362078, 1.611981373198448253, -1.131376696270647075 ) ) ;
#7742=CARTESIAN_POINT ( 'NONE',  ( 2.226030366740273880, 1.884328139559983573, 0.4695921692644353107 ) ) ;
#7746=CARTESIAN_POINT ( 'NONE',  ( 6.543805726556771951, 1.282826940501276880, 1.348393317287248205 ) ) ;
#7751=CARTESIAN_POINT ( 'NONE',  ( 2.226364491882920404, 2.126620374013419301, 0.5291077681483095096 ) ) ;
#7756=CARTESIAN_POINT ( 'NONE',  ( 2.613660848560446226, -1.805822647967849193, 0.2677728182119283318 ) ) ;
#7761=CARTESIAN_POINT ( 'NONE',  ( 2.525899207762692722, -1.109253551102797664, -1.574925972939792418 ) ) ;
#7762=CARTESIAN_POINT ( 'NONE',  ( 6.438335799692933570, -1.052282694883142078, 1.655480336553965648 ) ) ;
#7769=CARTESIAN_POINT ( 'NONE',  ( 4.662978783614929235, 1.603679166536524869, -1.309313232293010776 ) ) ;
#7770=CARTESIAN_POINT ( 'NONE',  ( -0.07694640568740516995, -1.131669979810394633, -1.452919414246391261 ) ) ;
#7773=CARTESIAN_POINT ( 'NONE',  ( 5.028124288008245735, -1.972403190421234687, 1.180361310613570414 ) ) ;
#7777=CARTESIAN_POINT ( 'NONE',  ( 0.3579208530809056543, 2.266420720034970415, -0.3425275222256763397 ) ) ;
#7780=CARTESIAN_POINT ( 'NONE',  ( 5.279219580190475547, 1.305526251850267272, 1.437786642569781614 ) ) ;
#7785=CARTESIAN_POINT ( 'NONE',  ( 6.240485052285455581, 1.095381943021833449, -1.567431287326017664 ) ) ;
#7786=CARTESIAN_POINT ( 'NONE',  ( 1.119288186499637794, -1.683610015651057168, 0.3742365367947718124 ) ) ;
#7787=CARTESIAN_POINT ( 'NONE',  ( 5.735564631760891707, 0.5807582108038509272, -1.931123567068816271 ) ) ;
#7791=CARTESIAN_POINT ( 'NONE',  ( 2.642619598058312036, -1.737709898662170183, 1.162055570667380300 ) ) ;
#7792=CARTESIAN_POINT ( 'NONE',  ( 0.6722625022101048620, -1.664400848580146919, -0.6021564899992714048 ) ) ;
#7793=CARTESIAN_POINT ( 'NONE',  ( 6.557263107265463020, -1.238491779027944162, 1.591905563659588907 ) ) ;
#7795=CARTESIAN_POINT ( 'NONE',  ( 4.611445210273608986, -2.248620548832699573, 0.4443846451570551692 ) ) ;
#7796=CARTESIAN_POINT ( 'NONE',  ( 2.501564275351343181, -0.6656319730054968131, -1.608207657179961947 ) ) ;
#7800=CARTESIAN_POINT ( 'NONE',  ( 2.248989396041571887, -1.699371294898213369, -0.3429280648484279714 ) ) ;
#7802=CARTESIAN_POINT ( 'NONE',  ( 1.785388869275974955, -1.753811856250932610, 0.6230531623785877660 ) ) ;
#7803=CARTESIAN_POINT ( 'NONE',  ( 2.207711330564741559, -1.742939566808225482, -1.294460726261867034 ) ) ;
#7805=CARTESIAN_POINT ( 'NONE',  ( 3.397672961473942266, -1.985868886743065609, 0.3494831190506141883 ) ) ;
#7806=CARTESIAN_POINT ( 'NONE',  ( 1.937500000000002220, 1.451031289061040841, -1.451031289061198049 ) ) ;
#7808=CARTESIAN_POINT ( 'NONE',  ( 1.500868375504460728, 1.576442195784112155, -1.106916717273882300 ) ) ;
#7810=CARTESIAN_POINT ( 'NONE',  ( 4.500347021246276391, -1.045864285740649935, 1.959767921951799829 ) ) ;
#7816=CARTESIAN_POINT ( 'NONE',  ( 6.381102873985867063, -2.030373413249999093, -0.9015990085984818547 ) ) ;
#7817=CARTESIAN_POINT ( 'NONE',  ( 4.475024536774164119, 1.792854848340214025, 0.7970393728587571447 ) ) ;
#7820=CARTESIAN_POINT ( 'NONE',  ( 5.237693395785977479, -1.594672120175673946, -1.605097536805524916 ) ) ;
#7823=CARTESIAN_POINT ( 'NONE',  ( 2.857939457652844073, -0.6493452292726099584, 1.957851178230881395 ) ) ;
#7827=CARTESIAN_POINT ( 'NONE',  ( 4.762891570102392613, -1.670096840553733752, -0.8426394062573672183 ) ) ;
#7828=CARTESIAN_POINT ( 'NONE',  ( 3.181945575597402431, 1.368952998951804556, 1.064414454346799266 ) ) ;
#7829=CARTESIAN_POINT ( 'NONE',  ( 2.841039829263870775, 0.6241981022326682504, -1.624847995071764917 ) ) ;
#7831=CARTESIAN_POINT ( 'NONE',  ( 0.2754559168597633390, 2.135984121793169432, -0.8326521888945382921 ) ) ;
#7832=CARTESIAN_POINT ( 'NONE',  ( 0.9388347430083656686, 2.174419798330699649, 0.3756190385216377492 ) ) ;
#7833=CARTESIAN_POINT ( 'NONE',  ( 4.353126977966869759, 0.4563941458865827805, -2.040161790709469791 ) ) ;
#7834=CARTESIAN_POINT ( 'NONE',  ( 5.455005553751488989, 0.3768678912985870544, -1.904869181234331910 ) ) ;
#7838=CARTESIAN_POINT ( 'NONE',  ( 0.5631252389872200004, -1.117830369828230808, 1.678006741548984770 ) ) ;
#7842=CARTESIAN_POINT ( 'NONE',  ( 6.504528880466823537, -1.955196382115764964, 0.4926337920100053447 ) ) ;
#7846=CARTESIAN_POINT ( 'NONE',  ( 4.863791234866603475, 1.805334366393744450, -0.2710410529033688842 ) ) ;
#7847=ADVANCED_FACE ( 'NONE', ( #174298 ), #39773, .T. ) ;
#7853=CARTESIAN_POINT ( 'NONE',  ( 2.373312353838610722, -1.759458965525468210, -0.9916931515873882441 ) ) ;
#7857=CARTESIAN_POINT ( 'NONE',  ( 3.361990069819278837, -1.859032935646281581, 0.08664877711485326206 ) ) ;
#7863=CARTESIAN_POINT ( 'NONE',  ( 4.986841741376339066, -0.2268417095559888130, -1.811474396668552700 ) ) ;
#7867=CARTESIAN_POINT ( 'NONE',  ( 6.837263156049210089, -1.242709075549037312, 1.588189626643407681 ) ) ;
#7868=CARTESIAN_POINT ( 'NONE',  ( 0.5677837317836741393, -1.637140195495973671, -0.5907660828440349787 ) ) ;
#7869=CARTESIAN_POINT ( 'NONE',  ( 3.932480676516422413, 1.235928489987428325, -1.948660470369364628 ) ) ;
#7871=CARTESIAN_POINT ( 'NONE',  ( 0.1809649437218979473, -0.1514441579043615538, -2.027393396774066936 ) ) ;
#7873=CARTESIAN_POINT ( 'NONE',  ( 5.940817214068299990, 1.361788364613376601, 1.851425077211141801 ) ) ;
#7877=CARTESIAN_POINT ( 'NONE',  ( 5.242975984329111050, -1.603930480038592510, 0.9624218375651683033 ) ) ;
#7878=CARTESIAN_POINT ( 'NONE',  ( 3.410326831400651404, -1.910418641682644969, -0.08914582809275289899 ) ) ;
#7880=CARTESIAN_POINT ( 'NONE',  ( 4.916741810085082598, 1.523553907054091328, -1.596827639139485777 ) ) ;
#7881=CARTESIAN_POINT ( 'NONE',  ( 4.575475080723796495, 1.571334676144776621, 1.419386683734702226 ) ) ;
#7883=CARTESIAN_POINT ( 'NONE',  ( 6.983263157960366563, -0.003091553303710344557, 1.945923119799706669 ) ) ;
#7886=CARTESIAN_POINT ( 'NONE',  ( 5.971359625099014856, -1.818578809777360972, -1.090262957368436147 ) ) ;
#7887=CARTESIAN_POINT ( 'NONE',  ( 2.819673282491507393, -0.2271757706859862669, 2.296386706371948527 ) ) ;
#7888=CARTESIAN_POINT ( 'NONE',  ( 4.141029529442549872, -0.1900441490861082827, -1.952618137025011746 ) ) ;
#7890=CARTESIAN_POINT ( 'NONE',  ( 6.877782380132525297, -2.002170498271789167, 0.4952429967341723804 ) ) ;
#7894=CARTESIAN_POINT ( 'NONE',  ( 5.753138727196851043, 0.1435251449807967150, -2.011451301405759118 ) ) ;
#7896=DIRECTION ( 'NONE',  ( -0.9999980456341539536, 0.000000000000000000, -0.001977050295949901899 ) ) ;
#7898=CARTESIAN_POINT ( 'NONE',  ( 1.745237678848761576, -0.3157848129633227807, -2.147843386395100751 ) ) ;
#7904=CARTESIAN_POINT ( 'NONE',  ( 1.475930922893650798, 1.225283507603215805, 1.656815433548680438 ) ) ;
#7910=CARTESIAN_POINT ( 'NONE',  ( 3.106014470790594562, -0.7728303494197851231, 1.749331318715248385 ) ) ;
#7912=CARTESIAN_POINT ( 'NONE',  ( 5.225387627957367442, -1.679756879107903833, 0.5577133518330120721 ) ) ;
#7917=CARTESIAN_POINT ( 'NONE',  ( -0.08802119743880723601, -1.811174541614871236, -0.04475806069833241502 ) ) ;
#7919=CARTESIAN_POINT ( 'NONE',  ( 6.099236069963973605, -0.2290726985337887822, 1.901777391499546166 ) ) ;
#7921=CARTESIAN_POINT ( 'NONE',  ( 0.3970419974134197783, 0.3524218036512065111, 2.039982198586967943 ) ) ;
#7923=CARTESIAN_POINT ( 'NONE',  ( 6.121928861531041655, -1.040746078065577063, -1.554202398018275755 ) ) ;
#7924=CARTESIAN_POINT ( 'NONE',  ( 3.369579884941567016, 1.780956498284639533, -0.4009276245297774266 ) ) ;
#7925=CARTESIAN_POINT ( 'NONE',  ( 6.199877634063251541, -0.7475181258948644381, 2.076568058718592624 ) ) ;
#7928=CARTESIAN_POINT ( 'NONE',  ( 3.068856176772206457, 1.495872946324308783, -1.420456422295824916 ) ) ;
#7933=CARTESIAN_POINT ( 'NONE',  ( 5.441872305809390298, 1.387781221417656141, 1.536568222347669987 ) ) ;
#7935=CARTESIAN_POINT ( 'NONE',  ( 3.866626755795209203, -1.454868229745639008, 1.598846606682593929 ) ) ;
#7936=CARTESIAN_POINT ( 'NONE',  ( 4.213539248340679499, 1.623360089863118860, 1.201376956910469307 ) ) ;
#7937=CARTESIAN_POINT ( 'NONE',  ( 1.961309178647975715, 1.629323162926434199, 1.092499269706406428 ) ) ;
#7944=CARTESIAN_POINT ( 'NONE',  ( 2.430875351317234756, -1.673853735218135741, 1.124246214196801485 ) ) ;
#7948=CARTESIAN_POINT ( 'NONE',  ( 5.924064563541377559, -1.897137492723115049, 0.2407653536913647030 ) ) ;
#7951=CARTESIAN_POINT ( 'NONE',  ( 2.917592388753763810, -1.356314522985989646, -1.492243612603139979 ) ) ;
#7954=CARTESIAN_POINT ( 'NONE',  ( 6.739270712165630783, -1.537707103621160476, 0.7812997327944263271 ) ) ;
#7958=CARTESIAN_POINT ( 'NONE',  ( 4.587079231881330266, 1.671727914585485530, -0.8392916717318499309 ) ) ;
#7960=CARTESIAN_POINT ( 'NONE',  ( 2.377862429009020229, -2.009158356589606953, 0.4988364127441884399 ) ) ;
#7965=CARTESIAN_POINT ( 'NONE',  ( 0.4569037783100584060, -1.553534471429316666, 0.9316326570649158256 ) ) ;
#7972=AXIS2_PLACEMENT_3D ( 'NONE', #102703, #136280, #56088 ) ;
#7973=CARTESIAN_POINT ( 'NONE',  ( 6.204688727450275110, 1.789332568231709608, 0.6845011832880606439 ) ) ;
#7977=CARTESIAN_POINT ( 'NONE',  ( 6.827182134110199030, -0.004087946457608307438, 2.088967824442849341 ) ) ;
#7981=CARTESIAN_POINT ( 'NONE',  ( 2.940462584922590938, 2.145230175562794717, 0.2658940370997217584 ) ) ;
#7984=CARTESIAN_POINT ( 'NONE',  ( 0.1410940620840978321, 2.031152781523197337, 0.6094965309384676733 ) ) ;
#7985=CARTESIAN_POINT ( 'NONE',  ( 5.614214418409626539, -0.8227427255552113294, -1.629729119005427496 ) ) ;
#7989=CARTESIAN_POINT ( 'NONE',  ( 0.9308618464644430324, 0.1408870404581187008, 1.966361230860876441 ) ) ;
#7990=CARTESIAN_POINT ( 'NONE',  ( 4.007995338699682719, -0.7271224857151190601, 1.768968726348684406 ) ) ;
#7992=CARTESIAN_POINT ( 'NONE',  ( 5.072688767047404568, 1.359683132420253182, -1.425145238552152582 ) ) ;
#7993=CARTESIAN_POINT ( 'NONE',  ( 0.6736475468689150370, -1.079418705485206020, 1.614127575861698416 ) ) ;
#7997=CARTESIAN_POINT ( 'NONE',  ( 6.205353461901607304, 1.844339991697005798, -1.046509186232460697 ) ) ;
#7999=CARTESIAN_POINT ( 'NONE',  ( 3.738835060935014276, 1.816739721148411757, 0.5971339541979635568 ) ) ;
#8002=CARTESIAN_POINT ( 'NONE',  ( 0.6752036787147744912, -2.078553970830565145, -0.7415856106591718344 ) ) ;
#8004=CARTESIAN_POINT ( 'NONE',  ( 6.235026786510912800, 1.879206351595325231, 0.7223523585505615685 ) ) ;
#8008=CARTESIAN_POINT ( 'NONE',  ( 2.365759603224312446, -0.4558734232973960521, 2.019384234097781672 ) ) ;
#8018=CARTESIAN_POINT ( 'NONE',  ( 6.825078400183526739, 3.708013787890347857, 2.270222819304415385 ) ) ;
#8020=CARTESIAN_POINT ( 'NONE',  ( 4.764171500175623741, 1.615563337074712225, -0.6307657835151522230 ) ) ;
#8022=CARTESIAN_POINT ( 'NONE',  ( 2.430607852509637290, -1.277051959022021066, 1.629327859714514659 ) ) ;
#8024=CARTESIAN_POINT ( 'NONE',  ( 3.902059883959855924, -1.090250183479730461, -1.814828101457645060 ) ) ;
#8027=CARTESIAN_POINT ( 'NONE',  ( 1.516386633922983895, 0.7932475597272764523, 1.802804710252394527 ) ) ;
#8030=CARTESIAN_POINT ( 'NONE',  ( -0.1757481403069499348, -0.8193859263425256056, -1.726394157293544840 ) ) ;
#8031=CARTESIAN_POINT ( 'NONE',  ( 3.468945898361298408, 0.05672114714776231581, -2.291715584554415930 ) ) ;
#8032=CARTESIAN_POINT ( 'NONE',  ( 1.541335573940459058, -1.321205422867760548, -1.260230113935792318 ) ) ;
#8036=CARTESIAN_POINT ( 'NONE',  ( 2.689700119490782360, 1.910346015757229177, -0.6353908363993918673 ) ) ;
#8038=CARTESIAN_POINT ( 'NONE',  ( 3.221486639279776298, 0.2924833653642990861, -1.939731193138781951 ) ) ;
#8040=B_SPLINE_CURVE_WITH_KNOTS ( 'NONE', 3,
 ( #68659, #200791, #64426, #31933, #34048, #66514, #151022, #166183, #149950, #52442 ),
 .UNSPECIFIED., .F., .F.,
 ( 4, 1, 1, 1, 1, 1, 1, 4 ),
 ( 0.000000000000000000, 0.09487947018404768729, 0.1878442364269655440, 0.2584026419818104547, 0.3617053504666527530, 0.5211417612611924932, 0.7337075935910832847, 1.000000000000000000 ),
 .UNSPECIFIED. ) ;
#8043=CARTESIAN_POINT ( 'NONE',  ( 5.999963288868293887, -0.7514721766869683073, -1.951089947871258001 ) ) ;
#8044=CARTESIAN_POINT ( 'NONE',  ( 4.715556530927702106, -1.735345248271908947, 0.3467660769565800161 ) ) ;
#8046=CARTESIAN_POINT ( 'NONE',  ( 1.148660753082946240, -1.725648174752218100, 1.350667304935410318 ) ) ;
#8047=CARTESIAN_POINT ( 'NONE',  ( 5.894438200647534210, 1.418812651433436933, -1.007543873543685020 ) ) ;
#8050=CARTESIAN_POINT ( 'NONE',  ( 0.2331713839410758660, 6.947498546895825022, -2.548426565200106353 ) ) ;
#8051=CARTESIAN_POINT ( 'NONE',  ( 0.1580921841808444750, -0.5169658338281759580, -2.248806653996893168 ) ) ;
#8052=( BOUNDED_SURFACE ( )  B_SPLINE_SURFACE ( 3, 3, ( 
 ( #148817, #127606, #118512, #50254, #82744, #389, #183441, #116374, #184496, #67529, #16658, #33992, #167203, #100066, #68604, #99010, #198608, #83803, #35045, #165067, #182362, #1464, #166129, #17715, #149896, #114264, #61439, #81680, #2529, #143806, #200734, #180260, #133672, #15593, #18792, #134727, #209804, #199676, #51319, #52384, #49198, #66461, #36115, #117447, #147766, #101116, #77686, #31884, #97961, #84875, #196508, #213782, #102198, #115319, #150964, #48150, #168264, #164019, #65405, #131552, #197554, #181309, #132602, #32936, #205008, #85950, #89170, #106518, #56655, #54516, #71803, #154157, #188777, #189843, #123878, #4658, #135777, #37193, #53442, #137914, #70730, #40415, #55582, #24129, #5724, #187703, #140063, #171464, #90231, #185564, #88085, #69671, #57720, #203934, #21975, #121737, #122818, #39331, #41490, #6803, #170386, #105428, #172544, #23052, #7880, #38265, #155222, #72879, #156296, #104342, #138987, #73968, #206085, #107602, #19865, #119580, #3593, #20915, #152025, #201800, #103269, #169331, #87010, #153082, #136843, #202868, #120660, #186639, #193039, #79304, #142201, #63052, #42563, #207159, #144353, #12160, #59848, #173633, #91309, #127077, #29495, #161636, #141150, #143282, #208216, #43626, #45760, #78231, #195193, #160552, #109741, #44693, #13230, #145420, #108665, #210355, #77160, #111878, #8960, #126000, #58782, #110801, #27343, #209273, #176805, #158423, #75035, #10023, #177882, #174696, #211420, #191959, #28421, #25204, #129218, #157366, #175752, #93446, #159484, #60918, #95587, #61994, #94514, #128150, #46829, #124936, #11084, #190899, #26270, #92387, #76098, #194110, #31632, #100872, #81438, #83554, #96649, #33741, #116124, #182111, #64126, #163767, #196258, #212484, #178955, #146466, #213537, #117193, #16408, #198360, #132357, #115067, #144, #149636, #97709, #181063, #200489, #30569, #1217, #162703, #67280, #147516, #15345, #51069, #34798, #18549, #133419, #166959, #150717, #84625, #82488, #50000, #65160, #99819, #130269, #112942, #32681, #197308, #114015, #66210, #148575, #98760, #131316, #199425, #14275, #165884, #183192, #2277, #48948, #164817, #17470, #68353, #134486, #80370, #47905, #180010, #69420, #85690, #104089, #36935, #6554, #87834, #56400, #38017, #5475, #172289, #203684, #122561, #3350, #120405, #101948, #89983, #21724, #54269, #186381, #154969, #153905, #156033, #39083, #202619, #71555, #138731, #137663, #40154, #70480, #170138, #55332, #72632, #136595, #121483, #187455, #105169, #171207, #22801, #151778, #35873, #53196, #188523, #118262, #23877, #135526, #88915, #201550, #204749, #106267, #184246, #7623, #73709, #139806, #103018, #52134, #168014, #19618, #119327, #185313, #169073, #20672, #4408, #86762, #152832, #95324, #205834, #9770, #75843, #141950, #93190, #61727, #28158, #60651, #109487, #79033, #107343, #207962, #27082, #26014, #59588, #157112, #41236, #76896, #108415, #57467, #174438, #125745, #159222, #189590, #45496, #43365, #111612, #42301, #94254, #160293, #127895, #191706, #74785, #175495, #10822, #177623, #143020, #209015, #24947, #8701, #176548, #140885, #161373, #58528, #126814, #110546, #92125, #91051, #144092, #11896, #173365, #206897, #77970, #158177, #29232, #123626, #192770, #44429, #193846, #124683, #210088, #12955, #190641, #65948, #34545, #953 ),
 ( #132096, #212218, #50802, #198106, #113746, #30300, #18282, #100615, #14013, #178687, #115863, #49735, #31368, #145149, #62779, #98492, #67019, #133155, #112677, #114801, #179750, #15083, #17210, #181848, #166691, #33485, #81174, #164556, #199157, #116930, #80099, #99557, #48685, #83286, #194919, #97444, #96385, #82226, #213285, #180800, #16141, #130010, #46557, #196001, #149371, #163500, #162437, #146203, #148317, #47635, #211155, #147253, #64911, #32425, #128942, #182929, #197048, #63854, #131060, #165622, #214316, #6295, #102761, #167753, #168816, #152567, #56142, #21467, #37756, #118004, #35607, #55077, #101684, #188260, #151518, #87576, #203421, #119066, #183993, #22548, #187196, #200231, #85433, #121226, #52932, #122303, #150456, #135277, #70225, #72369, #3086, #20420, #138470, #84365, #5216, #39901, #154714, #86502, #38824, #201291, #169877, #103829, #153646, #71291, #137403, #104908, #51881, #170948, #88654, #69157, #204492, #106010, #185048, #19353, #172032, #2017, #36672, #4154, #68086, #134221, #136336, #202356, #54006, #120144, #186122, #11646, #205573, #207716, #206644, #108160, #110295, #76649, #45243, #10575, #174188, #43120, #77717, #143839, #107088, #142764, #141705, #176303, #73443, #58277, #123371, #175245, #91872, #59339, #109235, #8443, #139547, #74531, #27906, #173110, #209834, #190391, #92934, #23624, #127636, #89733, #42049, #25759, #157928, #125493, #94003, #60397, #158978, #191455, #111360, #57211, #9521, #26831, #124433, #24690, #160042, #155781, #61471, #189338, #208769, #90794, #193601, #7366, #40977, #126561, #156858, #192521, #140631, #44175, #75593, #180551, #178438, #32172, #177365, #128695, #62533, #181602, #28979, #96133, #165363, #145957, #148066, #161113, #98249, #164305, #15894, #194663, #13772, #46308, #112424, #95064, #210906, #63606, #33230, #80923, #48443, #196801, #179501, #64665, #214072, #162186, #31123, #50548, #12699, #65698, #78777, #131845, #211967, #79848, #115607, #99313, #83037, #197855, #16956, #691, #149112, #147012, #114558, #129761, #81978, #30044, #144898, #97197, #47382, #195745, #130811, #213036, #163250, #113495, #49486, #14832, #66757, #132898, #198902, #151260, #168561, #36419, #71034, #72106, #6036, #101428, #18023, #133972, #150198, #20160, #167499, #137147, #152317, #120968, #102497, #69966, #22279, #53750, #186938, #67825, #184793, #166432, #154458, #86247, #118808, #3894, #4956, #136076, #138216, #103572, #52677, #202092, #203173, #119883, #104646, #135020, #185861, #37496, #54819, #201034, #169630, #21213, #87317, #153384, #38570, #1768, #100362, #170692, #88390, #204229, #116670, #182668, #34290, #84109, #199980, #51627, #117752, #183742, #35352, #19097, #85176, #2832, #68901, #25509, #191198, #91617, #9265, #75336, #89471, #39629, #56953, #192265, #122039, #176053, #155524, #157667, #205315, #208513, #43926, #188003, #141453, #142505, #173936, #40717, #42865, #159784, #59079, #123125, #125239, #55881, #7105, #73179, #60147, #105736, #189084, #110041, #24423, #26577, #171765, #108973, #174991, #92680, #139285, #106823, #172852, #90536, #23361, #156601, #8192, #126305, #207460, #158725, #10322, #58015, #76396, #27647, #74277, #124179, #143582, #140370, #93746, #206388, #11386, #190142, #41796, #77464, #107909, #115368, #98011, #49247, #32984, #197603, #179248 ),
 ( #128448, #180309, #61221, #64420, #81733, #31929, #29798, #47128, #129513, #164067, #165115, #99060, #194415, #111102, #12452, #28724, #113244, #46057, #15645, #30872, #213834, #195493, #162999, #181360, #146767, #65452, #160860, #63354, #44993, #16707, #96951, #79600, #131601, #209575, #130565, #82792, #127377, #211718, #147815, #112179, #80676, #14580, #196555, #212784, #48197, #193349, #177108, #114310, #94810, #62288, #78529, #144647, #178183, #210662, #95882, #161937, #13530, #145719, #119631, #201850, #35097, #148866, #66509, #102245, #4707, #136895, #116422, #118562, #117497, #18841, #20965, #53494, #173399, #135826, #84927, #168318, #202922, #54566, #17765, #185615, #52436, #87062, #198655, #183488, #34042, #85999, #2583, #184546, #19914, #133722, #50304, #199728, #153134, #83853, #120714, #101168, #3643, #440, #41268, #132651, #167255, #151015, #68653, #36166, #70781, #37248, #69722, #152073, #24981, #182413, #134776, #103318, #200784, #169380, #100115, #166177, #186687, #51374, #149943, #107376, #1513, #67577, #74818, #145184, #143053, #211190, #141982, #127930, #45530, #12991, #109518, #174469, #175525, #159253, #62815, #28193, #44464, #124715, #42335, #61762, #108450, #194955, #158211, #94288, #210121, #125779, #190674, #29265, #193882, #206932, #92158, #111645, #59623, #128976, #157144, #207996, #76927, #79066, #9800, #46591, #161407, #93221, #177657, #191741, #176582, #110580, #160328, #11932, #78004, #95357, #58561, #144128, #112709, #75875, #178721, #91084, #43396, #26045, #8737, #140918, #27115, #10854, #209048, #60684, #126848, #192805, #162472, #198138, #100648, #18317, #212253, #214349, #213317, #114832, #116963, #83317, #51912, #17242, #180831, #49769, #84400, #150488, #113780, #149404, #148349, #182961, #80132, #64941, #130042, #181880, #98526, #65979, #115895, #15117, #146236, #81206, #34576, #179782, #2047, #197081, #99589, #30336, #134254, #96421, #48718, #32456, #164587, #132129, #166725, #67051, #165655, #33517, #118035, #63887, #16173, #986, #131092, #82257, #196035, #47669, #133188, #147285, #14045, #199188, #50836, #68118, #31402, #200261, #97476, #163532, #20451, #6328, #138501, #106040, #202389, #52961, #54041, #37788, #155813, #121255, #137438, #3118, #135309, #154745, #201322, #73477, #36705, #187227, #88685, #4185, #69188, #122335, #72401, #85463, #185081, #204524, #152600, #7397, #35638, #86534, #169911, #172063, #102792, #120178, #23656, #184021, #104940, #89767, #101717, #139578, #119099, #5248, #168848, #188292, #205604, #167788, #55109, #56173, #87608, #70256, #170980, #57242, #38856, #136370, #22579, #19384, #186154, #103862, #39932, #151549, #21500, #153678, #71323, #203454, #107118, #44206, #126590, #192551, #74561, #174218, #206676, #8474, #189366, #156887, #9551, #127667, #26860, #208801, #142795, #125526, #10604, #94033, #42079, #191485, #210935, #41008, #11674, #173141, #160071, #157958, #25792, #61501, #45271, #29009, #77749, #177395, #161144, #111392, #92964, #60430, #75626, #110326, #140661, #123402, #43153, #207743, #124463, #76680, #159010, #109266, #108193, #143870, #24722, #176331, #209863, #193629, #141736, #175274, #27938, #95095, #78805, #12731, #91902, #90824, #58307, #190422, #144928, #59369, #16985, #98276, #66787, #48471, #15923, #182700, #214099, #132927, #13803 ),
 ( #34318, #128724, #113525, #114588, #198932, #129792, #147040, #50578, #62560, #197884, #166463, #116700, #64693, #165390, #179532, #148096, #99341, #131875, #180579, #150229, #178465, #130838, #164334, #97224, #80949, #79875, #112452, #65728, #31151, #194696, #163277, #196830, #82006, #46338, #100393, #32199, #18056, #14859, #83065, #149142, #84142, #213063, #145985, #49513, #115633, #30075, #181628, #33258, #96166, #211996, #722, #63637, #162216, #195772, #47411, #121003, #36455, #35386, #154492, #104680, #117785, #2864, #186971, #184825, #188036, #67857, #52710, #202126, #138251, #68933, #86280, #204264, #1800, #137184, #105775, #72142, #3928, #170728, #118842, #87353, #21246, #71067, #4990, #169662, #38602, #183775, #153421, #203206, #135056, #122075, #54852, #102531, #101461, #89506, #171801, #85208, #167532, #22315, #88427, #168593, #134006, #200011, #6071, #55916, #39665, #19129, #185893, #20193, #152352, #23393, #51661, #151293, #201068, #69997, #136110, #53786, #119918, #37528, #103605, #59112, #27681, #205350, #190176, #40752, #92710, #9299, #125271, #175022, #140406, #56985, #206425, #93778, #24460, #61251, #107942, #10352, #155560, #45025, #7143, #173968, #25542, #91650, #42896, #11419, #123158, #172886, #189118, #207492, #58048, #110070, #191233, #159816, #141486, #109005, #127408, #158757, #77495, #106859, #75371, #90574, #193381, #26610, #157702, #76427, #43955, #142537, #111136, #208543, #60178, #126336, #143614, #192295, #209607, #176083, #177139, #28756, #73214, #139320, #156634, #8226, #74310, #124214, #41830, #210691, #12486, #112208, #213864, #94840, #197635, #128479, #163031, #178216, #81765, #65487, #78560, #212817, #147846, #96982, #161968, #48230, #115400, #130598, #29831, #196587, #160891, #95915, #13559, #131634, #144679, #211750, #181393, #47161, #49280, #194447, #98043, #31960, #164096, #79630, #129542, #145749, #63388, #62320, #195524, #14613, #33017, #114342, #15679, #46091, #113277, #179282, #30907, #80710, #146800, #64453, #180338, #176764, #140028, #44651, #108633, #190865, #12118, #210316, #194069, #28380, #128111, #111841, #61952, #43589, #159445, #174660, #11043, #91275, #73934, #142164, #158390, #75004, #27302, #191924, #76065, #207124, #110765, #206053, #143245, #160515, #94474, #26235, #125968, #208181, #78192, #29458, #177845, #58749, #57688, #209234, #144318, #45722, #92352, #109707, #59813, #95547, #161599, #123845, #124902, #189806, #157332, #107566, #175711, #42528, #41458, #93408, #173601, #77122, #60879, #25173, #127038, #8923, #141113, #192998, #9987, #174647, #157319, #172499, #76052, #11030, #24085, #123833, #93394, #91260, #94461, #188732, #173588, #108619, #44638, #189795, #207109, #110753, #122772, #43576, #12106, #192984, #124888, #77108, #25158, #208168, #142153, #191912, #125956, #59799, #159431, #90190, #109694, #175698, #41446, #28366, #27288, #8910, #7832, #210298, #78176, #206041, #156253, #143232, #209222, #74990, #40370, #106472, #60864, #176751, #160501, #73923, #92339, #141098, #58736, #127026, #144304, #140016, #57675, #190852, #107554, #42513, #26223, #158381, #9974, #179955, #148522, #111825, #96595, #161584, #213483, #130212, #31578, #81378, #46774, #177827, #112888, #88, #145368, #182056, #14218, #131263, #61938, #165830, #128096, #80313, #146413, #212426, #163711 ),
 ( #29444, #147462, #64068, #62992, #15293, #97652, #196205, #195138, #32626, #194054, #197250, #66153, #98703, #162645, #113958, #47847, #16352, #17414, #83498, #178900, #95535, #79250, #13171, #65107, #30514, #82432, #48889, #132298, #115009, #181006, #33686, #164762, #198305, #211367, #49945, #129161, #116066, #99763, #149580, #45706, #104038, #36881, #39032, #202564, #151725, #169022, #87779, #20620, #203630, #19565, #119272, #4359, #170084, #85639, #185257, #136544, #102964, #86708, #152777, #34744, #199369, #2223, #137614, #67228, #121430, #100817, #70428, #150661, #153853, #55282, #133362, #54216, #5424, #120354, #200434, #186331, #105116, #37965, #68298, #21671, #1164, #166902, #18495, #71503, #51015, #134431, #187400, #184195, #171156, #117136, #22746, #88864, #183139, #84573, #52081, #118208, #35818, #101894, #167959, #3297, #69365, #135474, #201495, #53142, #157062, #42249, #125693, #73657, #8650, #28107, #6503, #43317, #72578, #191652, #189537, #57409, #93134, #76847, #60601, #109435, #208969, #192720, #142966, #124634, #25964, #41185, #92069, #172240, #154919, #74729, #138679, #205781, #140834, #126760, #7572, #24893, #44374, #204698, #75794, #110497, #10773, #206847, #175441, #123575, #158127, #174386, #9718, #141902, #108362, #27026, #56348, #207912, #59533, #139757, #176496, #159173, #107292, #40102, #122510, #188470, #23828, #106214, #89933, #155984, #173314, #90999, #58479, #190592, #164510, #82178, #61675, #63803, #62728, #178637, #180753, #147209, #115817, #81124, #30249, #113699, #148272, #214271, #177567, #213234, #212169, #32380, #144038, #128889, #193795, #31319, #162389, #129961, #179703, #78981, #210035, #145100, #98446, #29180, #65904, #46504, #163452, #94202, #198060, #160242, #112627, #96333, #13966, #195949, #16094, #131011, #15032, #47585, #181804, #127843, #80050, #97396, #194870, #146153, #45444, #111558, #64866, #211104, #11842, #197003, #48638, #114756, #77919, #132050, #49689, #95269, #161317, #12901, #202311, #169837, #51836, #116882, #117954, #101640, #5172, #185004, #201246, #66972, #199108, #4109, #50753, #137361, #100571, #36628, #85387, #68035, #83240, #52887, #136290, #149325, #34497, #70178, #1972, #71245, #183949, #35559, #167706, #135233, #103786, #53960, #102713, #151471, #121179, #903, #19308, #69111, #134175, #3042, #182881, #133111, #119022, #150405, #33437, #200183, #168770, #20375, #17166, #87533, #86460, #153600, #84319, #120098, #186076, #21424, #152524, #166644, #37710, #203378, #55031, #99514, #165571, #18235, #138424, #157878, #204443, #76600, #39852, #190341, #24639, #7317, #22496, #140585, #75544, #88608, #188212, #9471, #155732, #158930, #38777, #23574, #173059, #109184, #105958, #57161, #175197, #187148, #108111, #142713, #43071, #189287, #141653, #89683, #58225, #206596, #42003, #174138, #124383, #207665, #154663, #25712, #91821, #171982, #92885, #59284, #73395, #72318, #60348, #208722, #56097, #6249, #125443, #191404, #139498, #104859, #170903, #26780, #10526, #122253, #205526, #156809, #123324, #40929, #107033, #90749, #8396, #74480, #213772, #148807, #117434, #35032, #212724, #33980, #32923, #1451, #179188, #164005, #14521, #66450, #197542, #98999, #376, #114252, #30812, #180248, #67516, #64363, #101106, #81668, #198594, #126511, #18779, #192473, #133661 ),
 ( #47067, #100055, #15581, #31872, #199662, #51308, #167192, #17704, #183431, #84865, #150953, #165054, #132592, #147754, #50241, #146708, #113184, #49187, #65394, #130509, #82731, #16646, #131540, #48139, #166119, #96891, #116361, #2517, #83791, #115306, #181296, #182351, #149886, #162940, #80615, #97951, #196496, #85939, #102186, #120649, #53429, #23042, #104329, #72869, #54505, #21964, #188765, #5713, #138975, #19852, #136831, #118502, #135766, #55572, #172534, #89158, #171453, #170377, #106507, #121726, #4648, #88072, #155211, #154145, #56642, #86998, #186628, #71790, #6792, #153071, #38255, #203924, #137905, #187691, #39320, #168253, #52373, #69658, #204998, #134716, #40405, #152012, #105415, #3583, #122806, #24118, #200722, #90221, #156285, #68590, #119566, #184484, #36101, #201789, #185553, #37182, #103257, #169318, #20902, #70718, #202857, #141137, #210340, #190886, #193025, #206074, #143269, #11069, #77148, #173622, #58770, #91298, #107590, #73957, #41479, #108655, #44677, #42552, #59835, #142188, #176791, #177869, #111864, #207147, #123865, #25194, #157356, #125988, #124925, #28406, #43611, #12144, #208202, #175736, #128133, #159471, #78217, #8945, #76086, #57708, #75025, #209259, #29481, #94500, #110789, #109729, #45746, #60904, #158410, #27329, #160538, #93431, #61979, #26257, #191945, #127063, #144340, #92373, #194097, #95572, #7869, #140049, #189830, #174683, #10010, #162687, #83541, #13215, #67266, #46813, #197292, #96633, #99805, #149622, #79288, #32665, #33727, #65145, #146452, #148563, #51055, #164802, #14262, #16394, #161622, #112927, #178940, #165870, #145406, #80353, #1204, #130253, #132341, #211406, #82473, #129, #66197, #30554, #212467, #64111, #196244, #63036, #195180, #47887, #17456, #131301, #98744, #181049, #163751, #48933, #198347, #114000, #15330, #34784, #129203, #49987, #179995, #116105, #31619, #97693, #133405, #199410, #117179, #182096, #183180, #81420, #147501, #115051, #213522, #201535, #186368, #118251, #100859, #169060, #185297, #101934, #54256, #4395, #103004, #19606, #71541, #166943, #170123, #187442, #36921, #120393, #39069, #38003, #88902, #119311, #70466, #104075, #203671, #20657, #136583, #21709, #202603, #87820, #153892, #134472, #84613, #168000, #22785, #18536, #6541, #200476, #5461, #35856, #105156, #154955, #150702, #137651, #171195, #55320, #85678, #121471, #204736, #72619, #151766, #138718, #2264, #52122, #184232, #56385, #68340, #3335, #122548, #69406, #188510, #135513, #53183, #86747, #152819, #205820, #91038, #123613, #139793, #106253, #73695, #140873, #44415, #158164, #125731, #59574, #42289, #141938, #10810, #173353, #108400, #127882, #172277, #143005, #23864, #76885, #74769, #157098, #192758, #176535, #160280, #209003, #94241, #77958, #28146, #9756, #191692, #206884, #43352, #57453, #40140, #174424, #124671, #41224, #207951, #75831, #26000, #24935, #60640, #89971, #109472, #126802, #110534, #58516, #92109, #175480, #11882, #210075, #144079, #8687, #156023, #189576, #107329, #27067, #190628, #61714, #93175, #7612, #159209, #147242, #213269, #45483, #145137, #83270, #46544, #197035, #31355, #14001, #29219, #64898, #82211, #95309, #194906, #148304, #33469, #17196, #181834, #163485, #131045, #80085, #48670, #211143, #193832, #47620, #63840, #112664, #114787, #97430, #195987 ),
 ( #30287, #16127, #214303, #115849, #212204, #62765, #129997, #113732, #165606, #180787, #178672, #32410, #98476, #111599, #128929, #149358, #96372, #164542, #15067, #146189, #161358, #65934, #132083, #12941, #162424, #198093, #179738, #940, #177607, #81159, #49720, #99543, #67005, #79020, #55060, #133142, #53992, #22531, #203408, #135264, #21455, #35592, #4140, #152553, #202340, #136322, #86489, #103817, #34531, #70210, #120131, #200215, #38807, #186108, #101670, #18270, #6280, #88640, #2004, #166678, #169864, #37741, #19339, #199142, #50786, #87563, #121211, #187180, #100602, #102745, #167740, #3071, #5204, #153631, #154697, #71277, #69143, #137391, #104893, #170932, #68070, #116915, #36660, #182915, #84352, #85418, #150442, #134206, #201278, #168801, #51867, #117988, #183981, #151502, #52919, #119050, #185035, #20406, #141690, #72352, #176290, #73429, #25746, #190377, #74516, #205557, #43108, #138456, #207704, #158967, #109223, #107069, #124418, #206631, #26817, #27894, #93989, #57197, #188244, #89715, #105995, #42036, #123357, #92921, #108149, #76636, #75581, #155766, #10561, #7350, #142750, #23607, #140619, #122287, #139532, #59324, #160030, #208759, #175233, #174175, #110281, #125481, #8428, #91858, #60384, #157914, #126548, #90781, #9509, #191443, #192509, #156844, #44161, #204475, #56128, #39885, #172016, #189322, #40962, #173094, #24675, #58262, #131834, #111347, #47368, #161100, #164292, #214058, #77705, #97183, #98237, #129748, #210894, #213019, #115594, #14819, #12688, #80911, #11632, #177352, #28966, #15881, #143825, #144887, #65686, #194652, #196789, #209822, #147001, #64654, #130795, #95049, #62521, #78764, #128683, #61458, #45232, #112411, #81965, #195733, #163237, #31110, #13759, #113481, #48430, #46296, #79835, #99301, #127624, #114545, #193588, #180537, #178423, #30032, #148052, #197841, #49474, #32160, #181588, #33217, #96118, #179488, #162173, #145944, #211955, #63593, #165348, #19083, #35336, #86233, #168549, #20148, #116658, #1754, #34276, #50535, #16943, #198889, #51614, #169615, #68888, #36406, #184780, #167488, #52664, #136063, #84098, #85164, #38554, #83022, #53736, #149097, #202076, #199966, #67811, #103556, #87301, #71017, #119868, #4941, #203159, #153370, #135007, #102485, #117737, #152304, #182656, #678, #151248, #101415, #166415, #118793, #201020, #2816, #150185, #185847, #66744, #3880, #37479, #21199, #183728, #69951, #137130, #54804, #120952, #186923, #133958, #132886, #100349, #18008, #156582, #89454, #59061, #140353, #108954, #107891, #187989, #42847, #39614, #174974, #55865, #172834, #154441, #171747, #91599, #208493, #125220, #207442, #206371, #142486, #157650, #40701, #57998, #191179, #124162, #92663, #123108, #8176, #173919, #26556, #189066, #74260, #25492, #190124, #41778, #9248, #138201, #88374, #105718, #158707, #170678, #10304, #204213, #75319, #23343, #76378, #60128, #22265, #141436, #126286, #192245, #155506, #104631, #6021, #72091, #7088, #122021, #73161, #139267, #205297, #56935, #106805, #24405, #90519, #12431, #14561, #27627, #78511, #80658, #93727, #179228, #47108, #113224, #209556, #94791, #127359, #143563, #110021, #77445, #144628, #48181, #161918, #129494, #63335, #46039, #145699, #146749, #177089, #112160, #131585, #176035, #212767, #159767, #64403, #210643, #160839, #196538 ) ),
 .UNSPECIFIED., .T., .F., .F. ) 
 B_SPLINE_SURFACE_WITH_KNOTS ( ( 4, 3, 4 ),
 ( 4, 1, 1, 1, 1, 1, 1, 1, 1, 1, 1, 1, 1, 1, 1, 1, 1, 1, 1, 1, 1, 1, 1, 1, 1, 1, 1, 1, 1, 1, 1, 1, 1, 1, 1, 1, 1, 1, 1, 1, 1, 1, 1, 1, 1, 1, 1, 1, 1, 1, 1, 1, 1, 1, 1, 1, 1, 1, 1, 1, 1, 1, 1, 1, 1, 1, 1, 1, 1, 1, 1, 1, 1, 1, 1, 1, 1, 1, 1, 1, 1, 1, 1, 1, 1, 1, 1, 1, 1, 1, 1, 1, 1, 1, 1, 1, 1, 1, 1, 1, 1, 1, 1, 1, 1, 1, 1, 1, 1, 1, 1, 1, 1, 1, 1, 1, 1, 1, 1, 1, 1, 1, 1, 1, 1, 1, 1, 1, 1, 1, 1, 1, 1, 1, 1, 1, 1, 1, 1, 1, 1, 1, 1, 1, 1, 1, 1, 1, 1, 1, 1, 1, 1, 1, 1, 1, 1, 1, 1, 1, 1, 1, 1, 1, 1, 1, 1, 1, 1, 1, 1, 1, 1, 1, 1, 1, 1, 1, 1, 1, 1, 1, 1, 1, 1, 1, 1, 1, 1, 1, 1, 1, 1, 1, 1, 1, 1, 1, 1, 1, 1, 1, 1, 1, 1, 1, 1, 1, 1, 1, 1, 1, 1, 1, 1, 1, 1, 1, 1, 1, 1, 1, 1, 1, 1, 1, 1, 1, 1, 1, 1, 1, 1, 1, 1, 1, 1, 1, 1, 1, 1, 1, 1, 1, 1, 1, 1, 1, 1, 1, 1, 1, 1, 1, 1, 1, 1, 1, 1, 1, 1, 1, 1, 1, 1, 1, 1, 1, 1, 1, 1, 1, 1, 1, 1, 1, 1, 1, 1, 1, 1, 1, 1, 1, 1, 1, 1, 1, 1, 1, 1, 1, 1, 1, 1, 1, 1, 1, 1, 1, 1, 1, 1, 1, 1, 1, 1, 1, 1, 1, 1, 1, 1, 1, 1, 1, 1, 1, 1, 1, 1, 1, 1, 1, 1, 1, 1, 1, 1, 1, 1, 1, 1, 1, 1, 1, 1, 1, 1, 1, 1, 1, 1, 1, 1, 1, 1, 1, 1, 1, 1, 1, 1, 1, 1, 1, 1, 1, 1, 1, 1, 1, 1, 1, 1, 1, 1, 1, 1, 1, 1, 1, 1, 1, 1, 1, 1, 1, 1, 1, 1, 1, 1, 1, 4 ),
 ( 0.000000000000000000, 0.5000000000000000000, 1.000000000000000000 ),
 ( 0.000000000000000000, 0.002599878613971510263, 0.005208762566300055921, 0.007813076245110234588, 0.01041697056762492211, 0.01302017924898362516, 0.01562522799165661294, 0.01822895742955179393, 0.02083332403451576206, 0.02343772221867868391, 0.02604143078293654281, 0.02864626161639613477, 0.03124961764961396021, 0.03385452714844047750, 0.03645799780571232912, 0.03906266225314121432, 0.04166671052383312535, 0.04427076094224517699, 0.04687542278318937439, 0.04947889361195772356, 0.05208380280015859759, 0.05468715921365963767, 0.05729198803509916865, 0.05989568673917144287, 0.06250009379223495087, 0.06510449848632135494, 0.06770819839843210397, 0.07031302545632363288, 0.07291638160390327694, 0.07552129054917994244, 0.07812475961953217751, 0.08072942239586503033, 0.08333346963797970408, 0.08593751866472883194, 0.08854217935802578821, 0.09114564884740632145, 0.09375055680876714925, 0.09635391199924973893, 0.09895873945611717570, 0.1015624370353711836, 0.1041668426700886191, 0.1067712463110160465, 0.1093749448896196713, 0.1119797708301935452, 0.1145831257515418783, 0.1171880334468678037, 0.1197915013940491491, 0.1223961628153678316, 0.1250002090321265524, 0.1276042567216372492, 0.1302089163955687523, 0.1328123846563000476, 0.1354172914881497103, 0.1380206455552074885, 0.1406254717515977581, 0.1432291683081768907, 0.1458335726268597532, 0.1484379753169847160, 0.1510416726638619811, 0.1536464975900906083, 0.1562498513865758776, 0.1588547579349887939, 0.1614582248604825021, 0.1640628850295551278, 0.1666669303230295940, 0.1692709767774011609, 0.1718756355346959253, 0.1744791026682601387, 0.1770840084736199360, 0.1796873615186004858, 0.1822921865574477218, 0.1848958821930496710, 0.1875002852981585977, 0.1901046871399069693, 0.1927083833567690418, 0.1953132073715553307, 0.1979165601445126987, 0.2005214656490191816, 0.2031249316542690642, 0.2057295906738217384, 0.2083336351460475244, 0.2109376804673406547, 0.2135423384106908962, 0.2161458045185324639, 0.2187507094003866837, 0.2213540615246011867, 0.2239588855088016361, 0.2265625803250888304, 0.2291669823190463362, 0.2317713834148095453, 0.2343750786033309830, 0.2369799018095430365, 0.2395832536602726381, 0.2421881582238437913, 0.2447916234102597566, 0.2473962813829825302, 0.2500003251359625422, 0.2526043694262022354, 0.2552090266582678346, 0.2578124918417971090, 0.2604173959030967600, 0.2630207472078238129, 0.2656255702402394725, 0.2682292643388430320, 0.2708336653240377978, 0.2734380657761767419, 0.2760417600379992398, 0.2786465825384744077, 0.2812499335682448476, 0.2838548372938197173, 0.2864583017627815864, 0.2890629587913320364, 0.2916670019270400371, 0.2942710452882197347, 0.2968757019116316509, 0.2994791662722288139, 0.3020840696158954564, 0.3046874202023847622, 0.3072922423858477359, 0.3098959358683710530, 0.3125003359471613118, 0.3151047358580104651, 0.3177084292947467969, 0.3203132511922952008, 0.3229166015023476888, 0.3255215044928377321, 0.3281249683456989308, 0.3307296245327063788, 0.3333336671530912065, 0.3359377096871765112, 0.3385423658045411677, 0.3411458294435600336, 0.3437507321724898035, 0.3463540821419661686, 0.3489589035792820537, 0.3515625965473047621, 0.3541669958220223235, 0.3567713952938928457, 0.3593750880071304721, 0.3619799094045394461, 0.3645832590960911834, 0.3671881614543835437, 0.3697916247924753486, 0.3723962802405443862, 0.3750003224475334518, 0.3776043642564660408, 0.3802090199703688222, 0.3828124829891406122, 0.3854173852062082184, 0.3880207346598750218, 0.3906255554538268782, 0.3932292480089087938, 0.3958336465818629857, 0.3984380457170473289, 0.4010417378083525053, 0.4036465588083897882, 0.4062499079826380477, 0.4088548098116001062, 0.4114582727362346981, 0.4140629275479489335, 0.4166669694434522730, 0.4192710106291533956, 0.4218756660421624782, 0.4244791285419997062, 0.4270840303500617607, 0.4296873793891050619, 0.4322921996424575197, 0.4348958918861421385, 0.4375002898596233591, 0.4401046887603987101, 0.4427083803313200949, 0.4453132010367379379, 0.4479165497948640051, 0.4505214511973463787, 0.4531249138098211726, 0.4557295680877478938, 0.4583336097736617210, 0.4609376504380365280, 0.4635423056527069874, 0.4661457677349071238, 0.4687506692368063055, 0.4713540179623986193, 0.4739588377779012651, 0.4765625298117197040, 0.4791669272880037522, 0.4817713260566358624, 0.4843750172087082362, 0.4869798377222476216, 0.4895831861654201811, 0.4921880872442612742, 0.4947915496458628049, 0.4973962034925555886, 0.5000002450707665691, 0.5026042853157074441, 0.5052089404345847523, 0.5078124022004342208, 0.5104173034990032720, 0.5130206520123070657, 0.5156254714926987726, 0.5182291634181735995, 0.5208335604995248946, 0.5234379592382720769, 0.5260416500730202838, 0.5286464704974140894, 0.5312498187267931105, 0.5338547195848227789, 0.5364581818768299204, 0.5390628353948335727, 0.5416668769672219330, 0.5442709168946127107, 0.5468755720202369552, 0.5494790335710144635, 0.5520839347690799093, 0.5546872831712518215, 0.5572921024192640793, 0.5598957943379132551, 0.5625001911265891108, 0.5651045899377058479, 0.5677082805566486812, 0.5703131009946261765, 0.5729164491113668545, 0.5755213498514099024, 0.5781248121350983649, 0.5807294654269519185, 0.5833335070953961088, 0.5859375468071157389, 0.5885422020420250089, 0.5911456634790059894, 0.5937505646793920233, 0.5963539130715860281, 0.5989587321899475514, 0.6015624242032879820, 0.6041668208015419372, 0.6067712197872831004, 0.6093749102919370220, 0.6119797308462270324, 0.6145830789514836745, 0.6171879796763642956, 0.6197914420530098445, 0.6223960952212510556, 0.6250001370876311357, 0.6276041766855571247, 0.6302088321322918407, 0.6328122935567517260, 0.6354171948622837629, 0.6380205433456558328, 0.6406253624370956690, 0.6432290546466469250, 0.6458334511567334069, 0.6484378504193577530, 0.6510415409112403351, 0.6536463616845760161, 0.6562497098795055939, 0.6588546106920506462, 0.6614580732629331550, 0.6640627264101022220, 0.6666667685763031370, 0.6692708081623160998, 0.6718754639234225667, 0.6744789254366408970, 0.6770838269501499029, 0.6796871756258610064, 0.6822919947931124218, 0.6848956873004010681, 0.6875000838245786117, 0.6901044834663523364, 0.6927081740469867022, 0.6953129951421085364, 0.6979163435278744609, 0.7005212445309179081, 0.7031247073973251327, 0.7057293606259679164, 0.7083334031938842701, 0.7109374428698714832, 0.7135420990479055536, 0.7161455607511696408, 0.7187504625754957965, 0.7213538115447158949, 0.7239586308905210377, 0.7265623237970838533, 0.7291667204376187650, 0.7317711205608201652, 0.7343748113317387638, 0.7369796328513985584, 0.7395829815291747877, 0.7421878828255610294, 0.7447913460887924941, 0.7473959995014650692, 0.7500000425730045661, 0.7526040824408628538, 0.7552087391383944803, 0.7578122011330034047, 0.7604171033709996586, 0.7630204527349119248, 0.7656252723620247114, 0.7682289657694127971, 0.7708333626285834850, 0.7734377633355060677, 0.7760414543982535607, 0.7786462764452187768, 0.7812496255161931469, 0.7838545272087811266, 0.7864579909701516769, 0.7890626446694239959, 0.7916666883465109938, 0.7942707285081521684, 0.7968753858277685120, 0.7994788482150362308, 0.8020837509695725176, 0.8046871008293766669, 0.8072919208405671121, 0.8098956148503495545, 0.8125000120304503026, 0.8151044134234068927, 0.8177081048795449281, 0.8203129275566022338, 0.8229162771219805661, 0.8255211793136476572, 0.8281246436744912343, 0.8307292977629509023, 0.8333333421475307423, 0.8359373827048843797, 0.8385420407491936956, 0.8411455036304537058, 0.8437504070044209437, 0.8463537574613370085, 0.8489585779593948889, 0.8515622726731627568, 0.8541666702765071673, 0.8567710724578335713, 0.8593747644089445581, 0.8619795878189033811, 0.8645829379799131464, 0.8671878407735589267, 0.8697913058352330085, 0.8723959604154888359, 0.8750000056095312839, 0.8776040466645483873, 0.8802087055361843548, 0.8828121690127931354, 0.8854170731091063340, 0.8880204242643787715, 0.8906252453521178447, 0.8932289408714879642, 0.8958333390004131758, 0.8984377420724726226, 0.9010414346201626179, 0.9036462588658594752, 0.9062496097237539017, 0.9088545132223035949, 0.9114579790861923048, 0.9140626342608790811, 0.9166666803663815477, 0.9192707220210388774, 0.9218753818226663732, 0.9244788459960084914, 0.9270837509176034219, 0.9296871028724987829, 0.9322919246527909820, 0.9348956210794385768, 0.9375000198362011261, 0.9401044239011964176, 0.9427081171475072408, 0.9453129423329229564, 0.9479162939871883520, 0.9505211982878988275, 0.9531246650646376661, 0.9557293209618126228, 0.9583333680330715643, 0.9609374102905526849, 0.9635420713365114853, 0.9661455366701111602, 0.9687504417289087844, 0.9713537931426093897, 0.9739586182492501187, 0.9765623229037746489, 0.9791667147516245340, 0.9817710778420317697, 0.9843748014325267581, 0.9869798465897002826, 0.9895830499482988207, 0.9921869381715581193, 0.9947912477285243416, 0.9974001254724073062, 1.000000000000000000 ),
 .UNSPECIFIED. ) 
 GEOMETRIC_REPRESENTATION_ITEM ( )  RATIONAL_B_SPLINE_SURFACE ( (
 ( 1.000000000000000222, 1.000000000000000222, 1.000000000000000222, 1.000000000000000222, 1.000000000000000444, 1.000000000000000000, 1.000000000000000666, 0.9999999999999997780, 1.000000000000000444, 1.000000000000000000, 1.000000000000000444, 1.000000000000000444, 1.000000000000000000, 1.000000000000000444, 1.000000000000000000, 1.000000000000000444, 1.000000000000000222, 1.000000000000000222, 1.000000000000000222, 1.000000000000000444, 1.000000000000000444, 1.000000000000000000, 1.000000000000000444, 1.000000000000000000, 1.000000000000000222, 1.000000000000000222, 1.000000000000000444, 1.000000000000000222, 1.000000000000000222, 1.000000000000000444, 1.000000000000000444, 1.000000000000000444, 1.000000000000000000, 1.000000000000000444, 1.000000000000000444, 1.000000000000000000, 1.000000000000000444, 1.000000000000000444, 1.000000000000000000, 1.000000000000000444, 1.000000000000000444, 1.000000000000000000, 1.000000000000000222, 1.000000000000000444, 1.000000000000000222, 1.000000000000000222, 1.000000000000000000, 1.000000000000000444, 1.000000000000000222, 1.000000000000000222, 1.000000000000000222, 1.000000000000000222, 1.000000000000000222, 1.000000000000000222, 1.000000000000000444, 1.000000000000000000, 1.000000000000000444, 0.9999999999999997780, 1.000000000000000666, 1.000000000000000444, 1.000000000000000444, 1.000000000000000000, 1.000000000000000444, 1.000000000000000222, 1.000000000000000222, 1.000000000000000444, 1.000000000000000222, 1.000000000000000444, 1.000000000000000000, 1.000000000000000444, 1.000000000000000222, 1.000000000000000444, 1.000000000000000444, 1.000000000000000222, 1.000000000000000222, 1.000000000000000222, 1.000000000000000444, 0.9999999999999997780, 1.000000000000000444, 1.000000000000000000, 1.000000000000000444, 1.000000000000000000, 1.000000000000000444, 0.9999999999999997780, 1.000000000000000444, 0.9999999999999997780, 1.000000000000000444, 1.000000000000000222, 1.000000000000000444, 1.000000000000000000, 1.000000000000000222, 1.000000000000000444, 1.000000000000000444, 1.000000000000000222, 1.000000000000000444, 1.000000000000000444, 1.000000000000000222, 1.000000000000000222, 1.000000000000000222, 1.000000000000000222, 1.000000000000000000, 1.000000000000000222, 1.000000000000000222, 1.000000000000000222, 1.000000000000000444, 1.000000000000000000, 1.000000000000000444, 0.9999999999999997780, 1.000000000000000666, 1.000000000000000222, 1.000000000000000444, 1.000000000000000000, 1.000000000000000444, 1.000000000000000222, 1.000000000000000222, 1.000000000000000444, 1.000000000000000000, 1.000000000000000000, 1.000000000000000444, 1.000000000000000000, 1.000000000000000444, 1.000000000000000000, 1.000000000000000444, 1.000000000000000222, 1.000000000000000444, 1.000000000000000222, 1.000000000000000444, 1.000000000000000222, 1.000000000000000444, 1.000000000000000000, 1.000000000000000444, 1.000000000000000222, 1.000000000000000444, 1.000000000000000000, 1.000000000000000444, 1.000000000000000000, 1.000000000000000444, 1.000000000000000000, 1.000000000000000444, 1.000000000000000222, 1.000000000000000444, 1.000000000000000222, 1.000000000000000444, 0.9999999999999997780, 1.000000000000000444, 1.000000000000000000, 1.000000000000000444, 1.000000000000000222, 1.000000000000000222, 1.000000000000000222, 1.000000000000000222, 1.000000000000000444, 0.9999999999999997780, 1.000000000000000444, 1.000000000000000000, 1.000000000000000000, 1.000000000000000222, 1.000000000000000222, 1.000000000000000666, 0.9999999999999997780, 1.000000000000000000, 1.000000000000000444, 1.000000000000000222, 1.000000000000000444, 1.000000000000000000, 1.000000000000000222, 1.000000000000000444, 1.000000000000000222, 1.000000000000000000, 1.000000000000000444, 1.000000000000000222, 1.000000000000000222, 1.000000000000000444, 1.000000000000000222, 1.000000000000000000, 1.000000000000000444, 1.000000000000000000, 1.000000000000000444, 1.000000000000000222, 1.000000000000000222, 1.000000000000000444, 0.9999999999999997780, 1.000000000000000444, 0.9999999999999997780, 1.000000000000000444, 1.000000000000000222, 1.000000000000000444, 1.000000000000000222, 1.000000000000000222, 1.000000000000000444, 1.000000000000000000, 1.000000000000000222, 1.000000000000000444, 1.000000000000000000, 1.000000000000000444, 1.000000000000000000, 1.000000000000000222, 1.000000000000000444, 1.000000000000000000, 1.000000000000000444, 0.9999999999999997780, 1.000000000000000444, 1.000000000000000222, 1.000000000000000444, 1.000000000000000000, 1.000000000000000000, 1.000000000000000444, 1.000000000000000000, 1.000000000000000222, 1.000000000000000444, 1.000000000000000222, 1.000000000000000444, 1.000000000000000222, 1.000000000000000444, 1.000000000000000444, 1.000000000000000444, 1.000000000000000000, 1.000000000000000444, 1.000000000000000222, 1.000000000000000444, 1.000000000000000222, 1.000000000000000000, 1.000000000000000222, 1.000000000000000444, 1.000000000000000222, 1.000000000000000444, 1.000000000000000000, 1.000000000000000222, 1.000000000000000000, 1.000000000000000444, 1.000000000000000000, 1.000000000000000444, 1.000000000000000444, 1.000000000000000444, 1.000000000000000444, 1.000000000000000000, 1.000000000000000222, 1.000000000000000444, 1.000000000000000000, 1.000000000000000444, 1.000000000000000444, 1.000000000000000444, 1.000000000000000222, 1.000000000000000222, 1.000000000000000222, 0.9999999999999997780, 1.000000000000000444, 1.000000000000000222, 1.000000000000000222, 1.000000000000000000, 1.000000000000000444, 1.000000000000000000, 1.000000000000000444, 1.000000000000000000, 1.000000000000000000, 1.000000000000000666, 1.000000000000000000, 1.000000000000000444, 1.000000000000000000, 1.000000000000000444, 1.000000000000000222, 0.9999999999999997780, 1.000000000000000444, 1.000000000000000000, 1.000000000000000444, 1.000000000000000222, 1.000000000000000444, 1.000000000000000222, 1.000000000000000222, 1.000000000000000444, 1.000000000000000000, 1.000000000000000222, 1.000000000000000444, 1.000000000000000222, 1.000000000000000000, 1.000000000000000444, 0.9999999999999997780, 1.000000000000000444, 1.000000000000000222, 1.000000000000000222, 1.000000000000000222, 1.000000000000000000, 1.000000000000000444, 1.000000000000000222, 1.000000000000000666, 0.9999999999999997780, 1.000000000000000444, 1.000000000000000222, 1.000000000000000000, 1.000000000000000222, 1.000000000000000444, 1.000000000000000222, 1.000000000000000000, 1.000000000000000444, 1.000000000000000222, 1.000000000000000444, 1.000000000000000000, 1.000000000000000444, 1.000000000000000222, 1.000000000000000444, 1.000000000000000222, 1.000000000000000222, 1.000000000000000444, 1.000000000000000222, 1.000000000000000444, 1.000000000000000000, 1.000000000000000444, 1.000000000000000222, 1.000000000000000222, 1.000000000000000000, 1.000000000000000666, 0.9999999999999997780, 1.000000000000000444, 1.000000000000000222, 1.000000000000000444, 1.000000000000000222, 1.000000000000000444, 1.000000000000000000, 1.000000000000000444, 1.000000000000000222, 1.000000000000000222, 1.000000000000000444, 1.000000000000000222, 1.000000000000000444, 1.000000000000000000, 1.000000000000000444, 1.000000000000000444, 0.9999999999999997780, 1.000000000000000444, 1.000000000000000000, 1.000000000000000444, 1.000000000000000444, 1.000000000000000222, 1.000000000000000000, 1.000000000000000444, 1.000000000000000222, 1.000000000000000444, 1.000000000000000000, 1.000000000000000444, 1.000000000000000222, 1.000000000000000444, 1.000000000000000222, 1.000000000000000444, 1.000000000000000222, 1.000000000000000222, 1.000000000000000444, 1.000000000000000444, 1.000000000000000000, 1.000000000000000444, 0.9999999999999997780, 1.000000000000000444, 1.000000000000000222, 1.000000000000000222, 1.000000000000000222, 1.000000000000000444, 1.000000000000000222, 1.000000000000000222, 1.000000000000000444, 1.000000000000000000, 1.000000000000000444, 1.000000000000000000, 1.000000000000000444, 1.000000000000000222, 1.000000000000000000, 1.000000000000000222, 1.000000000000000444, 1.000000000000000000, 1.000000000000000444, 1.000000000000000000, 1.000000000000000444, 1.000000000000000444, 1.000000000000000000, 1.000000000000000444, 1.000000000000000000, 1.000000000000000444, 1.000000000000000000, 1.000000000000000444, 1.000000000000000000, 1.000000000000000444, 1.000000000000000000, 1.000000000000000444, 1.000000000000000000, 1.000000000000000444, 1.000000000000000222, 1.000000000000000222, 1.000000000000000222, 1.000000000000000222),
 ( 0.3333333333333334259, 0.3333333333333334259, 0.3333333333333333703, 0.3333333333333334259, 0.3333333333333334814, 0.3333333333333333148, 0.3333333333333335924, 0.3333333333333333148, 0.3333333333333334259, 0.3333333333333333703, 0.3333333333333334814, 0.3333333333333334814, 0.3333333333333333148, 0.3333333333333334814, 0.3333333333333333703, 0.3333333333333334259, 0.3333333333333334259, 0.3333333333333333703, 0.3333333333333334814, 0.3333333333333334259, 0.3333333333333335369, 0.3333333333333333148, 0.3333333333333335369, 0.3333333333333333703, 0.3333333333333333703, 0.3333333333333334259, 0.3333333333333334814, 0.3333333333333334814, 0.3333333333333333148, 0.3333333333333335369, 0.3333333333333335924, 0.3333333333333334259, 0.3333333333333333703, 0.3333333333333335369, 0.3333333333333334259, 0.3333333333333334259, 0.3333333333333334814, 0.3333333333333335369, 0.3333333333333333703, 0.3333333333333334259, 0.3333333333333335369, 0.3333333333333333148, 0.3333333333333334259, 0.3333333333333335369, 0.3333333333333333703, 0.3333333333333334259, 0.3333333333333333703, 0.3333333333333335369, 0.3333333333333333703, 0.3333333333333334814, 0.3333333333333333703, 0.3333333333333334259, 0.3333333333333333703, 0.3333333333333333703, 0.3333333333333334259, 0.3333333333333333703, 0.3333333333333334259, 0.3333333333333333148, 0.3333333333333336479, 0.3333333333333334259, 0.3333333333333334814, 0.3333333333333333703, 0.3333333333333335369, 0.3333333333333334259, 0.3333333333333334259, 0.3333333333333334259, 0.3333333333333334259, 0.3333333333333333703, 0.3333333333333333703, 0.3333333333333335369, 0.3333333333333333703, 0.3333333333333335369, 0.3333333333333334259, 0.3333333333333333703, 0.3333333333333334814, 0.3333333333333334259, 0.3333333333333333703, 0.3333333333333333148, 0.3333333333333335369, 0.3333333333333333703, 0.3333333333333335369, 0.3333333333333333703, 0.3333333333333334814, 0.3333333333333333703, 0.3333333333333334259, 0.3333333333333333148, 0.3333333333333335369, 0.3333333333333333703, 0.3333333333333334814, 0.3333333333333333148, 0.3333333333333334814, 0.3333333333333334259, 0.3333333333333335369, 0.3333333333333334259, 0.3333333333333334814, 0.3333333333333334259, 0.3333333333333334259, 0.3333333333333334259, 0.3333333333333334259, 0.3333333333333333703, 0.3333333333333333703, 0.3333333333333334814, 0.3333333333333333703, 0.3333333333333333703, 0.3333333333333335369, 0.3333333333333332593, 0.3333333333333335369, 0.3333333333333332593, 0.3333333333333335924, 0.3333333333333334259, 0.3333333333333334814, 0.3333333333333333703, 0.3333333333333334814, 0.3333333333333334259, 0.3333333333333334259, 0.3333333333333334814, 0.3333333333333333703, 0.3333333333333333703, 0.3333333333333334814, 0.3333333333333333703, 0.3333333333333334814, 0.3333333333333333703, 0.3333333333333334259, 0.3333333333333334259, 0.3333333333333335369, 0.3333333333333333703, 0.3333333333333335369, 0.3333333333333334259, 0.3333333333333335369, 0.3333333333333334259, 0.3333333333333334259, 0.3333333333333334814, 0.3333333333333334814, 0.3333333333333333703, 0.3333333333333334814, 0.3333333333333333148, 0.3333333333333335369, 0.3333333333333333148, 0.3333333333333335369, 0.3333333333333334259, 0.3333333333333334259, 0.3333333333333334814, 0.3333333333333334814, 0.3333333333333333703, 0.3333333333333335369, 0.3333333333333333703, 0.3333333333333334259, 0.3333333333333334814, 0.3333333333333334814, 0.3333333333333334259, 0.3333333333333334259, 0.3333333333333335369, 0.3333333333333333148, 0.3333333333333335924, 0.3333333333333333703, 0.3333333333333333703, 0.3333333333333335369, 0.3333333333333333703, 0.3333333333333335924, 0.3333333333333333148, 0.3333333333333333703, 0.3333333333333334814, 0.3333333333333333703, 0.3333333333333335369, 0.3333333333333333703, 0.3333333333333334259, 0.3333333333333334814, 0.3333333333333333703, 0.3333333333333334259, 0.3333333333333334259, 0.3333333333333334259, 0.3333333333333334814, 0.3333333333333333703, 0.3333333333333334259, 0.3333333333333333703, 0.3333333333333335369, 0.3333333333333333703, 0.3333333333333334259, 0.3333333333333334259, 0.3333333333333333703, 0.3333333333333334814, 0.3333333333333333703, 0.3333333333333334259, 0.3333333333333333703, 0.3333333333333334814, 0.3333333333333335369, 0.3333333333333334259, 0.3333333333333334259, 0.3333333333333333703, 0.3333333333333335369, 0.3333333333333333703, 0.3333333333333333703, 0.3333333333333335369, 0.3333333333333333703, 0.3333333333333335924, 0.3333333333333332593, 0.3333333333333335369, 0.3333333333333334259, 0.3333333333333333703, 0.3333333333333335369, 0.3333333333333333703, 0.3333333333333333703, 0.3333333333333334259, 0.3333333333333335369, 0.3333333333333333148, 0.3333333333333333703, 0.3333333333333335369, 0.3333333333333334259, 0.3333333333333333703, 0.3333333333333335369, 0.3333333333333333703, 0.3333333333333335924, 0.3333333333333333703, 0.3333333333333335369, 0.3333333333333334259, 0.3333333333333334814, 0.3333333333333334259, 0.3333333333333334259, 0.3333333333333334814, 0.3333333333333334259, 0.3333333333333334259, 0.3333333333333333148, 0.3333333333333333703, 0.3333333333333334814, 0.3333333333333334814, 0.3333333333333334259, 0.3333333333333333703, 0.3333333333333334259, 0.3333333333333333148, 0.3333333333333335369, 0.3333333333333333703, 0.3333333333333334814, 0.3333333333333335369, 0.3333333333333335369, 0.3333333333333335369, 0.3333333333333333703, 0.3333333333333334259, 0.3333333333333334259, 0.3333333333333333148, 0.3333333333333335369, 0.3333333333333334259, 0.3333333333333334259, 0.3333333333333334259, 0.3333333333333334814, 0.3333333333333334259, 0.3333333333333333148, 0.3333333333333334814, 0.3333333333333334259, 0.3333333333333333703, 0.3333333333333333703, 0.3333333333333334814, 0.3333333333333333703, 0.3333333333333334814, 0.3333333333333334814, 0.3333333333333333148, 0.3333333333333335924, 0.3333333333333333148, 0.3333333333333335369, 0.3333333333333333148, 0.3333333333333335924, 0.3333333333333333703, 0.3333333333333333148, 0.3333333333333334259, 0.3333333333333334259, 0.3333333333333334259, 0.3333333333333333703, 0.3333333333333334814, 0.3333333333333333703, 0.3333333333333334814, 0.3333333333333334814, 0.3333333333333333703, 0.3333333333333334259, 0.3333333333333334259, 0.3333333333333334814, 0.3333333333333333703, 0.3333333333333333703, 0.3333333333333334259, 0.3333333333333334259, 0.3333333333333333703, 0.3333333333333334259, 0.3333333333333333703, 0.3333333333333334259, 0.3333333333333334259, 0.3333333333333333703, 0.3333333333333335924, 0.3333333333333332593, 0.3333333333333335369, 0.3333333333333334259, 0.3333333333333333703, 0.3333333333333333148, 0.3333333333333335924, 0.3333333333333333148, 0.3333333333333333703, 0.3333333333333334259, 0.3333333333333334814, 0.3333333333333335369, 0.3333333333333333703, 0.3333333333333334259, 0.3333333333333333703, 0.3333333333333335369, 0.3333333333333333703, 0.3333333333333334259, 0.3333333333333334814, 0.3333333333333333703, 0.3333333333333335369, 0.3333333333333333148, 0.3333333333333335369, 0.3333333333333334259, 0.3333333333333334259, 0.3333333333333333703, 0.3333333333333335369, 0.3333333333333333703, 0.3333333333333335369, 0.3333333333333334814, 0.3333333333333333703, 0.3333333333333334814, 0.3333333333333333703, 0.3333333333333333703, 0.3333333333333335369, 0.3333333333333333703, 0.3333333333333334259, 0.3333333333333334814, 0.3333333333333333703, 0.3333333333333334259, 0.3333333333333333148, 0.3333333333333335369, 0.3333333333333334259, 0.3333333333333333703, 0.3333333333333334814, 0.3333333333333334259, 0.3333333333333334814, 0.3333333333333334259, 0.3333333333333333703, 0.3333333333333333703, 0.3333333333333334259, 0.3333333333333334259, 0.3333333333333334259, 0.3333333333333334259, 0.3333333333333333703, 0.3333333333333334814, 0.3333333333333334814, 0.3333333333333333703, 0.3333333333333335369, 0.3333333333333333703, 0.3333333333333334814, 0.3333333333333334814, 0.3333333333333335369, 0.3333333333333333148, 0.3333333333333335369, 0.3333333333333333703, 0.3333333333333333148, 0.3333333333333334814, 0.3333333333333333703, 0.3333333333333334814, 0.3333333333333333703, 0.3333333333333334814, 0.3333333333333333703, 0.3333333333333335369, 0.3333333333333333703, 0.3333333333333334814, 0.3333333333333334259, 0.3333333333333334814, 0.3333333333333334259, 0.3333333333333333703, 0.3333333333333333703, 0.3333333333333334814, 0.3333333333333334259, 0.3333333333333334814, 0.3333333333333334259, 0.3333333333333334259, 0.3333333333333334259, 0.3333333333333333703, 0.3333333333333334259, 0.3333333333333333703, 0.3333333333333334814, 0.3333333333333333148, 0.3333333333333335369, 0.3333333333333333703, 0.3333333333333334814, 0.3333333333333333703, 0.3333333333333335369, 0.3333333333333334259, 0.3333333333333334259, 0.3333333333333334259, 0.3333333333333334259, 0.3333333333333334259, 0.3333333333333334259),
 ( 0.3333333333333334259, 0.3333333333333334259, 0.3333333333333333703, 0.3333333333333334259, 0.3333333333333334814, 0.3333333333333333148, 0.3333333333333335924, 0.3333333333333333148, 0.3333333333333334259, 0.3333333333333333703, 0.3333333333333334814, 0.3333333333333334814, 0.3333333333333333148, 0.3333333333333334814, 0.3333333333333333703, 0.3333333333333334259, 0.3333333333333334259, 0.3333333333333333703, 0.3333333333333334814, 0.3333333333333334259, 0.3333333333333335369, 0.3333333333333333148, 0.3333333333333335369, 0.3333333333333333703, 0.3333333333333333703, 0.3333333333333334259, 0.3333333333333334814, 0.3333333333333334814, 0.3333333333333333148, 0.3333333333333335369, 0.3333333333333335924, 0.3333333333333334259, 0.3333333333333333703, 0.3333333333333335369, 0.3333333333333334259, 0.3333333333333334259, 0.3333333333333334814, 0.3333333333333335369, 0.3333333333333333703, 0.3333333333333334259, 0.3333333333333335369, 0.3333333333333333148, 0.3333333333333334259, 0.3333333333333335369, 0.3333333333333333703, 0.3333333333333334259, 0.3333333333333333703, 0.3333333333333335369, 0.3333333333333333703, 0.3333333333333334814, 0.3333333333333333703, 0.3333333333333334259, 0.3333333333333333703, 0.3333333333333333703, 0.3333333333333334259, 0.3333333333333333703, 0.3333333333333334259, 0.3333333333333333148, 0.3333333333333336479, 0.3333333333333334259, 0.3333333333333334814, 0.3333333333333333703, 0.3333333333333335369, 0.3333333333333334259, 0.3333333333333334259, 0.3333333333333334259, 0.3333333333333334259, 0.3333333333333333703, 0.3333333333333333703, 0.3333333333333335369, 0.3333333333333333703, 0.3333333333333335369, 0.3333333333333334259, 0.3333333333333333703, 0.3333333333333334814, 0.3333333333333334259, 0.3333333333333333703, 0.3333333333333333148, 0.3333333333333335369, 0.3333333333333333703, 0.3333333333333335369, 0.3333333333333333703, 0.3333333333333334814, 0.3333333333333333703, 0.3333333333333334259, 0.3333333333333333148, 0.3333333333333335369, 0.3333333333333333703, 0.3333333333333334814, 0.3333333333333333148, 0.3333333333333334814, 0.3333333333333334259, 0.3333333333333335369, 0.3333333333333334259, 0.3333333333333334814, 0.3333333333333334259, 0.3333333333333334259, 0.3333333333333334259, 0.3333333333333334259, 0.3333333333333333703, 0.3333333333333333703, 0.3333333333333334814, 0.3333333333333333703, 0.3333333333333333703, 0.3333333333333335369, 0.3333333333333332593, 0.3333333333333335369, 0.3333333333333332593, 0.3333333333333335924, 0.3333333333333334259, 0.3333333333333334814, 0.3333333333333333703, 0.3333333333333334814, 0.3333333333333334259, 0.3333333333333334259, 0.3333333333333334814, 0.3333333333333333703, 0.3333333333333333703, 0.3333333333333334814, 0.3333333333333333703, 0.3333333333333334814, 0.3333333333333333703, 0.3333333333333334259, 0.3333333333333334259, 0.3333333333333335369, 0.3333333333333333703, 0.3333333333333335369, 0.3333333333333334259, 0.3333333333333335369, 0.3333333333333334259, 0.3333333333333334259, 0.3333333333333334814, 0.3333333333333334814, 0.3333333333333333703, 0.3333333333333334814, 0.3333333333333333148, 0.3333333333333335369, 0.3333333333333333148, 0.3333333333333335369, 0.3333333333333334259, 0.3333333333333334259, 0.3333333333333334814, 0.3333333333333334814, 0.3333333333333333703, 0.3333333333333335369, 0.3333333333333333703, 0.3333333333333334259, 0.3333333333333334814, 0.3333333333333334814, 0.3333333333333334259, 0.3333333333333334259, 0.3333333333333335369, 0.3333333333333333148, 0.3333333333333335924, 0.3333333333333333703, 0.3333333333333333703, 0.3333333333333335369, 0.3333333333333333703, 0.3333333333333335924, 0.3333333333333333148, 0.3333333333333333703, 0.3333333333333334814, 0.3333333333333333703, 0.3333333333333335369, 0.3333333333333333703, 0.3333333333333334259, 0.3333333333333334814, 0.3333333333333333703, 0.3333333333333334259, 0.3333333333333334259, 0.3333333333333334259, 0.3333333333333334814, 0.3333333333333333703, 0.3333333333333334259, 0.3333333333333333703, 0.3333333333333335369, 0.3333333333333333703, 0.3333333333333334259, 0.3333333333333334259, 0.3333333333333333703, 0.3333333333333334814, 0.3333333333333333703, 0.3333333333333334259, 0.3333333333333333703, 0.3333333333333334814, 0.3333333333333335369, 0.3333333333333334259, 0.3333333333333334259, 0.3333333333333333703, 0.3333333333333335369, 0.3333333333333333703, 0.3333333333333333703, 0.3333333333333335369, 0.3333333333333333703, 0.3333333333333335924, 0.3333333333333332593, 0.3333333333333335369, 0.3333333333333334259, 0.3333333333333333703, 0.3333333333333335369, 0.3333333333333333703, 0.3333333333333333703, 0.3333333333333334259, 0.3333333333333335369, 0.3333333333333333148, 0.3333333333333333703, 0.3333333333333335369, 0.3333333333333334259, 0.3333333333333333703, 0.3333333333333335369, 0.3333333333333333703, 0.3333333333333335924, 0.3333333333333333703, 0.3333333333333335369, 0.3333333333333334259, 0.3333333333333334814, 0.3333333333333334259, 0.3333333333333334259, 0.3333333333333334814, 0.3333333333333334259, 0.3333333333333334259, 0.3333333333333333148, 0.3333333333333333703, 0.3333333333333334814, 0.3333333333333334814, 0.3333333333333334259, 0.3333333333333333703, 0.3333333333333334259, 0.3333333333333333148, 0.3333333333333335369, 0.3333333333333333703, 0.3333333333333334814, 0.3333333333333335369, 0.3333333333333335369, 0.3333333333333335369, 0.3333333333333333703, 0.3333333333333334259, 0.3333333333333334259, 0.3333333333333333148, 0.3333333333333335369, 0.3333333333333334259, 0.3333333333333334259, 0.3333333333333334259, 0.3333333333333334814, 0.3333333333333334259, 0.3333333333333333148, 0.3333333333333334814, 0.3333333333333334259, 0.3333333333333333703, 0.3333333333333333703, 0.3333333333333334814, 0.3333333333333333703, 0.3333333333333334814, 0.3333333333333334814, 0.3333333333333333148, 0.3333333333333335924, 0.3333333333333333148, 0.3333333333333335369, 0.3333333333333333148, 0.3333333333333335924, 0.3333333333333333703, 0.3333333333333333148, 0.3333333333333334259, 0.3333333333333334259, 0.3333333333333334259, 0.3333333333333333703, 0.3333333333333334814, 0.3333333333333333703, 0.3333333333333334814, 0.3333333333333334814, 0.3333333333333333703, 0.3333333333333334259, 0.3333333333333334259, 0.3333333333333334814, 0.3333333333333333703, 0.3333333333333333703, 0.3333333333333334259, 0.3333333333333334259, 0.3333333333333333703, 0.3333333333333334259, 0.3333333333333333703, 0.3333333333333334259, 0.3333333333333334259, 0.3333333333333333703, 0.3333333333333335924, 0.3333333333333332593, 0.3333333333333335369, 0.3333333333333334259, 0.3333333333333333703, 0.3333333333333333148, 0.3333333333333335924, 0.3333333333333333148, 0.3333333333333333703, 0.3333333333333334259, 0.3333333333333334814, 0.3333333333333335369, 0.3333333333333333703, 0.3333333333333334259, 0.3333333333333333703, 0.3333333333333335369, 0.3333333333333333703, 0.3333333333333334259, 0.3333333333333334814, 0.3333333333333333703, 0.3333333333333335369, 0.3333333333333333148, 0.3333333333333335369, 0.3333333333333334259, 0.3333333333333334259, 0.3333333333333333703, 0.3333333333333335369, 0.3333333333333333703, 0.3333333333333335369, 0.3333333333333334814, 0.3333333333333333703, 0.3333333333333334814, 0.3333333333333333703, 0.3333333333333333703, 0.3333333333333335369, 0.3333333333333333703, 0.3333333333333334259, 0.3333333333333334814, 0.3333333333333333703, 0.3333333333333334259, 0.3333333333333333148, 0.3333333333333335369, 0.3333333333333334259, 0.3333333333333333703, 0.3333333333333334814, 0.3333333333333334259, 0.3333333333333334814, 0.3333333333333334259, 0.3333333333333333703, 0.3333333333333333703, 0.3333333333333334259, 0.3333333333333334259, 0.3333333333333334259, 0.3333333333333334259, 0.3333333333333333703, 0.3333333333333334814, 0.3333333333333334814, 0.3333333333333333703, 0.3333333333333335369, 0.3333333333333333703, 0.3333333333333334814, 0.3333333333333334814, 0.3333333333333335369, 0.3333333333333333148, 0.3333333333333335369, 0.3333333333333333703, 0.3333333333333333148, 0.3333333333333334814, 0.3333333333333333703, 0.3333333333333334814, 0.3333333333333333703, 0.3333333333333334814, 0.3333333333333333703, 0.3333333333333335369, 0.3333333333333333703, 0.3333333333333334814, 0.3333333333333334259, 0.3333333333333334814, 0.3333333333333334259, 0.3333333333333333703, 0.3333333333333333703, 0.3333333333333334814, 0.3333333333333334259, 0.3333333333333334814, 0.3333333333333334259, 0.3333333333333334259, 0.3333333333333334259, 0.3333333333333333703, 0.3333333333333334259, 0.3333333333333333703, 0.3333333333333334814, 0.3333333333333333148, 0.3333333333333335369, 0.3333333333333333703, 0.3333333333333334814, 0.3333333333333333703, 0.3333333333333335369, 0.3333333333333334259, 0.3333333333333334259, 0.3333333333333334259, 0.3333333333333334259, 0.3333333333333334259, 0.3333333333333334259),
 ( 1.000000000000000222, 1.000000000000000222, 1.000000000000000222, 1.000000000000000222, 1.000000000000000444, 1.000000000000000000, 1.000000000000000666, 0.9999999999999997780, 1.000000000000000444, 1.000000000000000000, 1.000000000000000444, 1.000000000000000444, 1.000000000000000000, 1.000000000000000444, 1.000000000000000000, 1.000000000000000444, 1.000000000000000222, 1.000000000000000222, 1.000000000000000222, 1.000000000000000444, 1.000000000000000444, 1.000000000000000000, 1.000000000000000444, 1.000000000000000000, 1.000000000000000222, 1.000000000000000222, 1.000000000000000444, 1.000000000000000222, 1.000000000000000222, 1.000000000000000444, 1.000000000000000444, 1.000000000000000444, 1.000000000000000000, 1.000000000000000444, 1.000000000000000444, 1.000000000000000000, 1.000000000000000444, 1.000000000000000444, 1.000000000000000000, 1.000000000000000444, 1.000000000000000444, 1.000000000000000000, 1.000000000000000222, 1.000000000000000444, 1.000000000000000222, 1.000000000000000222, 1.000000000000000000, 1.000000000000000444, 1.000000000000000222, 1.000000000000000222, 1.000000000000000222, 1.000000000000000222, 1.000000000000000222, 1.000000000000000222, 1.000000000000000444, 1.000000000000000000, 1.000000000000000444, 0.9999999999999997780, 1.000000000000000666, 1.000000000000000444, 1.000000000000000444, 1.000000000000000000, 1.000000000000000444, 1.000000000000000222, 1.000000000000000222, 1.000000000000000444, 1.000000000000000222, 1.000000000000000444, 1.000000000000000000, 1.000000000000000444, 1.000000000000000222, 1.000000000000000444, 1.000000000000000444, 1.000000000000000222, 1.000000000000000222, 1.000000000000000222, 1.000000000000000444, 0.9999999999999997780, 1.000000000000000444, 1.000000000000000000, 1.000000000000000444, 1.000000000000000000, 1.000000000000000444, 0.9999999999999997780, 1.000000000000000444, 0.9999999999999997780, 1.000000000000000444, 1.000000000000000222, 1.000000000000000444, 1.000000000000000000, 1.000000000000000222, 1.000000000000000444, 1.000000000000000444, 1.000000000000000222, 1.000000000000000444, 1.000000000000000444, 1.000000000000000222, 1.000000000000000222, 1.000000000000000222, 1.000000000000000222, 1.000000000000000000, 1.000000000000000222, 1.000000000000000222, 1.000000000000000222, 1.000000000000000444, 1.000000000000000000, 1.000000000000000444, 0.9999999999999997780, 1.000000000000000666, 1.000000000000000222, 1.000000000000000444, 1.000000000000000000, 1.000000000000000444, 1.000000000000000222, 1.000000000000000222, 1.000000000000000444, 1.000000000000000000, 1.000000000000000000, 1.000000000000000444, 1.000000000000000000, 1.000000000000000444, 1.000000000000000000, 1.000000000000000444, 1.000000000000000222, 1.000000000000000444, 1.000000000000000222, 1.000000000000000444, 1.000000000000000222, 1.000000000000000444, 1.000000000000000000, 1.000000000000000444, 1.000000000000000222, 1.000000000000000444, 1.000000000000000000, 1.000000000000000444, 1.000000000000000000, 1.000000000000000444, 1.000000000000000000, 1.000000000000000444, 1.000000000000000222, 1.000000000000000444, 1.000000000000000222, 1.000000000000000444, 0.9999999999999997780, 1.000000000000000444, 1.000000000000000000, 1.000000000000000444, 1.000000000000000222, 1.000000000000000222, 1.000000000000000222, 1.000000000000000222, 1.000000000000000444, 0.9999999999999997780, 1.000000000000000444, 1.000000000000000000, 1.000000000000000000, 1.000000000000000222, 1.000000000000000222, 1.000000000000000666, 0.9999999999999997780, 1.000000000000000000, 1.000000000000000444, 1.000000000000000222, 1.000000000000000444, 1.000000000000000000, 1.000000000000000222, 1.000000000000000444, 1.000000000000000222, 1.000000000000000000, 1.000000000000000444, 1.000000000000000222, 1.000000000000000222, 1.000000000000000444, 1.000000000000000222, 1.000000000000000000, 1.000000000000000444, 1.000000000000000000, 1.000000000000000444, 1.000000000000000222, 1.000000000000000222, 1.000000000000000444, 0.9999999999999997780, 1.000000000000000444, 0.9999999999999997780, 1.000000000000000444, 1.000000000000000222, 1.000000000000000444, 1.000000000000000222, 1.000000000000000222, 1.000000000000000444, 1.000000000000000000, 1.000000000000000222, 1.000000000000000444, 1.000000000000000000, 1.000000000000000444, 1.000000000000000000, 1.000000000000000222, 1.000000000000000444, 1.000000000000000000, 1.000000000000000444, 0.9999999999999997780, 1.000000000000000444, 1.000000000000000222, 1.000000000000000444, 1.000000000000000000, 1.000000000000000000, 1.000000000000000444, 1.000000000000000000, 1.000000000000000222, 1.000000000000000444, 1.000000000000000222, 1.000000000000000444, 1.000000000000000222, 1.000000000000000444, 1.000000000000000444, 1.000000000000000444, 1.000000000000000000, 1.000000000000000444, 1.000000000000000222, 1.000000000000000444, 1.000000000000000222, 1.000000000000000000, 1.000000000000000222, 1.000000000000000444, 1.000000000000000222, 1.000000000000000444, 1.000000000000000000, 1.000000000000000222, 1.000000000000000000, 1.000000000000000444, 1.000000000000000000, 1.000000000000000444, 1.000000000000000444, 1.000000000000000444, 1.000000000000000444, 1.000000000000000000, 1.000000000000000222, 1.000000000000000444, 1.000000000000000000, 1.000000000000000444, 1.000000000000000444, 1.000000000000000444, 1.000000000000000222, 1.000000000000000222, 1.000000000000000222, 0.9999999999999997780, 1.000000000000000444, 1.000000000000000222, 1.000000000000000222, 1.000000000000000000, 1.000000000000000444, 1.000000000000000000, 1.000000000000000444, 1.000000000000000000, 1.000000000000000000, 1.000000000000000666, 1.000000000000000000, 1.000000000000000444, 1.000000000000000000, 1.000000000000000444, 1.000000000000000222, 0.9999999999999997780, 1.000000000000000444, 1.000000000000000000, 1.000000000000000444, 1.000000000000000222, 1.000000000000000444, 1.000000000000000222, 1.000000000000000222, 1.000000000000000444, 1.000000000000000000, 1.000000000000000222, 1.000000000000000444, 1.000000000000000222, 1.000000000000000000, 1.000000000000000444, 0.9999999999999997780, 1.000000000000000444, 1.000000000000000222, 1.000000000000000222, 1.000000000000000222, 1.000000000000000000, 1.000000000000000444, 1.000000000000000222, 1.000000000000000666, 0.9999999999999997780, 1.000000000000000444, 1.000000000000000222, 1.000000000000000000, 1.000000000000000222, 1.000000000000000444, 1.000000000000000222, 1.000000000000000000, 1.000000000000000444, 1.000000000000000222, 1.000000000000000444, 1.000000000000000000, 1.000000000000000444, 1.000000000000000222, 1.000000000000000444, 1.000000000000000222, 1.000000000000000222, 1.000000000000000444, 1.000000000000000222, 1.000000000000000444, 1.000000000000000000, 1.000000000000000444, 1.000000000000000222, 1.000000000000000222, 1.000000000000000000, 1.000000000000000666, 0.9999999999999997780, 1.000000000000000444, 1.000000000000000222, 1.000000000000000444, 1.000000000000000222, 1.000000000000000444, 1.000000000000000000, 1.000000000000000444, 1.000000000000000222, 1.000000000000000222, 1.000000000000000444, 1.000000000000000222, 1.000000000000000444, 1.000000000000000000, 1.000000000000000444, 1.000000000000000444, 0.9999999999999997780, 1.000000000000000444, 1.000000000000000000, 1.000000000000000444, 1.000000000000000444, 1.000000000000000222, 1.000000000000000000, 1.000000000000000444, 1.000000000000000222, 1.000000000000000444, 1.000000000000000000, 1.000000000000000444, 1.000000000000000222, 1.000000000000000444, 1.000000000000000222, 1.000000000000000444, 1.000000000000000222, 1.000000000000000222, 1.000000000000000444, 1.000000000000000444, 1.000000000000000000, 1.000000000000000444, 0.9999999999999997780, 1.000000000000000444, 1.000000000000000222, 1.000000000000000222, 1.000000000000000222, 1.000000000000000444, 1.000000000000000222, 1.000000000000000222, 1.000000000000000444, 1.000000000000000000, 1.000000000000000444, 1.000000000000000000, 1.000000000000000444, 1.000000000000000222, 1.000000000000000000, 1.000000000000000222, 1.000000000000000444, 1.000000000000000000, 1.000000000000000444, 1.000000000000000000, 1.000000000000000444, 1.000000000000000444, 1.000000000000000000, 1.000000000000000444, 1.000000000000000000, 1.000000000000000444, 1.000000000000000000, 1.000000000000000444, 1.000000000000000000, 1.000000000000000444, 1.000000000000000000, 1.000000000000000444, 1.000000000000000000, 1.000000000000000444, 1.000000000000000222, 1.000000000000000222, 1.000000000000000222, 1.000000000000000222),
 ( 0.3333333333333334259, 0.3333333333333334259, 0.3333333333333333703, 0.3333333333333334259, 0.3333333333333334814, 0.3333333333333333148, 0.3333333333333335924, 0.3333333333333333148, 0.3333333333333334259, 0.3333333333333333703, 0.3333333333333334814, 0.3333333333333334814, 0.3333333333333333148, 0.3333333333333334814, 0.3333333333333333703, 0.3333333333333334259, 0.3333333333333334259, 0.3333333333333333703, 0.3333333333333334814, 0.3333333333333334259, 0.3333333333333335369, 0.3333333333333333148, 0.3333333333333335369, 0.3333333333333333703, 0.3333333333333333703, 0.3333333333333334259, 0.3333333333333334814, 0.3333333333333334814, 0.3333333333333333148, 0.3333333333333335369, 0.3333333333333335924, 0.3333333333333334259, 0.3333333333333333703, 0.3333333333333335369, 0.3333333333333334259, 0.3333333333333334259, 0.3333333333333334814, 0.3333333333333335369, 0.3333333333333333703, 0.3333333333333334259, 0.3333333333333335369, 0.3333333333333333148, 0.3333333333333334259, 0.3333333333333335369, 0.3333333333333333703, 0.3333333333333334259, 0.3333333333333333703, 0.3333333333333335369, 0.3333333333333333703, 0.3333333333333334814, 0.3333333333333333703, 0.3333333333333334259, 0.3333333333333333703, 0.3333333333333333703, 0.3333333333333334259, 0.3333333333333333703, 0.3333333333333334259, 0.3333333333333333148, 0.3333333333333336479, 0.3333333333333334259, 0.3333333333333334814, 0.3333333333333333703, 0.3333333333333335369, 0.3333333333333334259, 0.3333333333333334259, 0.3333333333333334259, 0.3333333333333334259, 0.3333333333333333703, 0.3333333333333333703, 0.3333333333333335369, 0.3333333333333333703, 0.3333333333333335369, 0.3333333333333334259, 0.3333333333333333703, 0.3333333333333334814, 0.3333333333333334259, 0.3333333333333333703, 0.3333333333333333148, 0.3333333333333335369, 0.3333333333333333703, 0.3333333333333335369, 0.3333333333333333703, 0.3333333333333334814, 0.3333333333333333703, 0.3333333333333334259, 0.3333333333333333148, 0.3333333333333335369, 0.3333333333333333703, 0.3333333333333334814, 0.3333333333333333148, 0.3333333333333334814, 0.3333333333333334259, 0.3333333333333335369, 0.3333333333333334259, 0.3333333333333334814, 0.3333333333333334259, 0.3333333333333334259, 0.3333333333333334259, 0.3333333333333334259, 0.3333333333333333703, 0.3333333333333333703, 0.3333333333333334814, 0.3333333333333333703, 0.3333333333333333703, 0.3333333333333335369, 0.3333333333333332593, 0.3333333333333335369, 0.3333333333333332593, 0.3333333333333335924, 0.3333333333333334259, 0.3333333333333334814, 0.3333333333333333703, 0.3333333333333334814, 0.3333333333333334259, 0.3333333333333334259, 0.3333333333333334814, 0.3333333333333333703, 0.3333333333333333703, 0.3333333333333334814, 0.3333333333333333703, 0.3333333333333334814, 0.3333333333333333703, 0.3333333333333334259, 0.3333333333333334259, 0.3333333333333335369, 0.3333333333333333703, 0.3333333333333335369, 0.3333333333333334259, 0.3333333333333335369, 0.3333333333333334259, 0.3333333333333334259, 0.3333333333333334814, 0.3333333333333334814, 0.3333333333333333703, 0.3333333333333334814, 0.3333333333333333148, 0.3333333333333335369, 0.3333333333333333148, 0.3333333333333335369, 0.3333333333333334259, 0.3333333333333334259, 0.3333333333333334814, 0.3333333333333334814, 0.3333333333333333703, 0.3333333333333335369, 0.3333333333333333703, 0.3333333333333334259, 0.3333333333333334814, 0.3333333333333334814, 0.3333333333333334259, 0.3333333333333334259, 0.3333333333333335369, 0.3333333333333333148, 0.3333333333333335924, 0.3333333333333333703, 0.3333333333333333703, 0.3333333333333335369, 0.3333333333333333703, 0.3333333333333335924, 0.3333333333333333148, 0.3333333333333333703, 0.3333333333333334814, 0.3333333333333333703, 0.3333333333333335369, 0.3333333333333333703, 0.3333333333333334259, 0.3333333333333334814, 0.3333333333333333703, 0.3333333333333334259, 0.3333333333333334259, 0.3333333333333334259, 0.3333333333333334814, 0.3333333333333333703, 0.3333333333333334259, 0.3333333333333333703, 0.3333333333333335369, 0.3333333333333333703, 0.3333333333333334259, 0.3333333333333334259, 0.3333333333333333703, 0.3333333333333334814, 0.3333333333333333703, 0.3333333333333334259, 0.3333333333333333703, 0.3333333333333334814, 0.3333333333333335369, 0.3333333333333334259, 0.3333333333333334259, 0.3333333333333333703, 0.3333333333333335369, 0.3333333333333333703, 0.3333333333333333703, 0.3333333333333335369, 0.3333333333333333703, 0.3333333333333335924, 0.3333333333333332593, 0.3333333333333335369, 0.3333333333333334259, 0.3333333333333333703, 0.3333333333333335369, 0.3333333333333333703, 0.3333333333333333703, 0.3333333333333334259, 0.3333333333333335369, 0.3333333333333333148, 0.3333333333333333703, 0.3333333333333335369, 0.3333333333333334259, 0.3333333333333333703, 0.3333333333333335369, 0.3333333333333333703, 0.3333333333333335924, 0.3333333333333333703, 0.3333333333333335369, 0.3333333333333334259, 0.3333333333333334814, 0.3333333333333334259, 0.3333333333333334259, 0.3333333333333334814, 0.3333333333333334259, 0.3333333333333334259, 0.3333333333333333148, 0.3333333333333333703, 0.3333333333333334814, 0.3333333333333334814, 0.3333333333333334259, 0.3333333333333333703, 0.3333333333333334259, 0.3333333333333333148, 0.3333333333333335369, 0.3333333333333333703, 0.3333333333333334814, 0.3333333333333335369, 0.3333333333333335369, 0.3333333333333335369, 0.3333333333333333703, 0.3333333333333334259, 0.3333333333333334259, 0.3333333333333333148, 0.3333333333333335369, 0.3333333333333334259, 0.3333333333333334259, 0.3333333333333334259, 0.3333333333333334814, 0.3333333333333334259, 0.3333333333333333148, 0.3333333333333334814, 0.3333333333333334259, 0.3333333333333333703, 0.3333333333333333703, 0.3333333333333334814, 0.3333333333333333703, 0.3333333333333334814, 0.3333333333333334814, 0.3333333333333333148, 0.3333333333333335924, 0.3333333333333333148, 0.3333333333333335369, 0.3333333333333333148, 0.3333333333333335924, 0.3333333333333333703, 0.3333333333333333148, 0.3333333333333334259, 0.3333333333333334259, 0.3333333333333334259, 0.3333333333333333703, 0.3333333333333334814, 0.3333333333333333703, 0.3333333333333334814, 0.3333333333333334814, 0.3333333333333333703, 0.3333333333333334259, 0.3333333333333334259, 0.3333333333333334814, 0.3333333333333333703, 0.3333333333333333703, 0.3333333333333334259, 0.3333333333333334259, 0.3333333333333333703, 0.3333333333333334259, 0.3333333333333333703, 0.3333333333333334259, 0.3333333333333334259, 0.3333333333333333703, 0.3333333333333335924, 0.3333333333333332593, 0.3333333333333335369, 0.3333333333333334259, 0.3333333333333333703, 0.3333333333333333148, 0.3333333333333335924, 0.3333333333333333148, 0.3333333333333333703, 0.3333333333333334259, 0.3333333333333334814, 0.3333333333333335369, 0.3333333333333333703, 0.3333333333333334259, 0.3333333333333333703, 0.3333333333333335369, 0.3333333333333333703, 0.3333333333333334259, 0.3333333333333334814, 0.3333333333333333703, 0.3333333333333335369, 0.3333333333333333148, 0.3333333333333335369, 0.3333333333333334259, 0.3333333333333334259, 0.3333333333333333703, 0.3333333333333335369, 0.3333333333333333703, 0.3333333333333335369, 0.3333333333333334814, 0.3333333333333333703, 0.3333333333333334814, 0.3333333333333333703, 0.3333333333333333703, 0.3333333333333335369, 0.3333333333333333703, 0.3333333333333334259, 0.3333333333333334814, 0.3333333333333333703, 0.3333333333333334259, 0.3333333333333333148, 0.3333333333333335369, 0.3333333333333334259, 0.3333333333333333703, 0.3333333333333334814, 0.3333333333333334259, 0.3333333333333334814, 0.3333333333333334259, 0.3333333333333333703, 0.3333333333333333703, 0.3333333333333334259, 0.3333333333333334259, 0.3333333333333334259, 0.3333333333333334259, 0.3333333333333333703, 0.3333333333333334814, 0.3333333333333334814, 0.3333333333333333703, 0.3333333333333335369, 0.3333333333333333703, 0.3333333333333334814, 0.3333333333333334814, 0.3333333333333335369, 0.3333333333333333148, 0.3333333333333335369, 0.3333333333333333703, 0.3333333333333333148, 0.3333333333333334814, 0.3333333333333333703, 0.3333333333333334814, 0.3333333333333333703, 0.3333333333333334814, 0.3333333333333333703, 0.3333333333333335369, 0.3333333333333333703, 0.3333333333333334814, 0.3333333333333334259, 0.3333333333333334814, 0.3333333333333334259, 0.3333333333333333703, 0.3333333333333333703, 0.3333333333333334814, 0.3333333333333334259, 0.3333333333333334814, 0.3333333333333334259, 0.3333333333333334259, 0.3333333333333334259, 0.3333333333333333703, 0.3333333333333334259, 0.3333333333333333703, 0.3333333333333334814, 0.3333333333333333148, 0.3333333333333335369, 0.3333333333333333703, 0.3333333333333334814, 0.3333333333333333703, 0.3333333333333335369, 0.3333333333333334259, 0.3333333333333334259, 0.3333333333333334259, 0.3333333333333334259, 0.3333333333333334259, 0.3333333333333334259),
 ( 0.3333333333333334259, 0.3333333333333334259, 0.3333333333333333703, 0.3333333333333334259, 0.3333333333333334814, 0.3333333333333333148, 0.3333333333333335924, 0.3333333333333333148, 0.3333333333333334259, 0.3333333333333333703, 0.3333333333333334814, 0.3333333333333334814, 0.3333333333333333148, 0.3333333333333334814, 0.3333333333333333703, 0.3333333333333334259, 0.3333333333333334259, 0.3333333333333333703, 0.3333333333333334814, 0.3333333333333334259, 0.3333333333333335369, 0.3333333333333333148, 0.3333333333333335369, 0.3333333333333333703, 0.3333333333333333703, 0.3333333333333334259, 0.3333333333333334814, 0.3333333333333334814, 0.3333333333333333148, 0.3333333333333335369, 0.3333333333333335924, 0.3333333333333334259, 0.3333333333333333703, 0.3333333333333335369, 0.3333333333333334259, 0.3333333333333334259, 0.3333333333333334814, 0.3333333333333335369, 0.3333333333333333703, 0.3333333333333334259, 0.3333333333333335369, 0.3333333333333333148, 0.3333333333333334259, 0.3333333333333335369, 0.3333333333333333703, 0.3333333333333334259, 0.3333333333333333703, 0.3333333333333335369, 0.3333333333333333703, 0.3333333333333334814, 0.3333333333333333703, 0.3333333333333334259, 0.3333333333333333703, 0.3333333333333333703, 0.3333333333333334259, 0.3333333333333333703, 0.3333333333333334259, 0.3333333333333333148, 0.3333333333333336479, 0.3333333333333334259, 0.3333333333333334814, 0.3333333333333333703, 0.3333333333333335369, 0.3333333333333334259, 0.3333333333333334259, 0.3333333333333334259, 0.3333333333333334259, 0.3333333333333333703, 0.3333333333333333703, 0.3333333333333335369, 0.3333333333333333703, 0.3333333333333335369, 0.3333333333333334259, 0.3333333333333333703, 0.3333333333333334814, 0.3333333333333334259, 0.3333333333333333703, 0.3333333333333333148, 0.3333333333333335369, 0.3333333333333333703, 0.3333333333333335369, 0.3333333333333333703, 0.3333333333333334814, 0.3333333333333333703, 0.3333333333333334259, 0.3333333333333333148, 0.3333333333333335369, 0.3333333333333333703, 0.3333333333333334814, 0.3333333333333333148, 0.3333333333333334814, 0.3333333333333334259, 0.3333333333333335369, 0.3333333333333334259, 0.3333333333333334814, 0.3333333333333334259, 0.3333333333333334259, 0.3333333333333334259, 0.3333333333333334259, 0.3333333333333333703, 0.3333333333333333703, 0.3333333333333334814, 0.3333333333333333703, 0.3333333333333333703, 0.3333333333333335369, 0.3333333333333332593, 0.3333333333333335369, 0.3333333333333332593, 0.3333333333333335924, 0.3333333333333334259, 0.3333333333333334814, 0.3333333333333333703, 0.3333333333333334814, 0.3333333333333334259, 0.3333333333333334259, 0.3333333333333334814, 0.3333333333333333703, 0.3333333333333333703, 0.3333333333333334814, 0.3333333333333333703, 0.3333333333333334814, 0.3333333333333333703, 0.3333333333333334259, 0.3333333333333334259, 0.3333333333333335369, 0.3333333333333333703, 0.3333333333333335369, 0.3333333333333334259, 0.3333333333333335369, 0.3333333333333334259, 0.3333333333333334259, 0.3333333333333334814, 0.3333333333333334814, 0.3333333333333333703, 0.3333333333333334814, 0.3333333333333333148, 0.3333333333333335369, 0.3333333333333333148, 0.3333333333333335369, 0.3333333333333334259, 0.3333333333333334259, 0.3333333333333334814, 0.3333333333333334814, 0.3333333333333333703, 0.3333333333333335369, 0.3333333333333333703, 0.3333333333333334259, 0.3333333333333334814, 0.3333333333333334814, 0.3333333333333334259, 0.3333333333333334259, 0.3333333333333335369, 0.3333333333333333148, 0.3333333333333335924, 0.3333333333333333703, 0.3333333333333333703, 0.3333333333333335369, 0.3333333333333333703, 0.3333333333333335924, 0.3333333333333333148, 0.3333333333333333703, 0.3333333333333334814, 0.3333333333333333703, 0.3333333333333335369, 0.3333333333333333703, 0.3333333333333334259, 0.3333333333333334814, 0.3333333333333333703, 0.3333333333333334259, 0.3333333333333334259, 0.3333333333333334259, 0.3333333333333334814, 0.3333333333333333703, 0.3333333333333334259, 0.3333333333333333703, 0.3333333333333335369, 0.3333333333333333703, 0.3333333333333334259, 0.3333333333333334259, 0.3333333333333333703, 0.3333333333333334814, 0.3333333333333333703, 0.3333333333333334259, 0.3333333333333333703, 0.3333333333333334814, 0.3333333333333335369, 0.3333333333333334259, 0.3333333333333334259, 0.3333333333333333703, 0.3333333333333335369, 0.3333333333333333703, 0.3333333333333333703, 0.3333333333333335369, 0.3333333333333333703, 0.3333333333333335924, 0.3333333333333332593, 0.3333333333333335369, 0.3333333333333334259, 0.3333333333333333703, 0.3333333333333335369, 0.3333333333333333703, 0.3333333333333333703, 0.3333333333333334259, 0.3333333333333335369, 0.3333333333333333148, 0.3333333333333333703, 0.3333333333333335369, 0.3333333333333334259, 0.3333333333333333703, 0.3333333333333335369, 0.3333333333333333703, 0.3333333333333335924, 0.3333333333333333703, 0.3333333333333335369, 0.3333333333333334259, 0.3333333333333334814, 0.3333333333333334259, 0.3333333333333334259, 0.3333333333333334814, 0.3333333333333334259, 0.3333333333333334259, 0.3333333333333333148, 0.3333333333333333703, 0.3333333333333334814, 0.3333333333333334814, 0.3333333333333334259, 0.3333333333333333703, 0.3333333333333334259, 0.3333333333333333148, 0.3333333333333335369, 0.3333333333333333703, 0.3333333333333334814, 0.3333333333333335369, 0.3333333333333335369, 0.3333333333333335369, 0.3333333333333333703, 0.3333333333333334259, 0.3333333333333334259, 0.3333333333333333148, 0.3333333333333335369, 0.3333333333333334259, 0.3333333333333334259, 0.3333333333333334259, 0.3333333333333334814, 0.3333333333333334259, 0.3333333333333333148, 0.3333333333333334814, 0.3333333333333334259, 0.3333333333333333703, 0.3333333333333333703, 0.3333333333333334814, 0.3333333333333333703, 0.3333333333333334814, 0.3333333333333334814, 0.3333333333333333148, 0.3333333333333335924, 0.3333333333333333148, 0.3333333333333335369, 0.3333333333333333148, 0.3333333333333335924, 0.3333333333333333703, 0.3333333333333333148, 0.3333333333333334259, 0.3333333333333334259, 0.3333333333333334259, 0.3333333333333333703, 0.3333333333333334814, 0.3333333333333333703, 0.3333333333333334814, 0.3333333333333334814, 0.3333333333333333703, 0.3333333333333334259, 0.3333333333333334259, 0.3333333333333334814, 0.3333333333333333703, 0.3333333333333333703, 0.3333333333333334259, 0.3333333333333334259, 0.3333333333333333703, 0.3333333333333334259, 0.3333333333333333703, 0.3333333333333334259, 0.3333333333333334259, 0.3333333333333333703, 0.3333333333333335924, 0.3333333333333332593, 0.3333333333333335369, 0.3333333333333334259, 0.3333333333333333703, 0.3333333333333333148, 0.3333333333333335924, 0.3333333333333333148, 0.3333333333333333703, 0.3333333333333334259, 0.3333333333333334814, 0.3333333333333335369, 0.3333333333333333703, 0.3333333333333334259, 0.3333333333333333703, 0.3333333333333335369, 0.3333333333333333703, 0.3333333333333334259, 0.3333333333333334814, 0.3333333333333333703, 0.3333333333333335369, 0.3333333333333333148, 0.3333333333333335369, 0.3333333333333334259, 0.3333333333333334259, 0.3333333333333333703, 0.3333333333333335369, 0.3333333333333333703, 0.3333333333333335369, 0.3333333333333334814, 0.3333333333333333703, 0.3333333333333334814, 0.3333333333333333703, 0.3333333333333333703, 0.3333333333333335369, 0.3333333333333333703, 0.3333333333333334259, 0.3333333333333334814, 0.3333333333333333703, 0.3333333333333334259, 0.3333333333333333148, 0.3333333333333335369, 0.3333333333333334259, 0.3333333333333333703, 0.3333333333333334814, 0.3333333333333334259, 0.3333333333333334814, 0.3333333333333334259, 0.3333333333333333703, 0.3333333333333333703, 0.3333333333333334259, 0.3333333333333334259, 0.3333333333333334259, 0.3333333333333334259, 0.3333333333333333703, 0.3333333333333334814, 0.3333333333333334814, 0.3333333333333333703, 0.3333333333333335369, 0.3333333333333333703, 0.3333333333333334814, 0.3333333333333334814, 0.3333333333333335369, 0.3333333333333333148, 0.3333333333333335369, 0.3333333333333333703, 0.3333333333333333148, 0.3333333333333334814, 0.3333333333333333703, 0.3333333333333334814, 0.3333333333333333703, 0.3333333333333334814, 0.3333333333333333703, 0.3333333333333335369, 0.3333333333333333703, 0.3333333333333334814, 0.3333333333333334259, 0.3333333333333334814, 0.3333333333333334259, 0.3333333333333333703, 0.3333333333333333703, 0.3333333333333334814, 0.3333333333333334259, 0.3333333333333334814, 0.3333333333333334259, 0.3333333333333334259, 0.3333333333333334259, 0.3333333333333333703, 0.3333333333333334259, 0.3333333333333333703, 0.3333333333333334814, 0.3333333333333333148, 0.3333333333333335369, 0.3333333333333333703, 0.3333333333333334814, 0.3333333333333333703, 0.3333333333333335369, 0.3333333333333334259, 0.3333333333333334259, 0.3333333333333334259, 0.3333333333333334259, 0.3333333333333334259, 0.3333333333333334259),
 ( 1.000000000000000222, 1.000000000000000222, 1.000000000000000222, 1.000000000000000222, 1.000000000000000444, 1.000000000000000000, 1.000000000000000666, 0.9999999999999997780, 1.000000000000000444, 1.000000000000000000, 1.000000000000000444, 1.000000000000000444, 1.000000000000000000, 1.000000000000000444, 1.000000000000000000, 1.000000000000000444, 1.000000000000000222, 1.000000000000000222, 1.000000000000000222, 1.000000000000000444, 1.000000000000000444, 1.000000000000000000, 1.000000000000000444, 1.000000000000000000, 1.000000000000000222, 1.000000000000000222, 1.000000000000000444, 1.000000000000000222, 1.000000000000000222, 1.000000000000000444, 1.000000000000000444, 1.000000000000000444, 1.000000000000000000, 1.000000000000000444, 1.000000000000000444, 1.000000000000000000, 1.000000000000000444, 1.000000000000000444, 1.000000000000000000, 1.000000000000000444, 1.000000000000000444, 1.000000000000000000, 1.000000000000000222, 1.000000000000000444, 1.000000000000000222, 1.000000000000000222, 1.000000000000000000, 1.000000000000000444, 1.000000000000000222, 1.000000000000000222, 1.000000000000000222, 1.000000000000000222, 1.000000000000000222, 1.000000000000000222, 1.000000000000000444, 1.000000000000000000, 1.000000000000000444, 0.9999999999999997780, 1.000000000000000666, 1.000000000000000444, 1.000000000000000444, 1.000000000000000000, 1.000000000000000444, 1.000000000000000222, 1.000000000000000222, 1.000000000000000444, 1.000000000000000222, 1.000000000000000444, 1.000000000000000000, 1.000000000000000444, 1.000000000000000222, 1.000000000000000444, 1.000000000000000444, 1.000000000000000222, 1.000000000000000222, 1.000000000000000222, 1.000000000000000444, 0.9999999999999997780, 1.000000000000000444, 1.000000000000000000, 1.000000000000000444, 1.000000000000000000, 1.000000000000000444, 0.9999999999999997780, 1.000000000000000444, 0.9999999999999997780, 1.000000000000000444, 1.000000000000000222, 1.000000000000000444, 1.000000000000000000, 1.000000000000000222, 1.000000000000000444, 1.000000000000000444, 1.000000000000000222, 1.000000000000000444, 1.000000000000000444, 1.000000000000000222, 1.000000000000000222, 1.000000000000000222, 1.000000000000000222, 1.000000000000000000, 1.000000000000000222, 1.000000000000000222, 1.000000000000000222, 1.000000000000000444, 1.000000000000000000, 1.000000000000000444, 0.9999999999999997780, 1.000000000000000666, 1.000000000000000222, 1.000000000000000444, 1.000000000000000000, 1.000000000000000444, 1.000000000000000222, 1.000000000000000222, 1.000000000000000444, 1.000000000000000000, 1.000000000000000000, 1.000000000000000444, 1.000000000000000000, 1.000000000000000444, 1.000000000000000000, 1.000000000000000444, 1.000000000000000222, 1.000000000000000444, 1.000000000000000222, 1.000000000000000444, 1.000000000000000222, 1.000000000000000444, 1.000000000000000000, 1.000000000000000444, 1.000000000000000222, 1.000000000000000444, 1.000000000000000000, 1.000000000000000444, 1.000000000000000000, 1.000000000000000444, 1.000000000000000000, 1.000000000000000444, 1.000000000000000222, 1.000000000000000444, 1.000000000000000222, 1.000000000000000444, 0.9999999999999997780, 1.000000000000000444, 1.000000000000000000, 1.000000000000000444, 1.000000000000000222, 1.000000000000000222, 1.000000000000000222, 1.000000000000000222, 1.000000000000000444, 0.9999999999999997780, 1.000000000000000444, 1.000000000000000000, 1.000000000000000000, 1.000000000000000222, 1.000000000000000222, 1.000000000000000666, 0.9999999999999997780, 1.000000000000000000, 1.000000000000000444, 1.000000000000000222, 1.000000000000000444, 1.000000000000000000, 1.000000000000000222, 1.000000000000000444, 1.000000000000000222, 1.000000000000000000, 1.000000000000000444, 1.000000000000000222, 1.000000000000000222, 1.000000000000000444, 1.000000000000000222, 1.000000000000000000, 1.000000000000000444, 1.000000000000000000, 1.000000000000000444, 1.000000000000000222, 1.000000000000000222, 1.000000000000000444, 0.9999999999999997780, 1.000000000000000444, 0.9999999999999997780, 1.000000000000000444, 1.000000000000000222, 1.000000000000000444, 1.000000000000000222, 1.000000000000000222, 1.000000000000000444, 1.000000000000000000, 1.000000000000000222, 1.000000000000000444, 1.000000000000000000, 1.000000000000000444, 1.000000000000000000, 1.000000000000000222, 1.000000000000000444, 1.000000000000000000, 1.000000000000000444, 0.9999999999999997780, 1.000000000000000444, 1.000000000000000222, 1.000000000000000444, 1.000000000000000000, 1.000000000000000000, 1.000000000000000444, 1.000000000000000000, 1.000000000000000222, 1.000000000000000444, 1.000000000000000222, 1.000000000000000444, 1.000000000000000222, 1.000000000000000444, 1.000000000000000444, 1.000000000000000444, 1.000000000000000000, 1.000000000000000444, 1.000000000000000222, 1.000000000000000444, 1.000000000000000222, 1.000000000000000000, 1.000000000000000222, 1.000000000000000444, 1.000000000000000222, 1.000000000000000444, 1.000000000000000000, 1.000000000000000222, 1.000000000000000000, 1.000000000000000444, 1.000000000000000000, 1.000000000000000444, 1.000000000000000444, 1.000000000000000444, 1.000000000000000444, 1.000000000000000000, 1.000000000000000222, 1.000000000000000444, 1.000000000000000000, 1.000000000000000444, 1.000000000000000444, 1.000000000000000444, 1.000000000000000222, 1.000000000000000222, 1.000000000000000222, 0.9999999999999997780, 1.000000000000000444, 1.000000000000000222, 1.000000000000000222, 1.000000000000000000, 1.000000000000000444, 1.000000000000000000, 1.000000000000000444, 1.000000000000000000, 1.000000000000000000, 1.000000000000000666, 1.000000000000000000, 1.000000000000000444, 1.000000000000000000, 1.000000000000000444, 1.000000000000000222, 0.9999999999999997780, 1.000000000000000444, 1.000000000000000000, 1.000000000000000444, 1.000000000000000222, 1.000000000000000444, 1.000000000000000222, 1.000000000000000222, 1.000000000000000444, 1.000000000000000000, 1.000000000000000222, 1.000000000000000444, 1.000000000000000222, 1.000000000000000000, 1.000000000000000444, 0.9999999999999997780, 1.000000000000000444, 1.000000000000000222, 1.000000000000000222, 1.000000000000000222, 1.000000000000000000, 1.000000000000000444, 1.000000000000000222, 1.000000000000000666, 0.9999999999999997780, 1.000000000000000444, 1.000000000000000222, 1.000000000000000000, 1.000000000000000222, 1.000000000000000444, 1.000000000000000222, 1.000000000000000000, 1.000000000000000444, 1.000000000000000222, 1.000000000000000444, 1.000000000000000000, 1.000000000000000444, 1.000000000000000222, 1.000000000000000444, 1.000000000000000222, 1.000000000000000222, 1.000000000000000444, 1.000000000000000222, 1.000000000000000444, 1.000000000000000000, 1.000000000000000444, 1.000000000000000222, 1.000000000000000222, 1.000000000000000000, 1.000000000000000666, 0.9999999999999997780, 1.000000000000000444, 1.000000000000000222, 1.000000000000000444, 1.000000000000000222, 1.000000000000000444, 1.000000000000000000, 1.000000000000000444, 1.000000000000000222, 1.000000000000000222, 1.000000000000000444, 1.000000000000000222, 1.000000000000000444, 1.000000000000000000, 1.000000000000000444, 1.000000000000000444, 0.9999999999999997780, 1.000000000000000444, 1.000000000000000000, 1.000000000000000444, 1.000000000000000444, 1.000000000000000222, 1.000000000000000000, 1.000000000000000444, 1.000000000000000222, 1.000000000000000444, 1.000000000000000000, 1.000000000000000444, 1.000000000000000222, 1.000000000000000444, 1.000000000000000222, 1.000000000000000444, 1.000000000000000222, 1.000000000000000222, 1.000000000000000444, 1.000000000000000444, 1.000000000000000000, 1.000000000000000444, 0.9999999999999997780, 1.000000000000000444, 1.000000000000000222, 1.000000000000000222, 1.000000000000000222, 1.000000000000000444, 1.000000000000000222, 1.000000000000000222, 1.000000000000000444, 1.000000000000000000, 1.000000000000000444, 1.000000000000000000, 1.000000000000000444, 1.000000000000000222, 1.000000000000000000, 1.000000000000000222, 1.000000000000000444, 1.000000000000000000, 1.000000000000000444, 1.000000000000000000, 1.000000000000000444, 1.000000000000000444, 1.000000000000000000, 1.000000000000000444, 1.000000000000000000, 1.000000000000000444, 1.000000000000000000, 1.000000000000000444, 1.000000000000000000, 1.000000000000000444, 1.000000000000000000, 1.000000000000000444, 1.000000000000000000, 1.000000000000000444, 1.000000000000000222, 1.000000000000000222, 1.000000000000000222, 1.000000000000000222) ) ) 
 REPRESENTATION_ITEM ( '' )  SURFACE ( )  );
#8054=CARTESIAN_POINT ( 'NONE',  ( 5.659468189498653601, -0.4240490459222304165, -1.681042783800198448 ) ) ;
#8055=CARTESIAN_POINT ( 'NONE',  ( 1.436444770134176485, 1.085300811998829662, -1.921501399296850821 ) ) ;
#8057=CARTESIAN_POINT ( 'NONE',  ( 6.355955588539900170, -0.7375000094371157999, 2.042207395130499759 ) ) ;
#8059=CARTESIAN_POINT ( 'NONE',  ( 0.3920140705387532010, -2.106502388992930630, 0.2143382252216985973 ) ) ;
#8060=CARTESIAN_POINT ( 'NONE',  ( 2.812500000000002665, 1.451031289061236684, 1.451031289061000873 ) ) ;
#8063=CARTESIAN_POINT ( 'NONE',  ( 4.049766240643924320, 0.6497466500948418933, -1.813626049157530229 ) ) ;
#8065=CARTESIAN_POINT ( 'NONE',  ( 1.014661930782149168, -2.221473418436111125, 0.005229513783167742333 ) ) ;
#8070=CARTESIAN_POINT ( 'NONE',  ( 3.950012332353939559, -1.532167235135332373, -1.608510083909537869 ) ) ;
#8076=CARTESIAN_POINT ( 'NONE',  ( 0.9498425221252141393, -1.824119990893595888, -0.8596288560165299408 ) ) ;
#8078=CARTESIAN_POINT ( 'NONE',  ( 0.2509072133702301421, -0.4515964501156078392, -2.020277220192217449 ) ) ;
#8081=CARTESIAN_POINT ( 'NONE',  ( 6.181193141064822427, 1.207202257718576144, 1.253980304253142997 ) ) ;
#8084=CARTESIAN_POINT ( 'NONE',  ( 1.088686764528872919, 1.564356141470560679, -0.8274751086292527757 ) ) ;
#8085=CARTESIAN_POINT ( 'NONE',  ( 6.574911468446097196, -0.7340051069854407473, 1.570379515389648040 ) ) ;
#8086=CARTESIAN_POINT ( 'NONE',  ( 0.1339853816830008371, 0.3136495386693045062, 1.814181566856580607 ) ) ;
#8088=CARTESIAN_POINT ( 'NONE',  ( 4.529038776287770851, -2.096192991274762996, 0.9282860960324219590 ) ) ;
#8090=CARTESIAN_POINT ( 'NONE',  ( 1.921575063125853022, 1.060747535801230379, -1.504664925706208578 ) ) ;
#8092=CARTESIAN_POINT ( 'NONE',  ( 3.170728842436408179, -1.686227525993441834, -0.7000332573987508855 ) ) ;
#8093=CARTESIAN_POINT ( 'NONE',  ( 3.481092415823695774, -2.014232707597499505, -0.09613569647320965861 ) ) ;
#8095=CARTESIAN_POINT ( 'NONE',  ( 3.221791447092836602, -2.180992460559240786, 0.6016781482265749492 ) ) ;
#8097=CARTESIAN_POINT ( 'NONE',  ( 5.684633084330723563, -2.053880889230023321, -0.4646916863456708735 ) ) ;
#8099=CARTESIAN_POINT ( 'NONE',  ( 2.576698201331685922, 1.354182300986291887, -1.566139152919379107 ) ) ;
#8102=CARTESIAN_POINT ( 'NONE',  ( 5.584674446412367210, -1.345185468269005424, 1.639207791927596247 ) ) ;
#8105=CARTESIAN_POINT ( 'NONE',  ( 0.5922524703982982031, -1.911778602531236215, -0.2371815352125578036 ) ) ;
#8113=CARTESIAN_POINT ( 'NONE',  ( 0.2818602545999105424, 0.2096452599892709712, -2.211486639639495433 ) ) ;
#8114=CARTESIAN_POINT ( 'NONE',  ( 2.081218647941612154, -0.1023907900198107734, -2.103586654547675128 ) ) ;
#8117=CARTESIAN_POINT ( 'NONE',  ( 6.034019871906543209, 1.107478494666002344, 1.495390754572333725 ) ) ;
#8123=CARTESIAN_POINT ( 'NONE',  ( -0.03470293633787284449, -1.699275230904277789, 1.268407768021381221 ) ) ;
#8126=CARTESIAN_POINT ( 'NONE',  ( 3.807043925254738781, -1.605251362286563177, 1.127602784832412386 ) ) ;
#8127=CARTESIAN_POINT ( 'NONE',  ( 2.588937169860201504, -0.3686131662095324946, -2.129881858774537395 ) ) ;
#8131=CARTESIAN_POINT ( 'NONE',  ( 2.976183818757103250, -0.1284355763333933920, -1.735648432857107126 ) ) ;
#8136=CARTESIAN_POINT ( 'NONE',  ( 2.653672528425448540, -0.3418824089525332455, -1.986742401007553172 ) ) ;
#8137=FACE_OUTER_BOUND ( 'NONE', #57716, .T. ) ;
#8138=CARTESIAN_POINT ( 'NONE',  ( 0.2687375195599971400, -1.410744835756465365, 1.637978619736128127 ) ) ;
#8141=CARTESIAN_POINT ( 'NONE',  ( 2.078924955456124657, -0.09500079177627264448, -1.969288250925634642 ) ) ;
#8143=CARTESIAN_POINT ( 'NONE',  ( 6.521744167503259249, -0.4122283346772101509, 1.874327247564554266 ) ) ;
#8149=CARTESIAN_POINT ( 'NONE',  ( 2.824872690137433029, 1.461285568133148693, -1.394416722739227898 ) ) ;
#8151=CARTESIAN_POINT ( 'NONE',  ( 6.212023164884419302, -2.291203086667678690, 0.2740844210103609568 ) ) ;
#8153=CARTESIAN_POINT ( 'NONE',  ( 2.571086506140254357, 1.750134206675527437, 0.8865088104979682582 ) ) ;
#8155=CARTESIAN_POINT ( 'NONE',  ( 0.4225002777262388265, -1.427939226333583500, -1.423959630194884696 ) ) ;
#8157=CARTESIAN_POINT ( 'NONE',  ( 2.167340134605561630, 1.933669477944195636, -0.8630234182349978411 ) ) ;
#8160=CARTESIAN_POINT ( 'NONE',  ( 1.780954670855667388, 1.268887097626215876, 1.334285251370644021 ) ) ;
#8164=CARTESIAN_POINT ( 'NONE',  ( 3.955424862866574021, -1.843446357660895041, 1.048082435718917571 ) ) ;
#8165=CARTESIAN_POINT ( 'NONE',  ( 6.685517510867199142, -0.8268063683338886527, 1.755141085440144355 ) ) ;
#8169=CARTESIAN_POINT ( 'NONE',  ( 4.710263567924342532, -0.8773996900517248010, -1.864791387430650094 ) ) ;
#8171=CARTESIAN_POINT ( 'NONE',  ( 0.9074547957551477584, -0.8278116715597811925, -1.644758345054016191 ) ) ;
#8176=CARTESIAN_POINT ( 'NONE',  ( 1.172829962703396456, -1.397616723802884708, 1.707921395779465890 ) ) ;
#8177=CARTESIAN_POINT ( 'NONE',  ( 4.130342294306089457, 1.214786636354926452, -1.908452007788311366 ) ) ;
#8179=CARTESIAN_POINT ( 'NONE',  ( 3.656362025717549535, 1.803379273073001388, 0.1719060212231597329 ) ) ;
#8180=CARTESIAN_POINT ( 'NONE',  ( 3.590956263468424225, 1.645886154840708659, 0.9800325279442632098 ) ) ;
#8181=CARTESIAN_POINT ( 'NONE',  ( 3.701679681979888503, -1.565833156357125278, -1.354537944502069102 ) ) ;
#8183=CARTESIAN_POINT ( 'NONE',  ( 3.045733664408939223, 0.7109379216812520275, -1.838982635421481993 ) ) ;
#8184=CARTESIAN_POINT ( 'NONE',  ( 0.7274102002729305738, -1.830281784476958773, 0.6011100631785198933 ) ) ;
#8185=CARTESIAN_POINT ( 'NONE',  ( 3.748781033766034998, -1.529746656882627454, 1.076398355447941491 ) ) ;
#8186=CARTESIAN_POINT ( 'NONE',  ( 1.999037954658490213, -0.6180237258119178900, -2.223338030673171151 ) ) ;
#8187=CARTESIAN_POINT ( 'NONE',  ( 4.176097997218494839, -0.9553649929725913648, -1.596950837584124816 ) ) ;
#8192=CARTESIAN_POINT ( 'NONE',  ( 0.3816453311432427831, 1.964265557344764712, -0.7602060659359122230 ) ) ;
#8196=CARTESIAN_POINT ( 'NONE',  ( 2.426173717206762781, -2.096881089210366422, 0.3156149858808757203 ) ) ;
#8197=CARTESIAN_POINT ( 'NONE',  ( 0.2815179179852530522, 0.1935487615560542163, -2.010460980806235920 ) ) ;
#8201=CARTESIAN_POINT ( 'NONE',  ( 1.458524589769864210, 0.8745999688587955401, 1.976921506453344080 ) ) ;
#8206=CARTESIAN_POINT ( 'NONE',  ( 5.630092293170263495, 2.014432788975322630, 0.09412139267171715229 ) ) ;
#8210=CARTESIAN_POINT ( 'NONE',  ( 0.5150084580479041829, 1.557691122620246116, -1.641117935488043633 ) ) ;
#8214=CARTESIAN_POINT ( 'NONE',  ( 1.194790368808082759, 1.690169533058868190, 0.9015364962996033071 ) ) ;
#8218=CARTESIAN_POINT ( 'NONE',  ( 2.384998569339055408, 1.577468512335476358, -0.6981430484895093658 ) ) ;
#8221=CARTESIAN_POINT ( 'NONE',  ( 1.352431244980515146, -1.399367522912741135, 1.083307108726710100 ) ) ;
#8223=CARTESIAN_POINT ( 'NONE',  ( 2.385404357411140541, 0.09669159202466531822, -2.010876702762071311 ) ) ;
#8226=CARTESIAN_POINT ( 'NONE',  ( 3.698430944683338328, -2.204125419102770600, -0.1106900096672913392 ) ) ;
#8230=CARTESIAN_POINT ( 'NONE',  ( 3.914780425095893968, -0.6665358524936614293, -2.013057630646164942 ) ) ;
#8231=CARTESIAN_POINT ( 'NONE',  ( 3.304314702139679039, 1.277028363417181289, -1.560513873864778578 ) ) ;
#8232=CARTESIAN_POINT ( 'NONE',  ( 3.339928375916663139, -1.083189831351333954, -1.451890931963683684 ) ) ;
#8237=CARTESIAN_POINT ( 'NONE',  ( 1.024039198018782626, 1.117340804906666873, -1.500143343703803422 ) ) ;
#8238=CARTESIAN_POINT ( 'NONE',  ( 6.234959169399230561, 0.1841439077357870380, 1.816378869960999509 ) ) ;
#8247=CARTESIAN_POINT ( 'NONE',  ( 4.482752736079084421, -1.382999391253452615, 1.607682512923855445 ) ) ;
#8248=CARTESIAN_POINT ( 'NONE',  ( -0.02968770228137587730, 2.889947918782026726, -2.315223470976325526 ) ) ;
#8250=CARTESIAN_POINT ( 'NONE',  ( 4.200430055897656167, -0.6152532741215356316, -1.872979577440760046 ) ) ;
#8252=CARTESIAN_POINT ( 'NONE',  ( 6.398695753475230674, -1.876852914212179035, -0.3660984893600614520 ) ) ;
#8254=CARTESIAN_POINT ( 'NONE',  ( 0.2283145101530216492, 2.111890517744571927, 0.1509969543822299032 ) ) ;
#8256=CARTESIAN_POINT ( 'NONE',  ( 1.258353326579707776, -2.070544811992577561, -0.001879966208345739808 ) ) ;
#8260=CARTESIAN_POINT ( 'NONE',  ( 3.486350522754261494, -0.4081323730865527577, -2.050228346494194831 ) ) ;
#8263=CARTESIAN_POINT ( 'NONE',  ( 1.852308540880560850, 0.5694407911355814367, 1.734573797025913189 ) ) ;
#8264=CARTESIAN_POINT ( 'NONE',  ( 1.172180985828397581, 0.7336035429467204771, 1.656470807091579900 ) ) ;
#8266=CARTESIAN_POINT ( 'NONE',  ( 6.041676539500916654, -1.595688354349385607, -1.524751901930617715 ) ) ;
#8268=CARTESIAN_POINT ( 'NONE',  ( 4.260898339918250066, -1.637375743694971408, 1.479669880875638777 ) ) ;
#8271=CARTESIAN_POINT ( 'NONE',  ( 2.473184984502617478, -1.664690511387197702, -0.9409074295685518896 ) ) ;
#8273=CARTESIAN_POINT ( 'NONE',  ( 5.793440749948310042, -1.873300974885267589, 0.8818263447485861217 ) ) ;
#8276=CARTESIAN_POINT ( 'NONE',  ( 5.776942576169182608, 2.025397260235710206, -0.8375503648087383457 ) ) ;
#8286=CARTESIAN_POINT ( 'NONE',  ( 5.260626886859606444, -0.6923115906582855139, -1.951227211109484383 ) ) ;
#8287=CARTESIAN_POINT ( 'NONE',  ( 4.231024032915966515, 0.09596189134018082156, 1.924231256547383362 ) ) ;
#8288=EDGE_CURVE ( 'NONE', #112905, #202900, #86587, .T. ) ;
#8289=CARTESIAN_POINT ( 'NONE',  ( 6.433232048832024930, -1.700592621796994441, -1.261046147972416875 ) ) ;
#8293=CARTESIAN_POINT ( 'NONE',  ( 6.580031643469963498, -2.246689805010111396, -0.4540597329640746471 ) ) ;
#8294=CARTESIAN_POINT ( 'NONE',  ( 4.898959864523320107, 1.516061528642864253, -1.016892643307308441 ) ) ;
#8302=CARTESIAN_POINT ( 'NONE',  ( 2.436835438956724165, -1.365703447793526371, -1.235134912642745775 ) ) ;
#8303=CARTESIAN_POINT ( 'NONE',  ( 6.486586620031766337, -1.235515937849906321, 1.590312944162165287 ) ) ;
#8304=CARTESIAN_POINT ( 'NONE',  ( 0.8787516259003292918, -0.3353366030727308877, 2.273710652787809039 ) ) ;
#8305=CARTESIAN_POINT ( 'NONE',  ( 6.368018226480639754, -1.947316962026977682, 0.2367824842242904348 ) ) ;
#8309=CARTESIAN_POINT ( 'NONE',  ( 0.6607010325807397555, -0.6960017893198193750, -1.950014918625786020 ) ) ;
#8311=CARTESIAN_POINT ( 'NONE',  ( 3.017214641935324071, -2.014214092474704731, 0.5601794093188486867 ) ) ;
#8312=CARTESIAN_POINT ( 'NONE',  ( 1.621729638615863944, -1.036547396872866678, -1.557007864774778705 ) ) ;
#8313=CARTESIAN_POINT ( 'NONE',  ( 2.108749758911751204, 0.7741990562295970602, -1.861730988020185329 ) ) ;
#8315=ORIENTED_EDGE ( 'NONE', *, *, #92877, .F. ) ;
#8317=CARTESIAN_POINT ( 'NONE',  ( 2.507021497916587460, -1.721230695331811722, 0.2570161617474544524 ) ) ;
#8321=CARTESIAN_POINT ( 'NONE',  ( 3.000334558935643603, -0.5012536917932303160, -1.650428355875031228 ) ) ;
#8322=CARTESIAN_POINT ( 'NONE',  ( 3.087623348389135547, -0.8860277256741244667, 2.004638750299721828 ) ) ;
#8323=CARTESIAN_POINT ( 'NONE',  ( 0.1758332513315676859, 1.282751065617006248, 1.167194905859494591 ) ) ;
#8324=CARTESIAN_POINT ( 'NONE',  ( 5.426482453889071245, 1.317083479513626587, -1.770629405693980640 ) ) ;
#8326=CARTESIAN_POINT ( 'NONE',  ( 2.008858235458183650, 0.6779177425604805407, 2.062613225174831921 ) ) ;
#8327=CARTESIAN_POINT ( 'NONE',  ( 1.558932953716257730, -1.564965500463588732, -0.9399777662534372080 ) ) ;
#8328=CARTESIAN_POINT ( 'NONE',  ( 4.786377933101198856, -0.7163331637287263520, -1.992584184115009149 ) ) ;
#8329=CARTESIAN_POINT ( 'NONE',  ( 6.539320575229287336, 7.629137130509086262, 2.596737603865982624 ) ) ;
#8331=CARTESIAN_POINT ( 'NONE',  ( 4.230218865515364968, 2.248128804489764043, 0.4474220685124987162 ) ) ;
#8335=CARTESIAN_POINT ( 'NONE',  ( 0.7156801077207708417, 1.735845614737155707, 1.217653249118654468 ) ) ;
#8341=VERTEX_POINT ( 'NONE', #45463 ) ;
#8342=CARTESIAN_POINT ( 'NONE',  ( 5.449842333688053486, -1.824117940560719298, -0.8596331684956670660 ) ) ;
#8344=CARTESIAN_POINT ( 'NONE',  ( 3.502832280938583676, 0.4964207669093263497, 2.001847840641638232 ) ) ;
#8349=CARTESIAN_POINT ( 'NONE',  ( 6.439412520197737244, 0.8424478218750917069, -2.023249321508275855 ) ) ;
#8350=CARTESIAN_POINT ( 'NONE',  ( 3.375625116643202972, -0.3961014713874110305, -1.976955985980306307 ) ) ;
#8351=CARTESIAN_POINT ( 'NONE',  ( 3.052128622409277181, -1.392423357299840792, 1.204796875372941667 ) ) ;
#8353=CARTESIAN_POINT ( 'NONE',  ( 6.827182134110196365, 0.003888933837258023128, 1.810856214465895508 ) ) ;
#8354=CARTESIAN_POINT ( 'NONE',  ( 0.2648075084464130979, 2.141788565065712913, -0.8351287359565621182 ) ) ;
#8356=CARTESIAN_POINT ( 'NONE',  ( 6.403223674518304875, 1.876769595090790554, 1.263360297164903168 ) ) ;
#8357=CARTESIAN_POINT ( 'NONE',  ( 1.524195097446314318, -1.171203135327163913, -1.750160316008353201 ) ) ;
#8367=CARTESIAN_POINT ( 'NONE',  ( 3.937882119624159127, -2.125045857649208614, 0.6470787896058221023 ) ) ;
#8368=CARTESIAN_POINT ( 'NONE',  ( 1.693587955360946529, -0.7361150630936144079, 2.064250245950305374 ) ) ;
#8369=CARTESIAN_POINT ( 'NONE',  ( 0.3994152196779980346, 1.832435997337564348, -1.229551327501000380 ) ) ;
#8371=CARTESIAN_POINT ( 'NONE',  ( 4.510177812457000002, 1.961482754637720927, -0.04604004567236585910 ) ) ;
#8375=CARTESIAN_POINT ( 'NONE',  ( 6.610000000000001208, 3.709748940453510446, 2.234587373521100151 ) ) ;
#8378=CARTESIAN_POINT ( 'NONE',  ( 3.006218798242997980, -0.8556837461295877523, 1.940463308995137526 ) ) ;
#8380=CARTESIAN_POINT ( 'NONE',  ( 5.190363053866647647, -2.144918610114197488, -0.2683968819863768451 ) ) ;
#8381=CARTESIAN_POINT ( 'NONE',  ( 4.194743914777058436, 1.481411246205705412, 1.093257649623424754 ) ) ;
#8385=CARTESIAN_POINT ( 'NONE',  ( 0.4854153416827499679, -1.726952712381021326, -0.2154422717644439433 ) ) ;
#8386=CARTESIAN_POINT ( 'NONE',  ( 6.827182134110209688, 6.038954451951505042, 2.405852596708078384 ) ) ;
#8389=CARTESIAN_POINT ( 'NONE',  ( 4.610339536224768331, -0.9213992672730475508, -1.955631277330005968 ) ) ;
#8391=CARTESIAN_POINT ( 'NONE',  ( 5.606796008369615336, 0.8196459417171353401, -1.842166028910074527 ) ) ;
#8393=CARTESIAN_POINT ( 'NONE',  ( 3.608425205800522839, -0.8741791752944136906, -1.977237025433141504 ) ) ;
#8394=CARTESIAN_POINT ( 'NONE',  ( 4.007068486172041588, 1.689080509644375505, 1.016306131198143836 ) ) ;
#8396=CARTESIAN_POINT ( 'NONE',  ( 0.5523711044835468709, 0.7197940642212009577, -2.192503933474987843 ) ) ;
#8397=CARTESIAN_POINT ( 'NONE',  ( 3.321608758505911307, -1.986990267296639745, 0.5463351552400242950 ) ) ;
#8398=CARTESIAN_POINT ( 'NONE',  ( 5.724156413028869572, 1.872829174467111946, 0.5137480774947185136 ) ) ;
#8405=CARTESIAN_POINT ( 'NONE',  ( 2.555956245031346885, 0.5892994983645870599, -2.126554282292691500 ) ) ;
#8408=CARTESIAN_POINT ( 'NONE',  ( 6.578960362708798471, 1.829258725439562916, 0.7091506158454219388 ) ) ;
#8409=CARTESIAN_POINT ( 'NONE',  ( 6.539320575229281118, 7.629137130509070275, 2.703262396134015866 ) ) ;
#8414=CARTESIAN_POINT ( 'NONE',  ( 5.244037021109955177, 0.5378974813256987009, 1.760811445753920568 ) ) ;
#8416=CARTESIAN_POINT ( 'NONE',  ( 2.149359023125880341, -1.654445155856735905, -1.228624528962230400 ) ) ;
#8422=CARTESIAN_POINT ( 'NONE',  ( 0.5321925127804688627, 1.059884587108523402, -1.767317575122410167 ) ) ;
#8424=CARTESIAN_POINT ( 'NONE',  ( 4.774869596704574448, 1.716175909155163382, -0.6674964387535023969 ) ) ;
#8428=CARTESIAN_POINT ( 'NONE',  ( 4.248781725523794073, 0.5872999373685274804, 2.127227798101683387 ) ) ;
#8429=CARTESIAN_POINT ( 'NONE',  ( 0.5796411875719498230, 2.017120475678677582, -0.7774783797904263327 ) ) ;
#8431=CARTESIAN_POINT ( 'NONE',  ( 0.03522015555855115276, -0.09184495783944729430, 1.910282976853895587 ) ) ;
#8432=CARTESIAN_POINT ( 'NONE',  ( 6.403544266003773799, -1.856299428965903164, 0.4729442951737494183 ) ) ;
#8435=CARTESIAN_POINT ( 'NONE',  ( 6.340485057729076779, 1.096952271789692901, -1.566184530335120950 ) ) ;
#8438=CARTESIAN_POINT ( 'NONE',  ( 1.076777757339364205, -0.04213119042271313425, -1.870346338061685154 ) ) ;
#8439=CARTESIAN_POINT ( 'NONE',  ( 2.395720570290179374, -1.993893129684479293, 0.3006499569925198956 ) ) ;
#8443=CARTESIAN_POINT ( 'NONE',  ( 4.125680639212436773, -2.015421878069530326, 0.6112012065569141228 ) ) ;
#8449=CARTESIAN_POINT ( 'NONE',  ( 4.623309962349557267, 1.759429041943610716, 0.9917458525283324722 ) ) ;
#8452=CARTESIAN_POINT ( 'NONE',  ( 4.640002929648442631, 0.9288797265196678810, -1.951996720969489951 ) ) ;
#8458=CARTESIAN_POINT ( 'NONE',  ( 1.504584854702104124, 2.168655969765376224, 0.1073316571278438991 ) ) ;
#8462=CARTESIAN_POINT ( 'NONE',  ( 0.5382993156314471728, -1.579489783069366604, 0.9460463261394758128 ) ) ;
#8464=CARTESIAN_POINT ( 'NONE',  ( 3.017305944477025825, -2.111434807548946857, 0.5868732223921411251 ) ) ;
#8466=CARTESIAN_POINT ( 'NONE',  ( 4.083118212167598848, -0.2185186360062584821, -2.251932414709489905 ) ) ;
#8472=CARTESIAN_POINT ( 'NONE',  ( 4.182668740906975380, -0.1716826142807558186, -1.761352938113736277 ) ) ;
#8474=CARTESIAN_POINT ( 'NONE',  ( 1.202331507228219243, -2.106147100265920002, -0.0002331622408376087278 ) ) ;
#8478=CARTESIAN_POINT ( 'NONE',  ( 1.381238074367253876, -0.05158952566820934615, 1.969057209924016227 ) ) ;
#8481=CARTESIAN_POINT ( 'NONE',  ( 5.168131652730963310, 1.809155975298855523, -0.09671077906142805380 ) ) ;
#8486=CARTESIAN_POINT ( 'NONE',  ( 5.084763247618332649, -0.2297073032716222263, -1.856415652357709778 ) ) ;
#8488=CARTESIAN_POINT ( 'NONE',  ( 4.803616497939601437, -1.596918191575154911, -1.317456641179854504 ) ) ;
#8501=CARTESIAN_POINT ( 'NONE',  ( 3.877359892829432386, -0.1466975079335990917, 1.956454564409334296 ) ) ;
#8502=CARTESIAN_POINT ( 'NONE',  ( 1.932970024460831882, 1.034005469613193062, 1.730602090182407959 ) ) ;
#8506=CARTESIAN_POINT ( 'NONE',  ( 1.581098268704693055, 1.730367963306264301, -0.7109649657882493035 ) ) ;
#8508=CARTESIAN_POINT ( 'NONE',  ( 3.111590725901419940, 1.589763268213672420, 1.235112918372171187 ) ) ;
#8510=CARTESIAN_POINT ( 'NONE',  ( 3.743865479105834559, 2.100983596406953424, -0.2614307623071217557 ) ) ;
#8512=CARTESIAN_POINT ( 'NONE',  ( 4.896967953096117654, 0.3505727482827174502, 2.040303948762006492 ) ) ;
#8514=CARTESIAN_POINT ( 'NONE',  ( 0.08173368997131927327, -0.9817114319007680390, 1.845913477919949086 ) ) ;
#8515=CARTESIAN_POINT ( 'NONE',  ( 6.720655732516648051, 1.999557737031621540, 2.575425662770465252 ) ) ;
#8516=CARTESIAN_POINT ( 'NONE',  ( 5.614214418409627427, -0.8227427255552112184, -1.629729119005427496 ) ) ;
#8523=CARTESIAN_POINT ( 'NONE',  ( 6.094389051209717856, -1.018956457145767436, 1.618003106988876283 ) ) ;
#8531=VERTEX_POINT ( 'NONE', #179724 ) ;
#8533=CARTESIAN_POINT ( 'NONE',  ( 5.431267612114304200, -1.591330327768199382, -1.238307421737715019 ) ) ;
#8535=CARTESIAN_POINT ( 'NONE',  ( -0.1399997263889559695, 7.629137130509076492, -2.600276787041354343 ) ) ;
#8538=CARTESIAN_POINT ( 'NONE',  ( 2.254690153889327586, -0.5205305878250593432, -1.899364841092534339 ) ) ;
#8539=ADVANCED_FACE ( 'NONE', ( #97418 ), #108799, .F. ) ;
#8540=CARTESIAN_POINT ( 'NONE',  ( 3.550407796516129366, -1.352142120786763213, 1.496064415113136592 ) ) ;
#8542=CARTESIAN_POINT ( 'NONE',  ( 6.827182134110157286, 6.032625672350935275, 2.883942191975923830 ) ) ;
#8543=CARTESIAN_POINT ( 'NONE',  ( 3.380998015235132215, 1.981133383611884735, -0.9370748116589098231 ) ) ;
#8545=CARTESIAN_POINT ( 'NONE',  ( 2.801685564775885595, -0.6058112460363762608, 1.828711369353401617 ) ) ;
#8548=CARTESIAN_POINT ( 'NONE',  ( -0.1296875068448159751, 0.001480089298542403009, -1.826395826379861864 ) ) ;
#8549=CARTESIAN_POINT ( 'NONE',  ( 0.1333542156527295908, 7.629137130509112907, -2.645925523406994717 ) ) ;
#8556=CARTESIAN_POINT ( 'NONE',  ( 5.688959394570705541, 1.398425918548395153, 1.197878823674280779 ) ) ;
#8557=CARTESIAN_POINT ( 'NONE',  ( 3.404942666290892817, -0.3948933297331903014, -1.973820178108119272 ) ) ;
#8558=CARTESIAN_POINT ( 'NONE',  ( 5.079617024973425821, 1.589842341716392493, -1.660015637060639371 ) ) ;
#8559=CARTESIAN_POINT ( 'NONE',  ( 3.186215892106421421, 1.037744835847534741, -1.544512256342661427 ) ) ;
#8561=CARTESIAN_POINT ( 'NONE',  ( -0.1290005225502398323, 0.2247172878383028038, -2.207197350255707402 ) ) ;
#8565=CARTESIAN_POINT ( 'NONE',  ( 6.374567656919228220, -0.1030857042376011334, -2.088345373630628554 ) ) ;
#8571=CARTESIAN_POINT ( 'NONE',  ( 5.813083859329478464, 1.524454967706680319, 0.8070229810451818864 ) ) ;
#8573=CARTESIAN_POINT ( 'NONE',  ( 1.828352651294574249, 0.6632370903016276964, -1.602517542597500455 ) ) ;
#8577=CARTESIAN_POINT ( 'NONE',  ( 5.893482054836863604, -1.966010524246808666, 0.9213097603111667366 ) ) ;
#8578=CARTESIAN_POINT ( 'NONE',  ( 4.828627627824715773, 1.747987318788373656, 0.5269492854979712648 ) ) ;
#8579=CARTESIAN_POINT ( 'NONE',  ( 1.973419848571813295, -0.2453196125269933581, 1.946320556625024345 ) ) ;
#8583=CARTESIAN_POINT ( 'NONE',  ( 3.334745777049468618, 1.343786929377327466, -1.640352557257473309 ) ) ;
#8587=CARTESIAN_POINT ( 'NONE',  ( 1.428671948192638208, -1.316369429293560156, 1.597808059233512656 ) ) ;
#8589=CARTESIAN_POINT ( 'NONE',  ( 3.914843843660667400, -0.6973054565188941956, -2.109062029434173535 ) ) ;
#8591=CARTESIAN_POINT ( 'NONE',  ( 1.319383182065179128, 1.127869332580781148, -2.002907031218110312 ) ) ;
#8593=CARTESIAN_POINT ( 'NONE',  ( 6.209847231236663490, 0.6040719066883664112, -1.972102366942799945 ) ) ;
#8597=CARTESIAN_POINT ( 'NONE',  ( 6.585540641348407220, -0.7802508550805786758, 1.666130356082275998 ) ) ;
#8599=CARTESIAN_POINT ( 'NONE',  ( -0.1104750535120268828, 5.720715034752038797, -2.697548938405624597 ) ) ;
#8600=CARTESIAN_POINT ( 'NONE',  ( 2.625662686473359653, -0.9909224867145174365, -1.411489731159983219 ) ) ;
#8601=CARTESIAN_POINT ( 'NONE',  ( 2.167204200501818612, 1.841733140229084853, -0.8216742516050158374 ) ) ;
#8602=CARTESIAN_POINT ( 'NONE',  ( 3.287964078406432566, 1.811126957681759908, -1.415446460160358688 ) ) ;
#8604=CARTESIAN_POINT ( 'NONE',  ( 3.620660229735796154, 1.438486863682734818, -1.746180642158390084 ) ) ;
#8605=CARTESIAN_POINT ( 'NONE',  ( 5.426436078920066741, 1.255580583125959437, -1.690716914145540040 ) ) ;
#8607=CARTESIAN_POINT ( 'NONE',  ( 3.866244329565728943, -1.190307266767919536, 1.309773914726497734 ) ) ;
#8609=CARTESIAN_POINT ( 'NONE',  ( 6.409759596795807646, -1.076414324555999391, -2.023967322820482639 ) ) ;
#8610=CARTESIAN_POINT ( 'NONE',  ( 6.035073252477260120, -1.336788798515762489, -1.266260169258619284 ) ) ;
#8614=CARTESIAN_POINT ( 'NONE',  ( 6.123007039855313138, -2.064672272812938747, 0.7349105657750015785 ) ) ;
#8617=CARTESIAN_POINT ( 'NONE',  ( 6.338344951546218908, -1.110931056888088353, 1.746890944850580052 ) ) ;
#8618=CARTESIAN_POINT ( 'NONE',  ( 0.3918150239524306189, -2.006371095615328226, 0.2024682584410575914 ) ) ;
#8620=CARTESIAN_POINT ( 'NONE',  ( 4.336495953379083446, 1.889596944713485049, 0.3744603196194126182 ) ) ;
#8624=CARTESIAN_POINT ( 'NONE',  ( 0.5455723692351510667, 0.1713331888719657747, 2.214891930232844253 ) ) ;
#8634=CARTESIAN_POINT ( 'NONE',  ( 1.785527960060459440, -1.848404783191982315, 0.6579185095809261252 ) ) ;
#8638=CARTESIAN_POINT ( 'NONE',  ( 5.266048140081638351, -1.952571265509401854, 0.1905133553196102503 ) ) ;
#8642=CARTESIAN_POINT ( 'NONE',  ( 6.473507614529132148, 2.070149491355821159, -0.6224772505839873959 ) ) ;
#8643=CARTESIAN_POINT ( 'NONE',  ( -0.2104748580754183807, 2.005809028216706924, -2.517884123765606663 ) ) ;
#8646=CARTESIAN_POINT ( 'NONE',  ( 0.8252170375972631700, -1.778153878779257901, 0.5809004490327505099 ) ) ;
#8647=CARTESIAN_POINT ( 'NONE',  ( 6.274686883491842337, -1.720241393171379363, 0.2158021260532434760 ) ) ;
#8649=CARTESIAN_POINT ( 'NONE',  ( 3.034921719543516971, -1.931671641359738567, 1.035203715903771915 ) ) ;
#8650=CARTESIAN_POINT ( 'NONE',  ( 4.946439154741203659, 2.300974901101384695, 0.1755221459238848203 ) ) ;
#8651=CARTESIAN_POINT ( 'NONE',  ( 0.1454761644432709389, -1.592655978506152703, -1.307672486379028332 ) ) ;
#8652=CARTESIAN_POINT ( 'NONE',  ( 2.132666086734685162, -1.734545437858775463, 0.8733739462151270949 ) ) ;
#8656=CARTESIAN_POINT ( 'NONE',  ( 4.781546299372162245, 0.2051969522943071500, -2.110614603223801122 ) ) ;
#8658=CARTESIAN_POINT ( 'NONE',  ( 3.639296212489909532, 0.7283784247123014088, 1.880435045658496618 ) ) ;
#8662=CARTESIAN_POINT ( 'NONE',  ( 1.242498012622397674, 0.3540479964400863877, 1.790853789395550955 ) ) ;
#8667=CARTESIAN_POINT ( 'NONE',  ( 5.911025222378588850, 1.816451602635826612, 0.9735456368637726010 ) ) ;
#8671=CARTESIAN_POINT ( 'NONE',  ( 4.846356044401274765, 1.036295046036241674, -1.733382803446526621 ) ) ;
#8672=CARTESIAN_POINT ( 'NONE',  ( 5.971364366153397718, -1.903789954562478792, -1.144205655003695643 ) ) ;
#8677=CARTESIAN_POINT ( 'NONE',  ( 3.889569955515647326, 1.491445920024776051, 1.422513881352378107 ) ) ;
#8678=CARTESIAN_POINT ( 'NONE',  ( 4.184220324914634581, 1.621181886760931778, 1.198861198883696799 ) ) ;
#8685=CARTESIAN_POINT ( 'NONE',  ( 3.462267382487670631, 1.587593928739635896, 1.242537129137813556 ) ) ;
#8686=CARTESIAN_POINT ( 'NONE',  ( 2.888418961059231904, 1.578855305991919478, -0.9468669452540460219 ) ) ;
#8687=CARTESIAN_POINT ( 'NONE',  ( 0.6457025891282016650, -1.976290545051001768, 1.191322501153786906 ) ) ;
#8689=CARTESIAN_POINT ( 'NONE',  ( 3.462350783624254191, 0.9684823049558517472, 1.932541222812742987 ) ) ;
#8693=CARTESIAN_POINT ( 'NONE',  ( 3.409784427348498070, 0.5549599139818006677, 2.230294995599948926 ) ) ;
#8696=CARTESIAN_POINT ( 'NONE',  ( 2.869827659178546764, 0.9992216309704025079, 1.581230272166146644 ) ) ;
#8697=CARTESIAN_POINT ( 'NONE',  ( 5.770382930017874834, -1.251004719971451795, 1.523686133408495236 ) ) ;
#8701=CARTESIAN_POINT ( 'NONE',  ( 0.4170028235400899397, 1.518763190251697370, -1.601383572969114599 ) ) ;
#8706=CARTESIAN_POINT ( 'NONE',  ( 6.262572880032761802, -1.394454384559177695, 1.393866484745357459 ) ) ;
#8707=CARTESIAN_POINT ( 'NONE',  ( 5.971339433669736962, 0.1760496889521658836, -2.301030538967073991 ) ) ;
#8708=CARTESIAN_POINT ( 'NONE',  ( 5.828513650932020340, -1.180329482691832244, 1.438830759754748723 ) ) ;
#8709=CARTESIAN_POINT ( 'NONE',  ( 3.485269120655315689, 0.04592427588026624929, 2.062205569330832766 ) ) ;
#8716=CARTESIAN_POINT ( 'NONE',  ( 5.336453890206420247, -1.210535830701382709, 1.802210774359000567 ) ) ;
#8719=CARTESIAN_POINT ( 'NONE',  ( 4.018977146631536712, -1.760761141180338774, 0.5383908109771737838 ) ) ;
#8723=CARTESIAN_POINT ( 'NONE',  ( 6.720655732516653380, 6.038084619979597001, 2.521169617733058477 ) ) ;
#8724=CARTESIAN_POINT ( 'NONE',  ( 6.480031355044912900, -2.148842909532014289, -0.4297212958329286736 ) ) ;
#8726=CARTESIAN_POINT ( 'NONE',  ( 0.8435138722653515719, -1.939887490614403687, 1.163926157780611925 ) ) ;
#8732=CARTESIAN_POINT ( 'NONE',  ( 0.2231138172586397683, 1.663799575440491285, 0.9424754157791456199 ) ) ;
#8734=CARTESIAN_POINT ( 'NONE',  ( 1.902845806929494232, 1.469307612142495723, 0.9863148084752764166 ) ) ;
#8735=CARTESIAN_POINT ( 'NONE',  ( 5.637363213272434059, -0.04718591601137950980, 2.012692011999743791 ) ) ;
#8737=CARTESIAN_POINT ( 'NONE',  ( 3.715936783694527179, -2.075135040979354528, 0.3580079364009710052 ) ) ;
#8739=CARTESIAN_POINT ( 'NONE',  ( 3.532743792504475788, -1.564076696776861120, 1.105682177958314583 ) ) ;
#8740=CARTESIAN_POINT ( 'NONE',  ( -0.02244404828160087226, 6.946777552644228138, -2.784171975256703124 ) ) ;
#8741=CARTESIAN_POINT ( 'NONE',  ( 3.754321382136751595, -1.967203782747016128, -0.09899598954335629697 ) ) ;
#8742=CARTESIAN_POINT ( 'NONE',  ( 0.4047333657465709278, -2.105317319661216047, -0.2534319464195868843 ) ) ;
#8743=CARTESIAN_POINT ( 'NONE',  ( 2.360033908006432757, 0.7977434165707707470, 1.692156362554583460 ) ) ;
#8744=CARTESIAN_POINT ( 'NONE',  ( 5.619686913847246501, -1.681401280226066941, 0.3840984716911073349 ) ) ;
#8746=CARTESIAN_POINT ( 'NONE',  ( 2.666872310945223923, -1.521158656661812714, 1.599105504226288499 ) ) ;
#8749=CARTESIAN_POINT ( 'NONE',  ( 6.549272904993657995, 1.707534169505098953, -0.9658701945045378157 ) ) ;
#8756=CARTESIAN_POINT ( 'NONE',  ( 2.576698201331685922, 1.354182300986291887, -1.566139152919379107 ) ) ;
#8761=CARTESIAN_POINT ( 'NONE',  ( 6.604144390287855160, -0.9070803646254663732, 1.914764756563241965 ) ) ;
#8765=CARTESIAN_POINT ( 'NONE',  ( 6.877413162628407406, -0.1429737755889188000, 1.930079329684093237 ) ) ;
#8767=CARTESIAN_POINT ( 'NONE',  ( 5.431017465639029318, 0.9912489969874547224, 1.755499476546865445 ) ) ;
#8768=CARTESIAN_POINT ( 'NONE',  ( 4.909359874374886523, -1.816983420234472790, 0.6072180050544163654 ) ) ;
#8769=CARTESIAN_POINT ( 'NONE',  ( 2.349409277133751139, 0.5813161652389825518, -2.113004480973964760 ) ) ;
#8771=CARTESIAN_POINT ( 'NONE',  ( 2.584119536544440265, 1.026460374567798484, 1.613398670029235538 ) ) ;
#8774=CARTESIAN_POINT ( 'NONE',  ( 0.4742327405582689170, -2.001515332587662233, -0.2440062454662216829 ) ) ;
#8776=CARTESIAN_POINT ( 'NONE',  ( 3.210569733434172512, 1.891194753341999935, 0.8916721373675460249 ) ) ;
#8778=CARTESIAN_POINT ( 'NONE',  ( 2.397083457474056267, 1.331176160016230847, 1.096701253500545148 ) ) ;
#8790=CARTESIAN_POINT ( 'NONE',  ( 2.631291878999729938, -0.1756591012599724722, 1.802909387868474766 ) ) ;
#8795=CARTESIAN_POINT ( 'NONE',  ( 3.738735263490736926, 1.721172062854194218, 0.5650376532472713986 ) ) ;
#8796=CARTESIAN_POINT ( 'NONE',  ( 6.539320575229255361, 3.697401852651286180, 2.511149361313206096 ) ) ;
#8799=CARTESIAN_POINT ( 'NONE',  ( 4.017883236588020601, 1.847182159994051442, -0.2260418734564421939 ) ) ;
#8801=CARTESIAN_POINT ( 'NONE',  ( 1.317839660544089853, 0.9426401379578488449, -1.667518220840451981 ) ) ;
#8802=CARTESIAN_POINT ( 'NONE',  ( 1.184280053745472738, -1.780106929851841491, -0.4042017716930704219 ) ) ;
#8811=CARTESIAN_POINT ( 'NONE',  ( 5.981301965652664698, -0.05197358493889753933, 1.968944643851434639 ) ) ;
#8816=CARTESIAN_POINT ( 'NONE',  ( 0.9200049341780929257, 1.243975779098299927, -1.680105788963416780 ) ) ;
#8817=CARTESIAN_POINT ( 'NONE',  ( 6.545928648987922038, 0.7364953880720639390, -1.780233924599901929 ) ) ;
#8820=CARTESIAN_POINT ( 'NONE',  ( 1.606192798902779328, -0.6535759462080005244, -1.704761432720684144 ) ) ;
#8821=CARTESIAN_POINT ( 'NONE',  ( 2.948105999307056635, 0.7938017206191756436, -2.059354589195587337 ) ) ;
#8822=CARTESIAN_POINT ( 'NONE',  ( 0.5449873876890098945, 0.1430962203496731200, 1.907122450762772647 ) ) ;
#8823=CARTESIAN_POINT ( 'NONE',  ( 1.451539297965124264, 1.489159454907125646, 1.289083465231783299 ) ) ;
#8824=CARTESIAN_POINT ( 'NONE',  ( 3.122533544175498221, 0.05045625456868290531, 1.941573572215535393 ) ) ;
#8828=CARTESIAN_POINT ( 'NONE',  ( 6.297681919442434939, -1.347125180836796998, -1.284110876681610725 ) ) ;
#8833=CARTESIAN_POINT ( 'NONE',  ( 2.103317784989285677, -0.4765762082987561321, 2.138964651187735821 ) ) ;
#8836=CARTESIAN_POINT ( 'NONE',  ( 2.701551412915685457, -0.5726843992823158480, 1.733614832724015731 ) ) ;
#8839=CARTESIAN_POINT ( 'NONE',  ( 6.925078400183550364, 2.460400685555228950, 2.239421262742965268 ) ) ;
#8841=CARTESIAN_POINT ( 'NONE',  ( 1.576654987853912449, -1.829214484822901055, -0.6046830185306437677 ) ) ;
#8842=CARTESIAN_POINT ( 'NONE',  ( 5.576992410575341452, 1.811172876804711507, 0.7542287045681007607 ) ) ;
#8849=CARTESIAN_POINT ( 'NONE',  ( 5.629760504653214426, 1.996728726787128538, -0.5467053113129491937 ) ) ;
#8853=CARTESIAN_POINT ( 'NONE',  ( 4.834794202738506463, 0.7220915915403209873, -2.182417960738481710 ) ) ;
#8857=CARTESIAN_POINT ( 'NONE',  ( 0.1118211671861284034, -2.246746504121981403, 0.4537721782011410188 ) ) ;
#8860=CARTESIAN_POINT ( 'NONE',  ( 4.400292492776470610, 1.500370014523371154, -1.232902440404326727 ) ) ;
#8864=CARTESIAN_POINT ( 'NONE',  ( 5.783449990912790106, 0.1341079605299954347, -1.907733270042926810 ) ) ;
#8865=CARTESIAN_POINT ( 'NONE',  ( -0.02338929933905826986, 0.006294950389555685130, -1.710968156697996401 ) ) ;
#8866=CARTESIAN_POINT ( 'NONE',  ( 5.331267653506235327, -1.592659417495114083, -1.236803018183525449 ) ) ;
#8870=CARTESIAN_POINT ( 'NONE',  ( 1.464907584622468173, 0.1521959979720881595, -2.085151142678423497 ) ) ;
#8871=CARTESIAN_POINT ( 'NONE',  ( 6.907488038778298645, -0.3811802009726448226, 1.734239976993730670 ) ) ;
#8872=CARTESIAN_POINT ( 'NONE',  ( 5.695935454815424848, 1.779625283580280382, 0.9480427965274510482 ) ) ;
#8874=CARTESIAN_POINT ( 'NONE',  ( 2.625266749315146253, -2.138330473123546405, 0.8262727722977771805 ) ) ;
#8875=CARTESIAN_POINT ( 'NONE',  ( 2.009305037403839922, -0.8189296680943327633, -1.535607775426613086 ) ) ;
#8876=CARTESIAN_POINT ( 'NONE',  ( 2.672263739372262137, 2.109986773948614225, -0.2121620573234672125 ) ) ;
#8878=CARTESIAN_POINT ( 'NONE',  ( 2.143477642578191844, -0.07974179160761747653, -1.732128062886995057 ) ) ;
#8880=CARTESIAN_POINT ( 'NONE',  ( 2.049040314030759369, 1.621234533420016888, -0.9136741289750174300 ) ) ;
#8881=CARTESIAN_POINT ( 'NONE',  ( 2.242849641980674491, -2.128998374728574117, -0.4250897845002408193 ) ) ;
#8882=CARTESIAN_POINT ( 'NONE',  ( 3.485564796978508184, -0.5807542032013839339, 1.931124776463407189 ) ) ;
#8883=CARTESIAN_POINT ( 'NONE',  ( 5.125000000000002665, -2.052068128417943171, 3.046444613966958600E-13 ) ) ;
#8885=CARTESIAN_POINT ( 'NONE',  ( 0.6043602652519001195, -0.6458173669235712788, -1.815047198766789327 ) ) ;
#8887=CARTESIAN_POINT ( 'NONE',  ( 3.955514033904330873, -1.931546270572735979, 1.097109147590840550 ) ) ;
#8893=CARTESIAN_POINT ( 'NONE',  ( 6.135052730014136202, 2.072377209612641824, 0.8004311911904669063 ) ) ;
#8894=CARTESIAN_POINT ( 'NONE',  ( 4.879329150013382410, -0.09822140645733207220, 1.959542894978071992 ) ) ;
#8898=CARTESIAN_POINT ( 'NONE',  ( 5.923173471921922228, -0.06425113298673529316, 2.261675518886300473 ) ) ;
#8900=CARTESIAN_POINT ( 'NONE',  ( 2.031754214314248408, 1.974575511506712289, -0.5964607296059397656 ) ) ;
#8906=CARTESIAN_POINT ( 'NONE',  ( 4.428871017648271291, 0.08965458760558722706, 1.868499062828571367 ) ) ;
#8907=CARTESIAN_POINT ( 'NONE',  ( 3.129275142338799665, 0.4248101585269374869, 1.681139380183617194 ) ) ;
#8908=CARTESIAN_POINT ( 'NONE',  ( 2.559766225087984903, -1.198919528351283681, 1.261881593406234403 ) ) ;
#8909=CARTESIAN_POINT ( 'NONE',  ( 1.294905083876269236, 1.870644729521577565, -1.324771388537665961 ) ) ;
#8910=CARTESIAN_POINT ( 'NONE',  ( 0.9564373720404686363, 2.204146663617879476, -0.1098798544595935567 ) ) ;
#8911=CARTESIAN_POINT ( 'NONE',  ( 4.458587642939345841, -1.868375113230103857, -0.9383987773294580892 ) ) ;
#8912=CARTESIAN_POINT ( 'NONE',  ( 5.736261908918430130, 0.3809393362203088440, 1.904059320497718089 ) ) ;
#8915=CARTESIAN_POINT ( 'NONE',  ( 0.1412502902482688505, 0.7743183493036235321, 1.862015731718666078 ) ) ;
#8922=CARTESIAN_POINT ( 'NONE',  ( 4.705575438601840688, -0.4840451379145363497, 1.760283039881085809 ) ) ;
#8923=CARTESIAN_POINT ( 'NONE',  ( 1.659489206604364941, -1.893029981318217647, -1.133929415002648655 ) ) ;
#8928=CARTESIAN_POINT ( 'NONE',  ( 0.8615889817988997557, -1.594800366461980756, -1.239340803694780835 ) ) ;
#8932=CARTESIAN_POINT ( 'NONE',  ( 3.379601846096703888, -1.794663673993960540, 0.4920686967917423105 ) ) ;
#8939=CARTESIAN_POINT ( 'NONE',  ( 3.773894676421325478, 1.015518775504126614, 1.516979517045339509 ) ) ;
#8943=CARTESIAN_POINT ( 'NONE',  ( 6.872432811717262169, -0.4447407475622888740, 1.973694069355651282 ) ) ;
#8944=CARTESIAN_POINT ( 'NONE',  ( 6.175717916360309090, -0.9808100270635997653, 1.557957644481674730 ) ) ;
#8945=CARTESIAN_POINT ( 'NONE',  ( 4.336755680664809098, 2.262710760593138470, 0.4526611301470875870 ) ) ;
#8947=CARTESIAN_POINT ( 'NONE',  ( 0.4564140224992017658, 0.7863226074062683590, 1.905069713448727775 ) ) ;
#8951=CARTESIAN_POINT ( 'NONE',  ( 5.343244854357415363, -1.283103863925443955, 1.906741504182138502 ) ) ;
#8955=CARTESIAN_POINT ( 'NONE',  ( 6.244977087980838171, -1.579202250953464670, 1.002420361074819688 ) ) ;
#8958=CARTESIAN_POINT ( 'NONE',  ( 2.724755696555291262, 1.382288352666941389, -1.321784923088549446 ) ) ;
#8960=CARTESIAN_POINT ( 'NONE',  ( 3.967548030458594166, 0.2710504330169676845, -2.190103208553782821 ) ) ;
#8961=CARTESIAN_POINT ( 'NONE',  ( 4.733676700703519202, 0.6609272643324247687, -2.011644693266708916 ) ) ;
#8963=CARTESIAN_POINT ( 'NONE',  ( 6.883263157960373135, 0.5713788194823016253, 2.097868537683903245 ) ) ;
#8964=CARTESIAN_POINT ( 'NONE',  ( -0.2110808730067326444, 2.048707873362776599, -2.213945011526836204 ) ) ;
#8968=CARTESIAN_POINT ( 'NONE',  ( 2.854834436329793057, 0.7764391075696615019, 2.173172238055173455 ) ) ;
#8969=CARTESIAN_POINT ( 'NONE',  ( 3.156644782993088150, -0.5669402238272451822, -1.878178299617596192 ) ) ;
#8971=CARTESIAN_POINT ( 'NONE',  ( 6.948098685450462497, -0.8862217868219750549, 1.860397500250488001 ) ) ;
#8975=CARTESIAN_POINT ( 'NONE',  ( 5.067592334412735156, 1.357865985192594271, 1.490972259599515848 ) ) ;
#8980=CARTESIAN_POINT ( 'NONE',  ( 1.516727516949545107, 0.8775410692131856427, 1.985969635014148915 ) ) ;
#8981=FACE_OUTER_BOUND ( 'NONE', #67316, .T. ) ;
#8985=CARTESIAN_POINT ( 'NONE',  ( 0.6673476085290538373, 0.2044725723429566266, -2.050631486922994906 ) ) ;
#8986=CARTESIAN_POINT ( 'NONE',  ( 0.07775346131142897577, 1.984126704040774181, -2.702190870904349840 ) ) ;
#8991=CARTESIAN_POINT ( 'NONE',  ( 3.668532269402470458, 0.6909111621477401766, 1.783275653667259597 ) ) ;
#8992=CARTESIAN_POINT ( 'NONE',  ( 5.172599881030584434, -1.667270648082047835, -0.5941068299562983768 ) ) ;
#8996=CARTESIAN_POINT ( 'NONE',  ( -0.2236198635829286518, -0.4190533842500678841, -1.875677477222786438 ) ) ;
#8998=CARTESIAN_POINT ( 'NONE',  ( 0.9946828900261883710, 2.039433816042154124, 0.3556643922909968891 ) ) ;
#9000=CARTESIAN_POINT ( 'NONE',  ( 6.227412191919261986, -1.760757567598171480, 0.6321290105378990498 ) ) ;
#9001=CARTESIAN_POINT ( 'NONE',  ( 2.068725586703868746, -1.668841220716179130, -0.7407507213199536755 ) ) ;
#9002=CARTESIAN_POINT ( 'NONE',  ( 5.514374426699260923, -0.9893691592960799364, -1.972764877262770833 ) ) ;
#9005=CARTESIAN_POINT ( 'NONE',  ( 3.367685602802727551, -0.4050715705573506575, 2.022353529335896294 ) ) ;
#9009=CARTESIAN_POINT ( 'NONE',  ( 0.7730135719010817752, -2.035059957909639561, -0.7290066412228360937 ) ) ;
#9011=CARTESIAN_POINT ( 'NONE',  ( 5.793440749948310042, -1.873300974885267589, 0.8818263447485861217 ) ) ;
#9013=CARTESIAN_POINT ( 'NONE',  ( 3.761131992884462871, -1.904433681825665969, -1.022602951024270679 ) ) ;
#9015=CARTESIAN_POINT ( 'NONE',  ( 3.123699121837515413, -0.3918110498563053268, 1.981120561552232262 ) ) ;
#9016=CARTESIAN_POINT ( 'NONE',  ( 2.242563829109287088, -1.923402688547710904, -0.3857071251459272543 ) ) ;
#9017=CARTESIAN_POINT ( 'NONE',  ( 6.720655732516655156, 7.629137130509086262, 2.673739711112704143 ) ) ;
#9025=CARTESIAN_POINT ( 'NONE',  ( 1.622280145275534435, 1.995268681201247452, 0.2910785328335343536 ) ) ;
#9027=CARTESIAN_POINT ( 'NONE',  ( 6.251546423958430410, 2.185849743821382862, -0.1592787069685034917 ) ) ;
#9030=CARTESIAN_POINT ( 'NONE',  ( 6.099862406061942188, 1.323743610676546334, 1.380425988546908567 ) ) ;
#9034=CARTESIAN_POINT ( 'NONE',  ( 3.269157808572686896, 1.821735364950356484, -0.8647411805496332260 ) ) ;
#9037=CARTESIAN_POINT ( 'NONE',  ( -0.02338929933905826986, 0.006294950389555685130, -1.710968156697996401 ) ) ;
#9041=CARTESIAN_POINT ( 'NONE',  ( 4.253091631423633778, -1.553859266942819284, -1.041061106808522929 ) ) ;
#9042=ADVANCED_FACE ( 'NONE', ( #44812 ), #63180, .T. ) ;
#9044=CARTESIAN_POINT ( 'NONE',  ( 0.6903901511902330590, 1.067356595782501749, -1.773781848916009096 ) ) ;
#9049=CARTESIAN_POINT ( 'NONE',  ( 0.1580966392830873424, 1.806712829659435027, 0.1331060069221217668 ) ) ;
#9055=CARTESIAN_POINT ( 'NONE',  ( 1.680054527999317759, -1.087118939145682583, -1.632918184844594611 ) ) ;
#9057=CARTESIAN_POINT ( 'NONE',  ( 6.591422782704708716, -0.4110296003016626898, 1.877638232857116174 ) ) ;
#9064=CARTESIAN_POINT ( 'NONE',  ( 2.641676655999642076, -1.601130012699041982, -1.452526871000489495 ) ) ;
#9069=CARTESIAN_POINT ( 'NONE',  ( 6.036143291503483610, 0.8974207610169572247, -1.589712159477923992 ) ) ;
#9071=CARTESIAN_POINT ( 'NONE',  ( 1.387891646316425476, -0.8902153388929586741, 1.759007621864362214 ) ) ;
#9072=CARTESIAN_POINT ( 'NONE',  ( 4.060738401289211374, 0.5150538496448524572, 1.841637258418599155 ) ) ;
#9075=CARTESIAN_POINT ( 'NONE',  ( 5.389095231685527843, 0.1428881311146198430, 1.964408359074652388 ) ) ;
#9077=CARTESIAN_POINT ( 'NONE',  ( 6.269086997039995168, 1.857158234874217939, -0.5679118324898363435 ) ) ;
#9083=CARTESIAN_POINT ( 'NONE',  ( 4.107995242876061326, -0.7289348763114507079, 1.768098669557085056 ) ) ;
#9085=CARTESIAN_POINT ( 'NONE',  ( 0.09513611692719620150, -0.4880922032983874281, -2.160105283315366442 ) ) ;
#9087=CARTESIAN_POINT ( 'NONE',  ( 6.252595736715376162, 1.991502868314236174, 0.2931975281106109499 ) ) ;
#9089=CARTESIAN_POINT ( 'NONE',  ( 6.305291373979138747, 1.520805759102667132, 1.009792402853857407 ) ) ;
#9090=CARTESIAN_POINT ( 'NONE',  ( 1.732962091629593804, -1.965256999408044436, -0.6514315320021792921 ) ) ;
#9095=CARTESIAN_POINT ( 'NONE',  ( 6.244977087980838171, -1.579202250953464670, 1.002420361074819688 ) ) ;
#9097=FILL_AREA_STYLE ('',( #178013 ) ) ;
#9101=CARTESIAN_POINT ( 'NONE',  ( 6.825078400183581806, 2.095667212029386661, 2.065897939415714646 ) ) ;
#9103=CARTESIAN_POINT ( 'NONE',  ( 5.010307813345768579, -1.644221866518974728, 0.5513857468827707553 ) ) ;
#9105=CARTESIAN_POINT ( 'NONE',  ( 2.747004861044194612, -0.3495022371792326221, -2.040372298647576965 ) ) ;
#9106=CARTESIAN_POINT ( 'NONE',  ( 3.216528272283057710, 2.066224784428410732, 0.4612988732951432969 ) ) ;
#9109=CARTESIAN_POINT ( 'NONE',  ( 2.026157484158600752, 1.007934145216189625, 1.691802187876802810 ) ) ;
#9113=CARTESIAN_POINT ( 'NONE',  ( 3.925942518080671739, 1.227467849647005282, -1.935749465030587313 ) ) ;
#9114=CARTESIAN_POINT ( 'NONE',  ( 2.332394550857110893, 1.770734860448031300, 0.4440693575865002907 ) ) ;
#9115=AXIS2_PLACEMENT_3D ( 'NONE', #185231, #165004, #168998 ) ;
#9119=CARTESIAN_POINT ( 'NONE',  ( 2.812746579430201788, -0.5882912493809470122, -1.925304731621484633 ) ) ;
#9120=CARTESIAN_POINT ( 'NONE',  ( 2.553501467334079678, 1.513274546892771966, 1.248348448719404757 ) ) ;
#9124=CARTESIAN_POINT ( 'NONE',  ( 4.541018360983569480, -1.615799657739678263, -1.326631217474142366 ) ) ;
#9125=CARTESIAN_POINT ( 'NONE',  ( 4.522157790900214636, 1.087963700580677484, -1.395837783952274647 ) ) ;
#9128=CARTESIAN_POINT ( 'NONE',  ( 0.4983068789779531160, -0.7420642642406435341, -2.062120472104383317 ) ) ;
#9129=CARTESIAN_POINT ( 'NONE',  ( 5.525286087770139964, -1.108758243214434724, -1.341423578285575235 ) ) ;
#9132=CARTESIAN_POINT ( 'NONE',  ( 6.012345284929816458, -2.165844811509042511, 0.7704031996330994447 ) ) ;
#9134=CARTESIAN_POINT ( 'NONE',  ( 6.046190555029876457, 1.600718489819895174, -0.6667736897630163195 ) ) ;
#9135=CARTESIAN_POINT ( 'NONE',  ( 6.385953923436008317, -2.015982004707029596, 0.05432014494890363698 ) ) ;
#9136=CARTESIAN_POINT ( 'NONE',  ( 6.268071979561871565, -2.155543878041016992, 0.2595383615264702515 ) ) ;
#9138=CARTESIAN_POINT ( 'NONE',  ( 0.4798920220053382590, -0.7558346266652364864, 1.978032726644059158 ) ) ;
#9139=CARTESIAN_POINT ( 'NONE',  ( 4.031250000000002665, -0.7852924748301974844, -1.895863743163994863 ) ) ;
#9141=CARTESIAN_POINT ( 'NONE',  ( 4.788067677947292822, -0.9085903742032475083, 1.698673095886160000 ) ) ;
#9143=CARTESIAN_POINT ( 'NONE',  ( 1.032228388637240313, -2.166051452891520679, 0.4916964420428306948 ) ) ;
#9148=CARTESIAN_POINT ( 'NONE',  ( 3.159039748919801216, 0.5414197367904579616, 2.154182169225922205 ) ) ;
#9152=CARTESIAN_POINT ( 'NONE',  ( 0.6334356698059575574, 0.5880228326464317368, 1.928751028484784413 ) ) ;
#9154=CARTESIAN_POINT ( 'NONE',  ( 0.4970291366834606039, 0.3490122959711927098, 2.032667101136710563 ) ) ;
#9159=CARTESIAN_POINT ( 'NONE',  ( 0.8777613430710672349, -0.9896981104785051997, 1.466914328529956180 ) ) ;
#9160=CARTESIAN_POINT ( 'NONE',  ( 0.3346115673153668424, 0.6298721381652396811, -1.915601020889952322 ) ) ;
#9161=CARTESIAN_POINT ( 'NONE',  ( 5.319757424029775805, 1.030549729363830158, -1.402388650165889095 ) ) ;
#9162=CARTESIAN_POINT ( 'NONE',  ( 4.441175045773351648, -1.771670475836329306, -1.454733398674179945 ) ) ;
#9164=CARTESIAN_POINT ( 'NONE',  ( 1.904012794591736668, 1.364881752761820222, -1.235849761865935870 ) ) ;
#9167=CARTESIAN_POINT ( 'NONE',  ( 2.801551268311212262, -0.5745519774189576934, 1.732868645247707562 ) ) ;
#9168=CARTESIAN_POINT ( 'NONE',  ( 4.096327398540238640, -0.3419367296172080017, 1.987046374476949095 ) ) ;
#9170=CARTESIAN_POINT ( 'NONE',  ( 1.780510834742056847, -1.209543565243664798, 1.911899112700167880 ) ) ;
#9171=CARTESIAN_POINT ( 'NONE',  ( 0.07680821025393690105, 0.005952109439256307241, -1.810863387344714193 ) ) ;
#9172=CARTESIAN_POINT ( 'NONE',  ( 5.983450976520548359, 1.947180606154915727, -0.8027177699698545554 ) ) ;
#9174=CARTESIAN_POINT ( 'NONE',  ( 2.277862540309500083, -2.008769142935047380, 0.5008063122204224893 ) ) ;
#9177=CARTESIAN_POINT ( 'NONE',  ( 4.389387035479824561, -0.001039498178659337352, -2.120667954306009406 ) ) ;
#9182=CARTESIAN_POINT ( 'NONE',  ( 1.260239703848411441, 0.7801416839768731126, 1.761649912542123664 ) ) ;
#9189=CARTESIAN_POINT ( 'NONE',  ( 5.906510592826289319, -2.110524776404258507, -0.2060971850248518311 ) ) ;
#9190=CARTESIAN_POINT ( 'NONE',  ( 2.344876439239967247, 0.4604487725310001389, 2.054841016598129233 ) ) ;
#9193=CARTESIAN_POINT ( 'NONE',  ( 6.702007135557183304, 0.7127468228822000373, -1.719244972783180225 ) ) ;
#9198=CARTESIAN_POINT ( 'NONE',  ( 0.3871773095200456982, -1.998849835692744659, -0.7086421328065874992 ) ) ;
#9201=CARTESIAN_POINT ( 'NONE',  ( 3.701569118832209515, -1.483977648892897960, -1.283320388228793130 ) ) ;
#9202=CARTESIAN_POINT ( 'NONE',  ( 1.938557520917514987, 2.138169252768943984, 0.3173444169591658204 ) ) ;
#9206=CARTESIAN_POINT ( 'NONE',  ( 3.046520963529773862, -1.423092868940859956, -1.001465238821471315 ) ) ;
#9211=CARTESIAN_POINT ( 'NONE',  ( 1.880232294074701604, -0.2495702131940503166, 2.000550610736757218 ) ) ;
#9214=CARTESIAN_POINT ( 'NONE',  ( 2.588696453722662660, -0.3354253448964693574, -1.942569732146891770 ) ) ;
#9215=CARTESIAN_POINT ( 'NONE',  ( 5.713130151434068438, 1.559639147136464343, -1.106415316399149473 ) ) ;
#9220=CARTESIAN_POINT ( 'NONE',  ( 2.455728411619819251, -1.498007593246965419, -1.354850333784217709 ) ) ;
#9222=CARTESIAN_POINT ( 'NONE',  ( 5.667085135620930636, -2.082984650255703230, -0.9933455750401504192 ) ) ;
#9223=CARTESIAN_POINT ( 'NONE',  ( 6.637165056451467038, -0.09505199798197358496, -1.959668910398344233 ) ) ;
#9225=CARTESIAN_POINT ( 'NONE',  ( 3.450005804356533812, -0.7992637590314204399, 1.791754569076028147 ) ) ;
#9227=CARTESIAN_POINT ( 'NONE',  ( 0.5982800022500452952, -0.2930678230431381648, 1.994870242743536304 ) ) ;
#9229=CARTESIAN_POINT ( 'NONE',  ( 2.220046512049120846, 0.9935532346000598425, -1.869724544471425665 ) ) ;
#9232=CARTESIAN_POINT ( 'NONE',  ( 2.431387202150553151, 0.8680758514147070004, -1.623638265414374171 ) ) ;
#9236=CARTESIAN_POINT ( 'NONE',  ( 3.392942708002244068, -2.044739723715986113, -0.5619712599038150236 ) ) ;
#9240=CARTESIAN_POINT ( 'NONE',  ( 3.989569841107299286, 1.489977244407629131, 1.423887585670815747 ) ) ;
#9242=CARTESIAN_POINT ( 'NONE',  ( 1.469984750362408388, -1.748608032326857353, -0.5769476384821782267 ) ) ;
#9244=CARTESIAN_POINT ( 'NONE',  ( -0.02224634325197898804, 1.983040877609225872, -2.702260234736663325 ) ) ;
#9248=CARTESIAN_POINT ( 'NONE',  ( 1.032169062358662348, -1.402649970393770484, -1.703791656331831605 ) ) ;
#9249=CARTESIAN_POINT ( 'NONE',  ( 2.372703478119597698, -1.393307465234068898, 1.782356930206913770 ) ) ;
#9251=CARTESIAN_POINT ( 'NONE',  ( 4.007922362044618048, -0.6876924770315288038, 1.676191166192544157 ) ) ;
#9252=CARTESIAN_POINT ( 'NONE',  ( 3.221808243886138179, 0.8566008913209141040, -1.713579649959365403 ) ) ;
#9253=CARTESIAN_POINT ( 'NONE',  ( 4.123533666479628046, 0.2564666318346648377, -2.054367117340555549 ) ) ;
#9256=CARTESIAN_POINT ( 'NONE',  ( 3.291827724629258434, -0.8003651471039547882, 1.801871540228771273 ) ) ;
#9257=CARTESIAN_POINT ( 'NONE',  ( 0.5340448022827409824, 0.9932739084477918423, -1.650449964952714454 ) ) ;
#9258=CARTESIAN_POINT ( 'NONE',  ( 4.240975883383619305, -1.627667033997456381, 0.9218181776217827528 ) ) ;
#9259=CARTESIAN_POINT ( 'NONE',  ( 2.807580367715529324, 1.950013211217585196, 1.233794411958085036 ) ) ;
#9260=CARTESIAN_POINT ( 'NONE',  ( 3.455356687279837136, 1.465577529964179115, 1.146850193174092203 ) ) ;
#9265=CARTESIAN_POINT ( 'NONE',  ( 1.119907265981748168, -2.054334215221398807, 0.4631877017708794231 ) ) ;
#9269=CARTESIAN_POINT ( 'NONE',  ( 2.355864820516640812, -1.574449018071517825, -1.420800595792824028 ) ) ;
#9270=CARTESIAN_POINT ( 'NONE',  ( 6.235022398275627431, 1.885252722396244085, 0.7250032809389771460 ) ) ;
#9275=CARTESIAN_POINT ( 'NONE',  ( 1.370646902836635261, -1.372427557409527488, 1.669970663979184256 ) ) ;
#9278=CARTESIAN_POINT ( 'NONE',  ( 6.925078400183523719, 3.697131557392329348, 2.469975972695995559 ) ) ;
#9281=CARTESIAN_POINT ( 'NONE',  ( 4.751185534883737738, 0.1928377863454934504, -2.007255887737584121 ) ) ;
#9285=CARTESIAN_POINT ( 'NONE',  ( 0.4622851218389683603, 2.237382594954186565, -0.3354954470186234383 ) ) ;
#9289=CARTESIAN_POINT ( 'NONE',  ( 0.4213150654816185114, -1.355317750890722595, -1.354022888547769421 ) ) ;
#9293=CARTESIAN_POINT ( 'NONE',  ( 2.929983995618768322, 0.9579465210916816575, -1.434183166407378307 ) ) ;
#9296=CARTESIAN_POINT ( 'NONE',  ( 1.457869587114325460, 0.7109265171535653627, 1.620852848218183873 ) ) ;
#9297=CARTESIAN_POINT ( 'NONE',  ( 1.963540897105001459, -1.618223010570983611, -1.197281337589267247 ) ) ;
#9299=CARTESIAN_POINT ( 'NONE',  ( 4.647634198631804381, -1.703412986257560879, -1.402924735643434673 ) ) ;
#9303=CARTESIAN_POINT ( 'NONE',  ( 4.090573159264241809, -1.219870178150096462, 1.734285844867427651 ) ) ;
#9304=CARTESIAN_POINT ( 'NONE',  ( 2.671500097371417137, 1.427951006967288272, 1.423949442620517480 ) ) ;
#9305=CARTESIAN_POINT ( 'NONE',  ( 3.480526544955347301, -1.212856340575025005, 1.345865543471187253 ) ) ;
#9309=CARTESIAN_POINT ( 'NONE',  ( 0.4791068267422092797, 1.747065859276742072, -0.6691465683838908607 ) ) ;
#9311=CARTESIAN_POINT ( 'NONE',  ( 6.076747101522134820, -1.735163100867884500, -0.5679748894881069265 ) ) ;
#9313=CARTESIAN_POINT ( 'NONE',  ( 2.852642732684606663, -1.771934378248109399, -0.7286688389312511172 ) ) ;
#9322=CARTESIAN_POINT ( 'NONE',  ( 3.463236921083117537, -1.731491641549892213, 1.224000437801610941 ) ) ;
#9323=CARTESIAN_POINT ( 'NONE',  ( -0.1294898018152357000, 1.363479816416721446, -2.179679775322340696 ) ) ;
#9325=CARTESIAN_POINT ( 'NONE',  ( 4.868415619454742327, -1.289772430030609707, 1.490937899079747497 ) ) ;
#9327=CARTESIAN_POINT ( 'NONE',  ( -0.03490996608559569087, -1.614503017106348581, 1.202435150695363664 ) ) ;
#9328=ORIENTED_EDGE ( 'NONE', *, *, #198303, .F. ) ;
#9330=CARTESIAN_POINT ( 'NONE',  ( 6.280470216940358341, -0.5666190470481970998, -2.040018813895160044 ) ) ;
#9332=CARTESIAN_POINT ( 'NONE',  ( 1.557173632797459684, 1.693725193156172315, -1.190412882225246438 ) ) ;
#9333=CARTESIAN_POINT ( 'NONE',  ( 2.185399619353834311, -0.8303394849570409075, 1.755606585091240568 ) ) ;
#9336=CARTESIAN_POINT ( 'NONE',  ( 3.292999148915674468, 1.648261854606505983, 1.285964787075925431 ) ) ;
#9339=CARTESIAN_POINT ( 'NONE',  ( 0.9436867518335406713, -1.148578278726499757, -1.400746029399003501 ) ) ;
#9341=CARTESIAN_POINT ( 'NONE',  ( 5.444034239667132624, 0.8972360612293399651, -2.016436982482258333 ) ) ;
#9343=CARTESIAN_POINT ( 'NONE',  ( 4.594872931952145301, -0.4798491958124780910, -2.153818993410236970 ) ) ;
#9347=CARTESIAN_POINT ( 'NONE',  ( 2.842330330863319876, 1.060513762474508015, -1.591057744338888913 ) ) ;
#9349=CARTESIAN_POINT ( 'NONE',  ( 5.635237798060349412, -0.04710594754482424346, -2.069988403558701062 ) ) ;
#9351=CARTESIAN_POINT ( 'NONE',  ( 2.448304249002517974, 2.161202317112873139, 0.05382173394478938222 ) ) ;
#9352=CARTESIAN_POINT ( 'NONE',  ( 4.845371438081495619, 0.6875289519675978900, -2.081009137124201658 ) ) ;
#9362=CARTESIAN_POINT ( 'NONE',  ( 6.157099584139436033, 1.695871835526874483, -1.187180358042688511 ) ) ;
#9363=CARTESIAN_POINT ( 'NONE',  ( 4.652910101842601343, -1.546415465631932884, 1.148725279867918170 ) ) ;
#9364=CARTESIAN_POINT ( 'NONE',  ( -0.1351500440973339712, -0.1486198258836557429, -1.983738523497140305 ) ) ;
#9368=CARTESIAN_POINT ( 'NONE',  ( 5.436368237181718577, -1.097297496841664444, 1.635214795183062675 ) ) ;
#9369=CARTESIAN_POINT ( 'NONE',  ( 0.02373106683711476844, -1.352142385343929387, -1.725327757841053078 ) ) ;
#9370=CARTESIAN_POINT ( 'NONE',  ( 5.232948167349782409, 0.1380416123818763163, 1.820529236867339584 ) ) ;
#9376=CARTESIAN_POINT ( 'NONE',  ( 3.034521004542716227, -1.622529355458858236, 0.8704296449140033198 ) ) ;
#9377=CARTESIAN_POINT ( 'NONE',  ( 6.533470335063485734, -0.1341179537190802518, 1.982235210812468340 ) ) ;
#9378=CARTESIAN_POINT ( 'NONE',  ( 0.5975257653535933633, 1.179397575757964001, -1.972621981072789410 ) ) ;
#9379=CARTESIAN_POINT ( 'NONE',  ( 6.912952593004609625, -1.518390278170888008, 1.241885805282373134 ) ) ;
#9385=CARTESIAN_POINT ( 'NONE',  ( 3.140259756110568734, 0.5104685904834010968, 2.027328384984484533 ) ) ;
#9386=CARTESIAN_POINT ( 'NONE',  ( 1.059204734455133412, 0.3686402435371800013, -1.833797362824276078 ) ) ;
#9387=CARTESIAN_POINT ( 'NONE',  ( 1.458361007166041334, 1.524808354686446821, 1.319028796778199730 ) ) ;
#9390=CARTESIAN_POINT ( 'NONE',  ( 2.032363155619838935, -1.554395792557780487, 0.7831100076771575491 ) ) ;
#9394=CARTESIAN_POINT ( 'NONE',  ( 3.281609485064349130, 1.095178418435642120, 1.332575575002497681 ) ) ;
#9395=CARTESIAN_POINT ( 'NONE',  ( 3.245827600587628758, 2.191739723504753101, -0.002129563554123526260 ) ) ;
#9396=CARTESIAN_POINT ( 'NONE',  ( 5.127635347277352373, -2.096377701570474539, 0.6897739467496829535 ) ) ;
#9400=CARTESIAN_POINT ( 'NONE',  ( 2.694371920525945097, 1.027083080403013993, -1.912793749723267211 ) ) ;
#9401=CARTESIAN_POINT ( 'NONE',  ( 0.9788029507734037349, -0.04229004422508231970, -1.825371421953936757 ) ) ;
#9402=CARTESIAN_POINT ( 'NONE',  ( 3.573546900796530146, 1.536558363836796337, 1.457006447099787882 ) ) ;
#9405=CARTESIAN_POINT ( 'NONE',  ( 3.773197156129989516, 2.158245952819247471, -0.7729258541082913991 ) ) ;
#9410=CARTESIAN_POINT ( 'NONE',  ( 5.496814983966967993, -2.166796134289544984, -0.4884321829702345519 ) ) ;
#9416=CARTESIAN_POINT ( 'NONE',  ( 4.307267641921147749, 1.238321930042911578, -1.591317616567271775 ) ) ;
#9418=CARTESIAN_POINT ( 'NONE',  ( 3.590735542246026313, 2.011259174285257689, 0.4565010432640480564 ) ) ;
#9423=CARTESIAN_POINT ( 'NONE',  ( 5.912113082354764515, 1.474260358680115068, -1.621598248542432064 ) ) ;
#9424=CARTESIAN_POINT ( 'NONE',  ( 3.305314717767214638, 1.277042846462652204, -1.560500556308255238 ) ) ;
#9425=CARTESIAN_POINT ( 'NONE',  ( 2.331387312403776946, 0.8663521307504215008, -1.624669977836174839 ) ) ;
#9428=CARTESIAN_POINT ( 'NONE',  ( 6.440460073785046369, 1.806197173870389694, 0.2645596887278709453 ) ) ;
#9429=CARTESIAN_POINT ( 'NONE',  ( 0.3526649539562948243, 0.2173941373411722999, -2.288394520000771148 ) ) ;
#9431=CARTESIAN_POINT ( 'NONE',  ( 6.819229412991756334, -0.1648141603832406210, 2.226593352680195537 ) ) ;
#9432=CARTESIAN_POINT ( 'NONE',  ( 2.033940956955893498, -1.376631898319637726, -1.593950314443808969 ) ) ;
#9441=CARTESIAN_POINT ( 'NONE',  ( 4.412477314457364130, -2.220925182493800776, -0.05286738749475486387 ) ) ;
#9442=CARTESIAN_POINT ( 'NONE',  ( 0.2587985324217950689, 0.8487602207661277820, 2.037339956011212649 ) ) ;
#9445=CARTESIAN_POINT ( 'NONE',  ( 4.246505328441081417, -1.940195102956907336, -0.2900488188990399396 ) ) ;
#9453=CARTESIAN_POINT ( 'NONE',  ( 3.551138032611600437, 0.3147205237276836653, 2.097014573754731881 ) ) ;
#9455=CARTESIAN_POINT ( 'NONE',  ( 5.225516498768126183, -2.053876642077703707, 0.6744380372525200507 ) ) ;
#9456=CARTESIAN_POINT ( 'NONE',  ( 3.895923546780861724, -0.5813109859279728120, -1.747131793041277970 ) ) ;
#9457=CARTESIAN_POINT ( 'NONE',  ( 5.173064673083394460, 1.776168143800487043, -0.9548534231369476544 ) ) ;
#9460=CARTESIAN_POINT ( 'NONE',  ( 6.714805129994689814, -0.1247508129638870145, 1.711716247594262441 ) ) ;
#9461=CARTESIAN_POINT ( 'NONE',  ( 6.727182134110180733, 7.053024033604696541, 2.509100769544295950 ) ) ;
#9465=CARTESIAN_POINT ( 'NONE',  ( 3.661132068870280420, -1.905464569931826446, -1.020879743040298271 ) ) ;
#9466=CARTESIAN_POINT ( 'NONE',  ( 5.554064478179312481, 1.779353385700060075, -0.9478964821433707444 ) ) ;
#9468=CARTESIAN_POINT ( 'NONE',  ( 3.274459119871219848, -1.289031633699176949, 1.735169069618908821 ) ) ;
#9469=CARTESIAN_POINT ( 'NONE',  ( 3.567610853275906546, 1.924076846980572464, -0.4285291244595054727 ) ) ;
#9471=CARTESIAN_POINT ( 'NONE',  ( 1.413547897872836856, 2.036140070965312354, 1.085889434398391584 ) ) ;
#9472=CARTESIAN_POINT ( 'NONE',  ( 3.075518034276482293, 1.957894989606956182, -0.6432953703794060951 ) ) ;
#9473=CARTESIAN_POINT ( 'NONE',  ( 5.144061591681034606, 0.5672955765679200679, 1.857344180792292354 ) ) ;
#9482=CARTESIAN_POINT ( 'NONE',  ( 2.626236979526615389, -1.269917727785064843, -1.804575601930514139 ) ) ;
#9484=CARTESIAN_POINT ( 'NONE',  ( 6.034033239799157400, 1.165729394902741189, 1.577711426528668692 ) ) ;
#9485=CARTESIAN_POINT ( 'NONE',  ( 6.539320575229278454, 0.5749733277502915296, 2.156147827957733742 ) ) ;
#9491=CARTESIAN_POINT ( 'NONE',  ( 5.771403949166884040, 1.100151190403714452, 1.476150860297697154 ) ) ;
#9493=CARTESIAN_POINT ( 'NONE',  ( 2.500915792353772815, 1.655931770628838784, -1.226644000274518476 ) ) ;
#9500=CARTESIAN_POINT ( 'NONE',  ( 1.129840139894950246, -1.306895429219852467, -1.593522927358894004 ) ) ;
#9502=CARTESIAN_POINT ( 'NONE',  ( 2.031498134000471190, 1.782053568523461751, -0.5365169527500669444 ) ) ;
#9503=CARTESIAN_POINT ( 'NONE',  ( 4.370544011308346910, -0.004580445953385886559, -1.841430844414258861 ) ) ;
#9509=CARTESIAN_POINT ( 'NONE',  ( 4.143358556170802842, -1.920740624720223666, 1.086653567583625746 ) ) ;
#9510=CARTESIAN_POINT ( 'NONE',  ( 0.7378453340087381962, -1.528073262844112268, -1.529135702860604074 ) ) ;
#9512=CARTESIAN_POINT ( 'NONE',  ( -0.1757481403069499348, -0.8193859263425256056, -1.726394157293544840 ) ) ;
#9513=CARTESIAN_POINT ( 'NONE',  ( -0.1003747550864658999, -1.976661868047492998, 0.3981153667176607902 ) ) ;
#9516=CARTESIAN_POINT ( 'NONE',  ( 5.285773936917006921, 1.841837585529454202, -0.5139651673399318055 ) ) ;
#9517=CARTESIAN_POINT ( 'NONE',  ( 1.234984068473435892, -1.692697435815498919, 0.7966027930108383615 ) ) ;
#9519=CARTESIAN_POINT ( 'NONE',  ( 2.272673044126482189, -0.3494851828299732621, -1.985868527484459634 ) ) ;
#9521=CARTESIAN_POINT ( 'NONE',  ( 3.756553094297815143, 0.7580258897690328457, 1.965105124105433809 ) ) ;
#9526=CARTESIAN_POINT ( 'NONE',  ( 4.095966777872499520, 1.322572826423114911, 1.526597406435834081 ) ) ;
#9529=CARTESIAN_POINT ( 'NONE',  ( 4.341216920475977403, -1.883070171734081200, 1.061215411333437109 ) ) ;
#9534=CARTESIAN_POINT ( 'NONE',  ( 1.996751263802678533, 2.147379752972265354, 0.3199099038852480370 ) ) ;
#9537=CARTESIAN_POINT ( 'NONE',  ( 1.135996871135702024, 0.3593859243370273182, 1.805655672011026391 ) ) ;
#9539=CARTESIAN_POINT ( 'NONE',  ( 3.685266855566126321, 1.588411730319793769, 1.510178839762461811 ) ) ;
#9541=CARTESIAN_POINT ( 'NONE',  ( 4.188523121243816760, -2.237390873258153778, -0.3355513299154490592 ) ) ;
#9548=CARTESIAN_POINT ( 'NONE',  ( 4.850734264762338377, -1.421546097138610243, 1.053919008203674013 ) ) ;
#9551=CARTESIAN_POINT ( 'NONE',  ( 1.149603698739794400, -1.659950780972534012, -1.295870271070469260 ) ) ;
#9554=CARTESIAN_POINT ( 'NONE',  ( 0.7308274648059713829, -1.853293357156562404, -0.6670056901108140091 ) ) ;
#9560=CARTESIAN_POINT ( 'NONE',  ( 4.961713530105988923, 1.850188064717460223, -0.2750520410098392654 ) ) ;
#9561=CARTESIAN_POINT ( 'NONE',  ( 4.434477146351770926, -1.196200190851111511, 1.689492296227592893 ) ) ;
#9570=CARTESIAN_POINT ( 'NONE',  ( 3.894932841003693191, 0.2855096342280309396, 1.940843471192068570 ) ) ;
#9571=CARTESIAN_POINT ( 'NONE',  ( 2.073592080879012478, 1.495823877299466087, -1.351946161731142126 ) ) ;
#9574=CARTESIAN_POINT ( 'NONE',  ( 0.8427765623921362748, -1.607460297381148928, 0.9563107477488577146 ) ) ;
#9576=CARTESIAN_POINT ( 'NONE',  ( 3.463142787923169763, -1.643428793820296718, 1.162544664348450496 ) ) ;
#9578=CARTESIAN_POINT ( 'NONE',  ( 3.216528272283057710, 2.066224784428410732, 0.4612988732951432969 ) ) ;
#9581=CARTESIAN_POINT ( 'NONE',  ( 4.984861949208964305, 1.980195279717174905, 0.6042863919064264122 ) ) ;
#9583=CARTESIAN_POINT ( 'NONE',  ( 6.703094305332148117, -0.4564761572844484028, 2.047479069123214757 ) ) ;
#9584=CARTESIAN_POINT ( 'NONE',  ( 6.620655732516650183, 4.692022689331314389, 2.636326274693585159 ) ) ;
#9585=CARTESIAN_POINT ( 'NONE',  ( 5.350558509363329662, 0.5315954154057299652, 1.746479326997903092 ) ) ;
#9592=CARTESIAN_POINT ( 'NONE',  ( 6.217437059193511750, 1.592560689453832001, 1.058264445519964125 ) ) ;
#9600=CARTESIAN_POINT ( 'NONE',  ( 5.150017624212761547, 0.9963180513538304472, 1.753022482293864481 ) ) ;
#9603=CARTESIAN_POINT ( 'NONE',  ( 0.1394461523057137220, 2.891244824116427470, -2.208899952336295325 ) ) ;
#9607=CARTESIAN_POINT ( 'NONE',  ( 2.412896334679739851, -1.525488895468416706, 1.245673054583651407 ) ) ;
#9608=CARTESIAN_POINT ( 'NONE',  ( 3.673453983005552814, 1.462458373076291673, 1.388474078538141754 ) ) ;
#9610=CARTESIAN_POINT ( 'NONE',  ( 6.727182134110234024, -0.002100931800118072384, 2.089081857379895268 ) ) ;
#9611=CARTESIAN_POINT ( 'NONE',  ( 3.996163734398257894, -0.6867376513691285655, -2.081127982183433645 ) ) ;
#9613=CARTESIAN_POINT ( 'NONE',  ( 2.221590912301483645, -1.869112302256823011, 0.4658275329730912628 ) ) ;
#9615=CARTESIAN_POINT ( 'NONE',  ( 0.1333542156527113831, 2.876250315000815405, -2.534448870308704915 ) ) ;
#9621=CARTESIAN_POINT ( 'NONE',  ( 5.636236351835953506, 0.3653394402399374741, 1.804471444190151930 ) ) ;
#9622=CARTESIAN_POINT ( 'NONE',  ( 2.789700014133191797, 1.910882804325767070, -0.6334545493084097201 ) ) ;
#9623=CARTESIAN_POINT ( 'NONE',  ( 4.517165314107184138, 2.297965829929650372, -0.05084271438157876577 ) ) ;
#9624=CARTESIAN_POINT ( 'NONE',  ( -0.02900071798685524560, -0.004641455105012376459, -2.173770343569726649 ) ) ;
#9625=CARTESIAN_POINT ( 'NONE',  ( 3.520197291191272448, 0.8326901208413343136, 1.664296038758736440 ) ) ;
#9631=CARTESIAN_POINT ( 'NONE',  ( 5.970280646434825478, -1.985518398909513982, -0.6551979098984096472 ) ) ;
#9636=CARTESIAN_POINT ( 'NONE',  ( 6.217413168894407427, -0.2034119912461933299, 1.712789424573582409 ) ) ;
#9638=CARTESIAN_POINT ( 'NONE',  ( 1.318582137269165733, 0.8549262331399180015, -1.508633131004229133 ) ) ;
#9643=CARTESIAN_POINT ( 'NONE',  ( 5.700102493039955753, 0.8868678402436469543, -1.981866098488117789 ) ) ;
#9644=CARTESIAN_POINT ( 'NONE',  ( 4.143042835627613663, -1.587387879459275286, 0.9017181768668989239 ) ) ;
#9645=CARTESIAN_POINT ( 'NONE',  ( 2.746866186719683967, -0.3305370478365337039, -1.933541032166598894 ) ) ;
#9649=CARTESIAN_POINT ( 'NONE',  ( 3.651137946248568689, 0.3127203024623700367, 2.097190470537732221 ) ) ;
#9655=CARTESIAN_POINT ( 'NONE',  ( 0.8310238944931707117, -1.948087850137161459, -0.7009411469260096172 ) ) ;
#9658=CARTESIAN_POINT ( 'NONE',  ( 3.422728177422405871, -0.9015832817733639981, -2.030284994954335787 ) ) ;
#9660=CARTESIAN_POINT ( 'NONE',  ( 0.8976324851915818970, -1.040256531696292397, -2.049935236865876309 ) ) ;
#9662=CARTESIAN_POINT ( 'NONE',  ( 6.614137777011339203, 2.057435194276434842, -0.1460075293888435377 ) ) ;
#9668=CARTESIAN_POINT ( 'NONE',  ( -0.2106725631050020975, 7.629137130509112907, -2.603678913577145426 ) ) ;
#9669=CARTESIAN_POINT ( 'NONE',  ( 3.522183196695947593, 1.094745356718468399, -1.332776395737497399 ) ) ;
#9670=CARTESIAN_POINT ( 'NONE',  ( 1.411342602523329992, -1.897109289313267944, 0.6839406069230755669 ) ) ;
#9671=CARTESIAN_POINT ( 'NONE',  ( 2.461953032136819264, -2.200924886027255667, -0.6633417334961901890 ) ) ;
#9672=CARTESIAN_POINT ( 'NONE',  ( 3.023041696300738934, 2.129209760986842781, 0.7651156340112361676 ) ) ;
#9673=CARTESIAN_POINT ( 'NONE',  ( 5.531892221078217098, -1.335191642697653336, -1.628727054747380887 ) ) ;
#9675=ORIENTED_EDGE ( 'NONE', *, *, #16450, .T. ) ;
#9676=CARTESIAN_POINT ( 'NONE',  ( 3.584973236653755002, 1.601158291227417152, -0.7540797108817003380 ) ) ;
#9678=CARTESIAN_POINT ( 'NONE',  ( 0.1997390566700393277, -0.6049713359795177992, 2.210933144166931985 ) ) ;
#9679=CARTESIAN_POINT ( 'NONE',  ( 5.331922971087851515, 1.814509544241477146, 0.3110680438872318043 ) ) ;
#9683=CARTESIAN_POINT ( 'NONE',  ( 4.400438482046089561, 1.694813852089768869, -1.389250428430639950 ) ) ;
#9686=CARTESIAN_POINT ( 'NONE',  ( 5.389151899530504330, 0.1487064154041470299, 2.065066873896327593 ) ) ;
#9687=CARTESIAN_POINT ( 'NONE',  ( 0.005092704479254389627, -0.09411098085002241043, 2.014433268766747887 ) ) ;
#9690=CARTESIAN_POINT ( 'NONE',  ( 2.807156881705831442, 1.627618881652561411, 1.030384643589934646 ) ) ;
#9693=CARTESIAN_POINT ( 'NONE',  ( -0.05205951232617207075, -2.027416208471942038, 0.9083432681902519068 ) ) ;
#9703=CARTESIAN_POINT ( 'NONE',  ( 1.750371521623844462, -1.952110535733902585, -0.1955497077021361163 ) ) ;
#9707=CARTESIAN_POINT ( 'NONE',  ( 5.652778587040098834, -0.4750822840141955550, -1.903360745478323679 ) ) ;
#9710=CARTESIAN_POINT ( 'NONE',  ( 6.491117449447131982, 1.883434485765375310, -1.060826435891427666 ) ) ;
#9714=CARTESIAN_POINT ( 'NONE',  ( 0.2802489257003986656, -1.812731005579379051, -0.4610361243657657981 ) ) ;
#9715=CARTESIAN_POINT ( 'NONE',  ( 6.731818218530718489, -1.587343137472529309, -0.6980196547925822115 ) ) ;
#9717=CARTESIAN_POINT ( 'NONE',  ( 3.017305944477025825, -2.111434807548946857, 0.5868732223921411251 ) ) ;
#9718=CARTESIAN_POINT ( 'NONE',  ( 4.278580467222413475, -1.332036844872594994, 1.884138376372360479 ) ) ;
#9719=CARTESIAN_POINT ( 'NONE',  ( 0.4267267499857710367, 1.971919523859454237, 0.5989439635904010295 ) ) ;
#9720=CARTESIAN_POINT ( 'NONE',  ( 1.974458820771322953, -0.09541523299517583323, -1.939727210137192737 ) ) ;
#9724=CARTESIAN_POINT ( 'NONE',  ( 5.502226937873657242, -0.9515977829631333540, 1.895136135177949877 ) ) ;
#9725=CARTESIAN_POINT ( 'NONE',  ( 3.041638857185970046, -1.525043868314728934, 1.319228477497782714 ) ) ;
#9729=DIRECTION ( 'NONE',  ( 1.039099362110107450E-15, 1.000000000000000000, -4.583713267641621330E-32 ) ) ;
#9734=CARTESIAN_POINT ( 'NONE',  ( 5.207911835226475716, -2.051185258288893198, 0.1996322284415520676 ) ) ;
#9739=CARTESIAN_POINT ( 'NONE',  ( 4.389322685995568740, -0.002182162029157329840, -2.019862493239577894 ) ) ;
#9740=CARTESIAN_POINT ( 'NONE',  ( 6.164703477482621707, 0.6939275443377226349, 2.110173311658748663 ) ) ;
#9746=CARTESIAN_POINT ( 'NONE',  ( 4.065347389730957772, 0.2539501645208458447, -2.045120066754711363 ) ) ;
#9747=CARTESIAN_POINT ( 'NONE',  ( 3.393204081532863459, -0.8197727808607684352, -1.842447475547980495 ) ) ;
#9753=CARTESIAN_POINT ( 'NONE',  ( 3.005232341680406094, 2.000550758621592706, 0.2495690156183311137 ) ) ;
#9754=CARTESIAN_POINT ( 'NONE',  ( 2.062219658421380775, -1.683061746929171321, -0.7467898329211534181 ) ) ;
#9755=EDGE_CURVE ( 'NONE', #136413, #160735, #153595, .T. ) ;
#9756=CARTESIAN_POINT ( 'NONE',  ( 1.067484182866541564, -2.088262569869667740, -0.9824423588734966239 ) ) ;
#9758=CARTESIAN_POINT ( 'NONE',  ( 3.690839692606663558, -0.4176960054509891163, -2.120685484085436112 ) ) ;
#9761=CARTESIAN_POINT ( 'NONE',  ( 3.251609920728415037, -2.263897172838242877, -0.3959942320375854918 ) ) ;
#9764=CARTESIAN_POINT ( 'NONE',  ( 1.340467186903429253, 0.3614942610149494695, 1.835218787103513050 ) ) ;
#9765=CARTESIAN_POINT ( 'NONE',  ( 6.209841870239331207, -1.956602576295646490, 0.2410399859902948028 ) ) ;
#9770=CARTESIAN_POINT ( 'NONE',  ( 1.084930333755677045, -2.153824616689365978, -0.4803136671489223741 ) ) ;
#9774=CARTESIAN_POINT ( 'NONE',  ( 6.639320575229255894, 7.629137130509070275, 2.703262396134015866 ) ) ;
#9775=CARTESIAN_POINT ( 'NONE',  ( 4.610209453490740295, -0.8421727957172200352, -1.782655373600953386 ) ) ;
#9777=CARTESIAN_POINT ( 'NONE',  ( 6.199901738523720951, -0.7837251098280417771, 2.170682987836409783 ) ) ;
#9778=CARTESIAN_POINT ( 'NONE',  ( 5.547250370032299038, 1.641257983771953866, -0.8773172063531119447 ) ) ;
#9779=CARTESIAN_POINT ( 'NONE',  ( 2.606363979242664719, 2.062007909489747881, 0.05513178878350195877 ) ) ;
#9785=CARTESIAN_POINT ( 'NONE',  ( 5.160662515399747186, -0.7266353732918430230, -2.046117350891932141 ) ) ;
#9787=CARTESIAN_POINT ( 'NONE',  ( 4.036529152626888717, -1.599951230533543267, 0.9111318136766360931 ) ) ;
#9789=CARTESIAN_POINT ( 'NONE',  ( 6.720655732516655156, 7.629137130509086262, 2.526260288887293814 ) ) ;
#9790=CARTESIAN_POINT ( 'NONE',  ( 6.181208317857348256, 1.509947553572440704, 1.588605474358975478 ) ) ;
#9791=CARTESIAN_POINT ( 'NONE',  ( 0.2458944382301266607, -1.750094391731635168, -1.433289930825008218 ) ) ;
#9796=CARTESIAN_POINT ( 'NONE',  ( 0.1352199593073095951, -0.09384731153385186819, 1.910084486482076294 ) ) ;
#9797=CARTESIAN_POINT ( 'NONE',  ( 0.2327837997007513038, -1.621012357304358220, 0.7108589729635225174 ) ) ;
#9798=CARTESIAN_POINT ( 'NONE',  ( 5.813144886445268611, 1.644464822582414332, -1.160890557811714352 ) ) ;
#9800=CARTESIAN_POINT ( 'NONE',  ( 4.067482540003349634, 0.2598354432931935243, -2.089805856947650309 ) ) ;
#9801=CARTESIAN_POINT ( 'NONE',  ( 2.794441263998331149, 1.385543030692138133, -1.323043162562879349 ) ) ;
#9802=CARTESIAN_POINT ( 'NONE',  ( -0.02244404828157658613, 0.6916080914694566761, -2.270927585766496559 ) ) ;
#9803=CARTESIAN_POINT ( 'NONE',  ( 4.826587240018016089, -1.288162778474700287, 1.489951593160773635 ) ) ;
#9804=CARTESIAN_POINT ( 'NONE',  ( 5.695571270406009745, 1.864622851205568699, -0.7768453975713036641 ) ) ;
#9805=CARTESIAN_POINT ( 'NONE',  ( 3.186256133050053840, -1.842714570631575510, -0.3211874441736498054 ) ) ;
#9806=CARTESIAN_POINT ( 'NONE',  ( 4.723137274085514647, -0.08022016869785492110, 1.723147214940720762 ) ) ;
#9807=CARTESIAN_POINT ( 'NONE',  ( 1.757924209179074770, 0.7287868685415777037, -1.768279316124596878 ) ) ;
#9809=CARTESIAN_POINT ( 'NONE',  ( 1.963769682107346037, 0.3752889857368995608, -2.174583152744386627 ) ) ;
#9812=CARTESIAN_POINT ( 'NONE',  ( 6.531700620877029628, 1.877769495358465157, -0.5682946464737671510 ) ) ;
#9820=CARTESIAN_POINT ( 'NONE',  ( 2.242711981562468093, -2.029969483702593003, -0.4061203719310027549 ) ) ;
#9825=CARTESIAN_POINT ( 'NONE',  ( -0.1048592448738161903, -0.1538584160990438265, -1.986454975908092058 ) ) ;
#9830=CARTESIAN_POINT ( 'NONE',  ( 5.606796008369615336, 0.8196459417171354511, -1.842166028910074527 ) ) ;
#9831=CARTESIAN_POINT ( 'NONE',  ( 4.786306776965392196, -0.6515362397919061133, -1.801638605214391342 ) ) ;
#9833=CARTESIAN_POINT ( 'NONE',  ( 2.120887600855193345, 0.003649250790785373531, 2.191739723551556551 ) ) ;
#9836=CARTESIAN_POINT ( 'NONE',  ( 4.957293921627444533, -1.724444360862188885, 1.038707789177233831 ) ) ;
#9837=CARTESIAN_POINT ( 'NONE',  ( 1.722773492080275748, 1.414811824084385883, -1.286832238068566392 ) ) ;
#9840=CARTESIAN_POINT ( 'NONE',  ( 0.3687678296072604556, -0.2496303596870551866, -2.000855358883571800 ) ) ;
#9843=CARTESIAN_POINT ( 'NONE',  ( 3.702747019872438372, 1.794327276830971707, 1.072858563533698018 ) ) ;
#9845=CARTESIAN_POINT ( 'NONE',  ( 1.852176121455822777, 0.5370312411601232405, 1.639109186831126053 ) ) ;
#9855=CARTESIAN_POINT ( 'NONE',  ( 2.420317109208899531, -0.6946167411978272366, -1.673203699974361580 ) ) ;
#9859=CARTESIAN_POINT ( 'NONE',  ( 4.178215122889179511, 0.8575144648667647473, 1.595655492163786437 ) ) ;
#9863=CARTESIAN_POINT ( 'NONE',  ( 4.439814405351947713, 1.214877501302736862, 1.409928613244580742 ) ) ;
#9865=CARTESIAN_POINT ( 'NONE',  ( 2.020959903547480341, -1.710230010390185296, 0.8631189023672394267 ) ) ;
#9866=CARTESIAN_POINT ( 'NONE',  ( 0.5162701059127188241, 1.262803565755654001, -1.318596375272471199 ) ) ;
#9874=CARTESIAN_POINT ( 'NONE',  ( 5.524252356588593926, 0.9672068372908498857, 1.715464803677963834 ) ) ;
#9877=CARTESIAN_POINT ( 'NONE',  ( 0.7266515212380560973, 0.1555473773823950467, 2.084908828405390491 ) ) ;
#9879=CARTESIAN_POINT ( 'NONE',  ( 5.297847195631281814, -0.6933188941696236673, 1.797466220796402725 ) ) ;
#9882=CARTESIAN_POINT ( 'NONE',  ( 1.641335390984842491, -1.319735721761399638, -1.261605215524951085 ) ) ;
#9883=CARTESIAN_POINT ( 'NONE',  ( 1.998912159191484905, -0.5904864226158462737, -2.126349760018491963 ) ) ;
#9885=CARTESIAN_POINT ( 'NONE',  ( 1.265713261412576562, 0.5522810963098608861, -1.830935845731461953 ) ) ;
#9886=CARTESIAN_POINT ( 'NONE',  ( 6.930521655090660538, -1.214226768402311363, 1.551031149239000761 ) ) ;
#9887=CARTESIAN_POINT ( 'NONE',  ( 2.366656106817651040, 0.09313060749883492195, -1.939932752287050199 ) ) ;
#9888=CARTESIAN_POINT ( 'NONE',  ( 1.317732270343049406, -1.591076063098846749, 1.238129638497114771 ) ) ;
#9890=CARTESIAN_POINT ( 'NONE',  ( 6.157066405694873623, 1.522017207847397469, -1.070502804743376668 ) ) ;
#9896=CARTESIAN_POINT ( 'NONE',  ( 2.472451708263478931, -2.098117355222902436, -0.6331711661175795092 ) ) ;
#9901=CARTESIAN_POINT ( 'NONE',  ( 2.508196354075361789, -0.6984789837382252564, -1.686990664346368796 ) ) ;
#9907=CARTESIAN_POINT ( 'NONE',  ( 0.8735101492000696410, 1.856966920605634508, -0.5126664406217595893 ) ) ;
#9908=CARTESIAN_POINT ( 'NONE',  ( 6.069191303861535935, 1.728486752094374967, 0.9278679456784576507 ) ) ;
#9914=CARTESIAN_POINT ( 'NONE',  ( 4.950807510372833065, -1.851323926424643274, -1.172527737679923465 ) ) ;
#9917=CARTESIAN_POINT ( 'NONE',  ( 4.575093719746353038, 1.890691655113156289, 0.8438020912069632562 ) ) ;
#9921=CARTESIAN_POINT ( 'NONE',  ( 4.658965222740456547, 1.322560505849355694, 1.879950767321969529 ) ) ;
#9925=CARTESIAN_POINT ( 'NONE',  ( 0.2699993869635419208, 1.325028633338236839, 1.870336120953507875 ) ) ;
#9926=CARTESIAN_POINT ( 'NONE',  ( 6.620655732516683045, 6.038298567659169613, 2.521170675138622475 ) ) ;
#9928=CARTESIAN_POINT ( 'NONE',  ( 4.646391893561965247, -1.558859349912258718, 1.157878524630775230 ) ) ;
#9932=CARTESIAN_POINT ( 'NONE',  ( 4.675980034926481288, 1.890745994642643479, -0.2862527531290667837 ) ) ;
#9933=CARTESIAN_POINT ( 'NONE',  ( 6.282236785375785892, -0.9178991178065436518, 1.460045492214437246 ) ) ;
#9934=CARTESIAN_POINT ( 'NONE',  ( 6.087125082597877324, 1.679220375458953862, 1.116214469231976869 ) ) ;
#9938=CARTESIAN_POINT ( 'NONE',  ( 2.115285117227220901, -2.027561382914280674, 0.5091250600777631474 ) ) ;
#9939=CARTESIAN_POINT ( 'NONE',  ( 6.854783864179318620, -1.365764260946045860, 1.125274747944494891 ) ) ;
#9940=CARTESIAN_POINT ( 'NONE',  ( 5.361953999179126740, -0.05229508359532940298, -2.015913028294749942 ) ) ;
#9942=CARTESIAN_POINT ( 'NONE',  ( 3.029517917392979598, -1.539792254791607862, -1.698243321706040421 ) ) ;
#9943=CARTESIAN_POINT ( 'NONE',  ( 2.747703163511563407, 0.5864964929944632699, 1.638654499222062189 ) ) ;
#9945=CARTESIAN_POINT ( 'NONE',  ( 2.600625072996507470, 0.8205526226049694172, -1.527383475524378031 ) ) ;
#9947=CARTESIAN_POINT ( 'NONE',  ( 2.189708182147569460, -1.212837473668834098, -1.411683579110091458 ) ) ;
#9948=CARTESIAN_POINT ( 'NONE',  ( 2.365899470183946640, -0.4773124685180894500, 2.117905883517334775 ) ) ;
#9949=CARTESIAN_POINT ( 'NONE',  ( 3.116422982138194353, 1.968445132739887748, 0.4370783100892047801 ) ) ;
#9950=CARTESIAN_POINT ( 'NONE',  ( 3.937500000000001776, 1.451031289060957574, -1.451031289061275320 ) ) ;
#9952=CARTESIAN_POINT ( 'NONE',  ( 6.270143248794765256, 0.9928014866268529692, 1.650855525168734461 ) ) ;
#9954=CARTESIAN_POINT ( 'NONE',  ( 3.094184762719538906, 1.412074837861827303, 1.714815191315356868 ) ) ;
#9960=CARTESIAN_POINT ( 'NONE',  ( -0.03994651564155191764, -1.721383993196375251, -1.403517996469628493 ) ) ;
#9961=CARTESIAN_POINT ( 'NONE',  ( 4.369553226407375313, -0.3375162941181614751, 1.932460123137308861 ) ) ;
#9965=CARTESIAN_POINT ( 'NONE',  ( 5.308033872091713512, -2.252217787711635388, 0.2143866227288723780 ) ) ;
#9967=CARTESIAN_POINT ( 'NONE',  ( 2.682143534289625375, -1.185536078076434796, -1.687771684069488076 ) ) ;
#9971=CARTESIAN_POINT ( 'NONE',  ( 3.760894150569486616, -1.648321677062795976, -0.8843367818652316803 ) ) ;
#9972=CARTESIAN_POINT ( 'NONE',  ( 2.619397310362530096, 0.2141275842034353338, 1.720801833696316008 ) ) ;
#9973=CARTESIAN_POINT ( 'NONE',  ( 6.497619750234602698, -2.191128968173004843, 0.05151875470104508997 ) ) ;
#9974=CARTESIAN_POINT ( 'NONE',  ( 0.4818276840582723652, 2.058231501447154610, -0.7964225590989246761 ) ) ;
#9975=CARTESIAN_POINT ( 'NONE',  ( 5.613211309847925712, -1.894178568204254676, 0.4274185452872342195 ) ) ;
#9976=ADVANCED_FACE ( 'NONE', ( #93768 ), #11412, .T. ) ;
#9979=CARTESIAN_POINT ( 'NONE',  ( 0.9498425221252141393, -1.824119990893595888, -0.8596288560165299408 ) ) ;
#9980=CARTESIAN_POINT ( 'NONE',  ( 0.1059362375676886209, 1.575662574916199210, 1.419458935296296520 ) ) ;
#9982=CARTESIAN_POINT ( 'NONE',  ( 6.539686446881147752, -1.556848207870220602, 1.281141925495055123 ) ) ;
#9986=CARTESIAN_POINT ( 'NONE',  ( 4.090329635444483358, -1.806102819543849769, -0.2658631594732660530 ) ) ;
#9987=CARTESIAN_POINT ( 'NONE',  ( 1.606762454812577179, -0.7948807482080816333, -2.058825234118460745 ) ) ;
#9993=CARTESIAN_POINT ( 'NONE',  ( 0.8440173190735723585, -1.284739210308597723, -1.558479848626155961 ) ) ;
#9997=CARTESIAN_POINT ( 'NONE',  ( 2.535811996613965391, 1.140603387277869585, 1.470366759043324478 ) ) ;
#10004=CARTESIAN_POINT ( 'NONE',  ( 3.984828715814022981, -0.1808549858164226476, -1.816707794649790708 ) ) ;
#10008=CARTESIAN_POINT ( 'NONE',  ( 0.9656601056488465229, 1.412931828189394556, 1.004572000263863840 ) ) ;
#10009=CARTESIAN_POINT ( 'NONE',  ( 5.454971364017034752, 0.3553261626877933788, -1.806350769464920569 ) ) ;
#10010=CARTESIAN_POINT ( 'NONE',  ( 3.862222655691281759, 2.290455142492770602, -0.2811034502991411888 ) ) ;
#10012=CARTESIAN_POINT ( 'NONE',  ( 0.4388362695032248517, 0.3497011122354178325, 2.030714657000245893 ) ) ;
#10014=CARTESIAN_POINT ( 'NONE',  ( 2.120557540808472918, 0.002150750411172245441, 1.942234967187633110 ) ) ;
#10016=CARTESIAN_POINT ( 'NONE',  ( 5.431170548343748905, 1.126412363255802518, 2.003379520639406497 ) ) ;
#10019=CARTESIAN_POINT ( 'NONE',  ( 4.557402362779487959, 0.4096945884842878582, -1.825068887194372991 ) ) ;
#10020=CARTESIAN_POINT ( 'NONE',  ( 2.496234081663367022, -0.9796988711565941532, 1.642222327643327873 ) ) ;
#10023=CARTESIAN_POINT ( 'NONE',  ( 3.809358915828209735, 1.892446193107431451, 1.135094405146239049 ) ) ;
#10025=CARTESIAN_POINT ( 'NONE',  ( 6.983263157960404754, -0.005959781318053481922, 2.045923054782183392 ) ) ;
#10028=CARTESIAN_POINT ( 'NONE',  ( 1.387891646316425476, -0.8902153388929586741, 1.759007621864362214 ) ) ;
#10030=CARTESIAN_POINT ( 'NONE',  ( 2.485774399949276070, 2.109797628256422364, -0.9350972159218959856 ) ) ;
#10031=CARTESIAN_POINT ( 'NONE',  ( 1.996468121258226924, 1.940055844723225009, 0.2909814450420752929 ) ) ;
#10033=CARTESIAN_POINT ( 'NONE',  ( 6.139522945012108934, 1.907909241145373525, -0.7841019685283256990 ) ) ;
#10035=CARTESIAN_POINT ( 'NONE',  ( 3.731657894805060938, 0.6748485617756972976, -1.900415309456899182 ) ) ;
#10038=CARTESIAN_POINT ( 'NONE',  ( 4.382046175016578005, -2.016188710442788246, -0.04465648322755921829 ) ) ;
#10043=CARTESIAN_POINT ( 'NONE',  ( 2.237404288245536943, -0.1031769000767470690, -2.168708286310920386 ) ) ;
#10046=CARTESIAN_POINT ( 'NONE',  ( 2.038157526861613889, 1.849479306444936411, 0.2792354855166642724 ) ) ;
#10048=CARTESIAN_POINT ( 'NONE',  ( 0.4036811037357163623, -0.5522049309486184443, 1.985320814919430132 ) ) ;
#10049=CARTESIAN_POINT ( 'NONE',  ( 0.07775346131142638062, 0.2253410668615995205, -2.322482355083537175 ) ) ;
#10050=CARTESIAN_POINT ( 'NONE',  ( 6.827182134110200806, 1.308106637204756728, 1.828351192278207638 ) ) ;
#10052=CARTESIAN_POINT ( 'NONE',  ( 3.615784255950851289, -0.5524401208748200842, 1.830756043982272097 ) ) ;
#10053=CARTESIAN_POINT ( 'NONE',  ( 4.557331473417879586, 0.3865553534455662965, -1.726927170965624647 ) ) ;
#10054=CARTESIAN_POINT ( 'NONE',  ( 1.383307607624170155, 0.1396965592646744470, -1.907218110473147155 ) ) ;
#10057=CARTESIAN_POINT ( 'NONE',  ( -0.2411972340276360705, -0.002466136893084554509, -1.900252416837118430 ) ) ;
#10060=CARTESIAN_POINT ( 'NONE',  ( 0.5728211633247158874, 1.428863753495920763, -1.498466819491943269 ) ) ;
#10062=CARTESIAN_POINT ( 'NONE',  ( 6.104356062600288624, -0.6750377415852754082, -1.744797942764392928 ) ) ;
#10063=CARTESIAN_POINT ( 'NONE',  ( 1.611646134362737959, -1.812087876328593916, 0.2219229778191167957 ) ) ;
#10064=CARTESIAN_POINT ( 'NONE',  ( 5.813141826352885566, 1.944573597739504889, 1.043518232037063287 ) ) ;
#10067=CARTESIAN_POINT ( 'NONE',  ( 3.385269252200762580, 0.04793456357342047724, 2.062272590435239028 ) ) ;
#10071=CARTESIAN_POINT ( 'NONE',  ( 0.1929406647830470833, -0.4748886411078504510, -2.116594070111991410 ) ) ;
#10074=CARTESIAN_POINT ( 'NONE',  ( 5.020015195830264787, 2.048331326439792210, -0.3003445753073652469 ) ) ;
#10076=CARTESIAN_POINT ( 'NONE',  ( 2.847126979364768218, -1.798887516807456954, 1.198237791991546564 ) ) ;
#10078=CARTESIAN_POINT ( 'NONE',  ( 2.701824437540679469, 1.429832853698081108, 1.426684077065028422 ) ) ;
#10079=CARTESIAN_POINT ( 'NONE',  ( 2.101936620064443151, 0.7537240185569763495, -1.811501260397870405 ) ) ;
#10080=B_SPLINE_CURVE_WITH_KNOTS ( 'NONE', 3,
 ( #94114, #8561, #173226, #89846, #77827, #160155, #11753, #206759, #109347, #40015 ),
 .UNSPECIFIED., .F., .F.,
 ( 4, 1, 1, 1, 1, 1, 1, 4 ),
 ( 0.000000000000000000, 0.09123828766142533242, 0.1830323254715014447, 0.2554767746403809325, 0.3605042187413262100, 0.5206858269973231312, 0.7335850107976985557, 1.000000000000000000 ),
 .UNSPECIFIED. ) ;
#10081=CARTESIAN_POINT ( 'NONE',  ( 6.620655732516607550, 2.431211045237289703, 2.455576803978098521 ) ) ;
#10086=CARTESIAN_POINT ( 'NONE',  ( 1.077361674225948418, 1.530160568918725872, 1.313541346884481209 ) ) ;
#10088=CARTESIAN_POINT ( 'NONE',  ( 5.987848539424092564, -2.180829346447300310, -0.2163489798085171945 ) ) ;
#10090=CARTESIAN_POINT ( 'NONE',  ( 4.816621285000030284, -0.6497861859515661198, -1.798733151862880186 ) ) ;
#10094=CARTESIAN_POINT ( 'NONE',  ( 3.357046149680571023, 0.04665894677104672622, -2.016035383867887276 ) ) ;
#10096=CARTESIAN_POINT ( 'NONE',  ( 5.754863291335100328, -1.356889945763246841, 1.064653683861387812 ) ) ;
#10100=CARTESIAN_POINT ( 'NONE',  ( 4.833189656263336964, -1.710893631887340227, 0.7565425265826587475 ) ) ;
#10102=CARTESIAN_POINT ( 'NONE',  ( 0.5497785174156319954, 1.531638494488884339, 1.392999266381978130 ) ) ;
#10106=CARTESIAN_POINT ( 'NONE',  ( 5.900986446306966116, -0.2725449506757338658, -1.790729509878173475 ) ) ;
#10109=CARTESIAN_POINT ( 'NONE',  ( 0.1229364404080907497, 1.576183056183463993, 0.8927909362536170512 ) ) ;
#10113=CARTESIAN_POINT ( 'NONE',  ( 0.6429252097494702056, -0.2364460082661112295, -1.947484529462916836 ) ) ;
#10115=CARTESIAN_POINT ( 'NONE',  ( 4.692942998425689183, 1.668811738553135804, 0.9403632788237480389 ) ) ;
#10121=CARTESIAN_POINT ( 'NONE',  ( 2.360439101503517101, 0.9236781337260313585, 1.954550705658316678 ) ) ;
#10124=CARTESIAN_POINT ( 'NONE',  ( -0.1401555495076401980, -1.643345231473653190, -1.339971704266910812 ) ) ;
#10125=CARTESIAN_POINT ( 'NONE',  ( 4.840742024777624053, 0.3130767520662172121, 1.798364180563789327 ) ) ;
#10127=CARTESIAN_POINT ( 'NONE',  ( 1.598833994113032730, 1.614015922016404536, -1.131664812120122487 ) ) ;
#10128=CARTESIAN_POINT ( 'NONE',  ( 3.937688585161042809, -1.828529804631402023, 0.5600222464785462595 ) ) ;
#10131=CARTESIAN_POINT ( 'NONE',  ( 3.420317264040674932, 0.8831254867164675115, 1.760515127234823840 ) ) ;
#10133=CARTESIAN_POINT ( 'NONE',  ( 5.706574293107399498, 1.714631337756479912, 0.9119185223999854983 ) ) ;
#10137=CARTESIAN_POINT ( 'NONE',  ( 6.398696098476772676, -2.079943653215409416, -0.4123558718646391785 ) ) ;
#10139=CARTESIAN_POINT ( 'NONE',  ( 4.318947422894989785, 1.476084237994702786, -1.215703867470045774 ) ) ;
#10141=CARTESIAN_POINT ( 'NONE',  ( 0.1302870565101400258, -1.360178740744298675, -1.738515015553928400 ) ) ;
#10144=CARTESIAN_POINT ( 'NONE',  ( 5.549481842319204716, -1.818904971374595503, 0.8629315129762565872 ) ) ;
#10146=CARTESIAN_POINT ( 'NONE',  ( 5.936143289257818978, 0.8957264799932495025, -1.590785280889392528 ) ) ;
#10147=CARTESIAN_POINT ( 'NONE',  ( 1.469279758060072938, 1.824989553406907383, 0.9776941847434923449 ) ) ;
#10152=CARTESIAN_POINT ( 'NONE',  ( 6.631728656526095556, -1.223761959379562114, -1.414937998750566361 ) ) ;
#10164=CARTESIAN_POINT ( 'NONE',  ( 4.799290796133064418, 1.190976682166387413, -1.260762715536057899 ) ) ;
#10166=CARTESIAN_POINT ( 'NONE',  ( 2.360293207207576849, -2.069885933316969240, 0.04650197241463926989 ) ) ;
#10167=CARTESIAN_POINT ( 'NONE',  ( 3.304427501237202414, 1.341129661294770958, -1.638326698864990716 ) ) ;
#10170=CARTESIAN_POINT ( 'NONE',  ( 1.762491902426995605, -0.7040454445105134296, -1.839503732180563844 ) ) ;
#10175=CARTESIAN_POINT ( 'NONE',  ( 3.767766022312348362, 1.272560033980062455, 1.906398719306565681 ) ) ;
#10176=CARTESIAN_POINT ( 'NONE',  ( 0.5041868517345666767, -0.6120625888205477594, -1.720162557568189809 ) ) ;
#10181=CARTESIAN_POINT ( 'NONE',  ( 1.406495263175694399, -2.003875642784687994, -0.1933051647188162026 ) ) ;
#10182=CARTESIAN_POINT ( 'NONE',  ( 2.412880707699780025, -1.519673801815585312, 1.240645658979570909 ) ) ;
#10185=CARTESIAN_POINT ( 'NONE',  ( 0.07536363704235825300, -0.001874865094115065866, -2.144269471569634433 ) ) ;
#10186=CARTESIAN_POINT ( 'NONE',  ( 5.384749270845579083, 1.844215719714219492, -0.9846981469126301345 ) ) ;
#10187=CARTESIAN_POINT ( 'NONE',  ( 3.555294528146099697, 0.4307136429906773256, -1.716485385381610662 ) ) ;
#10189=CARTESIAN_POINT ( 'NONE',  ( 6.035170563425642953, -1.656272789430097703, -1.584931405618497990 ) ) ;
#10190=CARTESIAN_POINT ( 'NONE',  ( 5.279165678654878846, 1.172930834070673889, 1.285866470927458094 ) ) ;
#10192=CARTESIAN_POINT ( 'NONE',  ( 5.748750450937779810, 2.265299150918558269, -0.3897391249057541862 ) ) ;
#10194=CARTESIAN_POINT ( 'NONE',  ( 5.061730935934568798, 1.440722419422343803, -0.9642406207952100017 ) ) ;
#10195=CARTESIAN_POINT ( 'NONE',  ( 5.670445308384678640, -0.9712495897680500923, -1.941886722523916253 ) ) ;
#10197=CARTESIAN_POINT ( 'NONE',  ( 6.509000000000012776, 0.004788705324892602276, 2.000274819378269342 ) ) ;
#10198=CARTESIAN_POINT ( 'NONE',  ( 4.781250000000003553, 0.7852924748302358982, 1.895863743163977100 ) ) ;
#10200=CARTESIAN_POINT ( 'NONE',  ( 3.821244781301834426, -0.1429285350797465659, 1.921155437072092242 ) ) ;
#10202=CARTESIAN_POINT ( 'NONE',  ( 0.1885310067011408963, 1.284270987554763765, 1.812239126532013689 ) ) ;
#10207=CARTESIAN_POINT ( 'NONE',  ( 2.684490341743519082, 1.190536367853095578, 1.875150363231482098 ) ) ;
#10213=CARTESIAN_POINT ( 'NONE',  ( 0.7389079861009685279, 2.013985778099684154, -0.1017531103126300962 ) ) ;
#10215=CARTESIAN_POINT ( 'NONE',  ( 5.195784910611107144, -1.456250996468626768, -1.461061404345398440 ) ) ;
#10221=CARTESIAN_POINT ( 'NONE',  ( 0.4909911900966601461, 1.305473228555413812, 1.195063304280475025 ) ) ;
#10222=CARTESIAN_POINT ( 'NONE',  ( 6.012339335674446339, -1.629552802491928354, 0.5935831289462877303 ) ) ;
#10223=CARTESIAN_POINT ( 'NONE',  ( 5.952664183270127474, -1.497414089959566930, -0.8868285315999470120 ) ) ;
#10224=CARTESIAN_POINT ( 'NONE',  ( 2.718655769491088225, 2.159526321510790492, 0.7694321526581606729 ) ) ;
#10226=CARTESIAN_POINT ( 'NONE',  ( 2.396224210035051261, 1.478860665732561586, -1.096489538662905217 ) ) ;
#10227=ADVANCED_FACE ( 'NONE', ( #182175 ), #20146, .F. ) ;
#10229=CARTESIAN_POINT ( 'NONE',  ( 2.748829393344632166, -1.518919317350690967, 1.012417160375630898 ) ) ;
#10230=CARTESIAN_POINT ( 'NONE',  ( 3.410779880581996437, -1.203353552534730309, -1.617818353255597863 ) ) ;
#10233=CARTESIAN_POINT ( 'NONE',  ( 5.016683434392706253, 1.454383057171860116, -1.523333715015115608 ) ) ;
#10235=CARTESIAN_POINT ( 'NONE',  ( 2.313015868914463091, -1.601887806243259771, 1.311650804931147274 ) ) ;
#10238=CARTESIAN_POINT ( 'NONE',  ( 4.670628115925999246, 0.8122961462209904449, 1.958930372594757330 ) ) ;
#10240=CARTESIAN_POINT ( 'NONE',  ( 0.4692025345035084061, 0.1902923850431673669, -1.917074784726199965 ) ) ;
#10247=CARTESIAN_POINT ( 'NONE',  ( -0.1399463097118925359, -1.722747986054250058, -1.402038615606171046 ) ) ;
#10248=CARTESIAN_POINT ( 'NONE',  ( 2.520660759794272732, 1.376564137786383091, -1.593852158419235332 ) ) ;
#10251=CARTESIAN_POINT ( 'NONE',  ( 6.086726144739807332, 1.793049480792831440, 0.4976782122840143763 ) ) ;
#10258=CARTESIAN_POINT ( 'NONE',  ( 0.1410940620840978044, 2.031152781523197337, 0.6094965309384676733 ) ) ;
#10260=CARTESIAN_POINT ( 'NONE',  ( 2.224987305166142626, -1.792472147789250236, -0.7979012372742313453 ) ) ;
#10261=CARTESIAN_POINT ( 'NONE',  ( 0.8312129145573650124, 0.1600495679085281175, 2.155820468135719814 ) ) ;
#10265=CARTESIAN_POINT ( 'NONE',  ( 2.817972641794503019, 1.638747005868109285, 0.5862587914967545277 ) ) ;
#10268=CARTESIAN_POINT ( 'NONE',  ( 2.776720060080526853, -1.994564479802892087, 0.2930246351905210211 ) ) ;
#10269=CARTESIAN_POINT ( 'NONE',  ( 6.825078400183548943, 1.222324429417048330, 2.356141576552318817 ) ) ;
#10271=CARTESIAN_POINT ( 'NONE',  ( 1.815242386724497337, -0.2434097785052463103, 1.956328700473447979 ) ) ;
#10272=CARTESIAN_POINT ( 'NONE',  ( 5.976807594091997800, -1.347613670528555740, 1.357171208065083512 ) ) ;
#10278=CARTESIAN_POINT ( 'NONE',  ( 1.207682226051248753, 1.530763495831432452, 1.317637323925124671 ) ) ;
#10281=CARTESIAN_POINT ( 'NONE',  ( 5.315557996638371918, -0.3450676865139382099, 2.281540517825955128 ) ) ;
#10282=CARTESIAN_POINT ( 'NONE',  ( 5.406682003534418079, 0.5678430586343993225, 1.877905798087247335 ) ) ;
#10283=CARTESIAN_POINT ( 'NONE',  ( 2.658977320520792276, 1.578554556127611308, -1.164590279592196298 ) ) ;
#10285=CARTESIAN_POINT ( 'NONE',  ( 1.108046318188542489, -0.04667474159409169127, 2.016033875899234662 ) ) ;
#10287=CARTESIAN_POINT ( 'NONE',  ( 0.9896463964080002285, -0.5083134511523321741, 2.055333615346987663 ) ) ;
#10290=CARTESIAN_POINT ( 'NONE',  ( 1.640310086786896049, -1.556016536173940645, 0.9838780322720328542 ) ) ;
#10293=CARTESIAN_POINT ( 'NONE',  ( 2.689816194747224110, 2.012238202079220439, -0.6693303307304664385 ) ) ;
#10297=CARTESIAN_POINT ( 'NONE',  ( 3.638010413220875705, 0.9297346566990055683, -1.839232330223056433 ) ) ;
#10300=CARTESIAN_POINT ( 'NONE',  ( 1.294213439101927321, 1.504999338701202394, -1.060447551955064016 ) ) ;
#10304=CARTESIAN_POINT ( 'NONE',  ( 0.9267433102794273569, 1.311770220233858586, -1.774563083084364834 ) ) ;
#10305=CARTESIAN_POINT ( 'NONE',  ( 2.935161367736533133, 0.2740405928264351143, 2.245665650516134093 ) ) ;
#10307=CARTESIAN_POINT ( 'NONE',  ( 2.162115752888054576, 1.811270999727595976, 0.04120172278379052866 ) ) ;
#10308=CARTESIAN_POINT ( 'NONE',  ( 2.659291035590090058, 1.817528298045675061, -0.6055613653334031010 ) ) ;
#10309=CARTESIAN_POINT ( 'NONE',  ( 4.369627354678314646, -0.3570511267821044332, 2.039192500141631115 ) ) ;
#10311=CARTESIAN_POINT ( 'NONE',  ( 2.694160965578366262, -1.966063403948969057, -0.1468289651068572232 ) ) ;
#10312=CARTESIAN_POINT ( 'NONE',  ( 0.1121488755844394364, -0.8197171475488943537, -1.741376145853351431 ) ) ;
#10313=CARTESIAN_POINT ( 'NONE',  ( 3.906994808788874174, 1.604092888448312326, 0.9621832354540849064 ) ) ;
#10315=CARTESIAN_POINT ( 'NONE',  ( 2.491230068042503465, -0.3961224009183231809, -2.273300736686647117 ) ) ;
#10317=CARTESIAN_POINT ( 'NONE',  ( 3.402650393365719506, 0.4499446578831092780, 1.805719076957598368 ) ) ;
#10322=CARTESIAN_POINT ( 'NONE',  ( 0.3113324583694621617, 1.833617258854224552, 1.035894449818143270 ) ) ;
#10324=CARTESIAN_POINT ( 'NONE',  ( 6.204392391313840349, -0.7715976231806519481, -2.019385000091134419 ) ) ;
#10325=CARTESIAN_POINT ( 'NONE',  ( -0.2048590494372501680, -0.1558505989666530422, -1.986559690435693026 ) ) ;
#10329=CARTESIAN_POINT ( 'NONE',  ( 6.925078400183545035, 0.003529629153843985134, 1.755452343125718073 ) ) ;
#10331=CARTESIAN_POINT ( 'NONE',  ( -0.2104748580754183807, 4.084054299358617079, -2.658391380015924010 ) ) ;
#10332=CARTESIAN_POINT ( 'NONE',  ( 5.243375144629232487, 0.3886363430659239837, -1.978554426619572926 ) ) ;
#10335=CARTESIAN_POINT ( 'NONE',  ( 6.438358464623771482, 2.137424745569570295, 0.3223339197731683869 ) ) ;
#10339=CARTESIAN_POINT ( 'NONE',  ( 6.151970292378349470, 1.039009440890667824, 1.727993850779283802 ) ) ;
#10342=CARTESIAN_POINT ( 'NONE',  ( 6.883263157960362477, 3.690127339433949327, 2.567897385111846731 ) ) ;
#10344=CARTESIAN_POINT ( 'NONE',  ( 1.470901328764297800, 0.1297424413324743397, -1.720050270840302487 ) ) ;
#10348=CARTESIAN_POINT ( 'NONE',  ( 0.6668358675281795822, 0.1816249057532189626, -1.760414781625377234 ) ) ;
#10349=CARTESIAN_POINT ( 'NONE',  ( 1.840491241682026047, 1.157229580565920513, -1.647056139248611384 ) ) ;
#10352=CARTESIAN_POINT ( 'NONE',  ( 4.471826267013489620, 2.141383520707430321, -0.5327586567505787629 ) ) ;
#10353=CARTESIAN_POINT ( 'NONE',  ( 5.418865745523654631, -1.577555059383651814, 1.491859142196997334 ) ) ;
#10357=CARTESIAN_POINT ( 'NONE',  ( 3.211701520346501582, 1.672844727185973657, 1.303009041611735030 ) ) ;
#10358=CARTESIAN_POINT ( 'NONE',  ( 3.146111402376899235, 0.9091623069825971459, 1.799915193831227889 ) ) ;
#10359=CARTESIAN_POINT ( 'NONE',  ( 3.920002888225936566, -1.806327840557620412, 0.1390898763422818984 ) ) ;
#10364=CARTESIAN_POINT ( 'NONE',  ( 0.5318453760667535279, 0.9654296485097980662, -1.602142582367314549 ) ) ;
#10365=CARTESIAN_POINT ( 'NONE',  ( 5.777927443424748510, 1.091106472389313131, 1.463626628978510702 ) ) ;
#10367=CARTESIAN_POINT ( 'NONE',  ( 1.147507391605587568, 1.886754179610318438, -0.3309440326291489542 ) ) ;
#10375=CARTESIAN_POINT ( 'NONE',  ( 3.410498715577559015, -2.118327196165440185, -0.1003008382433126094 ) ) ;
#10379=CARTESIAN_POINT ( 'NONE',  ( 4.393795938483449071, -0.7573388051436024115, 1.820269059793070410 ) ) ;
#10380=CARTESIAN_POINT ( 'NONE',  ( 6.082274476537278041, 0.9889857280602430967, 1.636697341158253272 ) ) ;
#10382=CARTESIAN_POINT ( 'NONE',  ( 0.2986504545328653726, 1.456477371935499088, -1.536899124724122601 ) ) ;
#10384=CARTESIAN_POINT ( 'NONE',  ( 1.768117254402020277, -2.054967671486531255, 0.2513356459030794410 ) ) ;
#10385=CARTESIAN_POINT ( 'NONE',  ( 2.660020691486902233, -1.338829530657672073, 1.406886975181226296 ) ) ;
#10389=CARTESIAN_POINT ( 'NONE',  ( 3.205106881211945868, -0.4073652088906943858, 2.050380944992454602 ) ) ;
#10392=CARTESIAN_POINT ( 'NONE',  ( 0.4514444101613367955, -1.279852094280601760, -1.282217761895942720 ) ) ;
#10394=CARTESIAN_POINT ( 'NONE',  ( 5.127635347277352373, -2.096377701570474539, 0.6897739467496829535 ) ) ;
#10397=CARTESIAN_POINT ( 'NONE',  ( 3.135963548190400019, -1.480894843444351849, -1.636267651353009445 ) ) ;
#10400=CARTESIAN_POINT ( 'NONE',  ( 1.594246750649646494, -1.022002606473694675, 1.616071880676916317 ) ) ;
#10402=CARTESIAN_POINT ( 'NONE',  ( 5.459458695672200435, 1.690470114046587646, 1.195012289465044564 ) ) ;
#10404=CARTESIAN_POINT ( 'NONE',  ( 2.799875798528407511, -0.6792266858460673795, 2.052276964324008635 ) ) ;
#10405=CARTESIAN_POINT ( 'NONE',  ( 4.687173145698103838, 1.624054394666199830, 1.471728111018810070 ) ) ;
#10416=CARTESIAN_POINT ( 'NONE',  ( 5.453992358814952368, -0.7503507308065425763, 1.929658000011783336 ) ) ;
#10417=CARTESIAN_POINT ( 'NONE',  ( 3.932187577746598883, 1.029727551008235320, -1.628035494724868970 ) ) ;
#10418=CARTESIAN_POINT ( 'NONE',  ( 6.609000000000050612, -6.653734691735092887E-05, 2.100160721423645960 ) ) ;
#10422=CARTESIAN_POINT ( 'NONE',  ( 5.278159644759479185, -1.050164822159710853, -1.665878549478349013 ) ) ;
#10423=CARTESIAN_POINT ( 'NONE',  ( 6.544901331262317434, -1.836973039681317088, -1.370978055005685370 ) ) ;
#10424=CARTESIAN_POINT ( 'NONE',  ( 4.969292227364340953, 0.1756445257206709631, -1.817221496977147854 ) ) ;
#10431=CARTESIAN_POINT ( 'NONE',  ( 2.138008341990283778, 0.4048980806483238326, 1.796005048712509655 ) ) ;
#10432=CARTESIAN_POINT ( 'NONE',  ( 6.240495565780414644, 1.155569484861172391, -1.648366056897664800 ) ) ;
#10433=CARTESIAN_POINT ( 'NONE',  ( 1.142455020822298106, -0.05817821010643645790, -2.297781139197229372 ) ) ;
#10434=CARTESIAN_POINT ( 'NONE',  ( 5.067221110791254368, 1.704927679941736329, 0.9703409489375602881 ) ) ;
#10438=CARTESIAN_POINT ( 'NONE',  ( 0.6079806153083644471, 0.6509857562557037625, -1.965403638620793147 ) ) ;
#10440=CARTESIAN_POINT ( 'NONE',  ( 1.646151360528936625, 0.6591259108063004524, 1.984184313626126350 ) ) ;
#10441=CARTESIAN_POINT ( 'NONE',  ( 0.2857447052702493662, -0.8859512962964136706, 1.647562673099879138 ) ) ;
#10443=CARTESIAN_POINT ( 'NONE',  ( -0.2104748580754183529, 0.2283854016844401591, -2.137091067173245929 ) ) ;
#10444=CARTESIAN_POINT ( 'NONE',  ( 1.575334329707895664, -0.9311816076861539893, 1.470162731330543426 ) ) ;
#10448=CARTESIAN_POINT ( 'NONE',  ( 2.332253321102405685, 1.672780984221501122, 0.4201815020834080427 ) ) ;
#10449=CARTESIAN_POINT ( 'NONE',  ( 3.280998142716429200, 1.980384277226649559, -0.9389412094223739125 ) ) ;
#10450=CARTESIAN_POINT ( 'NONE',  ( 0.1407077508718111714, 0.6607813331330723017, 1.603534759577706303 ) ) ;
#10451=CARTESIAN_POINT ( 'NONE',  ( 5.092482806099829062, -2.189899077852827780, -0.2726905915074183673 ) ) ;
#10453=CARTESIAN_POINT ( 'NONE',  ( 2.764704757504053756, -0.8271204958998740198, -2.007528505447711886 ) ) ;
#10454=CARTESIAN_POINT ( 'NONE',  ( 1.418276456094772708, 1.227529518603141190, -1.351586893430449576 ) ) ;
#10455=CARTESIAN_POINT ( 'NONE',  ( 3.257133915093980203, 0.04755548373316278304, -2.116953498886654295 ) ) ;
#10456=CARTESIAN_POINT ( 'NONE',  ( 6.539320575229254473, 0.5926322452488984593, 1.950287522085321301 ) ) ;
#10458=CARTESIAN_POINT ( 'NONE',  ( 3.245926457026059531, 2.292545471606484142, -0.001860936589836299044 ) ) ;
#10462=CARTESIAN_POINT ( 'NONE',  ( 5.918639493159310483, -0.7970842504121906646, -2.073522590485813666 ) ) ;
#10468=CARTESIAN_POINT ( 'NONE',  ( 4.008435526009396455, -1.928752077057366732, 0.5880193435906443389 ) ) ;
#10470=CARTESIAN_POINT ( 'NONE',  ( 1.745062578162811073, -0.2986309630071918853, -2.040702096407704058 ) ) ;
#10475=CARTESIAN_POINT ( 'NONE',  ( 4.927760762764835434, 1.128268568998530563, -1.878541326455762661 ) ) ;
#10476=CARTESIAN_POINT ( 'NONE',  ( 3.815077410725797424, 1.076317812134291119, -1.704938119663282903 ) ) ;
#10477=CARTESIAN_POINT ( 'NONE',  ( 2.102840161960460197, -0.4018910908503615653, 1.796694178532439956 ) ) ;
#10481=CARTESIAN_POINT ( 'NONE',  ( 5.842758758449526191, 0.3585452818064547853, 1.789846783968067845 ) ) ;
#10483=CARTESIAN_POINT ( 'NONE',  ( 5.981380223923965289, 2.093118249296622491, -0.8594570314751952544 ) ) ;
#10485=CARTESIAN_POINT ( 'NONE',  ( 2.069099208297279002, -1.926018337604347597, -0.8524663740339888385 ) ) ;
#10496=CARTESIAN_POINT ( 'NONE',  ( 2.355864820516640812, -1.574449018071517825, -1.420800595792824028 ) ) ;
#10497=CARTESIAN_POINT ( 'NONE',  ( 2.496574912728947382, -1.137965521849234607, 1.907653428263719864 ) ) ;
#10498=CARTESIAN_POINT ( 'NONE',  ( 0.5400322017136415242, -1.563516176313231920, -1.557742479837947558 ) ) ;
#10501=CARTESIAN_POINT ( 'NONE',  ( 4.000408739481801312, 1.952204270133122810, 0.1946113827649766925 ) ) ;
#10509=CARTESIAN_POINT ( 'NONE',  ( 3.252298345715322281, 0.9499829135306799843, -1.895951488860507128 ) ) ;
#10511=CARTESIAN_POINT ( 'NONE',  ( 4.311504812833309330, -0.3723461477018601973, 2.129241309423899775 ) ) ;
#10512=CARTESIAN_POINT ( 'NONE',  ( 3.702549152423353807, 1.581054339307564449, 0.9433870219286569769 ) ) ;
#10515=CARTESIAN_POINT ( 'NONE',  ( 5.753775850233431299, 0.7111499035084413167, 1.588595604753391122 ) ) ;
#10516=CARTESIAN_POINT ( 'NONE',  ( 6.827182134110188372, 3.700652156503980716, 2.425390344263624431 ) ) ;
#10520=CARTESIAN_POINT ( 'NONE',  ( 2.483474991488154870, 1.976725341044349271, -0.8753317036461552014 ) ) ;
#10521=CARTESIAN_POINT ( 'NONE',  ( 5.184922634274871989, -1.076153828860962225, -1.704676470440001701 ) ) ;
#10523=CARTESIAN_POINT ( 'NONE',  ( 1.868271315571629509, 1.111147431007172726, 1.854118885846419262 ) ) ;
#10524=CARTESIAN_POINT ( 'NONE',  ( 3.532457849674102590, 1.922574350601889082, 0.4351428330651128662 ) ) ;
#10526=CARTESIAN_POINT ( 'NONE',  ( 0.6929124517485165669, -2.290651033777380441, -0.2787006195923043550 ) ) ;
#10527=CARTESIAN_POINT ( 'NONE',  ( 4.985854738014197984, -1.927824157794202353, -0.2341192097771953584 ) ) ;
#10532=CARTESIAN_POINT ( 'NONE',  ( -0.02224634325198420262, -0.007204097619508141419, -2.289079630542791399 ) ) ;
#10536=CARTESIAN_POINT ( 'NONE',  ( 2.274722540679521288, -1.357913018379176995, 1.739418515187239223 ) ) ;
#10538=CARTESIAN_POINT ( 'NONE',  ( 6.403176761927252159, -1.659045864033869666, 1.046607237317781269 ) ) ;
#10542=CARTESIAN_POINT ( 'NONE',  ( 0.1749903794560592751, 2.884130749173496877, -2.444045186936738112 ) ) ;
#10543=CARTESIAN_POINT ( 'NONE',  ( 5.613187951484799321, -1.795345830453990654, 0.4073638586896133340 ) ) ;
#10549=CARTESIAN_POINT ( 'NONE',  ( 6.539320575229233157, 0.001224430076711413356, 2.103502572931112091 ) ) ;
#10552=CARTESIAN_POINT ( 'NONE',  ( 0.3388364525104338165, 0.3516977924403408284, 2.030485180972623205 ) ) ;
#10554=CARTESIAN_POINT ( 'NONE',  ( 2.101794631558097315, 0.7159089574285321111, -1.718054499674229074 ) ) ;
#10555=CARTESIAN_POINT ( 'NONE',  ( 4.282634502089007533, 1.642705626968201216, -0.8318752211165170163 ) ) ;
#10561=CARTESIAN_POINT ( 'NONE',  ( 4.494872972331320327, -0.4818267175418550208, -2.153482813429814069 ) ) ;
#10562=CARTESIAN_POINT ( 'NONE',  ( 5.888003241735360938, -1.025016604251761221, 2.016990234832950701 ) ) ;
#10564=CARTESIAN_POINT ( 'NONE',  ( 5.800986464141828058, -0.2745434460682676936, -1.790553645544520345 ) ) ;
#10565=CARTESIAN_POINT ( 'NONE',  ( -0.01248194115436446205, -0.5331630387654020531, 1.944732228473695868 ) ) ;
#10568=CARTESIAN_POINT ( 'NONE',  ( 6.890000000000050306, -0.002781820520068867264, 1.999840353888074240 ) ) ;
#10569=CARTESIAN_POINT ( 'NONE',  ( 5.514289750425454883, -1.912461473380810961, 0.004301308668797076962 ) ) ;
#10572=CARTESIAN_POINT ( 'NONE',  ( 0.4087956859853311142, 1.625333209436867321, 0.9259686016569528277 ) ) ;
#10573=CARTESIAN_POINT ( 'NONE',  ( 2.852750215419812108, -1.865046845876184189, -0.7672916333427428626 ) ) ;
#10575=CARTESIAN_POINT ( 'NONE',  ( 4.406922956430887162, 1.628233754946675882, -1.335794222675233511 ) ) ;
#10580=CARTESIAN_POINT ( 'NONE',  ( 3.129170305635332383, 1.827809467758968243, 0.8596994449004448091 ) ) ;
#10583=CARTESIAN_POINT ( 'NONE',  ( 4.921240491056324551, -0.1114908479964340365, 2.158860929761210912 ) ) ;
#10589=CARTESIAN_POINT ( 'NONE',  ( 1.680376142759659075, -1.205403815041187210, -1.805639882349929781 ) ) ;
#10591=CARTESIAN_POINT ( 'NONE',  ( 0.5558949066124979632, -1.334021266253348381, 1.269314063962425854 ) ) ;
#10593=CARTESIAN_POINT ( 'NONE',  ( 1.786939262935317130, 1.904797134731281538, -1.083727916527020607 ) ) ;
#10595=CARTESIAN_POINT ( 'NONE',  ( 3.133911187764222728, -1.518274094020392706, -1.677614996870570918 ) ) ;
#10602=CARTESIAN_POINT ( 'NONE',  ( 4.200303217096891473, -0.5537481437246688509, -1.680960689856024537 ) ) ;
#10604=CARTESIAN_POINT ( 'NONE',  ( 1.044129769988952683, 0.8535497088724073311, -1.925424821390888663 ) ) ;
#10608=CARTESIAN_POINT ( 'NONE',  ( 6.345327396762703742, 0.3419173589993273477, -1.987050850726256979 ) ) ;
#10609=CARTESIAN_POINT ( 'NONE',  ( 5.115404481452859642, 1.485474843905653985, 1.036646722175238011 ) ) ;
#10612=CARTESIAN_POINT ( 'NONE',  ( 3.678450976403758066, -1.802590750232490491, -0.4997190347926713794 ) ) ;
#10613=CARTESIAN_POINT ( 'NONE',  ( 3.871986384844767315, -2.040452582458017083, 0.3490408808229996662 ) ) ;
#10621=CARTESIAN_POINT ( 'NONE',  ( 4.105873170248697690, 0.6631157982108953908, -1.846516426336957784 ) ) ;
#10622=CARTESIAN_POINT ( 'NONE',  ( 0.7552322466577044979, -2.000550463317086525, -0.2495714061315074117 ) ) ;
#10625=CARTESIAN_POINT ( 'NONE',  ( 1.545950201917587696, 1.868165254341861647, 0.09716206808172561660 ) ) ;
#10627=CARTESIAN_POINT ( 'NONE',  ( 3.164317521226766239, 2.013376229028215558, -0.004237188189804701709 ) ) ;
#10629=CARTESIAN_POINT ( 'NONE',  ( 2.952857568058687043, -1.957288919824872186, -0.8077276291160383481 ) ) ;
#10631=CARTESIAN_POINT ( 'NONE',  ( 5.353992430378140099, -0.7485205528568983357, 1.930488744064068785 ) ) ;
#10633=CARTESIAN_POINT ( 'NONE',  ( 0.01142647129402651375, -2.049560973810752085, 0.4120210816158270117 ) ) ;
#10635=CARTESIAN_POINT ( 'NONE',  ( 5.385714059857480862, 1.227405483141888132, 1.351559456777707835 ) ) ;
#10640=CARTESIAN_POINT ( 'NONE',  ( 6.370183515248876382, 1.128980158350336049, 1.895982279999992359 ) ) ;
#10642=CARTESIAN_POINT ( 'NONE',  ( 6.252599623108594074, 1.892168639490459325, 0.2757424028280440753 ) ) ;
#10654=CARTESIAN_POINT ( 'NONE',  ( 0.07700591528354228110, 6.948790505698306141, -2.505847838500625979 ) ) ;
#10658=CARTESIAN_POINT ( 'NONE',  ( -0.1405533004718703405, 5.725074605807632722, -2.314389626777931586 ) ) ;
#10661=CARTESIAN_POINT ( 'NONE',  ( 2.676555125969529048, 1.290216341703333436, -1.488019019629209572 ) ) ;
#10662=CARTESIAN_POINT ( 'NONE',  ( 3.849232595480827079, 0.2440098934328518987, -2.001514877671112025 ) ) ;
#10664=CARTESIAN_POINT ( 'NONE',  ( 6.827182134110199918, 0.5620517916639695688, 2.240906645742099190 ) ) ;
#10665=CARTESIAN_POINT ( 'NONE',  ( 3.802820697025221630, 1.879323313303274734, 1.126966401794778250 ) ) ;
#10667=CARTESIAN_POINT ( 'NONE',  ( 1.711812753757115502, -1.912122584522325086, 0.2334695860961126246 ) ) ;
#10670=CARTESIAN_POINT ( 'NONE',  ( 0.1329588055935214397, 0.7520877941899367647, -1.931583167801545819 ) ) ;
#10678=CARTESIAN_POINT ( 'NONE',  ( 5.935073298327618652, -1.338256116417003927, -1.264887592264056559 ) ) ;
#10679=CARTESIAN_POINT ( 'NONE',  ( 3.387361027847039185, 0.04724124570358113201, -2.012690625139363032 ) ) ;
#10680=CARTESIAN_POINT ( 'NONE',  ( 4.358954191739877082, -0.8846011062542002978, 2.121510506163324372 ) ) ;
#10681=CARTESIAN_POINT ( 'NONE',  ( -0.1290005225502433017, 0.6921039065478848951, -2.255494067288220439 ) ) ;
#10682=CARTESIAN_POINT ( 'NONE',  ( 2.149040161283378936, 1.622117262959487549, -0.9118680782764712056 ) ) ;
#10688=CARTESIAN_POINT ( 'NONE',  ( 4.599217410553211316, -0.5561919879800735211, 2.015351296096360656 ) ) ;
#10689=CARTESIAN_POINT ( 'NONE',  ( 4.908994958506140982, 1.627828031611065152, 0.9215782234750914403 ) ) ;
#10694=CARTESIAN_POINT ( 'NONE',  ( 6.445920802586958764, 0.6525945181424031016, -1.596887126696917791 ) ) ;
#10697=CARTESIAN_POINT ( 'NONE',  ( 1.160356219728400307, 1.032376606561947741, 1.393149478428891364 ) ) ;
#10702=CARTESIAN_POINT ( 'NONE',  ( 6.016515519638066856, 0.8726334679417474538, 1.988148615226674298 ) ) ;
#10703=CARTESIAN_POINT ( 'NONE',  ( 4.371595934376539816, 1.770262903079304451, -0.4459408992859363319 ) ) ;
#10704=CARTESIAN_POINT ( 'NONE',  ( 1.885527806591394961, -1.848987351811198998, 0.6559936482007988623 ) ) ;
#10705=CARTESIAN_POINT ( 'NONE',  ( 6.503150284217945831, -0.1439854277452867481, 2.084527530714448407 ) ) ;
#10710=CARTESIAN_POINT ( 'NONE',  ( 2.877707679121459083, 0.3088738507561124558, -2.097740099398600400 ) ) ;
#10714=CARTESIAN_POINT ( 'NONE',  ( 0.3036855567021545244, -1.598042064648269811, -1.315789336611736138 ) ) ;
#10717=CARTESIAN_POINT ( 'NONE',  ( 3.756649600333416217, 2.210663847611141986, 0.2169408864148083815 ) ) ;
#10719=CARTESIAN_POINT ( 'NONE',  ( 0.4054594355042361875, -1.236789717346518769, -1.937488090237641014 ) ) ;
#10721=CARTESIAN_POINT ( 'NONE',  ( 6.702015009205530838, 0.7948373677021604022, -1.903462506645931640 ) ) ;
#10724=CARTESIAN_POINT ( 'NONE',  ( 0.1331565106231571705, 2.881392620029461504, -2.434650611646618223 ) ) ;
#10725=CARTESIAN_POINT ( 'NONE',  ( 5.231922985772964552, 1.814955821992572993, 0.3091130605668013231 ) ) ;
#10727=CARTESIAN_POINT ( 'NONE',  ( -0.2102771530458459603, 6.947233595868168798, -2.798738817348767949 ) ) ;
#10728=CARTESIAN_POINT ( 'NONE',  ( 2.608071471510875039, -0.6576475463303601554, -1.594674760072743114 ) ) ;
#10729=CARTESIAN_POINT ( 'NONE',  ( 1.727750297885573882, 0.7672897036171549834, -1.865047645237365215 ) ) ;
#10730=CARTESIAN_POINT ( 'NONE',  ( 3.252836000005991046, 2.242300829042419785, -0.5054477054214584486 ) ) ;
#10731=CARTESIAN_POINT ( 'NONE',  ( 2.530887537405112298, 2.193952394701288000, 0.5517939747049571686 ) ) ;
#10732=CARTESIAN_POINT ( 'NONE',  ( 4.758481774355417748, 0.8053329972168337125, 1.946216683261194236 ) ) ;
#10734=CARTESIAN_POINT ( 'NONE',  ( 3.286155083303475166, -1.742946490318267205, -0.3057894240724549628 ) ) ;
#10737=CARTESIAN_POINT ( 'NONE',  ( 6.286719507307084065, 1.996765193862446885, -1.125943789698529818 ) ) ;
#10738=CARTESIAN_POINT ( 'NONE',  ( 4.435397664686764330, 0.7849604969769330420, -1.665558179074405620 ) ) ;
#10742=CARTESIAN_POINT ( 'NONE',  ( 4.716832014018703667, -0.1092502567305031480, 2.188841582221649595 ) ) ;
#10745=CARTESIAN_POINT ( 'NONE',  ( 4.967269779104159788, 1.799668380515653920, 1.023422521214325309 ) ) ;
#10746=CARTESIAN_POINT ( 'NONE',  ( 0.4093891192313535710, -1.913260280790154866, 0.6371585790938688598 ) ) ;
#10748=CARTESIAN_POINT ( 'NONE',  ( 3.475144788579834110, 0.04656949993332368254, -1.926097043150078791 ) ) ;
#10751=CARTESIAN_POINT ( 'NONE',  ( 0.01825978460381037782, -0.5840345307000054387, 2.143236301556954881 ) ) ;
#10752=ORIENTED_EDGE ( 'NONE', *, *, #6489, .F. ) ;
#10758=CARTESIAN_POINT ( 'NONE',  ( 1.732786548908150648, -1.861864252656076912, -0.6185235971247132758 ) ) ;
#10761=CARTESIAN_POINT ( 'NONE',  ( 5.037533845850875380, 1.831247050742194515, -0.7043679133837479345 ) ) ;
#10764=CARTESIAN_POINT ( 'NONE',  ( 6.666866396406604167, -1.974176978123330040, -0.8811043787171415342 ) ) ;
#10765=CARTESIAN_POINT ( 'NONE',  ( -0.2104748580754409182, 6.947232144882289795, -2.698723162346649662 ) ) ;
#10769=CARTESIAN_POINT ( 'NONE',  ( 6.925078400183515726, -0.002206826874838820583, 1.955452213090567160 ) ) ;
#10770=CARTESIAN_POINT ( 'NONE',  ( 6.485661447747480324, 1.619333758318822536, 0.6201139256068515238 ) ) ;
#10772=CARTESIAN_POINT ( 'NONE',  ( 2.595491417077447238, -0.6846416945752286098, 2.081959150545972914 ) ) ;
#10773=CARTESIAN_POINT ( 'NONE',  ( 4.383989010750934945, 1.503879422573949132, 1.750323999079455684 ) ) ;
#10774=CARTESIAN_POINT ( 'NONE',  ( 6.309851081105539272, -2.045767358615140807, 0.2475669877257078710 ) ) ;
#10775=CARTESIAN_POINT ( 'NONE',  ( 2.202979905913711178, -0.4252542987780962291, 1.894666818490578164 ) ) ;
#10778=CARTESIAN_POINT ( 'NONE',  ( 4.816704082729271086, -0.7169179515637627009, -1.995842421597990413 ) ) ;
#10779=CARTESIAN_POINT ( 'NONE',  ( 2.602185585689294367, -0.1948409242511044692, 2.006959980107574371 ) ) ;
#10781=CARTESIAN_POINT ( 'NONE',  ( 5.772568991252683190, -1.404203161598962968, 1.702366421003978392 ) ) ;
#10784=CARTESIAN_POINT ( 'NONE',  ( 0.1526014871912773629, -1.468541917219987836, 1.084465738218153064 ) ) ;
#10790=CARTESIAN_POINT ( 'NONE',  ( 5.313377624208335703, -0.3045090135303843981, 2.038146128872863283 ) ) ;
#10792=CARTESIAN_POINT ( 'NONE',  ( -0.2108831679771167866, 1.375689764684871808, -2.152500126786048185 ) ) ;
#10795=CARTESIAN_POINT ( 'NONE',  ( 4.125652552961744490, -0.3430436748357457710, 1.990152796604119034 ) ) ;
#10801=CARTESIAN_POINT ( 'NONE',  ( 3.819256682291353400, -0.1532216265913727837, 2.055260608361098473 ) ) ;
#10802=CARTESIAN_POINT ( 'NONE',  ( 2.549454116737331244, -1.388485404012842261, 1.462446031800922253 ) ) ;
#10808=CARTESIAN_POINT ( 'NONE',  ( 3.321638586175166719, -1.528507173905558014, 1.314795459203411676 ) ) ;
#10809=CARTESIAN_POINT ( 'NONE',  ( 2.695044507329581673, -0.5773736025265225891, 1.748335772842606106 ) ) ;
#10810=CARTESIAN_POINT ( 'NONE',  ( 1.366329765314050482, 2.272867617333930390, -0.3986118548820920537 ) ) ;
#10812=CARTESIAN_POINT ( 'NONE',  ( 2.548304106926166490, 2.161049004374314464, 0.05582717182670697553 ) ) ;
#10816=CARTESIAN_POINT ( 'NONE',  ( 1.639302681421180852, -1.352760811461351187, -1.292285834730775074 ) ) ;
#10818=CARTESIAN_POINT ( 'NONE',  ( 5.858272006539261056, 0.7985356142178706707, 1.802671990260945156 ) ) ;
#10822=CARTESIAN_POINT ( 'NONE',  ( 0.5048604690408053930, -0.7474223562033958101, -2.076596198196341003 ) ) ;
#10823=CARTESIAN_POINT ( 'NONE',  ( 6.725056259267968350, -1.891221747171191403, -0.8428681758992571105 ) ) ;
#10826=CARTESIAN_POINT ( 'NONE',  ( 6.539320575229233157, 0.001224430076711413356, 2.103502572931112091 ) ) ;
#10827=CARTESIAN_POINT ( 'NONE',  ( 5.225445458360559847, -1.872321802520343414, 0.6175577138636638708 ) ) ;
#10828=CARTESIAN_POINT ( 'NONE',  ( 6.205333298273250975, 1.755376394247827987, -0.9990029765977179732 ) ) ;
#10829=CARTESIAN_POINT ( 'NONE',  ( 3.985262446249608903, -0.2245550567474114134, -2.296750103337093396 ) ) ;
#10830=CARTESIAN_POINT ( 'NONE',  ( 2.676693276584718895, 1.350517573672470606, -1.558986216346124776 ) ) ;
#10837=CARTESIAN_POINT ( 'NONE',  ( 5.424361751532248199, 1.065549429306617446, 1.891644033573415040 ) ) ;
#10839=CARTESIAN_POINT ( 'NONE',  ( 4.563899478665734755, -1.199029595066217313, 1.397436126395680267 ) ) ;
#10842=CARTESIAN_POINT ( 'NONE',  ( 5.091441847573507928, -0.7891374179831472935, 2.044738775321436997 ) ) ;
#10844=CARTESIAN_POINT ( 'NONE',  ( 6.649321564832020748, -1.812311508879884459, -1.354277771019767762 ) ) ;
#10850=CARTESIAN_POINT ( 'NONE',  ( 0.6195364366361589825, -0.9414703481081601044, -1.498462015107356882 ) ) ;
#10852=CARTESIAN_POINT ( 'NONE',  ( 5.654944829759325664, 0.3949471196958070918, 1.973809479704929704 ) ) ;
#10854=CARTESIAN_POINT ( 'NONE',  ( 3.663195928028176063, -1.856456087625086182, -0.9943140874985546551 ) ) ;
#10855=CARTESIAN_POINT ( 'NONE',  ( 3.198755040744692302, 1.733147561012362559, 0.8161988141396243623 ) ) ;
#10857=CARTESIAN_POINT ( 'NONE',  ( 4.176189586714727398, -1.010410353755032409, -1.690456409470885824 ) ) ;
#10858=CARTESIAN_POINT ( 'NONE',  ( 5.396742217995451618, -1.971451684502657287, -0.4385051361721309937 ) ) ;
#10859=CARTESIAN_POINT ( 'NONE',  ( 1.498681428038322050, 1.531199225506232553, -1.074333469806128427 ) ) ;
#10860=CARTESIAN_POINT ( 'NONE',  ( 5.092313435308955860, -1.712476623254995278, -0.2059198849207622417 ) ) ;
#10861=CARTESIAN_POINT ( 'NONE',  ( 1.388764059443419407, -1.816923020173771830, -0.5969786173363604842 ) ) ;
#10863=CARTESIAN_POINT ( 'NONE',  ( 1.823171247573553311, 2.059948494222668014, 0.7922594597074559264 ) ) ;
#10866=CARTESIAN_POINT ( 'NONE',  ( 6.250445965835445428, -1.952298026214387194, -0.1936728439068043650 ) ) ;
#10873=CARTESIAN_POINT ( 'NONE',  ( 1.768117254402020277, -2.054967671486531255, 0.2513356459030794410 ) ) ;
#10878=CARTESIAN_POINT ( 'NONE',  ( 6.217454246653871586, 1.762742247767977055, 1.178343227268910054 ) ) ;
#10883=CARTESIAN_POINT ( 'NONE',  ( 5.307970166423544356, -1.730600239375930549, 1.034008556546859969 ) ) ;
#10884=CARTESIAN_POINT ( 'NONE',  ( 4.874201634824506080, -1.902012294098894829, -0.2279625308443770371 ) ) ;
#10886=CARTESIAN_POINT ( 'NONE',  ( 2.823975127348026248, 1.215230906543849354, -1.823574674616668556 ) ) ;
#10887=CARTESIAN_POINT ( 'NONE',  ( 0.1335669894368890498, 2.867242032283002562, -2.641834823421157719 ) ) ;
#10889=CARTESIAN_POINT ( 'NONE',  ( 5.396744779746093457, -1.965104602953187563, -0.4368240711251635822 ) ) ;
#10890=CARTESIAN_POINT ( 'NONE',  ( 1.652457426684301955, 1.892030339952909035, 0.2773405859870237133 ) ) ;
#10893=CARTESIAN_POINT ( 'NONE',  ( -0.1409997244346088141, -0.002808977843308038680, -2.000147647483838220 ) ) ;
#10895=CARTESIAN_POINT ( 'NONE',  ( 3.474242889556743652, -2.015522812629696237, -0.5555695364270489822 ) ) ;
#10897=CARTESIAN_POINT ( 'NONE',  ( 1.588428401085600461, -0.2480725091915989278, -1.706701089166535512 ) ) ;
#10898=EDGE_LOOP ( 'NONE', ( #50583, #111180 ) ) ;
#10907=CARTESIAN_POINT ( 'NONE',  ( 2.350024359177401490, 0.8526225883829393615, -1.598239438867412820 ) ) ;
#10913=CARTESIAN_POINT ( 'NONE',  ( 3.633306742369224462, -0.1297899475344466980, 1.806866856981071967 ) ) ;
#10917=CARTESIAN_POINT ( 'NONE',  ( 4.334314691326750513, -1.072585289120084440, 1.520660633866082634 ) ) ;
#10918=CARTESIAN_POINT ( 'NONE',  ( 1.915515091613760656, -1.252924113133683237, -1.449102840280371618 ) ) ;
#10919=CARTESIAN_POINT ( 'NONE',  ( 1.008509592878764183, 1.385430265305506170, -1.188947219173806413 ) ) ;
#10927=CARTESIAN_POINT ( 'NONE',  ( 6.157084851585769236, 1.612115889470520314, -1.131004145815546424 ) ) ;
#10930=CARTESIAN_POINT ( 'NONE',  ( 0.6563342376118604937, -1.512884991606887386, 1.443139479479842668 ) ) ;
#10932=CARTESIAN_POINT ( 'NONE',  ( 5.737312389570451643, -1.741366515823379757, 0.8240431586447917178 ) ) ;
#10934=CARTESIAN_POINT ( 'NONE',  ( 1.289775909805501719, -0.8246113042270180049, 1.628811597173693393 ) ) ;
#10935=CARTESIAN_POINT ( 'NONE',  ( 1.647397727484143592, -1.863059487452220386, 1.182652941231487453 ) ) ;
#10937=CARTESIAN_POINT ( 'NONE',  ( 1.212987991671743204, 1.561712320281399835, -1.103468303573502673 ) ) ;
#10939=CARTESIAN_POINT ( 'NONE',  ( 6.825064197248748243, -1.799304382776808930, -0.8012231885662893793 ) ) ;
#10940=CARTESIAN_POINT ( 'NONE',  ( 2.894010800797857108, -0.5660635412718226789, -1.857715926975093135 ) ) ;
#10942=CARTESIAN_POINT ( 'NONE',  ( 0.4212496859960760953, 0.7689994822442263178, 1.863884711849304487 ) ) ;
#10944=CARTESIAN_POINT ( 'NONE',  ( 6.455886261557550299, -0.6278800607443285609, 1.751925260802848827 ) ) ;
#10950=CARTESIAN_POINT ( 'NONE',  ( 2.033021410476544943, -1.955939774129427988, 0.9887309579383956049 ) ) ;
#10955=CARTESIAN_POINT ( 'NONE',  ( 2.297230901563730665, 1.410920830412419003, 1.158640757216542028 ) ) ;
#10961=CARTESIAN_POINT ( 'NONE',  ( 1.014139625077722595, -0.8655271193952519537, -1.721200913303379654 ) ) ;
#10963=CARTESIAN_POINT ( 'NONE',  ( 5.348475771816907809, -1.946495798708135938, -0.2439133590248846462 ) ) ;
#10968=CARTESIAN_POINT ( 'NONE',  ( 5.267185993530860699, 2.112242253262315739, -0.5839428218426812034 ) ) ;
#10971=CARTESIAN_POINT ( 'NONE',  ( 4.522371119077151391, 0.9712943915625820157, 1.828230030883712498 ) ) ;
#10975=CARTESIAN_POINT ( 'NONE',  ( 4.342621253679892490, 0.5038326875656545800, -2.242679570940506739 ) ) ;
#10979=CARTESIAN_POINT ( 'NONE',  ( 6.620655732516647518, 7.053381450551401421, 2.424417106520880161 ) ) ;
#10981=CARTESIAN_POINT ( 'NONE',  ( 4.242085645372923430, 0.5190250516928176516, 1.871238508296804604 ) ) ;
#10985=CARTESIAN_POINT ( 'NONE',  ( 5.713130151434068438, 1.559639147136464343, -1.106415316399149473 ) ) ;
#10986=CARTESIAN_POINT ( 'NONE',  ( 5.965779495465724835, 1.698367018877691370, -0.2996015908335278310 ) ) ;
#10987=CARTESIAN_POINT ( 'NONE',  ( 4.926970384345759513, -1.727065721694167832, 1.040790168839386798 ) ) ;
#10992=CARTESIAN_POINT ( 'NONE',  ( 1.359446872921949101, 2.059443214669457234, -0.3588360909314599612 ) ) ;
#10993=CARTESIAN_POINT ( 'NONE',  ( 6.872329512321287304, -1.085958120241878877, 1.397742320866280252 ) ) ;
#10994=CARTESIAN_POINT ( 'NONE',  ( 5.871720251644387822, -0.2986239867289949834, -1.994071864161291119 ) ) ;
#10996=CARTESIAN_POINT ( 'NONE',  ( 3.627152717534872561, -2.118219197452147373, 0.8765883884584676489 ) ) ;
#10997=CARTESIAN_POINT ( 'NONE',  ( 1.640152974701726496, -1.471428658003028911, 0.9289965205148569272 ) ) ;
#10998=CARTESIAN_POINT ( 'NONE',  ( 2.724977724663907530, 1.532976055022855499, -1.465462182430438798 ) ) ;
#11000=CARTESIAN_POINT ( 'NONE',  ( 0.5086469178660666390, 1.728604602589098205, 0.1357594709466679594 ) ) ;
#11002=CARTESIAN_POINT ( 'NONE',  ( 1.258004785490075994, -1.861241886096485221, -0.004951839839751126689 ) ) ;
#11003=CARTESIAN_POINT ( 'NONE',  ( 1.838563082212365085, -1.162459688571298111, 1.833603174184100792 ) ) ;
#11004=CARTESIAN_POINT ( 'NONE',  ( 3.134000194803722383, 2.016708403948695771, -0.004836970814638129855 ) ) ;
#11005=CARTESIAN_POINT ( 'NONE',  ( 4.437500000000002665, 1.451031289060936480, -1.451031289061293528 ) ) ;
#11008=CARTESIAN_POINT ( 'NONE',  ( 6.445928676245076261, 0.7346846062235148356, -1.781103304711729729 ) ) ;
#11010=CARTESIAN_POINT ( 'NONE',  ( 3.445754134864047025, -2.051236611594880799, 0.8531546545873994747 ) ) ;
#11017=CARTESIAN_POINT ( 'NONE',  ( -0.05755013669183139946, -1.372491973113322050, -1.747462644287574030 ) ) ;
#11018=CARTESIAN_POINT ( 'NONE',  ( 4.492601031306558745, 1.923586649950057792, 0.3847822903023030428 ) ) ;
#11022=CARTESIAN_POINT ( 'NONE',  ( 5.905634875922824989, -0.5580066813290808225, 2.192401876011939699 ) ) ;
#11023=CARTESIAN_POINT ( 'NONE',  ( 2.225118093709726352, -1.884898904786440177, -0.8381453960227978062 ) ) ;
#11027=CARTESIAN_POINT ( 'NONE',  ( 3.532352470753961082, 1.824241569866682289, 0.4128566369710484629 ) ) ;
#11028=CARTESIAN_POINT ( 'NONE',  ( 2.988574679986736093, -1.732066829584472556, 0.08781845822969887305 ) ) ;
#11029=CARTESIAN_POINT ( 'NONE',  ( -0.07607780150072247782, -1.417851297177070258, -1.802264747598992800 ) ) ;
#11030=CARTESIAN_POINT ( 'NONE',  ( 1.518904762042364354, 1.481482853740143657, -1.635709697223409531 ) ) ;
#11031=CARTESIAN_POINT ( 'NONE',  ( 4.293933718354110418, -0.8299404887524584051, 1.996233173270183681 ) ) ;
#11032=CARTESIAN_POINT ( 'NONE',  ( 5.279219580190475547, 1.305526251850267272, 1.437786642569781614 ) ) ;
#11034=CARTESIAN_POINT ( 'NONE',  ( 0.09375222243388467436, -1.895918425137008034, -0.7852924748299833224 ) ) ;
#11042=CARTESIAN_POINT ( 'NONE',  ( 3.721172816245840842, -0.1328194893376876962, 1.820914920514608459 ) ) ;
#11043=CARTESIAN_POINT ( 'NONE',  ( 2.450463542074859724, 2.206263077450395738, 0.05474276496272853509 ) ) ;
#11049=CARTESIAN_POINT ( 'NONE',  ( 1.054951293920348698, 0.3981946776167448188, 1.979963216457211850 ) ) ;
#11050=CARTESIAN_POINT ( 'NONE',  ( 1.664851754375612058, 0.6682523891239250391, 2.012492909199379731 ) ) ;
#11053=CARTESIAN_POINT ( 'NONE',  ( 2.992830011424299830, 0.2227009285440742226, 1.847472864794322156 ) ) ;
#11056=CARTESIAN_POINT ( 'NONE',  ( 1.147603855448702248, -1.704515299458901012, -1.329379018566230641 ) ) ;
#11062=CARTESIAN_POINT ( 'NONE',  ( 4.459475772512963232, 0.3974328844052883447, -1.781742007231662983 ) ) ;
#11066=CARTESIAN_POINT ( 'NONE',  ( 6.397814513887354337, 0.1948139983735352188, 2.006652364629394114 ) ) ;
#11067=CARTESIAN_POINT ( 'NONE',  ( 5.542853976212075651, -1.453887124689148935, -1.129494548679485844 ) ) ;
#11068=CARTESIAN_POINT ( 'NONE',  ( -0.02319159430947542386, 1.394398620246390275, -2.068318759734718792 ) ) ;
#11069=CARTESIAN_POINT ( 'NONE',  ( 4.864078691051298975, 2.283152030527708209, -0.3349727840419229330 ) ) ;
#11071=CARTESIAN_POINT ( 'NONE',  ( 6.919229410208834530, -0.1638780278429008419, 2.126154539342207883 ) ) ;
#11073=CARTESIAN_POINT ( 'NONE',  ( 1.839301188190944902, 0.7414227542083090539, -1.795152619562689233 ) ) ;
#11074=CARTESIAN_POINT ( 'NONE',  ( 5.606872354539667036, 0.9390355927846851802, -2.097984029676060125 ) ) ;
#11078=CARTESIAN_POINT ( 'NONE',  ( 4.821099876132087125, -0.09137817997613774390, 1.868553921495450965 ) ) ;
#11081=CARTESIAN_POINT ( 'NONE',  ( 2.039183100597967258, 0.003605121848727563250, 1.912571728241836633 ) ) ;
#11084=CARTESIAN_POINT ( 'NONE',  ( 3.475398437264758833, 0.05438942809191970457, -2.206374867412825402 ) ) ;
#11088=CARTESIAN_POINT ( 'NONE',  ( 2.108605603913331183, 1.463472826393363624, -1.321001006224751917 ) ) ;
#11089=CARTESIAN_POINT ( 'NONE',  ( 1.413547897872836856, 2.036140070965312354, 1.085889434398391584 ) ) ;
#11090=CARTESIAN_POINT ( 'NONE',  ( 2.928120951529111338, 1.047165451586975049, 1.658829547137883775 ) ) ;
#11092=CARTESIAN_POINT ( 'NONE',  ( 5.963753124799120897, -0.5065058054696270906, 1.999279329544477513 ) ) ;
#11094=CARTESIAN_POINT ( 'NONE',  ( 4.065638850954083061, 1.320825628876612479, 1.523796413913918846 ) ) ;
#11100=CARTESIAN_POINT ( 'NONE',  ( 2.483468006519026439, -0.003752633953101049049, 2.171239807183155790 ) ) ;
#11104=CARTESIAN_POINT ( 'NONE',  ( 3.022558680773678397, 1.760047114015901526, 0.6337009143728977723 ) ) ;
#11105=CARTESIAN_POINT ( 'NONE',  ( 6.309879873373573922, -2.146112031266556919, 0.2576265230809087758 ) ) ;
#11107=CARTESIAN_POINT ( 'NONE',  ( 0.07755575628183573877, -0.002876890934064984650, -2.188974970840869005 ) ) ;
#11108=CARTESIAN_POINT ( 'NONE',  ( 6.727182134110241130, 2.994815527893503138, 2.165292399158074588 ) ) ;
#11111=CARTESIAN_POINT ( 'NONE',  ( 1.998553653897700011, -1.875654816251038248, -0.3715787057524469472 ) ) ;
#11112=CARTESIAN_POINT ( 'NONE',  ( 3.994789325776046507, 1.495029845459275863, -0.9468837749658890468 ) ) ;
#11113=CARTESIAN_POINT ( 'NONE',  ( 2.051281676579026492, -1.707476168062868060, 0.8611843332394366612 ) ) ;
#11116=CARTESIAN_POINT ( 'NONE',  ( -0.1005721928965920831, -1.878210221491773524, 0.3762452260359094303 ) ) ;
#11118=CARTESIAN_POINT ( 'NONE',  ( 0.4673438449808891004, 1.800595422158430825, 1.021790579661909781 ) ) ;
#11120=CARTESIAN_POINT ( 'NONE',  ( 5.524238439434661530, 1.113281918156138639, -1.503147240406087271 ) ) ;
#11121=CARTESIAN_POINT ( 'NONE',  ( 1.418276456094772708, 1.227529518603141190, -1.351586893430449576 ) ) ;
#11122=CARTESIAN_POINT ( 'NONE',  ( 5.444034239667132624, 0.8972360612293399651, -2.016436982482258333 ) ) ;
#11125=CARTESIAN_POINT ( 'NONE',  ( 2.857939457652844073, -0.6493452292726099584, 1.957851178230881395 ) ) ;
#11127=CARTESIAN_POINT ( 'NONE',  ( 6.610000000000003872, 7.053606217926155608, 2.318153411789238838 ) ) ;
#11133=CARTESIAN_POINT ( 'NONE',  ( 5.951642636407409093, 1.565221049572671719, 1.355249363302114318 ) ) ;
#11135=CARTESIAN_POINT ( 'NONE',  ( 2.284651837757902371, -2.119410549416993916, -0.4241055355862289877 ) ) ;
#11137=CARTESIAN_POINT ( 'NONE',  ( 3.422525317731230032, -0.8204878289409988090, -1.845699721510121183 ) ) ;
#11138=CARTESIAN_POINT ( 'NONE',  ( 6.720655732516648051, 2.039834428248034293, 2.379457109286802208 ) ) ;
#11143=CARTESIAN_POINT ( 'NONE',  ( 1.587125413319636635, 1.679225032509903404, 1.116207499648947943 ) ) ;
#11145=CARTESIAN_POINT ( 'NONE',  ( 6.286699343557896391, 1.907799665397520883, -1.078441415684105120 ) ) ;
#11147=CARTESIAN_POINT ( 'NONE',  ( 4.201352949932454450, 1.705870964349815333, -0.8646410313453978258 ) ) ;
#11151=CARTESIAN_POINT ( 'NONE',  ( 3.321888824615967906, 0.9040932542298124597, -1.802426844439278142 ) ) ;
#11154=CARTESIAN_POINT ( 'NONE',  ( 5.420820933352582749, 1.595050213381223214, 0.6567411224575621098 ) ) ;
#11158=CARTESIAN_POINT ( 'NONE',  ( 4.885944009213345929, -0.8832235454491498272, 1.648918812636574804 ) ) ;
#11160=CARTESIAN_POINT ( 'NONE',  ( 1.498975721005956441, 0.3999860688887920679, 2.031077231357696355 ) ) ;
#11164=CARTESIAN_POINT ( 'NONE',  ( -0.2051949539778260834, -0.1395167590549877823, -1.781371329038708096 ) ) ;
#11167=CARTESIAN_POINT ( 'NONE',  ( 0.2283786121510515688, 1.249231189971045319, -1.312217732533569103 ) ) ;
#11173=CARTESIAN_POINT ( 'NONE',  ( 0.5726126529861442771, 1.355618539282506640, -1.418395753018865113 ) ) ;
#11175=CARTESIAN_POINT ( 'NONE',  ( 5.431221565750523617, -1.512988070448300970, -1.174818341023081913 ) ) ;
#11183=CARTESIAN_POINT ( 'NONE',  ( 1.551884642779034262, 0.6273040060550126862, -2.068667048528524344 ) ) ;
#11187=CARTESIAN_POINT ( 'NONE',  ( 0.1234922912959918878, 1.848187084301698757, 1.039613981531524400 ) ) ;
#11188=CARTESIAN_POINT ( 'NONE',  ( 4.629811725094972630, -1.123643258228578024, -1.438734611599351565 ) ) ;
#11190=CARTESIAN_POINT ( 'NONE',  ( 1.423050710548888542, -0.05258038247234024520, 1.970828066091591557 ) ) ;
#11191=CARTESIAN_POINT ( 'NONE',  ( 3.164218664783400747, 1.912571728330178855, -0.004505864839042527346 ) ) ;
#11193=CARTESIAN_POINT ( 'NONE',  ( 4.105875410593727182, 0.6658617523271005423, -1.853701319000864656 ) ) ;
#11195=CARTESIAN_POINT ( 'NONE',  ( 5.495633776345048460, -1.942234966517431660, 0.004081557570839721392 ) ) ;
#11199=CARTESIAN_POINT ( 'NONE',  ( 5.888958097455845753, -2.014202512972632420, -0.6635655960139997811 ) ) ;
#11201=CARTESIAN_POINT ( 'NONE',  ( 3.791585636498477463, 1.799617611794877670, -0.6470144256675299799 ) ) ;
#11207=CARTESIAN_POINT ( 'NONE',  ( 5.725249205227378013, 1.776381904961796154, 0.9470739834369249488 ) ) ;
#11209=CARTESIAN_POINT ( 'NONE',  ( 6.024025069106937913, -1.018266858664597763, -1.515143308444939274 ) ) ;
#11210=CARTESIAN_POINT ( 'NONE',  ( 5.805875103277515770, -1.124240986939632592, -1.673857227857282082 ) ) ;
#11211=CARTESIAN_POINT ( 'NONE',  ( 2.348173244826061268, -0.8873571809006628452, 1.870714752860686447 ) ) ;
#11215=CARTESIAN_POINT ( 'NONE',  ( 6.702024585102262400, -1.870183347854617040, 0.04844413084104796929 ) ) ;
#11223=CARTESIAN_POINT ( 'NONE',  ( 4.131323472851686773, 0.4681366286901997853, 1.669664985128198831 ) ) ;
#11227=CARTESIAN_POINT ( 'NONE',  ( 1.411079811451225074, -1.634442866182721277, 1.270590680402396311 ) ) ;
#11228=CARTESIAN_POINT ( 'NONE',  ( 2.988026824963069927, -2.114671507216555391, 0.1067447620008883935 ) ) ;
#11231=EDGE_CURVE ( 'NONE', #175232, #33823, #171598, .T. ) ;
#11232=CARTESIAN_POINT ( 'NONE',  ( 0.2859135117265668158, -1.207096249910791563, -1.556650298907244823 ) ) ;
#11236=CARTESIAN_POINT ( 'NONE',  ( -0.1405747822309927342, -1.479430311965252542, -1.211566217618691210 ) ) ;
#11237=CARTESIAN_POINT ( 'NONE',  ( 3.275583346405244622, 1.454120551940318418, 1.771997285204220507 ) ) ;
#11238=CARTESIAN_POINT ( 'NONE',  ( 1.013953575274041619, -0.8186894766500467657, -1.631917417583013341 ) ) ;
#11239=CARTESIAN_POINT ( 'NONE',  ( 3.832203377193269755, -0.9874410831685247469, -1.637625244210038300 ) ) ;
#11244=CARTESIAN_POINT ( 'NONE',  ( 1.863541034856039502, -1.619513613076409397, -1.195741390080407918 ) ) ;
#11245=CARTESIAN_POINT ( 'NONE',  ( 1.867943658074404434, -1.947550630801861526, 0.2349073745619503772 ) ) ;
#11249=CARTESIAN_POINT ( 'NONE',  ( 5.244118971382810912, 0.6063552182394044143, 2.000762070341703502 ) ) ;
#11250=CARTESIAN_POINT ( 'NONE',  ( 3.572906242625200068, 0.04398576871290219709, -1.769473305487194281 ) ) ;
#11252=CARTESIAN_POINT ( 'NONE',  ( -0.02321191073820921824, -0.1601477211686137825, -2.156400265872604471 ) ) ;
#11253=CARTESIAN_POINT ( 'NONE',  ( 5.050617384047394687, -1.472844127453584839, -0.9267575401476387809 ) ) ;
#11256=CARTESIAN_POINT ( 'NONE',  ( -0.1104750535120268828, 4.084583917300321332, -2.658209514912849514 ) ) ;
#11257=CARTESIAN_POINT ( 'NONE',  ( 4.516742233720687949, 1.733484511791906879, -0.04249706786149141935 ) ) ;
#11259=CARTESIAN_POINT ( 'NONE',  ( 6.162576015390932582, -0.7755629475397389783, -2.028117739495437277 ) ) ;
#11261=CARTESIAN_POINT ( 'NONE',  ( -0.2056253921914633354, -0.9106808701126485328, -1.909331193683319050 ) ) ;
#11262=CARTESIAN_POINT ( 'NONE',  ( 5.312500000000002665, 1.451031289061327501, 1.451031289060900065 ) ) ;
#11264=CARTESIAN_POINT ( 'NONE',  ( 3.381779240904962069, 1.220913077095790111, 1.490098802054098837 ) ) ;
#11266=CARTESIAN_POINT ( 'NONE',  ( 6.293255338728928727, -0.1078348580665164369, -2.218937141123643375 ) ) ;
#11268=CARTESIAN_POINT ( 'NONE',  ( -0.1411974294641681893, 1.383765339824583052, -2.157932961605046440 ) ) ;
#11271=CARTESIAN_POINT ( 'NONE',  ( 2.456000923045877027, -1.648014358291004733, -1.489564561520567487 ) ) ;
#11276=CARTESIAN_POINT ( 'NONE',  ( 0.2467204944939948574, 1.994070950632735428, -0.2986300710981006357 ) ) ;
#11278=CARTESIAN_POINT ( 'NONE',  ( 5.318824396150737321, -1.496427615725079097, 1.419873077484270496 ) ) ;
#11283=CARTESIAN_POINT ( 'NONE',  ( 0.2096995604969940641, -0.7494040810181783474, -1.602093636072899008 ) ) ;
#11284=CARTESIAN_POINT ( 'NONE',  ( 5.731065183167076249, 1.732634240323025043, 0.07581458514279926231 ) ) ;
#11285=CARTESIAN_POINT ( 'NONE',  ( 5.354937190278808323, 0.3318421670873850648, -1.708331137930273913 ) ) ;
#11286=CARTESIAN_POINT ( 'NONE',  ( 3.158078472442786833, 1.032628797542353816, 2.046708512074166819 ) ) ;
#11288=CARTESIAN_POINT ( 'NONE',  ( 2.782953997937851920, 1.302219384484751830, 1.301801165952347628 ) ) ;
#11290=CARTESIAN_POINT ( 'NONE',  ( 2.977373796215293300, 1.734057503958493118, -0.5710112477543202170 ) ) ;
#11291=CARTESIAN_POINT ( 'NONE',  ( 4.149064681782777875, 0.9530105817698063531, 1.777011888912001014 ) ) ;
#11294=CARTESIAN_POINT ( 'NONE',  ( 4.805753954608172229, -0.5644290981201576241, 2.028831172856554677 ) ) ;
#11297=CARTESIAN_POINT ( 'NONE',  ( 2.418496320782090869, 0.8830982243829659240, 1.872697815963566992 ) ) ;
#11300=CARTESIAN_POINT ( 'NONE',  ( 4.283913115580790354, 2.056533504189705930, -0.5163123687341104606 ) ) ;
#11302=CARTESIAN_POINT ( 'NONE',  ( 0.2231027806867662000, -0.09612335957175778545, 1.924217376148322334 ) ) ;
#11309=CARTESIAN_POINT ( 'NONE',  ( 6.533471381225442798, -0.1521382079053348602, 2.086446650026114735 ) ) ;
#11310=CARTESIAN_POINT ( 'NONE',  ( 1.079290920250153496, -0.05147710300976635067, -2.105495365820194920 ) ) ;
#11313=CARTESIAN_POINT ( 'NONE',  ( 5.858217239054963166, -1.861131630269092341, -0.001575894832107904492 ) ) ;
#11321=CARTESIAN_POINT ( 'NONE',  ( 2.260140581184489239, -1.961506502764579052, 0.04509734162668613960 ) ) ;
#11322=CARTESIAN_POINT ( 'NONE',  ( 1.200320640528436789, -2.161883444890321915, 0.0006282887012112879947 ) ) ;
#11327=CARTESIAN_POINT ( 'NONE',  ( 3.251044507966997177, -1.707695807076513805, -0.2988343314351063484 ) ) ;
#11328=CARTESIAN_POINT ( 'NONE',  ( 2.062088869592033635, -1.590637294955974390, -0.7065417998822677292 ) ) ;
#11331=CARTESIAN_POINT ( 'NONE',  ( 1.739611019359630584, -1.913509794028777522, -0.6351045200190530426 ) ) ;
#11332=CARTESIAN_POINT ( 'NONE',  ( 6.825078400183551608, 0.5660753733540256905, 2.196387875007102419 ) ) ;
#11334=CARTESIAN_POINT ( 'NONE',  ( 1.375784083019690351, 1.172551417808114893, 1.584734682399450145 ) ) ;
#11335=CARTESIAN_POINT ( 'NONE',  ( 6.310809538426106258, -0.5167911955388967415, -1.841158844219364044 ) ) ;
#11340=CARTESIAN_POINT ( 'NONE',  ( 1.699873857359509799, 1.394438142870989772, 1.461265194366095033 ) ) ;
#11342=CARTESIAN_POINT ( 'NONE',  ( 5.596783072813162896, -0.5536939349623200002, -2.240073236831362280 ) ) ;
#11343=CARTESIAN_POINT ( 'NONE',  ( 5.353941776413853937, -0.7077614321437855072, 1.829919609802006741 ) ) ;
#11344=CARTESIAN_POINT ( 'NONE',  ( 3.045700443693433179, 1.383923128670875746, 1.390673908496591782 ) ) ;
#11346=CARTESIAN_POINT ( 'NONE',  ( 0.2642963535325442148, 1.880433764241522088, -0.7283817610406126963 ) ) ;
#11348=CARTESIAN_POINT ( 'NONE',  ( 1.657563801924813784, 2.024516536105415820, -0.6199660602846206459 ) ) ;
#11351=CARTESIAN_POINT ( 'NONE',  ( 1.693040327840355408, -0.6214066371539993527, 1.733238834403828754 ) ) ;
#11354=CARTESIAN_POINT ( 'NONE',  ( 2.496466685713152334, -1.086271176545396067, 1.821091972856798913 ) ) ;
#11359=CARTESIAN_POINT ( 'NONE',  ( 2.723961130741957781, -1.183836802208296568, -1.686624133856133412 ) ) ;
#11367=CARTESIAN_POINT ( 'NONE',  ( 2.741812758617673040, -1.674694146245614412, -1.521292302590461665 ) ) ;
#11369=CARTESIAN_POINT ( 'NONE',  ( 2.777393361597128685, 0.2615887081860277519, -1.792441719956331170 ) ) ;
#11370=CARTESIAN_POINT ( 'NONE',  ( 3.608511690770484837, 1.820787697044351505, 0.5958877267112758780 ) ) ;
#11371=CARTESIAN_POINT ( 'NONE',  ( 3.771986465066007099, -2.040223509676724500, 0.3510349978646867264 ) ) ;
#11373=CARTESIAN_POINT ( 'NONE',  ( 2.500799400523348037, 1.584503739761052188, -1.172863459551294341 ) ) ;
#11374=CARTESIAN_POINT ( 'NONE',  ( 6.410771793481705672, 1.425725087049932505, -1.295833391663123724 ) ) ;
#11375=CARTESIAN_POINT ( 'NONE',  ( 3.028041890241763401, 1.040506211802554981, -1.554362669439563360 ) ) ;
#11377=CARTESIAN_POINT ( 'NONE',  ( 2.719673384174253972, -0.2251885735481904405, 2.296679687964820360 ) ) ;
#11379=CARTESIAN_POINT ( 'NONE',  ( 2.945584473374110779, 1.314022426170344815, 1.318171089286435560 ) ) ;
#11381=CARTESIAN_POINT ( 'NONE',  ( 6.777782349474076540, -2.001779569883685106, 0.4972090909861492936 ) ) ;
#11386=CARTESIAN_POINT ( 'NONE',  ( 0.1355649208573142805, -1.924581242375450030, 0.8557158107796616342 ) ) ;
#11388=CARTESIAN_POINT ( 'NONE',  ( 6.098930168602409552, 1.771044849343451633, -1.239067683784184748 ) ) ;
#11389=CARTESIAN_POINT ( 'NONE',  ( 6.428379779529339366, -0.9538188281377130151, -1.780268319267635846 ) ) ;
#11397=CARTESIAN_POINT ( 'NONE',  ( 4.276577519141481432, -0.4465006364167342645, -1.966305148836451577 ) ) ;
#11402=CARTESIAN_POINT ( 'NONE',  ( 5.981359018292748075, 1.999130597612966742, -0.8229454869796914984 ) ) ;
#11408=CARTESIAN_POINT ( 'NONE',  ( 6.573846656420020196, -0.8593871168269312522, 1.822298249534954673 ) ) ;
#11412=PLANE ( 'NONE',  #193551 ) ;
#11413=CARTESIAN_POINT ( 'NONE',  ( 2.086159243269372521, -1.691233086580298695, -0.3380474007560717031 ) ) ;
#11417=CARTESIAN_POINT ( 'NONE',  ( 1.053533388295304629, 1.768092659605845052, -0.07913920300933743879 ) ) ;
#11418=CARTESIAN_POINT ( 'NONE',  ( 1.699859389132576837, 1.389752512480733060, 1.456620396263593520 ) ) ;
#11419=CARTESIAN_POINT ( 'NONE',  ( 4.331241739176756589, 0.1049304944579672605, 2.204394592675275710 ) ) ;
#11420=CARTESIAN_POINT ( 'NONE',  ( 5.612245307067635025, 2.168910047263863827, -0.09915484274719725544 ) ) ;
#11424=CARTESIAN_POINT ( 'NONE',  ( 2.930460433956377564, -1.047063434655249647, -1.843881786051679850 ) ) ;
#11425=CARTESIAN_POINT ( 'NONE',  ( 3.040638836679772528, -1.525031945187466098, 1.319243992433154267 ) ) ;
#11426=CARTESIAN_POINT ( 'NONE',  ( 3.252039308394638173, 0.8100161731663655384, -1.620448113725055483 ) ) ;
#11432=CARTESIAN_POINT ( 'NONE',  ( 6.024025069106937913, -1.018266858664597763, -1.515143308444939274 ) ) ;
#11434=CARTESIAN_POINT ( 'NONE',  ( 1.516650397601801759, 0.1914660871255029484, 1.906153142492900132 ) ) ;
#11440=ORIENTED_EDGE ( 'NONE', *, *, #147573, .F. ) ;
#11441=CARTESIAN_POINT ( 'NONE',  ( 5.155217493315787713, -1.824165352752779246, -1.159627250419709155 ) ) ;
#11445=CARTESIAN_POINT ( 'NONE',  ( 2.865608904542978674, -1.736054085904148669, -1.217558864107195937 ) ) ;
#11449=CARTESIAN_POINT ( 'NONE',  ( 4.288322324034578692, -1.949444798393678013, -0.2924651067536877536 ) ) ;
#11450=CARTESIAN_POINT ( 'NONE',  ( -0.1228044941411730595, -1.800067586368118588, -0.9016598371343366169 ) ) ;
#11451=VERTEX_POINT ( 'NONE', #141756 ) ;
#11452=CARTESIAN_POINT ( 'NONE',  ( 6.051990796818580876, 1.090527953092842894, 1.814802726937503330 ) ) ;
#11454=CARTESIAN_POINT ( 'NONE',  ( 0.2739938332866619364, -2.030697503880642518, 0.4024348779970430834 ) ) ;
#11455=CARTESIAN_POINT ( 'NONE',  ( 2.607286591753724014, -1.920749920159558810, 0.2854125566163211447 ) ) ;
#11459=CARTESIAN_POINT ( 'NONE',  ( 3.310569631373377231, 1.890246369116010960, 0.8934441069041214600 ) ) ;
#11462=CARTESIAN_POINT ( 'NONE',  ( 0.1525891599635448848, 0.3075033511844190159, 1.785008687375288172 ) ) ;
#11464=CARTESIAN_POINT ( 'NONE',  ( 5.373716497573798101, 2.127666891504222502, -0.5857064233696291922 ) ) ;
#11466=CARTESIAN_POINT ( 'NONE',  ( 3.417197246517459597, 1.994164043739574232, 0.9453733912969732867 ) ) ;
#11470=CARTESIAN_POINT ( 'NONE',  ( 1.277824965264368728, 1.883817941867833134, -0.3277997056638781714 ) ) ;
#11473=CARTESIAN_POINT ( 'NONE',  ( 5.617656447048144486, 0.4075009240860454907, -2.029694874052537568 ) ) ;
#11475=CARTESIAN_POINT ( 'NONE',  ( 2.571340117545738657, 0.1069729528509130723, -2.159185227005658181 ) ) ;
#11476=CARTESIAN_POINT ( 'NONE',  ( 4.353197867323560288, 0.4795420089713005041, -2.138300074133951068 ) ) ;
#11484=CARTESIAN_POINT ( 'NONE',  ( 0.4400775573648734174, -1.704940109561555950, -1.076314675215600314 ) ) ;
#11487=CARTESIAN_POINT ( 'NONE',  ( 5.383670357325340383, -1.967593191946028996, 0.6441560278484458335 ) ) ;
#11488=CARTESIAN_POINT ( 'NONE',  ( 4.846275584324886587, 1.921458954407113451, 0.1401587531122197583 ) ) ;
#11489=CARTESIAN_POINT ( 'NONE',  ( 0.1929827526203631294, 1.755782054984224683, 0.9913788669043410717 ) ) ;
#11494=CARTESIAN_POINT ( 'NONE',  ( 3.608217298448283206, 1.969629311412910866, 0.004557946788486669405 ) ) ;
#11495=CARTESIAN_POINT ( 'NONE',  ( 0.4631483011842302266, 0.2107759881739781904, -2.181290363801504650 ) ) ;
#11496=CARTESIAN_POINT ( 'NONE',  ( 3.686012862905340803, -0.8985999850123352894, 1.589152278004740237 ) ) ;
#11503=CARTESIAN_POINT ( 'NONE',  ( 1.346931166825489967, 0.5339940059071214273, -1.762130705996706181 ) ) ;
#11504=CARTESIAN_POINT ( 'NONE',  ( 4.676043659170272093, 1.990676093108449951, -0.2997180003130732739 ) ) ;
#11505=CARTESIAN_POINT ( 'NONE',  ( 1.177631936369994303, -1.035077938576201451, -2.052156377449709357 ) ) ;
#11506=CARTESIAN_POINT ( 'NONE',  ( 5.383633123045536983, -1.864019207510819953, 0.6117972396969260096 ) ) ;
#11510=CARTESIAN_POINT ( 'NONE',  ( 0.9243811426856913815, 1.018911950503737174, 1.802186752163869699 ) ) ;
#11512=CARTESIAN_POINT ( 'NONE',  ( 0.9782033901477287241, -2.040585271250746846, -0.4545043172074214599 ) ) ;
#11513=CARTESIAN_POINT ( 'NONE',  ( 6.596581986989779267, -0.4770763175313968429, -1.704276504685025673 ) ) ;
#11515=CARTESIAN_POINT ( 'NONE',  ( -0.1102773484824119410, 4.081664357266182819, -2.758211214536327116 ) ) ;
#11516=CARTESIAN_POINT ( 'NONE',  ( 2.085156077859366519, -0.7432962182043149069, 1.573855765194108081 ) ) ;
#11521=CARTESIAN_POINT ( 'NONE',  ( 1.822448697576475540, 1.608646582964175176, 0.6229558172686412432 ) ) ;
#11522=CARTESIAN_POINT ( 'NONE',  ( 2.173600921376659834, 1.351110561487681716, 1.725424542402646422 ) ) ;
#11523=CARTESIAN_POINT ( 'NONE',  ( 3.914836437932368796, 1.561248537261412883, -1.560010120355350471 ) ) ;
#11525=CARTESIAN_POINT ( 'NONE',  ( 2.782273231148081116, -1.246650745954593464, -1.777310168556520464 ) ) ;
#11526=CARTESIAN_POINT ( 'NONE',  ( 0.8030139110496161692, 1.490934425176414502, 1.053415343471690857 ) ) ;
#11527=CARTESIAN_POINT ( 'NONE',  ( 3.538375268227810011, 0.7659831068804138221, 1.974087397274668643 ) ) ;
#11528=CARTESIAN_POINT ( 'NONE',  ( 6.539320575229257138, 2.987941927008979537, 2.250856951216452906 ) ) ;
#11530=CARTESIAN_POINT ( 'NONE',  ( 4.107168962890386688, -0.3918867163640211704, 2.258474592593032959 ) ) ;
#11534=CARTESIAN_POINT ( 'NONE',  ( 6.235052692738393354, 2.071546745583602522, 0.8022605484305275203 ) ) ;
#11540=CARTESIAN_POINT ( 'NONE',  ( 6.825078400183556049, 1.282741234726337165, 1.971047034039686174 ) ) ;
#11542=CARTESIAN_POINT ( 'NONE',  ( 4.149064681782777875, 0.9530105817698063531, 1.777011888912001014 ) ) ;
#11544=CARTESIAN_POINT ( 'NONE',  ( 2.676693276584718895, 1.350517573672470606, -1.558986216346124776 ) ) ;
#11549=CARTESIAN_POINT ( 'NONE',  ( 4.875033280109006384, 2.045454206080063120, -0.7869404205859964474 ) ) ;
#11550=CARTESIAN_POINT ( 'NONE',  ( 2.988907892087853568, -2.013985899409028946, 0.1017507309580278629 ) ) ;
#11551=CARTESIAN_POINT ( 'NONE',  ( 2.190726087351921425, 1.424366561657765207, 1.166803476217087576 ) ) ;
#11554=CARTESIAN_POINT ( 'NONE',  ( 5.965807262869926575, 1.798080572464531679, -0.3147057940002598864 ) ) ;
#11557=CARTESIAN_POINT ( 'NONE',  ( 5.506774338047922157, 1.717276559928378132, -1.473185486808053835 ) ) ;
#11559=CARTESIAN_POINT ( 'NONE',  ( 1.418734189139436275, 1.413363300903627717, -1.561561204404242842 ) ) ;
#11569=CARTESIAN_POINT ( 'NONE',  ( 1.652743449602233072, 2.098267697663995790, 0.3060111223712052020 ) ) ;
#11570=CARTESIAN_POINT ( 'NONE',  ( 2.391161334010579509, -2.127237363102509882, -0.6400520371602820280 ) ) ;
#11571=CARTESIAN_POINT ( 'NONE',  ( 6.883263157960364254, 6.036844454314826081, 2.541088405340941492 ) ) ;
#11574=CARTESIAN_POINT ( 'NONE',  ( 4.615648854252428102, 0.4318217149890530848, -1.913582009320368371 ) ) ;
#11580=CARTESIAN_POINT ( 'NONE',  ( 3.814780496183818315, -0.6684712460508880350, -2.012520831323429515 ) ) ;
#11582=CARTESIAN_POINT ( 'NONE',  ( 4.838837662799537753, 0.3661284547709364734, 2.130314178654398205 ) ) ;
#11583=CARTESIAN_POINT ( 'NONE',  ( 3.860763913883006992, 0.2215400755124704024, -1.827792592973469743 ) ) ;
#11586=CARTESIAN_POINT ( 'NONE',  ( 5.367066450689647716, 1.675684007255513475, -0.4696764748959629809 ) ) ;
#11587=CARTESIAN_POINT ( 'NONE',  ( 6.727182134110203826, 2.985950691969770254, 2.264927069331075238 ) ) ;
#11590=CARTESIAN_POINT ( 'NONE',  ( 2.553791647773369089, 0.5774160426356907960, -2.083079400968433248 ) ) ;
#11591=CARTESIAN_POINT ( 'NONE',  ( 5.395861176733054876, 0.1455124041884261754, 2.010896217931843921 ) ) ;
#11593=CARTESIAN_POINT ( 'NONE',  ( 2.641676655999642076, -1.601130012699041982, -1.452526871000489495 ) ) ;
#11594=CARTESIAN_POINT ( 'NONE',  ( 3.831288253049653481, -1.822718488796180925, 0.7514253593702052703 ) ) ;
#11596=CARTESIAN_POINT ( 'NONE',  ( 4.265135581495039574, 1.882949608596860669, -0.4750026310351186387 ) ) ;
#11605=CARTESIAN_POINT ( 'NONE',  ( 2.309865001130634976, -0.4838574416936823885, 2.152911442350906146 ) ) ;
#11607=CARTESIAN_POINT ( 'NONE',  ( 6.121922100595678096, 1.933298025717408608, -0.3319332437697538607 ) ) ;
#11611=FACE_OUTER_BOUND ( 'NONE', #114076, .T. ) ;
#11613=CARTESIAN_POINT ( 'NONE',  ( 5.349485151062910226, 1.838858031828109141, -0.09410559872920225277 ) ) ;
#11621=CARTESIAN_POINT ( 'NONE',  ( 6.678986887005352813, -0.09631167155637165855, -2.058642716137318640 ) ) ;
#11623=CARTESIAN_POINT ( 'NONE',  ( 2.084208510888691190, 1.074786400414856624, -1.519112143004421434 ) ) ;
#11624=CARTESIAN_POINT ( 'NONE',  ( 3.772867777003403589, 1.732451475078290448, -0.6238847238279123797 ) ) ;
#11632=CARTESIAN_POINT ( 'NONE',  ( 3.616033620774202983, -2.174319932014677548, 0.3768175846284789743 ) ) ;
#11633=CARTESIAN_POINT ( 'NONE',  ( 6.292268727954291485, -2.250598158220047385, -0.2311834041341890578 ) ) ;
#11635=CARTESIAN_POINT ( 'NONE',  ( 6.152603492317154199, 1.793228361101945056, 0.2563216274220745938 ) ) ;
#11636=CARTESIAN_POINT ( 'NONE',  ( 0.02267320670834571672, 0.3494893071277604402, 1.985867805234131644 ) ) ;
#11639=CARTESIAN_POINT ( 'NONE',  ( 6.438356904408193415, 1.850619875698428674, 0.2722718653145329015 ) ) ;
#11641=CARTESIAN_POINT ( 'NONE',  ( 5.109976026518994630, -0.6845719981980763480, 1.785733525123212928 ) ) ;
#11643=CARTESIAN_POINT ( 'NONE',  ( 0.8306673739700667358, 0.1335802410974036292, 1.865940672528036304 ) ) ;
#11644=CARTESIAN_POINT ( 'NONE',  ( 1.235564962061060257, 0.5807501988173838781, -1.931125984888550473 ) ) ;
#11646=CARTESIAN_POINT ( 'NONE',  ( 4.547555978022395529, -1.627529793438415417, -1.336665591334128100 ) ) ;
#11651=CARTESIAN_POINT ( 'NONE',  ( 2.900653795123844692, -1.990604234199357281, -0.3410580241900613707 ) ) ;
#11654=CARTESIAN_POINT ( 'NONE',  ( 3.620547430246877862, 1.374377816306590727, -1.668374205817772182 ) ) ;
#11660=CARTESIAN_POINT ( 'NONE',  ( 0.4323793472312524311, 1.250547990301904111, 1.774695861279996567 ) ) ;
#11664=CARTESIAN_POINT ( 'NONE',  ( 1.593588134247824639, -0.7342643958434189599, 2.065040727587868830 ) ) ;
#11666=CARTESIAN_POINT ( 'NONE',  ( 2.360583983009652442, 0.9673915393220763326, 2.045390427905840358 ) ) ;
#11672=CARTESIAN_POINT ( 'NONE',  ( 4.622157715239192832, 1.089468934077148399, -1.394508319181851697 ) ) ;
#11674=CARTESIAN_POINT ( 'NONE',  ( 0.9386647947689167326, 2.074798300807283447, 0.3599966696490787266 ) ) ;
#11678=CARTESIAN_POINT ( 'NONE',  ( 6.450795914701256351, -1.844717532910484570, -0.8146137538835170888 ) ) ;
#11679=CARTESIAN_POINT ( 'NONE',  ( 4.992358684838777982, -0.9999893916136384231, 1.510367140083505699 ) ) ;
#11682=CARTESIAN_POINT ( 'NONE',  ( 3.555401268124198655, 0.4554524271490404952, -1.814226883376020671 ) ) ;
#11683=CARTESIAN_POINT ( 'NONE',  ( 4.346580092118113470, -2.046995731385771400, -0.3088174131898810959 ) ) ;
#11692=CARTESIAN_POINT ( 'NONE',  ( 3.543363863352413823, 1.774678991803163575, -0.8365776047038612218 ) ) ;
#11693=CARTESIAN_POINT ( 'NONE',  ( 0.6497672626537411844, -0.2439889887937417567, -2.001205234435726066 ) ) ;
#11698=CARTESIAN_POINT ( 'NONE',  ( 1.176777557245082262, -0.04011917365428705612, -1.870279424122413658 ) ) ;
#11700=CARTESIAN_POINT ( 'NONE',  ( 2.812746579430201788, -0.5882912493809470122, -1.925304731621484633 ) ) ;
#11702=CARTESIAN_POINT ( 'NONE',  ( 2.495853057047519030, -2.093741659442478920, 0.3138373457529738397 ) ) ;
#11704=CARTESIAN_POINT ( 'NONE',  ( 3.754400092289136737, -2.067862582909282487, -0.1045053291982081939 ) ) ;
#11706=CARTESIAN_POINT ( 'NONE',  ( 0.3805629577237649719, -0.2597898305938106112, -2.074488238918821725 ) ) ;
#11708=CARTESIAN_POINT ( 'NONE',  ( 5.666980381186065507, -1.651371415153819688, -0.7785968546244539379 ) ) ;
#11713=CARTESIAN_POINT ( 'NONE',  ( 6.422910180798067969, 2.056742032306459578, 0.8002587082300142152 ) ) ;
#11715=CARTESIAN_POINT ( 'NONE',  ( 4.899028947338643469, -0.2378672112019977747, -1.897373119303269018 ) ) ;
#11723=CARTESIAN_POINT ( 'NONE',  ( -0.02299388927988389730, 0.001624902753813092359, -1.910968047046639251 ) ) ;
#11729=CARTESIAN_POINT ( 'NONE',  ( 2.746873616242023086, -0.3318220265390697254, -1.941108330032844664 ) ) ;
#11730=CARTESIAN_POINT ( 'NONE',  ( 3.058220425488000327, -1.198843740453523266, 1.621196181159669347 ) ) ;
#11733=CARTESIAN_POINT ( 'NONE',  ( 6.827182134110192813, 7.051736335826703339, 2.787205296604370108 ) ) ;
#11735=CARTESIAN_POINT ( 'NONE',  ( 3.978626637211603700, -0.2140425413966473567, -2.180973779111646138 ) ) ;
#11737=CARTESIAN_POINT ( 'NONE',  ( 1.641497204607924809, -1.393575563620005786, -1.330239063421148948 ) ) ;
#11739=CARTESIAN_POINT ( 'NONE',  ( 0.1331565106231328566, 1.371277436080810208, -2.201942895618694607 ) ) ;
#11746=CARTESIAN_POINT ( 'NONE',  ( 6.075717905342373548, -0.9791751913862613010, 1.559117742379905858 ) ) ;
#11747=CARTESIAN_POINT ( 'NONE',  ( 1.541653539051958122, -1.894817064119158401, 0.6801782934461576557 ) ) ;
#11748=CARTESIAN_POINT ( 'NONE',  ( 4.780793123113402210, -2.255322609370190357, 0.4421783396322577775 ) ) ;
#11749=CARTESIAN_POINT ( 'NONE',  ( -0.02919842301644676522, 2.866066704180502800, -2.562138095921069780 ) ) ;
#11750=CARTESIAN_POINT ( 'NONE',  ( 2.061162768541408230, 1.543764177570670970, 1.038864413082870142 ) ) ;
#11753=CARTESIAN_POINT ( 'NONE',  ( -0.1290005225502432740, 4.081813041011835175, -2.728655865233818201 ) ) ;
#11754=CARTESIAN_POINT ( 'NONE',  ( 5.150612376422202487, 1.885107930906554152, 0.3209214958604587054 ) ) ;
#11757=CARTESIAN_POINT ( 'NONE',  ( 4.476172314981810452, -2.028359691925533781, -0.5064535023821553628 ) ) ;
#11758=CARTESIAN_POINT ( 'NONE',  ( 3.485083742438867649, 1.691615344724434200, -0.7988839237506044633 ) ) ;
#11763=CARTESIAN_POINT ( 'NONE',  ( 6.639270748794153576, -1.536914537172892725, 0.7831451356504478545 ) ) ;
#11765=CARTESIAN_POINT ( 'NONE',  ( 1.476802972400652170, -1.725769044224190196, -0.1698483453264828802 ) ) ;
#11769=CARTESIAN_POINT ( 'NONE',  ( 6.332918745153389928, -2.058942774313234025, -0.6888473222384088324 ) ) ;
#11770=CARTESIAN_POINT ( 'NONE',  ( 4.723181480036696023, -0.08661695748878039947, 1.823760500460340550 ) ) ;
#11771=CARTESIAN_POINT ( 'NONE',  ( 1.867943658074404434, -1.947550630801861526, 0.2349073745619503772 ) ) ;
#11772=CARTESIAN_POINT ( 'NONE',  ( 6.403513597085680686, -2.053302684608013795, 0.5162988180226235624 ) ) ;
#11776=CARTESIAN_POINT ( 'NONE',  ( 2.930460433956377564, -1.047063434655249647, -1.843881786051679850 ) ) ;
#11781=CARTESIAN_POINT ( 'NONE',  ( 0.3212534483023680165, -1.847719145540312358, -0.9339786784923131968 ) ) ;
#11784=CARTESIAN_POINT ( 'NONE',  ( 3.826986476844072005, 1.570263387305373737, -1.571374446222243204 ) ) ;
#11785=VERTEX_POINT ( 'NONE', #9171 ) ;
#11786=CARTESIAN_POINT ( 'NONE',  ( 0.5460333347737976739, -1.659586600764794584, 1.590741637488497062 ) ) ;
#11788=CARTESIAN_POINT ( 'NONE',  ( 5.928601196466630086, -1.312702821215183002, 1.590880328853358394 ) ) ;
#11791=CARTESIAN_POINT ( 'NONE',  ( 0.1329588055935396196, 0.2493489391296536684, -1.880683181770840262 ) ) ;
#11792=CARTESIAN_POINT ( 'NONE',  ( 5.179192671508887180, 1.240781939916297372, 1.360553736468192554 ) ) ;
#11795=CARTESIAN_POINT ( 'NONE',  ( 2.156250000000001776, -1.895863743164040160, 0.7852924748301010061 ) ) ;
#11796=CARTESIAN_POINT ( 'NONE',  ( 2.906937612971383089, 1.455985047528246090, 0.9243032718214757582 ) ) ;
#11797=CARTESIAN_POINT ( 'NONE',  ( 1.024625454658374624, 0.3981145430279106057, 1.976669095394629982 ) ) ;
#11798=CARTESIAN_POINT ( 'NONE',  ( 2.866213343745026343, -0.1723225051825111875, -2.292302961975992037 ) ) ;
#11800=CARTESIAN_POINT ( 'NONE',  ( 2.249658590878771847, -1.816102774931172448, -1.348951556275684194 ) ) ;
#11801=CARTESIAN_POINT ( 'NONE',  ( 4.899102953068730670, 1.751457851224359041, -1.169261236274852012 ) ) ;
#11803=CARTESIAN_POINT ( 'NONE',  ( 3.338855477594515175, -1.562335520734370320, 0.8312421073871211208 ) ) ;
#11806=CARTESIAN_POINT ( 'NONE',  ( 6.163675082799745297, 1.174783243402954591, 1.968361872208840069 ) ) ;
#11807=CARTESIAN_POINT ( 'NONE',  ( 4.663899394030392997, -1.200468288914667614, 1.396033019000951336 ) ) ;
#11811=CARTESIAN_POINT ( 'NONE',  ( 4.189532503254236318, -0.8396404696654431454, 2.024412170900617092 ) ) ;
#11816=CARTESIAN_POINT ( 'NONE',  ( 2.982943389344643759, -0.1423259158175680661, -1.921303036959535415 ) ) ;
#11819=CARTESIAN_POINT ( 'NONE',  ( -0.1927127643980519056, -0.4999767001874329542, -2.172835435166208473 ) ) ;
#11828=CARTESIAN_POINT ( 'NONE',  ( 6.403215362905616992, 1.794359850238020693, 1.205212418099836480 ) ) ;
#11830=CARTESIAN_POINT ( 'NONE',  ( 5.934033239752055877, 1.167398200610193282, 1.576599764842034457 ) ) ;
#11833=CARTESIAN_POINT ( 'NONE',  ( 5.805597153138060129, -0.5296426447994294628, 2.095691122003799478 ) ) ;
#11837=CARTESIAN_POINT ( 'NONE',  ( 0.5263522483448194178, 1.788089326329355577, 0.5492086291003297482 ) ) ;
#11838=CARTESIAN_POINT ( 'NONE',  ( 5.975915019019427454, 1.530855338724030457, 0.8140783706773281336 ) ) ;
#11841=CARTESIAN_POINT ( 'NONE',  ( 3.140350738262797314, 0.5347024899306859202, 2.125194831261326911 ) ) ;
#11842=CARTESIAN_POINT ( 'NONE',  ( 2.942713080207468579, 2.290027058972336604, 0.2837140972290051466 ) ) ;
#11843=CARTESIAN_POINT ( 'NONE',  ( 5.395800779767854216, -0.7457615368846971515, 1.921284171288279996 ) ) ;
#11844=CARTESIAN_POINT ( 'NONE',  ( 1.271315641948435493, 1.156325127695263744, 1.560008962195078563 ) ) ;
#11848=CARTESIAN_POINT ( 'NONE',  ( 4.957343421279006179, -1.817532610912236724, 1.092287347377165485 ) ) ;
#11850=CARTESIAN_POINT ( 'NONE',  ( 2.443982611291168450, -1.755769474653746665, -0.9913988478210812305 ) ) ;
#11852=CARTESIAN_POINT ( 'NONE',  ( 6.018643902988223715, 1.486383190695803158, -1.631276885294789203 ) ) ;
#11861=CARTESIAN_POINT ( 'NONE',  ( 3.907146709503729110, 1.766719954806586612, 1.060879741047163316 ) ) ;
#11867=CARTESIAN_POINT ( 'NONE',  ( 4.406902263202909786, -0.4446603063312704607, -1.969940172527106625 ) ) ;
#11872=CARTESIAN_POINT ( 'NONE',  ( 2.764585236803930979, -1.422233405468891210, 1.491712647946776826 ) ) ;
#11873=CARTESIAN_POINT ( 'NONE',  ( 2.848279904836711118, 0.2930702634792031747, -1.994869876753922799 ) ) ;
#11880=CARTESIAN_POINT ( 'NONE',  ( 2.987657498945671897, 1.897406709466815444, 0.6818930838706839248 ) ) ;
#11881=CARTESIAN_POINT ( 'NONE',  ( 2.993917163610838816, -0.5349900852187582379, -1.761688665035024304 ) ) ;
#11882=CARTESIAN_POINT ( 'NONE',  ( 0.6984242042700332664, -0.8252692633385866339, 2.155259511649917137 ) ) ;
#11884=CARTESIAN_POINT ( 'NONE',  ( 2.917419293707240069, -0.2150262876145451196, 2.150894318904146729 ) ) ;
#11887=CARTESIAN_POINT ( 'NONE',  ( 2.671599042396528123, -0.8780164823973014565, -2.124237947079451683 ) ) ;
#11890=CARTESIAN_POINT ( 'NONE',  ( 1.779943879855113709, -1.003247456797161652, 1.578688272967261996 ) ) ;
#11891=CARTESIAN_POINT ( 'NONE',  ( 5.506699291815658093, 1.493407355681115378, -1.287129089984188290 ) ) ;
#11896=CARTESIAN_POINT ( 'NONE',  ( 0.2412292383832773390, 0.3817025157030576321, 2.173470055567463088 ) ) ;
#11897=CARTESIAN_POINT ( 'NONE',  ( 6.865700769154306826, -0.4580177224273937475, 2.026514595051785772 ) ) ;
#11900=CARTESIAN_POINT ( 'NONE',  ( 6.639320575229294086, 2.013432609116216021, 2.506292271646192393 ) ) ;
#11901=CARTESIAN_POINT ( 'NONE',  ( 4.522318884118472049, 1.213545612936163032, -1.553610194691892765 ) ) ;
#11902=CARTESIAN_POINT ( 'NONE',  ( -0.06985027309261250539, -2.078401542846250116, 0.4200961532789050379 ) ) ;
#11904=CARTESIAN_POINT ( 'NONE',  ( 4.776155900897590456, 1.325808183606682622, 1.888659687595494407 ) ) ;
#11906=CARTESIAN_POINT ( 'NONE',  ( 1.692308231870808921, 1.020316376917740575, -1.792489025137546044 ) ) ;
#11914=CARTESIAN_POINT ( 'NONE',  ( 4.018178019744323315, 2.155211776303669335, -0.2622048733134130782 ) ) ;
#11917=CARTESIAN_POINT ( 'NONE',  ( 3.895923546780861724, -0.5813109859279729230, -1.747131793041277970 ) ) ;
#11919=CARTESIAN_POINT ( 'NONE',  ( 6.720655732516650716, 2.467238681591706673, 2.210725262702870175 ) ) ;
#11920=CARTESIAN_POINT ( 'NONE',  ( 5.794512526436308875, 1.792401445336734733, -1.260760892635464980 ) ) ;
#11921=DIRECTION ( 'NONE',  ( -0.9999980456341537316, 0.000000000000000000, -0.001977050295958626257 ) ) ;
#11922=CARTESIAN_POINT ( 'NONE',  ( 6.350461102289020054, 0.7023508724467423248, 2.150821023316491498 ) ) ;
#11929=CARTESIAN_POINT ( 'NONE',  ( 0.7777615046654516862, -0.9880915000441170548, 1.468120464595161989 ) ) ;
#11931=CARTESIAN_POINT ( 'NONE',  ( 5.110025693318159590, -0.7223781944584523051, 1.879196401790662607 ) ) ;
#11932=CARTESIAN_POINT ( 'NONE',  ( 3.909285118862667829, 1.805215983022747439, 1.084321332058492571 ) ) ;
#11933=CARTESIAN_POINT ( 'NONE',  ( 2.442874106818424096, -1.667949397242382448, -0.9418811778915718858 ) ) ;
#11935=CARTESIAN_POINT ( 'NONE',  ( 2.945709429406599966, 1.390870048597905084, 1.394762357610879855 ) ) ;
#11936=CARTESIAN_POINT ( 'NONE',  ( 5.185809364388858533, 1.945378451193703118, -0.5428193807620449451 ) ) ;
#11937=CARTESIAN_POINT ( 'NONE',  ( 1.234984068473435892, -1.692697435815498919, 0.7966027930108383615 ) ) ;
#11938=CARTESIAN_POINT ( 'NONE',  ( 5.109832884134172026, -1.716065896558026216, 0.1740927981267632318 ) ) ;
#11939=CARTESIAN_POINT ( 'NONE',  ( 1.019614524654769872, -0.4619345408787678964, 1.855657206939323789 ) ) ;
#11941=CARTESIAN_POINT ( 'NONE',  ( 1.401302286655212948, 1.802556353783949517, -1.272968949304439379 ) ) ;
#11949=CARTESIAN_POINT ( 'NONE',  ( 2.488806849732328796, 2.007603858877416769, 0.5053560088097220904 ) ) ;
#11954=CARTESIAN_POINT ( 'NONE',  ( 6.094406630213895504, -1.134638919006492275, 1.791192486788994120 ) ) ;
#11960=CARTESIAN_POINT ( 'NONE',  ( 4.622422610786712127, 0.4444332032229811325, -1.966343831704894907 ) ) ;
#11961=CARTESIAN_POINT ( 'NONE',  ( 4.381993024020896854, -1.915445973796879864, -0.04088167158281148100 ) ) ;
#11963=CARTESIAN_POINT ( 'NONE',  ( 2.736070936638954176, 2.175344985778558726, 0.2654339622269741295 ) ) ;
#11966=CARTESIAN_POINT ( 'NONE',  ( 5.080342566386993219, 0.9961330521413218619, 1.749448578721881198 ) ) ;
#11969=CARTESIAN_POINT ( 'NONE',  ( 0.2984541275833849094, 1.388471424577278235, -1.462460896543740674 ) ) ;
#11971=CARTESIAN_POINT ( 'NONE',  ( 3.544548742447044987, -1.707904676211311479, 1.205638247120393247 ) ) ;
#11973=CARTESIAN_POINT ( 'NONE',  ( 2.186159124499872597, -1.690733796973374004, -0.3399922242280882245 ) ) ;
#11975=CARTESIAN_POINT ( 'NONE',  ( 5.642871316567687145, 2.044259226470702462, 0.5637153772257290640 ) ) ;
#11982=CARTESIAN_POINT ( 'NONE',  ( 1.154613445820645845, 0.3528100842024176620, 1.776585200675658172 ) ) ;
#11988=CARTESIAN_POINT ( 'NONE',  ( 3.070771698229213698, -1.370002115350689165, 1.185199408711124835 ) ) ;
#11989=CARTESIAN_POINT ( 'NONE',  ( 6.639320575229291421, 7.052752469465089824, 2.594893258668645952 ) ) ;
#11992=CARTESIAN_POINT ( 'NONE',  ( 3.490524873212813795, 1.815147244032933038, 0.4099927795770376693 ) ) ;
#11993=CARTESIAN_POINT ( 'NONE',  ( 1.106889576528688801, -0.04550283046177550778, 1.915226712711289636 ) ) ;
#11994=CARTESIAN_POINT ( 'NONE',  ( 0.7799652524137989928, -1.018268764971082430, 1.515009401286564694 ) ) ;
#12003=CARTESIAN_POINT ( 'NONE',  ( 6.209808219158968967, 0.5752867347804692111, -1.883509059051315271 ) ) ;
#12007=CARTESIAN_POINT ( 'NONE',  ( 0.2520486530714799445, 0.8021226228236020273, 1.930841216200715360 ) ) ;
#12009=CARTESIAN_POINT ( 'NONE',  ( 5.245112492223927170, -1.652184091924509879, 0.9903546681122497031 ) ) ;
#12011=CARTESIAN_POINT ( 'NONE',  ( 1.219449367515994309, -1.782015241123528826, 0.3957228718986585680 ) ) ;
#12012=CARTESIAN_POINT ( 'NONE',  ( 2.209865124170300898, -0.4819264253047173541, 2.153463223375853719 ) ) ;
#12016=CARTESIAN_POINT ( 'NONE',  ( 0.9945129418027212065, 1.939812372797902862, 0.3400383455644633290 ) ) ;
#12017=CARTESIAN_POINT ( 'NONE',  ( 3.034642427012054444, -1.711418951474739991, 0.9179939537737377142 ) ) ;
#12019=CARTESIAN_POINT ( 'NONE',  ( 0.4036724312478366938, 0.3418800534340654118, 1.986742826083332858 ) ) ;
#12021=CARTESIAN_POINT ( 'NONE',  ( 4.926513725511825648, -1.217676453003987191, 1.407301474667689956 ) ) ;
#12023=DIRECTION ( 'NONE',  ( 2.949029909160572061E-17, 1.000000000000000000, -8.673600428462354978E-15 ) ) ;
#12028=CARTESIAN_POINT ( 'NONE',  ( 1.874823134854076923, -0.1115055541827478930, -2.188858692977871279 ) ) ;
#12031=CARTESIAN_POINT ( 'NONE',  ( 3.211362085483655981, -0.3553965070040401852, 1.790585553824732390 ) ) ;
#12035=CARTESIAN_POINT ( 'NONE',  ( 6.925078400183558358, 1.280611897634201579, 1.970548662192173506 ) ) ;
#12038=CARTESIAN_POINT ( 'NONE',  ( 1.207505077391484161, -0.4687122323817956571, 1.868500445134027466 ) ) ;
#12039=CARTESIAN_POINT ( 'NONE',  ( 6.121922100595678096, 1.933298025717408608, -0.3319332437697538607 ) ) ;
#12042=CARTESIAN_POINT ( 'NONE',  ( 5.108995794240286159, -0.3219066699026683631, 2.167653318578148358 ) ) ;
#12045=CARTESIAN_POINT ( 'NONE',  ( 4.047765473330780850, 1.496028175931501947, 1.431257568052332729 ) ) ;
#12048=B_SPLINE_CURVE_WITH_KNOTS ( 'NONE', 3,
 ( #129398, #197492, #195377, #51259, #180196, #32870, #148758, #15530, #113125, #33929, #66398, #17658, #79485, #147699, #116310, #49134, #115251, #179130, #100004, #211599, #30753, #181242, #117383, #98946, #95766, #165000, #161820, #83741, #13409, #82674, #328, #72824, #69608, #6745, #34986, #155163, #153022, #184438, #55522, #138927, #19803, #85887, #137856, #183380, #84815, #151963, #36055, #134670, #101056, #121677, #3535, #167145, #37128, #170326, #5663, #204944, #135715, #118451, #22992, #4597, #21913, #200673, #88022, #86954, #201741, #18731, #154094, #56595, #150904, #2465, #68541, #102135, #185504, #70671, #52322, #71742, #168204, #53382, #119517, #103207, #169269, #203877, #20855, #136781, #202810, #54458, #120602, #186579, #38208, #187642, #104281, #39270, #105364, #171401, #89109, #172484, #108605, #77093, #25142, #189780, #73910, #42497, #123820, #107539, #173571, #78161, #91244, #160487, #41431, #144292, #159418, #12094, #28353, #157304, #210285, #8894, #122757, #188718, #94448, #92327, #74974, #57662, #24071, #59785, #141083, #143220, #40356, #90175, #207093, #58721, #140003, #106460, #60850, #124872, #156240, #190837, #109682, #11018, #7817, #174633, #26209, #158368, #206024, #175685, #9961, #27274, #76038, #142141, #208155, #93381, #125942, #191900, #43562, #209209, #127013, #192972, #44624, #110739, #176739, #29430, #61925, #96582, #182040, #95521, #130197, #198289, #177814, #131249, #128084, #165816, #194041, #161570, #99746, #213469, #197235, #13158, #147445, #65092, #111809, #149565, #79235, #62978, #211354, #98688, #145353, #49931, #129147, #116052, #74, #195123, #113944, #46761, #45694, #81365, #16337, #17399, #83483, #112872, #82418, #14205, #178887, #30500, #33671, #31564, #162630, #148507, #80300, #146397, #114993, #212411, #180991, #66138, #163696, #179940, #196191, #64054, #48875, #47834, #32611, #97639, #164745, #132284, #15278, #35801, #150646, #55266, #185240, #54196, #100802, #187385, #121413, #101878, #3280, #120337, #184181, #202547, #167945, #36863, #171139, #67212, #166888, #186313, #134416, #183124, #1149, #37948, #39016, #22731, #2207, #104020, #70409, #153836, #137596, #105098, #170067, #88847, #18477, #133347, #119256, #21653, #5406, #4342, #51001, #199353, #117121, #69347, #102947, #34730, #84557, #68284, #200420, #52067, #118193, #86691, #152760, #87760, #19546, #71484, #85624, #53123, #151711, #135458, #203614, #169007, #201481, #20605, #136527, #109421, #190577, #159159, #60587, #8634, #158112, #9703, #10758, #106198, #74715, #204684, #192704, #124619, #157046, #93118, #191637, #76831, #56334, #140818, #175426, #57394, #7557, #172225, #43301, #122493, #188455, #6488, #126745, #75780, #206832, #28092, #123559, #73643, #205765, #44360, #189523, #155971, #89918, #27012, #40087, #142952, #23814, #208951, #110482, #139741, #58465, #41169, #154905, #174370, #176481, #72564, #138662, #107278, #173297, #125677, #24879, #90984, #42233, #108348, #25949, #92056, #141887, #207896, #59519, #195933, #45429, #198046, #161303, #97381, #213220, #128874, #127829, #32365, #130997, #145086, #111545, #211090, #77902, #12888, #78966, #177554, #13953, #95254, #62713, #194856, #49675, #46489, #132036, #112611, #115800, #196986, #181788, #214257, #178623, #30233, #94188, #160228, #65888, #63788, #96319 ),
 .UNSPECIFIED., .F., .F.,
 ( 4, 1, 1, 1, 1, 1, 1, 1, 1, 1, 1, 1, 1, 1, 1, 1, 1, 1, 1, 1, 1, 1, 1, 1, 1, 1, 1, 1, 1, 1, 1, 1, 1, 1, 1, 1, 1, 1, 1, 1, 1, 1, 1, 1, 1, 1, 1, 1, 1, 1, 1, 1, 1, 1, 1, 1, 1, 1, 1, 1, 1, 1, 1, 1, 1, 1, 1, 1, 1, 1, 1, 1, 1, 1, 1, 1, 1, 1, 1, 1, 1, 1, 1, 1, 1, 1, 1, 1, 1, 1, 1, 1, 1, 1, 1, 1, 1, 1, 1, 1, 1, 1, 1, 1, 1, 1, 1, 1, 1, 1, 1, 1, 1, 1, 1, 1, 1, 1, 1, 1, 1, 1, 1, 1, 1, 1, 1, 1, 1, 1, 1, 1, 1, 1, 1, 1, 1, 1, 1, 1, 1, 1, 1, 1, 1, 1, 1, 1, 1, 1, 1, 1, 1, 1, 1, 1, 1, 1, 1, 1, 1, 1, 1, 1, 1, 1, 1, 1, 1, 1, 1, 1, 1, 1, 1, 1, 1, 1, 1, 1, 1, 1, 1, 1, 1, 1, 1, 1, 1, 1, 1, 1, 1, 1, 1, 1, 1, 1, 1, 1, 1, 1, 1, 1, 1, 1, 1, 1, 1, 1, 1, 1, 1, 1, 1, 1, 1, 1, 1, 1, 1, 1, 1, 1, 1, 1, 1, 1, 1, 1, 1, 1, 1, 1, 1, 1, 1, 1, 1, 1, 1, 1, 1, 1, 1, 1, 1, 1, 1, 1, 1, 1, 1, 1, 1, 1, 1, 1, 1, 1, 1, 1, 1, 1, 1, 1, 1, 1, 1, 1, 1, 1, 1, 1, 1, 1, 1, 1, 1, 1, 1, 1, 1, 1, 1, 1, 1, 1, 1, 1, 1, 1, 1, 1, 1, 1, 1, 1, 1, 1, 1, 1, 1, 1, 1, 1, 1, 1, 1, 1, 1, 1, 1, 1, 1, 1, 1, 1, 1, 1, 1, 1, 1, 1, 1, 1, 1, 1, 1, 1, 1, 1, 1, 1, 1, 1, 1, 1, 1, 1, 1, 1, 1, 1, 1, 1, 1, 1, 1, 1, 1, 1, 1, 1, 1, 1, 1, 1, 1, 1, 1, 1, 1, 1, 1, 1, 1, 1, 1, 1, 1, 1, 1, 1, 1, 1, 1, 1, 1, 1, 1, 1, 1, 1, 4 ),
 ( 0.000000000000000000, 0.002600063085273907840, 0.005208809393482579861, 0.007813201938950280895, 0.01041611862257568050, 0.01302098276518856741, 0.01562474632808895890, 0.01822919105953027183, 0.02083324087635668453, 0.02343728507989274734, 0.02604173773626635227, 0.02864548761524753420, 0.03125016255115702773, 0.03385383280295282959, 0.03645844125268089125, 0.03906229690237970897, 0.04166656525949016115, 0.04427081591349327910, 0.04687468903198145631, 0.04947928942627017462, 0.05208296534865054783, 0.05468764290212216328, 0.05729137561078536528, 0.05989584521530456201, 0.06249987723257615507, 0.06510392926424246607, 0.06770838613806146045, 0.07031213076997053224, 0.07291680575263978503, 0.07552047744215656389, 0.07812508546332513903, 0.08072894086165181837, 0.08333320924388483431, 0.08593745993457323207, 0.08854133291633270453, 0.09114593330519306369, 0.09374960916840779923, 0.09635428668231969807, 0.09895801939011879267, 0.1015624889210437753, 0.1041665209728785957, 0.1067705729027476208, 0.1093750297965602747, 0.1119787743537518920, 0.1145834493281674554, 0.1171871210017138010, 0.1197917289818775377, 0.1223955844170728779, 0.1249998527215379351, 0.1276041034591044177, 0.1302079763611066199, 0.1328125767709825433, 0.1354162526020633861, 0.1380209301064295735, 0.1406246628425296130, 0.1432291323291436380, 0.1458331644451768827, 0.1484372163025670099, 0.1510416732455448496, 0.1536454177576472568, 0.1562500927529001105, 0.1588537644400710158, 0.1614583724083656635, 0.1640622279099430147, 0.1666664961659596600, 0.1692707469797122277, 0.1718746198314790308, 0.1744792202914958457, 0.1770828961200470730, 0.1796875736439581817, 0.1822913064379278192, 0.1848957759094348730, 0.1874998081190861754, 0.1901038599334289314, 0.1927083169547665342, 0.1953120614513534081, 0.1979167364965291054, 0.2005204082269216870, 0.2031250162124720871, 0.2057288718099357372, 0.2083331400468157457, 0.2109373909660553770, 0.2135412637971000893, 0.2161458643363758370, 0.2187495401919937743, 0.2213542177645327069, 0.2239579506459335456, 0.2265624201315297737, 0.2291664524642116896, 0.2317705042649303715, 0.2343749613938155840, 0.2369787059044528299, 0.2395833810286300269, 0.2421870528318344207, 0.2447916608637582536, 0.2473955165866061623, 0.2499997848336539263, 0.2526040358876752157, 0.2552079087275039293, 0.2578125093751503782, 0.2604161852874245509, 0.2630208629376679097, 0.2656245959360551967, 0.2682290654649299166, 0.2708330979500496172, 0.2734371497665608608, 0.2760416070321756732, 0.2786453515864226738, 0.2812500268186742258, 0.2838536987242743503, 0.2864583068316831627, 0.2890621627094078216, 0.2916664309959213219, 0.2942706822140139789, 0.2968745550921262355, 0.2994791558772498252, 0.3020828318757637354, 0.3046875096327826826, 0.3072912427777066413, 0.3098957123790437307, 0.3124997450460035853, 0.3151037969077182255, 0.3177082543392401592, 0.3203119989666507461, 0.3229166743360447622, 0.3255203463736199843, 0.3281249545856204097, 0.3307288106477103140, 0.3333330790029824242, 0.3359373304144318562, 0.3385412033603223403, 0.3411458043120255135, 0.3437494804263583337, 0.3463541583192197293, 0.3489578916402267250, 0.3515623613432052874, 0.3541663942214042238, 0.3567704461577280162, 0.3593749037843310123, 0.3619786485144548260, 0.3645833240500557237, 0.3671869962491814965, 0.3697916045948764219, 0.3723954608708167080, 0.3749997293241361662, 0.3776039809582251716, 0.3802078540013843488, 0.3828124551487663840, 0.3854161314084936785, 0.3880208094662612184, 0.3906245429928945634, 0.3932290128266905938, 0.3958330459455252637, 0.3984370979858605777, 0.4010415558367163569, 0.4036453006990994852, 0.4062499764299690730, 0.4088536488202184072, 0.4114582573287078326, 0.4140621138479816388, 0.4166663824286341855, 0.4192706343146435644, 0.4218745074845589027, 0.4244791088567174686, 0.4270827852914125256, 0.4296874635431477407, 0.4322911973049493040, 0.4348956672987361882, 0.4374997006876018557, 0.4401037528613486738, 0.4427082109656274023, 0.4453119559898139901, 0.4479166319450127998, 0.4505203045559570407, 0.4531249132563394122, 0.4557287700484292658, 0.4583330387856985322, 0.4609372909529084184, 0.4635411642790657205, 0.4661457659050973201, 0.4687494425443319290, 0.4713541210190953512, 0.4739578550456061690, 0.4765623252285562383, 0.4791663589168480009, 0.4817704112534048067, 0.4843748696402766507, 0.4869786148558097882, 0.4895832910643978519, 0.4921869639256079565, 0.4947915728469811647, 0.4973954299413693159, 0.4999996988645384333, 0.5026039513422294602, 0.5052078248541136407, 0.5078124267631153321, 0.5104161036364611714, 0.5130207823633133879, 0.5156245166840751626, 0.5182289870853604707, 0.5208330211024742029, 0.5234370736312391470, 0.5260415323298749390, 0.5286452777662975500, 0.5312499542573357880, 0.5338536273983837122, 0.5364582365698458144, 0.5390620939960163449, 0.5416663631343685559, 0.5442706159518226894, 0.5468744896789192733, 0.5494790918999890028, 0.5520827690370186946, 0.5546874480450217915, 0.5572911826895774468, 0.5598956533383712131, 0.5624996877137050655, 0.5651037404640770756, 0.5677081995036498130, 0.5703119451905063197, 0.5729166219930570403, 0.5755202954435161278, 0.5781249048941674573, 0.5807287626816063364, 0.5833330320644263267, 0.5859372852509285856, 0.5885411592227242084, 0.5911457617849628088, 0.5937494392152512512, 0.5963541185334689798, 0.5989578535313645480, 0.6015623244568418793, 0.6041663592197970001, 0.6067704122211770024, 0.6093748716308627911, 0.6119786175976995590, 0.6145832947408284008, 0.6171869685302752151, 0.6197915782892181591, 0.6223954364674153528, 0.6249997061239902507, 0.6276039597088286515, 0.6302078339548128350, 0.6328124368873246919, 0.6354161146404495586, 0.6380207942979494451, 0.6406245296787346222, 0.6432290009100736228, 0.6458330360900554901, 0.6484370893718474083, 0.6510415491808263511, 0.6536452954571934093, 0.6562499729699700080, 0.6588536471279848872, 0.6614582572243260516, 0.6640621158227759668, 0.6666663857823964534, 0.6692706397948642305, 0.6718745143445301604, 0.6744791176764239893, 0.6770827957819672838, 0.6796874758078212952, 0.6822912116010506622, 0.6848956831674339885, 0.6874997187938534093, 0.6901037723854651640, 0.6927082326229228038, 0.6953119792383747333, 0.6979166571498732763, 0.7005203317060422208, 0.7031249421688929857, 0.7057288012170955804, 0.7083330715090569996, 0.7109373259784533827, 0.7135412008612989077, 0.7161458046216893081, 0.7187494831092385850, 0.7213541635325240176, 0.7239578997677582617, 0.7265623716983737879, 0.7291664078006476757, 0.7317704617314926274, 0.7343749224266207243, 0.7369786694107173242, 0.7395833477500189934, 0.7421870227339337767, 0.7447916335924112952, 0.7473954931198736329, 0.7499997637734774347, 0.7526040187291080930, 0.7552078939746372788, 0.7578124981926457338, 0.7604161770917949870, 0.7630208579415957981, 0.7656245946484027121, 0.7682290669724446408, 0.7708331035799980135, 0.7734371578794957403, 0.7760416190614934928, 0.7786453664438016675, 0.7812500452399944173, 0.7838537206812543623, 0.7864583319644831150, 0.7890621920007202528, 0.7916664630452742157, 0.7942707185164536998, 0.7968745941541772737, 0.7994791988589329268, 0.8020828781992835887, 0.8046875595046918406, 0.8072912967126475436, 0.8098957694593176271, 0.8124998066015838294, 0.8151038612991610144, 0.8177083229972362810, 0.8203120708073305956, 0.8229167500895105958, 0.8255204260177235742, 0.8281250377548363684, 0.8307288983293719120, 0.8333331697941922522, 0.8359374258102438837, 0.8385413018696807885, 0.8411459070903221091, 0.8437495869014844940, 0.8463542686916004643, 0.8489580064302900686, 0.8515624796287988296, 0.8541665173352209761, 0.8567705724603134065, 0.8593750347036837045, 0.8619787829711476057, 0.8645834627684209073, 0.8671871392132045608, 0.8697917514333429745, 0.8723956125757112989, 0.8749998844901232253, 0.8776041410803804288, 0.8802080175910590443, 0.8828126233567346048, 0.8854163036683286858, 0.8880209859722626442, 0.8906247242712825862, 0.8932291979508502067, 0.8958332362508822921, 0.8984372918329353030, 0.9010417546508288078, 0.9036455034052560675, 0.9062501837467389354, 0.9088538607377212308, 0.9114584734700372781, 0.9140623352097841936, 0.9166666076031229071, 0.9192708647969299873, 0.9218747417883903505, 0.9244793481282622682, 0.9270830289699085736, 0.9296877118167798937, 0.9322914507057830091, 0.9348959248956096868, 0.9374999638185942397, 0.9401040198872741005, 0.9427084833090058069, 0.9453122325795346725, 0.9479169134952544207, 0.9505205910598265584, 0.9531252043308329203, 0.9557290667238423909, 0.9583333396063040688, 0.9609375973010293448, 0.9635414750455153499, 0.9661460823481272664, 0.9687497623469286667, 0.9713544456720903941, 0.9739581901020435417, 0.9765626606554614897, 0.9791666924408860551, 0.9817707657828746992, 0.9843752055175947202, 0.9869789906880002128, 0.9895838567146432174, 0.9921867690109741345, 0.9947911791560083428, 0.9973999138825643263, 0.9999999999999998890 ),
 .UNSPECIFIED. ) ;
#12051=CARTESIAN_POINT ( 'NONE',  ( 3.551692777231782561, -1.542557649656286944, 1.704429084079077006 ) ) ;
#12058=CARTESIAN_POINT ( 'NONE',  ( 4.083879184154452169, -1.920976184332440662, -0.2838548334032560683 ) ) ;
#12063=CARTESIAN_POINT ( 'NONE',  ( 4.939673314881130040, -1.814047719456039154, 0.6055163330952323397 ) ) ;
#12064=CARTESIAN_POINT ( 'NONE',  ( 5.842733193948632220, 0.3409603658401075821, 1.690541223788865510 ) ) ;
#12065=CARTESIAN_POINT ( 'NONE',  ( 4.487517715496184501, -0.5331711073110931842, 1.944729879240604031 ) ) ;
#12067=CARTESIAN_POINT ( 'NONE',  ( 2.016531038934398445, -1.041976349804032420, -1.945408382319254503 ) ) ;
#12070=CARTESIAN_POINT ( 'NONE',  ( 1.693425821628431471, -0.7032018978916483309, 1.968960419152628871 ) ) ;
#12071=CARTESIAN_POINT ( 'NONE',  ( 6.468005306911782881, 0.9119784028226736172, 1.516475106587056532 ) ) ;
#12072=CARTESIAN_POINT ( 'NONE',  ( 6.223279759862190730, 1.994869330463379331, 0.2930738960792296233 ) ) ;
#12074=CARTESIAN_POINT ( 'NONE',  ( 2.871321604122719418, 2.176383266876817046, -0.7197843628353149947 ) ) ;
#12075=CARTESIAN_POINT ( 'NONE',  ( 0.8139225777531241546, 1.606474054549825503, 0.6698172574813018310 ) ) ;
#12076=CARTESIAN_POINT ( 'NONE',  ( 3.041385797112206912, 0.05609166564453024750, 2.120036961950934273 ) ) ;
#12078=CARTESIAN_POINT ( 'NONE',  ( 1.616079437515309136, 0.5095893236424541284, -1.657241410798731440 ) ) ;
#12081=CARTESIAN_POINT ( 'NONE',  ( 0.8718042753090318175, -0.3185811321036461363, 2.147578089749022645 ) ) ;
#12082=CARTESIAN_POINT ( 'NONE',  ( 3.801970467005914678, -1.040791964576088358, -1.727064642965264740 ) ) ;
#12083=CARTESIAN_POINT ( 'NONE',  ( 5.375000000000002665, 2.052068128417941395, -3.059081846666863488E-13 ) ) ;
#12085=CARTESIAN_POINT ( 'NONE',  ( 6.498663727319215155, -0.5164181641097148612, -1.855934172746701583 ) ) ;
#12087=CARTESIAN_POINT ( 'NONE',  ( 2.953626239309721679, -1.957189270898977762, 1.050815160798105552 ) ) ;
#12093=CARTESIAN_POINT ( 'NONE',  ( 5.249435226766168583, 1.738107782858036687, -0.09287461536438243459 ) ) ;
#12094=CARTESIAN_POINT ( 'NONE',  ( 4.949637131784443866, 1.452432516441283905, 1.319008059494260143 ) ) ;
#12098=CARTESIAN_POINT ( 'NONE',  ( 5.114671183409561728, 1.565253227384774792, -1.633764300155052807 ) ) ;
#12099=CARTESIAN_POINT ( 'NONE',  ( 1.926308760915905527, 1.058537693354057785, 1.770204612073868145 ) ) ;
#12103=CARTESIAN_POINT ( 'NONE',  ( 3.233525009082056201, -1.253693836546897700, -1.388425355430204622 ) ) ;
#12104=CARTESIAN_POINT ( 'NONE',  ( 2.724952806592676691, 1.721339412077933284, 0.2094855716100688936 ) ) ;
#12105=CARTESIAN_POINT ( 'NONE',  ( -0.005774900045998726007, -2.292045413227526751, -0.04753075064714216980 ) ) ;
#12106=CARTESIAN_POINT ( 'NONE',  ( 1.255210933454937283, -1.738917431694649407, 1.358592805172780693 ) ) ;
#12107=CARTESIAN_POINT ( 'NONE',  ( 3.977527890101069996, 2.036293384626610248, -0.7259696361804208742 ) ) ;
#12108=CARTESIAN_POINT ( 'NONE',  ( 5.050698599679353862, -1.641444558978710555, -1.037428038565652466 ) ) ;
#12113=CARTESIAN_POINT ( 'NONE',  ( 5.361953999179126740, -0.05229508359532940298, -2.015913028294749942 ) ) ;
#12117=CARTESIAN_POINT ( 'NONE',  ( 2.894927146036041510, 1.565677646668685696, -0.9388022922067614795 ) ) ;
#12118=CARTESIAN_POINT ( 'NONE',  ( 2.626236979526615389, -1.269917727785064843, -1.804575601930514139 ) ) ;
#12124=CARTESIAN_POINT ( 'NONE',  ( 0.5803392809272100994, 0.9991348162329892757, 1.755301537792392175 ) ) ;
#12125=CARTESIAN_POINT ( 'NONE',  ( 1.295735140135088281, 1.957893036122235531, -0.8148005001323217478 ) ) ;
#12129=CARTESIAN_POINT ( 'NONE',  ( 1.727181476345755806, 0.1432717513335572956, -1.855521175285803182 ) ) ;
#12131=CARTESIAN_POINT ( 'NONE',  ( 0.9190830904215805397, 1.997680973563022544, 0.8264451868333838602 ) ) ;
#12132=CARTESIAN_POINT ( 'NONE',  ( 6.592432824109000222, -0.4393352932590722792, 1.975308225066509049 ) ) ;
#12136=CARTESIAN_POINT ( 'NONE',  ( 3.510199737632841543, -0.7410081052188906003, -1.668730646197075673 ) ) ;
#12141=CARTESIAN_POINT ( 'NONE',  ( 6.134138708105167481, 0.1511139231759016377, -2.010518800921741622 ) ) ;
#12142=CARTESIAN_POINT ( 'NONE',  ( 5.824118960990139371, 1.775556191179916699, 0.4867722729226392486 ) ) ;
#12144=CARTESIAN_POINT ( 'NONE',  ( 4.442184936073533486, 0.9892916563519343898, -2.085014998049372625 ) ) ;
#12146=CARTESIAN_POINT ( 'NONE',  ( 6.098930168602409552, 1.771044849343451633, -1.239067683784184970 ) ) ;
#12148=CARTESIAN_POINT ( 'NONE',  ( 1.716251783418326848, 1.812799857666002934, 0.6971432602522424915 ) ) ;
#12151=CARTESIAN_POINT ( 'NONE',  ( 4.341395233127314235, -1.327617041990782010, 1.876015773706960932 ) ) ;
#12154=CARTESIAN_POINT ( 'NONE',  ( 4.979306205331720747, 1.745251617482036943, -0.6738592683939447214 ) ) ;
#12157=CARTESIAN_POINT ( 'NONE',  ( 2.250135261179100343, 0.8981609309555339538, -1.688322754368525747 ) ) ;
#12160=CARTESIAN_POINT ( 'NONE',  ( 4.371826309796801979, 2.140994599346605742, -0.5347268394074317088 ) ) ;
#12165=CARTESIAN_POINT ( 'NONE',  ( 1.932829124449897851, 0.1894527445373411501, 1.962211987329742113 ) ) ;
#12166=CARTESIAN_POINT ( 'NONE',  ( 1.729934149615200312, -2.172323606337727142, 0.7788181121253530126 ) ) ;
#12167=CARTESIAN_POINT ( 'NONE',  ( 2.558977423257744022, 1.577441344615847951, -1.166261179026031325 ) ) ;
#12169=CARTESIAN_POINT ( 'NONE',  ( 5.752800572348735209, -0.4956410525326099270, -2.002042340502646844 ) ) ;
#12176=CARTESIAN_POINT ( 'NONE',  ( 2.448294946665624749, -0.9317531996627312907, 1.961122280359078873 ) ) ;
#12180=CARTESIAN_POINT ( 'NONE',  ( 2.776451973220807279, -1.788819259240326698, -0.5467896145717602296 ) ) ;
#12181=CARTESIAN_POINT ( 'NONE',  ( 6.432923066502826082, 0.2047513753351773436, 2.151863363619124225 ) ) ;
#12182=CARTESIAN_POINT ( 'NONE',  ( -0.02244404828157658613, -0.004869073801674199918, -2.189079685368473527 ) ) ;
#12183=CARTESIAN_POINT ( 'NONE',  ( 6.827182134110205247, 0.5943742033862747798, 1.864010940340610212 ) ) ;
#12185=CARTESIAN_POINT ( 'NONE',  ( 2.297387027313551489, 1.747684631587187232, -0.7765785915121098393 ) ) ;
#12186=CARTESIAN_POINT ( 'NONE',  ( 4.399107752292472640, 1.421951945714538867, 1.053510053677222613 ) ) ;
#12188=CARTESIAN_POINT ( 'NONE',  ( 1.594246750649646494, -1.022002606473694675, 1.616071880676916317 ) ) ;
#12191=CARTESIAN_POINT ( 'NONE',  ( 5.255460224911852052, 1.844849436727209469, -0.5155117042133209315 ) ) ;
#12193=CARTESIAN_POINT ( 'NONE',  ( 6.830521637698823589, -1.212721230272953754, 1.552361911452035503 ) ) ;
#12196=CARTESIAN_POINT ( 'NONE',  ( 5.612129163471575310, -0.8422657237196762292, -1.670366365510121742 ) ) ;
#12197=CARTESIAN_POINT ( 'NONE',  ( 1.910518402784128433, 1.353611321597010253, -1.225282022559864625 ) ) ;
#12198=CARTESIAN_POINT ( 'NONE',  ( 4.037865812933420173, -1.521084700717803884, -1.599171214764223636 ) ) ;
#12201=CARTESIAN_POINT ( 'NONE',  ( 2.471201797017197777, 1.841352583063287529, 0.9297268146766042296 ) ) ;
#12207=CARTESIAN_POINT ( 'NONE',  ( 5.389151899530504330, 0.1487064154041470299, 2.065066873896327593 ) ) ;
#12209=CARTESIAN_POINT ( 'NONE',  ( 2.794378387653595475, -2.155598273342887339, -0.1620501260681943834 ) ) ;
#12211=CARTESIAN_POINT ( 'NONE',  ( 3.299477536675638145, 1.824990673169521793, -0.8654797531507262276 ) ) ;
#12217=CARTESIAN_POINT ( 'NONE',  ( 0.7961116948485976730, -0.9110139862544311962, -1.799120828532501326 ) ) ;
#12218=CARTESIAN_POINT ( 'NONE',  ( 5.724229345562060089, 2.111793275502030554, 0.5857118945327836057 ) ) ;
#12220=CARTESIAN_POINT ( 'NONE',  ( 4.552931727387078631, 0.3324577288378940954, 1.883125075537089854 ) ) ;
#12224=CARTESIAN_POINT ( 'NONE',  ( 2.935172905452135161, -1.650095542580119812, -1.158671029019647358 ) ) ;
#12227=CARTESIAN_POINT ( 'NONE',  ( 4.858271033065001632, 0.6623171007707692182, 1.592740567422048947 ) ) ;
#12232=CARTESIAN_POINT ( 'NONE',  ( 0.6024989291013755910, 2.064475859885641640, 0.1558578049991043990 ) ) ;
#12233=CARTESIAN_POINT ( 'NONE',  ( 6.830528382861658088, -1.277203763263988101, 1.630111558092485868 ) ) ;
#12235=CARTESIAN_POINT ( 'NONE',  ( 6.217428747564047065, 1.510149904227086504, 1.000116013982331076 ) ) ;
#12238=CARTESIAN_POINT ( 'NONE',  ( 6.059207019112636594, -1.526464042762348594, 0.9750640111952106892 ) ) ;
#12241=CARTESIAN_POINT ( 'NONE',  ( 3.047022719409075986, -1.791863632763015968, -1.261349808265788797 ) ) ;
#12243=CARTESIAN_POINT ( 'NONE',  ( 1.064813361795993618, 1.487921858168140377, -1.278797858372302088 ) ) ;
#12245=CARTESIAN_POINT ( 'NONE',  ( 5.448823958578076443, -1.733895640293681373, -0.8146214837579464074 ) ) ;
#12253=CARTESIAN_POINT ( 'NONE',  ( 1.956163130892615731, 2.155914767609674598, -0.1587918856347721730 ) ) ;
#12256=CARTESIAN_POINT ( 'NONE',  ( 2.115964440355810439, -0.8579360106165806465, -1.611413330227830176 ) ) ;
#12257=CARTESIAN_POINT ( 'NONE',  ( -0.2104748580754166598, -0.006608320950483163522, -2.103482951484026753 ) ) ;
#12258=CARTESIAN_POINT ( 'NONE',  ( 4.911078036072877850, 1.588895129109271442, 0.8988584441092376531 ) ) ;
#12261=CARTESIAN_POINT ( 'NONE',  ( 3.543367420142525148, 1.781686863328624026, -0.8397465311346365979 ) ) ;
#12263=CARTESIAN_POINT ( 'NONE',  ( 6.198774611348529362, 1.617120784385807974, 1.075137550886333004 ) ) ;
#12270=CARTESIAN_POINT ( 'NONE',  ( 3.545477442914763078, -1.765841875850767906, 0.7343832577718923948 ) ) ;
#12273=CARTESIAN_POINT ( 'NONE',  ( 0.1478802723770406002, -1.707511933842900564, -1.397569297917726550 ) ) ;
#12274=CARTESIAN_POINT ( 'NONE',  ( 4.863935948449842783, 0.6292040250746065988, -1.912316011988722586 ) ) ;
#12276=CARTESIAN_POINT ( 'NONE',  ( 6.393173274427864428, 1.585754722747900969, -0.9045919592586546543 ) ) ;
#12277=CARTESIAN_POINT ( 'NONE',  ( 0.5552397518338060278, 1.722184604005328357, -1.148819969904082861 ) ) ;
#12287=CARTESIAN_POINT ( 'NONE',  ( 4.078545790824074757, -0.6587176911285116399, 1.604389539659875297 ) ) ;
#12289=CARTESIAN_POINT ( 'NONE',  ( 1.569279613544020568, 1.823957739939351619, 0.9794188589333228112 ) ) ;
#12291=CARTESIAN_POINT ( 'NONE',  ( 2.109133483290903222, 0.003435389629122351501, 2.117403154539731602 ) ) ;
#12295=CARTESIAN_POINT ( 'NONE',  ( 0.4441182907778543631, -0.9332952320128800050, 1.734295555568473368 ) ) ;
#12300=CARTESIAN_POINT ( 'NONE',  ( 2.537429240164018385, -1.699656577751871289, -1.538240582240576693 ) ) ;
#12301=CARTESIAN_POINT ( 'NONE',  ( 1.119449510670032177, -1.781678707675336870, 0.3977030049751931196 ) ) ;
#12302=CARTESIAN_POINT ( 'NONE',  ( 3.023589307540079041, -0.3687504995396119201, 1.876329818327879817 ) ) ;
#12306=CARTESIAN_POINT ( 'NONE',  ( 2.074478728756317114, 0.8647236062047275462, 1.818190761793165189 ) ) ;
#12307=CARTESIAN_POINT ( 'NONE',  ( 1.709737484509077365, 0.5745576563440238926, -1.875703277996950469 ) ) ;
#12311=CARTESIAN_POINT ( 'NONE',  ( 4.681631697639319079, -0.9857103537862299536, 1.843662662672640007 ) ) ;
#12312=CARTESIAN_POINT ( 'NONE',  ( 2.940057854958120220, 1.756256042272446694, 0.2183286820098342407 ) ) ;
#12315=CARTESIAN_POINT ( 'NONE',  ( 0.006183538434290089709, -0.9405624870862170361, -1.977291442860461768 ) ) ;
#12316=CARTESIAN_POINT ( 'NONE',  ( 4.136439897933008147, -1.512742658674090857, 0.8602829033797516622 ) ) ;
#12318=CARTESIAN_POINT ( 'NONE',  ( -0.1104750535120268551, 0.2303756098476944791, -2.137063993957021513 ) ) ;
#12319=CARTESIAN_POINT ( 'NONE',  ( 4.112396791320716005, 0.5851491843551993588, -1.632232688200731197 ) ) ;
#12320=CARTESIAN_POINT ( 'NONE',  ( 4.176368576274028577, -1.112882343535037677, -1.864130199707826785 ) ) ;
#12322=CARTESIAN_POINT ( 'NONE',  ( 0.3568547849697421004, -1.996003273109921983, -0.7069239421778094057 ) ) ;
#12323=CARTESIAN_POINT ( 'NONE',  ( 6.218749999999983125, -0.7852924748301916003, 1.895863743164212467 ) ) ;
#12326=CARTESIAN_POINT ( 'NONE',  ( 3.803666480526507687, -0.5600534170543782775, 1.843171563392527856 ) ) ;
#12328=CARTESIAN_POINT ( 'NONE',  ( 0.6104036325267605534, -0.7939654203579590286, 2.074740863049700845 ) ) ;
#12330=CARTESIAN_POINT ( 'NONE',  ( 6.883263157960333167, 4.698395927207251077, 2.408847447403542841 ) ) ;
#12333=CARTESIAN_POINT ( 'NONE',  ( 2.420824200137431603, -0.8528996238171372424, -2.051222908810364842 ) ) ;
#12339=CARTESIAN_POINT ( 'NONE',  ( 0.8443752267504719411, 0.3905955241953715795, -1.978051186352240309 ) ) ;
#12341=CARTESIAN_POINT ( 'NONE',  ( 5.898899852458296955, 0.3987951208904988443, 2.023601990196000955 ) ) ;
#12346=CARTESIAN_POINT ( 'NONE',  ( 0.8074156707096367125, -1.761990802586909766, 0.1653023320123351292 ) ) ;
#12347=CARTESIAN_POINT ( 'NONE',  ( 6.381516696256908538, -0.4728550111133908995, -1.668365442416564814 ) ) ;
#12348=CARTESIAN_POINT ( 'NONE',  ( 5.671390581117805141, 1.043574818874394294, 1.392714124641497131 ) ) ;
#12349=CARTESIAN_POINT ( 'NONE',  ( 2.490095330609965796, -2.286454923436448183, -0.1652806634409968445 ) ) ;
#12351=CARTESIAN_POINT ( 'NONE',  ( 1.605144257462550517, -1.827384369528777031, 0.2241066044648756805 ) ) ;
#12354=CARTESIAN_POINT ( 'NONE',  ( 2.063248287022978467, 0.3151258922809499485, -1.798016661460503984 ) ) ;
#12355=CARTESIAN_POINT ( 'NONE',  ( 2.936172824561166905, -1.650081981912490336, -1.158688413653415239 ) ) ;
#12357=CARTESIAN_POINT ( 'NONE',  ( 1.060776890969020059, -1.982532595227912475, -0.9341070725938580566 ) ) ;
#12359=CARTESIAN_POINT ( 'NONE',  ( 4.208114709606614490, -2.100488694582537619, 0.1524824656061254391 ) ) ;
#12362=CARTESIAN_POINT ( 'NONE',  ( 1.504437137538238600, 2.067909592606699487, 0.1035681241481553605 ) ) ;
#12365=CARTESIAN_POINT ( 'NONE',  ( 4.547591073264711348, -1.938359017324686961, 0.8602097090630379528 ) ) ;
#12367=CARTESIAN_POINT ( 'NONE',  ( 6.568987803155795113, -1.671525225137669102, -0.7347104647430282576 ) ) ;
#12374=CARTESIAN_POINT ( 'NONE',  ( -0.06965283525045895541, -2.176852707449424607, 0.4419662969857121038 ) ) ;
#12375=CARTESIAN_POINT ( 'NONE',  ( 1.360533241671294746, 0.8531190763820644118, 1.925603555557230617 ) ) ;
#12378=CARTESIAN_POINT ( 'NONE',  ( 4.750749981963457991, -0.4049220142380467458, -1.816192249911535272 ) ) ;
#12386=CARTESIAN_POINT ( 'NONE',  ( 2.453501617077270769, 1.514643136537169310, 1.246875331876770243 ) ) ;
#12387=CARTESIAN_POINT ( 'NONE',  ( 0.7960496800812133511, -0.7770375076890515542, 2.017388685454111652 ) ) ;
#12391=CARTESIAN_POINT ( 'NONE',  ( 2.969770354771487320, 1.463018481607085475, 0.9301108516524180247 ) ) ;
#12392=CARTESIAN_POINT ( 'NONE',  ( 2.571852248423611709, -1.665254919270848344, -0.5056227470447529626 ) ) ;
#12396=CARTESIAN_POINT ( 'NONE',  ( 0.9837497097957871306, 1.861730512597782550, 0.7742002051285418185 ) ) ;
#12397=CARTESIAN_POINT ( 'NONE',  ( 6.925078400183577010, 2.950057911518182419, 2.596529392604688180 ) ) ;
#12399=CARTESIAN_POINT ( 'NONE',  ( 1.533988556244444856, 0.9736202887896376890, -1.714215200822625684 ) ) ;
#12400=CARTESIAN_POINT ( 'NONE',  ( 5.959226163113887864, -1.611951592244726950, 1.028742869173946861 ) ) ;
#12406=CARTESIAN_POINT ( 'NONE',  ( 1.436200859769844129, -1.123848162932556072, -1.677891559433869473 ) ) ;
#12408=CARTESIAN_POINT ( 'NONE',  ( 4.946439154741203659, 2.300974901101384695, 0.1755221459238848203 ) ) ;
#12409=CARTESIAN_POINT ( 'NONE',  ( 6.355910407107248083, -0.6622273607519140182, 1.846833223631501264 ) ) ;
#12410=CARTESIAN_POINT ( 'NONE',  ( 2.922649740298603138, -1.356309479035762378, 1.417576456850026867 ) ) ;
#12414=CARTESIAN_POINT ( 'NONE',  ( 0.9720387486300664515, -0.9465246498777776241, 1.894042457640370491 ) ) ;
#12417=CARTESIAN_POINT ( 'NONE',  ( 0.3394786764520755784, 1.835982197492795898, 0.1384515631646099088 ) ) ;
#12420=CARTESIAN_POINT ( 'NONE',  ( 3.181995841446764839, 2.068044944583770306, -0.4684364081647199307 ) ) ;
#12424=CARTESIAN_POINT ( 'NONE',  ( 3.532544388643095612, 2.009728383178956523, 0.4550750861811359571 ) ) ;
#12426=CARTESIAN_POINT ( 'NONE',  ( 0.06366010765614799061, -1.203631707120488947, 1.393476991864414760 ) ) ;
#12431=CARTESIAN_POINT ( 'NONE',  ( 0.5224629442122545875, -1.184049029929446828, -1.862174541895257995 ) ) ;
#12432=CARTESIAN_POINT ( 'NONE',  ( 2.759333473672697767, -1.967098484071924558, -1.117512413888957612 ) ) ;
#12434=CARTESIAN_POINT ( 'NONE',  ( 2.373076535756658778, -1.577936908029322849, -0.8897043057118164677 ) ) ;
#12436=CARTESIAN_POINT ( 'NONE',  ( 2.764735878068668384, -0.1456047134679704924, -1.910273805325033436 ) ) ;
#12437=CARTESIAN_POINT ( 'NONE',  ( 3.842288295254093100, -1.023014542950370975, 1.799900136785845817 ) ) ;
#12439=CARTESIAN_POINT ( 'NONE',  ( 1.744934968351062210, -1.666494570726485991, 1.053036000364399483 ) ) ;
#12440=CARTESIAN_POINT ( 'NONE',  ( 6.270143248794765256, 0.9928014866268529692, 1.650855525168734461 ) ) ;
#12441=CARTESIAN_POINT ( 'NONE',  ( 2.676452114398766291, -1.789519730395791486, -0.5449050523786898026 ) ) ;
#12442=CARTESIAN_POINT ( 'NONE',  ( 1.665117554179825321, -1.629454703905337087, 1.634364892973801719 ) ) ;
#12444=CARTESIAN_POINT ( 'NONE',  ( 3.068646357036347361, 1.349867735329785434, -1.281425607799644206 ) ) ;
#12447=CARTESIAN_POINT ( 'NONE',  ( 6.021949879679938000, 2.032782779420911456, -0.3490252056354887222 ) ) ;
#12452=CARTESIAN_POINT ( 'NONE',  ( 6.598663424749101836, -0.5579900645847408747, -2.030628608299019700 ) ) ;
#12456=CARTESIAN_POINT ( 'NONE',  ( 6.450466699499744827, 0.6713059571747861387, 2.054807225473152865 ) ) ;
#12457=CARTESIAN_POINT ( 'NONE',  ( 6.410808175004245157, -0.5408338447881118061, -1.945826018873537455 ) ) ;
#12462=CARTESIAN_POINT ( 'NONE',  ( 6.825078400183556937, 1.302289051367941708, 1.872899343898648983 ) ) ;
#12465=CARTESIAN_POINT ( 'NONE',  ( 4.716029918043215474, 1.032482702726954527, -1.731993998903176957 ) ) ;
#12470=CARTESIAN_POINT ( 'NONE',  ( 5.664953204072169513, -1.952404353424816774, -0.9282482345986733385 ) ) ;
#12476=CARTESIAN_POINT ( 'NONE',  ( 6.538686444676896414, -1.556836737174282836, 1.281159629702780078 ) ) ;
#12479=CARTESIAN_POINT ( 'NONE',  ( 1.541173760317329666, -1.247365581009220126, -1.191596266039594010 ) ) ;
#12483=CARTESIAN_POINT ( 'NONE',  ( 0.5613125002107671735, 1.751697300359332798, -0.2511290008074765212 ) ) ;
#12484=CARTESIAN_POINT ( 'NONE',  ( 1.137358842852369545, -0.04729656459989117767, 2.012689239070045488 ) ) ;
#12486=CARTESIAN_POINT ( 'NONE',  ( 3.610573252990852744, -0.8922430012947217826, -2.018528625508857921 ) ) ;
#12488=CARTESIAN_POINT ( 'NONE',  ( 5.647405056649561494, 1.918175650701968937, -1.016889183816371611 ) ) ;
#12492=CARTESIAN_POINT ( 'NONE',  ( 2.983181628360128013, -1.960071735995170927, -0.8095406527153580223 ) ) ;
#12493=CARTESIAN_POINT ( 'NONE',  ( 3.251577527157409886, 1.966640965408305686, -0.4445242805125593222 ) ) ;
#12494=CARTESIAN_POINT ( 'NONE',  ( 3.744242849288460295, 0.9642487561531964957, -1.533428966541541039 ) ) ;
#12498=CARTESIAN_POINT ( 'NONE',  ( 0.6197280442463182215, -0.9970892369244135356, -1.582582228963416382 ) ) ;
#12502=CARTESIAN_POINT ( 'NONE',  ( 1.481495926510235206, -0.6419399793253840469, 1.805124470068826037 ) ) ;
#12509=CARTESIAN_POINT ( 'NONE',  ( 5.032170685167933755, 1.114402916724830161, -1.852182961850391774 ) ) ;
#12512=CARTESIAN_POINT ( 'NONE',  ( 2.848016566918720294, -1.427295477286108394, -1.568503593382633454 ) ) ;
#12515=CARTESIAN_POINT ( 'NONE',  ( 4.446526809179438544, 0.5226573815438217974, 1.900768696068744434 ) ) ;
#12516=CARTESIAN_POINT ( 'NONE',  ( 6.533470333208203584, -0.1312131129157616261, 1.882018712217728318 ) ) ;
#12518=CARTESIAN_POINT ( 'NONE',  ( 5.507064729579815854, -0.04930729212004316547, 2.116909390494752685 ) ) ;
#12519=CARTESIAN_POINT ( 'NONE',  ( 6.877413706903859669, -0.1509731808640407125, 1.936391978998742269 ) ) ;
#12520=CARTESIAN_POINT ( 'NONE',  ( 2.115084705647510610, -1.883649903580833174, 0.4717843263111404783 ) ) ;
#12522=DIRECTION ( 'NONE',  ( 1.039099362110107450E-15, 1.000000000000000000, -4.583713267641621330E-32 ) ) ;
#12524=CARTESIAN_POINT ( 'NONE',  ( 1.992240001063511290, -0.5588421479580056861, -2.014483121414586186 ) ) ;
#12528=CARTESIAN_POINT ( 'NONE',  ( 0.5745104438982637785, -1.313040981126518902, 1.248171054211825171 ) ) ;
#12530=CARTESIAN_POINT ( 'NONE',  ( 4.934293700819583073, 1.136511309699510308, -1.891595316245115788 ) ) ;
#12532=CARTESIAN_POINT ( 'NONE',  ( 3.434799832723956392, 2.152550277175222515, 0.4854691814954179563 ) ) ;
#12533=CARTESIAN_POINT ( 'NONE',  ( 1.225099565173026761, 1.686864977381890451, 0.9006792851762451813 ) ) ;
#12536=CARTESIAN_POINT ( 'NONE',  ( 4.422371208857902580, 0.9731212702417373350, 1.827393648576709717 ) ) ;
#12537=CARTESIAN_POINT ( 'NONE',  ( 2.887745953747706373, 1.527789104365802286, 1.529575784674996886 ) ) ;
#12538=CARTESIAN_POINT ( 'NONE',  ( 5.249643141573060667, 2.189086832579402842, -0.1069518675670885766 ) ) ;
#12543=CARTESIAN_POINT ( 'NONE',  ( 0.4752326960846975923, -2.001511663014220677, -0.2440270837566413387 ) ) ;
#12546=CARTESIAN_POINT ( 'NONE',  ( 4.276279003695676373, -1.059865903354087813, -1.778221194881628220 ) ) ;
#12547=CARTESIAN_POINT ( 'NONE',  ( 3.316937275718701894, 1.741877725598478976, 0.8232385001258867296 ) ) ;
#12548=CARTESIAN_POINT ( 'NONE',  ( -0.07068620461728526705, -1.560437159073333468, -1.276799021846956705 ) ) ;
#12551=CARTESIAN_POINT ( 'NONE',  ( 3.537912347765668208, 1.245987026601946157, 1.525231921242198307 ) ) ;
#12552=CARTESIAN_POINT ( 'NONE',  ( -0.02321191073820921824, -0.1601477211686137825, -2.156400265872604471 ) ) ;
#12553=CARTESIAN_POINT ( 'NONE',  ( 4.582524934692378871, -1.771534430979417429, -0.4408631061849078714 ) ) ;
#12560=CARTESIAN_POINT ( 'NONE',  ( 1.856743374925871715, 0.3135980649527739250, -1.814175028193690808 ) ) ;
#12561=CARTESIAN_POINT ( 'NONE',  ( 4.570568844821727872, 0.7744313447282255014, 1.858482759491510095 ) ) ;
#12562=CARTESIAN_POINT ( 'NONE',  ( 0.4217922253725381321, 0.8825364984147118230, 2.122365683989856588 ) ) ;
#12563=CARTESIAN_POINT ( 'NONE',  ( 4.961744919065853132, -0.5270168765720646409, 1.889542207339139024 ) ) ;
#12570=CARTESIAN_POINT ( 'NONE',  ( 1.435225040761441972, -1.516673362169782990, -1.439332739067126443 ) ) ;
#12571=CARTESIAN_POINT ( 'NONE',  ( 0.4791068267422092797, 1.747065859276742072, -0.6691465683838908607 ) ) ;
#12573=CARTESIAN_POINT ( 'NONE',  ( -0.1106727585416227011, 0.2327126083698972114, -2.036986407471320426 ) ) ;
#12574=CARTESIAN_POINT ( 'NONE',  ( 0.4677839449492172674, -1.637930601595443125, -0.5889144675248291216 ) ) ;
#12578=CARTESIAN_POINT ( 'NONE',  ( 1.681838029686154146, -0.9247999101687879309, 1.455793735983588633 ) ) ;
#12579=CARTESIAN_POINT ( 'NONE',  ( 1.417800074541092137, -1.221294057239637576, -1.819523406426680090 ) ) ;
#12580=CARTESIAN_POINT ( 'NONE',  ( 3.651171877326536030, -1.804458330144659950, 1.270265763067345066 ) ) ;
#12582=CARTESIAN_POINT ( 'NONE',  ( 1.217902493145516463, 0.4257177869225349243, -2.128761017034991543 ) ) ;
#12584=CARTESIAN_POINT ( 'NONE',  ( 2.888026961012623239, -2.114693475102703779, 0.1087559668010943809 ) ) ;
#12585=CARTESIAN_POINT ( 'NONE',  ( 6.639320575229251453, 2.090987163941595561, 2.106969785032047238 ) ) ;
#12587=CARTESIAN_POINT ( 'NONE',  ( 3.615000845857639256, -0.1676676331447447266, 2.286275989141072440 ) ) ;
#12591=CARTESIAN_POINT ( 'NONE',  ( 5.971364366153397718, -1.903789954562478792, -1.144205655003695643 ) ) ;
#12593=ADVANCED_FACE ( 'NONE', ( #55545 ), #4940, .T. ) ;
#12600=CARTESIAN_POINT ( 'NONE',  ( 4.131482539099665452, 0.5404898895830790861, 1.942541833525657680 ) ) ;
#12602=CARTESIAN_POINT ( 'NONE',  ( 2.413000123442359701, -1.597275988187638607, 1.305004441579124208 ) ) ;
#12607=CARTESIAN_POINT ( 'NONE',  ( 5.507841377412062478, -0.9828142975771281264, -1.958786091674463714 ) ) ;
#12608=CARTESIAN_POINT ( 'NONE',  ( 2.373672848961404735, -0.3474683332905931232, -1.986100487175908258 ) ) ;
#12609=CARTESIAN_POINT ( 'NONE',  ( 2.366542893654680402, 0.08848056876738576160, -1.839231530397527736 ) ) ;
#12612=CARTESIAN_POINT ( 'NONE',  ( 5.245057492501287832, -1.564903486862476489, 0.9398553879134128319 ) ) ;
#12613=CARTESIAN_POINT ( 'NONE',  ( 6.258435431136967431, 1.928752767684217106, -0.5880170417187426946 ) ) ;
#12615=CARTESIAN_POINT ( 'NONE',  ( 5.875896723904014962, 1.342229061679913071, 1.821250878268846352 ) ) ;
#12617=CARTESIAN_POINT ( 'NONE',  ( 0.9441299549096024979, 0.8517545906277513845, -1.926334332536754346 ) ) ;
#12628=CARTESIAN_POINT ( 'NONE',  ( 1.336355901170083849, -1.182550835430173919, -1.760063440837428272 ) ) ;
#12629=CARTESIAN_POINT ( 'NONE',  ( 2.988771237642441569, -1.320003323290209751, 1.786578734224959497 ) ) ;
#12633=CARTESIAN_POINT ( 'NONE',  ( 3.807043925254738781, -1.605251362286563177, 1.127602784832412386 ) ) ;
#12641=CARTESIAN_POINT ( 'NONE',  ( 2.355864820516640812, -1.574449018071517825, -1.420800595792824028 ) ) ;
#12643=CARTESIAN_POINT ( 'NONE',  ( 4.663041391408608405, -1.929494027986548454, -0.9748474430888448561 ) ) ;
#12644=CARTESIAN_POINT ( 'NONE',  ( 2.348939331405873077, 0.4892633877765646400, -1.774999737812533063 ) ) ;
#12647=CARTESIAN_POINT ( 'NONE',  ( 5.208843366089195293, -0.2500283176610699210, 1.722145524253251514 ) ) ;
#12648=CARTESIAN_POINT ( 'NONE',  ( 6.727182134110186063, 1.310238205575515957, 1.828849833172506489 ) ) ;
#12651=CARTESIAN_POINT ( 'NONE',  ( 3.204151765443470357, -2.159293047372488950, 0.1044485798024074874 ) ) ;
#12652=CARTESIAN_POINT ( 'NONE',  ( 5.729842239849809893, -1.821464125411855761, -0.8645900286049985617 ) ) ;
#12654=CARTESIAN_POINT ( 'NONE',  ( 2.167066695894452888, -1.976221826324360498, -0.8764929760368763700 ) ) ;
#12655=CARTESIAN_POINT ( 'NONE',  ( 4.253168938266341570, -1.637241709590877781, -1.097755751903241483 ) ) ;
#12656=CARTESIAN_POINT ( 'NONE',  ( 4.774914120469089696, 1.810774457899359202, -0.7023516835302608952 ) ) ;
#12665=CARTESIAN_POINT ( 'NONE',  ( 0.8334014933106950185, 0.1641056870149599223, 2.200712145998296343 ) ) ;
#12667=CARTESIAN_POINT ( 'NONE',  ( 5.946142449018281262, -0.8852437533515828960, 1.750773106858094952 ) ) ;
#12670=CARTESIAN_POINT ( 'NONE',  ( 0.07499057489264347731, 1.360887136235461758, -2.209073988085366480 ) ) ;
#12671=CARTESIAN_POINT ( 'NONE',  ( 4.997927640213790212, -0.6233917918176261619, -1.732523409203725828 ) ) ;
#12676=CARTESIAN_POINT ( 'NONE',  ( 5.818629517237746462, -0.7649446623404360102, -1.977987144599784086 ) ) ;
#12679=CARTESIAN_POINT ( 'NONE',  ( 6.046181036401986120, 2.058226046012123334, 0.1054989004632029409 ) ) ;
#12681=CARTESIAN_POINT ( 'NONE',  ( 1.644728535064543529, -0.2685211301156094632, -1.841439677390522389 ) ) ;
#12682=CARTESIAN_POINT ( 'NONE',  ( 3.684953445348177148, 1.336164438771630714, 1.267087564277062484 ) ) ;
#12688=CARTESIAN_POINT ( 'NONE',  ( 3.651171877326536030, -1.804458330144659950, 1.270265763067345066 ) ) ;
#12689=CARTESIAN_POINT ( 'NONE',  ( 6.362609103649501385, -1.606607173180201187, 1.593162483179947575 ) ) ;
#12691=CARTESIAN_POINT ( 'NONE',  ( 5.308800944376626418, -0.4481363076810992996, -1.755139329022289196 ) ) ;
#12692=CARTESIAN_POINT ( 'NONE',  ( 6.456256392861089211, -1.172487466661990663, 1.515489988593403226 ) ) ;
#12694=CARTESIAN_POINT ( 'NONE',  ( 6.209813078548920728, -1.856259414618817383, 0.2309603555875269776 ) ) ;
#12696=CARTESIAN_POINT ( 'NONE',  ( 5.875818619555242428, 1.057306330162042451, 1.419162741687775231 ) ) ;
#12697=CARTESIAN_POINT ( 'NONE',  ( 1.516814941429758701, 0.2024661778830244008, 2.006371303556075958 ) ) ;
#12699=CARTESIAN_POINT ( 'NONE',  ( 2.842513320990670778, 2.090244732995512944, 0.2570852942500467808 ) ) ;
#12705=CARTESIAN_POINT ( 'NONE',  ( 2.601824576204377681, 1.431331034542600245, 1.425341822903106515 ) ) ;
#12709=CARTESIAN_POINT ( 'NONE',  ( 3.673254355229157664, 0.05708692194854488033, -2.161017345153878999 ) ) ;
#12715=CARTESIAN_POINT ( 'NONE',  ( 0.5202908490967810273, 2.147468835798187037, -0.3191156193892603632 ) ) ;
#12720=CARTESIAN_POINT ( 'NONE',  ( 2.595491417077447238, -0.6846416945752286098, 2.081959150545972914 ) ) ;
#12721=CARTESIAN_POINT ( 'NONE',  ( 6.883263157960367806, 2.959656548886806071, 2.506466465954690914 ) ) ;
#12722=CARTESIAN_POINT ( 'NONE',  ( 3.028476438156304962, 1.258033425225786983, -1.880328901638250505 ) ) ;
#12729=CARTESIAN_POINT ( 'NONE',  ( 4.340886628629798238, -1.540457278443696509, 0.8709714020649069743 ) ) ;
#12731=CARTESIAN_POINT ( 'NONE',  ( 0.3234443461216755522, -0.1028566021752069376, 2.103582624919388078 ) ) ;
#12734=CARTESIAN_POINT ( 'NONE',  ( 5.905875104417893873, -1.122515283938491537, -1.674877678029200068 ) ) ;
#12738=CARTESIAN_POINT ( 'NONE',  ( 3.643291952642300213, -1.415932857957047375, -1.222571138756740838 ) ) ;
#12739=CARTESIAN_POINT ( 'NONE',  ( 3.045825399726837635, 1.460771095745692527, 1.467265538693182991 ) ) ;
#12744=CARTESIAN_POINT ( 'NONE',  ( 6.209879897626497502, -2.145988306206991325, 0.2596296833028768347 ) ) ;
#12747=CARTESIAN_POINT ( 'NONE',  ( 2.857805160684105950, -0.6180756922911297968, 1.862011555624979886 ) ) ;
#12748=CARTESIAN_POINT ( 'NONE',  ( 0.8255457999647041190, -1.462224166115761337, 1.388270745661695837 ) ) ;
#12752=CARTESIAN_POINT ( 'NONE',  ( 0.8955150854165813135, -0.6789544621725839280, 1.743152336062703256 ) ) ;
#12754=CARTESIAN_POINT ( 'NONE',  ( 2.830340462983381489, -0.9960867002655849900, -1.749474899777081704 ) ) ;
#12756=CARTESIAN_POINT ( 'NONE',  ( 2.689187139871064502, 1.790190400678292715, 1.130151903539077463 ) ) ;
#12758=CARTESIAN_POINT ( 'NONE',  ( 4.281733463571851139, -1.982135700070002615, 0.5980053909793592304 ) ) ;
#12760=CARTESIAN_POINT ( 'NONE',  ( 0.3629773032866591143, 0.2007434131479734207, -2.081070348792604108 ) ) ;
#12762=CARTESIAN_POINT ( 'NONE',  ( 5.842758758449526191, 0.3585452818064547853, 1.789846783968067845 ) ) ;
#12763=ORIENTED_EDGE ( 'NONE', *, *, #151345, .T. ) ;
#12767=CARTESIAN_POINT ( 'NONE',  ( 6.756857042228312515, -1.710155547305733492, 1.394389531264042414 ) ) ;
#12769=CARTESIAN_POINT ( 'NONE',  ( 4.881465217424630687, 0.1836680969147831965, -1.903426456924644183 ) ) ;
#12780=CARTESIAN_POINT ( 'NONE',  ( 4.745289220334846902, -1.444806058459674691, -1.188008360142885245 ) ) ;
#12781=CARTESIAN_POINT ( 'NONE',  ( 0.07700591528354226722, 2.040803078245361224, -2.328119179575589559 ) ) ;
#12787=CARTESIAN_POINT ( 'NONE',  ( 1.586696308167453662, 1.896558138806573757, 0.5304675795299080843 ) ) ;
#12788=CARTESIAN_POINT ( 'NONE',  ( 3.901970389206737444, -1.039011544341267745, -1.727992587138134306 ) ) ;
#12792=CARTESIAN_POINT ( 'NONE',  ( 3.873126987144244193, 2.063651454400210028, -0.7377723227853100196 ) ) ;
#12794=CARTESIAN_POINT ( 'NONE',  ( 2.133698649363345190, -1.256510270340875035, -1.460289853754138445 ) ) ;
#12797=CARTESIAN_POINT ( 'NONE',  ( 0.1329588055935396196, 0.2493489391296536684, -1.880683181770840262 ) ) ;
#12804=CARTESIAN_POINT ( 'NONE',  ( 5.460457653299121361, -1.667157065227730106, -0.7818181906407914994 ) ) ;
#12805=CARTESIAN_POINT ( 'NONE',  ( 2.016272687986338852, -2.012595170092303043, 0.05167081324058443031 ) ) ;
#12806=CARTESIAN_POINT ( 'NONE',  ( 3.989890550291860016, 2.181093686755405603, 0.7249921343481547931 ) ) ;
#12807=CARTESIAN_POINT ( 'NONE',  ( -0.02880301295726198432, 6.946859453142047336, -2.868871865197111681 ) ) ;
#12808=CARTESIAN_POINT ( 'NONE',  ( 1.973285428892736171, -0.2338459910692871346, 1.846151439588203935 ) ) ;
#12811=CARTESIAN_POINT ( 'NONE',  ( 5.414289803398987466, -1.912571729023364364, 0.006307610287324683096 ) ) ;
#12814=CARTESIAN_POINT ( 'NONE',  ( 4.388279639374990104, -0.4598052185818923832, -2.039381826187444791 ) ) ;
#12815=CARTESIAN_POINT ( 'NONE',  ( 2.957714569337116295, 1.861795396119047208, -0.1817069356538636715 ) ) ;
#12819=CARTESIAN_POINT ( 'NONE',  ( 4.758271111750849158, 0.6642134669661412527, 1.592074403417756301 ) ) ;
#12823=CARTESIAN_POINT ( 'NONE',  ( 6.245327377194020535, 0.3399632236478037917, -1.987496870419297013 ) ) ;
#12825=CARTESIAN_POINT ( 'NONE',  ( 5.647405056649561494, 1.918175650701968937, -1.016889183816371611 ) ) ;
#12826=CARTESIAN_POINT ( 'NONE',  ( 4.494645072041675071, -0.4025399330690944133, -1.780595394402582077 ) ) ;
#12827=CARTESIAN_POINT ( 'NONE',  ( 1.199968502355329703, 0.8001272530510428194, -1.791371145023381350 ) ) ;
#12828=CARTESIAN_POINT ( 'NONE',  ( 6.298082486376491929, -1.000091913425070311, -1.866304853008766917 ) ) ;
#12833=CARTESIAN_POINT ( 'NONE',  ( 2.807414684038778141, 1.817529592918063708, -1.092056846721880969 ) ) ;
#12838=CARTESIAN_POINT ( 'NONE',  ( 1.059532578591013463, 1.690300726139557952, 1.195051122980017144 ) ) ;
#12841=CARTESIAN_POINT ( 'NONE',  ( 2.262617597476920039, 2.220861250988148683, 0.05131716197829398751 ) ) ;
#12843=CARTESIAN_POINT ( 'NONE',  ( 0.9327830709247152408, -1.816692068203207056, -1.408362870467388950 ) ) ;
#12845=CARTESIAN_POINT ( 'NONE',  ( 5.752800572348735209, -0.4956410525326099270, -2.002042340502646844 ) ) ;
#12849=CARTESIAN_POINT ( 'NONE',  ( 0.2329586101569866563, 2.046406029004425253, -2.262590835625963415 ) ) ;
#12850=CARTESIAN_POINT ( 'NONE',  ( 5.688959394570705541, 1.398425918548395153, 1.197878823674280779 ) ) ;
#12853=CARTESIAN_POINT ( 'NONE',  ( 3.012419478190906830, 1.250452035320260835, -1.188195685136491875 ) ) ;
#12854=CARTESIAN_POINT ( 'NONE',  ( 0.7257964430846426396, 0.8128130212789463904, -1.845628942776005088 ) ) ;
#12855=CARTESIAN_POINT ( 'NONE',  ( 1.635759689059889554, 0.7259864748365916221, 2.181091778573934103 ) ) ;
#12857=CARTESIAN_POINT ( 'NONE',  ( 2.337552072221838362, -2.021662389422747452, 1.015643474128526291 ) ) ;
#12858=CARTESIAN_POINT ( 'NONE',  ( 4.688165273298999125, -0.9932770932522380081, 1.857119049063939320 ) ) ;
#12860=CARTESIAN_POINT ( 'NONE',  ( 3.655294433216628391, 0.4326292253380575881, -1.715882644387234590 ) ) ;
#12864=CARTESIAN_POINT ( 'NONE',  ( 0.2172540613933468812, -0.1060665143617581102, 2.289936275665432674 ) ) ;
#12865=CARTESIAN_POINT ( 'NONE',  ( 4.980324010294663317, -0.2286266671043569454, -1.826820671449409295 ) ) ;
#12869=CARTESIAN_POINT ( 'NONE',  ( 4.980524279605372584, -0.2661484459187679064, -2.175167798947100994 ) ) ;
#12874=CARTESIAN_POINT ( 'NONE',  ( 2.930207584894477080, 1.069882305642521514, -1.601919868193351082 ) ) ;
#12877=CARTESIAN_POINT ( 'NONE',  ( 0.07096481000732741962, 0.8580841460674984988, 2.049194762706497031 ) ) ;
#12886=CARTESIAN_POINT ( 'NONE',  ( 2.348798421458723862, 0.4629176777091792983, -1.677682632058958845 ) ) ;
#12888=CARTESIAN_POINT ( 'NONE',  ( 0.4847190467827041105, 1.876267867961832980, 0.5731238010058883336 ) ) ;
#12893=CARTESIAN_POINT ( 'NONE',  ( 5.383715653711652394, 1.448795075966866852, 1.604530791579752202 ) ) ;
#12894=CARTESIAN_POINT ( 'NONE',  ( -0.2104748580754201015, 5.720428293583295520, -2.697747842008205943 ) ) ;
#12895=VERTEX_POINT ( 'NONE', #46781 ) ;
#12897=CARTESIAN_POINT ( 'NONE',  ( 0.6845637836509765872, -0.2226890396202323152, -1.857165095135074218 ) ) ;
#12898=CARTESIAN_POINT ( 'NONE',  ( 6.345060247669167097, -0.9239052495037097801, 1.466952517609141138 ) ) ;
#12900=CARTESIAN_POINT ( 'NONE',  ( 3.280998142716429200, 1.980384277226649559, -0.9389412094223739125 ) ) ;
#12901=CARTESIAN_POINT ( 'NONE',  ( 2.784532256742262568, -1.187036312555936890, 1.978742884264461654 ) ) ;
#12902=CARTESIAN_POINT ( 'NONE',  ( 5.624313186929686736, 1.231095119260311677, -1.652465237140358090 ) ) ;
#12903=CARTESIAN_POINT ( 'NONE',  ( 1.728360517318433542, 0.1903740514868361433, 1.932600189055997619 ) ) ;
#12908=CARTESIAN_POINT ( 'NONE',  ( 3.814780496183818315, -0.6684712460508880350, -2.012520831323429515 ) ) ;
#12910=CARTESIAN_POINT ( 'NONE',  ( 2.496720397819631732, -1.994071314890283553, 0.2986276487200872354 ) ) ;
#12912=CARTESIAN_POINT ( 'NONE',  ( 5.702238492974306183, -2.206952906645575307, -0.005361432510411765114 ) ) ;
#12921=CARTESIAN_POINT ( 'NONE',  ( 4.153237585930975584, -1.712380083513395768, -1.146421031332397922 ) ) ;
#12925=CARTESIAN_POINT ( 'NONE',  ( 3.580727245018202165, -1.354872245433702105, 1.497987768207516668 ) ) ;
#12930=CARTESIAN_POINT ( 'NONE',  ( 3.291920626085430346, -0.8366078139741841557, 1.883634853023412825 ) ) ;
#12931=CARTESIAN_POINT ( 'NONE',  ( 2.602185585689294367, -0.1948409242511044692, 2.006959980107574371 ) ) ;
#12939=CARTESIAN_POINT ( 'NONE',  ( 2.600935288962639369, 0.9528664403582010056, -1.776738882381201812 ) ) ;
#12940=CARTESIAN_POINT ( 'NONE',  ( 2.255570300226293234, 0.7868700230135963203, 1.664660379391752043 ) ) ;
#12941=CARTESIAN_POINT ( 'NONE',  ( 6.340462157465731607, 2.182225300935904055, 0.3281612982340698093 ) ) ;
#12943=CARTESIAN_POINT ( 'NONE',  ( 2.407699484934812784, -0.4761397456576694776, 2.108333575599189214 ) ) ;
#12945=CARTESIAN_POINT ( 'NONE',  ( 4.751218706475199838, 0.2043725092088227169, -2.107420708596031922 ) ) ;
#12947=CARTESIAN_POINT ( 'NONE',  ( 2.548584303619909175, 2.101849941811538169, -0.9302779420137051725 ) ) ;
#12950=CARTESIAN_POINT ( 'NONE',  ( 1.024039198018782626, 1.117340804906666873, -1.500143343703803422 ) ) ;
#12951=CARTESIAN_POINT ( 'NONE',  ( 5.401234739183408351, 1.611344100708357097, 1.135629011227519358 ) ) ;
#12955=CARTESIAN_POINT ( 'NONE',  ( 0.03028722099337673168, -1.361824662662258767, -1.737358624739212543 ) ) ;
#12957=CARTESIAN_POINT ( 'NONE',  ( 6.285608408418759119, -1.950803066209889636, 0.6937918898708083093 ) ) ;
#12961=CARTESIAN_POINT ( 'NONE',  ( 6.639320575229258559, 7.052241914652472410, 2.701414248926166994 ) ) ;
#12962=CARTESIAN_POINT ( 'NONE',  ( 5.032083864297879572, 1.014306426666331529, -1.690397665970795105 ) ) ;
#12963=CARTESIAN_POINT ( 'NONE',  ( 6.533471379370169529, -0.1492333671020330821, 1.986230151431379598 ) ) ;
#12965=CARTESIAN_POINT ( 'NONE',  ( 4.160959874251066282, -1.711463231979272859, 1.548185629304731581 ) ) ;
#12967=CARTESIAN_POINT ( 'NONE',  ( 1.973554268250839350, -0.2567932339846226708, 2.046489673661837205 ) ) ;
#12974=CARTESIAN_POINT ( 'NONE',  ( 4.211506895594858690, -1.802957179857124448, -1.209418758558492568 ) ) ;
#12977=CARTESIAN_POINT ( 'NONE',  ( 4.265079090171526310, 1.784866007061826298, -0.4516350764028759235 ) ) ;
#12979=CARTESIAN_POINT ( 'NONE',  ( 6.720655732516647163, 3.705577233864749687, 2.340827588962008488 ) ) ;
#12980=CARTESIAN_POINT ( 'NONE',  ( 5.548420995840112724, -1.728225626343689925, 1.347513067664840358 ) ) ;
#12982=CARTESIAN_POINT ( 'NONE',  ( 6.227429363453246935, -2.132905367568146637, 0.7551758973065140212 ) ) ;
#12988=CARTESIAN_POINT ( 'NONE',  ( 0.8656337812406755816, 0.8672032905003168590, 1.542741919674812223 ) ) ;
#12989=CARTESIAN_POINT ( 'NONE',  ( 5.127594652646677353, -0.2932247039480195827, 1.991498814599843792 ) ) ;
#12991=CARTESIAN_POINT ( 'NONE',  ( 4.577239374156605756, 0.002566705667105330900, -2.106147099847696325 ) ) ;
#12992=CARTESIAN_POINT ( 'NONE',  ( 2.319824818950954270, 0.9007672528749611773, -1.690582045118453225 ) ) ;
#12994=CARTESIAN_POINT ( 'NONE',  ( 2.682036910502568539, -1.131707915740775672, -1.611748346588251168 ) ) ;
#12995=CARTESIAN_POINT ( 'NONE',  ( 5.256120111591911837, 0.8147005317804748570, -1.848364005614275163 ) ) ;
#12996=CARTESIAN_POINT ( 'NONE',  ( 1.410794581852807150, 1.648159533202856686, 0.8848386531258023435 ) ) ;
#12997=CARTESIAN_POINT ( 'NONE',  ( 4.898908426394765314, 1.431408964483871227, -0.9620984105884394788 ) ) ;
#12998=CARTESIAN_POINT ( 'NONE',  ( 0.9492982845318720386, -1.727743609841876360, 0.8201845251225792222 ) ) ;
#13000=CARTESIAN_POINT ( 'NONE',  ( 1.383733252933561086, 2.037972573443189717, -0.8472329510355591786 ) ) ;
#13007=CARTESIAN_POINT ( 'NONE',  ( 6.121949425127414024, 2.040613181561203859, -0.3481179853092666865 ) ) ;
#13008=CARTESIAN_POINT ( 'NONE',  ( 1.012269475826784060, 2.068064858651061932, -0.09981174449213289779 ) ) ;
#13013=CARTESIAN_POINT ( 'NONE',  ( 4.951869195850400196, -1.499954228463634465, -1.499123153458590929 ) ) ;
#13019=CARTESIAN_POINT ( 'NONE',  ( 4.376327261493318410, -0.3474131038204917310, 1.985796694155849362 ) ) ;
#13020=CARTESIAN_POINT ( 'NONE',  ( 3.503066848181853654, -0.1354201214893405170, 1.910964455010273344 ) ) ;
#13022=CARTESIAN_POINT ( 'NONE',  ( 2.999763140970079345, -2.188934734890151113, 0.1099877568606702771 ) ) ;
#13023=CARTESIAN_POINT ( 'NONE',  ( -0.1399997263889594112, -0.002789056014654289761, -2.000146600338557956 ) ) ;
#13025=CARTESIAN_POINT ( 'NONE',  ( 4.851819109577236055, -1.426696570994885116, -1.420647396805594820 ) ) ;
#13028=CARTESIAN_POINT ( 'NONE',  ( 5.378551862015316765, -0.5151900214499178787, -2.053461258077380336 ) ) ;
#13030=CARTESIAN_POINT ( 'NONE',  ( 3.034800296023100419, -1.842769725714489493, 0.9876625208589999705 ) ) ;
#13032=CARTESIAN_POINT ( 'NONE',  ( 2.168594647197068070, -1.575507694510763335, -0.7022964154167319339 ) ) ;
#13034=CARTESIAN_POINT ( 'NONE',  ( 5.484674493353773883, -1.343714522216314489, 1.640574901390474460 ) ) ;
#13043=CARTESIAN_POINT ( 'NONE',  ( 1.435880962511564718, -1.006192904286895340, -1.506089461148002018 ) ) ;
#13049=CARTESIAN_POINT ( 'NONE',  ( 2.736723853829028830, 1.706320744115387811, 0.6085963735071827641 ) ) ;
#13053=CARTESIAN_POINT ( 'NONE',  ( 3.683913666659529795, -1.106983821303194171, -1.495880402381715824 ) ) ;
#13054=CARTESIAN_POINT ( 'NONE',  ( 1.440887319015681012, -1.643870157486097217, -0.9831960898977005758 ) ) ;
#13055=CARTESIAN_POINT ( 'NONE',  ( 6.821331454403446237, -0.1310627394537598467, 1.896496729248610125 ) ) ;
#13063=CARTESIAN_POINT ( 'NONE',  ( 5.770349169015823954, -0.8820018971720828826, -1.760941755123719421 ) ) ;
#13066=CARTESIAN_POINT ( 'NONE',  ( 6.667925998804712151, -1.351855065013835455, 1.725503752137508284 ) ) ;
#13068=CARTESIAN_POINT ( 'NONE',  ( 5.649420354817641154, -1.518837414639911065, -1.184835060848010713 ) ) ;
#13070=CARTESIAN_POINT ( 'NONE',  ( 1.184280053745472738, -1.780106929851841491, -0.4042017716930704219 ) ) ;
#13071=CARTESIAN_POINT ( 'NONE',  ( 2.157103830005083100, -1.704838622333640030, 1.401371054633032909 ) ) ;
#13073=CARTESIAN_POINT ( 'NONE',  ( -0.01753026575586694516, -1.247696154478775021, 1.449428981083925150 ) ) ;
#13076=CARTESIAN_POINT ( 'NONE',  ( 0.5726248362980547180, 1.360856580973464069, -1.424029402571887148 ) ) ;
#13077=CARTESIAN_POINT ( 'NONE',  ( 1.171315778946733888, 1.157996810922466313, 1.558895349155087873 ) ) ;
#13079=CARTESIAN_POINT ( 'NONE',  ( 0.2982036909132765867, -1.844429998007334648, 0.8144978490535054183 ) ) ;
#13081=CARTESIAN_POINT ( 'NONE',  ( 5.348444835920818541, -1.846650980718677726, -0.2298375257220597323 ) ) ;
#13087=CARTESIAN_POINT ( 'NONE',  ( 1.734175692058033347, 2.168326105380265378, 0.3173973903456903112 ) ) ;
#13092=CARTESIAN_POINT ( 'NONE',  ( 1.875362892791394787, 1.747422460009705913, -0.5287960245906262458 ) ) ;
#13097=CARTESIAN_POINT ( 'NONE',  ( 6.509000000000034980, 7.629137130509102249, 2.699999999999993516 ) ) ;
#13099=CARTESIAN_POINT ( 'NONE',  ( 1.348133503156129454, 1.924256495421622359, 0.09534579948072999245 ) ) ;
#13100=CARTESIAN_POINT ( 'NONE',  ( 5.946142449018281262, -0.8852437533515828960, 1.750773106858094952 ) ) ;
#13105=CARTESIAN_POINT ( 'NONE',  ( 5.319949580897746166, 1.306013235697962571, -1.759773446019400778 ) ) ;
#13107=B_SPLINE_CURVE_WITH_KNOTS ( 'NONE', 3,
 ( #139886, #205916, #136679, #57550, #202704, #123708, #117968, #115830, #133124, #149338 ),
 .UNSPECIFIED., .F., .F.,
 ( 4, 1, 1, 1, 1, 1, 1, 4 ),
 ( 0.000000000000000000, 0.09487947018404768729, 0.1878442364269655440, 0.2584026419818104547, 0.3617053504666527530, 0.5211417612611924932, 0.7337075935910832847, 1.000000000000000000 ),
 .UNSPECIFIED. ) ;
#13109=CARTESIAN_POINT ( 'NONE',  ( 3.854399998794607818, -2.067664388167046674, -0.1065051105964970740 ) ) ;
#13113=CARTESIAN_POINT ( 'NONE',  ( 4.201969167805962968, 2.101520711257957252, 0.9317802909727909144 ) ) ;
#13119=CARTESIAN_POINT ( 'NONE',  ( 3.661996979482002867, -1.303408580024501218, 1.439711300692345652 ) ) ;
#13124=CARTESIAN_POINT ( 'NONE',  ( 4.957238921819991262, -1.637161358497842389, 0.9882132959125531357 ) ) ;
#13126=CARTESIAN_POINT ( 'NONE',  ( 6.563511714949607168, 0.2886701521849396879, -1.700279369998755508 ) ) ;
#13127=CARTESIAN_POINT ( 'NONE',  ( 5.014861385384292269, 0.1531656238677771009, 2.010801456750747285 ) ) ;
#13129=CARTESIAN_POINT ( 'NONE',  ( 2.227434312139275896, 0.001603268854937638837, 2.207063162490217056 ) ) ;
#13132=CARTESIAN_POINT ( 'NONE',  ( 2.203177794981598492, -0.4570653145323905764, 2.039892330567660839 ) ) ;
#13133=CARTESIAN_POINT ( 'NONE',  ( 0.2327837997007513038, -1.621012357304358220, 0.7108589729635225174 ) ) ;
#13134=CARTESIAN_POINT ( 'NONE',  ( 6.082657761774013849, -0.6767167302549759178, 1.899617564980569995 ) ) ;
#13136=CARTESIAN_POINT ( 'NONE',  ( 3.556809736639905406, -2.021263576298555797, -1.081171400725000398 ) ) ;
#13137=CARTESIAN_POINT ( 'NONE',  ( 0.7611566575390321665, 0.8540426286860869354, 1.516288903859766890 ) ) ;
#13140=CARTESIAN_POINT ( 'NONE',  ( 0.9481301099739076754, 1.159027798429014045, 1.289721149823976676 ) ) ;
#13143=( BOUNDED_SURFACE ( )  B_SPLINE_SURFACE ( 3, 3, ( 
 ( #28499, #94590, #160632, #66020, #12233, #45839, #42643, #33555, #111959, #98567, #16213, #148390, #132169, #17282, #198175, #83358, #207239, #174776, #168884, #70293, #19423, #4223, #152638, #37823, #85502, #119136, #136409, #22615, #53001, #184061, #121290, #150526, #50877, #202425, #67090, #151589, #186190, #117000, #201360, #87645, #137477, #1025, #20488, #54080, #203491, #200300, #134293, #38892, #120216, #2087, #103901, #149443, #100686, #34616, #153715, #169947, #133225, #5283, #3156, #21535, #199230, #71361, #55144, #187266, #166764, #104978, #185118, #18359, #182999, #84437, #35679, #171018, #36743, #86574, #68161, #69228, #102829, #51952, #118074, #135346, #101757, #167824, #191516, #110356, #89802, #59399, #157992, #26890, #10631, #208830, #43181, #142823, #126617, #76706, #58339, #174250, #189401, #25822, #106076, #88724, #156923, #173177, #155846, #92994, #7433, #140697, #73514, #125555, #154782, #9581, #175303, #109294, #123439, #206711, #8512, #159038, #44235, #192580, #139616, #204560, #172099, #122372, #124495, #205639, #60460, #190454, #176360, #42113, #6366, #207772, #41043, #188329, #72435, #138536, #56208, #57278, #39969, #107152, #23692, #24757, #90859, #74593, #108225, #91932, #75657, #141764, #27967, #163303, #131903, #12758, #113552, #62586, #161172, #177422, #146010, #48495, #127696, #46361, #114614, #197911, #143898, #14884, #95123, #148127, #80979, #78832, #144953, #194722, #210959, #111418, #61530, #213089, #147068, #128749, #94061, #160101, #195800, #196857, #162241, #11704, #96190, #112481, #178490, #180605, #64719, #193656, #214127, #82033, #30100, #15950, #65756, #29040, #130861, #212021, #32230, #77778, #13827, #45299, #179555, #79901, #63664, #47437, #129818, #209892, #31176, #97249, #98301, #164366, #49539, #115665, #181659, #71100, #33286, #200041, #51692, #117814, #68965, #37559, #3960, #36485, #85236, #54883, #83094, #183804, #2892, #35414, #135084, #152382, #101492, #52738, #84172, #99370, #150261, #167562, #201097, #165422, #21280, #19162, #87385, #18084, #70028, #136143, #103639, #151324, #50605, #118872, #184858, #153453, #102562, #182730, #17018, #116731, #149173, #132959, #137218, #34349, #168622, #20224, #5026, #86310, #202161, #53819, #119949, #185924, #169691, #203239, #750, #66816, #198962, #100422, #166493, #1829, #67888, #134033, #155589, #92743, #122104, #22350, #124243, #38635, #57020, #157735, #88462, #172918, #59144, #109036, #187004, #206454, #107971, #175055, #171833, #105808, #10384, #190202, #188069, #41861, #121037, #72172, #6102, #125302, #91682, #104713, #191261, #123188, #9332, #170761, #173999, #25571, #75404, #138280, #141517, #24493, #204295, #154523, #55951, #7173, #42926, #90604, #58081, #140443, #189149, #8256, #207525, #39698, #40786, #208575, #23426, #26642, #142568, #89537, #158787, #76460, #73244, #139351, #205381, #106891, #156664, #74339, #48257, #29862, #145778, #160925, #211781, #77527, #60208, #128511, #144712, #61284, #64484, #193416, #112239, #45060, #30936, #126369, #129571, #146828, #97012, #94872, #178249, #194479, #14646, #15709, #164126, #111171, #176116, #143648, #93810, #95945, #177172, #80740, #162000, #130626, #13589, #192328, #62350, #46122, #196618, #11454, #79663, #110105, #98071, #63419, #195558, #47194, #163065, #27716, #113309 ),
 ( #28789, #12519, #81795, #179315, #127445, #212847, #43987, #209643, #159851, #114371, #180366, #78592, #31990, #147878, #210724, #197665, #134835, #2640, #200838, #165174, #52489, #117554, #99124, #65517, #33047, #100174, #3701, #183548, #84985, #18901, #1573, #101232, #184606, #132711, #67634, #87120, #131662, #102302, #21024, #501, #36223, #68713, #152133, #135885, #119689, #168375, #53556, #37303, #201904, #35155, #151076, #166239, #118619, #16768, #213894, #133781, #83912, #66569, #69777, #198716, #51434, #50362, #19972, #49309, #86056, #185674, #103377, #34103, #167314, #199789, #169439, #115426, #181417, #116485, #82852, #148928, #182474, #17829, #150003, #107714, #188885, #157480, #40526, #153191, #155328, #6912, #9075, #104453, #72989, #202982, #191006, #122927, #139092, #205119, #41603, #106630, #42673, #140174, #89280, #172659, #25318, #24234, #74083, #23164, #7992, #156405, #173741, #56762, #90336, #206196, #26383, #57824, #187813, #125051, #154268, #123986, #189953, #4763, #54623, #91419, #75149, #141259, #207267, #58898, #108781, #174807, #55686, #70840, #121842, #136956, #120770, #186750, #38372, #170500, #22083, #204037, #88194, #5842, #71913, #171567, #138022, #39439, #105533, #64235, #29605, #93551, #76206, #175865, #208326, #43738, #196369, #159595, #95691, #211527, #127189, #126112, #30678, #195304, #59957, #11193, #63162, #61028, #130379, #158534, #143386, #78338, #94623, #160666, #113053, #14389, #92495, #13337, #48009, #77274, #177992, #193156, #209384, #27453, #210465, #179059, #192072, #110910, #96761, #114126, #109851, #79412, #44806, #212597, #145529, #176916, #28531, #12261, #144461, #62103, #128262, #129328, #46935, #194224, #10131, #142316, #45868, #162812, #111990, #161746, #80480, #146580, #180118, #118373, #84741, #131416, #3463, #85810, #132471, #19731, #151889, #115178, #150829, #149754, #184361, #81543, #66326, #197416, #183301, #99933, #1331, #51182, #16518, #147626, #82601, #65270, #165995, #168129, #213644, #100980, #31743, #135640, #97817, #50118, #116238, #182228, #133533, #102064, #68470, #181173, #49058, #32798, #201661, #98872, #34908, #2391, #198473, #164925, #35983, #134597, #148686, #255, #200598, #33852, #69533, #163881, #17580, #83663, #67392, #199540, #52245, #53310, #15456, #167069, #119442, #117305, #18661, #5584, #104204, #120522, #89030, #205951, #70593, #203796, #57583, #141008, #86877, #172404, #38132, #91169, #23992, #170251, #87944, #137778, #21836, #54384, #4520, #156160, #90095, #71664, #185429, #103132, #138845, #139924, #105283, #169190, #39192, #154018, #55442, #123741, #7741, #136708, #157228, #25067, #121594, #173491, #8823, #186501, #73828, #155085, #189702, #20782, #187566, #202733, #122677, #171319, #6671, #204862, #22914, #152944, #72748, #56517, #188640, #107465, #40270, #106381, #37048, #74899, #41355, #207016, #58647, #209137, #12016, #195043, #161496, #193966, #28277, #212338, #26135, #126935, #160411, #60776, #78089, #95447, #192893, #210210, #27200, #124801, #93307, #44549, #144214, #108529, #178810, #176665, #30425, #175613, #13076, #79156, #46680, #143143, #208079, #110664, #94371, #96510, #61846, #125866, #174559, #128013, #45614, #111730, #177737, #145272, #43488, #29352, #190760, #42424, #211279, #146323, #191825, #62902, #129072, #112798, #162560 ),
 ( #92247, #14132, #80224, #158295, #9886, #75962, #142065, #59706, #159342, #109607, #10939, #77014, #99672, #47759, #118119, #115983, #184104, #114920, #100731, #18404, #200344, #82345, #147374, #148436, #132211, #35724, #1074, #65022, #113873, #213400, #179868, #15206, #167869, #131177, #67139, #183046, #98615, #97568, #2132, #166810, #31493, #197167, #34661, #32540, #101800, #130132, #180919, #49856, #66069, #198220, #84480, #51993, #63978, #199281, #19467, #48803, #149491, #164676, #16260, #4, #181971, #150570, #163625, #33601, #68207, #85543, #81297, #50923, #165741, #151634, #117049, #17328, #83409, #133273, #134339, #196120, #36786, #191299, #59178, #103945, #3200, #135383, #171058, #175091, #137515, #136451, #42967, #201404, #141551, #9368, #207558, #168929, #125336, #121332, #102870, #69269, #20532, #169988, #10422, #187308, #91718, #22654, #5323, #105018, #109075, #202468, #71403, #93849, #53043, #26679, #27754, #4264, #92781, #75439, #158826, #142605, #126404, #76494, #60247, #44023, #208614, #38935, #157768, #21574, #192364, #86614, #119176, #203532, #87680, #70334, #110141, #54121, #55186, #120257, #176154, #185162, #152682, #186233, #37867, #153753, #211818, #79698, #114405, #115463, #49344, #144750, #61324, #177211, #193455, #63455, #210762, #180404, #195594, #164160, #47229, #159887, #162034, #13625, #15745, #111208, #145811, #209680, #197702, #129609, #113346, #179351, #48293, #30973, #181454, #146866, #95982, #97048, #32023, #163101, #80778, #29896, #14681, #212887, #98108, #64518, #130664, #196653, #33084, #81830, #194512, #131696, #160961, #127484, #147913, #77566, #213929, #65551, #45099, #11494, #143688, #28824, #94912, #12551, #78626, #62382, #128546, #46160, #112273, #178288, #100207, #102338, #99159, #50398, #198751, #103412, #200878, #183583, #152167, #17865, #69811, #82887, #20007, #168410, #86091, #116518, #3736, #2677, #182508, #165212, #132748, #199827, #169473, #68749, #34138, #35191, #167350, #70876, #36259, #166274, #148963, #83948, #535, #150039, #203016, #1610, #135917, #201936, #133813, #67669, #37339, #53592, #66602, #51468, #119726, #117592, #136989, #16802, #101266, #85022, #18937, #151111, #185705, #21058, #134871, #87155, #54658, #52523, #184641, #118656, #153226, #4796, #120806, #186783, #138057, #56794, #125087, #208363, #154300, #25353, #105572, #158571, #91453, #171604, #155360, #205151, #23198, #121876, #71947, #9109, #157514, #139124, #38409, #170534, #206232, #5874, #191045, #75185, #42710, #6945, #122963, #108818, #141297, #204070, #10170, #92531, #188922, #26419, #76244, #187847, #207306, #156443, #174842, #88231, #73026, #55722, #189987, #106667, #8027, #57859, #89313, #39473, #40560, #172691, #24269, #142353, #90374, #107752, #104491, #59994, #22119, #74117, #140213, #124021, #41638, #126147, #58929, #173778, #95729, #65301, #93591, #194260, #13372, #128298, #145563, #162846, #45906, #63196, #94658, #192110, #160701, #112024, #79446, #175900, #31779, #29644, #97851, #28570, #14424, #146611, #114160, #210503, #129360, #78375, #195338, #209420, #43774, #178026, #62138, #193193, #196402, #110947, #161781, #176954, #80514, #109887, #46970, #64270, #212629, #12295, #211561, #113086, #130415, #147661, #81578, #144495, #159635, #61065, #11232, #179092, #30714, #48047, #96797 ),
 ( #180153, #163914, #15490, #213678, #27491, #77311, #143424, #127224, #44841, #150861, #52280, #1361, #200632, #134628, #19760, #67423, #101014, #118407, #4553, #34942, #166028, #103161, #132505, #32830, #184393, #49092, #133566, #168162, #98907, #183337, #69562, #119474, #197451, #2423, #36013, #185462, #182261, #116272, #20814, #102092, #198503, #85842, #131450, #82634, #16551, #135672, #18692, #199572, #151919, #50148, #3492, #115212, #201697, #53340, #37082, #148718, #169222, #167105, #288, #181202, #164959, #17613, #86910, #84774, #68500, #152978, #51216, #66359, #33886, #99964, #117340, #83699, #149787, #173522, #92279, #71699, #41385, #139954, #8849, #207047, #190791, #25096, #124825, #108559, #58677, #40306, #174587, #73860, #137811, #205979, #70627, #21870, #170282, #74929, #172436, #155120, #123772, #203830, #107496, #54414, #57614, #189733, #91197, #87976, #157257, #188673, #154050, #136738, #104236, #171354, #141039, #106414, #156193, #90126, #72779, #24024, #42453, #55475, #138878, #158324, #202764, #26163, #120555, #121629, #186534, #38163, #5617, #187598, #39225, #105316, #22948, #89062, #6702, #7769, #204896, #56549, #122710, #27229, #9917, #78115, #94401, #10971, #14160, #143173, #61874, #209166, #195072, #75991, #79186, #96538, #46712, #44579, #128039, #144245, #178841, #179896, #113901, #60804, #125896, #93336, #43516, #193994, #126965, #30453, #45643, #80254, #111760, #142096, #12045, #210237, #146353, #175643, #177766, #59738, #47788, #29381, #95476, #161524, #112825, #13109, #31519, #211307, #160440, #145301, #162585, #62932, #129100, #212365, #64007, #130156, #196147, #97593, #208108, #191855, #109639, #159372, #110693, #77044, #192923, #176692, #28305, #81322, #99703, #200375, #65048, #1107, #101831, #151663, #15234, #34689, #150600, #3235, #34, #148465, #2161, #114946, #68237, #67168, #48832, #147400, #197193, #49887, #167900, #133303, #100759, #183077, #165774, #50954, #134371, #82375, #17357, #36818, #213426, #52023, #185193, #164702, #118149, #18436, #19498, #85574, #69300, #184133, #135413, #201434, #53075, #199308, #166840, #116012, #84512, #180946, #163652, #83441, #33630, #16290, #119209, #66098, #117078, #132240, #35757, #131205, #32568, #98645, #198248, #181998, #149521, #22685, #57351, #58418, #206786, #87715, #4295, #120292, #136480, #154857, #153786, #123514, #138612, #107233, #204636, #102899, #105055, #171091, #173254, #54153, #88797, #152713, #140771, #72516, #6439, #56286, #205715, #122446, #124571, #89872, #38969, #188404, #189479, #40042, #23767, #187341, #172177, #106151, #41121, #155924, #7509, #73591, #190532, #139693, #137550, #74668, #103977, #70366, #24835, #20562, #90934, #157000, #202503, #8587, #168958, #86645, #186265, #37900, #170020, #21607, #5356, #71438, #203568, #55220, #121365, #45381, #42188, #207849, #141844, #46440, #143978, #126697, #95201, #175380, #12838, #25898, #177503, #111497, #160180, #76783, #13905, #43254, #158067, #29116, #174323, #192658, #78912, #9655, #94142, #194804, #30179, #108303, #127780, #161251, #96270, #93071, #26965, #146090, #145034, #109373, #211037, #92009, #59475, #125632, #112559, #209969, #44312, #62663, #159113, #128822, #75731, #178572, #162320, #79986, #191593, #212101, #11781, #10714, #142905, #208905, #60538, #63738, #77854 ),
 ( #110434, #129896, #176436, #28048, #61610, #193735, #199044, #84257, #67970, #18170, #49622, #99449, #98380, #165506, #81060, #195881, #214209, #82114, #130946, #166581, #48577, #197996, #114693, #133043, #47519, #837, #100506, #50691, #164443, #115747, #131987, #182817, #51776, #200123, #180687, #163389, #213171, #147145, #181737, #32312, #34433, #33368, #150342, #17098, #113632, #83176, #149259, #1911, #64800, #66903, #14963, #179637, #116815, #134114, #31257, #97331, #196937, #16030, #148207, #65838, #128480, #47163, #194448, #95916, #45026, #29832, #178217, #63389, #111139, #144681, #161970, #48231, #77496, #94841, #210692, #158758, #14614, #12488, #80711, #11420, #211751, #129543, #96983, #193382, #43956, #177140, #28757, #146801, #112209, #176084, #10353, #110072, #76429, #126337, #64455, #27682, #13560, #79632, #209609, #208544, #113278, #195525, #142538, #93780, #145750, #143615, #212818, #26611, #61252, #160892, #78561, #62321, #179284, #163033, #175024, #30909, #130599, #159817, #46092, #127410, #196588, #92712, #60179, #192297, #79568, #181327, #198624, #212755, #182378, #17730, #95850, #115336, #16676, #83819, #80645, #14548, #133688, #32955, #30841, #99029, #29765, #195464, #129482, #34008, #131571, #114280, #82761, #162969, #405, #13493, #165085, #148834, #66478, #47093, #132617, #147783, #113211, #161906, #63321, #130534, #100083, #213799, #50271, #49216, #31901, #197572, #116389, #146737, #97978, #117463, #145687, #166144, #51338, #96918, #149912, #1479, #67545, #199693, #211685, #179216, #64389, #196525, #48168, #65422, #180277, #164037, #15612, #81700, #183456, #37211, #53461, #184512, #187721, #102215, #20932, #168281, #154174, #35062, #38282, #55598, #71819, #205027, #36132, #5741, #104359, #121753, #105445, #89188, #137929, #23072, #6821, #171481, #153100, #54533, #69688, #120678, #200752, #101133, #103285, #119598, #19881, #39349, #85965, #87028, #152040, #203950, #167221, #170404, #155239, #72900, #3610, #4675, #169347, #139005, #56673, #18807, #135792, #84893, #52401, #2545, #70749, #201816, #150980, #136861, #68620, #202885, #134743, #185581, #186656, #118528, #21993, #88103, #172562, #160568, #92403, #124956, #42582, #11100, #158442, #12176, #109760, #58801, #76117, #209289, #142222, #43646, #207177, #191979, #126019, #77176, #190918, #10043, #175769, #210371, #26289, #157388, #94530, #123895, #24145, #27362, #40434, #90248, #59867, #143298, #91328, #60936, #110817, #188798, #208235, #93463, #176822, #173651, #107620, #78248, #159502, #189863, #127093, #122837, #73986, #7898, #193056, #44710, #108686, #28437, #41506, #144371, #106536, #156314, #140081, #206104, #57737, #25225, #8980, #75054, #141168, #174715, #162719, #66227, #180027, #147532, #81455, #64142, #163783, #32697, #195208, #130286, #149654, #128167, #31648, #96667, #33759, #63068, #177899, #65176, #194129, #111895, #213553, #16424, #30585, #160, #50017, #45778, #131331, #48965, #116141, #112959, #46845, #165902, #197325, #129236, #115083, #62011, #13248, #161653, #132374, #15362, #146482, #181079, #178970, #98779, #29512, #164834, #82504, #148591, #79321, #198376, #97725, #145437, #95605, #211437, #14291, #182130, #99836, #17486, #83572, #196274, #80386, #212501, #47921, #114033, #88930, #67297, #104105, #22817, #2294, #186398, #70496 ),
 ( #119345, #1235, #117211, #3368, #36955, #151794, #169090, #38035, #69437, #86780, #118278, #133436, #184263, #135543, #103035, #199443, #55347, #53214, #121499, #52150, #170155, #21741, #137680, #19635, #84643, #85706, #201568, #187471, #152851, #68371, #51086, #150734, #183208, #166976, #105186, #134503, #4426, #120424, #35889, #34814, #153921, #87850, #100889, #200507, #5491, #101965, #39101, #18567, #168031, #185332, #20689, #136612, #71572, #203701, #202637, #54287, #171222, #107359, #139820, #23893, #188539, #125762, #207977, #41251, #154985, #72650, #108433, #56416, #27098, #191724, #93205, #123642, #24965, #159236, #59604, #40169, #126830, #209032, #173381, #143037, #60667, #89999, #43380, #58543, #10837, #204764, #189605, #106283, #92139, #8716, #124698, #174453, #205850, #122577, #57483, #172304, #74801, #76911, #156050, #9785, #6570, #44445, #138746, #91067, #157127, #140902, #42317, #192787, #109501, #75857, #190656, #28174, #7639, #206913, #26029, #158194, #141965, #175508, #110563, #176565, #73724, #94270, #211171, #14029, #130026, #77987, #148332, #146220, #214332, #145166, #131076, #48702, #16156, #112693, #177641, #178704, #162453, #65964, #31384, #95341, #144110, #29249, #210104, #45512, #198121, #161391, #97460, #213300, #128958, #127911, #32441, #197064, #61744, #12974, #64927, #62796, #132113, #160310, #194937, #80115, #96403, #212238, #114816, #82241, #11914, #15102, #49752, #79050, #179768, #46574, #30318, #63871, #196017, #180814, #193863, #81190, #111628, #115879, #47653, #147268, #113764, #181864, #98509, #163515, #164571, #101700, #169893, #149387, #102774, #33500, #137419, #99573, #51895, #118018, #184007, #135291, #103845, #70238, #168830, #151532, #121241, #970, #35621, #69171, #167770, #201305, #4168, #19367, #119083, #150471, #165637, #2032, #85447, #52945, #17225, #87591, #3100, #153663, #84384, #136353, #202373, #21482, #185063, #116944, #36688, #20434, #5231, #86517, #34560, #83302, #182944, #67035, #199172, #203438, #100630, #152582, #54022, #68101, #133172, #186136, #120161, #50818, #166707, #37771, #134237, #71306, #18298, #200245, #55092, #189351, #40991, #207728, #109251, #187211, #108176, #76664, #172047, #58291, #7381, #106025, #122319, #90808, #59351, #72386, #174202, #154729, #208784, #39916, #25774, #23640, #92948, #91887, #89748, #155797, #139562, #73461, #56156, #6312, #157942, #9534, #205589, #38840, #104923, #140645, #88670, #125507, #75608, #191470, #57226, #123386, #43137, #141719, #138485, #158994, #26844, #107102, #175259, #10589, #188276, #142778, #156872, #60414, #22564, #173125, #204507, #124447, #24706, #8458, #206658, #74546, #190406, #42062, #170964, #100117, #192535, #195757, #1515, #166179, #161128, #178450, #46321, #83856, #84929, #18844, #111375, #27922, #143855, #160056, #30058, #177379, #149945, #162199, #133724, #13786, #126575, #128708, #194677, #199730, #77733, #112437, #176317, #167258, #96148, #79860, #145969, #17767, #211981, #151018, #113508, #62545, #63621, #67579, #129775, #47395, #210919, #179516, #34044, #51376, #117499, #183490, #35099, #2585, #101170, #12715, #44189, #127651, #94017, #110309, #11660, #209847, #61486, #193615, #95079, #45256, #28993, #78789, #144912, #55631, #56704, #119634, #53497, #172598, #71856, #69724, #137963, #68655, #19916 ),
 ( #86001, #121787, #186689, #168321, #134778, #102247, #169382, #72933, #38317, #154207, #88137, #70784, #170440, #39383, #201852, #136897, #156349, #200787, #171512, #90280, #135828, #105479, #203984, #6854, #205062, #188832, #23106, #122871, #106570, #40468, #104393, #5777, #20967, #187754, #152075, #52438, #202926, #153136, #185618, #139037, #37250, #120716, #103320, #89221, #22027, #24177, #155274, #4709, #118564, #184548, #36170, #3645, #54568, #87064, #11133, #110850, #92435, #192014, #143328, #95638, #126051, #42612, #194164, #9011, #123930, #77210, #140112, #57769, #159535, #176857, #190948, #160604, #210406, #74021, #93495, #209322, #62048, #58834, #207210, #111931, #60969, #75087, #127125, #7933, #173683, #107654, #12207, #109796, #158474, #193095, #141199, #44744, #206138, #28470, #94562, #78278, #25259, #144406, #43677, #91359, #189898, #41540, #108721, #128203, #175803, #45811, #27395, #10074, #177932, #29546, #124989, #76150, #157420, #174748, #26321, #142254, #208266, #59899, #16459, #99871, #83607, #67328, #50055, #1271, #199475, #149688, #131362, #32732, #47954, #98813, #179005, #161689, #15396, #31684, #162757, #165934, #80421, #213586, #146520, #132410, #13283, #82539, #33793, #198412, #196310, #65211, #81488, #116177, #117242, #51119, #212538, #63103, #30619, #195243, #197357, #64179, #182162, #49000, #17519, #115118, #79356, #163818, #147565, #133473, #112992, #181114, #211469, #183242, #164865, #148627, #193, #66262, #145474, #34846, #129271, #46880, #130320, #96708, #14331, #114069, #180061, #97760, #185365, #169126, #72685, #38070, #101998, #84680, #184297, #2330, #52185, #204800, #168068, #104140, #5522, #135578, #134533, #39134, #203734, #68406, #19668, #71603, #69471, #138780, #167009, #151829, #86814, #103071, #20720, #121535, #22851, #100921, #21773, #56451, #85747, #186432, #201600, #3402, #35922, #4458, #187505, #200539, #87882, #118311, #122611, #53248, #153955, #119378, #6604, #137714, #36988, #152880, #70528, #136645, #202671, #54319, #55380, #105217, #120460, #18601, #150768, #170187, #171256, #88965, #155020, #188574, #8756, #124736, #126867, #93240, #139855, #11949, #94306, #140938, #28213, #160347, #123677, #159274, #158229, #192825, #90032, #74838, #205885, #191761, #108468, #9820, #59641, #25002, #156091, #91104, #73760, #174490, #176601, #7676, #109541, #40206, #144146, #106316, #58581, #190695, #42356, #142000, #110600, #76948, #175545, #75896, #127948, #57519, #26066, #208015, #92179, #125799, #10873, #43416, #27134, #157165, #172340, #206952, #143073, #189639, #41290, #209066, #60702, #44483, #23928, #107398, #78021, #173420, #210138, #61782, #65996, #162492, #63904, #132146, #32470, #79085, #165670, #33532, #80151, #181896, #99604, #62834, #98542, #97494, #198152, #29282, #14064, #145203, #131107, #47685, #163551, #213330, #178741, #95375, #30354, #13008, #113797, #115911, #161425, #48735, #193901, #83335, #45549, #212269, #130059, #196053, #81222, #49785, #16191, #114848, #15134, #67067, #211209, #179799, #147304, #31418, #64955, #164605, #197094, #180848, #96441, #111665, #146256, #82272, #148367, #177672, #17259, #214366, #149420, #1003, #128996, #194973, #46609, #112730, #2066, #3135, #201339, #104956, #70271, #134271, #116979, #68138, #34596, #84417, #22595, #200279, #136387 ) ),
 .UNSPECIFIED., .T., .F., .F. ) 
 B_SPLINE_SURFACE_WITH_KNOTS ( ( 4, 3, 4 ),
 ( 4, 1, 1, 1, 1, 1, 1, 1, 1, 1, 1, 1, 1, 1, 1, 1, 1, 1, 1, 1, 1, 1, 1, 1, 1, 1, 1, 1, 1, 1, 1, 1, 1, 1, 1, 1, 1, 1, 1, 1, 1, 1, 1, 1, 1, 1, 1, 1, 1, 1, 1, 1, 1, 1, 1, 1, 1, 1, 1, 1, 1, 1, 1, 1, 1, 1, 1, 1, 1, 1, 1, 1, 1, 1, 1, 1, 1, 1, 1, 1, 1, 1, 1, 1, 1, 1, 1, 1, 1, 1, 1, 1, 1, 1, 1, 1, 1, 1, 1, 1, 1, 1, 1, 1, 1, 1, 1, 1, 1, 1, 1, 1, 1, 1, 1, 1, 1, 1, 1, 1, 1, 1, 1, 1, 1, 1, 1, 1, 1, 1, 1, 1, 1, 1, 1, 1, 1, 1, 1, 1, 1, 1, 1, 1, 1, 1, 1, 1, 1, 1, 1, 1, 1, 1, 1, 1, 1, 1, 1, 1, 1, 1, 1, 1, 1, 1, 1, 1, 1, 1, 1, 1, 1, 1, 1, 1, 1, 1, 1, 1, 1, 1, 1, 1, 1, 1, 1, 1, 1, 1, 1, 1, 1, 1, 1, 1, 1, 1, 1, 1, 1, 1, 1, 1, 1, 1, 1, 1, 1, 1, 1, 1, 1, 1, 1, 1, 1, 1, 1, 1, 1, 1, 1, 1, 1, 1, 1, 1, 1, 1, 1, 1, 1, 1, 1, 1, 1, 1, 1, 1, 1, 1, 1, 1, 1, 1, 1, 1, 1, 1, 1, 1, 1, 1, 1, 1, 1, 1, 1, 1, 1, 1, 1, 1, 1, 1, 1, 1, 1, 1, 1, 1, 1, 1, 1, 1, 1, 1, 1, 1, 1, 1, 1, 1, 1, 1, 1, 1, 1, 1, 1, 1, 1, 1, 1, 1, 1, 1, 1, 1, 1, 1, 1, 1, 1, 1, 1, 1, 1, 1, 1, 1, 1, 1, 1, 1, 1, 1, 1, 1, 1, 1, 1, 1, 1, 1, 1, 1, 1, 1, 1, 1, 1, 1, 1, 1, 1, 1, 1, 1, 1, 1, 1, 1, 1, 1, 1, 1, 1, 1, 1, 1, 1, 1, 1, 1, 1, 1, 1, 1, 1, 1, 1, 1, 1, 1, 1, 1, 1, 1, 1, 1, 1, 1, 1, 1, 1, 1, 1, 1, 1, 1, 1, 1, 4 ),
 ( 0.000000000000000000, 0.5000000000000000000, 1.000000000000000000 ),
 ( 0.000000000000000000, 0.002599974731368114196, 0.005208790931971673047, 0.007813145979665977320, 0.01041652777592116073, 0.01302061325022423749, 0.01562498222773845216, 0.01822909327250534645, 0.02083329118620782031, 0.02343750764584028035, 0.02604160881127103033, 0.02864587273906003470, 0.03124992668191499748, 0.03385418289307650513, 0.03645825757725845717, 0.03906249379052053466, 0.04166666320740203266, 0.04427081823557592333, 0.04687506849204003262, 0.04947913642841410276, 0.05208339700068515682, 0.05468745344639398126, 0.05729170333903113588, 0.05989581325979084075, 0.06250002080062810883, 0.06510424464624173235, 0.06770834408375023261, 0.07031260355790951155, 0.07291665769283758869, 0.07552091454841564078, 0.07812498837240108851, 0.08072922377910608793, 0.08333339284475561881, 0.08593754734057650058, 0.08854179710653446722, 0.09114586450482109470, 0.09375012458370637902, 0.09635418052565795921, 0.09895842987840544613, 0.1015625393267825388, 0.1041667463075427041, 0.1067709697059155277, 0.1093750686050062593, 0.1119793276133541904, 0.1145833812402851093, 0.1171876375884709082, 0.1197917109360151500, 0.1223959458003068407, 0.1250001144218755300, 0.1276042683764700425, 0.1302085177025434359, 0.1328125845892443313, 0.1354168441945610146, 0.1380208996559441903, 0.1406251484930516882, 0.1432292574929059925, 0.1458334639374244401, 0.1484376869122458475, 0.1510417852965526830, 0.1536460438630466996, 0.1562500970055218374, 0.1588543528702505148, 0.1614584257649260002, 0.1640626601106844606, 0.1666668283118819260, 0.1692709817489688462, 0.1718752306590244638, 0.1744792970577103974, 0.1770835562133957763, 0.1796876112177483997, 0.1822918595631332073, 0.1848959681380851483, 0.1875001740701665309, 0.1901043966452301559, 0.1927084945383780445, 0.1953127526869259389, 0.1979168053684795814, 0.2005210607736844508, 0.2031251332390507092, 0.2057293670901427229, 0.2083335348946688259, 0.2109376878379560227, 0.2135419363558502259, 0.2161460022900811573, 0.2187502610200618980, 0.2213543155909112325, 0.2239585634684796434, 0.2265626716421396125, 0.2291668770855771753, 0.2317710992846666596, 0.2343751967102698508, 0.2369794544647692847, 0.2395835067089256143, 0.2421877616785296505, 0.2447918337381362330, 0.2473960671184182170, 0.2500002345499632850, 0.2526043870231480248, 0.2552086351727278490, 0.2578127006660536624, 0.2604169589942467167, 0.2630210131551104502, 0.2656252605887587936, 0.2682293683847277177, 0.2708335733633049913, 0.2734377952101950116, 0.2760418921918580404, 0.2786461495761977103, 0.2812502014064713896, 0.2838544559643880194, 0.2864585276417753179, 0.2890627605750938911, 0.2916669276573394809, 0.2942710796841097043, 0.2968753274892133587, 0.2994793925651746958, 0.3020836505154881335, 0.3046877042898750165, 0.3072919513034905736, 0.3098960587453611915, 0.3125002632828523530, 0.3151044848013095923, 0.3177085813626279731, 0.3203128384006882490, 0.3229168898405855304, 0.3255211440107198539, 0.3281252153294201834, 0.3307294478396133885, 0.3333336145962333963, 0.3359377662002681064, 0.3385420136847264727, 0.3411460783668558427, 0.3437503359631899347, 0.3463543893746011126, 0.3489586359920627823, 0.3515627431034201722, 0.3541669472235909888, 0.3567711684373747749, 0.3593752646019360286, 0.3619795213175900916, 0.3645835723906095116, 0.3671878261968588575, 0.3697918971803975663, 0.3723961292912953969, 0.3750002957459567798, 0.3776044469509276524, 0.3802086941385645069, 0.3828127584503868142, 0.3854170157166348365, 0.3880210687885642384, 0.3906253150337437030, 0.3932294218381663375, 0.3958336255647753599, 0.3984378464976386924, 0.4010419422890235119, 0.4036461987061379930, 0.4062502494357712601, 0.4088545029020263510, 0.4114585735739221262, 0.4140628053093475813, 0.4166669714857112461, 0.4192711223152827404, 0.4218753692299160307, 0.4244794331949501842, 0.4270836901549991405, 0.4296877429109347002, 0.4322919888076972583, 0.4348960953287579478, 0.4375002986855570652, 0.4401045193612476147, 0.4427086148030301427, 0.4453128709454660106, 0.4479169213551993378, 0.4505211745053449013, 0.4531252448891109341, 0.4557294762728811288, 0.4583336421946030970, 0.4609377926724337327, 0.4635420393378766879, 0.4661461029796354349, 0.4687503596573671660, 0.4713544121207915438, 0.4739586576929967765, 0.4765627639542633909, 0.4791669669649988861, 0.4817711874072597711, 0.4843752825230089321, 0.4869795384146229367, 0.4895835885279371524, 0.4921878413858530310, 0.4947919115049980165, 0.4973961425609249032, 0.5000003082516567554, 0.5026044584014001115, 0.5052087048414615200, 0.5078127681834534446, 0.5104170246027455171, 0.5130210767971369323, 0.5156253220686399796, 0.5182294280936764475, 0.5208336307820899957, 0.5234378510146604491, 0.5260419458279406157, 0.5286462014925853437, 0.5312502513329574461, 0.5338545039225196520, 0.5364585738005485105, 0.5390628045524396006, 0.5416669700358295314, 0.5442711198811350792, 0.5468753661196208427, 0.5494794291853500878, 0.5520836853700766822, 0.5546877373189100791, 0.5572919823135623618, 0.5598960881259297251, 0.5625002905157588939, 0.5651045105623757614, 0.5677086050967478092, 0.5703128605582734600, 0.5729169101491768945, 0.5755211624942581095, 0.5781252321546730411, 0.5807294626263322934, 0.5833336279260263879, 0.5859377774905402125, 0.5885420235512536236, 0.5911460863642216124, 0.5937503423382545220, 0.5963543940650019026, 0.5989586388066517886, 0.6015627444299086468, 0.6041669465448881171, 0.6067711664292861906, 0.6093752607083083861, 0.6119795159905627724, 0.6145835653554690969, 0.6171878174799397820, 0.6197918869462408775, 0.6223961171614702526, 0.6250002823011129305, 0.6276044316084782304, 0.6302086775152213605, 0.6328127400989277396, 0.6354169958861367595, 0.6380210474142689048, 0.6406252919267632073, 0.6432293973844667168, 0.6458335992483292820, 0.6484378189942425763, 0.6510419130414711875, 0.6536461681683013447, 0.6562502173306804520, 0.6588544692584096252, 0.6614585385540960871, 0.6640627685366956579, 0.6666669335399304508, 0.6692710826137896474, 0.6718753283903641238, 0.6744793907683068745, 0.6770836463925611337, 0.6796876977455479363, 0.6822919420527318035, 0.6848960473684391204, 0.6875002490049163528, 0.6901044686360783276, 0.6927085624750688453, 0.6953128174703216979, 0.6979168664536427036, 0.7005211182084990496, 0.7031251873570698585, 0.7057294171308388098, 0.7083335820213095824, 0.7109377308853042088, 0.7135419765555117699, 0.7161460387511890957, 0.7187502942363581671, 0.7213543454376690756, 0.7239585895633880996, 0.7265626947606567132, 0.7291668961934797411, 0.7317711157336249661, 0.7343752093879328813, 0.7369794642754557978, 0.7395835131031885945, 0.7421877647090413532, 0.7447918337339959338, 0.7473960633227341166, 0.7500002281240860658, 0.7526043768018576552, 0.7552086223895014827, 0.7578126844264116979, 0.7604169397963658206, 0.7630209908694718379, 0.7656252348375721661, 0.7682293399399604539, 0.7708335411928610714, 0.7734377606657260040, 0.7760418541589074737, 0.7786461089625497101, 0.7812501576581653007, 0.7838544091388848223, 0.7864584780637244865, 0.7890627074912324179, 0.7916668722271122949, 0.7942710207423038238, 0.7968752662711893198, 0.7994793281728324041, 0.8020835834514440377, 0.8046876344198176101, 0.8072918782541467220, 0.8098959832852158369, 0.8125001843819276148, 0.8151044038112509327, 0.8177084971668638902, 0.8203127519104773668, 0.8229168004974481976, 0.8255210518769072747, 0.8281251207251358881, 0.8307293500152160837, 0.8333335147092740813, 0.8359376630855301915, 0.8385419085794658667, 0.8411459703693440204, 0.8437502255804886220, 0.8463542764676049712, 0.8489585201920134550, 0.8515626251753276588, 0.8541668261395859441, 0.8567710455491102106, 0.8593751387907155870, 0.8619793934981552219, 0.8645834419999574028, 0.8671876933020320477, 0.8697917620971562513, 0.8723959912736143352, 0.8750001559495040881, 0.8776043042104727521, 0.8802085496932706699, 0.8828126113948897569, 0.8854168665624462253, 0.8880209173917842369, 0.8906251610301256783, 0.8932292659892527853, 0.8958334668447968108, 0.8984376862582688084, 0.9010417794094305322, 0.9036460341045560174, 0.9062500825446693220, 0.9088543337932389887, 0.9114584025587700866, 0.9140626316454156797, 0.9166667963267953745, 0.9192709444961273402, 0.9218751899916067805, 0.9244792516284782158, 0.9270835067763207871, 0.9296875575713596795, 0.9322918011475309630, 0.9348959061060417852, 0.9375001068764983181, 0.9401043263176916964, 0.9427084194022110619, 0.9453126741091559815, 0.9479167225106870376, 0.9505209737258253355, 0.9531250424882484751, 0.9557292715345466760, 0.9583334362123939743, 0.9609375841976093291, 0.9635418299546441023, 0.9661458919105455623, 0.9687501459642621215, 0.9713541960184646218, 0.9739584433044384815, 0.9765625494917742344, 0.9791667425299969141, 0.9817709508269629737, 0.9843750450459556323, 0.9869794226472197174, 0.9895834977571079660, 0.9921868632736227100, 0.9947912224625704569, 0.9974000159472320437, 1.000000000000000000 ),
 .UNSPECIFIED. ) 
 GEOMETRIC_REPRESENTATION_ITEM ( )  RATIONAL_B_SPLINE_SURFACE ( (
 ( 1.000000000000000000, 1.000000000000000000, 1.000000000000000000, 1.000000000000000222, 0.9999999999999997780, 1.000000000000000444, 0.9999999999999997780, 1.000000000000000222, 0.9999999999999996669, 1.000000000000000000, 1.000000000000000000, 1.000000000000000222, 1.000000000000000000, 1.000000000000000000, 0.9999999999999997780, 1.000000000000000000, 1.000000000000000000, 1.000000000000000000, 0.9999999999999997780, 1.000000000000000444, 0.9999999999999997780, 1.000000000000000222, 1.000000000000000000, 0.9999999999999997780, 1.000000000000000000, 1.000000000000000222, 0.9999999999999997780, 1.000000000000000222, 0.9999999999999997780, 1.000000000000000222, 1.000000000000000000, 0.9999999999999997780, 1.000000000000000444, 0.9999999999999997780, 1.000000000000000222, 0.9999999999999997780, 1.000000000000000444, 1.000000000000000000, 1.000000000000000000, 1.000000000000000000, 1.000000000000000000, 1.000000000000000000, 1.000000000000000000, 0.9999999999999997780, 1.000000000000000222, 0.9999999999999996669, 1.000000000000000444, 0.9999999999999994449, 1.000000000000000222, 1.000000000000000000, 1.000000000000000000, 1.000000000000000000, 1.000000000000000000, 1.000000000000000000, 0.9999999999999996669, 1.000000000000000444, 0.9999999999999997780, 1.000000000000000222, 0.9999999999999996669, 1.000000000000000000, 1.000000000000000000, 1.000000000000000222, 0.9999999999999997780, 1.000000000000000000, 1.000000000000000222, 0.9999999999999997780, 1.000000000000000000, 0.9999999999999997780, 1.000000000000000222, 0.9999999999999997780, 1.000000000000000444, 0.9999999999999994449, 1.000000000000000444, 0.9999999999999997780, 0.9999999999999997780, 1.000000000000000444, 0.9999999999999996669, 1.000000000000000000, 1.000000000000000000, 1.000000000000000000, 1.000000000000000000, 1.000000000000000222, 1.000000000000000000, 1.000000000000000000, 0.9999999999999996669, 1.000000000000000222, 1.000000000000000000, 0.9999999999999997780, 0.9999999999999997780, 0.9999999999999997780, 1.000000000000000000, 1.000000000000000222, 0.9999999999999997780, 1.000000000000000222, 0.9999999999999996669, 1.000000000000000444, 0.9999999999999997780, 1.000000000000000222, 1.000000000000000222, 0.9999999999999997780, 1.000000000000000222, 1.000000000000000000, 0.9999999999999997780, 1.000000000000000444, 1.000000000000000000, 1.000000000000000000, 1.000000000000000222, 1.000000000000000000, 1.000000000000000000, 1.000000000000000222, 0.9999999999999993339, 1.000000000000000444, 1.000000000000000222, 0.9999999999999997780, 1.000000000000000000, 1.000000000000000222, 1.000000000000000444, 1.000000000000000000, 1.000000000000000222, 0.9999999999999997780, 1.000000000000000222, 0.9999999999999997780, 1.000000000000000222, 1.000000000000000000, 0.9999999999999997780, 0.9999999999999996669, 1.000000000000000444, 0.9999999999999997780, 1.000000000000000444, 0.9999999999999997780, 1.000000000000000222, 1.000000000000000222, 1.000000000000000000, 0.9999999999999997780, 1.000000000000000222, 0.9999999999999997780, 1.000000000000000000, 1.000000000000000000, 1.000000000000000000, 0.9999999999999997780, 1.000000000000000222, 1.000000000000000000, 1.000000000000000000, 1.000000000000000000, 1.000000000000000222, 1.000000000000000222, 0.9999999999999994449, 1.000000000000000222, 1.000000000000000000, 0.9999999999999994449, 1.000000000000000444, 0.9999999999999997780, 1.000000000000000222, 0.9999999999999996669, 1.000000000000000444, 1.000000000000000000, 0.9999999999999996669, 1.000000000000000444, 0.9999999999999997780, 1.000000000000000000, 1.000000000000000444, 1.000000000000000000, 1.000000000000000222, 0.9999999999999996669, 1.000000000000000000, 0.9999999999999997780, 0.9999999999999997780, 1.000000000000000222, 1.000000000000000000, 1.000000000000000444, 0.9999999999999996669, 1.000000000000000222, 0.9999999999999997780, 0.9999999999999997780, 1.000000000000000444, 0.9999999999999997780, 1.000000000000000444, 0.9999999999999996669, 1.000000000000000222, 0.9999999999999996669, 1.000000000000000222, 0.9999999999999997780, 1.000000000000000444, 1.000000000000000222, 0.9999999999999996669, 1.000000000000000444, 0.9999999999999996669, 1.000000000000000000, 0.9999999999999997780, 1.000000000000000000, 1.000000000000000000, 1.000000000000000222, 0.9999999999999994449, 1.000000000000000444, 0.9999999999999993339, 1.000000000000000666, 0.9999999999999994449, 1.000000000000000222, 1.000000000000000222, 1.000000000000000000, 1.000000000000000000, 0.9999999999999997780, 1.000000000000000222, 0.9999999999999996669, 1.000000000000000222, 0.9999999999999996669, 1.000000000000000222, 1.000000000000000000, 1.000000000000000222, 0.9999999999999997780, 1.000000000000000222, 1.000000000000000222, 1.000000000000000000, 0.9999999999999997780, 1.000000000000000222, 1.000000000000000222, 1.000000000000000000, 1.000000000000000000, 1.000000000000000222, 0.9999999999999997780, 1.000000000000000000, 1.000000000000000222, 0.9999999999999996669, 0.9999999999999997780, 1.000000000000000222, 0.9999999999999997780, 1.000000000000000000, 0.9999999999999997780, 0.9999999999999997780, 1.000000000000000222, 1.000000000000000000, 1.000000000000000000, 1.000000000000000222, 0.9999999999999996669, 1.000000000000000444, 1.000000000000000000, 1.000000000000000222, 0.9999999999999997780, 1.000000000000000222, 0.9999999999999997780, 1.000000000000000444, 0.9999999999999997780, 1.000000000000000222, 0.9999999999999997780, 1.000000000000000222, 0.9999999999999997780, 1.000000000000000222, 1.000000000000000000, 1.000000000000000222, 1.000000000000000000, 1.000000000000000000, 1.000000000000000222, 1.000000000000000000, 1.000000000000000000, 0.9999999999999997780, 1.000000000000000000, 1.000000000000000444, 0.9999999999999996669, 1.000000000000000222, 0.9999999999999997780, 1.000000000000000000, 0.9999999999999997780, 1.000000000000000222, 1.000000000000000222, 1.000000000000000000, 1.000000000000000000, 0.9999999999999996669, 1.000000000000000444, 0.9999999999999997780, 1.000000000000000000, 1.000000000000000222, 0.9999999999999996669, 1.000000000000000444, 1.000000000000000000, 0.9999999999999997780, 1.000000000000000222, 0.9999999999999997780, 1.000000000000000000, 1.000000000000000000, 1.000000000000000000, 1.000000000000000000, 1.000000000000000000, 1.000000000000000222, 1.000000000000000444, 0.9999999999999997780, 1.000000000000000222, 1.000000000000000000, 1.000000000000000444, 0.9999999999999997780, 1.000000000000000222, 0.9999999999999997780, 1.000000000000000222, 0.9999999999999997780, 1.000000000000000222, 1.000000000000000000, 1.000000000000000222, 1.000000000000000222, 1.000000000000000222, 0.9999999999999997780, 1.000000000000000222, 0.9999999999999997780, 1.000000000000000222, 0.9999999999999997780, 1.000000000000000444, 0.9999999999999996669, 1.000000000000000444, 1.000000000000000000, 1.000000000000000000, 0.9999999999999997780, 1.000000000000000222, 1.000000000000000000, 0.9999999999999997780, 1.000000000000000000, 0.9999999999999997780, 1.000000000000000222, 1.000000000000000000, 1.000000000000000000, 1.000000000000000222, 0.9999999999999997780, 1.000000000000000444, 0.9999999999999996669, 1.000000000000000222, 1.000000000000000222, 0.9999999999999997780, 1.000000000000000000, 0.9999999999999997780, 1.000000000000000000, 0.9999999999999996669, 1.000000000000000444, 0.9999999999999997780, 1.000000000000000222, 1.000000000000000000, 1.000000000000000000, 1.000000000000000000, 0.9999999999999997780, 0.9999999999999997780, 1.000000000000000000, 0.9999999999999997780, 1.000000000000000444, 0.9999999999999996669, 1.000000000000000222, 1.000000000000000000, 1.000000000000000444, 1.000000000000000222, 1.000000000000000000, 0.9999999999999997780, 1.000000000000000222, 1.000000000000000444, 0.9999999999999997780, 1.000000000000000222, 0.9999999999999997780, 1.000000000000000000, 1.000000000000000000, 1.000000000000000222, 0.9999999999999997780, 1.000000000000000222, 1.000000000000000000, 1.000000000000000222, 0.9999999999999997780, 1.000000000000000000, 1.000000000000000222, 1.000000000000000000, 1.000000000000000222, 1.000000000000000000, 1.000000000000000000, 0.9999999999999997780, 1.000000000000000444, 0.9999999999999997780, 1.000000000000000000, 1.000000000000000000, 1.000000000000000444, 0.9999999999999996669, 1.000000000000000222, 1.000000000000000000, 0.9999999999999996669, 1.000000000000000444, 0.9999999999999996669, 1.000000000000000444, 0.9999999999999997780, 1.000000000000000222, 0.9999999999999997780, 1.000000000000000222, 1.000000000000000222, 1.000000000000000222, 1.000000000000000000, 1.000000000000000000, 1.000000000000000000),
 ( 0.3333333333333333703, 0.3333333333333333703, 0.3333333333333334259, 0.3333333333333334259, 0.3333333333333333703, 0.3333333333333334259, 0.3333333333333333148, 0.3333333333333333703, 0.3333333333333333148, 0.3333333333333333703, 0.3333333333333333703, 0.3333333333333334259, 0.3333333333333333703, 0.3333333333333333703, 0.3333333333333333703, 0.3333333333333333703, 0.3333333333333333703, 0.3333333333333333148, 0.3333333333333333703, 0.3333333333333334814, 0.3333333333333333148, 0.3333333333333334259, 0.3333333333333333148, 0.3333333333333334259, 0.3333333333333332593, 0.3333333333333335369, 0.3333333333333333703, 0.3333333333333333703, 0.3333333333333333703, 0.3333333333333333703, 0.3333333333333333703, 0.3333333333333333703, 0.3333333333333334259, 0.3333333333333333703, 0.3333333333333333703, 0.3333333333333333703, 0.3333333333333334814, 0.3333333333333333703, 0.3333333333333333703, 0.3333333333333333703, 0.3333333333333334259, 0.3333333333333332593, 0.3333333333333334814, 0.3333333333333332593, 0.3333333333333334259, 0.3333333333333332038, 0.3333333333333335369, 0.3333333333333332593, 0.3333333333333334814, 0.3333333333333333703, 0.3333333333333333148, 0.3333333333333333703, 0.3333333333333333703, 0.3333333333333333148, 0.3333333333333333148, 0.3333333333333334814, 0.3333333333333332593, 0.3333333333333334259, 0.3333333333333332593, 0.3333333333333333703, 0.3333333333333333703, 0.3333333333333334259, 0.3333333333333333148, 0.3333333333333333148, 0.3333333333333334259, 0.3333333333333333703, 0.3333333333333333703, 0.3333333333333333703, 0.3333333333333334814, 0.3333333333333332038, 0.3333333333333335924, 0.3333333333333332593, 0.3333333333333335369, 0.3333333333333333148, 0.3333333333333332593, 0.3333333333333335924, 0.3333333333333332038, 0.3333333333333333703, 0.3333333333333333703, 0.3333333333333334259, 0.3333333333333333148, 0.3333333333333334259, 0.3333333333333333703, 0.3333333333333334259, 0.3333333333333332038, 0.3333333333333333703, 0.3333333333333333703, 0.3333333333333333703, 0.3333333333333332593, 0.3333333333333333703, 0.3333333333333333148, 0.3333333333333334259, 0.3333333333333333148, 0.3333333333333334259, 0.3333333333333333148, 0.3333333333333334814, 0.3333333333333333703, 0.3333333333333334259, 0.3333333333333333703, 0.3333333333333333148, 0.3333333333333333703, 0.3333333333333334259, 0.3333333333333333148, 0.3333333333333334814, 0.3333333333333334259, 0.3333333333333333703, 0.3333333333333334259, 0.3333333333333333703, 0.3333333333333334259, 0.3333333333333334814, 0.3333333333333332038, 0.3333333333333334259, 0.3333333333333334259, 0.3333333333333333703, 0.3333333333333333148, 0.3333333333333334259, 0.3333333333333334259, 0.3333333333333334259, 0.3333333333333333703, 0.3333333333333333148, 0.3333333333333334259, 0.3333333333333333703, 0.3333333333333334259, 0.3333333333333333703, 0.3333333333333333148, 0.3333333333333332593, 0.3333333333333334259, 0.3333333333333333148, 0.3333333333333335369, 0.3333333333333332593, 0.3333333333333334814, 0.3333333333333334259, 0.3333333333333334259, 0.3333333333333333148, 0.3333333333333334259, 0.3333333333333333148, 0.3333333333333333148, 0.3333333333333333703, 0.3333333333333333703, 0.3333333333333332593, 0.3333333333333334259, 0.3333333333333333148, 0.3333333333333333703, 0.3333333333333334259, 0.3333333333333333148, 0.3333333333333334814, 0.3333333333333332593, 0.3333333333333333703, 0.3333333333333334259, 0.3333333333333332038, 0.3333333333333335369, 0.3333333333333333703, 0.3333333333333333703, 0.3333333333333333148, 0.3333333333333334259, 0.3333333333333333703, 0.3333333333333332593, 0.3333333333333335369, 0.3333333333333332593, 0.3333333333333333703, 0.3333333333333334814, 0.3333333333333333703, 0.3333333333333334259, 0.3333333333333332593, 0.3333333333333334259, 0.3333333333333332593, 0.3333333333333333703, 0.3333333333333334259, 0.3333333333333333703, 0.3333333333333334814, 0.3333333333333332593, 0.3333333333333333703, 0.3333333333333333703, 0.3333333333333333703, 0.3333333333333334259, 0.3333333333333333148, 0.3333333333333334259, 0.3333333333333332593, 0.3333333333333333703, 0.3333333333333332593, 0.3333333333333334814, 0.3333333333333333703, 0.3333333333333334259, 0.3333333333333334259, 0.3333333333333332593, 0.3333333333333334814, 0.3333333333333333148, 0.3333333333333333148, 0.3333333333333333148, 0.3333333333333333703, 0.3333333333333333703, 0.3333333333333334259, 0.3333333333333332593, 0.3333333333333335369, 0.3333333333333332038, 0.3333333333333335924, 0.3333333333333332593, 0.3333333333333334814, 0.3333333333333333703, 0.3333333333333333703, 0.3333333333333333703, 0.3333333333333333148, 0.3333333333333334259, 0.3333333333333333703, 0.3333333333333333703, 0.3333333333333333148, 0.3333333333333333703, 0.3333333333333333148, 0.3333333333333333703, 0.3333333333333332593, 0.3333333333333334259, 0.3333333333333333703, 0.3333333333333334259, 0.3333333333333333148, 0.3333333333333334259, 0.3333333333333333703, 0.3333333333333334259, 0.3333333333333334259, 0.3333333333333334259, 0.3333333333333332593, 0.3333333333333334259, 0.3333333333333333703, 0.3333333333333333148, 0.3333333333333333148, 0.3333333333333335369, 0.3333333333333332593, 0.3333333333333333148, 0.3333333333333333703, 0.3333333333333333148, 0.3333333333333334814, 0.3333333333333333703, 0.3333333333333334814, 0.3333333333333333703, 0.3333333333333332593, 0.3333333333333334259, 0.3333333333333333703, 0.3333333333333335369, 0.3333333333333333148, 0.3333333333333334259, 0.3333333333333333148, 0.3333333333333335924, 0.3333333333333332593, 0.3333333333333334259, 0.3333333333333334259, 0.3333333333333333703, 0.3333333333333333703, 0.3333333333333334259, 0.3333333333333334259, 0.3333333333333334259, 0.3333333333333333703, 0.3333333333333333703, 0.3333333333333334259, 0.3333333333333333148, 0.3333333333333333703, 0.3333333333333332038, 0.3333333333333334259, 0.3333333333333334814, 0.3333333333333332593, 0.3333333333333333703, 0.3333333333333333148, 0.3333333333333334814, 0.3333333333333332593, 0.3333333333333334259, 0.3333333333333333703, 0.3333333333333333703, 0.3333333333333333703, 0.3333333333333333148, 0.3333333333333334259, 0.3333333333333333703, 0.3333333333333333148, 0.3333333333333334259, 0.3333333333333332038, 0.3333333333333334259, 0.3333333333333333703, 0.3333333333333333703, 0.3333333333333333703, 0.3333333333333334259, 0.3333333333333333148, 0.3333333333333333703, 0.3333333333333333703, 0.3333333333333333703, 0.3333333333333333703, 0.3333333333333334259, 0.3333333333333334814, 0.3333333333333332593, 0.3333333333333333703, 0.3333333333333334259, 0.3333333333333334814, 0.3333333333333333148, 0.3333333333333333703, 0.3333333333333333703, 0.3333333333333334259, 0.3333333333333333148, 0.3333333333333334814, 0.3333333333333333148, 0.3333333333333334814, 0.3333333333333333703, 0.3333333333333334814, 0.3333333333333333148, 0.3333333333333334259, 0.3333333333333332593, 0.3333333333333335369, 0.3333333333333333148, 0.3333333333333334814, 0.3333333333333333148, 0.3333333333333334259, 0.3333333333333333703, 0.3333333333333333148, 0.3333333333333333703, 0.3333333333333333703, 0.3333333333333334259, 0.3333333333333333148, 0.3333333333333334259, 0.3333333333333333148, 0.3333333333333334814, 0.3333333333333333148, 0.3333333333333334259, 0.3333333333333334259, 0.3333333333333333703, 0.3333333333333334259, 0.3333333333333333703, 0.3333333333333333703, 0.3333333333333335369, 0.3333333333333332593, 0.3333333333333334259, 0.3333333333333333703, 0.3333333333333333703, 0.3333333333333333148, 0.3333333333333335369, 0.3333333333333333148, 0.3333333333333334259, 0.3333333333333333703, 0.3333333333333333703, 0.3333333333333334259, 0.3333333333333333148, 0.3333333333333333703, 0.3333333333333333148, 0.3333333333333333148, 0.3333333333333334814, 0.3333333333333332593, 0.3333333333333334259, 0.3333333333333333703, 0.3333333333333334814, 0.3333333333333334259, 0.3333333333333333148, 0.3333333333333333703, 0.3333333333333333703, 0.3333333333333335369, 0.3333333333333333148, 0.3333333333333334259, 0.3333333333333333703, 0.3333333333333333148, 0.3333333333333334259, 0.3333333333333334259, 0.3333333333333333703, 0.3333333333333333703, 0.3333333333333334259, 0.3333333333333334259, 0.3333333333333333703, 0.3333333333333333148, 0.3333333333333334259, 0.3333333333333333703, 0.3333333333333334814, 0.3333333333333333703, 0.3333333333333333703, 0.3333333333333333703, 0.3333333333333334259, 0.3333333333333333148, 0.3333333333333333703, 0.3333333333333334259, 0.3333333333333334259, 0.3333333333333333148, 0.3333333333333333703, 0.3333333333333333148, 0.3333333333333333703, 0.3333333333333335369, 0.3333333333333333148, 0.3333333333333334259, 0.3333333333333333703, 0.3333333333333334259, 0.3333333333333333148, 0.3333333333333333148, 0.3333333333333335369, 0.3333333333333333703, 0.3333333333333333148, 0.3333333333333333703, 0.3333333333333333703),
 ( 0.3333333333333333703, 0.3333333333333333703, 0.3333333333333334259, 0.3333333333333334259, 0.3333333333333333703, 0.3333333333333334259, 0.3333333333333333148, 0.3333333333333333703, 0.3333333333333333148, 0.3333333333333333703, 0.3333333333333333703, 0.3333333333333334259, 0.3333333333333333703, 0.3333333333333333703, 0.3333333333333333703, 0.3333333333333333703, 0.3333333333333333703, 0.3333333333333333148, 0.3333333333333333703, 0.3333333333333334814, 0.3333333333333333148, 0.3333333333333334259, 0.3333333333333333148, 0.3333333333333334259, 0.3333333333333332593, 0.3333333333333335369, 0.3333333333333333703, 0.3333333333333333703, 0.3333333333333333703, 0.3333333333333333703, 0.3333333333333333703, 0.3333333333333333703, 0.3333333333333334259, 0.3333333333333333703, 0.3333333333333333703, 0.3333333333333333703, 0.3333333333333334814, 0.3333333333333333703, 0.3333333333333333703, 0.3333333333333333703, 0.3333333333333334259, 0.3333333333333332593, 0.3333333333333334814, 0.3333333333333332593, 0.3333333333333334259, 0.3333333333333332038, 0.3333333333333335369, 0.3333333333333332593, 0.3333333333333334814, 0.3333333333333333703, 0.3333333333333333148, 0.3333333333333333703, 0.3333333333333333703, 0.3333333333333333148, 0.3333333333333333148, 0.3333333333333334814, 0.3333333333333332593, 0.3333333333333334259, 0.3333333333333332593, 0.3333333333333333703, 0.3333333333333333703, 0.3333333333333334259, 0.3333333333333333148, 0.3333333333333333148, 0.3333333333333334259, 0.3333333333333333703, 0.3333333333333333703, 0.3333333333333333703, 0.3333333333333334814, 0.3333333333333332038, 0.3333333333333335924, 0.3333333333333332593, 0.3333333333333335369, 0.3333333333333333148, 0.3333333333333332593, 0.3333333333333335924, 0.3333333333333332038, 0.3333333333333333703, 0.3333333333333333703, 0.3333333333333334259, 0.3333333333333333148, 0.3333333333333334259, 0.3333333333333333703, 0.3333333333333334259, 0.3333333333333332038, 0.3333333333333333703, 0.3333333333333333703, 0.3333333333333333703, 0.3333333333333332593, 0.3333333333333333703, 0.3333333333333333148, 0.3333333333333334259, 0.3333333333333333148, 0.3333333333333334259, 0.3333333333333333148, 0.3333333333333334814, 0.3333333333333333703, 0.3333333333333334259, 0.3333333333333333703, 0.3333333333333333148, 0.3333333333333333703, 0.3333333333333334259, 0.3333333333333333148, 0.3333333333333334814, 0.3333333333333334259, 0.3333333333333333703, 0.3333333333333334259, 0.3333333333333333703, 0.3333333333333334259, 0.3333333333333334814, 0.3333333333333332038, 0.3333333333333334259, 0.3333333333333334259, 0.3333333333333333703, 0.3333333333333333148, 0.3333333333333334259, 0.3333333333333334259, 0.3333333333333334259, 0.3333333333333333703, 0.3333333333333333148, 0.3333333333333334259, 0.3333333333333333703, 0.3333333333333334259, 0.3333333333333333703, 0.3333333333333333148, 0.3333333333333332593, 0.3333333333333334259, 0.3333333333333333148, 0.3333333333333335369, 0.3333333333333332593, 0.3333333333333334814, 0.3333333333333334259, 0.3333333333333334259, 0.3333333333333333148, 0.3333333333333334259, 0.3333333333333333148, 0.3333333333333333148, 0.3333333333333333703, 0.3333333333333333703, 0.3333333333333332593, 0.3333333333333334259, 0.3333333333333333148, 0.3333333333333333703, 0.3333333333333334259, 0.3333333333333333148, 0.3333333333333334814, 0.3333333333333332593, 0.3333333333333333703, 0.3333333333333334259, 0.3333333333333332038, 0.3333333333333335369, 0.3333333333333333703, 0.3333333333333333703, 0.3333333333333333148, 0.3333333333333334259, 0.3333333333333333703, 0.3333333333333332593, 0.3333333333333335369, 0.3333333333333332593, 0.3333333333333333703, 0.3333333333333334814, 0.3333333333333333703, 0.3333333333333334259, 0.3333333333333332593, 0.3333333333333334259, 0.3333333333333332593, 0.3333333333333333703, 0.3333333333333334259, 0.3333333333333333703, 0.3333333333333334814, 0.3333333333333332593, 0.3333333333333333703, 0.3333333333333333703, 0.3333333333333333703, 0.3333333333333334259, 0.3333333333333333148, 0.3333333333333334259, 0.3333333333333332593, 0.3333333333333333703, 0.3333333333333332593, 0.3333333333333334814, 0.3333333333333333703, 0.3333333333333334259, 0.3333333333333334259, 0.3333333333333332593, 0.3333333333333334814, 0.3333333333333333148, 0.3333333333333333148, 0.3333333333333333148, 0.3333333333333333703, 0.3333333333333333703, 0.3333333333333334259, 0.3333333333333332593, 0.3333333333333335369, 0.3333333333333332038, 0.3333333333333335924, 0.3333333333333332593, 0.3333333333333334814, 0.3333333333333333703, 0.3333333333333333703, 0.3333333333333333703, 0.3333333333333333148, 0.3333333333333334259, 0.3333333333333333703, 0.3333333333333333703, 0.3333333333333333148, 0.3333333333333333703, 0.3333333333333333148, 0.3333333333333333703, 0.3333333333333332593, 0.3333333333333334259, 0.3333333333333333703, 0.3333333333333334259, 0.3333333333333333148, 0.3333333333333334259, 0.3333333333333333703, 0.3333333333333334259, 0.3333333333333334259, 0.3333333333333334259, 0.3333333333333332593, 0.3333333333333334259, 0.3333333333333333703, 0.3333333333333333148, 0.3333333333333333148, 0.3333333333333335369, 0.3333333333333332593, 0.3333333333333333148, 0.3333333333333333703, 0.3333333333333333148, 0.3333333333333334814, 0.3333333333333333703, 0.3333333333333334814, 0.3333333333333333703, 0.3333333333333332593, 0.3333333333333334259, 0.3333333333333333703, 0.3333333333333335369, 0.3333333333333333148, 0.3333333333333334259, 0.3333333333333333148, 0.3333333333333335924, 0.3333333333333332593, 0.3333333333333334259, 0.3333333333333334259, 0.3333333333333333703, 0.3333333333333333703, 0.3333333333333334259, 0.3333333333333334259, 0.3333333333333334259, 0.3333333333333333703, 0.3333333333333333703, 0.3333333333333334259, 0.3333333333333333148, 0.3333333333333333703, 0.3333333333333332038, 0.3333333333333334259, 0.3333333333333334814, 0.3333333333333332593, 0.3333333333333333703, 0.3333333333333333148, 0.3333333333333334814, 0.3333333333333332593, 0.3333333333333334259, 0.3333333333333333703, 0.3333333333333333703, 0.3333333333333333703, 0.3333333333333333148, 0.3333333333333334259, 0.3333333333333333703, 0.3333333333333333148, 0.3333333333333334259, 0.3333333333333332038, 0.3333333333333334259, 0.3333333333333333703, 0.3333333333333333703, 0.3333333333333333703, 0.3333333333333334259, 0.3333333333333333148, 0.3333333333333333703, 0.3333333333333333703, 0.3333333333333333703, 0.3333333333333333703, 0.3333333333333334259, 0.3333333333333334814, 0.3333333333333332593, 0.3333333333333333703, 0.3333333333333334259, 0.3333333333333334814, 0.3333333333333333148, 0.3333333333333333703, 0.3333333333333333703, 0.3333333333333334259, 0.3333333333333333148, 0.3333333333333334814, 0.3333333333333333148, 0.3333333333333334814, 0.3333333333333333703, 0.3333333333333334814, 0.3333333333333333148, 0.3333333333333334259, 0.3333333333333332593, 0.3333333333333335369, 0.3333333333333333148, 0.3333333333333334814, 0.3333333333333333148, 0.3333333333333334259, 0.3333333333333333703, 0.3333333333333333148, 0.3333333333333333703, 0.3333333333333333703, 0.3333333333333334259, 0.3333333333333333148, 0.3333333333333334259, 0.3333333333333333148, 0.3333333333333334814, 0.3333333333333333148, 0.3333333333333334259, 0.3333333333333334259, 0.3333333333333333703, 0.3333333333333334259, 0.3333333333333333703, 0.3333333333333333703, 0.3333333333333335369, 0.3333333333333332593, 0.3333333333333334259, 0.3333333333333333703, 0.3333333333333333703, 0.3333333333333333148, 0.3333333333333335369, 0.3333333333333333148, 0.3333333333333334259, 0.3333333333333333703, 0.3333333333333333703, 0.3333333333333334259, 0.3333333333333333148, 0.3333333333333333703, 0.3333333333333333148, 0.3333333333333333148, 0.3333333333333334814, 0.3333333333333332593, 0.3333333333333334259, 0.3333333333333333703, 0.3333333333333334814, 0.3333333333333334259, 0.3333333333333333148, 0.3333333333333333703, 0.3333333333333333703, 0.3333333333333335369, 0.3333333333333333148, 0.3333333333333334259, 0.3333333333333333703, 0.3333333333333333148, 0.3333333333333334259, 0.3333333333333334259, 0.3333333333333333703, 0.3333333333333333703, 0.3333333333333334259, 0.3333333333333334259, 0.3333333333333333703, 0.3333333333333333148, 0.3333333333333334259, 0.3333333333333333703, 0.3333333333333334814, 0.3333333333333333703, 0.3333333333333333703, 0.3333333333333333703, 0.3333333333333334259, 0.3333333333333333148, 0.3333333333333333703, 0.3333333333333334259, 0.3333333333333334259, 0.3333333333333333148, 0.3333333333333333703, 0.3333333333333333148, 0.3333333333333333703, 0.3333333333333335369, 0.3333333333333333148, 0.3333333333333334259, 0.3333333333333333703, 0.3333333333333334259, 0.3333333333333333148, 0.3333333333333333148, 0.3333333333333335369, 0.3333333333333333703, 0.3333333333333333148, 0.3333333333333333703, 0.3333333333333333703),
 ( 1.000000000000000000, 1.000000000000000000, 1.000000000000000000, 1.000000000000000222, 0.9999999999999997780, 1.000000000000000444, 0.9999999999999997780, 1.000000000000000222, 0.9999999999999996669, 1.000000000000000000, 1.000000000000000000, 1.000000000000000222, 1.000000000000000000, 1.000000000000000000, 0.9999999999999997780, 1.000000000000000000, 1.000000000000000000, 1.000000000000000000, 0.9999999999999997780, 1.000000000000000444, 0.9999999999999997780, 1.000000000000000222, 1.000000000000000000, 0.9999999999999997780, 1.000000000000000000, 1.000000000000000222, 0.9999999999999997780, 1.000000000000000222, 0.9999999999999997780, 1.000000000000000222, 1.000000000000000000, 0.9999999999999997780, 1.000000000000000444, 0.9999999999999997780, 1.000000000000000222, 0.9999999999999997780, 1.000000000000000444, 1.000000000000000000, 1.000000000000000000, 1.000000000000000000, 1.000000000000000000, 1.000000000000000000, 1.000000000000000000, 0.9999999999999997780, 1.000000000000000222, 0.9999999999999996669, 1.000000000000000444, 0.9999999999999994449, 1.000000000000000222, 1.000000000000000000, 1.000000000000000000, 1.000000000000000000, 1.000000000000000000, 1.000000000000000000, 0.9999999999999996669, 1.000000000000000444, 0.9999999999999997780, 1.000000000000000222, 0.9999999999999996669, 1.000000000000000000, 1.000000000000000000, 1.000000000000000222, 0.9999999999999997780, 1.000000000000000000, 1.000000000000000222, 0.9999999999999997780, 1.000000000000000000, 0.9999999999999997780, 1.000000000000000222, 0.9999999999999997780, 1.000000000000000444, 0.9999999999999994449, 1.000000000000000444, 0.9999999999999997780, 0.9999999999999997780, 1.000000000000000444, 0.9999999999999996669, 1.000000000000000000, 1.000000000000000000, 1.000000000000000000, 1.000000000000000000, 1.000000000000000222, 1.000000000000000000, 1.000000000000000000, 0.9999999999999996669, 1.000000000000000222, 1.000000000000000000, 0.9999999999999997780, 0.9999999999999997780, 0.9999999999999997780, 1.000000000000000000, 1.000000000000000222, 0.9999999999999997780, 1.000000000000000222, 0.9999999999999996669, 1.000000000000000444, 0.9999999999999997780, 1.000000000000000222, 1.000000000000000222, 0.9999999999999997780, 1.000000000000000222, 1.000000000000000000, 0.9999999999999997780, 1.000000000000000444, 1.000000000000000000, 1.000000000000000000, 1.000000000000000222, 1.000000000000000000, 1.000000000000000000, 1.000000000000000222, 0.9999999999999993339, 1.000000000000000444, 1.000000000000000222, 0.9999999999999997780, 1.000000000000000000, 1.000000000000000222, 1.000000000000000444, 1.000000000000000000, 1.000000000000000222, 0.9999999999999997780, 1.000000000000000222, 0.9999999999999997780, 1.000000000000000222, 1.000000000000000000, 0.9999999999999997780, 0.9999999999999996669, 1.000000000000000444, 0.9999999999999997780, 1.000000000000000444, 0.9999999999999997780, 1.000000000000000222, 1.000000000000000222, 1.000000000000000000, 0.9999999999999997780, 1.000000000000000222, 0.9999999999999997780, 1.000000000000000000, 1.000000000000000000, 1.000000000000000000, 0.9999999999999997780, 1.000000000000000222, 1.000000000000000000, 1.000000000000000000, 1.000000000000000000, 1.000000000000000222, 1.000000000000000222, 0.9999999999999994449, 1.000000000000000222, 1.000000000000000000, 0.9999999999999994449, 1.000000000000000444, 0.9999999999999997780, 1.000000000000000222, 0.9999999999999996669, 1.000000000000000444, 1.000000000000000000, 0.9999999999999996669, 1.000000000000000444, 0.9999999999999997780, 1.000000000000000000, 1.000000000000000444, 1.000000000000000000, 1.000000000000000222, 0.9999999999999996669, 1.000000000000000000, 0.9999999999999997780, 0.9999999999999997780, 1.000000000000000222, 1.000000000000000000, 1.000000000000000444, 0.9999999999999996669, 1.000000000000000222, 0.9999999999999997780, 0.9999999999999997780, 1.000000000000000444, 0.9999999999999997780, 1.000000000000000444, 0.9999999999999996669, 1.000000000000000222, 0.9999999999999996669, 1.000000000000000222, 0.9999999999999997780, 1.000000000000000444, 1.000000000000000222, 0.9999999999999996669, 1.000000000000000444, 0.9999999999999996669, 1.000000000000000000, 0.9999999999999997780, 1.000000000000000000, 1.000000000000000000, 1.000000000000000222, 0.9999999999999994449, 1.000000000000000444, 0.9999999999999993339, 1.000000000000000666, 0.9999999999999994449, 1.000000000000000222, 1.000000000000000222, 1.000000000000000000, 1.000000000000000000, 0.9999999999999997780, 1.000000000000000222, 0.9999999999999996669, 1.000000000000000222, 0.9999999999999996669, 1.000000000000000222, 1.000000000000000000, 1.000000000000000222, 0.9999999999999997780, 1.000000000000000222, 1.000000000000000222, 1.000000000000000000, 0.9999999999999997780, 1.000000000000000222, 1.000000000000000222, 1.000000000000000000, 1.000000000000000000, 1.000000000000000222, 0.9999999999999997780, 1.000000000000000000, 1.000000000000000222, 0.9999999999999996669, 0.9999999999999997780, 1.000000000000000222, 0.9999999999999997780, 1.000000000000000000, 0.9999999999999997780, 0.9999999999999997780, 1.000000000000000222, 1.000000000000000000, 1.000000000000000000, 1.000000000000000222, 0.9999999999999996669, 1.000000000000000444, 1.000000000000000000, 1.000000000000000222, 0.9999999999999997780, 1.000000000000000222, 0.9999999999999997780, 1.000000000000000444, 0.9999999999999997780, 1.000000000000000222, 0.9999999999999997780, 1.000000000000000222, 0.9999999999999997780, 1.000000000000000222, 1.000000000000000000, 1.000000000000000222, 1.000000000000000000, 1.000000000000000000, 1.000000000000000222, 1.000000000000000000, 1.000000000000000000, 0.9999999999999997780, 1.000000000000000000, 1.000000000000000444, 0.9999999999999996669, 1.000000000000000222, 0.9999999999999997780, 1.000000000000000000, 0.9999999999999997780, 1.000000000000000222, 1.000000000000000222, 1.000000000000000000, 1.000000000000000000, 0.9999999999999996669, 1.000000000000000444, 0.9999999999999997780, 1.000000000000000000, 1.000000000000000222, 0.9999999999999996669, 1.000000000000000444, 1.000000000000000000, 0.9999999999999997780, 1.000000000000000222, 0.9999999999999997780, 1.000000000000000000, 1.000000000000000000, 1.000000000000000000, 1.000000000000000000, 1.000000000000000000, 1.000000000000000222, 1.000000000000000444, 0.9999999999999997780, 1.000000000000000222, 1.000000000000000000, 1.000000000000000444, 0.9999999999999997780, 1.000000000000000222, 0.9999999999999997780, 1.000000000000000222, 0.9999999999999997780, 1.000000000000000222, 1.000000000000000000, 1.000000000000000222, 1.000000000000000222, 1.000000000000000222, 0.9999999999999997780, 1.000000000000000222, 0.9999999999999997780, 1.000000000000000222, 0.9999999999999997780, 1.000000000000000444, 0.9999999999999996669, 1.000000000000000444, 1.000000000000000000, 1.000000000000000000, 0.9999999999999997780, 1.000000000000000222, 1.000000000000000000, 0.9999999999999997780, 1.000000000000000000, 0.9999999999999997780, 1.000000000000000222, 1.000000000000000000, 1.000000000000000000, 1.000000000000000222, 0.9999999999999997780, 1.000000000000000444, 0.9999999999999996669, 1.000000000000000222, 1.000000000000000222, 0.9999999999999997780, 1.000000000000000000, 0.9999999999999997780, 1.000000000000000000, 0.9999999999999996669, 1.000000000000000444, 0.9999999999999997780, 1.000000000000000222, 1.000000000000000000, 1.000000000000000000, 1.000000000000000000, 0.9999999999999997780, 0.9999999999999997780, 1.000000000000000000, 0.9999999999999997780, 1.000000000000000444, 0.9999999999999996669, 1.000000000000000222, 1.000000000000000000, 1.000000000000000444, 1.000000000000000222, 1.000000000000000000, 0.9999999999999997780, 1.000000000000000222, 1.000000000000000444, 0.9999999999999997780, 1.000000000000000222, 0.9999999999999997780, 1.000000000000000000, 1.000000000000000000, 1.000000000000000222, 0.9999999999999997780, 1.000000000000000222, 1.000000000000000000, 1.000000000000000222, 0.9999999999999997780, 1.000000000000000000, 1.000000000000000222, 1.000000000000000000, 1.000000000000000222, 1.000000000000000000, 1.000000000000000000, 0.9999999999999997780, 1.000000000000000444, 0.9999999999999997780, 1.000000000000000000, 1.000000000000000000, 1.000000000000000444, 0.9999999999999996669, 1.000000000000000222, 1.000000000000000000, 0.9999999999999996669, 1.000000000000000444, 0.9999999999999996669, 1.000000000000000444, 0.9999999999999997780, 1.000000000000000222, 0.9999999999999997780, 1.000000000000000222, 1.000000000000000222, 1.000000000000000222, 1.000000000000000000, 1.000000000000000000, 1.000000000000000000),
 ( 0.3333333333333333703, 0.3333333333333333703, 0.3333333333333334259, 0.3333333333333334259, 0.3333333333333333703, 0.3333333333333334259, 0.3333333333333333148, 0.3333333333333333703, 0.3333333333333333148, 0.3333333333333333703, 0.3333333333333333703, 0.3333333333333334259, 0.3333333333333333703, 0.3333333333333333703, 0.3333333333333333703, 0.3333333333333333703, 0.3333333333333333703, 0.3333333333333333148, 0.3333333333333333703, 0.3333333333333334814, 0.3333333333333333148, 0.3333333333333334259, 0.3333333333333333148, 0.3333333333333334259, 0.3333333333333332593, 0.3333333333333335369, 0.3333333333333333703, 0.3333333333333333703, 0.3333333333333333703, 0.3333333333333333703, 0.3333333333333333703, 0.3333333333333333703, 0.3333333333333334259, 0.3333333333333333703, 0.3333333333333333703, 0.3333333333333333703, 0.3333333333333334814, 0.3333333333333333703, 0.3333333333333333703, 0.3333333333333333703, 0.3333333333333334259, 0.3333333333333332593, 0.3333333333333334814, 0.3333333333333332593, 0.3333333333333334259, 0.3333333333333332038, 0.3333333333333335369, 0.3333333333333332593, 0.3333333333333334814, 0.3333333333333333703, 0.3333333333333333148, 0.3333333333333333703, 0.3333333333333333703, 0.3333333333333333148, 0.3333333333333333148, 0.3333333333333334814, 0.3333333333333332593, 0.3333333333333334259, 0.3333333333333332593, 0.3333333333333333703, 0.3333333333333333703, 0.3333333333333334259, 0.3333333333333333148, 0.3333333333333333148, 0.3333333333333334259, 0.3333333333333333703, 0.3333333333333333703, 0.3333333333333333703, 0.3333333333333334814, 0.3333333333333332038, 0.3333333333333335924, 0.3333333333333332593, 0.3333333333333335369, 0.3333333333333333148, 0.3333333333333332593, 0.3333333333333335924, 0.3333333333333332038, 0.3333333333333333703, 0.3333333333333333703, 0.3333333333333334259, 0.3333333333333333148, 0.3333333333333334259, 0.3333333333333333703, 0.3333333333333334259, 0.3333333333333332038, 0.3333333333333333703, 0.3333333333333333703, 0.3333333333333333703, 0.3333333333333332593, 0.3333333333333333703, 0.3333333333333333148, 0.3333333333333334259, 0.3333333333333333148, 0.3333333333333334259, 0.3333333333333333148, 0.3333333333333334814, 0.3333333333333333703, 0.3333333333333334259, 0.3333333333333333703, 0.3333333333333333148, 0.3333333333333333703, 0.3333333333333334259, 0.3333333333333333148, 0.3333333333333334814, 0.3333333333333334259, 0.3333333333333333703, 0.3333333333333334259, 0.3333333333333333703, 0.3333333333333334259, 0.3333333333333334814, 0.3333333333333332038, 0.3333333333333334259, 0.3333333333333334259, 0.3333333333333333703, 0.3333333333333333148, 0.3333333333333334259, 0.3333333333333334259, 0.3333333333333334259, 0.3333333333333333703, 0.3333333333333333148, 0.3333333333333334259, 0.3333333333333333703, 0.3333333333333334259, 0.3333333333333333703, 0.3333333333333333148, 0.3333333333333332593, 0.3333333333333334259, 0.3333333333333333148, 0.3333333333333335369, 0.3333333333333332593, 0.3333333333333334814, 0.3333333333333334259, 0.3333333333333334259, 0.3333333333333333148, 0.3333333333333334259, 0.3333333333333333148, 0.3333333333333333148, 0.3333333333333333703, 0.3333333333333333703, 0.3333333333333332593, 0.3333333333333334259, 0.3333333333333333148, 0.3333333333333333703, 0.3333333333333334259, 0.3333333333333333148, 0.3333333333333334814, 0.3333333333333332593, 0.3333333333333333703, 0.3333333333333334259, 0.3333333333333332038, 0.3333333333333335369, 0.3333333333333333703, 0.3333333333333333703, 0.3333333333333333148, 0.3333333333333334259, 0.3333333333333333703, 0.3333333333333332593, 0.3333333333333335369, 0.3333333333333332593, 0.3333333333333333703, 0.3333333333333334814, 0.3333333333333333703, 0.3333333333333334259, 0.3333333333333332593, 0.3333333333333334259, 0.3333333333333332593, 0.3333333333333333703, 0.3333333333333334259, 0.3333333333333333703, 0.3333333333333334814, 0.3333333333333332593, 0.3333333333333333703, 0.3333333333333333703, 0.3333333333333333703, 0.3333333333333334259, 0.3333333333333333148, 0.3333333333333334259, 0.3333333333333332593, 0.3333333333333333703, 0.3333333333333332593, 0.3333333333333334814, 0.3333333333333333703, 0.3333333333333334259, 0.3333333333333334259, 0.3333333333333332593, 0.3333333333333334814, 0.3333333333333333148, 0.3333333333333333148, 0.3333333333333333148, 0.3333333333333333703, 0.3333333333333333703, 0.3333333333333334259, 0.3333333333333332593, 0.3333333333333335369, 0.3333333333333332038, 0.3333333333333335924, 0.3333333333333332593, 0.3333333333333334814, 0.3333333333333333703, 0.3333333333333333703, 0.3333333333333333703, 0.3333333333333333148, 0.3333333333333334259, 0.3333333333333333703, 0.3333333333333333703, 0.3333333333333333148, 0.3333333333333333703, 0.3333333333333333148, 0.3333333333333333703, 0.3333333333333332593, 0.3333333333333334259, 0.3333333333333333703, 0.3333333333333334259, 0.3333333333333333148, 0.3333333333333334259, 0.3333333333333333703, 0.3333333333333334259, 0.3333333333333334259, 0.3333333333333334259, 0.3333333333333332593, 0.3333333333333334259, 0.3333333333333333703, 0.3333333333333333148, 0.3333333333333333148, 0.3333333333333335369, 0.3333333333333332593, 0.3333333333333333148, 0.3333333333333333703, 0.3333333333333333148, 0.3333333333333334814, 0.3333333333333333703, 0.3333333333333334814, 0.3333333333333333703, 0.3333333333333332593, 0.3333333333333334259, 0.3333333333333333703, 0.3333333333333335369, 0.3333333333333333148, 0.3333333333333334259, 0.3333333333333333148, 0.3333333333333335924, 0.3333333333333332593, 0.3333333333333334259, 0.3333333333333334259, 0.3333333333333333703, 0.3333333333333333703, 0.3333333333333334259, 0.3333333333333334259, 0.3333333333333334259, 0.3333333333333333703, 0.3333333333333333703, 0.3333333333333334259, 0.3333333333333333148, 0.3333333333333333703, 0.3333333333333332038, 0.3333333333333334259, 0.3333333333333334814, 0.3333333333333332593, 0.3333333333333333703, 0.3333333333333333148, 0.3333333333333334814, 0.3333333333333332593, 0.3333333333333334259, 0.3333333333333333703, 0.3333333333333333703, 0.3333333333333333703, 0.3333333333333333148, 0.3333333333333334259, 0.3333333333333333703, 0.3333333333333333148, 0.3333333333333334259, 0.3333333333333332038, 0.3333333333333334259, 0.3333333333333333703, 0.3333333333333333703, 0.3333333333333333703, 0.3333333333333334259, 0.3333333333333333148, 0.3333333333333333703, 0.3333333333333333703, 0.3333333333333333703, 0.3333333333333333703, 0.3333333333333334259, 0.3333333333333334814, 0.3333333333333332593, 0.3333333333333333703, 0.3333333333333334259, 0.3333333333333334814, 0.3333333333333333148, 0.3333333333333333703, 0.3333333333333333703, 0.3333333333333334259, 0.3333333333333333148, 0.3333333333333334814, 0.3333333333333333148, 0.3333333333333334814, 0.3333333333333333703, 0.3333333333333334814, 0.3333333333333333148, 0.3333333333333334259, 0.3333333333333332593, 0.3333333333333335369, 0.3333333333333333148, 0.3333333333333334814, 0.3333333333333333148, 0.3333333333333334259, 0.3333333333333333703, 0.3333333333333333148, 0.3333333333333333703, 0.3333333333333333703, 0.3333333333333334259, 0.3333333333333333148, 0.3333333333333334259, 0.3333333333333333148, 0.3333333333333334814, 0.3333333333333333148, 0.3333333333333334259, 0.3333333333333334259, 0.3333333333333333703, 0.3333333333333334259, 0.3333333333333333703, 0.3333333333333333703, 0.3333333333333335369, 0.3333333333333332593, 0.3333333333333334259, 0.3333333333333333703, 0.3333333333333333703, 0.3333333333333333148, 0.3333333333333335369, 0.3333333333333333148, 0.3333333333333334259, 0.3333333333333333703, 0.3333333333333333703, 0.3333333333333334259, 0.3333333333333333148, 0.3333333333333333703, 0.3333333333333333148, 0.3333333333333333148, 0.3333333333333334814, 0.3333333333333332593, 0.3333333333333334259, 0.3333333333333333703, 0.3333333333333334814, 0.3333333333333334259, 0.3333333333333333148, 0.3333333333333333703, 0.3333333333333333703, 0.3333333333333335369, 0.3333333333333333148, 0.3333333333333334259, 0.3333333333333333703, 0.3333333333333333148, 0.3333333333333334259, 0.3333333333333334259, 0.3333333333333333703, 0.3333333333333333703, 0.3333333333333334259, 0.3333333333333334259, 0.3333333333333333703, 0.3333333333333333148, 0.3333333333333334259, 0.3333333333333333703, 0.3333333333333334814, 0.3333333333333333703, 0.3333333333333333703, 0.3333333333333333703, 0.3333333333333334259, 0.3333333333333333148, 0.3333333333333333703, 0.3333333333333334259, 0.3333333333333334259, 0.3333333333333333148, 0.3333333333333333703, 0.3333333333333333148, 0.3333333333333333703, 0.3333333333333335369, 0.3333333333333333148, 0.3333333333333334259, 0.3333333333333333703, 0.3333333333333334259, 0.3333333333333333148, 0.3333333333333333148, 0.3333333333333335369, 0.3333333333333333703, 0.3333333333333333148, 0.3333333333333333703, 0.3333333333333333703),
 ( 0.3333333333333333703, 0.3333333333333333703, 0.3333333333333334259, 0.3333333333333334259, 0.3333333333333333703, 0.3333333333333334259, 0.3333333333333333148, 0.3333333333333333703, 0.3333333333333333148, 0.3333333333333333703, 0.3333333333333333703, 0.3333333333333334259, 0.3333333333333333703, 0.3333333333333333703, 0.3333333333333333703, 0.3333333333333333703, 0.3333333333333333703, 0.3333333333333333148, 0.3333333333333333703, 0.3333333333333334814, 0.3333333333333333148, 0.3333333333333334259, 0.3333333333333333148, 0.3333333333333334259, 0.3333333333333332593, 0.3333333333333335369, 0.3333333333333333703, 0.3333333333333333703, 0.3333333333333333703, 0.3333333333333333703, 0.3333333333333333703, 0.3333333333333333703, 0.3333333333333334259, 0.3333333333333333703, 0.3333333333333333703, 0.3333333333333333703, 0.3333333333333334814, 0.3333333333333333703, 0.3333333333333333703, 0.3333333333333333703, 0.3333333333333334259, 0.3333333333333332593, 0.3333333333333334814, 0.3333333333333332593, 0.3333333333333334259, 0.3333333333333332038, 0.3333333333333335369, 0.3333333333333332593, 0.3333333333333334814, 0.3333333333333333703, 0.3333333333333333148, 0.3333333333333333703, 0.3333333333333333703, 0.3333333333333333148, 0.3333333333333333148, 0.3333333333333334814, 0.3333333333333332593, 0.3333333333333334259, 0.3333333333333332593, 0.3333333333333333703, 0.3333333333333333703, 0.3333333333333334259, 0.3333333333333333148, 0.3333333333333333148, 0.3333333333333334259, 0.3333333333333333703, 0.3333333333333333703, 0.3333333333333333703, 0.3333333333333334814, 0.3333333333333332038, 0.3333333333333335924, 0.3333333333333332593, 0.3333333333333335369, 0.3333333333333333148, 0.3333333333333332593, 0.3333333333333335924, 0.3333333333333332038, 0.3333333333333333703, 0.3333333333333333703, 0.3333333333333334259, 0.3333333333333333148, 0.3333333333333334259, 0.3333333333333333703, 0.3333333333333334259, 0.3333333333333332038, 0.3333333333333333703, 0.3333333333333333703, 0.3333333333333333703, 0.3333333333333332593, 0.3333333333333333703, 0.3333333333333333148, 0.3333333333333334259, 0.3333333333333333148, 0.3333333333333334259, 0.3333333333333333148, 0.3333333333333334814, 0.3333333333333333703, 0.3333333333333334259, 0.3333333333333333703, 0.3333333333333333148, 0.3333333333333333703, 0.3333333333333334259, 0.3333333333333333148, 0.3333333333333334814, 0.3333333333333334259, 0.3333333333333333703, 0.3333333333333334259, 0.3333333333333333703, 0.3333333333333334259, 0.3333333333333334814, 0.3333333333333332038, 0.3333333333333334259, 0.3333333333333334259, 0.3333333333333333703, 0.3333333333333333148, 0.3333333333333334259, 0.3333333333333334259, 0.3333333333333334259, 0.3333333333333333703, 0.3333333333333333148, 0.3333333333333334259, 0.3333333333333333703, 0.3333333333333334259, 0.3333333333333333703, 0.3333333333333333148, 0.3333333333333332593, 0.3333333333333334259, 0.3333333333333333148, 0.3333333333333335369, 0.3333333333333332593, 0.3333333333333334814, 0.3333333333333334259, 0.3333333333333334259, 0.3333333333333333148, 0.3333333333333334259, 0.3333333333333333148, 0.3333333333333333148, 0.3333333333333333703, 0.3333333333333333703, 0.3333333333333332593, 0.3333333333333334259, 0.3333333333333333148, 0.3333333333333333703, 0.3333333333333334259, 0.3333333333333333148, 0.3333333333333334814, 0.3333333333333332593, 0.3333333333333333703, 0.3333333333333334259, 0.3333333333333332038, 0.3333333333333335369, 0.3333333333333333703, 0.3333333333333333703, 0.3333333333333333148, 0.3333333333333334259, 0.3333333333333333703, 0.3333333333333332593, 0.3333333333333335369, 0.3333333333333332593, 0.3333333333333333703, 0.3333333333333334814, 0.3333333333333333703, 0.3333333333333334259, 0.3333333333333332593, 0.3333333333333334259, 0.3333333333333332593, 0.3333333333333333703, 0.3333333333333334259, 0.3333333333333333703, 0.3333333333333334814, 0.3333333333333332593, 0.3333333333333333703, 0.3333333333333333703, 0.3333333333333333703, 0.3333333333333334259, 0.3333333333333333148, 0.3333333333333334259, 0.3333333333333332593, 0.3333333333333333703, 0.3333333333333332593, 0.3333333333333334814, 0.3333333333333333703, 0.3333333333333334259, 0.3333333333333334259, 0.3333333333333332593, 0.3333333333333334814, 0.3333333333333333148, 0.3333333333333333148, 0.3333333333333333148, 0.3333333333333333703, 0.3333333333333333703, 0.3333333333333334259, 0.3333333333333332593, 0.3333333333333335369, 0.3333333333333332038, 0.3333333333333335924, 0.3333333333333332593, 0.3333333333333334814, 0.3333333333333333703, 0.3333333333333333703, 0.3333333333333333703, 0.3333333333333333148, 0.3333333333333334259, 0.3333333333333333703, 0.3333333333333333703, 0.3333333333333333148, 0.3333333333333333703, 0.3333333333333333148, 0.3333333333333333703, 0.3333333333333332593, 0.3333333333333334259, 0.3333333333333333703, 0.3333333333333334259, 0.3333333333333333148, 0.3333333333333334259, 0.3333333333333333703, 0.3333333333333334259, 0.3333333333333334259, 0.3333333333333334259, 0.3333333333333332593, 0.3333333333333334259, 0.3333333333333333703, 0.3333333333333333148, 0.3333333333333333148, 0.3333333333333335369, 0.3333333333333332593, 0.3333333333333333148, 0.3333333333333333703, 0.3333333333333333148, 0.3333333333333334814, 0.3333333333333333703, 0.3333333333333334814, 0.3333333333333333703, 0.3333333333333332593, 0.3333333333333334259, 0.3333333333333333703, 0.3333333333333335369, 0.3333333333333333148, 0.3333333333333334259, 0.3333333333333333148, 0.3333333333333335924, 0.3333333333333332593, 0.3333333333333334259, 0.3333333333333334259, 0.3333333333333333703, 0.3333333333333333703, 0.3333333333333334259, 0.3333333333333334259, 0.3333333333333334259, 0.3333333333333333703, 0.3333333333333333703, 0.3333333333333334259, 0.3333333333333333148, 0.3333333333333333703, 0.3333333333333332038, 0.3333333333333334259, 0.3333333333333334814, 0.3333333333333332593, 0.3333333333333333703, 0.3333333333333333148, 0.3333333333333334814, 0.3333333333333332593, 0.3333333333333334259, 0.3333333333333333703, 0.3333333333333333703, 0.3333333333333333703, 0.3333333333333333148, 0.3333333333333334259, 0.3333333333333333703, 0.3333333333333333148, 0.3333333333333334259, 0.3333333333333332038, 0.3333333333333334259, 0.3333333333333333703, 0.3333333333333333703, 0.3333333333333333703, 0.3333333333333334259, 0.3333333333333333148, 0.3333333333333333703, 0.3333333333333333703, 0.3333333333333333703, 0.3333333333333333703, 0.3333333333333334259, 0.3333333333333334814, 0.3333333333333332593, 0.3333333333333333703, 0.3333333333333334259, 0.3333333333333334814, 0.3333333333333333148, 0.3333333333333333703, 0.3333333333333333703, 0.3333333333333334259, 0.3333333333333333148, 0.3333333333333334814, 0.3333333333333333148, 0.3333333333333334814, 0.3333333333333333703, 0.3333333333333334814, 0.3333333333333333148, 0.3333333333333334259, 0.3333333333333332593, 0.3333333333333335369, 0.3333333333333333148, 0.3333333333333334814, 0.3333333333333333148, 0.3333333333333334259, 0.3333333333333333703, 0.3333333333333333148, 0.3333333333333333703, 0.3333333333333333703, 0.3333333333333334259, 0.3333333333333333148, 0.3333333333333334259, 0.3333333333333333148, 0.3333333333333334814, 0.3333333333333333148, 0.3333333333333334259, 0.3333333333333334259, 0.3333333333333333703, 0.3333333333333334259, 0.3333333333333333703, 0.3333333333333333703, 0.3333333333333335369, 0.3333333333333332593, 0.3333333333333334259, 0.3333333333333333703, 0.3333333333333333703, 0.3333333333333333148, 0.3333333333333335369, 0.3333333333333333148, 0.3333333333333334259, 0.3333333333333333703, 0.3333333333333333703, 0.3333333333333334259, 0.3333333333333333148, 0.3333333333333333703, 0.3333333333333333148, 0.3333333333333333148, 0.3333333333333334814, 0.3333333333333332593, 0.3333333333333334259, 0.3333333333333333703, 0.3333333333333334814, 0.3333333333333334259, 0.3333333333333333148, 0.3333333333333333703, 0.3333333333333333703, 0.3333333333333335369, 0.3333333333333333148, 0.3333333333333334259, 0.3333333333333333703, 0.3333333333333333148, 0.3333333333333334259, 0.3333333333333334259, 0.3333333333333333703, 0.3333333333333333703, 0.3333333333333334259, 0.3333333333333334259, 0.3333333333333333703, 0.3333333333333333148, 0.3333333333333334259, 0.3333333333333333703, 0.3333333333333334814, 0.3333333333333333703, 0.3333333333333333703, 0.3333333333333333703, 0.3333333333333334259, 0.3333333333333333148, 0.3333333333333333703, 0.3333333333333334259, 0.3333333333333334259, 0.3333333333333333148, 0.3333333333333333703, 0.3333333333333333148, 0.3333333333333333703, 0.3333333333333335369, 0.3333333333333333148, 0.3333333333333334259, 0.3333333333333333703, 0.3333333333333334259, 0.3333333333333333148, 0.3333333333333333148, 0.3333333333333335369, 0.3333333333333333703, 0.3333333333333333148, 0.3333333333333333703, 0.3333333333333333703),
 ( 1.000000000000000000, 1.000000000000000000, 1.000000000000000000, 1.000000000000000222, 0.9999999999999997780, 1.000000000000000444, 0.9999999999999997780, 1.000000000000000222, 0.9999999999999996669, 1.000000000000000000, 1.000000000000000000, 1.000000000000000222, 1.000000000000000000, 1.000000000000000000, 0.9999999999999997780, 1.000000000000000000, 1.000000000000000000, 1.000000000000000000, 0.9999999999999997780, 1.000000000000000444, 0.9999999999999997780, 1.000000000000000222, 1.000000000000000000, 0.9999999999999997780, 1.000000000000000000, 1.000000000000000222, 0.9999999999999997780, 1.000000000000000222, 0.9999999999999997780, 1.000000000000000222, 1.000000000000000000, 0.9999999999999997780, 1.000000000000000444, 0.9999999999999997780, 1.000000000000000222, 0.9999999999999997780, 1.000000000000000444, 1.000000000000000000, 1.000000000000000000, 1.000000000000000000, 1.000000000000000000, 1.000000000000000000, 1.000000000000000000, 0.9999999999999997780, 1.000000000000000222, 0.9999999999999996669, 1.000000000000000444, 0.9999999999999994449, 1.000000000000000222, 1.000000000000000000, 1.000000000000000000, 1.000000000000000000, 1.000000000000000000, 1.000000000000000000, 0.9999999999999996669, 1.000000000000000444, 0.9999999999999997780, 1.000000000000000222, 0.9999999999999996669, 1.000000000000000000, 1.000000000000000000, 1.000000000000000222, 0.9999999999999997780, 1.000000000000000000, 1.000000000000000222, 0.9999999999999997780, 1.000000000000000000, 0.9999999999999997780, 1.000000000000000222, 0.9999999999999997780, 1.000000000000000444, 0.9999999999999994449, 1.000000000000000444, 0.9999999999999997780, 0.9999999999999997780, 1.000000000000000444, 0.9999999999999996669, 1.000000000000000000, 1.000000000000000000, 1.000000000000000000, 1.000000000000000000, 1.000000000000000222, 1.000000000000000000, 1.000000000000000000, 0.9999999999999996669, 1.000000000000000222, 1.000000000000000000, 0.9999999999999997780, 0.9999999999999997780, 0.9999999999999997780, 1.000000000000000000, 1.000000000000000222, 0.9999999999999997780, 1.000000000000000222, 0.9999999999999996669, 1.000000000000000444, 0.9999999999999997780, 1.000000000000000222, 1.000000000000000222, 0.9999999999999997780, 1.000000000000000222, 1.000000000000000000, 0.9999999999999997780, 1.000000000000000444, 1.000000000000000000, 1.000000000000000000, 1.000000000000000222, 1.000000000000000000, 1.000000000000000000, 1.000000000000000222, 0.9999999999999993339, 1.000000000000000444, 1.000000000000000222, 0.9999999999999997780, 1.000000000000000000, 1.000000000000000222, 1.000000000000000444, 1.000000000000000000, 1.000000000000000222, 0.9999999999999997780, 1.000000000000000222, 0.9999999999999997780, 1.000000000000000222, 1.000000000000000000, 0.9999999999999997780, 0.9999999999999996669, 1.000000000000000444, 0.9999999999999997780, 1.000000000000000444, 0.9999999999999997780, 1.000000000000000222, 1.000000000000000222, 1.000000000000000000, 0.9999999999999997780, 1.000000000000000222, 0.9999999999999997780, 1.000000000000000000, 1.000000000000000000, 1.000000000000000000, 0.9999999999999997780, 1.000000000000000222, 1.000000000000000000, 1.000000000000000000, 1.000000000000000000, 1.000000000000000222, 1.000000000000000222, 0.9999999999999994449, 1.000000000000000222, 1.000000000000000000, 0.9999999999999994449, 1.000000000000000444, 0.9999999999999997780, 1.000000000000000222, 0.9999999999999996669, 1.000000000000000444, 1.000000000000000000, 0.9999999999999996669, 1.000000000000000444, 0.9999999999999997780, 1.000000000000000000, 1.000000000000000444, 1.000000000000000000, 1.000000000000000222, 0.9999999999999996669, 1.000000000000000000, 0.9999999999999997780, 0.9999999999999997780, 1.000000000000000222, 1.000000000000000000, 1.000000000000000444, 0.9999999999999996669, 1.000000000000000222, 0.9999999999999997780, 0.9999999999999997780, 1.000000000000000444, 0.9999999999999997780, 1.000000000000000444, 0.9999999999999996669, 1.000000000000000222, 0.9999999999999996669, 1.000000000000000222, 0.9999999999999997780, 1.000000000000000444, 1.000000000000000222, 0.9999999999999996669, 1.000000000000000444, 0.9999999999999996669, 1.000000000000000000, 0.9999999999999997780, 1.000000000000000000, 1.000000000000000000, 1.000000000000000222, 0.9999999999999994449, 1.000000000000000444, 0.9999999999999993339, 1.000000000000000666, 0.9999999999999994449, 1.000000000000000222, 1.000000000000000222, 1.000000000000000000, 1.000000000000000000, 0.9999999999999997780, 1.000000000000000222, 0.9999999999999996669, 1.000000000000000222, 0.9999999999999996669, 1.000000000000000222, 1.000000000000000000, 1.000000000000000222, 0.9999999999999997780, 1.000000000000000222, 1.000000000000000222, 1.000000000000000000, 0.9999999999999997780, 1.000000000000000222, 1.000000000000000222, 1.000000000000000000, 1.000000000000000000, 1.000000000000000222, 0.9999999999999997780, 1.000000000000000000, 1.000000000000000222, 0.9999999999999996669, 0.9999999999999997780, 1.000000000000000222, 0.9999999999999997780, 1.000000000000000000, 0.9999999999999997780, 0.9999999999999997780, 1.000000000000000222, 1.000000000000000000, 1.000000000000000000, 1.000000000000000222, 0.9999999999999996669, 1.000000000000000444, 1.000000000000000000, 1.000000000000000222, 0.9999999999999997780, 1.000000000000000222, 0.9999999999999997780, 1.000000000000000444, 0.9999999999999997780, 1.000000000000000222, 0.9999999999999997780, 1.000000000000000222, 0.9999999999999997780, 1.000000000000000222, 1.000000000000000000, 1.000000000000000222, 1.000000000000000000, 1.000000000000000000, 1.000000000000000222, 1.000000000000000000, 1.000000000000000000, 0.9999999999999997780, 1.000000000000000000, 1.000000000000000444, 0.9999999999999996669, 1.000000000000000222, 0.9999999999999997780, 1.000000000000000000, 0.9999999999999997780, 1.000000000000000222, 1.000000000000000222, 1.000000000000000000, 1.000000000000000000, 0.9999999999999996669, 1.000000000000000444, 0.9999999999999997780, 1.000000000000000000, 1.000000000000000222, 0.9999999999999996669, 1.000000000000000444, 1.000000000000000000, 0.9999999999999997780, 1.000000000000000222, 0.9999999999999997780, 1.000000000000000000, 1.000000000000000000, 1.000000000000000000, 1.000000000000000000, 1.000000000000000000, 1.000000000000000222, 1.000000000000000444, 0.9999999999999997780, 1.000000000000000222, 1.000000000000000000, 1.000000000000000444, 0.9999999999999997780, 1.000000000000000222, 0.9999999999999997780, 1.000000000000000222, 0.9999999999999997780, 1.000000000000000222, 1.000000000000000000, 1.000000000000000222, 1.000000000000000222, 1.000000000000000222, 0.9999999999999997780, 1.000000000000000222, 0.9999999999999997780, 1.000000000000000222, 0.9999999999999997780, 1.000000000000000444, 0.9999999999999996669, 1.000000000000000444, 1.000000000000000000, 1.000000000000000000, 0.9999999999999997780, 1.000000000000000222, 1.000000000000000000, 0.9999999999999997780, 1.000000000000000000, 0.9999999999999997780, 1.000000000000000222, 1.000000000000000000, 1.000000000000000000, 1.000000000000000222, 0.9999999999999997780, 1.000000000000000444, 0.9999999999999996669, 1.000000000000000222, 1.000000000000000222, 0.9999999999999997780, 1.000000000000000000, 0.9999999999999997780, 1.000000000000000000, 0.9999999999999996669, 1.000000000000000444, 0.9999999999999997780, 1.000000000000000222, 1.000000000000000000, 1.000000000000000000, 1.000000000000000000, 0.9999999999999997780, 0.9999999999999997780, 1.000000000000000000, 0.9999999999999997780, 1.000000000000000444, 0.9999999999999996669, 1.000000000000000222, 1.000000000000000000, 1.000000000000000444, 1.000000000000000222, 1.000000000000000000, 0.9999999999999997780, 1.000000000000000222, 1.000000000000000444, 0.9999999999999997780, 1.000000000000000222, 0.9999999999999997780, 1.000000000000000000, 1.000000000000000000, 1.000000000000000222, 0.9999999999999997780, 1.000000000000000222, 1.000000000000000000, 1.000000000000000222, 0.9999999999999997780, 1.000000000000000000, 1.000000000000000222, 1.000000000000000000, 1.000000000000000222, 1.000000000000000000, 1.000000000000000000, 0.9999999999999997780, 1.000000000000000444, 0.9999999999999997780, 1.000000000000000000, 1.000000000000000000, 1.000000000000000444, 0.9999999999999996669, 1.000000000000000222, 1.000000000000000000, 0.9999999999999996669, 1.000000000000000444, 0.9999999999999996669, 1.000000000000000444, 0.9999999999999997780, 1.000000000000000222, 0.9999999999999997780, 1.000000000000000222, 1.000000000000000222, 1.000000000000000222, 1.000000000000000000, 1.000000000000000000, 1.000000000000000000) ) ) 
 REPRESENTATION_ITEM ( '' )  SURFACE ( )  );
#13144=CARTESIAN_POINT ( 'NONE',  ( 1.487047289068929246, 2.092300142875534341, 0.5796043027312002272 ) ) ;
#13145=CARTESIAN_POINT ( 'NONE',  ( 2.219935720625454412, 0.9462983093676997637, -1.780669029686342331 ) ) ;
#13146=CARTESIAN_POINT ( 'NONE',  ( 5.406250000000002665, 1.895863743163962223, -0.7852924748302683167 ) ) ;
#13148=CARTESIAN_POINT ( 'NONE',  ( 6.516243422921982109, -0.9108434941001318785, -1.697579817862464147 ) ) ;
#13150=CARTESIAN_POINT ( 'NONE',  ( 3.041495853084168921, 0.05845243686668395028, 2.220815690970390222 ) ) ;
#13156=AXIS2_PLACEMENT_3D ( 'NONE', #103741, #87490, #6203 ) ;
#13157=CARTESIAN_POINT ( 'NONE',  ( 5.671390581117805141, 1.043574818874394294, 1.392714124641497131 ) ) ;
#13158=CARTESIAN_POINT ( 'NONE',  ( 3.824618516750320385, -1.319357783791510919, 1.452116237791359232 ) ) ;
#13162=CARTESIAN_POINT ( 'NONE',  ( 4.165478197628463164, 0.2823181557158191968, -2.244685958880874743 ) ) ;
#13163=CARTESIAN_POINT ( 'NONE',  ( 1.715356188534086224, -1.767971037936959089, -1.062312629515406170 ) ) ;
#13165=CARTESIAN_POINT ( 'NONE',  ( 2.712116605023757288, -2.238012884330255581, 0.3312714459411686962 ) ) ;
#13168=CARTESIAN_POINT ( 'NONE',  ( 3.901501827272614964, -0.5455803081039903857, 1.789184164884791706 ) ) ;
#13169=CARTESIAN_POINT ( 'NONE',  ( 2.215074966175926363, 1.682300057933778126, 0.4202854259360877531 ) ) ;
#13170=CARTESIAN_POINT ( 'NONE',  ( 6.515165533258342023, -2.126321577054360201, 0.5302794918828001025 ) ) ;
#13171=CARTESIAN_POINT ( 'NONE',  ( 6.458097596740710600, 2.302054065074070177, -0.1608065221961554325 ) ) ;
#13173=CARTESIAN_POINT ( 'NONE',  ( 3.749029689823797806, -1.768526636652943296, 1.242828150824742961 ) ) ;
#13174=CARTESIAN_POINT ( 'NONE',  ( 5.015543440151827959, -1.040391601716946557, -1.639569664018299289 ) ) ;
#13176=CARTESIAN_POINT ( 'NONE',  ( 6.344977084850584426, -1.580176071495458023, 1.000667393836668362 ) ) ;
#13183=CARTESIAN_POINT ( 'NONE',  ( 5.590470263882489910, -0.4872053753022275169, 1.956560708789633285 ) ) ;
#13187=CARTESIAN_POINT ( 'NONE',  ( 3.387140609607977026, 1.650079954178599539, -0.7815607168924765258 ) ) ;
#13194=CARTESIAN_POINT ( 'NONE',  ( 0.6330766797960291070, 1.867852534778514428, 0.7690482435470397116 ) ) ;
#13195=CARTESIAN_POINT ( 'NONE',  ( 1.366058183223411771, 0.6122477967837879342, -2.030190212274018524 ) ) ;
#13198=CARTESIAN_POINT ( 'NONE',  ( 2.342426049922683884, -1.823874001192757666, -0.3686824239186973218 ) ) ;
#13200=CARTESIAN_POINT ( 'NONE',  ( 6.473517581629535833, 1.972881934646727231, -0.5958391983454867091 ) ) ;
#13201=CARTESIAN_POINT ( 'NONE',  ( 6.029922689959810178, -1.701949372586025744, 1.081063231324945528 ) ) ;
#13206=CARTESIAN_POINT ( 'NONE',  ( 3.914527900857078357, 1.289819402409349669, -1.292354223553587644 ) ) ;
#13212=CARTESIAN_POINT ( 'NONE',  ( 5.923203835008548523, 0.8145033986626595279, 1.844426808122232142 ) ) ;
#13213=CARTESIAN_POINT ( 'NONE',  ( 5.402248404572855378, 1.391679675130308880, -1.205515946264820615 ) ) ;
#13214=CARTESIAN_POINT ( 'NONE',  ( 0.07680821025391781909, 4.096870002413341538, -2.365840309731046975 ) ) ;
#13215=CARTESIAN_POINT ( 'NONE',  ( 3.809432652880593739, 1.978559473273227232, 1.187534574604662607 ) ) ;
#13217=CARTESIAN_POINT ( 'NONE',  ( 5.571600594950134600, 2.084881007647599205, -0.5705972643132785072 ) ) ;
#13219=CARTESIAN_POINT ( 'NONE',  ( 0.8900594323104525918, -0.4731300603538539096, -1.883416623991182481 ) ) ;
#13221=CARTESIAN_POINT ( 'NONE',  ( 4.165566195501821056, -0.7159155550505342802, -2.184124419653421523 ) ) ;
#13224=CARTESIAN_POINT ( 'NONE',  ( 4.627732503263369601, -1.150995203733524930, -1.474563928533303869 ) ) ;
#13227=CARTESIAN_POINT ( 'NONE',  ( 1.863391182279940494, -1.538030936729195552, -1.136358088520472931 ) ) ;
#13230=CARTESIAN_POINT ( 'NONE',  ( 4.073040751519330094, -2.058760688187323495, -0.7953439701907027981 ) ) ;
#13232=CARTESIAN_POINT ( 'NONE',  ( 6.883263157960408662, 2.979503955789930547, 2.299731230128279513 ) ) ;
#13237=CARTESIAN_POINT ( 'NONE',  ( 2.003138245156708130, 1.636809484843353868, 1.098402624201348488 ) ) ;
#13238=CARTESIAN_POINT ( 'NONE',  ( 0.8687466845767909396, 1.140460243972157395, 2.005982166855703852 ) ) ;
#13239=CARTESIAN_POINT ( 'NONE',  ( 3.068751266904270025, 1.422870340827029345, -1.350941015047700366 ) ) ;
#13241=CARTESIAN_POINT ( 'NONE',  ( 5.137578304370245874, 1.926469575665398448, -0.7373178810637993630 ) ) ;
#13248=CARTESIAN_POINT ( 'NONE',  ( 0.8136159317379263456, -1.833160233796997218, -1.162963494187698510 ) ) ;
#13250=ADVANCED_FACE ( 'NONE', ( #18963 ), #49281, .T. ) ;
#13253=CARTESIAN_POINT ( 'NONE',  ( 2.952262541859524969, 0.6266372353985818489, 1.762611677789377440 ) ) ;
#13254=CARTESIAN_POINT ( 'NONE',  ( 6.784453917077649443, -2.118420112955111456, -0.4290502581522498415 ) ) ;
#13256=CARTESIAN_POINT ( 'NONE',  ( 6.827182134110233669, 2.103728865748891508, 2.021873693915546610 ) ) ;
#13258=CARTESIAN_POINT ( 'NONE',  ( 2.772007568003355793, 1.902874960710929431, -0.1895390408453850317 ) ) ;
#13259=CARTESIAN_POINT ( 'NONE',  ( 4.469463222250699808, 1.716395428585426153, -0.4311418314640375615 ) ) ;
#13260=CARTESIAN_POINT ( 'NONE',  ( 1.787617358713189386, 1.829539840090635749, -0.5563488465884156575 ) ) ;
#13263=CARTESIAN_POINT ( 'NONE',  ( 5.448823958578076443, -1.733895640293681373, -0.8146214837579464074 ) ) ;
#13264=CARTESIAN_POINT ( 'NONE',  ( 0.2212536527127808295, -1.848710500310095872, -0.9322282823912150240 ) ) ;
#13266=CARTESIAN_POINT ( 'NONE',  ( 2.461320219219771843, -1.760565900816572826, 1.181798851529712646 ) ) ;
#13268=CARTESIAN_POINT ( 'NONE',  ( 4.856247981345184428, 0.7163626499266174674, 1.728251504774950709 ) ) ;
#13269=CARTESIAN_POINT ( 'NONE',  ( 1.154616158753757338, -1.440623569337009968, 1.121372061650728558 ) ) ;
#13271=CARTESIAN_POINT ( 'NONE',  ( 5.127635347277352373, -2.096377701570474539, 0.6897739467496829535 ) ) ;
#13274=CARTESIAN_POINT ( 'NONE',  ( 1.434110160756268737, 1.226943730116908160, 1.657962230405624515 ) ) ;
#13283=CARTESIAN_POINT ( 'NONE',  ( 4.439934286204096914, 1.349936692791346093, 1.569845735447549906 ) ) ;
#13285=CARTESIAN_POINT ( 'NONE',  ( 2.126461914815626297, 1.246462439515462650, -1.765816729463750123 ) ) ;
#13287=CARTESIAN_POINT ( 'NONE',  ( 3.440107494509841768, -1.204893485711604484, -1.620726792054197452 ) ) ;
#13288=CARTESIAN_POINT ( 'NONE',  ( 6.620655732516651071, 4.689394895873098434, 2.736297475404291024 ) ) ;
#13293=CARTESIAN_POINT ( 'NONE',  ( 1.411342602523330214, -1.897109289313268166, 0.6839406069230756779 ) ) ;
#13294=CARTESIAN_POINT ( 'NONE',  ( 5.530878137806295669, -1.981686641427220286, 0.9361944923952856268 ) ) ;
#13296=CARTESIAN_POINT ( 'NONE',  ( 4.289254230599209627, -0.005406649120142519548, -1.912571728590661380 ) ) ;
#13300=CARTESIAN_POINT ( 'NONE',  ( 1.775017769237042353, 1.753020666602569166, -0.9963212463810557917 ) ) ;
#13303=CARTESIAN_POINT ( 'NONE',  ( 4.805503449324158183, -0.4579143662744952770, 1.662777411968613839 ) ) ;
#13309=CARTESIAN_POINT ( 'NONE',  ( 1.059532578591013463, 1.690300726139557952, 1.195051122980017144 ) ) ;
#13311=CARTESIAN_POINT ( 'NONE',  ( 5.232992382607310589, 1.676000702356477134, 0.6878641890804160219 ) ) ;
#13314=CARTESIAN_POINT ( 'NONE',  ( 6.569024019911770651, -1.395121139060730542, 1.155258474184825745 ) ) ;
#13318=CARTESIAN_POINT ( 'NONE',  ( 3.328257738700185264, 2.138080787187321086, 0.4799892483983853042 ) ) ;
#13320=CARTESIAN_POINT ( 'NONE',  ( 0.6956633456795427994, -1.384754418207832405, -1.389998539416361423 ) ) ;
#13322=CARTESIAN_POINT ( 'NONE',  ( 4.429236352518686637, -1.483253864829991775, -1.212251590588450112 ) ) ;
#13328=CARTESIAN_POINT ( 'NONE',  ( 1.587033755777764510, -0.3173376132806354222, -2.138153673666403964 ) ) ;
#13331=CARTESIAN_POINT ( 'NONE',  ( 1.975362765405625609, 1.747911882041437659, -0.5268472171036930884 ) ) ;
#13333=CARTESIAN_POINT ( 'NONE',  ( 4.770415466175468744, -1.191763575130764696, 1.382976834283907053 ) ) ;
#13337=CARTESIAN_POINT ( 'NONE',  ( 3.894935592111925526, 0.2864876570476772022, 1.948460325470881660 ) ) ;
#13339=CARTESIAN_POINT ( 'NONE',  ( 6.497608386930124880, -1.941524946301041554, 0.05238333795444527485 ) ) ;
#13343=CARTESIAN_POINT ( 'NONE',  ( 4.922192346260840345, -2.110166376318895587, 0.2103620946037400852 ) ) ;
#13345=CARTESIAN_POINT ( 'NONE',  ( 3.352119889487484183, 0.8575151890419380196, -1.709291564166728783 ) ) ;
#13350=CARTESIAN_POINT ( 'NONE',  ( 5.092444288794719220, -1.116435683446183713, 1.674956235503543889 ) ) ;
#13352=CARTESIAN_POINT ( 'NONE',  ( 6.621730190220365131, -1.769489810573118049, 0.4491385735008179836 ) ) ;
#13353=CARTESIAN_POINT ( 'NONE',  ( 0.6431357727456864515, -0.2518013131528433757, -2.054909676291870380 ) ) ;
#13366=CARTESIAN_POINT ( 'NONE',  ( 3.304998880318401167, 1.097559245703746855, -1.342624595404175780 ) ) ;
#13368=CARTESIAN_POINT ( 'NONE',  ( 1.217730340897508645, 0.4076058164220326407, -2.029561569317724690 ) ) ;
#13369=CARTESIAN_POINT ( 'NONE',  ( 2.267339977356534142, 1.934377090824404455, -0.8611398932509596316 ) ) ;
#13372=CARTESIAN_POINT ( 'NONE',  ( 1.094512790084944287, 1.939365640515663181, 0.3419967617025142514 ) ) ;
#13377=CARTESIAN_POINT ( 'NONE',  ( 2.695625570186571895, -0.7177931702126126856, 2.177047689787997342 ) ) ;
#13378=CARTESIAN_POINT ( 'NONE',  ( 0.5920835508136900183, -1.811502216344462735, -0.2265648652611390590 ) ) ;
#13379=CARTESIAN_POINT ( 'NONE',  ( 3.638835171272115421, 1.817485770107383436, 0.5952672491930725007 ) ) ;
#13382=CARTESIAN_POINT ( 'NONE',  ( 1.459241111239812705, -1.698469834904120290, 1.080578982646386743 ) ) ;
#13383=CARTESIAN_POINT ( 'NONE',  ( 2.658977320520792276, 1.578554556127611308, -1.164590279592196298 ) ) ;
#13387=CARTESIAN_POINT ( 'NONE',  ( 4.945306066807232170, 0.6564501001628511023, -1.984974157428524899 ) ) ;
#13388=CARTESIAN_POINT ( 'NONE',  ( 3.942089010115860326, 1.761346036062165332, 0.1732582469678861092 ) ) ;
#13390=CARTESIAN_POINT ( 'NONE',  ( 6.456980045808101032, 0.3985590825250818203, -2.257207781175464056 ) ) ;
#13391=CARTESIAN_POINT ( 'NONE',  ( 4.083748955185668272, -1.721791984697383482, -0.2523947965055831633 ) ) ;
#13395=CARTESIAN_POINT ( 'NONE',  ( 4.938689436542594180, 0.9992198110298566860, 1.416717458774526373 ) ) ;
#13396=CARTESIAN_POINT ( 'NONE',  ( 4.650930581473819991, -0.4712930505080668575, -2.119270573956061554 ) ) ;
#13398=CARTESIAN_POINT ( 'NONE',  ( 5.946499988598237252, -1.422611626450220434, 1.429444749906971790 ) ) ;
#13399=CARTESIAN_POINT ( 'NONE',  ( 5.031250000000002665, -0.7852924748302606561, -1.895863743163967108 ) ) ;
#13401=CARTESIAN_POINT ( 'NONE',  ( 2.854421793556624731, 0.6472853923233500284, 1.814523859438036624 ) ) ;
#13403=CARTESIAN_POINT ( 'NONE',  ( 0.08310686162707729696, -1.445780664108237801, 1.686489957186103839 ) ) ;
#13405=CARTESIAN_POINT ( 'NONE',  ( 6.983263157960370116, 1.266851337794393961, 2.060309365732877485 ) ) ;
#13408=CARTESIAN_POINT ( 'NONE',  ( 3.000855645084123946, -2.188801376007823762, -0.3777086580352209122 ) ) ;
#13409=CARTESIAN_POINT ( 'NONE',  ( 6.408651779211167465, 0.6141799454031526828, 1.863335524608072502 ) ) ;
#13414=CARTESIAN_POINT ( 'NONE',  ( 0.03578008775950020093, -1.617816776142148250, 1.203357013023528932 ) ) ;
#13416=CARTESIAN_POINT ( 'NONE',  ( 5.353991443295786468, -0.7455691153513328562, 1.923382134945450295 ) ) ;
#13421=CARTESIAN_POINT ( 'NONE',  ( 6.925078400183548588, 0.0006614011395407459748, 1.855452278108092656 ) ) ;
#13422=CARTESIAN_POINT ( 'NONE',  ( 6.328739007766592373, 0.6541968508507016722, -1.606262126034884608 ) ) ;
#13423=CARTESIAN_POINT ( 'NONE',  ( 5.548340067360077121, -1.366870494764490296, 1.077293122972399431 ) ) ;
#13425=CARTESIAN_POINT ( 'NONE',  ( 3.421668107411596882, -1.366637645153226055, -1.840301194555084230 ) ) ;
#13427=CARTESIAN_POINT ( 'NONE',  ( 1.622747808203903963, -1.734053015003593101, 0.6191010992530541213 ) ) ;
#13430=CARTESIAN_POINT ( 'NONE',  ( 1.817148636465517164, -0.2269042555285011864, 1.811363274943120771 ) ) ;
#13431=CARTESIAN_POINT ( 'NONE',  ( 3.147111449167848019, 0.9091449406319618287, 1.799922684605055556 ) ) ;
#13432=CARTESIAN_POINT ( 'NONE',  ( 1.675987266036529588, -1.170314894790158933, 1.852603040092118070 ) ) ;
#13434=CARTESIAN_POINT ( 'NONE',  ( 4.225680580359360228, -2.015911352056736661, 0.6092541954213681610 ) ) ;
#13437=CARTESIAN_POINT ( 'NONE',  ( 1.064989848632340363, 1.568927673159369762, -1.351003706900590018 ) ) ;
#13440=CARTESIAN_POINT ( 'NONE',  ( 5.197945112634200449, 1.424400718755761908, 1.570990128125760554 ) ) ;
#13442=CARTESIAN_POINT ( 'NONE',  ( 6.621730190220365131, -1.769489810573118049, 0.4491385735008179836 ) ) ;
#13450=CARTESIAN_POINT ( 'NONE',  ( 6.222909436229170588, 1.570324008046734221, -1.425282903188800798 ) ) ;
#13451=CARTESIAN_POINT ( 'NONE',  ( 1.342952632442768302, 0.4104956981533373628, 2.065382446648211801 ) ) ;
#13454=CARTESIAN_POINT ( 'NONE',  ( 5.752756584690191133, -0.4505887142414471969, -1.805456089952769183 ) ) ;
#13460=CARTESIAN_POINT ( 'NONE',  ( 1.978885927095444863, 1.829411362569667743, 0.7090815385668995940 ) ) ;
#13461=CARTESIAN_POINT ( 'NONE',  ( 0.8839147992780393981, 1.452536163361785260, 1.601146772000871188 ) ) ;
#13465=CARTESIAN_POINT ( 'NONE',  ( 3.163173391212137808, -0.5009769021222918450, -1.659887746298273514 ) ) ;
#13466=CARTESIAN_POINT ( 'NONE',  ( 2.185155941524752787, -0.7450687668543712894, 1.572906677108532936 ) ) ;
#13469=CARTESIAN_POINT ( 'NONE',  ( 3.057942249777849675, 2.051182028257723999, -0.1983934154812707074 ) ) ;
#13470=CARTESIAN_POINT ( 'NONE',  ( 1.177110994959302825, -0.9039684864705423983, -1.802142742073430171 ) ) ;
#13471=CARTESIAN_POINT ( 'NONE',  ( 6.825078400183551608, 1.261667030487168439, 2.159888225955305163 ) ) ;
#13473=CARTESIAN_POINT ( 'NONE',  ( 1.041797052332312568, 0.8010751512182741063, -1.801556251716707413 ) ) ;
#13475=CARTESIAN_POINT ( 'NONE',  ( 5.519756697582541172, -0.4584384640409416289, 1.856529252577573619 ) ) ;
#13480=CARTESIAN_POINT ( 'NONE',  ( 0.7682301616282152246, 2.017272972751768645, -0.1012717401170943471 ) ) ;
#13482=CARTESIAN_POINT ( 'NONE',  ( 4.366487424706978260, 1.084006333436113634, 2.037121594781437839 ) ) ;
#13483=CARTESIAN_POINT ( 'NONE',  ( 5.705508943770692731, -1.545575431542939970, -1.208212526538715137 ) ) ;
#13484=CARTESIAN_POINT ( 'NONE',  ( 1.885527806591394961, -1.848987351811198998, 0.6559936482007987513 ) ) ;
#13486=CARTESIAN_POINT ( 'NONE',  ( 0.0006249722829775038483, -1.976948959267275541, 0.3961041280396286890 ) ) ;
#13488=CARTESIAN_POINT ( 'NONE',  ( 1.306030339497979531, -1.181222338749428280, -1.757047197724722620 ) ) ;
#13491=CARTESIAN_POINT ( 'NONE',  ( 1.429379046243149931, 0.9088080074306194023, -1.601118750654044964 ) ) ;
#13493=CARTESIAN_POINT ( 'NONE',  ( 4.381792451580825976, -2.079388800107518698, 0.6243644347086656499 ) ) ;
#13495=CARTESIAN_POINT ( 'NONE',  ( 3.287459871768631636, 0.04819156399121089784, -2.120204644799832394 ) ) ;
#13502=CARTESIAN_POINT ( 'NONE',  ( 3.304032624679804631, -2.058584765098357749, 0.09746896435120806779 ) ) ;
#13504=CARTESIAN_POINT ( 'NONE',  ( 0.4152503475762688856, -0.9843521281015167324, -1.555853522519357934 ) ) ;
#13510=CARTESIAN_POINT ( 'NONE',  ( 2.495744459589462227, 1.747532462024743882, 1.436835450399133407 ) ) ;
#13512=CARTESIAN_POINT ( 'NONE',  ( 2.390610142633019741, -1.734584137932100312, -0.5226098844451251280 ) ) ;
#13513=CARTESIAN_POINT ( 'NONE',  ( 1.991283197800724825, -0.4156388933829333610, 1.869923353789121556 ) ) ;
#13514=CARTESIAN_POINT ( 'NONE',  ( 3.420434311836465291, 0.9283866757503267397, 1.850595421526677775 ) ) ;
#13516=CARTESIAN_POINT ( 'NONE',  ( 1.621884544099384096, -1.093522035911981050, -1.640203223306810232 ) ) ;
#13517=CARTESIAN_POINT ( 'NONE',  ( 6.129514107576198967, -1.813157573415961066, 0.6514091821806231586 ) ) ;
#13518=CARTESIAN_POINT ( 'NONE',  ( 2.957714569337116295, 1.861795396119047208, -0.1817069356538636715 ) ) ;
#13519=CARTESIAN_POINT ( 'NONE',  ( 1.471738413253330879, 0.1659702479998256264, -2.301786031945464828 ) ) ;
#13521=CARTESIAN_POINT ( 'NONE',  ( 2.470971460243949203, 1.660895280785526618, 0.8397924955986632023 ) ) ;
#13523=CARTESIAN_POINT ( 'NONE',  ( 5.143062936040889710, -0.2492579690161021710, -2.047486851065055458 ) ) ;
#13530=CARTESIAN_POINT ( 'NONE',  ( 5.860410395878546730, 0.8502751990519905601, 1.926866089339970056 ) ) ;
#13532=CARTESIAN_POINT ( 'NONE',  ( 5.659502677682959337, 0.4278135246765999988, -2.118672983663777654 ) ) ;
#13533=CARTESIAN_POINT ( 'NONE',  ( 0.01783989211246589379, -0.5346760324982450241, 1.947684760809722304 ) ) ;
#13537=CARTESIAN_POINT ( 'NONE',  ( 6.925078400183575233, 4.701279733332940580, 2.318349140213359583 ) ) ;
#13540=CARTESIAN_POINT ( 'NONE',  ( 4.241422899474024177, 0.4370803545316758743, -1.968444674787086512 ) ) ;
#13544=CARTESIAN_POINT ( 'NONE',  ( 5.963787895669664607, 2.130530397400759668, -0.3648857593604309391 ) ) ;
#13548=CARTESIAN_POINT ( 'NONE',  ( 0.1928052069046156669, 1.667086954950956157, 0.9433992581227236274 ) ) ;
#13550=CARTESIAN_POINT ( 'NONE',  ( 2.314726122855132129, 1.540323329518531903, 0.7764098835694576151 ) ) ;
#13556=CARTESIAN_POINT ( 'NONE',  ( 6.555916519444559221, 1.865492442988415656, -0.1378669075578625169 ) ) ;
#13557=CARTESIAN_POINT ( 'NONE',  ( 1.119790083981372142, -0.4868965817936173335, 1.953217858147300090 ) ) ;
#13559=CARTESIAN_POINT ( 'NONE',  ( 3.223846859376262142, -2.127229092858519799, 0.5869343725257711863 ) ) ;
#13560=CARTESIAN_POINT ( 'NONE',  ( 5.313404054176891655, -1.830285002536722549, -1.167499077736388724 ) ) ;
#13561=EDGE_LOOP ( 'NONE', ( #211456, #181237 ) ) ;
#13564=CARTESIAN_POINT ( 'NONE',  ( 3.071057173463411338, -1.604308532545582366, 1.386676294644908713 ) ) ;
#13565=CARTESIAN_POINT ( 'NONE',  ( 2.109000121467627498, 0.002830143620808495131, 2.016598147190066914 ) ) ;
#13566=CARTESIAN_POINT ( 'NONE',  ( 1.757782220650351723, 0.6909716962627761028, -1.674832866754811578 ) ) ;
#13573=CARTESIAN_POINT ( 'NONE',  ( 0.8662487887013297083, -1.869732701101217476, -0.4164899194021577933 ) ) ;
#13580=CARTESIAN_POINT ( 'NONE',  ( 5.454052192070484750, 2.159419290912270029, -0.1019294599445344923 ) ) ;
#13583=CARTESIAN_POINT ( 'NONE',  ( 3.533539421053990104, -0.1523460092780377639, 2.115156586662121363 ) ) ;
#13586=CARTESIAN_POINT ( 'NONE',  ( 3.075414692445295195, 1.873101151500027317, -0.6148835396118810248 ) ) ;
#13589=CARTESIAN_POINT ( 'NONE',  ( 0.3618904354094238385, -0.5536326762660361833, 1.994880328902041589 ) ) ;
#13590=CARTESIAN_POINT ( 'NONE',  ( 2.624863168539525393, -1.811862388431908721, 0.6992392096202125762 ) ) ;
#13595=CARTESIAN_POINT ( 'NONE',  ( 2.765665077289869433, 1.118955468730401526, 1.765788254259098800 ) ) ;
#13598=CARTESIAN_POINT ( 'NONE',  ( 6.235011639695052565, 1.786057601157979180, 0.6837302122261402770 ) ) ;
#13600=CARTESIAN_POINT ( 'NONE',  ( 3.914836437932368796, 1.561248537261412883, -1.560010120355350693 ) ) ;
#13602=CARTESIAN_POINT ( 'NONE',  ( 3.048105859194950362, 0.7956334958073747465, -2.058523145315640956 ) ) ;
#13604=CARTESIAN_POINT ( 'NONE',  ( 2.227084300891319035, 1.708885092217244051, 0.8583199515034345417 ) ) ;
#13606=CARTESIAN_POINT ( 'NONE',  ( 3.895033709675084221, 0.3008086390649654662, 2.048262060622765279 ) ) ;
#13608=CARTESIAN_POINT ( 'NONE',  ( 3.186554565756247737, -2.129457467500107004, -0.3711038070777841202 ) ) ;
#13609=CARTESIAN_POINT ( 'NONE',  ( 5.144143540903125533, 0.6357783856077160456, 2.097287126430439130 ) ) ;
#13618=CARTESIAN_POINT ( 'NONE',  ( -0.05211191391743182078, -1.802403943428915412, -0.9041556775107384425 ) ) ;
#13620=CARTESIAN_POINT ( 'NONE',  ( 5.190316231837919680, 1.068962568377257671, -1.772817291931286787 ) ) ;
#13621=CARTESIAN_POINT ( 'NONE',  ( 2.789578772358902281, 1.362584191422511415, 1.362147869459982230 ) ) ;
#13622=CARTESIAN_POINT ( 'NONE',  ( 5.431313658478175377, -1.669672585088026517, -1.301796502452344129 ) ) ;
#13625=CARTESIAN_POINT ( 'NONE',  ( 4.241030189111538284, -0.1885853823969813603, -1.960358720193545068 ) ) ;
#13626=CARTESIAN_POINT ( 'NONE',  ( 6.316396932256916230, 2.136508426756661638, 0.8310160958180726753 ) ) ;
#13627=CARTESIAN_POINT ( 'NONE',  ( 3.721172816245840842, -0.1328194893376876962, 1.820914920514608459 ) ) ;
#13633=CARTESIAN_POINT ( 'NONE',  ( 1.171164436615620863, 1.096940724416964885, 1.478650282607060662 ) ) ;
#13634=CARTESIAN_POINT ( 'NONE',  ( 5.080342566386993219, 0.9961330521413218619, 1.749448578721881198 ) ) ;
#13635=CARTESIAN_POINT ( 'NONE',  ( 5.836663081169705336, 0.6703748249779170054, -2.198801845021758350 ) ) ;
#13636=CARTESIAN_POINT ( 'NONE',  ( 5.735196368693616265, -0.04450293679344322767, -1.961403813732150780 ) ) ;
#13641=CARTESIAN_POINT ( 'NONE',  ( 1.786781105396139102, 1.817558579408204089, -1.033184933219722934 ) ) ;
#13642=CARTESIAN_POINT ( 'NONE',  ( 6.754783849477350444, -1.364574176550734208, 1.126888093558385817 ) ) ;
#13644=CARTESIAN_POINT ( 'NONE',  ( -0.1106727585415837045, 2.018984206239351042, -2.418200238751634146 ) ) ;
#13645=CARTESIAN_POINT ( 'NONE',  ( 0.4854153416827499679, -1.726952712381021326, -0.2154422717644439433 ) ) ;
#13649=CARTESIAN_POINT ( 'NONE',  ( 1.576317393346495344, -1.636983117988626946, -0.5438251031371076349 ) ) ;
#13650=CARTESIAN_POINT ( 'NONE',  ( 1.874823134854076923, -0.1115055541827478930, -2.188858692977871279 ) ) ;
#13651=CARTESIAN_POINT ( 'NONE',  ( 4.600333186373093852, -2.206333364838486411, -0.05604163552313382035 ) ) ;
#13654=CARTESIAN_POINT ( 'NONE',  ( 1.024573611315128252, 1.068414711107899429, 1.889872971959544401 ) ) ;
#13656=CARTESIAN_POINT ( 'NONE',  ( 2.167340134605561630, 1.933669477944195636, -0.8630234182349978411 ) ) ;
#13657=CARTESIAN_POINT ( 'NONE',  ( 6.539320575229251808, 2.472926584938171413, 2.181659282373017650 ) ) ;
#13659=CARTESIAN_POINT ( 'NONE',  ( 2.876852093609012950, -0.1713799144957695864, -2.286037302510893099 ) ) ;
#13663=CARTESIAN_POINT ( 'NONE',  ( 6.041669411999269990, -2.092492953876758044, 0.7457244993839227121 ) ) ;
#13669=CARTESIAN_POINT ( 'NONE',  ( 3.568982563115063567, -0.9913999084223242830, 1.755768870528086056 ) ) ;
#13671=CARTESIAN_POINT ( 'NONE',  ( 2.553648762129530958, 1.591643574212991297, 1.311770128662164137 ) ) ;
#13678=CARTESIAN_POINT ( 'NONE',  ( 5.455090197064776270, 0.4301712223657681022, -2.148646160378755443 ) ) ;
#13679=CARTESIAN_POINT ( 'NONE',  ( 2.742814741689561853, 2.006446121045248887, -0.2004354718553730264 ) ) ;
#13680=CARTESIAN_POINT ( 'NONE',  ( 2.419273308677453826, -1.061688697878185206, -1.504126257600538974 ) ) ;
#13683=CARTESIAN_POINT ( 'NONE',  ( 5.561492448144861989, 0.3540975402388062965, -1.790731494587729067 ) ) ;
#13684=CARTESIAN_POINT ( 'NONE',  ( 6.604150280000163242, -0.1430408514614608939, 1.983920101186954721 ) ) ;
#13686=CARTESIAN_POINT ( 'NONE',  ( 5.682586732044571320, -2.206005490488979426, -0.5019008842952320526 ) ) ;
#13688=CARTESIAN_POINT ( 'NONE',  ( 1.155059408868217119, -1.659095468083382041, 1.297160957089478206 ) ) ;
#13698=CARTESIAN_POINT ( 'NONE',  ( 2.426306324659221136, -2.196553987802750907, 0.3307981192552343352 ) ) ;
#13703=CARTESIAN_POINT ( 'NONE',  ( 3.508209890309890167, 1.962046631884439174, 0.002529298861464468473 ) ) ;
#13709=CARTESIAN_POINT ( 'NONE',  ( 1.933984528066152953, -2.055706711753771287, 0.5200354980386610038 ) ) ;
#13711=CARTESIAN_POINT ( 'NONE',  ( 4.733375416736937069, -1.977748744329570263, 0.8730265686548792647 ) ) ;
#13712=CARTESIAN_POINT ( 'NONE',  ( 2.770863647982471534, 1.747605724785822767, -0.5798694457997202178 ) ) ;
#13715=CARTESIAN_POINT ( 'NONE',  ( 5.437372246358883388, 0.6999822053482355200, -1.593550356025658976 ) ) ;
#13716=CARTESIAN_POINT ( 'NONE',  ( 6.727182134110195832, 0.008744176509076214548, 1.710970312420513784 ) ) ;
#13718=CARTESIAN_POINT ( 'NONE',  ( 6.720655732516645386, 0.002698097948191865297, 1.926293798961113080 ) ) ;
#13719=CARTESIAN_POINT ( 'NONE',  ( 2.782270202741622178, -1.112240752214749273, 1.853481441253836071 ) ) ;
#13721=CARTESIAN_POINT ( 'NONE',  ( 4.710314442360476583, -1.556670644073439913, -1.281164596596932936 ) ) ;
#13723=CARTESIAN_POINT ( 'NONE',  ( 2.465889518630470789, 2.120156730345585938, -0.4209195040108040797 ) ) ;
#13724=( BOUNDED_SURFACE ( )  B_SPLINE_SURFACE ( 3, 3, ( 
 ( #107605, #126002, #141153, #138990, #191963, #171467, #27345, #92389, #190902, #6806, #173636 ),
 ( #25208, #157369, #56658, #207162, #43628, #42566, #40418, #39334, #159486, #8963, #142203 ),
 ( #75038, #23056, #93448, #122821, #109743, #72883, #58785, #143283, #187706, #156300, #10025 ),
 ( #124940, #174698, #175754, #77161, #209274, #172547, #105431, #140066, #60920, #90234, #7883 ),
 ( #73971, #48950, #147517, #63053, #15346, #161637, #213538, #81439, #65161, #194111, #176806 ),
 ( #112943, #177883, #64127, #111879, #29496, #13232, #95588, #28422, #128151, #129219, #145 ),
 ( #79305, #82489, #145421, #45761, #131317, #115068, #193040, #162704, #61995, #14276, #197309 ) ),
 .UNSPECIFIED., .T., .F., .T. ) 
 B_SPLINE_SURFACE_WITH_KNOTS ( ( 4, 3, 4 ),
 ( 4, 1, 1, 1, 1, 1, 1, 1, 4 ),
 ( 0.000000000000000000, 0.5000000000000000000, 1.000000000000000000 ),
 ( 0.000000000000000000, 0.2254704865597413344, 0.3973194950497592193, 0.5246576192285303808, 0.6166070239209043846, 0.6823180413592140336, 0.7309932997181896042, 0.7717238569598857678, 1.000000000000000000 ),
 .UNSPECIFIED. ) 
 GEOMETRIC_REPRESENTATION_ITEM ( )  RATIONAL_B_SPLINE_SURFACE ( (
 ( 1.000000000000000000, 1.000000000000000000, 1.000000000000000222, 0.9999999999999997780, 1.000000000000000444, 0.9999999999999996669, 1.000000000000000222, 1.000000000000000222, 1.000000000000000222, 1.000000000000000222, 1.000000000000000222),
 ( 0.3333333333333333703, 0.3333333333333334259, 0.3333333333333333703, 0.3333333333333333703, 0.3333333333333334814, 0.3333333333333332038, 0.3333333333333334814, 0.3333333333333334259, 0.3333333333333334259, 0.3333333333333334259, 0.3333333333333334259),
 ( 0.3333333333333333703, 0.3333333333333334259, 0.3333333333333333703, 0.3333333333333333703, 0.3333333333333334814, 0.3333333333333332038, 0.3333333333333334814, 0.3333333333333334259, 0.3333333333333334259, 0.3333333333333334259, 0.3333333333333334259),
 ( 1.000000000000000000, 1.000000000000000000, 1.000000000000000222, 0.9999999999999997780, 1.000000000000000444, 0.9999999999999996669, 1.000000000000000222, 1.000000000000000222, 1.000000000000000222, 1.000000000000000222, 1.000000000000000222),
 ( 0.3333333333333333703, 0.3333333333333334259, 0.3333333333333333703, 0.3333333333333333703, 0.3333333333333334814, 0.3333333333333332038, 0.3333333333333334814, 0.3333333333333334259, 0.3333333333333334259, 0.3333333333333334259, 0.3333333333333334259),
 ( 0.3333333333333333703, 0.3333333333333334259, 0.3333333333333333703, 0.3333333333333333703, 0.3333333333333334814, 0.3333333333333332038, 0.3333333333333334814, 0.3333333333333334259, 0.3333333333333334259, 0.3333333333333334259, 0.3333333333333334259),
 ( 1.000000000000000000, 1.000000000000000000, 1.000000000000000222, 0.9999999999999997780, 1.000000000000000444, 0.9999999999999996669, 1.000000000000000222, 1.000000000000000222, 1.000000000000000222, 1.000000000000000222, 1.000000000000000222) ) ) 
 REPRESENTATION_ITEM ( '' )  SURFACE ( )  );
#13725=CARTESIAN_POINT ( 'NONE',  ( 2.512907010818050679, 1.759183109745281692, 0.8898679072262619671 ) ) ;
#13727=CARTESIAN_POINT ( 'NONE',  ( 4.423342042002774477, -1.197376356234590933, -1.528922412636232631 ) ) ;
#13736=CARTESIAN_POINT ( 'NONE',  ( 0.7278961316968115547, -2.094849050945537972, 0.6941159686642893734 ) ) ;
#13738=CARTESIAN_POINT ( 'NONE',  ( 4.785966450049039089, -1.203721183051874810, -1.548998264137561254 ) ) ;
#13742=CARTESIAN_POINT ( 'NONE',  ( 0.07479286986305369589, 4.095183424177953668, -2.410510762676120411 ) ) ;
#13743=CARTESIAN_POINT ( 'NONE',  ( 4.329911453333429527, 1.806054511993939515, 0.3568155486674411958 ) ) ;
#13752=CARTESIAN_POINT ( 'NONE',  ( 6.643830136542335119, 0.7930364421293911725, -1.902288772117090687 ) ) ;
#13754=CARTESIAN_POINT ( 'NONE',  ( 1.451354471725987860, 1.406072211568440755, 1.219298000798328507 ) ) ;
#13755=CARTESIAN_POINT ( 'NONE',  ( 3.210337823311388394, 1.665856106666419034, 0.7845605768846477535 ) ) ;
#13759=CARTESIAN_POINT ( 'NONE',  ( 3.194164748978207680, -0.8942147705085048415, 2.017778291555922809 ) ) ;
#13760=CARTESIAN_POINT ( 'NONE',  ( 5.677129043647218154, -0.04737763303009440846, -2.262073803551585272 ) ) ;
#13762=CARTESIAN_POINT ( 'NONE',  ( 6.064714483498689468, 0.5772776769059180246, 1.717211531030158556 ) ) ;
#13763=CARTESIAN_POINT ( 'NONE',  ( 4.962082351039136086, -1.058791762104252632, 1.596325305674146433 ) ) ;
#13766=CARTESIAN_POINT ( 'NONE',  ( 6.578970801323708706, -0.09418725797194843485, -1.868394071727994543 ) ) ;
#13767=CARTESIAN_POINT ( 'NONE',  ( 6.514093505496237668, 1.855963486094978965, -0.1381079127797563977 ) ) ;
#13769=CARTESIAN_POINT ( 'NONE',  ( 6.807488043635657959, -0.3792581958518992935, 1.734866861734218446 ) ) ;
#13770=CARTESIAN_POINT ( 'NONE',  ( 0.9015777671340443611, -1.966303774932298021, 0.4465067697373495403 ) ) ;
#13772=CARTESIAN_POINT ( 'NONE',  ( 3.123755640277770418, -2.029568314945415786, 0.5621985482912382759 ) ) ;
#13778=CARTESIAN_POINT ( 'NONE',  ( 3.340107562988120726, -1.206563586372558561, -1.619613960689977761 ) ) ;
#13781=CARTESIAN_POINT ( 'NONE',  ( 3.479894426560462328, 1.368377867093536482, 1.673357603396708360 ) ) ;
#13786=CARTESIAN_POINT ( 'NONE',  ( 1.047617182619766885, 1.914800503461089543, -1.023450759211230521 ) ) ;
#13790=CARTESIAN_POINT ( 'NONE',  ( 2.138457411672203712, 0.4836887423533155483, 2.137355272389021899 ) ) ;
#13792=CARTESIAN_POINT ( 'NONE',  ( 2.800010096142038218, -0.7105090101824761417, 2.148112714708799942 ) ) ;
#13799=CARTESIAN_POINT ( 'NONE',  ( 3.233429047156919811, -1.186097956103189910, -1.313638963288694228 ) ) ;
#13803=CARTESIAN_POINT ( 'NONE',  ( 0.07735805125222078305, -0.0005418671161615954465, -2.088975025666544472 ) ) ;
#13807=CARTESIAN_POINT ( 'NONE',  ( 5.765249964824501028, 1.862012222821707308, -0.7743297468396084238 ) ) ;
#13810=CARTESIAN_POINT ( 'NONE',  ( 3.942156681999692491, 1.861596489644477437, 0.1839347620080991064 ) ) ;
#13811=CARTESIAN_POINT ( 'NONE',  ( 3.397389602098393802, -1.828008730618407629, 0.9717071122367710867 ) ) ;
#13817=CARTESIAN_POINT ( 'NONE',  ( 3.033595934319989418, 1.863777508880835487, -0.6128360024686765328 ) ) ;
#13818=CARTESIAN_POINT ( 'NONE',  ( 1.247422469434919412, -1.966343046301596509, -0.4444367004674750210 ) ) ;
#13821=CARTESIAN_POINT ( 'NONE',  ( 0.5087955169046609605, 1.624258005607306599, 0.9276666955444978768 ) ) ;
#13823=CARTESIAN_POINT ( 'NONE',  ( 1.863541034856039502, -1.619513613076409397, -1.195741390080407918 ) ) ;
#13825=CARTESIAN_POINT ( 'NONE',  ( 2.548581339128490608, -1.457745987184940306, 1.535692819318078550 ) ) ;
#13827=CARTESIAN_POINT ( 'NONE',  ( 3.455589482447298355, 1.630370400113918095, 1.275915752658786095 ) ) ;
#13829=CARTESIAN_POINT ( 'NONE',  ( 6.123005977957785007, -1.968908147963293942, 0.7033269742807277680 ) ) ;
#13831=CARTESIAN_POINT ( 'NONE',  ( 4.155160913615768337, -1.517764731708035386, -1.014145119915064841 ) ) ;
#13836=CARTESIAN_POINT ( 'NONE',  ( 6.299877592275240801, -0.7493655176046759570, 2.075778730795534877 ) ) ;
#13838=CARTESIAN_POINT ( 'NONE',  ( 4.863870654145381778, 0.5962773724161560818, -1.817021391602848812 ) ) ;
#13845=CARTESIAN_POINT ( 'NONE',  ( 0.6086344939593493208, -0.2706599535906920040, 1.821105742621460744 ) ) ;
#13847=CARTESIAN_POINT ( 'NONE',  ( -0.2108831679770946654, 7.629137130509072939, -2.497154329497498715 ) ) ;
#13849=CARTESIAN_POINT ( 'NONE',  ( 4.253091631423633778, -1.553859266942819284, -1.041061106808522929 ) ) ;
#13856=CARTESIAN_POINT ( 'NONE',  ( 0.7429342955292950190, -0.2353911671746557188, -1.955230025236649682 ) ) ;
#13857=CARTESIAN_POINT ( 'NONE',  ( 2.337517745082304810, 0.5350678814987767096, -1.944078148028173914 ) ) ;
#13861=CARTESIAN_POINT ( 'NONE',  ( 2.291216553123593958, 1.694975396412688351, 1.389067552005143424 ) ) ;
#13871=ORIENTED_EDGE ( 'NONE', *, *, #45298, .F. ) ;
#13872=CARTESIAN_POINT ( 'NONE',  ( 5.231922985772964552, 1.814955821992572993, 0.3091130605668013231 ) ) ;
#13873=CARTESIAN_POINT ( 'NONE',  ( 2.104154084628720334, -0.8588668247239000797, 1.820802598171267439 ) ) ;
#13874=CARTESIAN_POINT ( 'NONE',  ( 3.708664688178139102, -1.738024148615105569, -1.504010254680566483 ) ) ;
#13875=CARTESIAN_POINT ( 'NONE',  ( -0.1290005225502676156, 1.324981729379502537, -2.425680704180297464 ) ) ;
#13876=CARTESIAN_POINT ( 'NONE',  ( 2.113880859634624354, 1.856391821545114951, -0.1307286092924550835 ) ) ;
#13878=CARTESIAN_POINT ( 'NONE',  ( 5.642805672956042962, 1.844803604357934779, 0.5037821151940986564 ) ) ;
#13881=CARTESIAN_POINT ( 'NONE',  ( 5.144118995967028596, 0.6083014027435985627, 2.000272865920887266 ) ) ;
#13882=CARTESIAN_POINT ( 'NONE',  ( 3.731198135974967300, -1.728734619261709904, 0.7151963084984153118 ) ) ;
#13884=CARTESIAN_POINT ( 'NONE',  ( 5.354971380013192395, 0.3533838956982695567, -1.806849549699687696 ) ) ;
#13887=CARTESIAN_POINT ( 'NONE',  ( 5.584504578548418863, -1.684151958202559252, -0.3718293602123431962 ) ) ;
#13889=CARTESIAN_POINT ( 'NONE',  ( 0.7032560681843272876, 1.601581415593232860, 0.6654971025301190668 ) ) ;
#13892=CARTESIAN_POINT ( 'NONE',  ( 4.539989016966003099, 1.413352768409949389, 1.648148102320112329 ) ) ;
#13893=CARTESIAN_POINT ( 'NONE',  ( 3.422296110638740174, 1.157362003623555236, -1.411967061744797691 ) ) ;
#13894=CARTESIAN_POINT ( 'NONE',  ( 1.024179675629211861, 0.9620134025654383247, 1.709582039726687430 ) ) ;
#13895=CARTESIAN_POINT ( 'NONE',  ( 0.2107725088618967457, 2.027540257690120029, 0.6097772466436711669 ) ) ;
#13896=CARTESIAN_POINT ( 'NONE',  ( 0.3227791477718846558, 2.195406398872503217, 0.6593016323864949735 ) ) ;
#13901=CARTESIAN_POINT ( 'NONE',  ( 2.983181628360128013, -1.960071735995170927, -0.8095406527153580223 ) ) ;
#13905=CARTESIAN_POINT ( 'NONE',  ( 0.9540663221972445207, -0.7486024665571254788, 1.930331157511067097 ) ) ;
#13907=CARTESIAN_POINT ( 'NONE',  ( 2.332966905468473406, 1.448476307009987307, -1.684171307209429314 ) ) ;
#13909=CARTESIAN_POINT ( 'NONE',  ( 0.1944798361989338309, 2.004116887782161349, 1.125739740898183294 ) ) ;
#13911=CARTESIAN_POINT ( 'NONE',  ( 6.016483441405136467, 0.8307744727026479259, 1.888021813390627246 ) ) ;
#13916=CARTESIAN_POINT ( 'NONE',  ( 0.2331563151865486683, 7.629137130509099585, -2.545728013813946422 ) ) ;
#13917=CARTESIAN_POINT ( 'NONE',  ( 5.091278345985558396, -0.6575378499774006125, 1.720029930423284448 ) ) ;
#13920=CARTESIAN_POINT ( 'NONE',  ( 1.729112849636908367, -1.625594568690587050, 0.5768372424696955880 ) ) ;
#13921=CARTESIAN_POINT ( 'NONE',  ( 0.8840003597419334724, -2.016708404047353742, 0.004841148455551891328 ) ) ;
#13922=CARTESIAN_POINT ( 'NONE',  ( 1.916985526034093335, -1.504927692415005014, -1.737642283433957768 ) ) ;
#13924=CARTESIAN_POINT ( 'NONE',  ( 2.021152898351881166, 2.110506920502265960, 0.8154138738461161884 ) ) ;
#13925=CARTESIAN_POINT ( 'NONE',  ( 4.512399653719460169, -0.8998888299811370617, -1.904278430835882885 ) ) ;
#13927=CARTESIAN_POINT ( 'NONE',  ( 2.530210103492841256, 1.715365446638704494, 0.4347029418121580169 ) ) ;
#13930=CARTESIAN_POINT ( 'NONE',  ( 4.827800031893906052, 1.179792396777184615, -1.965320743881134646 ) ) ;
#13933=CARTESIAN_POINT ( 'NONE',  ( 4.048915112334880106, -1.821525731582713359, -1.218098874207810933 ) ) ;
#13936=CARTESIAN_POINT ( 'NONE',  ( 6.639320575229281651, -0.0007625845807879281287, 2.103388539994067497 ) ) ;
#13938=CARTESIAN_POINT ( 'NONE',  ( 2.648949911425259263, -1.601578617359520340, 1.070393023584510050 ) ) ;
#13941=CARTESIAN_POINT ( 'NONE',  ( 5.765915565743810589, 0.6138260544302427402, -2.029845472315944921 ) ) ;
#13947=CARTESIAN_POINT ( 'NONE',  ( 6.005383971424570255, -1.826508537601937432, 0.2321369796495567073 ) ) ;
#13951=CARTESIAN_POINT ( 'NONE',  ( 1.891783327304029205, -0.4647161096258972668, -1.677148923195219243 ) ) ;
#13953=CARTESIAN_POINT ( 'NONE',  ( 0.4319881149899909567, 1.126445828788334991, 1.606065282034954578 ) ) ;
#13958=CARTESIAN_POINT ( 'NONE',  ( 5.647404790089923132, -1.701416311724871067, -1.333359258283283166 ) ) ;
#13962=CARTESIAN_POINT ( 'NONE',  ( 6.274684828636788225, -1.871173557121402542, -0.6205748305461754599 ) ) ;
#13963=CARTESIAN_POINT ( 'NONE',  ( 5.079290571759123019, 1.194821443462086963, -1.256652284620445759 ) ) ;
#13965=CARTESIAN_POINT ( 'NONE',  ( 1.470551405592795957, -2.082434148983134392, -0.6831980896230758216 ) ) ;
#13966=CARTESIAN_POINT ( 'NONE',  ( 3.223938161889360110, -2.224449554215703895, 0.6136290147475926826 ) ) ;
#13967=CARTESIAN_POINT ( 'NONE',  ( 6.257116178607133428, -1.765205416791076010, -1.063208849337776485 ) ) ;
#13968=CARTESIAN_POINT ( 'NONE',  ( 1.693202460532976295, -0.6543010362765960819, 1.828533997230662234 ) ) ;
#13972=CARTESIAN_POINT ( 'NONE',  ( 3.902672080109194752, -2.098000727953463151, -0.3078000538283761078 ) ) ;
#13973=CARTESIAN_POINT ( 'NONE',  ( 2.514296259408643319, -1.880434619097739013, 0.7283795345095490648 ) ) ;
#13975=CARTESIAN_POINT ( 'NONE',  ( 4.876106637443972325, 1.267215935518750669, 1.806476597341267087 ) ) ;
#13978=( BOUNDED_SURFACE ( )  B_SPLINE_SURFACE ( 3, 3, ( 
 ( #57975, #7062, #41753, #107865, #138175, #5994, #173891, #108931, #121997, #87276, #154415, #89428, #157626, #155479, #139239, #9223, #75295, #141411, #153345, #207418, #59037, #125195, #191158, #42825, #70993, #96907, #161896, #64379, #143541, #208471, #44952, #12409, #160817, #95840, #30831, #194374, #114270, #195454, #27604, #144606, #94769, #26534, #78489, #111060, #93705, #193307, #146726, #159745, #77424, #28683, #61177, #79558, #210621, #62247, #179207, #129472, #130524, #128407, #158683, #162959, #46018, #142463, #43886, #60107, #112137, #126266, #178141, #196515, #13483, #176012, #127337, #177067, #29755, #92641, #212745, #192223, #145677, #211674, #63310, #47083, #113201, #209535, #14537, #80634, #48158, #10282, #76356, #110000, #11343, #168272, #198616, #83810, #183449, #81689, #49206, #84884, #149903, #1470, #133679, #199684, #213789, #51327, #16667, #397, #68611, #115326, #147773, #82751, #97968, #116381, #148824, #19873, #18800, #52392, #67537, #165076, #167212, #180267, #100073, #200743, #184504, #31891, #131561, #65412, #36123, #197562, #182369, #33999, #117455, #166135, #66468, #150971, #132609, #2536, #35053, #181316, #164026, #32945, #15601, #99018, #50262, #101124, #85957, #17722, #134735, #118520, #102207, #152032, #3602, #69680, #135784, #201808, #53450, #153091, #138996, #170394, #154166, #7888, #54524, #20923, #21983, #37202, #55589, #88092, #173640, #172552, #206093, #23062, #104350, #106526, #119589, #39339, #140070, #123885, #185572, #70739, #4666, #189851, #136852, #121744, #187711, #56663, #105437, #5731, #24137, #71810, #156305, #72889, #120669, #103276, #202876, #169338, #186647, #137921, #203941, #171472, #89178, #87018, #205017, #38273, #122826, #90239, #155230, #6811, #40423, #73975, #41496, #57728, #157374, #188788, #107609, #25213, #91317, #8969, #75042, #141159, #207166, #146473, #13239, #59855, #176813, #127083, #58790, #193046, #143288, #126007, #11090, #178962, #191968, #109749, #60926, #93454, #111886, #44700, #110807, #211429, #161644, #162711, #28428, #190907, #63059, #94521, #174702, #76105, #92393, #160559, #26277, #12167, #96658, #194118, #208223, #159491, #209279, #78239, #124945, #30577, #158429, #62002, #77167, #144361, #210362, #128158, #175759, #45769, #195200, #177890, #27351, #29503, #95596, #43634, #79312, #145428, #129227, #46837, #112951, #14283, #80378, #42571, #108674, #10031, #142209, #2285, #116132, #114023, #15353, #31640, #50008, #180019, #152, #35880, #133427, #147524, #32689, #148583, #182120, #64134, #118269, #97717, #1226, #98769, #33750, #66218, #82496, #48957, #83562, #134494, #132366, #115075, #99827, #164826, #149644, #200498, #16416, #165893, #67288, #163775, #81447, #117202, #17478, #199434, #51076, #183199, #213545, #34805, #181071, #198368, #100880, #65168, #131323, #166967, #130278, #18557, #84634, #52141, #150725, #68361, #184253, #197316, #101955, #212493, #168022, #19626, #85697, #196266, #47913, #36945, #156041, #103026, #153913, #5483, #88923, #71564, #136603, #204756, #120414, #188531, #105178, #152842, #69429, #169081, #3358, #185322, #38026, #202627, #104097, #54277, #53204, #22808, #135534, #154976, #56407, #201558, #186389, #72641, #106275, #7630, #138738, #189597, #170146, #119335, #21733, #137671, #203692, #6561, #73715, #171214, #24956 ),
 ( #139813, #87842, #20680, #55339, #122568, #173372, #151785, #121491, #40161, #187463, #4416, #172296, #205841, #107350, #23884, #89990, #57475, #41243, #123634, #86770, #70487, #39091, #13767, #163244, #131841, #164299, #178432, #79843, #15888, #158185, #30039, #124690, #145952, #195740, #157119, #81972, #96125, #196797, #207969, #197849, #43372, #48438, #112418, #108423, #114553, #180545, #59595, #147008, #63601, #125752, #92131, #191714, #190648, #181596, #49481, #115601, #162181, #213026, #140894, #211962, #91058, #8708, #47377, #129755, #113488, #26021, #58535, #179496, #42308, #74792, #97192, #31118, #14827, #206904, #174445, #148059, #214067, #9778, #64660, #75850, #141957, #80918, #32167, #130805, #98245, #65693, #185857, #182663, #51623, #199974, #102493, #151256, #86243, #165355, #2826, #101424, #132893, #36414, #168557, #167496, #68897, #135016, #84106, #166427, #201030, #54815, #150193, #120964, #149106, #35346, #52672, #33224, #99308, #20156, #19092, #152313, #53745, #1762, #198896, #136072, #118803, #3890, #119879, #184788, #203170, #34284, #133967, #83032, #66752, #21209, #153380, #116665, #69960, #16951, #50543, #685, #37489, #202087, #100357, #103567, #169626, #18017, #117747, #183738, #87311, #4951, #71029, #67820, #137143, #85172, #72102, #190137, #41791, #106817, #90531, #8187, #23356, #105730, #156593, #208506, #89465, #60141, #88385, #189079, #74272, #186935, #38567, #107904, #40712, #91611, #207455, #155519, #138213, #75331, #140364, #173930, #59074, #206383, #142500, #188000, #73172, #141448, #108966, #205310, #55877, #139278, #25503, #104642, #170689, #58009, #157662, #123119, #39625, #124173, #174986, #22276, #9260, #125234, #191192, #10317, #42859, #26570, #92675, #158719, #172847, #76391, #154455, #6033, #56947, #24418, #204225, #171760, #122034, #7100, #144640, #46051, #192257, #179242, #12444, #63347, #193342, #80670, #177102, #129506, #28717, #11379, #195487, #47121, #44987, #79594, #128443, #111096, #143576, #94804, #93740, #64414, #146761, #212779, #78523, #145713, #110035, #160852, #126298, #176047, #178176, #210655, #29791, #209568, #159779, #62283, #77458, #27640, #13521, #161931, #112172, #211711, #113238, #95876, #61214, #127371, #14575, #43920, #30866, #194409, #162994, #96944, #126998, #43547, #9947, #60837, #42482, #109669, #40339, #123804, #57644, #174619, #8880, #158354, #22976, #74959, #173554, #204930, #108591, #26195, #25127, #141069, #207076, #156225, #24056, #58707, #192957, #7802, #105348, #6730, #107523, #124857, #171385, #89094, #92311, #91230, #76023, #125928, #73894, #56581, #208139, #190821, #142126, #191886, #59769, #155148, #106445, #206009, #175671, #27259, #189764, #188703, #41416, #93367, #72809, #138910, #159403, #11002, #157290, #172468, #77079, #143207, #122740, #209197, #90159, #139988, #38494, #134950, #169556, #5958, #86175, #200957, #136002, #36342, #21138, #72029, #102420, #202015, #87241, #199906, #167430, #203095, #53674, #119806, #37419, #103495, #117677, #153306, #52605, #118734, #186864, #19022, #51552, #184718, #1695, #20087, #168488, #138141, #137070, #170617, #185785, #68828, #70960, #84033, #3818, #104572, #88317, #150122, #35273, #183670, #154381, #101351, #152245, #69889, #4881, #54740, #120890, #22204, #85102, #204150, #55806, #121960, #187927 ),
 ( #67749, #151187, #105658, #39557, #171686, #133899, #2759, #175981, #172776, #41722, #190070, #92610, #141378, #76327, #155443, #205235, #107832, #9193, #157598, #158653, #27574, #191125, #111030, #192192, #24350, #207389, #91539, #23283, #75264, #173857, #90460, #25433, #143507, #156526, #74205, #59010, #57942, #142433, #125166, #42791, #93672, #126231, #127306, #108900, #7028, #159715, #174923, #139205, #40646, #56876, #26503, #123052, #10251, #61144, #208441, #8117, #124107, #60075, #43856, #89395, #209504, #189003, #109970, #73104, #140299, #11313, #77391, #206318, #193277, #44922, #106749, #13454, #14508, #129441, #48127, #165041, #195424, #80599, #180237, #78458, #45986, #81656, #146695, #212711, #130498, #196485, #210590, #114239, #79530, #211644, #65382, #112107, #144576, #145648, #94739, #113170, #63279, #16634, #15569, #49176, #64352, #161864, #163994, #177035, #96877, #197531, #181284, #28652, #128377, #62220, #32911, #30798, #194345, #31861, #97936, #162927, #147743, #213759, #47054, #95808, #131528, #198583, #179174, #50229, #178110, #115293, #98988, #160785, #12378, #82718, #148795, #365, #66438, #132580, #29726, #4633, #19840, #103246, #202845, #152000, #71778, #117422, #2506, #70705, #38242, #134705, #199651, #68579, #37168, #137894, #116349, #85926, #86987, #52361, #183419, #135754, #104316, #203913, #69645, #154131, #20891, #200710, #54494, #53417, #153058, #201777, #36090, #185540, #5701, #186616, #118490, #102174, #170366, #35022, #184473, #149872, #168241, #3572, #182339, #21949, #119554, #136818, #18769, #33967, #169306, #120638, #88059, #133651, #100044, #166107, #84853, #17693, #83780, #150943, #101094, #1440, #67504, #51297, #167180, #159455, #57696, #174670, #105402, #156273, #55560, #187679, #8932, #7857, #75012, #204984, #23030, #189817, #89145, #39307, #58758, #207133, #157343, #171440, #155199, #43597, #175721, #138962, #26243, #121715, #6780, #77134, #208190, #92362, #11053, #124910, #59823, #56629, #73942, #140037, #190873, #72855, #206061, #158399, #123853, #107576, #122794, #41467, #93418, #42539, #188752, #90209, #173610, #25183, #40391, #27313, #106495, #108642, #172521, #24106, #9997, #76074, #91284, #141122, #191933, #142174, #125976, #109716, #143255, #80337, #200194, #13198, #112913, #917, #110775, #78201, #116894, #178924, #30539, #162673, #14243, #28390, #149337, #45731, #29466, #100583, #144326, #176775, #111850, #127048, #145392, #177854, #51847, #50765, #84331, #96619, #194079, #199121, #209244, #129187, #18247, #1984, #60888, #160524, #94486, #68048, #12129, #211390, #63018, #66984, #195165, #95557, #182893, #161608, #34510, #133122, #210325, #193008, #61962, #44661, #128119, #79274, #46800, #166657, #150417, #134185, #117966, #183960, #35571, #101651, #167718, #19321, #85397, #105973, #38789, #102724, #73407, #151483, #119031, #169848, #137372, #71259, #6260, #155745, #104870, #24653, #171995, #152534, #55042, #5183, #3053, #203389, #21435, #4120, #103798, #57174, #70189, #202323, #153612, #186089, #204455, #121191, #187160, #89694, #39864, #40940, #170915, #69122, #7330, #22510, #52897, #168781, #185013, #88620, #139510, #23587, #107045, #154675, #135243, #205537, #72331, #36640, #20386, #86470, #138437, #136301, #56109, #189300, #122266, #53973, #37720, #87543, #188224 ),
 ( #123336, #120110, #173072, #201257, #176267, #78741, #109198, #208734, #93965, #206609, #174151, #209799, #60361, #126524, #44137, #110258, #124395, #27869, #141667, #125456, #193567, #25724, #58239, #207678, #8408, #26792, #59297, #144865, #143802, #177328, #192485, #75557, #77681, #90760, #10538, #111325, #95026, #156821, #42015, #190353, #161076, #108124, #92897, #158943, #160006, #76611, #191418, #61434, #43085, #127601, #11607, #91833, #74493, #157892, #140599, #9484, #175210, #142725, #45210, #28942, #12667, #210872, #62497, #128662, #194630, #46271, #112388, #178400, #198867, #131812, #195710, #166393, #30012, #211935, #48411, #15860, #164271, #99279, #34254, #197821, #117715, #50514, #31088, #148029, #98219, #96096, #81946, #114523, #97161, #196768, #150162, #163216, #80890, #32139, #64634, #83000, #214039, #49453, #65664, #165327, #67787, #100326, #180518, #115571, #17984, #14799, #181567, #63570, #33196, #16920, #162151, #84074, #149076, #132863, #146980, #133937, #653, #116637, #66720, #47345, #182632, #1730, #212997, #199943, #51591, #130773, #13738, #79811, #129726, #145923, #113459, #179464, #185823, #88352, #19061, #69928, #183705, #101391, #137107, #136040, #203136, #118771, #151226, #103533, #2795, #167465, #186898, #120925, #70994, #85139, #68866, #171722, #89429, #52641, #154416, #35313, #134986, #205272, #121998, #5995, #139240, #38530, #187964, #184754, #202052, #53712, #104608, #200996, #119845, #72066, #37454, #169592, #36382, #170655, #22242, #21175, #87278, #4917, #20124, #102460, #153347, #56912, #86210, #168526, #152282, #54778, #138176, #3855, #204186, #55842, #39592, #105695, #23321, #155480, #7063, #73136, #26535, #110001, #209536, #158685, #78490, #124139, #9225, #77425, #44954, #141412, #206349, #75297, #43887, #144607, #123085, #92643, #93706, #59038, #190101, #142464, #111062, #210622, #76357, #160818, #27606, #207419, #61178, #60108, #159746, #11344, #125196, #41754, #208472, #177068, #189042, #126267, #12410, #143542, #191159, #127338, #192224, #193308, #176014, #42826, #28684, #40679, #94770, #108932, #174953, #106782, #107866, #10283, #156558, #172810, #24382, #90495, #8153, #74237, #140330, #25467, #57976, #173892, #91575, #157627, #79559, #16668, #165077, #179208, #115327, #31892, #30832, #63312, #96908, #161897, #149904, #166136, #17723, #64380, #181318, #112138, #162960, #62248, #194376, #15603, #14539, #81690, #211676, #29756, #196516, #95841, #46019, #65413, #213790, #164028, #178142, #13484, #50264, #182371, #145678, #32946, #128409, #129473, #83811, #398, #99020, #195455, #131562, #66469, #47084, #80636, #146728, #197563, #113202, #212746, #82752, #130525, #48159, #114271, #49207, #148825, #180268, #97969, #147774, #132610, #198617, #116382, #34000, #100074, #89180, #117456, #3604, #37204, #1471, #67538, #4668, #69681, #120671, #21985, #118521, #101125, #104352, #119591, #202878, #88094, #103278, #171474, #2537, #102208, #170397, #137922, #19874, #84885, #168273, #136854, #23064, #133680, #185574, #5733, #199685, #167213, #18801, #71812, #150972, #135785, #201809, #153093, #53452, #200744, #54526, #184505, #38275, #169340, #68612, #51329, #134737, #183450, #35054, #85958, #52393, #152033, #36124, #20925, #87021, #70741, #186649, #154167, #203943, #55590, #121745, #187713, #39342 ),
 ( #105438, #156306, #58792, #8971, #155232, #75045, #25215, #7890, #107611, #60928, #73978, #206096, #157377, #189853, #208225, #141160, #207168, #93456, #43636, #44702, #124947, #72891, #159493, #190909, #56665, #172554, #188790, #42573, #122829, #108676, #193048, #76107, #90240, #41498, #91319, #174704, #6813, #127085, #40425, #158432, #138997, #140072, #142211, #109751, #57730, #26280, #77169, #92394, #123887, #10033, #173642, #59857, #143290, #126009, #191970, #175761, #106528, #24138, #27354, #11092, #209281, #110810, #176815, #28430, #205019, #145430, #129228, #197317, #29505, #210364, #211430, #12169, #30578, #63061, #148584, #147525, #181072, #212494, #79314, #81448, #94523, #14284, #115076, #160561, #64135, #65169, #96659, #161646, #114024, #16417, #50009, #47914, #132367, #213546, #112952, #32690, #31641, #131324, #180020, #80379, #163776, #198369, #164827, #178963, #146475, #82497, #13241, #162712, #128160, #130279, #196267, #78241, #153, #97718, #48958, #195201, #116133, #46838, #98771, #15355, #111888, #66219, #182122, #144363, #62004, #194121, #45771, #95598, #177892, #133428, #121492, #137672, #203694, #35881, #152843, #83563, #134496, #33751, #165894, #201559, #200499, #53205, #183200, #1227, #168023, #67289, #17479, #36947, #185323, #135535, #149645, #199435, #21734, #153914, #117203, #4417, #99828, #51078, #55340, #186390, #70488, #34806, #103027, #38027, #100881, #52142, #118270, #169082, #166968, #184254, #136604, #101956, #19627, #18558, #20681, #86772, #85698, #151786, #69430, #84635, #150726, #3360, #2286, #68362, #119336, #202628, #54278, #120416, #104098, #170148, #87843, #5484, #71565, #207970, #89991, #72643, #75851, #91059, #174446, #59596, #8709, #143028, #188532, #73716, #141958, #109494, #205843, #56408, #139814, #108425, #209024, #107351, #42309, #191716, #140895, #60660, #125753, #40162, #157120, #41244, #187464, #173373, #57476, #106276, #123635, #93198, #172297, #23885, #189598, #7631, #26022, #24958, #74794, #43373, #175501, #76904, #206905, #105179, #27091, #58536, #88924, #204757, #6562, #124691, #154977, #190649, #10830, #92132, #122570, #158187, #9779, #159229, #39093, #171215, #138739, #22809, #156043, #127904, #113756, #81183, #177633, #212230, #48695, #128951, #29242, #178696, #79043, #63864, #114809, #145159, #30310, #130019, #28167, #210097, #31377, #96396, #162446, #80108, #146213, #160302, #196010, #95333, #161382, #15093, #61737, #94263, #12967, #44438, #62789, #211164, #180808, #179761, #213293, #14022, #111621, #97453, #126823, #46567, #147261, #131068, #192780, #77979, #11906, #197056, #144103, #194929, #112686, #47645, #163508, #64919, #32434, #98502, #164564, #16149, #193856, #110556, #45505, #176557, #82234, #148325, #214324, #166698, #182936, #181857, #151524, #132106, #3093, #185055, #115872, #34552, #201297, #20427, #167762, #17218, #202364, #65956, #33493, #84376, #51887, #54013, #186129, #149379, #36681, #198114, #99566, #87583, #4161, #102768, #21474, #69163, #70231, #962, #150463, #18289, #135283, #83294, #2024, #168823, #68093, #134228, #165630, #52938, #119074, #200237, #183999, #101691, #116936, #199164, #35613, #153655, #100623, #49745, #67027, #118010, #19359, #133164, #50810, #86510, #85439, #152574, #136343, #120153, #37764, #103836, #169885, #209571, #94806 ),
 ( #154721, #39909, #155789, #60143, #71298, #128445, #187203, #11381, #5224, #6303, #61216, #177104, #56149, #93742, #144642, #7373, #122311, #126300, #172039, #159781, #210657, #23632, #192260, #77460, #121233, #88661, #127373, #43922, #110037, #176049, #27642, #38832, #143578, #188268, #106018, #111098, #72378, #104915, #89739, #137410, #73452, #139554, #62285, #193344, #160855, #44989, #204499, #28719, #203430, #205581, #12447, #78525, #55084, #170956, #22556, #194411, #138477, #46053, #112174, #178178, #29794, #95878, #435, #130561, #198651, #115362, #162996, #79596, #47124, #180304, #65448, #165111, #63349, #30868, #66506, #131598, #197600, #181354, #32980, #195489, #99056, #212781, #196551, #50300, #96946, #129508, #64417, #145715, #98005, #48194, #1507, #132645, #34038, #49243, #146763, #148862, #161933, #81729, #182409, #166172, #13523, #113240, #179244, #17761, #14577, #164062, #15641, #16703, #147811, #114306, #116418, #31926, #100111, #82789, #80672, #211713, #213830, #83849, #149938, #67573, #133718, #199723, #51369, #117492, #183483, #35092, #186682, #5771, #151009, #3638, #22021, #55625, #202917, #52431, #23100, #101163, #68648, #119626, #87057, #20959, #170434, #105474, #54561, #188827, #121782, #102240, #4700, #169375, #167248, #153129, #185611, #168312, #53489, #6849, #19909, #152068, #103313, #135820, #154202, #70776, #136890, #39377, #203978, #205057, #120707, #18836, #171507, #38310, #2578, #118557, #134771, #104387, #200779, #88131, #139033, #71850, #36161, #201844, #37242, #137958, #84920, #72927, #184539, #187749, #85994, #69717, #89216, #155268, #56699, #122866, #176849, #42606, #91352, #92427, #207204, #126041, #28462, #143321, #157414, #93487, #10067, #9005, #41534, #75080, #140106, #128194, #144397, #210398, #108713, #159526, #90274, #141193, #40462, #172593, #208259, #58828, #59892, #189892, #7928, #174741, #74014, #24171, #43669, #192004, #142246, #156343, #206133, #94556, #160595, #123924, #11125, #106565, #57763, #62041, #193086, #77203, #107645, #109786, #44737, #173677, #124982, #190942, #175795, #25252, #26314, #209315, #158467, #76143, #27387, #60962, #127119, #110843, #12201, #78271, #30611, #112986, #97752, #1262, #96700, #67320, #95630, #196300, #15387, #194155, #45803, #197350, #47946, #98805, #186, #162747, #79348, #82532, #163811, #181107, #66254, #81481, #149681, #195234, #80413, #148618, #116169, #212528, #63095, #146511, #115110, #111924, #177924, #147558, #164858, #130312, #46872, #213580, #182155, #29539, #65203, #17512, #16451, #64169, #132402, #131355, #198404, #48992, #114061, #32723, #83599, #50046, #180053, #31675, #33785, #178996, #99864, #13274, #165927, #161680, #145465, #211460, #129264, #14320, #35915, #171247, #85736, #21767, #151821, #150760, #87875, #101990, #22843, #3395, #153947, #69464, #2322, #5516, #71596, #168059, #186424, #103063, #19661, #134526, #135569, #18593, #6596, #88958, #155011, #201593, #38063, #183235, #53241, #133464, #51110, #86807, #119370, #152873, #68398, #100914, #185358, #167002, #117235, #136637, #70521, #20714, #34839, #84671, #121527, #39127, #200532, #104133, #199468, #52178, #118303, #137705, #170179, #184290, #202662, #203725, #36980, #169117, #4451, #54312, #120450, #55373, #187497, #105210, #24994, #40198, #108462, #174482, #91097 ),
 ( #72677, #138773, #26058, #157157, #75887, #125791, #123670, #23920, #208009, #206944, #158223, #191753, #124729, #143065, #73753, #107391, #59633, #27127, #173413, #156082, #8749, #9812, #204791, #56444, #190688, #43408, #74831, #57512, #92172, #93233, #122603, #141995, #188566, #109532, #140930, #159266, #175537, #10866, #76940, #42347, #106309, #172332, #90026, #7668, #139848, #205877, #189633, #41282, #58573, #37683, #153573, #117929, #122228, #53936, #154640, #52862, #4081, #171955, #118995, #102686, #120072, #86433, #104834, #186048, #103760, #204416, #6221, #155707, #169809, #183923, #56072, #21399, #167679, #69084, #85361, #87509, #19279, #5143, #89654, #187120, #201221, #152498, #202283, #71218, #35535, #23544, #151443, #55005, #51811, #184974, #38753, #72291, #168744, #137335, #188188, #203352, #20348, #121155, #70152, #170879, #39823, #136263, #22471, #88582, #3015, #135204, #138398, #105931, #7288, #73366, #139471, #36599, #101611, #41973, #25686, #93928, #140558, #107008, #108084, #123300, #141628, #174113, #45175, #44102, #77644, #109158, #190315, #192447, #205500, #125413, #11574, #209760, #57133, #156785, #90723, #61401, #8371, #207637, #59255, #142686, #191379, #91794, #110222, #157851, #27832, #158905, #206572, #189263, #74454, #40902, #24614, #9445, #75516, #43045, #175170, #173032, #76574, #58199, #208696, #176230, #124358, #26757, #126483, #159969, #92858, #10501, #127564, #60323, #143766, #193533, #111287, #177293, #28907, #94992, #161038, #78704, #12633, #145888, #48373, #212960, #144830, #64598, #14764, #130739, #112354, #128626, #147995, #81907, #32101, #194593, #178367, #132829, #50478, #13703, #49417, #210838, #29975, #166356, #82966, #115537, #100289, #214005, #149039, #79776, #163179, #97127, #65627, #162113, #80854, #181532, #146945, #196732, #96060, #131776, #197779, #114485, #180482, #98186, #195674, #63536, #164234, #17946, #47310, #62464, #46237, #15822, #33160, #211899, #129691, #99241, #165290, #16884, #614, #113424, #179430, #66682, #198833, #116599, #182593, #34216, #31051, #123935, #56708, #172602, #188836, #207215, #122875, #157425, #196040, #79072, #90284, #189903, #91365, #58839, #6858, #63892, #40472, #158479, #155278, #156353, #145190, #112715, #206143, #26326, #80139, #9016, #57774, #124994, #107659, #92440, #146242, #173688, #190953, #10079, #106575, #24181, #62822, #42617, #108727, #174753, #211196, #7937, #128982, #41545, #25264, #46597, #74027, #140117, #75092, #72937, #141204, #194961, #212258, #178727, #30342, #96427, #162478, #14050, #139041, #130047, #47674, #113785, #205066, #179787, #31407, #101723, #48724, #99594, #165660, #34582, #214355, #135314, #49774, #200267, #115901, #114838, #51919, #118042, #65985, #150494, #67057, #132135, #98532, #198142, #197086, #185086, #201328, #52966, #17247, #2053, #147291, #181886, #97481, #15123, #50843, #33522, #116970, #32463, #64945, #83324, #131097, #81211, #100654, #166732, #199195, #213323, #180836, #85468, #3124, #164593, #68126, #163538, #16179, #119104, #35644, #134261, #82263, #18323, #167794, #148356, #149411, #993, #84406, #133193, #182967, #184028, #19389, #151556, #69193, #39937, #106045, #170985, #154750, #72406, #87612, #169917, #6334, #58313, #153683, #124468, #152605, #38862, #138506, #36710, #102796, #172068, #104945 ) ),
 .UNSPECIFIED., .T., .F., .F. ) 
 B_SPLINE_SURFACE_WITH_KNOTS ( ( 4, 3, 4 ),
 ( 4, 1, 1, 1, 1, 1, 1, 1, 1, 1, 1, 1, 1, 1, 1, 1, 1, 1, 1, 1, 1, 1, 1, 1, 1, 1, 1, 1, 1, 1, 1, 1, 1, 1, 1, 1, 1, 1, 1, 1, 1, 1, 1, 1, 1, 1, 1, 1, 1, 1, 1, 1, 1, 1, 1, 1, 1, 1, 1, 1, 1, 1, 1, 1, 1, 1, 1, 1, 1, 1, 1, 1, 1, 1, 1, 1, 1, 1, 1, 1, 1, 1, 1, 1, 1, 1, 1, 1, 1, 1, 1, 1, 1, 1, 1, 1, 1, 1, 1, 1, 1, 1, 1, 1, 1, 1, 1, 1, 1, 1, 1, 1, 1, 1, 1, 1, 1, 1, 1, 1, 1, 1, 1, 1, 1, 1, 1, 1, 1, 1, 1, 1, 1, 1, 1, 1, 1, 1, 1, 1, 1, 1, 1, 1, 1, 1, 1, 1, 1, 1, 1, 1, 1, 1, 1, 1, 1, 1, 1, 1, 1, 1, 1, 1, 1, 1, 1, 1, 1, 1, 1, 1, 1, 1, 1, 1, 1, 1, 1, 1, 1, 1, 1, 1, 1, 1, 1, 1, 1, 1, 1, 1, 1, 1, 1, 1, 1, 1, 1, 1, 1, 1, 1, 1, 1, 1, 1, 1, 1, 1, 1, 1, 1, 1, 1, 1, 1, 1, 1, 1, 1, 1, 1, 1, 1, 1, 1, 1, 1, 1, 1, 1, 1, 1, 1, 1, 1, 1, 1, 1, 1, 1, 1, 1, 1, 1, 1, 1, 1, 1, 1, 1, 1, 1, 1, 1, 1, 1, 1, 1, 1, 1, 1, 1, 1, 1, 1, 1, 1, 1, 1, 1, 1, 1, 1, 1, 1, 1, 1, 1, 1, 1, 1, 1, 1, 1, 1, 1, 1, 1, 1, 1, 1, 1, 1, 1, 1, 1, 1, 1, 1, 1, 1, 1, 1, 1, 1, 1, 1, 1, 1, 1, 1, 1, 1, 1, 1, 1, 1, 1, 1, 1, 1, 1, 1, 1, 1, 1, 1, 1, 1, 1, 1, 1, 1, 1, 1, 1, 1, 1, 1, 1, 1, 1, 1, 1, 1, 1, 1, 1, 1, 1, 1, 1, 1, 1, 1, 1, 1, 1, 1, 1, 1, 1, 1, 1, 1, 1, 1, 1, 1, 1, 1, 1, 1, 1, 1, 1, 1, 1, 1, 1, 1, 1, 4 ),
 ( 0.000000000000000000, 0.5000000000000000000, 1.000000000000000000 ),
 ( 0.000000000000000000, 0.002600063085273907840, 0.005208809393482579861, 0.007813201938950280895, 0.01041611862257568050, 0.01302098276518856741, 0.01562474632808895890, 0.01822919105953027183, 0.02083324087635668453, 0.02343728507989274734, 0.02604173773626635227, 0.02864548761524753420, 0.03125016255115702773, 0.03385383280295282959, 0.03645844125268089125, 0.03906229690237970897, 0.04166656525949016115, 0.04427081591349327910, 0.04687468903198145631, 0.04947928942627017462, 0.05208296534865054783, 0.05468764290212216328, 0.05729137561078536528, 0.05989584521530456201, 0.06249987723257615507, 0.06510392926424246607, 0.06770838613806146045, 0.07031213076997053224, 0.07291680575263978503, 0.07552047744215656389, 0.07812508546332513903, 0.08072894086165181837, 0.08333320924388483431, 0.08593745993457323207, 0.08854133291633270453, 0.09114593330519306369, 0.09374960916840779923, 0.09635428668231969807, 0.09895801939011879267, 0.1015624889210437753, 0.1041665209728785957, 0.1067705729027476208, 0.1093750297965602747, 0.1119787743537518920, 0.1145834493281674554, 0.1171871210017138010, 0.1197917289818775377, 0.1223955844170728779, 0.1249998527215379351, 0.1276041034591044177, 0.1302079763611066199, 0.1328125767709825433, 0.1354162526020633861, 0.1380209301064295735, 0.1406246628425296130, 0.1432291323291436380, 0.1458331644451768827, 0.1484372163025670099, 0.1510416732455448496, 0.1536454177576472568, 0.1562500927529001105, 0.1588537644400710158, 0.1614583724083656635, 0.1640622279099430147, 0.1666664961659596600, 0.1692707469797122277, 0.1718746198314790308, 0.1744792202914958457, 0.1770828961200470730, 0.1796875736439581817, 0.1822913064379278192, 0.1848957759094348730, 0.1874998081190861754, 0.1901038599334289314, 0.1927083169547665342, 0.1953120614513534081, 0.1979167364965291054, 0.2005204082269216870, 0.2031250162124720871, 0.2057288718099357372, 0.2083331400468157457, 0.2109373909660553770, 0.2135412637971000893, 0.2161458643363758370, 0.2187495401919937743, 0.2213542177645327069, 0.2239579506459335456, 0.2265624201315297737, 0.2291664524642116896, 0.2317705042649303715, 0.2343749613938155840, 0.2369787059044528299, 0.2395833810286300269, 0.2421870528318344207, 0.2447916608637582536, 0.2473955165866061623, 0.2499997848336539263, 0.2526040358876752157, 0.2552079087275039293, 0.2578125093751503782, 0.2604161852874245509, 0.2630208629376679097, 0.2656245959360551967, 0.2682290654649299166, 0.2708330979500496172, 0.2734371497665608608, 0.2760416070321756732, 0.2786453515864226738, 0.2812500268186742258, 0.2838536987242743503, 0.2864583068316831627, 0.2890621627094078216, 0.2916664309959213219, 0.2942706822140139789, 0.2968745550921262355, 0.2994791558772498252, 0.3020828318757637354, 0.3046875096327826826, 0.3072912427777066413, 0.3098957123790437307, 0.3124997450460035853, 0.3151037969077182255, 0.3177082543392401592, 0.3203119989666507461, 0.3229166743360447622, 0.3255203463736199843, 0.3281249545856204097, 0.3307288106477103140, 0.3333330790029824242, 0.3359373304144318562, 0.3385412033603223403, 0.3411458043120255135, 0.3437494804263583337, 0.3463541583192197293, 0.3489578916402267250, 0.3515623613432052874, 0.3541663942214042238, 0.3567704461577280162, 0.3593749037843310123, 0.3619786485144548260, 0.3645833240500557237, 0.3671869962491814965, 0.3697916045948764219, 0.3723954608708167080, 0.3749997293241361662, 0.3776039809582251716, 0.3802078540013843488, 0.3828124551487663840, 0.3854161314084936785, 0.3880208094662612184, 0.3906245429928945634, 0.3932290128266905938, 0.3958330459455252637, 0.3984370979858605777, 0.4010415558367163569, 0.4036453006990994852, 0.4062499764299690730, 0.4088536488202184072, 0.4114582573287078326, 0.4140621138479816388, 0.4166663824286341855, 0.4192706343146435644, 0.4218745074845589027, 0.4244791088567174686, 0.4270827852914125256, 0.4296874635431477407, 0.4322911973049493040, 0.4348956672987361882, 0.4374997006876018557, 0.4401037528613486738, 0.4427082109656274023, 0.4453119559898139901, 0.4479166319450127998, 0.4505203045559570407, 0.4531249132563394122, 0.4557287700484292658, 0.4583330387856985322, 0.4609372909529084184, 0.4635411642790657205, 0.4661457659050973201, 0.4687494425443319290, 0.4713541210190953512, 0.4739578550456061690, 0.4765623252285562383, 0.4791663589168480009, 0.4817704112534048067, 0.4843748696402766507, 0.4869786148558097882, 0.4895832910643978519, 0.4921869639256079565, 0.4947915728469811647, 0.4973954299413693159, 0.4999996988645384333, 0.5026039513422294602, 0.5052078248541136407, 0.5078124267631153321, 0.5104161036364611714, 0.5130207823633133879, 0.5156245166840751626, 0.5182289870853604707, 0.5208330211024742029, 0.5234370736312391470, 0.5260415323298749390, 0.5286452777662975500, 0.5312499542573357880, 0.5338536273983837122, 0.5364582365698458144, 0.5390620939960163449, 0.5416663631343685559, 0.5442706159518226894, 0.5468744896789192733, 0.5494790918999890028, 0.5520827690370186946, 0.5546874480450217915, 0.5572911826895774468, 0.5598956533383712131, 0.5624996877137050655, 0.5651037404640770756, 0.5677081995036498130, 0.5703119451905063197, 0.5729166219930570403, 0.5755202954435161278, 0.5781249048941674573, 0.5807287626816063364, 0.5833330320644263267, 0.5859372852509285856, 0.5885411592227242084, 0.5911457617849628088, 0.5937494392152512512, 0.5963541185334689798, 0.5989578535313645480, 0.6015623244568418793, 0.6041663592197970001, 0.6067704122211770024, 0.6093748716308627911, 0.6119786175976995590, 0.6145832947408284008, 0.6171869685302752151, 0.6197915782892181591, 0.6223954364674153528, 0.6249997061239902507, 0.6276039597088286515, 0.6302078339548128350, 0.6328124368873246919, 0.6354161146404495586, 0.6380207942979494451, 0.6406245296787346222, 0.6432290009100736228, 0.6458330360900554901, 0.6484370893718474083, 0.6510415491808263511, 0.6536452954571934093, 0.6562499729699700080, 0.6588536471279848872, 0.6614582572243260516, 0.6640621158227759668, 0.6666663857823964534, 0.6692706397948642305, 0.6718745143445301604, 0.6744791176764239893, 0.6770827957819672838, 0.6796874758078212952, 0.6822912116010506622, 0.6848956831674339885, 0.6874997187938534093, 0.6901037723854651640, 0.6927082326229228038, 0.6953119792383747333, 0.6979166571498732763, 0.7005203317060422208, 0.7031249421688929857, 0.7057288012170955804, 0.7083330715090569996, 0.7109373259784533827, 0.7135412008612989077, 0.7161458046216893081, 0.7187494831092385850, 0.7213541635325240176, 0.7239578997677582617, 0.7265623716983737879, 0.7291664078006476757, 0.7317704617314926274, 0.7343749224266207243, 0.7369786694107173242, 0.7395833477500189934, 0.7421870227339337767, 0.7447916335924112952, 0.7473954931198736329, 0.7499997637734774347, 0.7526040187291080930, 0.7552078939746372788, 0.7578124981926457338, 0.7604161770917949870, 0.7630208579415957981, 0.7656245946484027121, 0.7682290669724446408, 0.7708331035799980135, 0.7734371578794957403, 0.7760416190614934928, 0.7786453664438016675, 0.7812500452399944173, 0.7838537206812543623, 0.7864583319644831150, 0.7890621920007202528, 0.7916664630452742157, 0.7942707185164536998, 0.7968745941541772737, 0.7994791988589329268, 0.8020828781992835887, 0.8046875595046918406, 0.8072912967126475436, 0.8098957694593176271, 0.8124998066015838294, 0.8151038612991610144, 0.8177083229972362810, 0.8203120708073305956, 0.8229167500895105958, 0.8255204260177235742, 0.8281250377548363684, 0.8307288983293719120, 0.8333331697941922522, 0.8359374258102438837, 0.8385413018696807885, 0.8411459070903221091, 0.8437495869014844940, 0.8463542686916004643, 0.8489580064302900686, 0.8515624796287988296, 0.8541665173352209761, 0.8567705724603134065, 0.8593750347036837045, 0.8619787829711476057, 0.8645834627684209073, 0.8671871392132045608, 0.8697917514333429745, 0.8723956125757112989, 0.8749998844901232253, 0.8776041410803804288, 0.8802080175910590443, 0.8828126233567346048, 0.8854163036683286858, 0.8880209859722626442, 0.8906247242712825862, 0.8932291979508502067, 0.8958332362508822921, 0.8984372918329353030, 0.9010417546508288078, 0.9036455034052560675, 0.9062501837467389354, 0.9088538607377212308, 0.9114584734700372781, 0.9140623352097841936, 0.9166666076031229071, 0.9192708647969299873, 0.9218747417883903505, 0.9244793481282622682, 0.9270830289699085736, 0.9296877118167798937, 0.9322914507057830091, 0.9348959248956096868, 0.9374999638185942397, 0.9401040198872741005, 0.9427084833090058069, 0.9453122325795346725, 0.9479169134952544207, 0.9505205910598265584, 0.9531252043308329203, 0.9557290667238423909, 0.9583333396063040688, 0.9609375973010293448, 0.9635414750455153499, 0.9661460823481272664, 0.9687497623469286667, 0.9713544456720903941, 0.9739581901020435417, 0.9765626606554614897, 0.9791666924408860551, 0.9817707657828746992, 0.9843752055175947202, 0.9869789906880002128, 0.9895838567146432174, 0.9921867690109741345, 0.9947911791560083428, 0.9973999138825643263, 0.9999999999999998890 ),
 .UNSPECIFIED. ) 
 GEOMETRIC_REPRESENTATION_ITEM ( )  RATIONAL_B_SPLINE_SURFACE ( (
 ( 1.000000000000000222, 1.000000000000000222, 1.000000000000000222, 1.000000000000000222, 1.000000000000000444, 1.000000000000000444, 1.000000000000000222, 1.000000000000000444, 1.000000000000000222, 1.000000000000000444, 1.000000000000000444, 1.000000000000000000, 1.000000000000000222, 1.000000000000000000, 1.000000000000000222, 1.000000000000000222, 1.000000000000000444, 1.000000000000000000, 1.000000000000000444, 1.000000000000000444, 1.000000000000000222, 1.000000000000000222, 1.000000000000000000, 1.000000000000000222, 1.000000000000000000, 1.000000000000000444, 1.000000000000000000, 1.000000000000000444, 1.000000000000000222, 1.000000000000000000, 1.000000000000000666, 1.000000000000000000, 1.000000000000000222, 1.000000000000000666, 1.000000000000000222, 1.000000000000000444, 1.000000000000000222, 1.000000000000000444, 1.000000000000000000, 1.000000000000000444, 1.000000000000000000, 1.000000000000000444, 1.000000000000000000, 1.000000000000000444, 1.000000000000000000, 1.000000000000000222, 1.000000000000000444, 1.000000000000000000, 1.000000000000000444, 1.000000000000000222, 1.000000000000000222, 1.000000000000000444, 1.000000000000000222, 1.000000000000000444, 1.000000000000000222, 1.000000000000000222, 1.000000000000000444, 1.000000000000000444, 1.000000000000000222, 1.000000000000000222, 1.000000000000000444, 1.000000000000000222, 1.000000000000000444, 1.000000000000000000, 1.000000000000000222, 1.000000000000000222, 1.000000000000000222, 1.000000000000000222, 1.000000000000000444, 1.000000000000000000, 0.9999999999999997780, 1.000000000000000444, 1.000000000000000444, 1.000000000000000222, 1.000000000000000222, 1.000000000000000444, 0.9999999999999997780, 1.000000000000000666, 1.000000000000000000, 1.000000000000000000, 1.000000000000000444, 1.000000000000000222, 1.000000000000000222, 0.9999999999999997780, 1.000000000000000222, 1.000000000000000444, 0.9999999999999997780, 1.000000000000000444, 1.000000000000000000, 1.000000000000000000, 1.000000000000000444, 1.000000000000000000, 1.000000000000000444, 1.000000000000000444, 0.9999999999999997780, 1.000000000000000444, 1.000000000000000444, 1.000000000000000444, 1.000000000000000444, 1.000000000000000000, 1.000000000000000444, 1.000000000000000222, 1.000000000000000000, 1.000000000000000444, 1.000000000000000444, 1.000000000000000222, 1.000000000000000000, 1.000000000000000444, 1.000000000000000444, 1.000000000000000000, 1.000000000000000222, 1.000000000000000000, 1.000000000000000444, 1.000000000000000222, 1.000000000000000444, 1.000000000000000222, 1.000000000000000444, 1.000000000000000444, 1.000000000000000000, 1.000000000000000666, 1.000000000000000222, 1.000000000000000222, 1.000000000000000000, 1.000000000000000222, 1.000000000000000222, 1.000000000000000222, 1.000000000000000444, 1.000000000000000222, 1.000000000000000222, 1.000000000000000444, 0.9999999999999997780, 1.000000000000000666, 0.9999999999999997780, 1.000000000000000222, 1.000000000000000000, 1.000000000000000444, 1.000000000000000000, 1.000000000000000444, 1.000000000000000000, 1.000000000000000222, 1.000000000000000222, 1.000000000000000444, 1.000000000000000444, 1.000000000000000222, 1.000000000000000444, 1.000000000000000444, 1.000000000000000000, 1.000000000000000666, 1.000000000000000222, 1.000000000000000222, 1.000000000000000444, 1.000000000000000000, 1.000000000000000222, 1.000000000000000444, 1.000000000000000000, 1.000000000000000222, 1.000000000000000222, 1.000000000000000444, 1.000000000000000222, 1.000000000000000222, 1.000000000000000444, 1.000000000000000000, 1.000000000000000222, 1.000000000000000000, 1.000000000000000444, 1.000000000000000222, 1.000000000000000444, 1.000000000000000222, 1.000000000000000222, 1.000000000000000444, 1.000000000000000000, 1.000000000000000222, 1.000000000000000444, 1.000000000000000000, 1.000000000000000444, 1.000000000000000222, 1.000000000000000444, 1.000000000000000444, 1.000000000000000222, 1.000000000000000222, 1.000000000000000000, 1.000000000000000444, 1.000000000000000444, 1.000000000000000000, 1.000000000000000444, 1.000000000000000222, 1.000000000000000444, 1.000000000000000444, 1.000000000000000222, 1.000000000000000000, 1.000000000000000444, 1.000000000000000222, 1.000000000000000444, 1.000000000000000000, 1.000000000000000444, 1.000000000000000222, 1.000000000000000222, 1.000000000000000444, 1.000000000000000222, 1.000000000000000222, 1.000000000000000222, 1.000000000000000222, 1.000000000000000444, 1.000000000000000000, 1.000000000000000666, 1.000000000000000000, 1.000000000000000222, 1.000000000000000444, 1.000000000000000000, 1.000000000000000222, 1.000000000000000444, 1.000000000000000000, 1.000000000000000666, 0.9999999999999997780, 1.000000000000000222, 1.000000000000000444, 1.000000000000000000, 1.000000000000000444, 1.000000000000000222, 1.000000000000000444, 1.000000000000000000, 1.000000000000000444, 1.000000000000000222, 1.000000000000000222, 1.000000000000000000, 1.000000000000000444, 1.000000000000000222, 1.000000000000000000, 1.000000000000000222, 1.000000000000000222, 1.000000000000000222, 1.000000000000000444, 1.000000000000000000, 1.000000000000000444, 1.000000000000000222, 1.000000000000000222, 1.000000000000000222, 1.000000000000000000, 1.000000000000000666, 1.000000000000000000, 1.000000000000000000, 1.000000000000000222, 1.000000000000000444, 1.000000000000000222, 1.000000000000000444, 0.9999999999999997780, 1.000000000000000444, 1.000000000000000444, 0.9999999999999997780, 1.000000000000000444, 1.000000000000000444, 1.000000000000000444, 1.000000000000000222, 1.000000000000000444, 1.000000000000000444, 1.000000000000000000, 1.000000000000000444, 0.9999999999999997780, 1.000000000000000444, 0.9999999999999997780, 1.000000000000000444, 1.000000000000000000, 1.000000000000000444, 1.000000000000000444, 1.000000000000000444, 1.000000000000000222, 1.000000000000000444, 1.000000000000000444, 1.000000000000000222, 1.000000000000000222, 1.000000000000000000, 1.000000000000000222, 1.000000000000000444, 0.9999999999999997780, 1.000000000000000666, 0.9999999999999997780, 1.000000000000000444, 1.000000000000000222, 1.000000000000000222, 1.000000000000000000, 1.000000000000000222, 1.000000000000000222, 1.000000000000000000, 1.000000000000000000, 1.000000000000000444, 1.000000000000000222, 1.000000000000000444, 0.9999999999999997780, 1.000000000000000444, 1.000000000000000444, 1.000000000000000222, 1.000000000000000444, 1.000000000000000000, 1.000000000000000444, 1.000000000000000444, 0.9999999999999997780, 1.000000000000000444, 1.000000000000000222, 1.000000000000000444, 1.000000000000000222, 1.000000000000000222, 1.000000000000000444, 1.000000000000000000, 1.000000000000000000, 1.000000000000000444, 1.000000000000000444, 1.000000000000000444, 0.9999999999999997780, 1.000000000000000444, 1.000000000000000222, 1.000000000000000222, 1.000000000000000444, 1.000000000000000000, 1.000000000000000444, 1.000000000000000222, 1.000000000000000444, 1.000000000000000000, 1.000000000000000444, 1.000000000000000444, 1.000000000000000444, 1.000000000000000000, 1.000000000000000444, 1.000000000000000000, 1.000000000000000222, 1.000000000000000444, 1.000000000000000444, 1.000000000000000000, 1.000000000000000444, 1.000000000000000444, 1.000000000000000000, 1.000000000000000444, 1.000000000000000222, 1.000000000000000000, 1.000000000000000444, 1.000000000000000222, 1.000000000000000222, 1.000000000000000444, 1.000000000000000444, 1.000000000000000000, 1.000000000000000000, 1.000000000000000444, 1.000000000000000000, 1.000000000000000222, 1.000000000000000444, 1.000000000000000000, 1.000000000000000222, 1.000000000000000444, 0.9999999999999997780, 1.000000000000000444, 1.000000000000000222, 1.000000000000000000, 1.000000000000000444, 1.000000000000000000, 1.000000000000000444, 1.000000000000000444, 1.000000000000000000, 1.000000000000000222, 1.000000000000000222, 1.000000000000000222, 1.000000000000000444, 1.000000000000000222, 1.000000000000000000, 1.000000000000000222, 1.000000000000000444, 1.000000000000000444, 1.000000000000000222, 1.000000000000000444, 1.000000000000000444, 1.000000000000000000, 1.000000000000000000, 1.000000000000000666, 0.9999999999999997780, 1.000000000000000444, 0.9999999999999997780, 1.000000000000000222, 0.9999999999999997780, 1.000000000000000444, 1.000000000000000000, 1.000000000000000222, 1.000000000000000222, 1.000000000000000444, 1.000000000000000000, 1.000000000000000000, 1.000000000000000444, 1.000000000000000000, 1.000000000000000222, 1.000000000000000222),
 ( 0.3333333333333334259, 0.3333333333333334259, 0.3333333333333334814, 0.3333333333333333703, 0.3333333333333335369, 0.3333333333333335369, 0.3333333333333334259, 0.3333333333333334259, 0.3333333333333334259, 0.3333333333333334814, 0.3333333333333334259, 0.3333333333333334259, 0.3333333333333334259, 0.3333333333333334259, 0.3333333333333333148, 0.3333333333333334259, 0.3333333333333334814, 0.3333333333333333703, 0.3333333333333335369, 0.3333333333333335924, 0.3333333333333334259, 0.3333333333333334814, 0.3333333333333333703, 0.3333333333333334259, 0.3333333333333333703, 0.3333333333333334814, 0.3333333333333333703, 0.3333333333333334259, 0.3333333333333333703, 0.3333333333333333703, 0.3333333333333335369, 0.3333333333333334259, 0.3333333333333333703, 0.3333333333333335924, 0.3333333333333334259, 0.3333333333333334259, 0.3333333333333333703, 0.3333333333333334814, 0.3333333333333333703, 0.3333333333333334814, 0.3333333333333333703, 0.3333333333333335369, 0.3333333333333333148, 0.3333333333333334814, 0.3333333333333333703, 0.3333333333333334814, 0.3333333333333334259, 0.3333333333333333703, 0.3333333333333334259, 0.3333333333333334259, 0.3333333333333334814, 0.3333333333333333703, 0.3333333333333335369, 0.3333333333333334259, 0.3333333333333334259, 0.3333333333333334814, 0.3333333333333334259, 0.3333333333333334259, 0.3333333333333333703, 0.3333333333333333703, 0.3333333333333335924, 0.3333333333333334259, 0.3333333333333335369, 0.3333333333333333703, 0.3333333333333333703, 0.3333333333333333703, 0.3333333333333334814, 0.3333333333333333703, 0.3333333333333335369, 0.3333333333333332593, 0.3333333333333333703, 0.3333333333333334259, 0.3333333333333335369, 0.3333333333333334259, 0.3333333333333333703, 0.3333333333333334814, 0.3333333333333333703, 0.3333333333333335369, 0.3333333333333334259, 0.3333333333333333148, 0.3333333333333334814, 0.3333333333333334814, 0.3333333333333334259, 0.3333333333333333148, 0.3333333333333333703, 0.3333333333333334814, 0.3333333333333333703, 0.3333333333333334814, 0.3333333333333333148, 0.3333333333333334259, 0.3333333333333334814, 0.3333333333333333703, 0.3333333333333335369, 0.3333333333333334814, 0.3333333333333333148, 0.3333333333333335369, 0.3333333333333334814, 0.3333333333333334259, 0.3333333333333334814, 0.3333333333333333703, 0.3333333333333334814, 0.3333333333333334259, 0.3333333333333333703, 0.3333333333333334259, 0.3333333333333335369, 0.3333333333333334259, 0.3333333333333334259, 0.3333333333333334814, 0.3333333333333335369, 0.3333333333333333148, 0.3333333333333334259, 0.3333333333333333148, 0.3333333333333335924, 0.3333333333333334259, 0.3333333333333334814, 0.3333333333333333703, 0.3333333333333334814, 0.3333333333333334259, 0.3333333333333333703, 0.3333333333333335924, 0.3333333333333334259, 0.3333333333333334259, 0.3333333333333333703, 0.3333333333333334259, 0.3333333333333333703, 0.3333333333333333703, 0.3333333333333335369, 0.3333333333333334259, 0.3333333333333333703, 0.3333333333333334814, 0.3333333333333333148, 0.3333333333333335924, 0.3333333333333333148, 0.3333333333333334259, 0.3333333333333333148, 0.3333333333333335924, 0.3333333333333333703, 0.3333333333333335369, 0.3333333333333333148, 0.3333333333333334259, 0.3333333333333334814, 0.3333333333333334259, 0.3333333333333334259, 0.3333333333333334259, 0.3333333333333334259, 0.3333333333333334259, 0.3333333333333334259, 0.3333333333333334814, 0.3333333333333334259, 0.3333333333333333703, 0.3333333333333334814, 0.3333333333333333148, 0.3333333333333334259, 0.3333333333333334814, 0.3333333333333334259, 0.3333333333333333703, 0.3333333333333334259, 0.3333333333333334814, 0.3333333333333333703, 0.3333333333333334259, 0.3333333333333334814, 0.3333333333333333703, 0.3333333333333333703, 0.3333333333333333703, 0.3333333333333335369, 0.3333333333333333703, 0.3333333333333334814, 0.3333333333333334259, 0.3333333333333333703, 0.3333333333333334814, 0.3333333333333333703, 0.3333333333333334259, 0.3333333333333335369, 0.3333333333333333703, 0.3333333333333334259, 0.3333333333333334814, 0.3333333333333334259, 0.3333333333333335924, 0.3333333333333333703, 0.3333333333333334259, 0.3333333333333333148, 0.3333333333333335369, 0.3333333333333334259, 0.3333333333333334259, 0.3333333333333334259, 0.3333333333333333703, 0.3333333333333335369, 0.3333333333333334259, 0.3333333333333333703, 0.3333333333333334259, 0.3333333333333334259, 0.3333333333333333703, 0.3333333333333335369, 0.3333333333333333703, 0.3333333333333335369, 0.3333333333333333703, 0.3333333333333334814, 0.3333333333333334259, 0.3333333333333333703, 0.3333333333333334259, 0.3333333333333333703, 0.3333333333333334814, 0.3333333333333334259, 0.3333333333333333703, 0.3333333333333335369, 0.3333333333333333703, 0.3333333333333333703, 0.3333333333333334814, 0.3333333333333333703, 0.3333333333333333148, 0.3333333333333335924, 0.3333333333333333148, 0.3333333333333335924, 0.3333333333333332593, 0.3333333333333334814, 0.3333333333333334814, 0.3333333333333334259, 0.3333333333333334259, 0.3333333333333334814, 0.3333333333333334259, 0.3333333333333333703, 0.3333333333333335369, 0.3333333333333334259, 0.3333333333333334814, 0.3333333333333333703, 0.3333333333333334259, 0.3333333333333333703, 0.3333333333333334814, 0.3333333333333333703, 0.3333333333333335369, 0.3333333333333333148, 0.3333333333333335924, 0.3333333333333333703, 0.3333333333333334259, 0.3333333333333333703, 0.3333333333333334259, 0.3333333333333333703, 0.3333333333333333703, 0.3333333333333335924, 0.3333333333333334259, 0.3333333333333333148, 0.3333333333333334814, 0.3333333333333335369, 0.3333333333333333703, 0.3333333333333334814, 0.3333333333333333703, 0.3333333333333334259, 0.3333333333333335369, 0.3333333333333333148, 0.3333333333333334814, 0.3333333333333334814, 0.3333333333333333703, 0.3333333333333334259, 0.3333333333333334259, 0.3333333333333335369, 0.3333333333333333148, 0.3333333333333335369, 0.3333333333333333148, 0.3333333333333335369, 0.3333333333333332593, 0.3333333333333335924, 0.3333333333333333148, 0.3333333333333335369, 0.3333333333333335369, 0.3333333333333334814, 0.3333333333333334259, 0.3333333333333334814, 0.3333333333333334814, 0.3333333333333334259, 0.3333333333333334259, 0.3333333333333334259, 0.3333333333333334814, 0.3333333333333334259, 0.3333333333333333703, 0.3333333333333334814, 0.3333333333333333703, 0.3333333333333335369, 0.3333333333333333703, 0.3333333333333334259, 0.3333333333333333148, 0.3333333333333334259, 0.3333333333333334259, 0.3333333333333333703, 0.3333333333333333703, 0.3333333333333335924, 0.3333333333333334259, 0.3333333333333335369, 0.3333333333333333148, 0.3333333333333335369, 0.3333333333333334814, 0.3333333333333334259, 0.3333333333333334814, 0.3333333333333334259, 0.3333333333333333703, 0.3333333333333335369, 0.3333333333333333148, 0.3333333333333335369, 0.3333333333333333703, 0.3333333333333335369, 0.3333333333333333703, 0.3333333333333334814, 0.3333333333333334259, 0.3333333333333333703, 0.3333333333333334259, 0.3333333333333333703, 0.3333333333333335924, 0.3333333333333334259, 0.3333333333333333148, 0.3333333333333334259, 0.3333333333333334259, 0.3333333333333334259, 0.3333333333333335924, 0.3333333333333333703, 0.3333333333333334259, 0.3333333333333334259, 0.3333333333333335369, 0.3333333333333333703, 0.3333333333333334814, 0.3333333333333334814, 0.3333333333333334814, 0.3333333333333333703, 0.3333333333333334814, 0.3333333333333333148, 0.3333333333333335369, 0.3333333333333334259, 0.3333333333333334814, 0.3333333333333333703, 0.3333333333333334259, 0.3333333333333334259, 0.3333333333333334259, 0.3333333333333334259, 0.3333333333333333703, 0.3333333333333333703, 0.3333333333333334814, 0.3333333333333333703, 0.3333333333333334259, 0.3333333333333334814, 0.3333333333333334259, 0.3333333333333334259, 0.3333333333333333703, 0.3333333333333334814, 0.3333333333333333703, 0.3333333333333334259, 0.3333333333333335369, 0.3333333333333333148, 0.3333333333333333703, 0.3333333333333334814, 0.3333333333333333148, 0.3333333333333334259, 0.3333333333333333703, 0.3333333333333333703, 0.3333333333333334814, 0.3333333333333333703, 0.3333333333333334259, 0.3333333333333334814, 0.3333333333333333703, 0.3333333333333334259, 0.3333333333333334259, 0.3333333333333334259, 0.3333333333333335369, 0.3333333333333334259, 0.3333333333333334259, 0.3333333333333333703, 0.3333333333333334259, 0.3333333333333334259, 0.3333333333333334259, 0.3333333333333334814, 0.3333333333333335369, 0.3333333333333333148, 0.3333333333333333703, 0.3333333333333335924, 0.3333333333333333148, 0.3333333333333334259, 0.3333333333333334259, 0.3333333333333333703, 0.3333333333333333148, 0.3333333333333335369, 0.3333333333333334259, 0.3333333333333333703, 0.3333333333333334814, 0.3333333333333334259, 0.3333333333333334259, 0.3333333333333333148, 0.3333333333333335369, 0.3333333333333333703, 0.3333333333333334259, 0.3333333333333334259),
 ( 0.3333333333333334259, 0.3333333333333334259, 0.3333333333333334814, 0.3333333333333333703, 0.3333333333333335369, 0.3333333333333335369, 0.3333333333333334259, 0.3333333333333334259, 0.3333333333333334259, 0.3333333333333334814, 0.3333333333333334259, 0.3333333333333334259, 0.3333333333333334259, 0.3333333333333334259, 0.3333333333333333148, 0.3333333333333334259, 0.3333333333333334814, 0.3333333333333333703, 0.3333333333333335369, 0.3333333333333335924, 0.3333333333333334259, 0.3333333333333334814, 0.3333333333333333703, 0.3333333333333334259, 0.3333333333333333703, 0.3333333333333334814, 0.3333333333333333703, 0.3333333333333334259, 0.3333333333333333703, 0.3333333333333333703, 0.3333333333333335369, 0.3333333333333334259, 0.3333333333333333703, 0.3333333333333335924, 0.3333333333333334259, 0.3333333333333334259, 0.3333333333333333703, 0.3333333333333334814, 0.3333333333333333703, 0.3333333333333334814, 0.3333333333333333703, 0.3333333333333335369, 0.3333333333333333148, 0.3333333333333334814, 0.3333333333333333703, 0.3333333333333334814, 0.3333333333333334259, 0.3333333333333333703, 0.3333333333333334259, 0.3333333333333334259, 0.3333333333333334814, 0.3333333333333333703, 0.3333333333333335369, 0.3333333333333334259, 0.3333333333333334259, 0.3333333333333334814, 0.3333333333333334259, 0.3333333333333334259, 0.3333333333333333703, 0.3333333333333333703, 0.3333333333333335924, 0.3333333333333334259, 0.3333333333333335369, 0.3333333333333333703, 0.3333333333333333703, 0.3333333333333333703, 0.3333333333333334814, 0.3333333333333333703, 0.3333333333333335369, 0.3333333333333332593, 0.3333333333333333703, 0.3333333333333334259, 0.3333333333333335369, 0.3333333333333334259, 0.3333333333333333703, 0.3333333333333334814, 0.3333333333333333703, 0.3333333333333335369, 0.3333333333333334259, 0.3333333333333333148, 0.3333333333333334814, 0.3333333333333334814, 0.3333333333333334259, 0.3333333333333333148, 0.3333333333333333703, 0.3333333333333334814, 0.3333333333333333703, 0.3333333333333334814, 0.3333333333333333148, 0.3333333333333334259, 0.3333333333333334814, 0.3333333333333333703, 0.3333333333333335369, 0.3333333333333334814, 0.3333333333333333148, 0.3333333333333335369, 0.3333333333333334814, 0.3333333333333334259, 0.3333333333333334814, 0.3333333333333333703, 0.3333333333333334814, 0.3333333333333334259, 0.3333333333333333703, 0.3333333333333334259, 0.3333333333333335369, 0.3333333333333334259, 0.3333333333333334259, 0.3333333333333334814, 0.3333333333333335369, 0.3333333333333333148, 0.3333333333333334259, 0.3333333333333333148, 0.3333333333333335924, 0.3333333333333334259, 0.3333333333333334814, 0.3333333333333333703, 0.3333333333333334814, 0.3333333333333334259, 0.3333333333333333703, 0.3333333333333335924, 0.3333333333333334259, 0.3333333333333334259, 0.3333333333333333703, 0.3333333333333334259, 0.3333333333333333703, 0.3333333333333333703, 0.3333333333333335369, 0.3333333333333334259, 0.3333333333333333703, 0.3333333333333334814, 0.3333333333333333148, 0.3333333333333335924, 0.3333333333333333148, 0.3333333333333334259, 0.3333333333333333148, 0.3333333333333335924, 0.3333333333333333703, 0.3333333333333335369, 0.3333333333333333148, 0.3333333333333334259, 0.3333333333333334814, 0.3333333333333334259, 0.3333333333333334259, 0.3333333333333334259, 0.3333333333333334259, 0.3333333333333334259, 0.3333333333333334259, 0.3333333333333334814, 0.3333333333333334259, 0.3333333333333333703, 0.3333333333333334814, 0.3333333333333333148, 0.3333333333333334259, 0.3333333333333334814, 0.3333333333333334259, 0.3333333333333333703, 0.3333333333333334259, 0.3333333333333334814, 0.3333333333333333703, 0.3333333333333334259, 0.3333333333333334814, 0.3333333333333333703, 0.3333333333333333703, 0.3333333333333333703, 0.3333333333333335369, 0.3333333333333333703, 0.3333333333333334814, 0.3333333333333334259, 0.3333333333333333703, 0.3333333333333334814, 0.3333333333333333703, 0.3333333333333334259, 0.3333333333333335369, 0.3333333333333333703, 0.3333333333333334259, 0.3333333333333334814, 0.3333333333333334259, 0.3333333333333335924, 0.3333333333333333703, 0.3333333333333334259, 0.3333333333333333148, 0.3333333333333335369, 0.3333333333333334259, 0.3333333333333334259, 0.3333333333333334259, 0.3333333333333333703, 0.3333333333333335369, 0.3333333333333334259, 0.3333333333333333703, 0.3333333333333334259, 0.3333333333333334259, 0.3333333333333333703, 0.3333333333333335369, 0.3333333333333333703, 0.3333333333333335369, 0.3333333333333333703, 0.3333333333333334814, 0.3333333333333334259, 0.3333333333333333703, 0.3333333333333334259, 0.3333333333333333703, 0.3333333333333334814, 0.3333333333333334259, 0.3333333333333333703, 0.3333333333333335369, 0.3333333333333333703, 0.3333333333333333703, 0.3333333333333334814, 0.3333333333333333703, 0.3333333333333333148, 0.3333333333333335924, 0.3333333333333333148, 0.3333333333333335924, 0.3333333333333332593, 0.3333333333333334814, 0.3333333333333334814, 0.3333333333333334259, 0.3333333333333334259, 0.3333333333333334814, 0.3333333333333334259, 0.3333333333333333703, 0.3333333333333335369, 0.3333333333333334259, 0.3333333333333334814, 0.3333333333333333703, 0.3333333333333334259, 0.3333333333333333703, 0.3333333333333334814, 0.3333333333333333703, 0.3333333333333335369, 0.3333333333333333148, 0.3333333333333335924, 0.3333333333333333703, 0.3333333333333334259, 0.3333333333333333703, 0.3333333333333334259, 0.3333333333333333703, 0.3333333333333333703, 0.3333333333333335924, 0.3333333333333334259, 0.3333333333333333148, 0.3333333333333334814, 0.3333333333333335369, 0.3333333333333333703, 0.3333333333333334814, 0.3333333333333333703, 0.3333333333333334259, 0.3333333333333335369, 0.3333333333333333148, 0.3333333333333334814, 0.3333333333333334814, 0.3333333333333333703, 0.3333333333333334259, 0.3333333333333334259, 0.3333333333333335369, 0.3333333333333333148, 0.3333333333333335369, 0.3333333333333333148, 0.3333333333333335369, 0.3333333333333332593, 0.3333333333333335924, 0.3333333333333333148, 0.3333333333333335369, 0.3333333333333335369, 0.3333333333333334814, 0.3333333333333334259, 0.3333333333333334814, 0.3333333333333334814, 0.3333333333333334259, 0.3333333333333334259, 0.3333333333333334259, 0.3333333333333334814, 0.3333333333333334259, 0.3333333333333333703, 0.3333333333333334814, 0.3333333333333333703, 0.3333333333333335369, 0.3333333333333333703, 0.3333333333333334259, 0.3333333333333333148, 0.3333333333333334259, 0.3333333333333334259, 0.3333333333333333703, 0.3333333333333333703, 0.3333333333333335924, 0.3333333333333334259, 0.3333333333333335369, 0.3333333333333333148, 0.3333333333333335369, 0.3333333333333334814, 0.3333333333333334259, 0.3333333333333334814, 0.3333333333333334259, 0.3333333333333333703, 0.3333333333333335369, 0.3333333333333333148, 0.3333333333333335369, 0.3333333333333333703, 0.3333333333333335369, 0.3333333333333333703, 0.3333333333333334814, 0.3333333333333334259, 0.3333333333333333703, 0.3333333333333334259, 0.3333333333333333703, 0.3333333333333335924, 0.3333333333333334259, 0.3333333333333333148, 0.3333333333333334259, 0.3333333333333334259, 0.3333333333333334259, 0.3333333333333335924, 0.3333333333333333703, 0.3333333333333334259, 0.3333333333333334259, 0.3333333333333335369, 0.3333333333333333703, 0.3333333333333334814, 0.3333333333333334814, 0.3333333333333334814, 0.3333333333333333703, 0.3333333333333334814, 0.3333333333333333148, 0.3333333333333335369, 0.3333333333333334259, 0.3333333333333334814, 0.3333333333333333703, 0.3333333333333334259, 0.3333333333333334259, 0.3333333333333334259, 0.3333333333333334259, 0.3333333333333333703, 0.3333333333333333703, 0.3333333333333334814, 0.3333333333333333703, 0.3333333333333334259, 0.3333333333333334814, 0.3333333333333334259, 0.3333333333333334259, 0.3333333333333333703, 0.3333333333333334814, 0.3333333333333333703, 0.3333333333333334259, 0.3333333333333335369, 0.3333333333333333148, 0.3333333333333333703, 0.3333333333333334814, 0.3333333333333333148, 0.3333333333333334259, 0.3333333333333333703, 0.3333333333333333703, 0.3333333333333334814, 0.3333333333333333703, 0.3333333333333334259, 0.3333333333333334814, 0.3333333333333333703, 0.3333333333333334259, 0.3333333333333334259, 0.3333333333333334259, 0.3333333333333335369, 0.3333333333333334259, 0.3333333333333334259, 0.3333333333333333703, 0.3333333333333334259, 0.3333333333333334259, 0.3333333333333334259, 0.3333333333333334814, 0.3333333333333335369, 0.3333333333333333148, 0.3333333333333333703, 0.3333333333333335924, 0.3333333333333333148, 0.3333333333333334259, 0.3333333333333334259, 0.3333333333333333703, 0.3333333333333333148, 0.3333333333333335369, 0.3333333333333334259, 0.3333333333333333703, 0.3333333333333334814, 0.3333333333333334259, 0.3333333333333334259, 0.3333333333333333148, 0.3333333333333335369, 0.3333333333333333703, 0.3333333333333334259, 0.3333333333333334259),
 ( 1.000000000000000222, 1.000000000000000222, 1.000000000000000222, 1.000000000000000222, 1.000000000000000444, 1.000000000000000444, 1.000000000000000222, 1.000000000000000444, 1.000000000000000222, 1.000000000000000444, 1.000000000000000444, 1.000000000000000000, 1.000000000000000222, 1.000000000000000000, 1.000000000000000222, 1.000000000000000222, 1.000000000000000444, 1.000000000000000000, 1.000000000000000444, 1.000000000000000444, 1.000000000000000222, 1.000000000000000222, 1.000000000000000000, 1.000000000000000222, 1.000000000000000000, 1.000000000000000444, 1.000000000000000000, 1.000000000000000444, 1.000000000000000222, 1.000000000000000000, 1.000000000000000666, 1.000000000000000000, 1.000000000000000222, 1.000000000000000666, 1.000000000000000222, 1.000000000000000444, 1.000000000000000222, 1.000000000000000444, 1.000000000000000000, 1.000000000000000444, 1.000000000000000000, 1.000000000000000444, 1.000000000000000000, 1.000000000000000444, 1.000000000000000000, 1.000000000000000222, 1.000000000000000444, 1.000000000000000000, 1.000000000000000444, 1.000000000000000222, 1.000000000000000222, 1.000000000000000444, 1.000000000000000222, 1.000000000000000444, 1.000000000000000222, 1.000000000000000222, 1.000000000000000444, 1.000000000000000444, 1.000000000000000222, 1.000000000000000222, 1.000000000000000444, 1.000000000000000222, 1.000000000000000444, 1.000000000000000000, 1.000000000000000222, 1.000000000000000222, 1.000000000000000222, 1.000000000000000222, 1.000000000000000444, 1.000000000000000000, 0.9999999999999997780, 1.000000000000000444, 1.000000000000000444, 1.000000000000000222, 1.000000000000000222, 1.000000000000000444, 0.9999999999999997780, 1.000000000000000666, 1.000000000000000000, 1.000000000000000000, 1.000000000000000444, 1.000000000000000222, 1.000000000000000222, 0.9999999999999997780, 1.000000000000000222, 1.000000000000000444, 0.9999999999999997780, 1.000000000000000444, 1.000000000000000000, 1.000000000000000000, 1.000000000000000444, 1.000000000000000000, 1.000000000000000444, 1.000000000000000444, 0.9999999999999997780, 1.000000000000000444, 1.000000000000000444, 1.000000000000000444, 1.000000000000000444, 1.000000000000000000, 1.000000000000000444, 1.000000000000000222, 1.000000000000000000, 1.000000000000000444, 1.000000000000000444, 1.000000000000000222, 1.000000000000000000, 1.000000000000000444, 1.000000000000000444, 1.000000000000000000, 1.000000000000000222, 1.000000000000000000, 1.000000000000000444, 1.000000000000000222, 1.000000000000000444, 1.000000000000000222, 1.000000000000000444, 1.000000000000000444, 1.000000000000000000, 1.000000000000000666, 1.000000000000000222, 1.000000000000000222, 1.000000000000000000, 1.000000000000000222, 1.000000000000000222, 1.000000000000000222, 1.000000000000000444, 1.000000000000000222, 1.000000000000000222, 1.000000000000000444, 0.9999999999999997780, 1.000000000000000666, 0.9999999999999997780, 1.000000000000000222, 1.000000000000000000, 1.000000000000000444, 1.000000000000000000, 1.000000000000000444, 1.000000000000000000, 1.000000000000000222, 1.000000000000000222, 1.000000000000000444, 1.000000000000000444, 1.000000000000000222, 1.000000000000000444, 1.000000000000000444, 1.000000000000000000, 1.000000000000000666, 1.000000000000000222, 1.000000000000000222, 1.000000000000000444, 1.000000000000000000, 1.000000000000000222, 1.000000000000000444, 1.000000000000000000, 1.000000000000000222, 1.000000000000000222, 1.000000000000000444, 1.000000000000000222, 1.000000000000000222, 1.000000000000000444, 1.000000000000000000, 1.000000000000000222, 1.000000000000000000, 1.000000000000000444, 1.000000000000000222, 1.000000000000000444, 1.000000000000000222, 1.000000000000000222, 1.000000000000000444, 1.000000000000000000, 1.000000000000000222, 1.000000000000000444, 1.000000000000000000, 1.000000000000000444, 1.000000000000000222, 1.000000000000000444, 1.000000000000000444, 1.000000000000000222, 1.000000000000000222, 1.000000000000000000, 1.000000000000000444, 1.000000000000000444, 1.000000000000000000, 1.000000000000000444, 1.000000000000000222, 1.000000000000000444, 1.000000000000000444, 1.000000000000000222, 1.000000000000000000, 1.000000000000000444, 1.000000000000000222, 1.000000000000000444, 1.000000000000000000, 1.000000000000000444, 1.000000000000000222, 1.000000000000000222, 1.000000000000000444, 1.000000000000000222, 1.000000000000000222, 1.000000000000000222, 1.000000000000000222, 1.000000000000000444, 1.000000000000000000, 1.000000000000000666, 1.000000000000000000, 1.000000000000000222, 1.000000000000000444, 1.000000000000000000, 1.000000000000000222, 1.000000000000000444, 1.000000000000000000, 1.000000000000000666, 0.9999999999999997780, 1.000000000000000222, 1.000000000000000444, 1.000000000000000000, 1.000000000000000444, 1.000000000000000222, 1.000000000000000444, 1.000000000000000000, 1.000000000000000444, 1.000000000000000222, 1.000000000000000222, 1.000000000000000000, 1.000000000000000444, 1.000000000000000222, 1.000000000000000000, 1.000000000000000222, 1.000000000000000222, 1.000000000000000222, 1.000000000000000444, 1.000000000000000000, 1.000000000000000444, 1.000000000000000222, 1.000000000000000222, 1.000000000000000222, 1.000000000000000000, 1.000000000000000666, 1.000000000000000000, 1.000000000000000000, 1.000000000000000222, 1.000000000000000444, 1.000000000000000222, 1.000000000000000444, 0.9999999999999997780, 1.000000000000000444, 1.000000000000000444, 0.9999999999999997780, 1.000000000000000444, 1.000000000000000444, 1.000000000000000444, 1.000000000000000222, 1.000000000000000444, 1.000000000000000444, 1.000000000000000000, 1.000000000000000444, 0.9999999999999997780, 1.000000000000000444, 0.9999999999999997780, 1.000000000000000444, 1.000000000000000000, 1.000000000000000444, 1.000000000000000444, 1.000000000000000444, 1.000000000000000222, 1.000000000000000444, 1.000000000000000444, 1.000000000000000222, 1.000000000000000222, 1.000000000000000000, 1.000000000000000222, 1.000000000000000444, 0.9999999999999997780, 1.000000000000000666, 0.9999999999999997780, 1.000000000000000444, 1.000000000000000222, 1.000000000000000222, 1.000000000000000000, 1.000000000000000222, 1.000000000000000222, 1.000000000000000000, 1.000000000000000000, 1.000000000000000444, 1.000000000000000222, 1.000000000000000444, 0.9999999999999997780, 1.000000000000000444, 1.000000000000000444, 1.000000000000000222, 1.000000000000000444, 1.000000000000000000, 1.000000000000000444, 1.000000000000000444, 0.9999999999999997780, 1.000000000000000444, 1.000000000000000222, 1.000000000000000444, 1.000000000000000222, 1.000000000000000222, 1.000000000000000444, 1.000000000000000000, 1.000000000000000000, 1.000000000000000444, 1.000000000000000444, 1.000000000000000444, 0.9999999999999997780, 1.000000000000000444, 1.000000000000000222, 1.000000000000000222, 1.000000000000000444, 1.000000000000000000, 1.000000000000000444, 1.000000000000000222, 1.000000000000000444, 1.000000000000000000, 1.000000000000000444, 1.000000000000000444, 1.000000000000000444, 1.000000000000000000, 1.000000000000000444, 1.000000000000000000, 1.000000000000000222, 1.000000000000000444, 1.000000000000000444, 1.000000000000000000, 1.000000000000000444, 1.000000000000000444, 1.000000000000000000, 1.000000000000000444, 1.000000000000000222, 1.000000000000000000, 1.000000000000000444, 1.000000000000000222, 1.000000000000000222, 1.000000000000000444, 1.000000000000000444, 1.000000000000000000, 1.000000000000000000, 1.000000000000000444, 1.000000000000000000, 1.000000000000000222, 1.000000000000000444, 1.000000000000000000, 1.000000000000000222, 1.000000000000000444, 0.9999999999999997780, 1.000000000000000444, 1.000000000000000222, 1.000000000000000000, 1.000000000000000444, 1.000000000000000000, 1.000000000000000444, 1.000000000000000444, 1.000000000000000000, 1.000000000000000222, 1.000000000000000222, 1.000000000000000222, 1.000000000000000444, 1.000000000000000222, 1.000000000000000000, 1.000000000000000222, 1.000000000000000444, 1.000000000000000444, 1.000000000000000222, 1.000000000000000444, 1.000000000000000444, 1.000000000000000000, 1.000000000000000000, 1.000000000000000666, 0.9999999999999997780, 1.000000000000000444, 0.9999999999999997780, 1.000000000000000222, 0.9999999999999997780, 1.000000000000000444, 1.000000000000000000, 1.000000000000000222, 1.000000000000000222, 1.000000000000000444, 1.000000000000000000, 1.000000000000000000, 1.000000000000000444, 1.000000000000000000, 1.000000000000000222, 1.000000000000000222),
 ( 0.3333333333333334259, 0.3333333333333334259, 0.3333333333333334814, 0.3333333333333333703, 0.3333333333333335369, 0.3333333333333335369, 0.3333333333333334259, 0.3333333333333334259, 0.3333333333333334259, 0.3333333333333334814, 0.3333333333333334259, 0.3333333333333334259, 0.3333333333333334259, 0.3333333333333334259, 0.3333333333333333148, 0.3333333333333334259, 0.3333333333333334814, 0.3333333333333333703, 0.3333333333333335369, 0.3333333333333335924, 0.3333333333333334259, 0.3333333333333334814, 0.3333333333333333703, 0.3333333333333334259, 0.3333333333333333703, 0.3333333333333334814, 0.3333333333333333703, 0.3333333333333334259, 0.3333333333333333703, 0.3333333333333333703, 0.3333333333333335369, 0.3333333333333334259, 0.3333333333333333703, 0.3333333333333335924, 0.3333333333333334259, 0.3333333333333334259, 0.3333333333333333703, 0.3333333333333334814, 0.3333333333333333703, 0.3333333333333334814, 0.3333333333333333703, 0.3333333333333335369, 0.3333333333333333148, 0.3333333333333334814, 0.3333333333333333703, 0.3333333333333334814, 0.3333333333333334259, 0.3333333333333333703, 0.3333333333333334259, 0.3333333333333334259, 0.3333333333333334814, 0.3333333333333333703, 0.3333333333333335369, 0.3333333333333334259, 0.3333333333333334259, 0.3333333333333334814, 0.3333333333333334259, 0.3333333333333334259, 0.3333333333333333703, 0.3333333333333333703, 0.3333333333333335924, 0.3333333333333334259, 0.3333333333333335369, 0.3333333333333333703, 0.3333333333333333703, 0.3333333333333333703, 0.3333333333333334814, 0.3333333333333333703, 0.3333333333333335369, 0.3333333333333332593, 0.3333333333333333703, 0.3333333333333334259, 0.3333333333333335369, 0.3333333333333334259, 0.3333333333333333703, 0.3333333333333334814, 0.3333333333333333703, 0.3333333333333335369, 0.3333333333333334259, 0.3333333333333333148, 0.3333333333333334814, 0.3333333333333334814, 0.3333333333333334259, 0.3333333333333333148, 0.3333333333333333703, 0.3333333333333334814, 0.3333333333333333703, 0.3333333333333334814, 0.3333333333333333148, 0.3333333333333334259, 0.3333333333333334814, 0.3333333333333333703, 0.3333333333333335369, 0.3333333333333334814, 0.3333333333333333148, 0.3333333333333335369, 0.3333333333333334814, 0.3333333333333334259, 0.3333333333333334814, 0.3333333333333333703, 0.3333333333333334814, 0.3333333333333334259, 0.3333333333333333703, 0.3333333333333334259, 0.3333333333333335369, 0.3333333333333334259, 0.3333333333333334259, 0.3333333333333334814, 0.3333333333333335369, 0.3333333333333333148, 0.3333333333333334259, 0.3333333333333333148, 0.3333333333333335924, 0.3333333333333334259, 0.3333333333333334814, 0.3333333333333333703, 0.3333333333333334814, 0.3333333333333334259, 0.3333333333333333703, 0.3333333333333335924, 0.3333333333333334259, 0.3333333333333334259, 0.3333333333333333703, 0.3333333333333334259, 0.3333333333333333703, 0.3333333333333333703, 0.3333333333333335369, 0.3333333333333334259, 0.3333333333333333703, 0.3333333333333334814, 0.3333333333333333148, 0.3333333333333335924, 0.3333333333333333148, 0.3333333333333334259, 0.3333333333333333148, 0.3333333333333335924, 0.3333333333333333703, 0.3333333333333335369, 0.3333333333333333148, 0.3333333333333334259, 0.3333333333333334814, 0.3333333333333334259, 0.3333333333333334259, 0.3333333333333334259, 0.3333333333333334259, 0.3333333333333334259, 0.3333333333333334259, 0.3333333333333334814, 0.3333333333333334259, 0.3333333333333333703, 0.3333333333333334814, 0.3333333333333333148, 0.3333333333333334259, 0.3333333333333334814, 0.3333333333333334259, 0.3333333333333333703, 0.3333333333333334259, 0.3333333333333334814, 0.3333333333333333703, 0.3333333333333334259, 0.3333333333333334814, 0.3333333333333333703, 0.3333333333333333703, 0.3333333333333333703, 0.3333333333333335369, 0.3333333333333333703, 0.3333333333333334814, 0.3333333333333334259, 0.3333333333333333703, 0.3333333333333334814, 0.3333333333333333703, 0.3333333333333334259, 0.3333333333333335369, 0.3333333333333333703, 0.3333333333333334259, 0.3333333333333334814, 0.3333333333333334259, 0.3333333333333335924, 0.3333333333333333703, 0.3333333333333334259, 0.3333333333333333148, 0.3333333333333335369, 0.3333333333333334259, 0.3333333333333334259, 0.3333333333333334259, 0.3333333333333333703, 0.3333333333333335369, 0.3333333333333334259, 0.3333333333333333703, 0.3333333333333334259, 0.3333333333333334259, 0.3333333333333333703, 0.3333333333333335369, 0.3333333333333333703, 0.3333333333333335369, 0.3333333333333333703, 0.3333333333333334814, 0.3333333333333334259, 0.3333333333333333703, 0.3333333333333334259, 0.3333333333333333703, 0.3333333333333334814, 0.3333333333333334259, 0.3333333333333333703, 0.3333333333333335369, 0.3333333333333333703, 0.3333333333333333703, 0.3333333333333334814, 0.3333333333333333703, 0.3333333333333333148, 0.3333333333333335924, 0.3333333333333333148, 0.3333333333333335924, 0.3333333333333332593, 0.3333333333333334814, 0.3333333333333334814, 0.3333333333333334259, 0.3333333333333334259, 0.3333333333333334814, 0.3333333333333334259, 0.3333333333333333703, 0.3333333333333335369, 0.3333333333333334259, 0.3333333333333334814, 0.3333333333333333703, 0.3333333333333334259, 0.3333333333333333703, 0.3333333333333334814, 0.3333333333333333703, 0.3333333333333335369, 0.3333333333333333148, 0.3333333333333335924, 0.3333333333333333703, 0.3333333333333334259, 0.3333333333333333703, 0.3333333333333334259, 0.3333333333333333703, 0.3333333333333333703, 0.3333333333333335924, 0.3333333333333334259, 0.3333333333333333148, 0.3333333333333334814, 0.3333333333333335369, 0.3333333333333333703, 0.3333333333333334814, 0.3333333333333333703, 0.3333333333333334259, 0.3333333333333335369, 0.3333333333333333148, 0.3333333333333334814, 0.3333333333333334814, 0.3333333333333333703, 0.3333333333333334259, 0.3333333333333334259, 0.3333333333333335369, 0.3333333333333333148, 0.3333333333333335369, 0.3333333333333333148, 0.3333333333333335369, 0.3333333333333332593, 0.3333333333333335924, 0.3333333333333333148, 0.3333333333333335369, 0.3333333333333335369, 0.3333333333333334814, 0.3333333333333334259, 0.3333333333333334814, 0.3333333333333334814, 0.3333333333333334259, 0.3333333333333334259, 0.3333333333333334259, 0.3333333333333334814, 0.3333333333333334259, 0.3333333333333333703, 0.3333333333333334814, 0.3333333333333333703, 0.3333333333333335369, 0.3333333333333333703, 0.3333333333333334259, 0.3333333333333333148, 0.3333333333333334259, 0.3333333333333334259, 0.3333333333333333703, 0.3333333333333333703, 0.3333333333333335924, 0.3333333333333334259, 0.3333333333333335369, 0.3333333333333333148, 0.3333333333333335369, 0.3333333333333334814, 0.3333333333333334259, 0.3333333333333334814, 0.3333333333333334259, 0.3333333333333333703, 0.3333333333333335369, 0.3333333333333333148, 0.3333333333333335369, 0.3333333333333333703, 0.3333333333333335369, 0.3333333333333333703, 0.3333333333333334814, 0.3333333333333334259, 0.3333333333333333703, 0.3333333333333334259, 0.3333333333333333703, 0.3333333333333335924, 0.3333333333333334259, 0.3333333333333333148, 0.3333333333333334259, 0.3333333333333334259, 0.3333333333333334259, 0.3333333333333335924, 0.3333333333333333703, 0.3333333333333334259, 0.3333333333333334259, 0.3333333333333335369, 0.3333333333333333703, 0.3333333333333334814, 0.3333333333333334814, 0.3333333333333334814, 0.3333333333333333703, 0.3333333333333334814, 0.3333333333333333148, 0.3333333333333335369, 0.3333333333333334259, 0.3333333333333334814, 0.3333333333333333703, 0.3333333333333334259, 0.3333333333333334259, 0.3333333333333334259, 0.3333333333333334259, 0.3333333333333333703, 0.3333333333333333703, 0.3333333333333334814, 0.3333333333333333703, 0.3333333333333334259, 0.3333333333333334814, 0.3333333333333334259, 0.3333333333333334259, 0.3333333333333333703, 0.3333333333333334814, 0.3333333333333333703, 0.3333333333333334259, 0.3333333333333335369, 0.3333333333333333148, 0.3333333333333333703, 0.3333333333333334814, 0.3333333333333333148, 0.3333333333333334259, 0.3333333333333333703, 0.3333333333333333703, 0.3333333333333334814, 0.3333333333333333703, 0.3333333333333334259, 0.3333333333333334814, 0.3333333333333333703, 0.3333333333333334259, 0.3333333333333334259, 0.3333333333333334259, 0.3333333333333335369, 0.3333333333333334259, 0.3333333333333334259, 0.3333333333333333703, 0.3333333333333334259, 0.3333333333333334259, 0.3333333333333334259, 0.3333333333333334814, 0.3333333333333335369, 0.3333333333333333148, 0.3333333333333333703, 0.3333333333333335924, 0.3333333333333333148, 0.3333333333333334259, 0.3333333333333334259, 0.3333333333333333703, 0.3333333333333333148, 0.3333333333333335369, 0.3333333333333334259, 0.3333333333333333703, 0.3333333333333334814, 0.3333333333333334259, 0.3333333333333334259, 0.3333333333333333148, 0.3333333333333335369, 0.3333333333333333703, 0.3333333333333334259, 0.3333333333333334259),
 ( 0.3333333333333334259, 0.3333333333333334259, 0.3333333333333334814, 0.3333333333333333703, 0.3333333333333335369, 0.3333333333333335369, 0.3333333333333334259, 0.3333333333333334259, 0.3333333333333334259, 0.3333333333333334814, 0.3333333333333334259, 0.3333333333333334259, 0.3333333333333334259, 0.3333333333333334259, 0.3333333333333333148, 0.3333333333333334259, 0.3333333333333334814, 0.3333333333333333703, 0.3333333333333335369, 0.3333333333333335924, 0.3333333333333334259, 0.3333333333333334814, 0.3333333333333333703, 0.3333333333333334259, 0.3333333333333333703, 0.3333333333333334814, 0.3333333333333333703, 0.3333333333333334259, 0.3333333333333333703, 0.3333333333333333703, 0.3333333333333335369, 0.3333333333333334259, 0.3333333333333333703, 0.3333333333333335924, 0.3333333333333334259, 0.3333333333333334259, 0.3333333333333333703, 0.3333333333333334814, 0.3333333333333333703, 0.3333333333333334814, 0.3333333333333333703, 0.3333333333333335369, 0.3333333333333333148, 0.3333333333333334814, 0.3333333333333333703, 0.3333333333333334814, 0.3333333333333334259, 0.3333333333333333703, 0.3333333333333334259, 0.3333333333333334259, 0.3333333333333334814, 0.3333333333333333703, 0.3333333333333335369, 0.3333333333333334259, 0.3333333333333334259, 0.3333333333333334814, 0.3333333333333334259, 0.3333333333333334259, 0.3333333333333333703, 0.3333333333333333703, 0.3333333333333335924, 0.3333333333333334259, 0.3333333333333335369, 0.3333333333333333703, 0.3333333333333333703, 0.3333333333333333703, 0.3333333333333334814, 0.3333333333333333703, 0.3333333333333335369, 0.3333333333333332593, 0.3333333333333333703, 0.3333333333333334259, 0.3333333333333335369, 0.3333333333333334259, 0.3333333333333333703, 0.3333333333333334814, 0.3333333333333333703, 0.3333333333333335369, 0.3333333333333334259, 0.3333333333333333148, 0.3333333333333334814, 0.3333333333333334814, 0.3333333333333334259, 0.3333333333333333148, 0.3333333333333333703, 0.3333333333333334814, 0.3333333333333333703, 0.3333333333333334814, 0.3333333333333333148, 0.3333333333333334259, 0.3333333333333334814, 0.3333333333333333703, 0.3333333333333335369, 0.3333333333333334814, 0.3333333333333333148, 0.3333333333333335369, 0.3333333333333334814, 0.3333333333333334259, 0.3333333333333334814, 0.3333333333333333703, 0.3333333333333334814, 0.3333333333333334259, 0.3333333333333333703, 0.3333333333333334259, 0.3333333333333335369, 0.3333333333333334259, 0.3333333333333334259, 0.3333333333333334814, 0.3333333333333335369, 0.3333333333333333148, 0.3333333333333334259, 0.3333333333333333148, 0.3333333333333335924, 0.3333333333333334259, 0.3333333333333334814, 0.3333333333333333703, 0.3333333333333334814, 0.3333333333333334259, 0.3333333333333333703, 0.3333333333333335924, 0.3333333333333334259, 0.3333333333333334259, 0.3333333333333333703, 0.3333333333333334259, 0.3333333333333333703, 0.3333333333333333703, 0.3333333333333335369, 0.3333333333333334259, 0.3333333333333333703, 0.3333333333333334814, 0.3333333333333333148, 0.3333333333333335924, 0.3333333333333333148, 0.3333333333333334259, 0.3333333333333333148, 0.3333333333333335924, 0.3333333333333333703, 0.3333333333333335369, 0.3333333333333333148, 0.3333333333333334259, 0.3333333333333334814, 0.3333333333333334259, 0.3333333333333334259, 0.3333333333333334259, 0.3333333333333334259, 0.3333333333333334259, 0.3333333333333334259, 0.3333333333333334814, 0.3333333333333334259, 0.3333333333333333703, 0.3333333333333334814, 0.3333333333333333148, 0.3333333333333334259, 0.3333333333333334814, 0.3333333333333334259, 0.3333333333333333703, 0.3333333333333334259, 0.3333333333333334814, 0.3333333333333333703, 0.3333333333333334259, 0.3333333333333334814, 0.3333333333333333703, 0.3333333333333333703, 0.3333333333333333703, 0.3333333333333335369, 0.3333333333333333703, 0.3333333333333334814, 0.3333333333333334259, 0.3333333333333333703, 0.3333333333333334814, 0.3333333333333333703, 0.3333333333333334259, 0.3333333333333335369, 0.3333333333333333703, 0.3333333333333334259, 0.3333333333333334814, 0.3333333333333334259, 0.3333333333333335924, 0.3333333333333333703, 0.3333333333333334259, 0.3333333333333333148, 0.3333333333333335369, 0.3333333333333334259, 0.3333333333333334259, 0.3333333333333334259, 0.3333333333333333703, 0.3333333333333335369, 0.3333333333333334259, 0.3333333333333333703, 0.3333333333333334259, 0.3333333333333334259, 0.3333333333333333703, 0.3333333333333335369, 0.3333333333333333703, 0.3333333333333335369, 0.3333333333333333703, 0.3333333333333334814, 0.3333333333333334259, 0.3333333333333333703, 0.3333333333333334259, 0.3333333333333333703, 0.3333333333333334814, 0.3333333333333334259, 0.3333333333333333703, 0.3333333333333335369, 0.3333333333333333703, 0.3333333333333333703, 0.3333333333333334814, 0.3333333333333333703, 0.3333333333333333148, 0.3333333333333335924, 0.3333333333333333148, 0.3333333333333335924, 0.3333333333333332593, 0.3333333333333334814, 0.3333333333333334814, 0.3333333333333334259, 0.3333333333333334259, 0.3333333333333334814, 0.3333333333333334259, 0.3333333333333333703, 0.3333333333333335369, 0.3333333333333334259, 0.3333333333333334814, 0.3333333333333333703, 0.3333333333333334259, 0.3333333333333333703, 0.3333333333333334814, 0.3333333333333333703, 0.3333333333333335369, 0.3333333333333333148, 0.3333333333333335924, 0.3333333333333333703, 0.3333333333333334259, 0.3333333333333333703, 0.3333333333333334259, 0.3333333333333333703, 0.3333333333333333703, 0.3333333333333335924, 0.3333333333333334259, 0.3333333333333333148, 0.3333333333333334814, 0.3333333333333335369, 0.3333333333333333703, 0.3333333333333334814, 0.3333333333333333703, 0.3333333333333334259, 0.3333333333333335369, 0.3333333333333333148, 0.3333333333333334814, 0.3333333333333334814, 0.3333333333333333703, 0.3333333333333334259, 0.3333333333333334259, 0.3333333333333335369, 0.3333333333333333148, 0.3333333333333335369, 0.3333333333333333148, 0.3333333333333335369, 0.3333333333333332593, 0.3333333333333335924, 0.3333333333333333148, 0.3333333333333335369, 0.3333333333333335369, 0.3333333333333334814, 0.3333333333333334259, 0.3333333333333334814, 0.3333333333333334814, 0.3333333333333334259, 0.3333333333333334259, 0.3333333333333334259, 0.3333333333333334814, 0.3333333333333334259, 0.3333333333333333703, 0.3333333333333334814, 0.3333333333333333703, 0.3333333333333335369, 0.3333333333333333703, 0.3333333333333334259, 0.3333333333333333148, 0.3333333333333334259, 0.3333333333333334259, 0.3333333333333333703, 0.3333333333333333703, 0.3333333333333335924, 0.3333333333333334259, 0.3333333333333335369, 0.3333333333333333148, 0.3333333333333335369, 0.3333333333333334814, 0.3333333333333334259, 0.3333333333333334814, 0.3333333333333334259, 0.3333333333333333703, 0.3333333333333335369, 0.3333333333333333148, 0.3333333333333335369, 0.3333333333333333703, 0.3333333333333335369, 0.3333333333333333703, 0.3333333333333334814, 0.3333333333333334259, 0.3333333333333333703, 0.3333333333333334259, 0.3333333333333333703, 0.3333333333333335924, 0.3333333333333334259, 0.3333333333333333148, 0.3333333333333334259, 0.3333333333333334259, 0.3333333333333334259, 0.3333333333333335924, 0.3333333333333333703, 0.3333333333333334259, 0.3333333333333334259, 0.3333333333333335369, 0.3333333333333333703, 0.3333333333333334814, 0.3333333333333334814, 0.3333333333333334814, 0.3333333333333333703, 0.3333333333333334814, 0.3333333333333333148, 0.3333333333333335369, 0.3333333333333334259, 0.3333333333333334814, 0.3333333333333333703, 0.3333333333333334259, 0.3333333333333334259, 0.3333333333333334259, 0.3333333333333334259, 0.3333333333333333703, 0.3333333333333333703, 0.3333333333333334814, 0.3333333333333333703, 0.3333333333333334259, 0.3333333333333334814, 0.3333333333333334259, 0.3333333333333334259, 0.3333333333333333703, 0.3333333333333334814, 0.3333333333333333703, 0.3333333333333334259, 0.3333333333333335369, 0.3333333333333333148, 0.3333333333333333703, 0.3333333333333334814, 0.3333333333333333148, 0.3333333333333334259, 0.3333333333333333703, 0.3333333333333333703, 0.3333333333333334814, 0.3333333333333333703, 0.3333333333333334259, 0.3333333333333334814, 0.3333333333333333703, 0.3333333333333334259, 0.3333333333333334259, 0.3333333333333334259, 0.3333333333333335369, 0.3333333333333334259, 0.3333333333333334259, 0.3333333333333333703, 0.3333333333333334259, 0.3333333333333334259, 0.3333333333333334259, 0.3333333333333334814, 0.3333333333333335369, 0.3333333333333333148, 0.3333333333333333703, 0.3333333333333335924, 0.3333333333333333148, 0.3333333333333334259, 0.3333333333333334259, 0.3333333333333333703, 0.3333333333333333148, 0.3333333333333335369, 0.3333333333333334259, 0.3333333333333333703, 0.3333333333333334814, 0.3333333333333334259, 0.3333333333333334259, 0.3333333333333333148, 0.3333333333333335369, 0.3333333333333333703, 0.3333333333333334259, 0.3333333333333334259),
 ( 1.000000000000000222, 1.000000000000000222, 1.000000000000000222, 1.000000000000000222, 1.000000000000000444, 1.000000000000000444, 1.000000000000000222, 1.000000000000000444, 1.000000000000000222, 1.000000000000000444, 1.000000000000000444, 1.000000000000000000, 1.000000000000000222, 1.000000000000000000, 1.000000000000000222, 1.000000000000000222, 1.000000000000000444, 1.000000000000000000, 1.000000000000000444, 1.000000000000000444, 1.000000000000000222, 1.000000000000000222, 1.000000000000000000, 1.000000000000000222, 1.000000000000000000, 1.000000000000000444, 1.000000000000000000, 1.000000000000000444, 1.000000000000000222, 1.000000000000000000, 1.000000000000000666, 1.000000000000000000, 1.000000000000000222, 1.000000000000000666, 1.000000000000000222, 1.000000000000000444, 1.000000000000000222, 1.000000000000000444, 1.000000000000000000, 1.000000000000000444, 1.000000000000000000, 1.000000000000000444, 1.000000000000000000, 1.000000000000000444, 1.000000000000000000, 1.000000000000000222, 1.000000000000000444, 1.000000000000000000, 1.000000000000000444, 1.000000000000000222, 1.000000000000000222, 1.000000000000000444, 1.000000000000000222, 1.000000000000000444, 1.000000000000000222, 1.000000000000000222, 1.000000000000000444, 1.000000000000000444, 1.000000000000000222, 1.000000000000000222, 1.000000000000000444, 1.000000000000000222, 1.000000000000000444, 1.000000000000000000, 1.000000000000000222, 1.000000000000000222, 1.000000000000000222, 1.000000000000000222, 1.000000000000000444, 1.000000000000000000, 0.9999999999999997780, 1.000000000000000444, 1.000000000000000444, 1.000000000000000222, 1.000000000000000222, 1.000000000000000444, 0.9999999999999997780, 1.000000000000000666, 1.000000000000000000, 1.000000000000000000, 1.000000000000000444, 1.000000000000000222, 1.000000000000000222, 0.9999999999999997780, 1.000000000000000222, 1.000000000000000444, 0.9999999999999997780, 1.000000000000000444, 1.000000000000000000, 1.000000000000000000, 1.000000000000000444, 1.000000000000000000, 1.000000000000000444, 1.000000000000000444, 0.9999999999999997780, 1.000000000000000444, 1.000000000000000444, 1.000000000000000444, 1.000000000000000444, 1.000000000000000000, 1.000000000000000444, 1.000000000000000222, 1.000000000000000000, 1.000000000000000444, 1.000000000000000444, 1.000000000000000222, 1.000000000000000000, 1.000000000000000444, 1.000000000000000444, 1.000000000000000000, 1.000000000000000222, 1.000000000000000000, 1.000000000000000444, 1.000000000000000222, 1.000000000000000444, 1.000000000000000222, 1.000000000000000444, 1.000000000000000444, 1.000000000000000000, 1.000000000000000666, 1.000000000000000222, 1.000000000000000222, 1.000000000000000000, 1.000000000000000222, 1.000000000000000222, 1.000000000000000222, 1.000000000000000444, 1.000000000000000222, 1.000000000000000222, 1.000000000000000444, 0.9999999999999997780, 1.000000000000000666, 0.9999999999999997780, 1.000000000000000222, 1.000000000000000000, 1.000000000000000444, 1.000000000000000000, 1.000000000000000444, 1.000000000000000000, 1.000000000000000222, 1.000000000000000222, 1.000000000000000444, 1.000000000000000444, 1.000000000000000222, 1.000000000000000444, 1.000000000000000444, 1.000000000000000000, 1.000000000000000666, 1.000000000000000222, 1.000000000000000222, 1.000000000000000444, 1.000000000000000000, 1.000000000000000222, 1.000000000000000444, 1.000000000000000000, 1.000000000000000222, 1.000000000000000222, 1.000000000000000444, 1.000000000000000222, 1.000000000000000222, 1.000000000000000444, 1.000000000000000000, 1.000000000000000222, 1.000000000000000000, 1.000000000000000444, 1.000000000000000222, 1.000000000000000444, 1.000000000000000222, 1.000000000000000222, 1.000000000000000444, 1.000000000000000000, 1.000000000000000222, 1.000000000000000444, 1.000000000000000000, 1.000000000000000444, 1.000000000000000222, 1.000000000000000444, 1.000000000000000444, 1.000000000000000222, 1.000000000000000222, 1.000000000000000000, 1.000000000000000444, 1.000000000000000444, 1.000000000000000000, 1.000000000000000444, 1.000000000000000222, 1.000000000000000444, 1.000000000000000444, 1.000000000000000222, 1.000000000000000000, 1.000000000000000444, 1.000000000000000222, 1.000000000000000444, 1.000000000000000000, 1.000000000000000444, 1.000000000000000222, 1.000000000000000222, 1.000000000000000444, 1.000000000000000222, 1.000000000000000222, 1.000000000000000222, 1.000000000000000222, 1.000000000000000444, 1.000000000000000000, 1.000000000000000666, 1.000000000000000000, 1.000000000000000222, 1.000000000000000444, 1.000000000000000000, 1.000000000000000222, 1.000000000000000444, 1.000000000000000000, 1.000000000000000666, 0.9999999999999997780, 1.000000000000000222, 1.000000000000000444, 1.000000000000000000, 1.000000000000000444, 1.000000000000000222, 1.000000000000000444, 1.000000000000000000, 1.000000000000000444, 1.000000000000000222, 1.000000000000000222, 1.000000000000000000, 1.000000000000000444, 1.000000000000000222, 1.000000000000000000, 1.000000000000000222, 1.000000000000000222, 1.000000000000000222, 1.000000000000000444, 1.000000000000000000, 1.000000000000000444, 1.000000000000000222, 1.000000000000000222, 1.000000000000000222, 1.000000000000000000, 1.000000000000000666, 1.000000000000000000, 1.000000000000000000, 1.000000000000000222, 1.000000000000000444, 1.000000000000000222, 1.000000000000000444, 0.9999999999999997780, 1.000000000000000444, 1.000000000000000444, 0.9999999999999997780, 1.000000000000000444, 1.000000000000000444, 1.000000000000000444, 1.000000000000000222, 1.000000000000000444, 1.000000000000000444, 1.000000000000000000, 1.000000000000000444, 0.9999999999999997780, 1.000000000000000444, 0.9999999999999997780, 1.000000000000000444, 1.000000000000000000, 1.000000000000000444, 1.000000000000000444, 1.000000000000000444, 1.000000000000000222, 1.000000000000000444, 1.000000000000000444, 1.000000000000000222, 1.000000000000000222, 1.000000000000000000, 1.000000000000000222, 1.000000000000000444, 0.9999999999999997780, 1.000000000000000666, 0.9999999999999997780, 1.000000000000000444, 1.000000000000000222, 1.000000000000000222, 1.000000000000000000, 1.000000000000000222, 1.000000000000000222, 1.000000000000000000, 1.000000000000000000, 1.000000000000000444, 1.000000000000000222, 1.000000000000000444, 0.9999999999999997780, 1.000000000000000444, 1.000000000000000444, 1.000000000000000222, 1.000000000000000444, 1.000000000000000000, 1.000000000000000444, 1.000000000000000444, 0.9999999999999997780, 1.000000000000000444, 1.000000000000000222, 1.000000000000000444, 1.000000000000000222, 1.000000000000000222, 1.000000000000000444, 1.000000000000000000, 1.000000000000000000, 1.000000000000000444, 1.000000000000000444, 1.000000000000000444, 0.9999999999999997780, 1.000000000000000444, 1.000000000000000222, 1.000000000000000222, 1.000000000000000444, 1.000000000000000000, 1.000000000000000444, 1.000000000000000222, 1.000000000000000444, 1.000000000000000000, 1.000000000000000444, 1.000000000000000444, 1.000000000000000444, 1.000000000000000000, 1.000000000000000444, 1.000000000000000000, 1.000000000000000222, 1.000000000000000444, 1.000000000000000444, 1.000000000000000000, 1.000000000000000444, 1.000000000000000444, 1.000000000000000000, 1.000000000000000444, 1.000000000000000222, 1.000000000000000000, 1.000000000000000444, 1.000000000000000222, 1.000000000000000222, 1.000000000000000444, 1.000000000000000444, 1.000000000000000000, 1.000000000000000000, 1.000000000000000444, 1.000000000000000000, 1.000000000000000222, 1.000000000000000444, 1.000000000000000000, 1.000000000000000222, 1.000000000000000444, 0.9999999999999997780, 1.000000000000000444, 1.000000000000000222, 1.000000000000000000, 1.000000000000000444, 1.000000000000000000, 1.000000000000000444, 1.000000000000000444, 1.000000000000000000, 1.000000000000000222, 1.000000000000000222, 1.000000000000000222, 1.000000000000000444, 1.000000000000000222, 1.000000000000000000, 1.000000000000000222, 1.000000000000000444, 1.000000000000000444, 1.000000000000000222, 1.000000000000000444, 1.000000000000000444, 1.000000000000000000, 1.000000000000000000, 1.000000000000000666, 0.9999999999999997780, 1.000000000000000444, 0.9999999999999997780, 1.000000000000000222, 0.9999999999999997780, 1.000000000000000444, 1.000000000000000000, 1.000000000000000222, 1.000000000000000222, 1.000000000000000444, 1.000000000000000000, 1.000000000000000000, 1.000000000000000444, 1.000000000000000000, 1.000000000000000222, 1.000000000000000222) ) ) 
 REPRESENTATION_ITEM ( '' )  SURFACE ( )  );
#13986=CARTESIAN_POINT ( 'NONE',  ( 4.873930702218094879, 1.184903577025652188, 1.686001177547257424 ) ) ;
#13990=CARTESIAN_POINT ( 'NONE',  ( 3.985024733980116363, -1.885273983189727831, -0.7249480779877092163 ) ) ;
#13995=CARTESIAN_POINT ( 'NONE',  ( 3.098563410164618226, -0.5969507786072983935, -1.972546241584592241 ) ) ;
#13996=CARTESIAN_POINT ( 'NONE',  ( 3.322888845334175389, 0.9041102021897020613, -1.802417075407992897 ) ) ;
#14000=CARTESIAN_POINT ( 'NONE',  ( 1.306327274835542784, 1.622920506532832929, 0.8694138843568788300 ) ) ;
#14001=CARTESIAN_POINT ( 'NONE',  ( 0.3293365701910222487, 2.210228212078951149, 0.6636047247109229108 ) ) ;
#14003=CARTESIAN_POINT ( 'NONE',  ( 2.108864864398530159, 1.603267699958549342, -1.450045708023157687 ) ) ;
#14005=CARTESIAN_POINT ( 'NONE',  ( 4.346934998023818331, -1.892857631927163498, -0.9488708475321022684 ) ) ;
#14007=CARTESIAN_POINT ( 'NONE',  ( 1.727212824277712944, -1.762453432929488528, 0.6273722324065673650 ) ) ;
#14008=CARTESIAN_POINT ( 'NONE',  ( 4.698096894549816049, -1.971010956759836397, -0.04940921540304286930 ) ) ;
#14009=CARTESIAN_POINT ( 'NONE',  ( 5.190638768449240992, 1.523797776992100284, -1.320824044268428255 ) ) ;
#14013=CARTESIAN_POINT ( 'NONE',  ( 6.604139054488365801, -2.105657007711879469, 0.04960021190137350877 ) ) ;
#14017=CARTESIAN_POINT ( 'NONE',  ( 5.524284814141814159, 1.174771371627521876, -1.583071389104006244 ) ) ;
#14018=CARTESIAN_POINT ( 'NONE',  ( 5.924083597509600452, -2.004057273996622701, 0.2512124657789679971 ) ) ;
#14020=CARTESIAN_POINT ( 'NONE',  ( 4.547712581667567200, -1.782031661950409962, -1.466240793230636275 ) ) ;
#14022=CARTESIAN_POINT ( 'NONE',  ( 1.850508050571671559, -2.052242141108654661, -0.2064673365099172486 ) ) ;
#14029=CARTESIAN_POINT ( 'NONE',  ( 4.738842072872849087, -2.104903140973454434, -0.5318641579697135358 ) ) ;
#14032=CARTESIAN_POINT ( 'NONE',  ( 3.016969003575611818, -1.773741936391802332, 0.4936923545346691977 ) ) ;
#14034=CARTESIAN_POINT ( 'NONE',  ( 6.620655732516644854, 4.701125524277991907, 2.388986273831222640 ) ) ;
#14035=CARTESIAN_POINT ( 'NONE',  ( 5.460537066722415567, -1.980877156148381335, -0.9378266216248376530 ) ) ;
#14037=CARTESIAN_POINT ( 'NONE',  ( 5.471622919743277969, 2.182126815565027300, -0.5975609995224858695 ) ) ;
#14042=CARTESIAN_POINT ( 'NONE',  ( 0.1448901830083254016, -1.363511527656173339, -1.128195317737596293 ) ) ;
#14043=CARTESIAN_POINT ( 'NONE',  ( 4.406893533441514244, -0.4431801161997659944, -1.963548474556547685 ) ) ;
#14045=CARTESIAN_POINT ( 'NONE',  ( 2.590967463960031303, -0.3587740299011917267, -2.075001757462133778 ) ) ;
#14046=CARTESIAN_POINT ( 'NONE',  ( 2.460426067449926535, -1.833815074015308300, -0.5538200352182551800 ) ) ;
#14048=CARTESIAN_POINT ( 'NONE',  ( 2.998452255303164726, 1.954363348466476857, 0.2436675063324095225 ) ) ;
#14049=CARTESIAN_POINT ( 'NONE',  ( 1.674454752297813265, -1.775319108138155633, -0.5897529795871117031 ) ) ;
#14050=CARTESIAN_POINT ( 'NONE',  ( 1.680054527999317759, -1.087118939145682583, -1.632918184844594611 ) ) ;
#14051=CARTESIAN_POINT ( 'NONE',  ( 4.353923116202039978, 1.724447095217627401, -0.04574849716902986557 ) ) ;
#14052=CARTESIAN_POINT ( 'NONE',  ( 1.283307755816986528, 0.1377011610334301639, -1.907463248872851569 ) ) ;
#14054=CARTESIAN_POINT ( 'NONE',  ( 1.524350002934187653, -1.228176919886795782, -1.833354347511229498 ) ) ;
#14060=CARTESIAN_POINT ( 'NONE',  ( 6.754772315933175619, -1.444328698515121800, 1.188528157999017454 ) ) ;
#14063=CARTESIAN_POINT ( 'NONE',  ( 6.526242037438201749, 1.059062773735760521, 1.778703558766213000 ) ) ;
#14064=CARTESIAN_POINT ( 'NONE',  ( 1.170471352854907776, -0.9292243337341490328, -1.850172451097586990 ) ) ;
#14069=CARTESIAN_POINT ( 'NONE',  ( 5.813165546740090228, 1.733599321496303691, -1.220823391460408303 ) ) ;
#14072=CARTESIAN_POINT ( 'NONE',  ( 6.109812101310618360, 0.5708666350849945781, -1.876949146916474298 ) ) ;
#14074=CARTESIAN_POINT ( 'NONE',  ( 4.745470142856022200, -1.954873481938533608, -0.4925652823710227612 ) ) ;
#14075=CARTESIAN_POINT ( 'NONE',  ( 4.100734417499996454, 1.753908128398029787, 0.7709784123341425488 ) ) ;
#14077=CARTESIAN_POINT ( 'NONE',  ( 1.874823134854076923, -0.1115055541827478930, -2.188858692977871279 ) ) ;
#14080=CARTESIAN_POINT ( 'NONE',  ( 4.763936024516410406, 0.6273381447981136727, -1.913061789696899995 ) ) ;
#14083=CARTESIAN_POINT ( 'NONE',  ( 5.905892042933183816, -1.176582040423958642, -1.760015123184681007 ) ) ;
#14085=CARTESIAN_POINT ( 'NONE',  ( 2.068024735862358021, -1.283949768261948288, 1.649988806608338798 ) ) ;
#14087=CARTESIAN_POINT ( 'NONE',  ( 0.4106395295978342297, 1.496939291644447279, 0.8566152473860905170 ) ) ;
#14099=CARTESIAN_POINT ( 'NONE',  ( 2.226969132303910470, 1.618658205268191930, 0.8133494039403755815 ) ) ;
#14103=CARTESIAN_POINT ( 'NONE',  ( 3.211360534488953977, 1.429591190403207035, 1.112411576641762379 ) ) ;
#14104=CARTESIAN_POINT ( 'NONE',  ( 6.539320575229256249, 2.979067782826943844, 2.350490835693248126 ) ) ;
#14109=CARTESIAN_POINT ( 'NONE',  ( 2.963170385688845609, 1.570644928931948181, 0.9979875196418576122 ) ) ;
#14110=CARTESIAN_POINT ( 'NONE',  ( 0.9135317552573400945, -1.216341065326152160, -1.479849217926126004 ) ) ;
#14111=CARTESIAN_POINT ( 'NONE',  ( 0.1119280604304096899, -0.7754228321929098611, -1.651232954423286436 ) ) ;
#14117=CARTESIAN_POINT ( 'NONE',  ( 4.241030189111538284, -0.1885853823969813603, -1.960358720193545068 ) ) ;
#14121=CARTESIAN_POINT ( 'NONE',  ( 6.562441972333600937, -2.001882313047067985, -0.8919867065708479981 ) ) ;
#14123=CARTESIAN_POINT ( 'NONE',  ( 5.614262457756467484, -0.8664596825185383322, -1.720589126903127264 ) ) ;
#14125=CARTESIAN_POINT ( 'NONE',  ( 0.3404811318320750679, 0.3065618842239410946, 1.799498403862239693 ) ) ;
#14126=CARTESIAN_POINT ( 'NONE',  ( 2.403190426070573871, 1.771669130372434564, -1.315670724662293178 ) ) ;
#14132=CARTESIAN_POINT ( 'NONE',  ( 6.977413706903823787, -0.1529601955215283693, 1.936277946061695898 ) ) ;
#14133=CARTESIAN_POINT ( 'NONE',  ( 1.382261328670054246, -0.2867773604850975544, -1.920668630092968732 ) ) ;
#14134=CARTESIAN_POINT ( 'NONE',  ( 0.7200771085676247463, -1.701685607325746252, -1.080902626906909747 ) ) ;
#14136=CARTESIAN_POINT ( 'NONE',  ( 5.594539833219323022, 1.833072992967394788, 0.3199324213378691439 ) ) ;
#14142=CARTESIAN_POINT ( 'NONE',  ( 1.294752383181968503, 1.788903229852260246, -1.265732775075766092 ) ) ;
#14147=CARTESIAN_POINT ( 'NONE',  ( 1.998415063578623085, -0.4859047700337820741, -1.759764234465097221 ) ) ;
#14151=CARTESIAN_POINT ( 'NONE',  ( 6.509000000000037645, 2.054060622569788386, 2.307050226316338382 ) ) ;
#14153=CARTESIAN_POINT ( 'NONE',  ( 0.2055245034400269288, -0.5150763003200479195, 1.856310442892949553 ) ) ;
#14154=CARTESIAN_POINT ( 'NONE',  ( 4.838696733575553743, -1.901848327180942766, -0.4805237247276354928 ) ) ;
#14157=CARTESIAN_POINT ( 'NONE',  ( 4.511385190476093321, -2.149204750630455241, 0.4279282578087198474 ) ) ;
#14160=CARTESIAN_POINT ( 'NONE',  ( 4.504778988403771223, 0.5471568804141565545, 1.996604337080605474 ) ) ;
#14163=CARTESIAN_POINT ( 'NONE',  ( 3.745041490520171212, 2.281215052333289250, -0.2826575254791847680 ) ) ;
#14170=CARTESIAN_POINT ( 'NONE',  ( 3.574105527548767647, -1.871835235816914578, -0.5168888941823551741 ) ) ;
#14173=EDGE_CURVE ( 'NONE', #29350, #88820, #120799, .T. ) ;
#14174=CARTESIAN_POINT ( 'NONE',  ( 5.379139070037473935, -1.731557697741787916, -0.8120211572784155063 ) ) ;
#14176=CARTESIAN_POINT ( 'NONE',  ( 4.717633463169556229, -1.691034389814783712, 0.3384810450017295969 ) ) ;
#14177=CARTESIAN_POINT ( 'NONE',  ( 4.100796195634116792, 1.845626398921360822, 0.8128187495666516771 ) ) ;
#14178=CARTESIAN_POINT ( 'NONE',  ( 4.975319123388493914, -2.281077821084981583, -0.2834334243917625562 ) ) ;
#14180=CARTESIAN_POINT ( 'NONE',  ( 0.4521680116954321371, 0.6883007682146925488, -2.096869779678663281 ) ) ;
#14183=CARTESIAN_POINT ( 'NONE',  ( 5.641803817319237524, 0.7161603046910887116, -1.618556768665664114 ) ) ;
#14184=CARTESIAN_POINT ( 'NONE',  ( 5.115861365725078436, 0.1511377038382749338, 2.010826595755777824 ) ) ;
#14186=CARTESIAN_POINT ( 'NONE',  ( 2.221020806870691366, 0.002245647979397680065, 2.292435215953308791 ) ) ;
#14187=CARTESIAN_POINT ( 'NONE',  ( 1.060061488152568510, -1.571881217706198042, -0.7472303940359821262 ) ) ;
#14190=CARTESIAN_POINT ( 'NONE',  ( 1.088703816646944267, 1.038853075768126910, -1.387971508864824788 ) ) ;
#14193=CARTESIAN_POINT ( 'NONE',  ( 1.117902646172004522, 0.4237721370383492059, -2.129260471988907000 ) ) ;
#14194=CARTESIAN_POINT ( 'NONE',  ( 2.448454179885679149, -1.387098808145654560, 1.463928423225707931 ) ) ;
#14196=CARTESIAN_POINT ( 'NONE',  ( 6.721331456258776704, -0.1291123375851965516, 1.896827325797964869 ) ) ;
#14198=CARTESIAN_POINT ( 'NONE',  ( 2.848112528106065078, -1.494902295879830589, -1.643281164644925907 ) ) ;
#14203=CARTESIAN_POINT ( 'NONE',  ( 5.899919523139840472, -0.6348737135929006792, -1.620717943835482844 ) ) ;
#14205=CARTESIAN_POINT ( 'NONE',  ( 3.402741375674179114, 0.4741672551989496998, 1.903589013717405853 ) ) ;
#14209=CARTESIAN_POINT ( 'NONE',  ( 4.253392140805613231, -1.877938019876054243, -1.261413133637336204 ) ) ;
#14210=CARTESIAN_POINT ( 'NONE',  ( 0.7661727470247855498, -2.052889565338772204, 0.2005107248105562623 ) ) ;
#14212=CARTESIAN_POINT ( 'NONE',  ( 2.342968712349004168, 0.4955985968413346709, 2.207426715909040826 ) ) ;
#14215=CARTESIAN_POINT ( 'NONE',  ( 3.444469828353763141, 0.4513171681363346566, 1.815172769691273835 ) ) ;
#14216=CARTESIAN_POINT ( 'NONE',  ( 2.689770611714628945, 1.466270380367465043, 0.9255270069659697896 ) ) ;
#14217=CARTESIAN_POINT ( 'NONE',  ( 6.620655732516649294, -0.002413161512292843602, 2.173887093218459743 ) ) ;
#14218=CARTESIAN_POINT ( 'NONE',  ( 0.2005908178989434243, -2.206344910233990486, -0.05143828380192031619 ) ) ;
#14219=CARTESIAN_POINT ( 'NONE',  ( 4.329101982860062314, 0.1031891237209987822, 2.159356164053369387 ) ) ;
#14220=CARTESIAN_POINT ( 'NONE',  ( 4.505766059781188382, -0.8317635995198893184, -1.754939027834252485 ) ) ;
#14222=CARTESIAN_POINT ( 'NONE',  ( 6.274654046616443992, -1.776150972019393093, -0.5868208112121617859 ) ) ;
#14227=CARTESIAN_POINT ( 'NONE',  ( 5.942029771888944545, -1.730864577151491890, -1.034168155301495862 ) ) ;
#14231=CARTESIAN_POINT ( 'NONE',  ( 3.105874302609371362, -1.823586186413633126, 0.09019715141062728536 ) ) ;
#14239=CARTESIAN_POINT ( 'NONE',  ( -0.01731643392406666954, -1.316173432332496507, 1.532187831819804780 ) ) ;
#14240=CARTESIAN_POINT ( 'NONE',  ( 1.524255003590764046, -2.104078925693805502, 0.2628582283784736684 ) ) ;
#14243=CARTESIAN_POINT ( 'NONE',  ( 2.184208379282841950, 1.076359544750982389, -1.517863362848305808 ) ) ;
#14245=CARTESIAN_POINT ( 'NONE',  ( 6.508673417949426110, 1.528841652884159963, -1.382195874861185336 ) ) ;
#14246=CARTESIAN_POINT ( 'NONE',  ( 5.924453975591452703, -1.462443569488897754, -1.388487997949397368 ) ) ;
#14251=CARTESIAN_POINT ( 'NONE',  ( -0.2108831679771167866, 1.375689764684871808, -2.152500126786048185 ) ) ;
#14258=CARTESIAN_POINT ( 'NONE',  ( 5.835314490094169138, -1.281163661392352493, 1.556671411349755285 ) ) ;
#14259=CARTESIAN_POINT ( 'NONE',  ( 4.171694865975253741, -1.058263924308279424, 1.506412014522513720 ) ) ;
#14261=CARTESIAN_POINT ( 'NONE',  ( -0.02299388927988389730, 0.001624902753813092359, -1.910968047046639251 ) ) ;
#14262=CARTESIAN_POINT ( 'NONE',  ( 3.545847025713305012, -1.747029255069532550, -1.507864240153370172 ) ) ;
#14264=CARTESIAN_POINT ( 'NONE',  ( 6.520800673124607982, 2.014292100380775885, 0.7847517145297827623 ) ) ;
#14265=CARTESIAN_POINT ( 'NONE',  ( 0.7318534483069280006, 1.913536139905326339, 0.3307262847246707493 ) ) ;
#14268=CARTESIAN_POINT ( 'NONE',  ( 4.534687899768989006, 2.230887184458398398, -0.5525863250545393068 ) ) ;
#14271=CARTESIAN_POINT ( 'NONE',  ( 5.049604242677837362, 0.5861553263475408615, -1.776501995420045832 ) ) ;
#14272=CARTESIAN_POINT ( 'NONE',  ( 1.019614524654769872, -0.4619345408787678964, 1.855657206939323789 ) ) ;
#14275=CARTESIAN_POINT ( 'NONE',  ( 2.455956380646412196, 0.5873987694336445520, -2.127207350628975924 ) ) ;
#14276=CARTESIAN_POINT ( 'NONE',  ( 6.883263157960367806, 0.5819222519044697783, 1.998722019247618276 ) ) ;
#14281=CARTESIAN_POINT ( 'NONE',  ( 1.282427153303007605, -1.922404290768309432, -0.4359020612285709473 ) ) ;
#14282=CARTESIAN_POINT ( 'NONE',  ( 1.132322824279883955, -1.466084937595305560, -1.782028031347275832 ) ) ;
#14283=CARTESIAN_POINT ( 'NONE',  ( 2.066782613880484565, 1.455849762852476248, -1.315278764014264912 ) ) ;
#14284=CARTESIAN_POINT ( 'NONE',  ( 5.577030875653865571, 1.903616248300431746, 0.7944661687919268855 ) ) ;
#14291=CARTESIAN_POINT ( 'NONE',  ( 0.4972420419220639487, 0.3698279840313797862, 2.139175918340649574 ) ) ;
#14296=CARTESIAN_POINT ( 'NONE',  ( 2.284254421533092216, -1.833544361078912388, -0.3693468884775340522 ) ) ;
#14297=CARTESIAN_POINT ( 'NONE',  ( 6.749309733681256418, -1.731629633356733589, -1.293610171197785652 ) ) ;
#14300=CARTESIAN_POINT ( 'NONE',  ( -0.02244404828160087226, 4.081832076214893412, -2.743766916979750281 ) ) ;
#14301=CARTESIAN_POINT ( 'NONE',  ( 6.827182134110164391, 0.5838490905608649806, 1.963161153048794905 ) ) ;
#14303=CARTESIAN_POINT ( 'NONE',  ( 2.104032245951466429, -0.8162354410432022256, 1.729450509904674416 ) ) ;
#14304=CARTESIAN_POINT ( 'NONE',  ( 3.625649997064513297, -1.053871202854910871, -1.421704988934450409 ) ) ;
#14305=CARTESIAN_POINT ( 'NONE',  ( 2.367698891403247519, 0.5082884949165042965, -1.843433491391050838 ) ) ;
#14308=CARTESIAN_POINT ( 'NONE',  ( 5.536718839138406345, -1.507006759595967305, 1.182436279247323085 ) ) ;
#14309=CARTESIAN_POINT ( 'NONE',  ( 0.2036857628631080219, -1.599406074100502506, -1.314310892166506095 ) ) ;
#14311=CARTESIAN_POINT ( 'NONE',  ( 1.793382672576701919, -0.1090974814243403090, -2.117938670719583527 ) ) ;
#14314=CARTESIAN_POINT ( 'NONE',  ( 4.785944050937030347, -0.8815013282119155136, 1.649949660215948688 ) ) ;
#14315=CARTESIAN_POINT ( 'NONE',  ( 0.5744775230259161480, -1.718042477583326066, -0.6180270036199516648 ) ) ;
#14317=CARTESIAN_POINT ( 'NONE',  ( 4.512475528931441104, -0.9420208833846724916, -1.995868093903986118 ) ) ;
#14320=CARTESIAN_POINT ( 'NONE',  ( 1.328664801108740523, -1.309985447229580213, 1.593267124675311841 ) ) ;
#14331=CARTESIAN_POINT ( 'NONE',  ( 3.771986465066007099, -2.040223509676724500, 0.3510349978646867264 ) ) ;
#14333=CARTESIAN_POINT ( 'NONE',  ( 2.056162960589353883, 2.155939639820044107, -0.1567802445739118478 ) ) ;
#14335=CARTESIAN_POINT ( 'NONE',  ( 2.016276777042900203, -2.019190368190917795, 0.05175015523710930349 ) ) ;
#14344=CARTESIAN_POINT ( 'NONE',  ( -0.1706859984542466180, -1.561801110730935971, -1.275320528755889526 ) ) ;
#14345=CARTESIAN_POINT ( 'NONE',  ( 4.968408144156592599, -2.063508908063705238, -0.7385586828293492223 ) ) ;
#14347=CARTESIAN_POINT ( 'NONE',  ( 4.131050151015442928, 1.750605847248308145, 0.7702136748066327199 ) ) ;
#14351=CARTESIAN_POINT ( 'NONE',  ( 2.302361438560030393, 1.314982760645909465, -1.528754769246756018 ) ) ;
#14354=CARTESIAN_POINT ( 'NONE',  ( 5.086778385480665854, -0.2138867007538784171, -1.711364050844576434 ) ) ;
#14355=CARTESIAN_POINT ( 'NONE',  ( 0.1405533004714279999, 2.862415582289945526, -2.767767315042678700 ) ) ;
#14361=DIRECTION ( 'NONE',  ( -3.451266460341926649E-31, -5.200009205990155575E-32, 1.000000000000000000 ) ) ;
#14363=CARTESIAN_POINT ( 'NONE',  ( 4.512255818007496977, -1.811207030272870000, -0.03965706671436861758 ) ) ;
#14366=CARTESIAN_POINT ( 'NONE',  ( 6.586573151046549945, -1.108064789702201569, 1.433474704228101748 ) ) ;
#14369=CARTESIAN_POINT ( 'NONE',  ( 3.064592470464472473, -2.024993410009158890, -0.8382372354380845936 ) ) ;
#14371=CARTESIAN_POINT ( 'NONE',  ( 6.848144937404742727, -0.7948834574948275833, 1.681425573653466676 ) ) ;
#14373=CARTESIAN_POINT ( 'NONE',  ( 5.360912872498101223, -0.05169663686300975808, -1.915091480415902048 ) ) ;
#14375=DIRECTION ( 'NONE',  ( -1.000000000000000000, 0.000000000000000000, 0.000000000000000000 ) ) ;
#14379=CARTESIAN_POINT ( 'NONE',  ( 1.762795743007524063, -1.528684080660724920, 1.528680807790387286 ) ) ;
#14382=CARTESIAN_POINT ( 'NONE',  ( 1.412830140145465263, 1.608106816955911178, 0.8641515426408912237 ) ) ;
#14384=CARTESIAN_POINT ( 'NONE',  ( 4.471595891589618788, 1.770651423122941548, -0.4439726157009425411 ) ) ;
#14387=CARTESIAN_POINT ( 'NONE',  ( 2.988426722125224977, -1.135634098421594240, 1.538566774472991616 ) ) ;
#14389=CARTESIAN_POINT ( 'NONE',  ( 3.930098287398839041, 1.092129198686382141, 1.638800773490353802 ) ) ;
#14391=CARTESIAN_POINT ( 'NONE',  ( 4.950698622930713277, -1.642605121802564350, -1.035792469189389386 ) ) ;
#14395=CARTESIAN_POINT ( 'NONE',  ( 5.449516625918088053, -1.916229881892789866, 0.9086369058012438993 ) ) ;
#14402=CARTESIAN_POINT ( 'NONE',  ( 4.986981296356192139, -1.896340117422308236, -0.6759883393069978652 ) ) ;
#14405=CARTESIAN_POINT ( 'NONE',  ( 4.688025921862073453, -0.8580590012943272171, 1.611482198803436905 ) ) ;
#14406=CARTESIAN_POINT ( 'NONE',  ( 0.4673438449808891559, 1.800595422158430825, 1.021790579661910003 ) ) ;
#14411=CARTESIAN_POINT ( 'NONE',  ( 5.418772907935071714, 1.728844841293469159, 0.7149302089985640762 ) ) ;
#14420=CARTESIAN_POINT ( 'NONE',  ( 1.692325190600419305, 1.023896122633965566, -1.799289093316607469 ) ) ;
#14421=CARTESIAN_POINT ( 'NONE',  ( 2.126704408204147967, 0.4671447874508818932, 2.064898165909804906 ) ) ;
#14424=CARTESIAN_POINT ( 'NONE',  ( 0.8132587859420150611, -1.660809389245621492, -1.058212622827129357 ) ) ;
#14428=FACE_OUTER_BOUND ( 'NONE', #102166, .T. ) ;
#14429=CARTESIAN_POINT ( 'NONE',  ( 3.082263327019618249, -2.258438545724365643, -0.3914850642001906356 ) ) ;
#14430=CARTESIAN_POINT ( 'NONE',  ( 0.6447967512687136082, -1.567379569643694515, 0.9359695128687425258 ) ) ;
#14432=CARTESIAN_POINT ( 'NONE',  ( 2.109489925670060551, 1.480643174185194200, 1.210387159491378650 ) ) ;
#14435=CARTESIAN_POINT ( 'NONE',  ( 2.232683648988046610, 1.311727534961094177, -1.527327462066043084 ) ) ;
#14436=CARTESIAN_POINT ( 'NONE',  ( 1.410910527293834260, -1.549868713165471590, 1.202602906592651788 ) ) ;
#14441=CARTESIAN_POINT ( 'NONE',  ( 3.433613042289254569, 0.9395709039844526433, -1.867677030932006765 ) ) ;
#14442=CARTESIAN_POINT ( 'NONE',  ( 3.168565732603556562, -1.634766719728536266, -0.6786406015907071598 ) ) ;
#14445=CARTESIAN_POINT ( 'NONE',  ( 6.175753646036172384, -1.231511006544892206, 1.933186584637256678 ) ) ;
#14446=CARTESIAN_POINT ( 'NONE',  ( 4.365022556061240344, 1.687170946148343953, -0.4262992432423305389 ) ) ;
#14449=CARTESIAN_POINT ( 'NONE',  ( 4.674945122873967129, -0.7415060156777570910, -1.567401138452922060 ) ) ;
#14450=CARTESIAN_POINT ( 'NONE',  ( 5.055217142685058285, 1.807878865648751221, -1.202052933306910765 ) ) ;
#14452=CARTESIAN_POINT ( 'NONE',  ( 6.227749967195368441, 0.7672974224810541477, -1.865044430435198741 ) ) ;
#14453=CARTESIAN_POINT ( 'NONE',  ( 4.968750000000002665, 0.7852924748297213098, -1.895863743164188042 ) ) ;
#14455=CARTESIAN_POINT ( 'NONE',  ( 2.836843495735667187, 0.2342426253194809793, 1.912026175940540140 ) ) ;
#14457=CARTESIAN_POINT ( 'NONE',  ( 6.310783679736120533, -0.5911123833974815112, -2.141223572898354188 ) ) ;
#14459=CARTESIAN_POINT ( 'NONE',  ( 6.883263157960399781, 2.038134514454426505, 2.350812138539408735 ) ) ;
#14462=CARTESIAN_POINT ( 'NONE',  ( 1.331071098547026654, 1.488246241617418697, -1.649206797639357180 ) ) ;
#14471=CARTESIAN_POINT ( 'NONE',  ( 5.494603814743470593, 2.031562770168824361, 0.3561260095714424700 ) ) ;
#14476=CARTESIAN_POINT ( 'NONE',  ( 6.555916519444559221, 1.865492442988415656, -0.1378669075578625169 ) ) ;
#14477=CARTESIAN_POINT ( 'NONE',  ( 5.906827578720975858, -0.9711093913858243054, -1.436504219383877290 ) ) ;
#14478=CARTESIAN_POINT ( 'NONE',  ( 4.141972075035261547, 0.4693275899197508760, 1.675879475284934195 ) ) ;
#14480=CARTESIAN_POINT ( 'NONE',  ( 3.509589594912354116, -2.258262956851801118, 0.3931918642409871212 ) ) ;
#14482=CARTESIAN_POINT ( 'NONE',  ( 1.446930991382020748, 0.5358794165791405106, -1.761430032344503349 ) ) ;
#14485=CARTESIAN_POINT ( 'NONE',  ( 2.028078973712159172, 1.053637016394028292, -1.490636434207486261 ) ) ;
#14486=CARTESIAN_POINT ( 'NONE',  ( 2.637342451166882373, 0.6819965276749391236, 1.897697610567940174 ) ) ;
#14487=CARTESIAN_POINT ( 'NONE',  ( 1.131117939106265791, -1.979831898266545487, 0.9398196729281658168 ) ) ;
#14489=CARTESIAN_POINT ( 'NONE',  ( 3.944438254296574797, 2.095630017474863660, 0.2083849179023259668 ) ) ;
#14492=CARTESIAN_POINT ( 'NONE',  ( 1.311079954825690619, -1.633285661836245906, 1.272233187909928454 ) ) ;
#14495=CARTESIAN_POINT ( 'NONE',  ( 3.387459763963754700, 0.05019612904376415108, -2.120051327867578550 ) ) ;
#14496=CARTESIAN_POINT ( 'NONE',  ( 6.094357461763901362, -1.817385979143220309, -0.1739998769475574192 ) ) ;
#14503=CARTESIAN_POINT ( 'NONE',  ( 3.181903496825384092, 1.969597418195143446, -0.4466673548119536319 ) ) ;
#14504=CARTESIAN_POINT ( 'NONE',  ( 0.6222711621935803628, -1.126682295963852276, -1.779026129514348353 ) ) ;
#14508=CARTESIAN_POINT ( 'NONE',  ( 5.735155330654303718, -0.04388460642621531960, -1.860581820771879835 ) ) ;
#14514=CARTESIAN_POINT ( 'NONE',  ( 2.435929278166943490, 1.204617592564939166, 1.548422000036096202 ) ) ;
#14515=CARTESIAN_POINT ( 'NONE',  ( 0.2687375195599971400, -1.410744835756465365, 1.637978619736128127 ) ) ;
#14519=CARTESIAN_POINT ( 'NONE',  ( 2.899396954618923772, 0.2085115220819243054, 1.721149687620449953 ) ) ;
#14520=CARTESIAN_POINT ( 'NONE',  ( 2.536699030922508591, -1.289252169270055370, -1.169197435003018315 ) ) ;
#14521=CARTESIAN_POINT ( 'NONE',  ( 0.3414292828918061296, 0.3991051782518301727, 2.272663865251875581 ) ) ;
#14524=CARTESIAN_POINT ( 'NONE',  ( 2.319669497725483254, -1.999663683883694532, 0.4976976026799494468 ) ) ;
#14525=CARTESIAN_POINT ( 'NONE',  ( 1.651720012567552853, -0.2930234437087535504, -1.994564656426714988 ) ) ;
#14526=CARTESIAN_POINT ( 'NONE',  ( 6.925078400183519278, 1.259550266093687920, 2.159391284976417857 ) ) ;
#14528=CARTESIAN_POINT ( 'NONE',  ( 1.112115884188523918, -0.8845927946041342027, -1.761928416731074476 ) ) ;
#14529=CARTESIAN_POINT ( 'NONE',  ( 4.183787391381143195, 1.853651273288700718, -0.4697857328580385960 ) ) ;
#14534=CARTESIAN_POINT ( 'NONE',  ( 0.8033855960881201019, 1.780198652630104794, -0.9539489498650125521 ) ) ;
#14536=CARTESIAN_POINT ( 'NONE',  ( 5.069473898719869531, 0.2322026582469650102, -2.295885384840197663 ) ) ;
#14537=CARTESIAN_POINT ( 'NONE',  ( 5.459412808053472510, 1.602871733476991079, 1.130958114227413436 ) ) ;
#14539=CARTESIAN_POINT ( 'NONE',  ( 2.078885752709497492, 1.828579749420868872, 0.7109141669488158177 ) ) ;
#14543=CARTESIAN_POINT ( 'NONE',  ( 1.692723046232265105, 1.565162839624185898, -1.426121385913220019 ) ) ;
#14546=CARTESIAN_POINT ( 'NONE',  ( 1.323879276782027770, 1.773944146221797746, 0.4926282247687193139 ) ) ;
#14548=CARTESIAN_POINT ( 'NONE',  ( 4.627881963378519536, 2.107464937132212501, -0.5213077441503320975 ) ) ;
#14551=CARTESIAN_POINT ( 'NONE',  ( 2.162495577681341707, 2.120227376586072854, 0.04728746717985036346 ) ) ;
#14554=CARTESIAN_POINT ( 'NONE',  ( 2.847006562934909280, -1.715207642559450685, 1.141990792043580338 ) ) ;
#14556=CARTESIAN_POINT ( 'NONE',  ( 0.2218712608162629052, 1.761692264604281633, 0.5354471447000588302 ) ) ;
#14558=CARTESIAN_POINT ( 'NONE',  ( -0.02264175331119500090, 1.349762599094967763, -2.344447671987642146 ) ) ;
#14561=CARTESIAN_POINT ( 'NONE',  ( 0.5048604690408053930, -0.7474223562033958101, -2.076596198196341003 ) ) ;
#14562=CARTESIAN_POINT ( 'NONE',  ( 1.001694622806301060, 1.849986872810194694, 1.302049432249830607 ) ) ;
#14565=CARTESIAN_POINT ( 'NONE',  ( 2.812559491778331200, -0.5300286150072616165, -1.732275345909091380 ) ) ;
#14566=CARTESIAN_POINT ( 'NONE',  ( 1.692462117551472911, 1.416773270106906235, -1.289619884002331407 ) ) ;
#14567=CARTESIAN_POINT ( 'NONE',  ( 3.033707436314789785, 1.966763487489433970, -0.6469820378900912328 ) ) ;
#14569=EDGE_CURVE ( 'NONE', #126082, #26543, #127168, .T. ) ;
#14570=CARTESIAN_POINT ( 'NONE',  ( 1.709780583834107803, -1.956794704801574358, 0.2394988650771395777 ) ) ;
#14571=CARTESIAN_POINT ( 'NONE',  ( 0.1297406284284522426, -1.182532350666727128, -1.521449160436913584 ) ) ;
#14572=CARTESIAN_POINT ( 'NONE',  ( 3.168673215318769110, -1.727878594304608217, -0.7172629358194044791 ) ) ;
#14573=CARTESIAN_POINT ( 'NONE',  ( 1.524504908422112726, -1.285150704446396341, -1.916548379014111791 ) ) ;
#14575=CARTESIAN_POINT ( 'NONE',  ( 2.330303589177587398, -1.147911989558418222, 1.464751052146954224 ) ) ;
#14577=CARTESIAN_POINT ( 'NONE',  ( 5.072745416573516408, 1.424789591659934684, -1.491725785151225336 ) ) ;
#14580=CARTESIAN_POINT ( 'NONE',  ( 6.124072230051534227, -1.166888049220366597, -1.752910934067633875 ) ) ;
#14582=CARTESIAN_POINT ( 'NONE',  ( 6.011032505573889573, 1.903242638633116712, 1.024824547371510075 ) ) ;
#14583=CARTESIAN_POINT ( 'NONE',  ( 0.5910386730991653570, -0.6632029860377097741, 1.717849102829023922 ) ) ;
#14584=CARTESIAN_POINT ( 'NONE',  ( 5.391273274344085209, -0.05166147132495273880, -2.019192591660509351 ) ) ;
#14593=CARTESIAN_POINT ( 'NONE',  ( 3.380092458137720968, -2.014432998692190058, -0.09411721906785883163 ) ) ;
#14597=CARTESIAN_POINT ( 'NONE',  ( 5.471600609837615536, 2.084441204114939161, -0.5725544205837928002 ) ) ;
#14602=CARTESIAN_POINT ( 'NONE',  ( 5.185172808627552143, 1.650094130669476522, 1.158673036085342112 ) ) ;
#14604=CARTESIAN_POINT ( 'NONE',  ( 2.068594797844982125, -1.576417056545238893, -0.7005022305992656406 ) ) ;
#14610=CARTESIAN_POINT ( 'NONE',  ( 0.2976568962721929390, -1.769157359987379996, -0.05240849467303894393 ) ) ;
#14611=CARTESIAN_POINT ( 'NONE',  ( 0.2760392706695756759, 1.990868297383071139, -0.2976099395228733457 ) ) ;
#14613=CARTESIAN_POINT ( 'NONE',  ( 2.925073249431627165, 2.077443920948469192, 0.7446974470129495982 ) ) ;
#14614=CARTESIAN_POINT ( 'NONE',  ( 5.664936021742177807, 1.649023742746661192, -1.412335049966114253 ) ) ;
#14618=CARTESIAN_POINT ( 'NONE',  ( 3.088655771522513582, -1.261447869382603004, 1.704333039148818507 ) ) ;
#14619=CARTESIAN_POINT ( 'NONE',  ( 1.441030037510174777, -1.730879250949714843, -1.034145807338890277 ) ) ;
#14620=CARTESIAN_POINT ( 'NONE',  ( 2.408236768384981019, -1.806978867004911171, -0.1295660047265032311 ) ) ;
#14626=CARTESIAN_POINT ( 'NONE',  ( 1.586979130512996772, 1.594871783843774260, 1.060967117046989427 ) ) ;
#14634=CARTESIAN_POINT ( 'NONE',  ( 4.751185534883737738, 0.1928377863454934504, -2.007255887737584121 ) ) ;
#14635=CARTESIAN_POINT ( 'NONE',  ( 5.629794960336353071, -1.368038101806166029, -1.673757646710342550 ) ) ;
#14638=CARTESIAN_POINT ( 'NONE',  ( 1.916421503514931679, -2.120014230100770725, 0.05699577502370903326 ) ) ;
#14639=CARTESIAN_POINT ( 'NONE',  ( -0.1298852118743840378, 0.7651466308506644776, -1.811855282322960781 ) ) ;
#14642=CARTESIAN_POINT ( 'NONE',  ( 3.690661264905565009, -0.3812834177611671982, -1.933973196684968920 ) ) ;
#14643=CARTESIAN_POINT ( 'NONE',  ( 5.185773951807310489, 1.841398108398510480, -0.5159224025059682139 ) ) ;
#14646=CARTESIAN_POINT ( 'NONE',  ( 0.5728211633247158874, 1.428863753495920763, -1.498466819491943269 ) ) ;
#14647=CARTESIAN_POINT ( 'NONE',  ( 2.062350447250702157, -1.775486198902403778, -0.7870378659600388849 ) ) ;
#14652=CARTESIAN_POINT ( 'NONE',  ( 2.537156728381038118, -1.549654062961543177, -1.403521045075975415 ) ) ;
#14655=CARTESIAN_POINT ( 'NONE',  ( 6.604189988765333474, -0.8127675640051763573, 1.729262449380222222 ) ) ;
#14657=CARTESIAN_POINT ( 'NONE',  ( 4.688207069967821106, -1.042061291317699423, 1.945354640606362873 ) ) ;
#14659=CARTESIAN_POINT ( 'NONE',  ( 2.626236979526615389, -1.269917727785064843, -1.804575601930514139 ) ) ;
#14662=CARTESIAN_POINT ( 'NONE',  ( 1.400873256076972329, -0.2815782128867699852, -1.891321520182134286 ) ) ;
#14665=CARTESIAN_POINT ( 'NONE',  ( 4.299325596424930396, -1.802881993240162961, 1.017688063649782482 ) ) ;
#14667=CARTESIAN_POINT ( 'NONE',  ( 1.305796196612364124, -0.5247483525172502716, 2.096912610238470975 ) ) ;
#14668=CARTESIAN_POINT ( 'NONE',  ( 4.071962858106247474, -1.261020321617589479, 1.792237525612811355 ) ) ;
#14669=CARTESIAN_POINT ( 'NONE',  ( -0.07968760456310633455, 7.629137130509075604, -2.426417496045676803 ) ) ;
#14674=CARTESIAN_POINT ( 'NONE',  ( 0.3346115673153668424, 0.6298721381652396811, -1.915601020889952322 ) ) ;
#14676=CARTESIAN_POINT ( 'NONE',  ( 4.944224162298806569, -0.9806570695735459253, 1.823293813017504039 ) ) ;
#14677=CARTESIAN_POINT ( 'NONE',  ( 2.842313889931574522, 1.911971217405187495, 0.2356370756458354143 ) ) ;
#14678=CARTESIAN_POINT ( 'NONE',  ( 5.993796379919574591, -2.101200072677239739, 0.2596931833054038630 ) ) ;
#14681=CARTESIAN_POINT ( 'NONE',  ( 3.907052821786443975, -1.612583007836394966, 1.130340192709837766 ) ) ;
#14682=CARTESIAN_POINT ( 'NONE',  ( 5.490252784120214002, -0.5523235152877626897, -2.224609438220140234 ) ) ;
#14683=CARTESIAN_POINT ( 'NONE',  ( 4.617693566336190436, -1.789886777702164089, 0.3589094947460610974 ) ) ;
#14691=CARTESIAN_POINT ( 'NONE',  ( 5.414319639144633101, -2.013376227731620283, 0.004290823026709827959 ) ) ;
#14692=CARTESIAN_POINT ( 'NONE',  ( 5.731119460814408484, 2.295830932937119595, 0.1164615576392889484 ) ) ;
#14693=CARTESIAN_POINT ( 'NONE',  ( 5.875826477234550538, -1.914729252524836056, 0.4262945716600323731 ) ) ;
#14699=CARTESIAN_POINT ( 'NONE',  ( 1.487951815845720338, -2.081006265264739419, -0.2013860056617396421 ) ) ;
#14700=CARTESIAN_POINT ( 'NONE',  ( 0.5670072068131201126, 0.1877032549213939472, -1.861219751863735672 ) ) ;
#14702=CARTESIAN_POINT ( 'NONE',  ( 5.736261908918430130, 0.3809393362203088440, 1.904059320497718089 ) ) ;
#14703=CARTESIAN_POINT ( 'NONE',  ( -0.2104748580754183807, 2.005809028216706924, -2.517884123765606663 ) ) ;
#14704=CARTESIAN_POINT ( 'NONE',  ( 1.206182128890446403, 1.534490571913693868, 0.8211921505957423539 ) ) ;
#14707=CARTESIAN_POINT ( 'NONE',  ( 1.312684994149786455, 1.519677550804766852, 0.8159285863849721210 ) ) ;
#14708=CARTESIAN_POINT ( 'NONE',  ( 1.470551405592795957, -2.082434148983134392, -0.6831980896230758216 ) ) ;
#14709=CARTESIAN_POINT ( 'NONE',  ( 6.854911444608583260, -0.7389736882487309977, 1.567799899397160912 ) ) ;
#14710=CARTESIAN_POINT ( 'NONE',  ( 3.633602750639616019, -2.039237483250630589, 0.8441791899983088765 ) ) ;
#14712=CARTESIAN_POINT ( 'NONE',  ( 1.305810364819631753, -1.710103357748852027, -1.337415221091219353 ) ) ;
#14713=CARTESIAN_POINT ( 'NONE',  ( 0.3108172448005979138, 1.586703044182024458, 0.9029097728878652251 ) ) ;
#14714=CARTESIAN_POINT ( 'NONE',  ( 2.413409855213846544, -1.973772631060242144, 0.7668006401621522139 ) ) ;
#14716=CARTESIAN_POINT ( 'NONE',  ( 6.639320575229231025, 3.706874577532508486, 2.311316081152973823 ) ) ;
#14718=CARTESIAN_POINT ( 'NONE',  ( 2.156203017566417302, 0.9840264443441574249, 2.070573632387271434 ) ) ;
#14722=CARTESIAN_POINT ( 'NONE',  ( 5.145291483242067088, 0.1622298597842904699, 2.215448774714718461 ) ) ;
#14729=CARTESIAN_POINT ( 'NONE',  ( 2.426407915648312930, -1.496052118593782065, -1.352154011671408362 ) ) ;
#14731=CARTESIAN_POINT ( 'NONE',  ( 2.114201203919101157, 2.057314814202032771, -0.1476098556340669499 ) ) ;
#14737=CARTESIAN_POINT ( 'NONE',  ( 5.367185978643659539, 2.112682091867735146, -0.5819856738719306755 ) ) ;
#14738=CARTESIAN_POINT ( 'NONE',  ( 2.057267738415057057, -1.238319999287675888, 1.591319116112683618 ) ) ;
#14739=CARTESIAN_POINT ( 'NONE',  ( 0.6261898170028465938, 0.1349980957352381883, 1.836376839866371569 ) ) ;
#14742=CARTESIAN_POINT ( 'NONE',  ( 5.772426501671443333, -1.156275361458743545, 1.412693073426966262 ) ) ;
#14743=CARTESIAN_POINT ( 'NONE',  ( 6.276017556857773627, 1.753032240926259311, -0.9962986157117934560 ) ) ;
#14745=CARTESIAN_POINT ( 'NONE',  ( 4.768612610038791111, -1.481304060603398032, 1.710260256980479898 ) ) ;
#14747=CARTESIAN_POINT ( 'NONE',  ( 0.4695305163736606668, 0.2040741594158005934, -2.096154701512464413 ) ) ;
#14749=CARTESIAN_POINT ( 'NONE',  ( 4.527825515032589898, 2.008996319933327612, -0.4998958796476050681 ) ) ;
#14759=CARTESIAN_POINT ( 'NONE',  ( 2.566880079249767022, 0.7526719050801253807, 2.090118821510750458 ) ) ;
#14764=CARTESIAN_POINT ( 'NONE',  ( 3.701569118832209515, -1.483977648892897960, -1.283320388228793130 ) ) ;
#14770=CARTESIAN_POINT ( 'NONE',  ( 2.689816194747224110, 2.012238202079220439, -0.6693303307304664385 ) ) ;
#14772=CARTESIAN_POINT ( 'NONE',  ( 4.258765444007106105, -1.603684720688375975, 1.449730421305382544 ) ) ;
#14773=CARTESIAN_POINT ( 'NONE',  ( 3.069684041021227827, -1.094477399149307306, 1.480508570315848482 ) ) ;
#14776=CARTESIAN_POINT ( 'NONE',  ( 6.087833319296645840, -1.732659258567319505, -0.1633284621618599775 ) ) ;
#14780=CARTESIAN_POINT ( 'NONE',  ( 2.729541802387557059, -2.017400560480298033, 0.7770373237434913261 ) ) ;
#14781=CARTESIAN_POINT ( 'NONE',  ( 4.007185349139028574, 2.006139037694018690, 0.2004037502189442987 ) ) ;
#14783=CARTESIAN_POINT ( 'NONE',  ( 2.483474991488154870, 1.976725341044349271, -0.8753317036461552014 ) ) ;
#14785=CARTESIAN_POINT ( 'NONE',  ( 3.128153591792836252, 1.098079186366843985, -1.637025598404780791 ) ) ;
#14786=CARTESIAN_POINT ( 'NONE',  ( 6.509000000000039421, 4.695815278351551214, 2.562658139094181386 ) ) ;
#14787=CARTESIAN_POINT ( 'NONE',  ( 4.353030786369998850, 0.4220677823760305980, -1.895499586301018224 ) ) ;
#14796=CARTESIAN_POINT ( 'NONE',  ( 1.413402608508182556, 1.946665536341249503, 1.039416302365432587 ) ) ;
#14799=CARTESIAN_POINT ( 'NONE',  ( 5.155110299917927463, 1.633153276354940342, -1.086568599608192409 ) ) ;
#14802=CARTESIAN_POINT ( 'NONE',  ( 0.1745949693968797123, 1.415412180343596837, -2.016327490378281073 ) ) ;
#14803=CARTESIAN_POINT ( 'NONE',  ( 4.435397664686764330, 0.7849604969769330420, -1.665558179074405620 ) ) ;
#14808=CARTESIAN_POINT ( 'NONE',  ( 5.133110336712339183, 1.960249873928998410, 0.8093987030339530042 ) ) ;
#14811=CARTESIAN_POINT ( 'NONE',  ( 6.925078400183531713, -0.004750840071900476122, 2.044148492825672569 ) ) ;
#14813=CARTESIAN_POINT ( 'NONE',  ( 0.9591554131188588794, 1.518337787816389284, 1.075887112759424280 ) ) ;
#14814=CARTESIAN_POINT ( 'NONE',  ( 3.737712173649463399, 1.832726675769575486, 0.1767833568970395008 ) ) ;
#14819=CARTESIAN_POINT ( 'NONE',  ( 3.668774463136436736, -1.482526648764719734, 1.634931011441637771 ) ) ;
#14820=CARTESIAN_POINT ( 'NONE',  ( 6.169232171785941965, 0.1756554044750150145, -2.255672955852848993 ) ) ;
#14822=CARTESIAN_POINT ( 'NONE',  ( 5.888875516108613262, -1.723027129771546484, -0.5597982944235294633 ) ) ;
#14823=CARTESIAN_POINT ( 'NONE',  ( 5.700375016119385130, 1.281441245451527600, -1.424251128553160273 ) ) ;
#14826=CARTESIAN_POINT ( 'NONE',  ( 6.368025811218641863, 0.9635043244729593059, 1.603280169136585220 ) ) ;
#14827=CARTESIAN_POINT ( 'NONE',  ( 5.635155393647417910, -0.04589315835645593061, -1.860648885492953486 ) ) ;
#14829=CARTESIAN_POINT ( 'NONE',  ( 6.420749384593221087, 1.653102913324438816, 0.6326092773807339142 ) ) ;
#14830=CARTESIAN_POINT ( 'NONE',  ( 1.358611653602972646, -1.916354379050893009, -0.6279873632355145174 ) ) ;
#14832=CARTESIAN_POINT ( 'NONE',  ( 2.367922061077184726, 2.065251240347278472, -0.4117205849265455075 ) ) ;
#14837=CARTESIAN_POINT ( 'NONE',  ( 2.531515522815621200, -0.1936091499190935594, 2.010454966646264552 ) ) ;
#14840=CARTESIAN_POINT ( 'NONE',  ( 3.005316911853897821, 1.824354345256746557, 1.159134172154026032 ) ) ;
#14841=CARTESIAN_POINT ( 'NONE',  ( 6.610000000000010090, 4.687934210475516394, 2.842562027763709587 ) ) ;
#14848=CARTESIAN_POINT ( 'NONE',  ( 1.417800074541092137, -1.221294057239637576, -1.819523406426680090 ) ) ;
#14850=CARTESIAN_POINT ( 'NONE',  ( 2.219920553356643289, -2.194584817558010936, 0.5498286310916412623 ) ) ;
#14857=CARTESIAN_POINT ( 'NONE',  ( 3.532247091833766284, 1.725908789131404220, 0.3905704408769093416 ) ) ;
#14859=CARTESIAN_POINT ( 'NONE',  ( 6.194375513154499302, -2.195555142843173879, -0.2223249613259313806 ) ) ;
#14864=CARTESIAN_POINT ( 'NONE',  ( 5.607046053289695742, -0.04666138757647776691, 2.016035322322209389 ) ) ;
#14866=CARTESIAN_POINT ( 'NONE',  ( 3.766346201128992988, -1.256895078192099335, 1.385637336983977397 ) ) ;
#14867=CARTESIAN_POINT ( 'NONE',  ( 3.186448005867897670, 1.153939711166888982, -1.718631068965512210 ) ) ;
#14872=CARTESIAN_POINT ( 'NONE',  ( 1.845825534506392085, -1.251752223804462272, -1.445855903880132631 ) ) ;
#14873=CARTESIAN_POINT ( 'NONE',  ( 3.174217076811707727, -0.9646401420641316227, -1.708233030250068785 ) ) ;
#14874=CARTESIAN_POINT ( 'NONE',  ( 1.440779594245532369, 1.198675164295496920, 1.620935466883965503 ) ) ;
#14878=CARTESIAN_POINT ( 'NONE',  ( 6.186792457355818620, -0.2869052490914354991, -1.950236548312431317 ) ) ;
#14880=CARTESIAN_POINT ( 'NONE',  ( 1.845949328209312901, -1.318067166357287379, -1.521789114188701664 ) ) ;
#14882=CARTESIAN_POINT ( 'NONE',  ( 2.583745723679788497, -0.6611301898758483730, 2.011445711247431323 ) ) ;
#14884=CARTESIAN_POINT ( 'NONE',  ( 4.070807014193541740, 1.466255041752505539, -1.461937513464212079 ) ) ;
#14886=CARTESIAN_POINT ( 'NONE',  ( 5.525362607580523111, -1.325732906064909677, -1.616523167544873241 ) ) ;
#14888=CARTESIAN_POINT ( 'NONE',  ( 4.700122295916242088, -1.825221593135372578, -0.04401369772454033491 ) ) ;
#14891=CARTESIAN_POINT ( 'NONE',  ( 6.890000000000005898, 7.052460701731090076, 2.598152593539102551 ) ) ;
#14894=CARTESIAN_POINT ( 'NONE',  ( 6.821333372217227797, -0.1664864972488830919, 2.170661319153658564 ) ) ;
#14897=CARTESIAN_POINT ( 'NONE',  ( 4.986922676292999235, -1.801926769106906745, -0.6406197933803285949 ) ) ;
#14904=CARTESIAN_POINT ( 'NONE',  ( 0.4504185290156898502, -1.555054577268409899, -0.9855837367087336709 ) ) ;
#14907=CARTESIAN_POINT ( 'NONE',  ( 5.237510374101456812, -1.321932271818569093, -1.323673891312632245 ) ) ;
#14914=CARTESIAN_POINT ( 'NONE',  ( 1.727339394501678838, 0.1499709341525606032, -1.963822474445919175 ) ) ;
#14915=CARTESIAN_POINT ( 'NONE',  ( 2.021111450618333194, -1.799914642762674433, 0.9091633978678403949 ) ) ;
#14919=CARTESIAN_POINT ( 'NONE',  ( 2.519692321801832335, -1.262790281060278907, -1.790845962237663791 ) ) ;
#14928=CARTESIAN_POINT ( 'NONE',  ( 4.880324068823122197, -0.2306306682541107433, -1.826696389425507938 ) ) ;
#14929=CARTESIAN_POINT ( 'NONE',  ( 1.330727748098162078, 1.350296381755649922, -1.493239990923441951 ) ) ;
#14930=CARTESIAN_POINT ( 'NONE',  ( 3.620768967900461099, 0.5618574718093732878, -2.228542275653460969 ) ) ;
#14932=CARTESIAN_POINT ( 'NONE',  ( 2.201794467188260995, 0.7177229581568910222, -1.717183780122087056 ) ) ;
#14935=CARTESIAN_POINT ( 'NONE',  ( 5.660397963661894849, 1.910509065610028090, 0.08734628876111423523 ) ) ;
#14939=CARTESIAN_POINT ( 'NONE',  ( 4.669523271137602904, 1.205110262999141701, 1.708276167780866661 ) ) ;
#14940=CARTESIAN_POINT ( 'NONE',  ( 3.133525119713890472, -1.255248497922526463, -1.387151338369890574 ) ) ;
#14942=CARTESIAN_POINT ( 'NONE',  ( 5.653808312887880660, 0.7519890275384639722, 1.680886247995525773 ) ) ;
#14945=CARTESIAN_POINT ( 'NONE',  ( 4.828557952505812878, 1.651878126777156730, 0.4964739870837226454 ) ) ;
#14947=CARTESIAN_POINT ( 'NONE',  ( 0.8087042982808723135, 1.034539495461658465, -1.391586887084266921 ) ) ;
#14950=CARTESIAN_POINT ( 'NONE',  ( 4.329095027809041873, -2.023602029403932079, -0.7869089946421561343 ) ) ;
#14951=CARTESIAN_POINT ( 'NONE',  ( 3.316849939159485228, 1.650902842016691130, 0.7798126646740562995 ) ) ;
#14952=CARTESIAN_POINT ( 'NONE',  ( 0.8132426064601482318, -1.654215606812576400, -1.054277637385622857 ) ) ;
#14953=CARTESIAN_POINT ( 'NONE',  ( 5.841034576552271318, -1.817201478619561383, -1.086431860386444681 ) ) ;
#14954=CARTESIAN_POINT ( 'NONE',  ( 5.917577160708873407, -1.270305590232129633, -1.908037719346373784 ) ) ;
#14958=CARTESIAN_POINT ( 'NONE',  ( 1.612141420133822223, -0.7113448269009944314, 1.997755531611951962 ) ) ;
#14963=CARTESIAN_POINT ( 'NONE',  ( 6.121977192509519661, 2.140326789316211453, -0.3632143409003502077 ) ) ;
#14964=CARTESIAN_POINT ( 'NONE',  ( 6.983263157960333700, 2.949816178198962024, 2.606004571833001382 ) ) ;
#14966=CARTESIAN_POINT ( 'NONE',  ( 2.666879960053496479, 0.7507478997158049117, 2.090701262698462681 ) ) ;
#14968=CARTESIAN_POINT ( 'NONE',  ( -0.1219072497536327904, -0.5225375287686329084, -2.247936139081475382 ) ) ;
#14970=CARTESIAN_POINT ( 'NONE',  ( 5.260619331934998755, -0.6897241169346832734, -1.943984935097947675 ) ) ;
#14976=CARTESIAN_POINT ( 'NONE',  ( 0.2331563151865486128, 1.372759770070256291, -2.202161770551560149 ) ) ;
#14977=CARTESIAN_POINT ( 'NONE',  ( 6.075717905342373548, -0.9791751913862613010, 1.559117742379905858 ) ) ;
#14980=CARTESIAN_POINT ( 'NONE',  ( 1.465380626080296400, 1.700101026837578466, -0.2896415544312477830 ) ) ;
#14981=CARTESIAN_POINT ( 'NONE',  ( -0.2409995289980038091, -0.004801160710915519658, -2.000252362011435636 ) ) ;
#14982=CARTESIAN_POINT ( 'NONE',  ( 2.004881263662112723, -2.228613174808518060, 0.5628491883087839431 ) ) ;
#14985=CARTESIAN_POINT ( 'NONE',  ( 2.407839351892237634, -0.4975810599385386834, 2.206854368276117917 ) ) ;
#14986=CARTESIAN_POINT ( 'NONE',  ( 4.529967234949650035, -1.295318019757265349, -1.660530462842347177 ) ) ;
#14988=CARTESIAN_POINT ( 'NONE',  ( 2.758786678070863196, -1.537680025927037786, -0.8759604286991302668 ) ) ;
#14994=CARTESIAN_POINT ( 'NONE',  ( 5.765950734523942245, 0.6451602502356535984, -2.125694943049365904 ) ) ;
#14995=CARTESIAN_POINT ( 'NONE',  ( 3.890727776643727598, 1.851661642969665067, -1.171806376371389957 ) ) ;
#14999=CARTESIAN_POINT ( 'NONE',  ( 6.428397668822618094, -0.9990526908794925554, -1.870407359624715937 ) ) ;
#15004=CARTESIAN_POINT ( 'NONE',  ( 6.047156637250688860, 0.2094617991648151656, 2.110256208591613003 ) ) ;
#15012=CARTESIAN_POINT ( 'NONE',  ( 5.864778394761136049, 0.1288883805774850844, -1.836796581567698539 ) ) ;
#15016=CARTESIAN_POINT ( 'NONE',  ( 2.524636229566870060, -1.623295675544262906, 0.6281775017502010394 ) ) ;
#15021=CARTESIAN_POINT ( 'NONE',  ( 6.209879897626497502, -2.145988306206991325, 0.2596296833028768347 ) ) ;
#15024=CARTESIAN_POINT ( 'NONE',  ( 5.946190753372003535, 2.158995856162956084, 0.1107517376499680406 ) ) ;
#15028=CARTESIAN_POINT ( 'NONE',  ( 5.782488548463037503, -1.922744423562244620, -0.4343835447332323740 ) ) ;
#15029=CARTESIAN_POINT ( 'NONE',  ( 4.921093860428086941, 0.6645110682935355673, 1.601655696547391594 ) ) ;
#15031=CARTESIAN_POINT ( 'NONE',  ( 2.366952063387484095, 0.1042156695447923470, -2.189191704635709890 ) ) ;
#15032=CARTESIAN_POINT ( 'NONE',  ( 3.153680125570026416, -1.885591857120081372, -1.329971080218894874 ) ) ;
#15033=CARTESIAN_POINT ( 'NONE',  ( 6.186805567823734364, -0.2977626877682394424, -2.039013576910824632 ) ) ;
#15034=CARTESIAN_POINT ( 'NONE',  ( 0.8494333778440340543, 1.939759575794866242, -0.09477157414044742878 ) ) ;
#15038=CARTESIAN_POINT ( 'NONE',  ( 3.463236921083117981, -1.731491641549892435, 1.224000437801611163 ) ) ;
#15040=CARTESIAN_POINT ( 'NONE',  ( 1.793592486599729252, 1.492254607734722072, -1.356300734917381678 ) ) ;
#15042=CARTESIAN_POINT ( 'NONE',  ( 5.087059579022827904, -0.2656672225294122169, -2.190654145894948890 ) ) ;
#15051=CARTESIAN_POINT ( 'NONE',  ( 4.645419472943275174, -1.591690889772362283, -1.309095959863779246 ) ) ;
#15056=CARTESIAN_POINT ( 'NONE',  ( 3.194014839594649491, 1.283080201803546538, 1.559715919771433867 ) ) ;
#15060=CARTESIAN_POINT ( 'NONE',  ( 3.379809591947144032, 1.306296513425331263, 1.594013207155994261 ) ) ;
#15063=CARTESIAN_POINT ( 'NONE',  ( 3.186732694495420848, 1.586669336078951664, -1.244385354607212335 ) ) ;
#15065=CARTESIAN_POINT ( 'NONE',  ( -0.1409997244346088141, 7.629137130509076492, -2.600278764091648487 ) ) ;
#15066=CARTESIAN_POINT ( 'NONE',  ( 1.552429278155377679, -1.578373273985161473, -0.9476568548090894550 ) ) ;
#15067=CARTESIAN_POINT ( 'NONE',  ( 6.428370569364434850, 1.274405893209800356, -1.801548588985131039 ) ) ;
#15069=CARTESIAN_POINT ( 'NONE',  ( 2.302237272444170202, -2.161155982280529297, 0.05054500047013688047 ) ) ;
#15071=CARTESIAN_POINT ( 'NONE',  ( 1.956267901341804283, -1.236798062192035363, 1.592663274815858676 ) ) ;
#15072=CARTESIAN_POINT ( 'NONE',  ( 2.460726772196987433, 1.776095029035225537, 1.458756201258274210 ) ) ;
#15078=CARTESIAN_POINT ( 'NONE',  ( 4.047701786889636111, 0.6652045265579300537, -1.855968581334372702 ) ) ;
#15079=CARTESIAN_POINT ( 'NONE',  ( 4.610564714392807240, 1.931124171932835809, 0.5807562064495259690 ) ) ;
#15083=CARTESIAN_POINT ( 'NONE',  ( 6.375619162920919791, 2.015872221316476143, -0.6097100970045774559 ) ) ;
#15085=CARTESIAN_POINT ( 'NONE',  ( 6.215297738502283842, -1.773692237561547147, -1.067698627785176768 ) ) ;
#15089=CARTESIAN_POINT ( 'NONE',  ( 5.853772736177474734, -1.465772220379698343, -1.389892856972896329 ) ) ;
#15091=CARTESIAN_POINT ( 'NONE',  ( 4.213705752388523962, -0.3967513169967327724, 2.273188601971836142 ) ) ;
#15093=CARTESIAN_POINT ( 'NONE',  ( 2.026308614600486280, 1.056755808076353276, 1.771133502622779243 ) ) ;
#15100=B_SPLINE_CURVE_WITH_KNOTS ( 'NONE', 3,
 ( #90352, #142331, #75166, #43753, #207284, #24249, #26399, #191024, #42691, #174823, #6927 ),
 .UNSPECIFIED., .F., .F.,
 ( 4, 1, 1, 1, 1, 1, 1, 1, 4 ),
 ( 0.000000000000000000, 0.2254101072112788262, 0.3970395454107691902, 0.5239558410346354389, 0.6152342776129972046, 0.6800502191696807808, 0.7279184599320936977, 0.7685697607527866015, 1.000000000000000000 ),
 .UNSPECIFIED. ) ;
#15102=CARTESIAN_POINT ( 'NONE',  ( 4.000555764329702946, 2.160365084594504381, 0.2165898760093481201 ) ) ;
#15105=CARTESIAN_POINT ( 'NONE',  ( 2.911469271472226339, -0.9098125248445630975, -1.600700954789348263 ) ) ;
#15107=CARTESIAN_POINT ( 'NONE',  ( 5.759372899636661991, 2.159370146098410714, -0.3733810082120898044 ) ) ;
#15109=CARTESIAN_POINT ( 'NONE',  ( 5.893528310750998145, 1.708867279757080748, 1.482922863094847443 ) ) ;
#15114=CARTESIAN_POINT ( 'NONE',  ( 6.186734212497608354, -0.2616995340462315300, -1.750118319643848119 ) ) ;
#15115=CARTESIAN_POINT ( 'NONE',  ( 4.635406539864527886, -0.09663638271006223801, 2.010879464324326626 ) ) ;
#15117=CARTESIAN_POINT ( 'NONE',  ( 3.100711275163593239, -0.6099987009138232441, -2.015686496682663087 ) ) ;
#15118=CARTESIAN_POINT ( 'NONE',  ( 2.091283074759576532, -0.4175699524238601357, 1.869371669076219211 ) ) ;
#15121=CARTESIAN_POINT ( 'NONE',  ( 2.699605434738296506, -1.457443026130700758, -1.324932107022150918 ) ) ;
#15122=CARTESIAN_POINT ( 'NONE',  ( 1.358040219746913024, 0.7549631825471068147, 1.711723683848711985 ) ) ;
#15123=CARTESIAN_POINT ( 'NONE',  ( 1.047228354049560828, 1.731870006261830630, -0.9216698261682305660 ) ) ;
#15124=CARTESIAN_POINT ( 'NONE',  ( 3.738627921261325149, 0.2550716744767547728, 1.705777993037333129 ) ) ;
#15125=CARTESIAN_POINT ( 'NONE',  ( -0.07025823700084612988, -1.875094440630159065, 0.3749275819610526916 ) ) ;
#15127=CARTESIAN_POINT ( 'NONE',  ( 0.8739773845415178544, 2.125910683164092152, -0.5920798734769525673 ) ) ;
#15133=CARTESIAN_POINT ( 'NONE',  ( 6.754741982670550371, -0.5462536098296209008, -1.996853278248729824 ) ) ;
#15134=CARTESIAN_POINT ( 'NONE',  ( 0.7485892145711986467, -2.054541080789675789, -0.2550698046258002005 ) ) ;
#15139=CARTESIAN_POINT ( 'NONE',  ( 5.320985837513584116, 1.605487267134264595, -1.385306402853322405 ) ) ;
#15146=CARTESIAN_POINT ( 'NONE',  ( 6.478960399985357554, 1.830089090633261417, 0.7073212282268787066 ) ) ;
#15148=CARTESIAN_POINT ( 'NONE',  ( 4.095077249698628741, 1.080899603560569799, -1.701687522498253946 ) ) ;
#15149=CARTESIAN_POINT ( 'NONE',  ( 3.731564767512856040, 0.6402975007456043199, -1.805710188498848456 ) ) ;
#15151=CARTESIAN_POINT ( 'NONE',  ( 1.083813775577105565, -0.9808430935620198188, 1.959877696171570927 ) ) ;
#15152=CARTESIAN_POINT ( 'NONE',  ( 0.1333692844072559003, 5.722267537706915874, -2.647605121726896105 ) ) ;
#15153=CARTESIAN_POINT ( 'NONE',  ( 2.723731132150861711, -1.073666234122659713, -1.531540996774889640 ) ) ;
#15157=CARTESIAN_POINT ( 'NONE',  ( 5.237957716521472129, 2.114759263080950635, -0.1049963987776857816 ) ) ;
#15159=CARTESIAN_POINT ( 'NONE',  ( 2.700817844316987237, 1.767710524334182853, 1.116111477495850934 ) ) ;
#15161=CARTESIAN_POINT ( 'NONE',  ( 0.8676543833149966689, 0.8442763457921966808, 1.503926039954103677 ) ) ;
#15169=ORIENTED_EDGE ( 'NONE', *, *, #122354, .F. ) ;
#15173=CARTESIAN_POINT ( 'NONE',  ( 1.558926746901686089, -1.530267751544078347, 0.9690644009569903128 ) ) ;
#15177=CARTESIAN_POINT ( 'NONE',  ( 6.639320575229263888, 6.039109382135522175, 2.391643382086404923 ) ) ;
#15181=CARTESIAN_POINT ( 'NONE',  ( 2.804952713220637328, -1.548975583508698683, 1.031263495014663523 ) ) ;
#15182=CARTESIAN_POINT ( 'NONE',  ( 0.4037314067151754893, -1.025472807287574506, -1.617813098647686632 ) ) ;
#15183=CARTESIAN_POINT ( 'NONE',  ( 6.510771785681003010, 1.426997308145862453, -1.294280627073117529 ) ) ;
#15190=CARTESIAN_POINT ( 'NONE',  ( 5.014487319174643964, 0.7500019944287477092, 1.821250405324719823 ) ) ;
#15191=CARTESIAN_POINT ( 'NONE',  ( 1.981254353800803836, -1.939921095825656305, -0.8566514584813912370 ) ) ;
#15195=CARTESIAN_POINT ( 'NONE',  ( 5.982419568921026887, -0.3181065885738461607, -2.168126298386578110 ) ) ;
#15197=CARTESIAN_POINT ( 'NONE',  ( 4.207974007929848881, -1.921269893987355593, 0.1410920886178046452 ) ) ;
#15199=CARTESIAN_POINT ( 'NONE',  ( 0.4459769555512117511, 1.820297760642339391, 0.1397589855641478973 ) ) ;
#15200=CARTESIAN_POINT ( 'NONE',  ( 1.524350002934187653, -1.228176919886795559, -1.833354347511229498 ) ) ;
#15206=CARTESIAN_POINT ( 'NONE',  ( 6.455907338579963017, -0.6669464233056993097, 1.853184144328771543 ) ) ;
#15207=CARTESIAN_POINT ( 'NONE',  ( 1.048265877425518688, -1.530107816300673829, 1.195853197770081255 ) ) ;
#15208=CARTESIAN_POINT ( 'NONE',  ( 6.837282040791485827, -1.423258038995322661, 1.805902563099166080 ) ) ;
#15210=CARTESIAN_POINT ( 'NONE',  ( 5.225394145299861570, 0.1845887361094991075, -1.851793659149820082 ) ) ;
#15217=CARTESIAN_POINT ( 'NONE',  ( 1.066276686178056377, -1.386418637449363889, 1.697306931840412370 ) ) ;
#15221=CARTESIAN_POINT ( 'NONE',  ( 2.174178736149934732, -1.123764393468742684, 1.438770255985911684 ) ) ;
#15224=CARTESIAN_POINT ( 'NONE',  ( 6.509000000000011887, 2.430396405248925529, 2.482145556523357222 ) ) ;
#15226=CARTESIAN_POINT ( 'NONE',  ( -0.02299388927988389730, 0.001624902753813092359, -1.910968047046639251 ) ) ;
#15227=CARTESIAN_POINT ( 'NONE',  ( 4.909014596843685574, -1.577992517845404619, 1.165349624694256736 ) ) ;
#15230=CARTESIAN_POINT ( 'NONE',  ( 3.667680160636753506, 1.218766932906123479, 1.821211977396507198 ) ) ;
#15234=CARTESIAN_POINT ( 'NONE',  ( 3.344645782512998267, -2.038826501179476391, -0.3585456059004287765 ) ) ;
#15238=CARTESIAN_POINT ( 'NONE',  ( 4.219567396149206395, 2.254377101126247229, 0.4485144814023647730 ) ) ;
#15242=CARTESIAN_POINT ( 'NONE',  ( 6.620655732516684822, 7.053712996964945248, 2.324417015927725760 ) ) ;
#15244=CARTESIAN_POINT ( 'NONE',  ( 3.415898659897542267, 1.231191954956109447, -1.501781470047100386 ) ) ;
#15248=CARTESIAN_POINT ( 'NONE',  ( 3.621269620730773298, 1.642686141288721480, 0.9789267784374030557 ) ) ;
#15250=CARTESIAN_POINT ( 'NONE',  ( 5.737229663476812291, -1.557457729854847983, 0.7413209835094927147 ) ) ;
#15251=CARTESIAN_POINT ( 'NONE',  ( 4.716029918043215474, 1.032482702726954527, -1.731993998903176957 ) ) ;
#15253=CARTESIAN_POINT ( 'NONE',  ( 4.782019082252658926, 1.911913310736196081, -1.275919496871528169 ) ) ;
#15254=CARTESIAN_POINT ( 'NONE',  ( 0.7860941533469123499, 1.484900681275106438, 1.632775826992872492 ) ) ;
#15257=CARTESIAN_POINT ( 'NONE',  ( 6.116413106003639300, 1.187136285548880066, -1.312641305385914947 ) ) ;
#15259=CARTESIAN_POINT ( 'NONE',  ( 1.430038810223871026, 1.126473215625309887, -1.996311628086711254 ) ) ;
#15260=CARTESIAN_POINT ( 'NONE',  ( 1.183123967286016986, -0.7853004192260810701, 1.553138493749019133 ) ) ;
#15262=CARTESIAN_POINT ( 'NONE',  ( 1.510678448032206189, 1.731588368038105896, 0.09119125932234918575 ) ) ;
#15265=CARTESIAN_POINT ( 'NONE',  ( 0.8190779338598102033, -1.572544420714114821, 1.497277704674306431 ) ) ;
#15266=CARTESIAN_POINT ( 'NONE',  ( 2.729704159269104924, 0.7212915320151757070, -1.883313052590728454 ) ) ;
#15268=CARTESIAN_POINT ( 'NONE',  ( 5.391212663409540973, 1.697947877755761947, -0.9101574019480199729 ) ) ;
#15270=CARTESIAN_POINT ( 'NONE',  ( 2.514199509032362112, -0.6922678517280489441, 2.110887004458279481 ) ) ;
#15277=CARTESIAN_POINT ( 'NONE',  ( 5.390116981161272136, -0.4305884537129686662, -1.686203596905116342 ) ) ;
#15278=CARTESIAN_POINT ( 'NONE',  ( 2.998438581075290266, 1.946722116546204306, 0.2428724957088539971 ) ) ;
#15283=CARTESIAN_POINT ( 'NONE',  ( 4.675235532476687439, 0.006304645973906687281, -2.262578822721802219 ) ) ;
#15284=CARTESIAN_POINT ( 'NONE',  ( 1.170463292146912915, -0.9257924050831314311, -1.843294045186917085 ) ) ;
#15287=CARTESIAN_POINT ( 'NONE',  ( 2.553932558351139193, 0.6037834209405189556, -2.180390065951258283 ) ) ;
#15290=CARTESIAN_POINT ( 'NONE',  ( 3.092876253348992410, 1.606159189733218140, -0.9584765265276545820 ) ) ;
#15291=CARTESIAN_POINT ( 'NONE',  ( 1.810757103121255707, 0.9981641815470091439, -1.417837687506792621 ) ) ;
#15292=CARTESIAN_POINT ( 'NONE',  ( 5.267185993530860699, 2.112242253262315739, -0.5839428218426812034 ) ) ;
#15293=CARTESIAN_POINT ( 'NONE',  ( 6.774459802350780713, -1.427793189328768753, 1.813748355473641549 ) ) ;
#15294=CARTESIAN_POINT ( 'NONE',  ( 3.907220446582274853, 1.852832235905249370, 1.113321777468062823 ) ) ;
#15295=CARTESIAN_POINT ( 'NONE',  ( 5.085854714555574141, -1.927481041573789744, -0.2360958376807794079 ) ) ;
#15297=CARTESIAN_POINT ( 'NONE',  ( 6.854772330626868637, -1.445518619047950981, 1.186913843143226233 ) ) ;
#15298=CARTESIAN_POINT ( 'NONE',  ( 0.6250000000000001110, -2.052068128417942283, 3.751950811937565850E-14 ) ) ;
#15301=CARTESIAN_POINT ( 'NONE',  ( 6.152970239395502361, 1.038990588714868490, 1.728003889287746286 ) ) ;
#15305=CARTESIAN_POINT ( 'NONE',  ( 3.562960707638890501, -1.610701098693729350, -0.8595150645765645692 ) ) ;
#15312=CARTESIAN_POINT ( 'NONE',  ( -0.07004771093476865051, -1.979950378243084730, 0.3982260095720979165 ) ) ;
#15313=CARTESIAN_POINT ( 'NONE',  ( 1.559403367407938390, -1.789607135292633266, 1.137164086494051096 ) ) ;
#15318=CARTESIAN_POINT ( 'NONE',  ( 6.332896556214961947, 0.1992470125839322093, 2.051223679500746133 ) ) ;
#15319=CARTESIAN_POINT ( 'NONE',  ( 6.522112240665402183, -1.799906897009293738, 0.9091900463213120620 ) ) ;
#15327=CARTESIAN_POINT ( 'NONE',  ( 5.554064478179312481, 1.779353385700060075, -0.9478964821433707444 ) ) ;
#15328=CARTESIAN_POINT ( 'NONE',  ( 5.244037021109955177, 0.5378974813256987009, 1.760811445753920346 ) ) ;
#15330=CARTESIAN_POINT ( 'NONE',  ( 3.018547437338540806, -1.137872740210974287, -2.007595131770247843 ) ) ;
#15333=CARTESIAN_POINT ( 'NONE',  ( 5.923154835166896781, -0.05960684409221649049, 2.160954015416292506 ) ) ;
#15335=CARTESIAN_POINT ( 'NONE',  ( 0.9427985035241670531, -1.531986193156938292, -1.193500027965375354 ) ) ;
#15338=CARTESIAN_POINT ( 'NONE',  ( 5.062018989497997445, 1.914771916633486448, -1.271085502950035417 ) ) ;
#15341=CARTESIAN_POINT ( 'NONE',  ( 3.362029495745801899, 0.8400119854848131506, 1.671504782411597612 ) ) ;
#15342=CARTESIAN_POINT ( 'NONE',  ( 1.582132296805271787, 0.9858968508435607125, 1.638552900098678045 ) ) ;
#15345=CARTESIAN_POINT ( 'NONE',  ( 2.842613246588860942, 2.190307313262893185, 0.2694104812042824038 ) ) ;
#15346=CARTESIAN_POINT ( 'NONE',  ( 6.983263157960361234, 3.701227967198342128, 2.360532479264612071 ) ) ;
#15351=CARTESIAN_POINT ( 'NONE',  ( 1.071480742727632940, 1.901078573484305201, -0.5215319001752088957 ) ) ;
#15352=CARTESIAN_POINT ( 'NONE',  ( 1.079649059555651824, -0.05968906897618533880, -2.306965765669062751 ) ) ;
#15353=CARTESIAN_POINT ( 'NONE',  ( 1.908577322519442454, 0.6123880975643315461, 1.863924812142327525 ) ) ;
#15355=CARTESIAN_POINT ( 'NONE',  ( 4.909062464502076395, -1.659793021533024548, 1.224303311577365161 ) ) ;
#15362=CARTESIAN_POINT ( 'NONE',  ( 0.7608744453060071189, -0.7297706024342350828, -2.044895412143563185 ) ) ;
#15364=CARTESIAN_POINT ( 'NONE',  ( 6.058133912487986272, -1.297239342979487509, 1.306937132449899508 ) ) ;
#15367=CARTESIAN_POINT ( 'NONE',  ( 0.8427765623921362748, -1.607460297381148928, 0.9563107477488577146 ) ) ;
#15368=CARTESIAN_POINT ( 'NONE',  ( 5.958325562381369345, 0.8699925256120243366, 1.978967057501494820 ) ) ;
#15370=CARTESIAN_POINT ( 'NONE',  ( 0.07755575628183573877, 5.720052600789671260, -2.782970829007725744 ) ) ;
#15372=CARTESIAN_POINT ( 'NONE',  ( 2.561071438676546741, -1.588783617390630898, 1.063917234122884858 ) ) ;
#15373=CARTESIAN_POINT ( 'NONE',  ( 2.553260254243350680, 0.4745879851475919842, -1.704939281604215706 ) ) ;
#15374=CARTESIAN_POINT ( 'NONE',  ( 0.3988866192712777758, -0.2342882197893907670, -1.897819253221716851 ) ) ;
#15376=CARTESIAN_POINT ( 'NONE',  ( 5.923430108280006934, -1.391030039757386039, -1.317302766908773126 ) ) ;
#15377=CARTESIAN_POINT ( 'NONE',  ( 6.285607346219458158, -1.855037422363578381, 0.6622139934589140742 ) ) ;
#15379=CARTESIAN_POINT ( 'NONE',  ( 1.160570123509139906, 2.118417766304943495, 0.09849428607798524360 ) ) ;
#15381=CARTESIAN_POINT ( 'NONE',  ( 5.489076674590072535, 1.649195787720953987, -0.8828566466120502110 ) ) ;
#15382=CARTESIAN_POINT ( 'NONE',  ( 0.6975366375942676500, -0.6598540886826111951, 1.702458561391326342 ) ) ;
#15384=CARTESIAN_POINT ( 'NONE',  ( 4.864015066594513215, 2.183220759563545776, -0.3215228633955333759 ) ) ;
#15387=CARTESIAN_POINT ( 'NONE',  ( 2.295447401932719345, -1.843475527790199964, 0.9254330757148797604 ) ) ;
#15394=CARTESIAN_POINT ( 'NONE',  ( 0.1753634416057740786, 1.334841368177059895, -2.397339160348281428 ) ) ;
#15396=CARTESIAN_POINT ( 'NONE',  ( 4.580570967453869713, 1.276285970795057345, -1.630082184409971324 ) ) ;
#15399=CARTESIAN_POINT ( 'NONE',  ( 1.511231465835579879, 1.905624552496063995, 1.020381674553122231 ) ) ;
#15401=CARTESIAN_POINT ( 'NONE',  ( 2.279949990775688384, 1.980252038983502993, -0.3961774098769352825 ) ) ;
#15404=EDGE_CURVE ( 'NONE', #8341, #21442, #182089, .T. ) ;
#15408=CARTESIAN_POINT ( 'NONE',  ( 0.6554828803995507158, 1.942095732595986890, -0.5424746339172461518 ) ) ;
#15409=CARTESIAN_POINT ( 'NONE',  ( 5.390230798962840630, -0.5317533105795355652, -2.125930911514521959 ) ) ;
#15412=CARTESIAN_POINT ( 'NONE',  ( 3.445477555875466891, -1.765175379189663607, 0.7362804355328658179 ) ) ;
#15416=CARTESIAN_POINT ( 'NONE',  ( 2.390250109419411295, -0.7743331304885041622, -1.862010821188607945 ) ) ;
#15418=CARTESIAN_POINT ( 'NONE',  ( 0.9609334056123096657, -2.075215392668391168, -0.9741618742916816620 ) ) ;
#15420=CARTESIAN_POINT ( 'NONE',  ( 4.313312247719586878, -0.2936513069345859650, 1.699412160066446909 ) ) ;
#15425=CARTESIAN_POINT ( 'NONE',  ( 0.07536363704230969462, 1.333366039338843789, -2.397125032416930424 ) ) ;
#15429=CARTESIAN_POINT ( 'NONE',  ( 5.250580378299275708, 1.785639943600283219, 0.3038008075236381389 ) ) ;
#15431=ORIENTED_EDGE ( 'NONE', *, *, #78162, .T. ) ;
#15433=PLANE ( 'NONE',  #194463 ) ;
#15434=CARTESIAN_POINT ( 'NONE',  ( 6.041655779063732190, -1.703243848673033023, 0.6171442250446981248 ) ) ;
#15437=CARTESIAN_POINT ( 'NONE',  ( 2.906388222866810978, 1.586772471669075424, -1.511725739355776366 ) ) ;
#15438=CARTESIAN_POINT ( 'NONE',  ( 5.793359732304666387, -1.682316520808274429, 0.7960761923023454978 ) ) ;
#15440=CARTESIAN_POINT ( 'NONE',  ( 4.218306492681688447, 1.879367783149912929, 0.3698934672397135581 ) ) ;
#15446=CARTESIAN_POINT ( 'NONE',  ( 0.2511322555047851290, -1.735185354305257110, 1.289038484408123963 ) ) ;
#15450=CARTESIAN_POINT ( 'NONE',  ( 0.3404811318320751234, 0.3065618842239411501, 1.799498403862239915 ) ) ;
#15452=CARTESIAN_POINT ( 'NONE',  ( 3.451995160207482094, 1.825762228170942914, 0.001041782061617091849 ) ) ;
#15454=CARTESIAN_POINT ( 'NONE',  ( 2.566550162062298579, 0.6480892470011965223, 1.799338185917313870 ) ) ;
#15456=CARTESIAN_POINT ( 'NONE',  ( 2.225000061332568890, -1.799552404990023113, -0.8009105870329900068 ) ) ;
#15458=CARTESIAN_POINT ( 'NONE',  ( 5.407742453289367646, -0.8769457196468108950, -1.732881886176732777 ) ) ;
#15462=CARTESIAN_POINT ( 'NONE',  ( 5.467072749063267345, -1.670387955228332277, 1.306269166133757986 ) ) ;
#15464=CARTESIAN_POINT ( 'NONE',  ( 3.369685512061989741, 0.4621021693036463374, -1.855490417808260961 ) ) ;
#15470=CARTESIAN_POINT ( 'NONE',  ( 3.879544890376307453, 0.2443292893146010170, -1.998135132051428231 ) ) ;
#15472=CARTESIAN_POINT ( 'NONE',  ( 5.373610676068619973, 1.758448663713826132, -0.4906839848310071139 ) ) ;
#15473=CARTESIAN_POINT ( 'NONE',  ( 0.2564123431100414074, -2.069877475643782994, -0.05227228806716639753 ) ) ;
#15477=CARTESIAN_POINT ( 'NONE',  ( 5.225416543158964977, -1.776039340814106637, 0.5876355328483380269 ) ) ;
#15486=CARTESIAN_POINT ( 'NONE',  ( 1.709917326824461181, 0.6048241955843024487, -1.979901091156407666 ) ) ;
#15487=CARTESIAN_POINT ( 'NONE',  ( 1.810321443220731075, 1.215999664948445913, -1.733040945678490319 ) ) ;
#15490=CARTESIAN_POINT ( 'NONE',  ( 6.965700764728601335, -0.4599482372066622249, 2.025938098699997525 ) ) ;
#15495=CARTESIAN_POINT ( 'NONE',  ( 2.133172796342793998, -2.046422403899459841, 1.032916798664377911 ) ) ;
#15497=CARTESIAN_POINT ( 'NONE',  ( 2.654443970922310214, 1.898414275235399407, 0.2300336082040748686 ) ) ;
#15500=CARTESIAN_POINT ( 'NONE',  ( 0.9846361663228007099, -1.273826410524713459, 1.558997777263083417 ) ) ;
#15501=CARTESIAN_POINT ( 'NONE',  ( 1.446067858876250112, -0.8869304882095051523, 1.749921244195346004 ) ) ;
#15505=CARTESIAN_POINT ( 'NONE',  ( 3.767594164193796669, 1.161519562870310329, 1.738068047407430816 ) ) ;
#15506=CARTESIAN_POINT ( 'NONE',  ( 2.254462534575492949, -1.370001101035130509, 1.120467526443365891 ) ) ;
#15510=CARTESIAN_POINT ( 'NONE',  ( 5.841781729209135854, 2.289337533263948288, 0.1180171966539828449 ) ) ;
#15511=CARTESIAN_POINT ( 'NONE',  ( 4.189205958701418986, -0.6631863921694808317, 1.609220651327713414 ) ) ;
#15515=CARTESIAN_POINT ( 'NONE',  ( 4.217908468276907463, -1.441162302510163640, -0.9635822893686758484 ) ) ;
#15516=CARTESIAN_POINT ( 'NONE',  ( 5.037629062015871462, 2.027634951229041693, -0.7768168075839574360 ) ) ;
#15518=CARTESIAN_POINT ( 'NONE',  ( 5.436732529336289588, -1.586671906620169104, 1.244382051841623538 ) ) ;
#15519=CARTESIAN_POINT ( 'NONE',  ( 6.750000000000005329, 2.348403055487757740, 2.372725748337465745 ) ) ;
#15521=CARTESIAN_POINT ( 'NONE',  ( 3.276308702328960099, -1.148522560162130501, 1.546420931960400758 ) ) ;
#15523=CARTESIAN_POINT ( 'NONE',  ( 5.326523995474015116, -0.9991460305027520805, -1.984133879135864920 ) ) ;
#15524=VERTEX_POINT ( 'NONE', #190175 ) ;
#15525=CARTESIAN_POINT ( 'NONE',  ( 6.983263157960402090, -0.0002233252893329463486, 1.845923184817334084 ) ) ;
#15529=CARTESIAN_POINT ( 'NONE',  ( 1.225557454335997054, 1.961257301181002388, 1.042886780478131215 ) ) ;
#15530=CARTESIAN_POINT ( 'NONE',  ( 6.777797683793751915, -1.903277019102869616, 0.4755351429900215310 ) ) ;
#15537=CARTESIAN_POINT ( 'NONE',  ( 4.861816908638716406, -0.5531579045409695805, 1.987044815706548562 ) ) ;
#15540=CARTESIAN_POINT ( 'NONE',  ( 5.764887228985436707, -1.690807747980655584, -0.8004016547063924625 ) ) ;
#15541=CARTESIAN_POINT ( 'NONE',  ( 5.063005163341266268, -0.9570555141230531193, 1.445894719807367723 ) ) ;
#15542=CARTESIAN_POINT ( 'NONE',  ( 4.282551955697760704, 1.552239185393188947, -0.7873791831930468943 ) ) ;
#15544=CARTESIAN_POINT ( 'NONE',  ( 2.261634143469380742, 2.247403939606710477, -0.4510662058269006569 ) ) ;
#15546=CARTESIAN_POINT ( 'NONE',  ( 0.8140990769837243013, 1.700254657383609036, 0.7068247239481675326 ) ) ;
#15548=CARTESIAN_POINT ( 'NONE',  ( 2.362075219488588562, 0.7782009281872975803, 1.651537983114875763 ) ) ;
#15549=CARTESIAN_POINT ( 'NONE',  ( 2.443982611291168450, -1.755769474653746665, -0.9913988478210812305 ) ) ;
#15550=CARTESIAN_POINT ( 'NONE',  ( 1.728746526384251858, 0.2170652002222578369, 2.180672313318913869 ) ) ;
#15553=CARTESIAN_POINT ( 'NONE',  ( 1.645070734656968625, -0.3017366986639741788, -2.048123538821471801 ) ) ;
#15556=CARTESIAN_POINT ( 'NONE',  ( 3.914780425095893968, -0.6665358524936615403, -2.013057630646164942 ) ) ;
#15558=CARTESIAN_POINT ( 'NONE',  ( 6.270122753791413928, 0.9430518052575274091, 1.563124558401955300 ) ) ;
#15565=CARTESIAN_POINT ( 'NONE',  ( 3.287372214357705325, 0.04529362468645367623, -2.019439401957975111 ) ) ;
#15566=CARTESIAN_POINT ( 'NONE',  ( 1.255059265495124476, -1.660252808076821296, 1.295518548220045529 ) ) ;
#15569=CARTESIAN_POINT ( 'NONE',  ( 5.278104476702146108, -0.9935453584285673934, -1.573305019461817444 ) ) ;
#15574=CARTESIAN_POINT ( 'NONE',  ( 6.174695665487812235, -1.956078286930991394, -0.6490473743868007128 ) ) ;
#15579=CARTESIAN_POINT ( 'NONE',  ( 3.321388563693925544, -1.314311947043474538, 1.130952296748084951 ) ) ;
#15580=CARTESIAN_POINT ( 'NONE',  ( 1.358879374581365429, 1.715036991836488056, -0.2946001921160408821 ) ) ;
#15581=CARTESIAN_POINT ( 'NONE',  ( 6.709642313893407817, -0.5169605766506181199, 2.257632290342121539 ) ) ;
#15584=CARTESIAN_POINT ( 'NONE',  ( 2.196623993872096392, -0.5467073567838857118, -1.986887711889900432 ) ) ;
#15586=CARTESIAN_POINT ( 'NONE',  ( 1.634138513624566302, 0.1511188354343559470, -2.010518437453466589 ) ) ;
#15587=CARTESIAN_POINT ( 'NONE',  ( 6.925078400183521943, 1.220207665023531174, 2.355644635573426182 ) ) ;
#15589=CARTESIAN_POINT ( 'NONE',  ( 0.6374961883623613268, -1.392493025731633027, -1.395827840033945000 ) ) ;
#15591=CARTESIAN_POINT ( 'NONE',  ( 5.027564050633359649, -0.2746679736120913318, 1.892429487827557599 ) ) ;
#15593=CARTESIAN_POINT ( 'NONE',  ( 6.164705905600972535, -1.563586322211576674, 1.557672334054376773 ) ) ;
#15598=CARTESIAN_POINT ( 'NONE',  ( 0.5924517288934522119, -1.120073279264972799, 1.680413856445305498 ) ) ;
#15600=CARTESIAN_POINT ( 'NONE',  ( 5.104635005266920267, -0.7716809915320420599, -2.174869537816104703 ) ) ;
#15601=CARTESIAN_POINT ( 'NONE',  ( 4.475024536774164119, 1.792854848340214025, 0.7970393728587571447 ) ) ;
#15603=CARTESIAN_POINT ( 'NONE',  ( 2.096468001391890823, 1.939661435718213811, 0.2929505381348077031 ) ) ;
#15607=CARTESIAN_POINT ( 'NONE',  ( -0.2056253921914633354, -0.9106808701126485328, -1.909331193683319050 ) ) ;
#15610=CARTESIAN_POINT ( 'NONE',  ( 1.253568445147245525, 0.7445567558202557112, 1.684058134371092752 ) ) ;
#15612=CARTESIAN_POINT ( 'NONE',  ( 3.731445244768144764, 0.05858319805804703545, -2.170454240781857003 ) ) ;
#15614=CARTESIAN_POINT ( 'NONE',  ( 1.951583061186522583, -1.892041120407188304, 0.9578705467366486204 ) ) ;
#15619=CARTESIAN_POINT ( 'NONE',  ( 2.530605077378933920, 1.998055600607269833, 0.5039824654343558752 ) ) ;
#15621=CARTESIAN_POINT ( 'NONE',  ( 0.3273695209934923689, 0.9472894719858866441, -1.578709817245539604 ) ) ;
#15623=CARTESIAN_POINT ( 'NONE',  ( -0.02264175331115596268, 2.007280006360371960, -2.503048469261221598 ) ) ;
#15626=CARTESIAN_POINT ( 'NONE',  ( 5.742805640131908973, 1.844151595126357179, 0.5056804652876015771 ) ) ;
#15627=B_SPLINE_CURVE_WITH_KNOTS ( 'NONE', 3,
 ( #87554, #71269, #30549, #96627, #162682, #80346, #212460, #130247, #56120, #190364 ),
 .UNSPECIFIED., .F., .F.,
 ( 4, 1, 1, 1, 1, 1, 1, 4 ),
 ( 0.000000000000000000, 0.09884949474608377418, 0.1930937302289311708, 0.2616037862002966730, 0.3630310524065313849, 0.5216543902990324888, 0.7338513509102306820, 0.9999999999999998890 ),
 .UNSPECIFIED. ) ;
#15630=CARTESIAN_POINT ( 'NONE',  ( 1.915646641569005659, -0.2780824042511415017, 2.245213254143724413 ) ) ;
#15632=CARTESIAN_POINT ( 'NONE',  ( 1.669862777068024995, 1.806593842016694484, -0.1355503349984941153 ) ) ;
#15633=CARTESIAN_POINT ( 'NONE',  ( 1.745192250125559008, 0.3234662751879986975, -1.888026716711376674 ) ) ;
#15634=CARTESIAN_POINT ( 'NONE',  ( 3.455589482447298355, 1.630370400113918095, 1.275915752658786095 ) ) ;
#15636=CARTESIAN_POINT ( 'NONE',  ( 1.551575459862795325, 0.5740822587161975576, -1.886020533208163430 ) ) ;
#15637=CARTESIAN_POINT ( 'NONE',  ( 5.233004834321499210, 0.1438781470856145273, 1.921186297865638215 ) ) ;
#15638=CARTESIAN_POINT ( 'NONE',  ( 1.700300771062040361, -0.7742048122164610913, 2.174079040713126076 ) ) ;
#15641=CARTESIAN_POINT ( 'NONE',  ( 5.037578369333176376, 1.925844591945893747, -0.7392275334625797445 ) ) ;
#15645=CARTESIAN_POINT ( 'NONE',  ( 6.528360061338796427, 1.215782546000489850, -1.719372923949607390 ) ) ;
#15648=CARTESIAN_POINT ( 'NONE',  ( 4.323607124742586016, -2.069909602744592014, 0.6229453038564189971 ) ) ;
#15649=CARTESIAN_POINT ( 'NONE',  ( 5.901037506996139825, -0.2983434833860042490, -1.997397228102874234 ) ) ;
#15658=CARTESIAN_POINT ( 'NONE',  ( 3.538296236868877731, 0.7303062672313584969, 1.879804216660937666 ) ) ;
#15663=CARTESIAN_POINT ( 'NONE',  ( 4.698204674003193304, -2.161138953124014161, -0.05634304724232848394 ) ) ;
#15668=CARTESIAN_POINT ( 'NONE',  ( 5.308220328704632784, 1.198845711980157214, -1.621194722098241003 ) ) ;
#15670=CARTESIAN_POINT ( 'NONE',  ( 0.9610595616070281011, 0.3405255003954327786, -1.690740162648683320 ) ) ;
#15675=CARTESIAN_POINT ( 'NONE',  ( 6.344977084850584426, -1.580176071495458023, 1.000667393836668362 ) ) ;
#15677=CARTESIAN_POINT ( 'NONE',  ( 0.9791529934419791470, -1.820790759202662423, -0.8588917989246074303 ) ) ;
#15679=CARTESIAN_POINT ( 'NONE',  ( 2.872332416675418276, 1.179501869419818494, 1.864919306664609921 ) ) ;
#15683=CARTESIAN_POINT ( 'NONE',  ( 2.508575005364023003, -2.114979441823850337, -0.1534387461676611220 ) ) ;
#15684=CARTESIAN_POINT ( 'NONE',  ( 1.985954055300429344, -2.015913623055834325, 0.05231662700833779323 ) ) ;
#15685=CARTESIAN_POINT ( 'NONE',  ( 2.742218629285391174, 1.002941080561991161, -1.508394886552874237 ) ) ;
#15692=CARTESIAN_POINT ( 'NONE',  ( -0.2236198635829286518, -0.4190533842500678841, -1.875677477222786438 ) ) ;
#15700=CARTESIAN_POINT ( 'NONE',  ( 5.331013795412237855, 0.1550192300789655642, 2.156197635354038411 ) ) ;
#15703=CARTESIAN_POINT ( 'NONE',  ( 1.476976393720277780, -1.495863523836362896, 1.503369785937097136 ) ) ;
#15705=CARTESIAN_POINT ( 'NONE',  ( 2.864479682042244679, -1.362014001507254379, 1.425398218059505728 ) ) ;
#15706=CARTESIAN_POINT ( 'NONE',  ( 5.783449990912790106, 0.1341079605299954347, -1.907733270042926810 ) ) ;
#15709=CARTESIAN_POINT ( 'NONE',  ( 0.5552397518338060278, 1.722184604005328357, -1.148819969904082861 ) ) ;
#15711=CARTESIAN_POINT ( 'NONE',  ( 1.271315641948435493, 1.156325127695263744, 1.560008962195078563 ) ) ;
#15716=CARTESIAN_POINT ( 'NONE',  ( 2.607466773009491146, -2.067780616408128935, 0.3074339443978144626 ) ) ;
#15720=CARTESIAN_POINT ( 'NONE',  ( 5.707647354773449422, 1.450964518888698596, 1.245719642194928811 ) ) ;
#15721=EDGE_LOOP ( 'NONE', ( #161453, #145540, #126899, #189962 ) ) ;
#15722=CARTESIAN_POINT ( 'NONE',  ( 4.740968412965463230, 0.3751893352213676591, 2.174603215771487630 ) ) ;
#15723=CARTESIAN_POINT ( 'NONE',  ( 1.571597221169357628, 0.1616201177277211132, -2.200922231076734903 ) ) ;
#15724=CARTESIAN_POINT ( 'NONE',  ( 0.5570965697654255422, -1.639946202723217450, 0.9833419947904218361 ) ) ;
#15727=CARTESIAN_POINT ( 'NONE',  ( 4.141125838365485201, -0.1998502692034490602, -2.060677327190631569 ) ) ;
#15730=CARTESIAN_POINT ( 'NONE',  ( 1.692469166403000491, -2.151312531270420436, -0.2117842694067117448 ) ) ;
#15731=CARTESIAN_POINT ( 'NONE',  ( 4.230150181147958044, 2.149441460308566754, 0.4267382380854707336 ) ) ;
#15738=CARTESIAN_POINT ( 'NONE',  ( 0.7213275451133926985, 1.987047012402185731, 0.3419330716275259530 ) ) ;
#15741=CARTESIAN_POINT ( 'NONE',  ( 4.821179601816666604, -1.846891146645711412, -0.9356023351853595127 ) ) ;
#15742=CARTESIAN_POINT ( 'NONE',  ( 5.501600788752927684, -2.065472302299308893, 0.4645820118519652930 ) ) ;
#15745=CARTESIAN_POINT ( 'NONE',  ( 4.223468175789964363, 0.2452432568937177593, -1.954070501097299850 ) ) ;
#15746=CARTESIAN_POINT ( 'NONE',  ( 5.806620824396801162, 2.019002025885249463, 1.085389930784508961 ) ) ;
#15747=CARTESIAN_POINT ( 'NONE',  ( 4.512205841073367196, -0.7830535718562798841, -1.649371741558727678 ) ) ;
#15754=CARTESIAN_POINT ( 'NONE',  ( 4.711194051470749322, 1.671412949727559383, -1.121937078508246755 ) ) ;
#15755=CARTESIAN_POINT ( 'NONE',  ( 6.293571109369822558, 1.706569967861866877, -1.540138442258129459 ) ) ;
#15756=CARTESIAN_POINT ( 'NONE',  ( 4.311346321947408633, -1.628642355029306987, -1.093319670275281652 ) ) ;
#15759=CARTESIAN_POINT ( 'NONE',  ( -0.1409997244346075651, 7.629137130509101361, -2.600278764091648487 ) ) ;
#15761=CARTESIAN_POINT ( 'NONE',  ( 0.7496951219271037470, 2.088183804393455301, -0.1063107438588738879 ) ) ;
#15762=CARTESIAN_POINT ( 'NONE',  ( 6.069200897874186040, 0.1259568369440123015, -1.765440829579780990 ) ) ;
#15764=CARTESIAN_POINT ( 'NONE',  ( 6.333930032320489900, 1.921166581771537318, 0.2825802787540276917 ) ) ;
#15765=CARTESIAN_POINT ( 'NONE',  ( 1.482659311839970684, -0.3241159351022730450, -2.167229700873399612 ) ) ;
#15766=CARTESIAN_POINT ( 'NONE',  ( 1.171013094284451439, 1.035884637911354877, 1.398405216058955514 ) ) ;
#15768=CARTESIAN_POINT ( 'NONE',  ( 0.1335669894368500255, -0.0009366757763962055587, -2.153671288142432250 ) ) ;
#15769=CARTESIAN_POINT ( 'NONE',  ( 1.242334483997083572, 0.3330332824765611099, 1.692230457194281223 ) ) ;
#15770=CARTESIAN_POINT ( 'NONE',  ( 1.716621854089026344, 2.046377219401524616, 0.7848826361863747714 ) ) ;
#15771=CARTESIAN_POINT ( 'NONE',  ( 4.582781371344160526, -2.140174514510746029, -0.5380331057033281850 ) ) ;
#15772=CARTESIAN_POINT ( 'NONE',  ( 0.9366657375849207767, -1.207674400081097721, 1.803990093267322736 ) ) ;
#15773=CARTESIAN_POINT ( 'NONE',  ( 0.3459771380207553593, 1.820543102168985961, 0.1377627428671979182 ) ) ;
#15774=CARTESIAN_POINT ( 'NONE',  ( 2.307945874296753797, -1.223308491024234224, -1.728006348806595316 ) ) ;
#15775=CARTESIAN_POINT ( 'NONE',  ( 6.639320575229254118, 2.070803455257670844, 2.204946390281757207 ) ) ;
#15777=CARTESIAN_POINT ( 'NONE',  ( 2.490095330609965796, -2.286454923436448183, -0.1652806634409968445 ) ) ;
#15781=CARTESIAN_POINT ( 'NONE',  ( 5.250715360749964589, 2.188191852258320136, 0.3812115871067219275 ) ) ;
#15789=CARTESIAN_POINT ( 'NONE',  ( 3.375625116643202972, -0.3961014713874110305, -1.976955985980306307 ) ) ;
#15791=CARTESIAN_POINT ( 'NONE',  ( 1.446217529737943153, -0.9311174319141333200, 1.840543939966767351 ) ) ;
#15796=CARTESIAN_POINT ( 'NONE',  ( 4.031328258368102269, -1.510625130563835627, -1.587819133214096734 ) ) ;
#15797=CARTESIAN_POINT ( 'NONE',  ( 1.934220422044398813, -1.621183349045727473, -1.198859219795316955 ) ) ;
#15798=CARTESIAN_POINT ( 'NONE',  ( 1.118424870118275738, -0.04499623084481922664, 1.840855209834332928 ) ) ;
#15801=CARTESIAN_POINT ( 'NONE',  ( 4.823181420811452291, -0.08861582515604787824, 1.823562061424352621 ) ) ;
#15802=CARTESIAN_POINT ( 'NONE',  ( 5.942029771888944545, -1.730864577151491890, -1.034168155301495862 ) ) ;
#15804=CARTESIAN_POINT ( 'NONE',  ( 4.469752058069711431, 2.195618827641317772, -0.5456854893412068641 ) ) ;
#15806=CARTESIAN_POINT ( 'NONE',  ( 1.295691649255722888, 1.595764685746006384, 1.374534258749359861 ) ) ;
#15808=CARTESIAN_POINT ( 'NONE',  ( 4.492674960910642667, 2.029786422369950216, 0.4070406814440513665 ) ) ;
#15817=CARTESIAN_POINT ( 'NONE',  ( 1.494549364340029163, -1.129948290531690658, 1.794289463044356436 ) ) ;
#15818=CARTESIAN_POINT ( 'NONE',  ( 2.197798511016679335, 2.028856164703813025, -0.9050913924920337417 ) ) ;
#15822=CARTESIAN_POINT ( 'NONE',  ( 2.945700582358207864, 1.385421296276163838, 1.389331660621349274 ) ) ;
#15828=CARTESIAN_POINT ( 'NONE',  ( 2.180079139336263516, 2.078761533942363737, -0.4183221158333137457 ) ) ;
#15830=CARTESIAN_POINT ( 'NONE',  ( 5.916451087343006954, 0.7937011933104149985, 1.794315766958521241 ) ) ;
#15831=CARTESIAN_POINT ( 'NONE',  ( 3.467792127863758456, 2.109446376165153847, -0.4717452660116944196 ) ) ;
#15832=CARTESIAN_POINT ( 'NONE',  ( 2.489598673502769977, -1.836455140896048999, -0.1334285330320400531 ) ) ;
#15835=CARTESIAN_POINT ( 'NONE',  ( 4.734162553523208139, 0.3016713478377709423, 1.713805963711847680 ) ) ;
#15836=CARTESIAN_POINT ( 'NONE',  ( 6.727182134110202050, 7.629137130509070275, 2.410944104600750038 ) ) ;
#15839=CARTESIAN_POINT ( 'NONE',  ( 1.569428280142046717, 0.1587979871724466974, -2.155937297210829495 ) ) ;
#15841=CARTESIAN_POINT ( 'NONE',  ( 4.429064430395744267, 0.9478954142983322395, 1.779353956671766657 ) ) ;
#15843=CARTESIAN_POINT ( 'NONE',  ( 1.112450467520700537, -0.9725818059473789745, -1.930612204972524282 ) ) ;
#15844=CARTESIAN_POINT ( 'NONE',  ( 2.337131052746133975, -1.762546391092616238, 0.8830908230641126844 ) ) ;
#15845=CIRCLE ( 'NONE', #105895, 0.05000000000000056483 ) ;
#15847=CARTESIAN_POINT ( 'NONE',  ( 3.931145062177692218, -1.341491907185809795, -1.404491712913302104 ) ) ;
#15857=CARTESIAN_POINT ( 'NONE',  ( 1.659489206604364941, -1.893029981318217647, -1.133929415002648655 ) ) ;
#15860=CARTESIAN_POINT ( 'NONE',  ( 5.682460714699895554, 1.171467074228413674, -1.573401077569417605 ) ) ;
#15862=CARTESIAN_POINT ( 'NONE',  ( 3.819616621146375568, -1.462967937902563964, -1.530840818714680029 ) ) ;
#15864=CARTESIAN_POINT ( 'NONE',  ( 0.1745949693968874838, 0.2569705180060793404, -1.790672585839627740 ) ) ;
#15865=CARTESIAN_POINT ( 'NONE',  ( 4.470543924053159479, -0.002573283451708791025, -1.841320590191763973 ) ) ;
#15869=CARTESIAN_POINT ( 'NONE',  ( 5.273731010124149243, 0.4114677744767555878, -2.080124947408354963 ) ) ;
#15872=CARTESIAN_POINT ( 'NONE',  ( 6.919229409281150822, -0.1609914934341447335, 2.026046322553672674 ) ) ;
#15874=CARTESIAN_POINT ( 'NONE',  ( 0.3087543870234563115, -1.498283157731963966, 1.103738804280843366 ) ) ;
#15875=CARTESIAN_POINT ( 'NONE',  ( 3.825598141381767903, 0.9817388958630569595, -1.557492293685861284 ) ) ;
#15881=CARTESIAN_POINT ( 'NONE',  ( 3.563272299071856164, -1.946135509614330239, -1.040604674307284316 ) ) ;
#15882=CARTESIAN_POINT ( 'NONE',  ( 4.481858567196604248, 1.473221693029845181, 1.717120190082993103 ) ) ;
#15884=CARTESIAN_POINT ( 'NONE',  ( 4.869312882171149326, -1.534379415642408651, -0.9627496050425389251 ) ) ;
#15885=CARTESIAN_POINT ( 'NONE',  ( 5.717977451880697615, 0.9379096786080630688, -1.670315906950563534 ) ) ;
#15887=CARTESIAN_POINT ( 'NONE',  ( 6.086763352761943580, -0.2763008855245497331, -1.850001521387992565 ) ) ;
#15888=CARTESIAN_POINT ( 'NONE',  ( 6.408657378324259746, 0.5850815967071677504, 1.766781856238110127 ) ) ;
#15891=CARTESIAN_POINT ( 'NONE',  ( 6.209784286858486269, -1.755916252942066436, 0.2208807251847556830 ) ) ;
#15892=CARTESIAN_POINT ( 'NONE',  ( 1.059780186608853203, 1.205045252304644210, 1.616690996016925563 ) ) ;
#15894=CARTESIAN_POINT ( 'NONE',  ( 3.158910222468692908, -1.594458197781272846, 1.376041720736504992 ) ) ;
#15899=CARTESIAN_POINT ( 'NONE',  ( 2.179950100978587990, 1.979969115219997189, -0.3981650194792104025 ) ) ;
#15904=CARTESIAN_POINT ( 'NONE',  ( 3.286554482555790191, -2.129011082553730727, -0.3730605165198074835 ) ) ;
#15905=CARTESIAN_POINT ( 'NONE',  ( 6.890000000000014779, 6.038692643467888921, 2.314896014905319266 ) ) ;
#15913=CARTESIAN_POINT ( 'NONE',  ( 1.189316404147572337, 1.662717542896676504, 1.427817766309902314 ) ) ;
#15915=CARTESIAN_POINT ( 'NONE',  ( 1.587200854914575077, -0.3333832325802545404, -2.237697771577638051 ) ) ;
#15922=CARTESIAN_POINT ( 'NONE',  ( 3.672906134817868651, 0.04599029964666952880, -1.769319831623831663 ) ) ;
#15923=CARTESIAN_POINT ( 'NONE',  ( 0.1300960903409088820, -1.296115720595720333, -1.660425602283533308 ) ) ;
#15927=CARTESIAN_POINT ( 'NONE',  ( 5.396111305808362957, -0.9091601233324579923, -1.799916296964368279 ) ) ;
#15929=CARTESIAN_POINT ( 'NONE',  ( 2.904993682805886213, 1.579364189935757778, 1.002181356900035070 ) ) ;
#15930=CARTESIAN_POINT ( 'NONE',  ( 2.905202624773517872, -1.723727875341171556, 1.146311801414557241 ) ) ;
#15933=CARTESIAN_POINT ( 'NONE',  ( 1.933716311909071006, -1.854087253938462521, 0.4680378644332866545 ) ) ;
#15937=CARTESIAN_POINT ( 'NONE',  ( 0.9141475326900461162, -1.912571728325638931, 0.002704284578637640782 ) ) ;
#15938=CARTESIAN_POINT ( 'NONE',  ( 2.910546574502240968, 0.6583626327048962557, 1.848246418561696913 ) ) ;
#15939=CARTESIAN_POINT ( 'NONE',  ( 0.1751529202326657098, -0.8592662624449104447, -1.822031250676876768 ) ) ;
#15943=CARTESIAN_POINT ( 'NONE',  ( 0.4033012769992084245, -0.5052730135347226481, 1.800932346938296069 ) ) ;
#15945=CARTESIAN_POINT ( 'NONE',  ( 1.652591521987197831, 1.991881122867325660, 0.2913371046347946747 ) ) ;
#15948=CARTESIAN_POINT ( 'NONE',  ( 1.687271568794300070, 1.762372639767064042, 1.173053760763353104 ) ) ;
#15950=CARTESIAN_POINT ( 'NONE',  ( 3.578635096964689843, 1.315621898185691974, -1.598582974826658010 ) ) ;
#15952=CARTESIAN_POINT ( 'NONE',  ( 5.947236541613409422, 0.6080794538029854479, -2.000250932508009782 ) ) ;
#15954=CARTESIAN_POINT ( 'NONE',  ( 4.137589658204786858, -1.258905094989383189, -1.322318538811013688 ) ) ;
#15959=CARTESIAN_POINT ( 'NONE',  ( 5.297975422827020608, -0.7987165953184969247, 2.057335881587420534 ) ) ;
#15962=CARTESIAN_POINT ( 'NONE',  ( 5.303337639526568559, 1.684534858470821961, -0.9050978215178404618 ) ) ;
#15969=CARTESIAN_POINT ( 'NONE',  ( 0.2043192855987647494, 1.601443664334546213, 0.9084302959305108338 ) ) ;
#15972=CARTESIAN_POINT ( 'NONE',  ( 4.780451015977909002, -1.813929833846049666, -0.4561423458772846939 ) ) ;
#15978=CARTESIAN_POINT ( 'NONE',  ( 1.674589265674136129, 1.326639880153294371, -1.455732889183375178 ) ) ;
#15979=CARTESIAN_POINT ( 'NONE',  ( 1.898064762488653079, -0.9530305783747442527, -1.777002450075705120 ) ) ;
#15983=CARTESIAN_POINT ( 'NONE',  ( 2.133021248740565756, -1.956732443736847182, 0.9868821405488172882 ) ) ;
#15986=CARTESIAN_POINT ( 'NONE',  ( 6.825078400183575589, 6.038285016609903799, 2.450557349082567171 ) ) ;
#15993=CARTESIAN_POINT ( 'NONE',  ( 5.144037045698616417, 0.5398437887287730330, 1.760322748975438500 ) ) ;
#15994=CARTESIAN_POINT ( 'NONE',  ( 1.576815760046655912, -1.422047136828644476, 1.425140908648862448 ) ) ;
#15995=CARTESIAN_POINT ( 'NONE',  ( 3.655889646864494580, -0.4445778678274399098, -2.254845314064676032 ) ) ;
#15997=CARTESIAN_POINT ( 'NONE',  ( 0.5669689972240202769, 1.615300940711749789, 0.9240007631576854230 ) ) ;
#16000=CARTESIAN_POINT ( 'NONE',  ( 5.273660385517703553, 0.3669835118517566497, -1.876681294024808988 ) ) ;
#16003=CARTESIAN_POINT ( 'NONE',  ( 4.177344015168626079, 1.367166224251268547, 1.581858325755406858 ) ) ;
#16004=CARTESIAN_POINT ( 'NONE',  ( 2.641296366799699147, -1.384790685969448099, -1.257831364775918503 ) ) ;
#16006=CARTESIAN_POINT ( 'NONE',  ( 5.952668924537682038, -1.582617586749142102, -0.9407850039931386910 ) ) ;
#16010=CARTESIAN_POINT ( 'NONE',  ( 5.461458274417386072, 0.3306134467882023142, -1.692711794494299538 ) ) ;
#16012=CARTESIAN_POINT ( 'NONE',  ( 0.8614527929159084829, -0.04078779759817893064, -1.733857029152048757 ) ) ;
#16016=CARTESIAN_POINT ( 'NONE',  ( 4.663029205760478746, 1.682383395889605282, -1.372325453836314768 ) ) ;
#16017=CARTESIAN_POINT ( 'NONE',  ( 3.070728972534173096, -1.687097908962056803, -0.6982200720766564839 ) ) ;
#16018=CARTESIAN_POINT ( 'NONE',  ( 0.6374591745182572877, 1.832550977151351290, -0.7006947966294306829 ) ) ;
#16019=CARTESIAN_POINT ( 'NONE',  ( 6.034383107294147841, 0.6662506799693500570, 2.009816206752083723 ) ) ;
#16020=CARTESIAN_POINT ( 'NONE',  ( 5.776963781812925802, 2.119385065811297597, -0.8740618393795733798 ) ) ;
#16026=CARTESIAN_POINT ( 'NONE',  ( 1.524255003590764046, -2.104078925693805502, 0.2628582283784736684 ) ) ;
#16030=CARTESIAN_POINT ( 'NONE',  ( 5.998927374810688384, 0.4157333352466702769, 2.130747042934706403 ) ) ;
#16031=CARTESIAN_POINT ( 'NONE',  ( 6.883263157960363365, 3.690127339433949327, 2.567897385111846731 ) ) ;
#16034=CARTESIAN_POINT ( 'NONE',  ( 1.893536009595264469, -0.1129285828431712546, -2.218558826778730619 ) ) ;
#16036=CARTESIAN_POINT ( 'NONE',  ( 5.801407773674092105, 1.352156682446105984, -1.496049708713815374 ) ) ;
#16038=CARTESIAN_POINT ( 'NONE',  ( 6.069198595068595381, 1.816300881853601723, 0.9774375683993684616 ) ) ;
#16040=CARTESIAN_POINT ( 'NONE',  ( -0.2409995289980003397, 0.7158067089181943121, -2.082568332340509087 ) ) ;
#16043=CARTESIAN_POINT ( 'NONE',  ( 0.1331565106231571705, 2.881392620029461504, -2.434650611646618223 ) ) ;
#16044=CARTESIAN_POINT ( 'NONE',  ( 4.915489835137424102, -0.9894786724786635013, -1.552603174752004600 ) ) ;
#16047=CARTESIAN_POINT ( 'NONE',  ( 2.080655396751258213, -0.08067463971387846267, -1.723007254337567407 ) ) ;
#16048=CARTESIAN_POINT ( 'NONE',  ( 0.005092704479254389627, -0.09411098085002241043, 2.014433268766747887 ) ) ;
#16049=CARTESIAN_POINT ( 'NONE',  ( 2.391599454647721945, -0.8833308501894185927, -2.122370812339502422 ) ) ;
#16051=CARTESIAN_POINT ( 'NONE',  ( 1.300488321244117618, -2.262578820359177012, 9.798025588786393801E-05 ) ) ;
#16052=CARTESIAN_POINT ( 'NONE',  ( 3.862027066150780730, 2.090197335813360979, -0.2575193119012611498 ) ) ;
#16054=CARTESIAN_POINT ( 'NONE',  ( 2.002845679596281681, 1.468101958376843985, 0.9879206967360052438 ) ) ;
#16060=CARTESIAN_POINT ( 'NONE',  ( 4.834350099735578610, -1.189287197132185669, -1.876079791293260079 ) ) ;
#16061=CARTESIAN_POINT ( 'NONE',  ( 3.837968455498752096, 2.180838135830205804, 0.2153102754597763235 ) ) ;
#16066=CARTESIAN_POINT ( 'NONE',  ( 6.890000000000025437, 1.315307137738566556, 1.839292676857922304 ) ) ;
#16068=CARTESIAN_POINT ( 'NONE',  ( 5.906510592826289319, -2.110524776404258507, -0.2060971850248518311 ) ) ;
#16078=CARTESIAN_POINT ( 'NONE',  ( 1.522608870468153741, -1.638875412371978646, 0.5861679430564836757 ) ) ;
#16083=CARTESIAN_POINT ( 'NONE',  ( 6.385629968321593353, 1.486944277142748572, 1.569300510047972219 ) ) ;
#16086=CARTESIAN_POINT ( 'NONE',  ( 6.209879897626497502, -2.145988306206991325, 0.2596296833028768347 ) ) ;
#16090=CARTESIAN_POINT ( 'NONE',  ( 5.571542166969843279, 1.900665388187183114, -0.5230325980125193341 ) ) ;
#16091=CARTESIAN_POINT ( 'NONE',  ( 4.885968428070557756, -0.08385511083567295798, 1.731956597358391470 ) ) ;
#16093=CARTESIAN_POINT ( 'NONE',  ( 2.226364491882920404, 2.126620374013419301, 0.5291077681483095096 ) ) ;
#16094=CARTESIAN_POINT ( 'NONE',  ( 3.188805362043587888, -2.273175341261697291, -0.3962186847288259317 ) ) ;
#16095=CARTESIAN_POINT ( 'NONE',  ( 4.446593522994434444, 0.5459629501111874506, 1.987092823586662504 ) ) ;
#16096=CARTESIAN_POINT ( 'NONE',  ( 0.2693405865131668353, 1.117251289913205881, 1.588187351064213715 ) ) ;
#16101=CARTESIAN_POINT ( 'NONE',  ( 3.639029512587122372, 2.014767915268770082, 0.6618469929612482705 ) ) ;
#16103=CARTESIAN_POINT ( 'NONE',  ( 0.8443752267504719411, 0.3905955241953715795, -1.978051186352240309 ) ) ;
#16105=CARTESIAN_POINT ( 'NONE',  ( 4.946401613871811875, 2.200551846729232430, 0.1665617540023768828 ) ) ;
#16114=CARTESIAN_POINT ( 'NONE',  ( 4.012614562483146408, 1.458688259485216854, -1.456115939812257620 ) ) ;
#16118=CARTESIAN_POINT ( 'NONE',  ( 3.668621814757520916, 0.7290426041848938610, 1.883679974206926122 ) ) ;
#16122=CARTESIAN_POINT ( 'NONE',  ( 2.852473085487742477, 0.6931051061056427987, 1.940986274177344706 ) ) ;
#16125=CARTESIAN_POINT ( 'NONE',  ( -0.2409995289980003397, 2.873648158547074338, -2.488896373646624749 ) ) ;
#16126=CARTESIAN_POINT ( 'NONE',  ( 1.640310086786896049, -1.556016536173940645, 0.9838780322720328542 ) ) ;
#16127=CARTESIAN_POINT ( 'NONE',  ( 6.721333373144884327, -0.1645177889858795151, 2.170883633896856679 ) ) ;
#16129=CARTESIAN_POINT ( 'NONE',  ( 0.9136071317731933039, -0.3180670004044767740, 2.137961049616762921 ) ) ;
#16131=CARTESIAN_POINT ( 'NONE',  ( 2.237517880698642880, 0.5331670712399002587, -1.944730990508992008 ) ) ;
#16134=CARTESIAN_POINT ( 'NONE',  ( 0.3560485870845608858, 0.7116971694140910021, 1.730184004908103867 ) ) ;
#16135=CARTESIAN_POINT ( 'NONE',  ( 4.768415704089838947, -1.288333767974993327, 1.492341041399107393 ) ) ;
#16137=CARTESIAN_POINT ( 'NONE',  ( 4.452361426671761713, -1.313546101436880109, 1.530156479064001207 ) ) ;
#16141=CARTESIAN_POINT ( 'NONE',  ( 6.041652760897754604, -1.524265013729691143, -1.453574456173498231 ) ) ;
#16142=CARTESIAN_POINT ( 'NONE',  ( 5.353992430378140099, -0.7485205528568983357, 1.930488744064068785 ) ) ;
#16145=CARTESIAN_POINT ( 'NONE',  ( 6.539320575229258026, 7.052651068779801413, 2.601414540040230428 ) ) ;
#16146=CARTESIAN_POINT ( 'NONE',  ( 5.642833896779382741, 1.947644361699039983, 0.5348221497712030148 ) ) ;
#16148=CARTESIAN_POINT ( 'NONE',  ( 2.860362167425280600, 2.296499369387979606, -0.2270692390979132391 ) ) ;
#16149=CARTESIAN_POINT ( 'NONE',  ( 1.498963261266316183, 0.3983865470186908064, 2.023570823014529729 ) ) ;
#16156=CARTESIAN_POINT ( 'NONE',  ( 4.580651514471745678, 1.339088007528920210, -1.708959110978137019 ) ) ;
#16159=CARTESIAN_POINT ( 'NONE',  ( 2.806014743833367131, 1.331929863061011465, -1.271513748034671654 ) ) ;
#16162=CARTESIAN_POINT ( 'NONE',  ( 4.493798347139664529, -2.191065130646638437, -0.05333993539427539510 ) ) ;
#16164=CARTESIAN_POINT ( 'NONE',  ( 6.315309700038255869, -0.2845791475536703086, 2.244501093609466924 ) ) ;
#16169=CARTESIAN_POINT ( 'NONE',  ( 6.468005306911782881, 0.9119784028226736172, 1.516475106587056532 ) ) ;
#16171=CARTESIAN_POINT ( 'NONE',  ( 4.688143804000614701, 1.160868117455503556, 1.644480612105477579 ) ) ;
#16173=CARTESIAN_POINT ( 'NONE',  ( 2.731583703245387351, -1.965451047913500116, 0.7568412939000405126 ) ) ;
#16174=CARTESIAN_POINT ( 'NONE',  ( 1.950665421479770067, -1.752291233380006474, -0.7743663792006536539 ) ) ;
#16176=CARTESIAN_POINT ( 'NONE',  ( 3.262113425008953183, -1.967426182293503079, 0.09390151542597660606 ) ) ;
#16177=CARTESIAN_POINT ( 'NONE',  ( 4.834242814930416188, -1.083969679716361156, -1.704088710659272810 ) ) ;
#16178=CARTESIAN_POINT ( 'NONE',  ( 0.1626889888870358680, -1.668787113083155305, -0.8454427722031019332 ) ) ;
#16179=CARTESIAN_POINT ( 'NONE',  ( 0.7132427667453158371, -1.655377960257615966, -1.052639099659122390 ) ) ;
#16180=CARTESIAN_POINT ( 'NONE',  ( 0.2637284958507991606, 0.5978344860198721022, -1.816641584731902626 ) ) ;
#16185=CARTESIAN_POINT ( 'NONE',  ( 5.893391625361732444, 1.417579469995243091, 1.220656814419220249 ) ) ;
#16188=CARTESIAN_POINT ( 'NONE',  ( 6.977413707831522593, -0.1558467299303326059, 2.036386162850227333 ) ) ;
#16191=CARTESIAN_POINT ( 'NONE',  ( 0.7837444799244470683, -1.966470238067185905, 0.6478734989143407619 ) ) ;
#16196=CARTESIAN_POINT ( 'NONE',  ( 5.795592431653455279, 1.959276243578732091, -0.8114611383256833399 ) ) ;
#16200=CARTESIAN_POINT ( 'NONE',  ( 5.986763597034562068, 1.890319730748804439, 0.5246630281777532323 ) ) ;
#16202=CARTESIAN_POINT ( 'NONE',  ( 4.850935385407137979, -0.9528642855485233154, 1.776740034556321568 ) ) ;
#16203=CARTESIAN_POINT ( 'NONE',  ( 3.590956263468424225, 1.645886154840708659, 0.9800325279442632098 ) ) ;
#16205=CARTESIAN_POINT ( 'NONE',  ( 1.259612756803454303, 2.158328104161820526, -0.3793702838810894540 ) ) ;
#16206=CARTESIAN_POINT ( 'NONE',  ( 0.2331713839410602396, 7.629137130509072939, -2.553349835631549603 ) ) ;
#16207=CARTESIAN_POINT ( 'NONE',  ( 3.497188413392815498, 1.472618687456558773, 1.153256759092120554 ) ) ;
#16211=CARTESIAN_POINT ( 'NONE',  ( 5.079753589751704546, -0.7609352437839884686, 1.975942822842210234 ) ) ;
#16213=CARTESIAN_POINT ( 'NONE',  ( 6.725056259267968350, -1.891221747171191403, -0.8428681758992571105 ) ) ;
#16214=CARTESIAN_POINT ( 'NONE',  ( 2.876600747729184615, -0.1562720264073799992, -2.084980456524800019 ) ) ;
#16216=CARTESIAN_POINT ( 'NONE',  ( 1.148929321228649991, -1.355925326379325391, -1.065857193176344309 ) ) ;
#16217=ORIENTED_EDGE ( 'NONE', *, *, #910, .T. ) ;
#16226=CARTESIAN_POINT ( 'NONE',  ( 1.805022944457121081, 1.575911691392884117, -0.8931387472532796856 ) ) ;
#16237=CARTESIAN_POINT ( 'NONE',  ( 3.385049140913086507, 0.04320281034062402326, 1.860716667189839635 ) ) ;
#16238=CARTESIAN_POINT ( 'NONE',  ( 0.03459428079104728826, -1.538086888106354522, 1.141608027856432450 ) ) ;
#16239=CARTESIAN_POINT ( 'NONE',  ( 6.247092716751994068, -1.627016005604764670, 1.031123616215999794 ) ) ;
#16244=CARTESIAN_POINT ( 'NONE',  ( 4.715651637508523564, 0.4355733895117944177, -1.920488317121961108 ) ) ;
#16245=CARTESIAN_POINT ( 'NONE',  ( 1.910938629679886480, -0.5684797485801665884, -2.042784538176869003 ) ) ;
#16250=CARTESIAN_POINT ( 'NONE',  ( 5.419949545929089396, 1.307550890958172785, -1.758484179531449421 ) ) ;
#16252=CARTESIAN_POINT ( 'NONE',  ( 4.243131921826915232, -1.676359970754065731, 0.9489593035170663660 ) ) ;
#16254=CARTESIAN_POINT ( 'NONE',  ( 0.4811275135914867551, 1.705355465787803171, -0.6520327999673739550 ) ) ;
#16255=CARTESIAN_POINT ( 'NONE',  ( 0.5224629442122545875, -1.184049029929446828, -1.862174541895258217 ) ) ;
#16260=CARTESIAN_POINT ( 'NONE',  ( 5.981301965652664698, -0.05197358493889753933, 1.968944643851434639 ) ) ;
#16261=CARTESIAN_POINT ( 'NONE',  ( 1.136160399770862250, 0.3804006922196729867, 1.904278901077125052 ) ) ;
#16263=CARTESIAN_POINT ( 'NONE',  ( 6.854781963242574605, -0.9897500569795645298, 2.071502949204959254 ) ) ;
#16265=CARTESIAN_POINT ( 'NONE',  ( 5.506657433377460720, 0.5384353192533465338, 1.781376027434707687 ) ) ;
#16270=CARTESIAN_POINT ( 'NONE',  ( 0.8904706703079521279, -0.5376514911656914419, -2.124458794526106864 ) ) ;
#16276=CARTESIAN_POINT ( 'NONE',  ( 2.103868193876055503, -1.825329726703457833, 0.04394198290156441783 ) ) ;
#16279=CARTESIAN_POINT ( 'NONE',  ( 6.509000000000014552, 2.959959533984284352, 2.552917358632576850 ) ) ;
#16280=CARTESIAN_POINT ( 'NONE',  ( 0.1331565106231598072, 7.629137130509052511, -2.545925718843544239 ) ) ;
#16281=CARTESIAN_POINT ( 'NONE',  ( 6.182242880246401562, -0.9723386526096773341, 1.545037271442825100 ) ) ;
#16282=CARTESIAN_POINT ( 'NONE',  ( 4.715648799723409113, 0.4337510919622395988, -1.913030730064477547 ) ) ;
#16285=EDGE_CURVE ( 'NONE', #95583, #60268, #124474, .T. ) ;
#16286=CARTESIAN_POINT ( 'NONE',  ( 4.406960118137589255, -0.4655763551070742912, -2.068578822641816473 ) ) ;
#16290=CARTESIAN_POINT ( 'NONE',  ( 2.553653463975919635, 1.597511423921485818, 1.316731848974454833 ) ) ;
#16294=CARTESIAN_POINT ( 'NONE',  ( 2.760663040853128525, 2.181856774409622890, -0.7236605881647265592 ) ) ;
#16298=CARTESIAN_POINT ( 'NONE',  ( 6.620655732516647518, 0.007553340620044743381, 1.826407896915738238 ) ) ;
#16303=CARTESIAN_POINT ( 'NONE',  ( 4.131050151015442928, 1.750605847248308145, 0.7702136748066327199 ) ) ;
#16305=CARTESIAN_POINT ( 'NONE',  ( 5.491107761985050573, 1.519353413045966494, -0.8162815091526542943 ) ) ;
#16306=CARTESIAN_POINT ( 'NONE',  ( 3.784388871581423786, -0.6371526190629381858, -1.913262240507591416 ) ) ;
#16307=CARTESIAN_POINT ( 'NONE',  ( 5.256544959696739738, 2.216068975266134000, -0.6104820095701003480 ) ) ;
#16309=CARTESIAN_POINT ( 'NONE',  ( 0.4345545588612038657, 1.130843733186673639, -1.894998796914903139 ) ) ;
#16311=CARTESIAN_POINT ( 'NONE',  ( 5.518734381310105519, 1.635532185772445857, 0.6765044976165290880 ) ) ;
#16313=CARTESIAN_POINT ( 'NONE',  ( 1.834309667284042433, 2.267783887084608097, 0.3333485250246841503 ) ) ;
#16314=CARTESIAN_POINT ( 'NONE',  ( 6.263598714517844890, 0.9507720431706818687, 1.576509192756641697 ) ) ;
#16320=CARTESIAN_POINT ( 'NONE',  ( 6.812946544903684121, -1.603000239855886466, 1.309962327488790157 ) ) ;
#16321=CARTESIAN_POINT ( 'NONE',  ( 2.167204200501818612, 1.841733140229084853, -0.8216742516050157263 ) ) ;
#16323=( BOUNDED_CURVE ( )  B_SPLINE_CURVE ( 3, ( #170962, #54020, #120159, #87589 ),
 .UNSPECIFIED., .F., .T. ) 
 B_SPLINE_CURVE_WITH_KNOTS ( ( 4, 4 ),
 ( 0.000000000000000000, 0.4999999999999995004 ),
 .UNSPECIFIED. ) 
 CURVE ( )  GEOMETRIC_REPRESENTATION_ITEM ( )  RATIONAL_B_SPLINE_CURVE ( ( 1.000000000000000000, 0.3333333333333340365, 0.3333333333333333703, 0.9999999999999993339 ) ) 
 REPRESENTATION_ITEM ( '' )  );
#16325=CARTESIAN_POINT ( 'NONE',  ( 5.813098442667213206, 1.700071987003290763, 0.9061822306820240813 ) ) ;
#16327=CARTESIAN_POINT ( 'NONE',  ( 2.373529451608622054, -1.935128245189758012, -1.090680762624636868 ) ) ;
#16335=CARTESIAN_POINT ( 'NONE',  ( 4.950617407298735451, -1.474004690277466834, -0.9251219707713809193 ) ) ;
#16337=CARTESIAN_POINT ( 'NONE',  ( 3.490630252122445931, 1.913478943654752129, 0.4322817992908412621 ) ) ;
#16341=CARTESIAN_POINT ( 'NONE',  ( 4.464347054923422320, 1.061364745222750372, 1.997979292561928633 ) ) ;
#16342=CARTESIAN_POINT ( 'NONE',  ( 1.381380011782725958, -0.05272402391268657396, 2.062171479924046036 ) ) ;
#16345=CARTESIAN_POINT ( 'NONE',  ( 2.026610535765199561, 1.302222112816675326, -1.850007447375429104 ) ) ;
#16349=CARTESIAN_POINT ( 'NONE',  ( 2.161206213664386144, 0.3243885794495802721, -1.842051381961368639 ) ) ;
#16350=CARTESIAN_POINT ( 'NONE',  ( 1.758077109659747395, 1.659224110165247179, -0.5040892880595440051 ) ) ;
#16351=CARTESIAN_POINT ( 'NONE',  ( 5.601184584505256581, -0.5335315006234629953, 2.125516261704554211 ) ) ;
#16352=CARTESIAN_POINT ( 'NONE',  ( 6.563506341781633502, 0.4036857245812221495, -2.271876217655709240 ) ) ;
#16353=CARTESIAN_POINT ( 'NONE',  ( 1.182575006203628210, -2.010449142642761089, -0.4523898644508434486 ) ) ;
#16354=CARTESIAN_POINT ( 'NONE',  ( 4.066302494797935374, -1.812431348068560988, -0.6977731361806001065 ) ) ;
#16359=CARTESIAN_POINT ( 'NONE',  ( 1.250000000000001110, 7.216295638291068821E-14, 2.052068128417951609 ) ) ;
#16361=CARTESIAN_POINT ( 'NONE',  ( 6.819686488043297246, -1.560180513003786462, 1.276622200526676743 ) ) ;
#16363=CARTESIAN_POINT ( 'NONE',  ( 5.063125043234593115, -1.117834493326537393, 1.678003986596336761 ) ) ;
#16367=CARTESIAN_POINT ( 'NONE',  ( 1.787459277025660542, 1.258035843444211155, 1.323286951131589895 ) ) ;
#16376=CARTESIAN_POINT ( 'NONE',  ( 6.516272353977101695, -2.019191618876531091, 0.05163682429563941356 ) ) ;
#16377=CARTESIAN_POINT ( 'NONE',  ( -0.04015575566676531788, -1.641981170221142872, -1.341450104213978589 ) ) ;
#16381=CARTESIAN_POINT ( 'NONE',  ( 0.08116279290028630133, -0.1557560750096824431, -2.127278773206460638 ) ) ;
#16382=CARTESIAN_POINT ( 'NONE',  ( 4.623672751230786027, 0.3474658942751901458, 1.986100912583692812 ) ) ;
#16391=CARTESIAN_POINT ( 'NONE',  ( 5.325545996062735377, -1.462220743079494012, 1.388274341532859335 ) ) ;
#16392=CARTESIAN_POINT ( 'NONE',  ( 4.470543924053159479, -0.002573283451708791025, -1.841320590191763973 ) ) ;
#16393=CARTESIAN_POINT ( 'NONE',  ( -0.02319159430947542733, 0.7471999394491578572, -1.895068635927643630 ) ) ;
#16394=CARTESIAN_POINT ( 'NONE',  ( 3.528207577792912719, -1.374008478127983546, -1.853924954965507466 ) ) ;
#16396=CARTESIAN_POINT ( 'NONE',  ( 5.887991582945824476, -0.9777203880148609416, 1.927937229880334113 ) ) ;
#16397=CARTESIAN_POINT ( 'NONE',  ( 3.432827581131673522, -1.645759781613131967, 1.164986487700324425 ) ) ;
#16399=CARTESIAN_POINT ( 'NONE',  ( 1.540467339043756434, -1.639628711884850265, 1.040515435762645380 ) ) ;
#16401=CARTESIAN_POINT ( 'NONE',  ( 4.868718825205943901, -0.6189299756741394321, 2.213421903294809034 ) ) ;
#16404=CARTESIAN_POINT ( 'NONE',  ( 3.748781033766034998, -1.529746656882627454, 1.076398355447941491 ) ) ;
#16405=CARTESIAN_POINT ( 'NONE',  ( 1.423922367354793606, -1.897583212610975734, 0.2371896777705190806 ) ) ;
#16408=CARTESIAN_POINT ( 'NONE',  ( 3.088704478669739295, -2.174299887604825177, -0.3769171259565203269 ) ) ;
#16414=CARTESIAN_POINT ( 'NONE',  ( 0.9660189047021714437, 0.9680410686894457273, 1.717217487461615955 ) ) ;
#16415=CARTESIAN_POINT ( 'NONE',  ( 0.09532371275382427178, -0.5158531520006398585, -2.257940698305866967 ) ) ;
#16416=CARTESIAN_POINT ( 'NONE',  ( 1.416376618315864144, 0.7919773292732554815, 1.795081228748253377 ) ) ;
#16417=CARTESIAN_POINT ( 'NONE',  ( 5.436407774000851845, -1.150348206634976833, 1.711801118168945202 ) ) ;
#16424=CARTESIAN_POINT ( 'NONE',  ( 1.077284259287077495, 2.005170101804130578, 0.8328141809181826005 ) ) ;
#16427=FACE_OUTER_BOUND ( 'NONE', #166921, .T. ) ;
#16431=CARTESIAN_POINT ( 'NONE',  ( 1.809613641711980359, -1.857008771552502768, 0.2239427725650791623 ) ) ;
#16432=CARTESIAN_POINT ( 'NONE',  ( 5.659502677682959337, 0.4278135246765999988, -2.118672983663777654 ) ) ;
#16436=CARTESIAN_POINT ( 'NONE',  ( 1.207504981961624813, 1.448612403150219885, 1.248453992567559512 ) ) ;
#16437=CARTESIAN_POINT ( 'NONE',  ( 2.887294646099856532, 1.250245360129684791, 1.252957939402859600 ) ) ;
#16438=CARTESIAN_POINT ( 'NONE',  ( 0.2934254677693093338, 1.784247535656303230, -0.6883866973072181317 ) ) ;
#16440=CARTESIAN_POINT ( 'NONE',  ( 5.114804650195723390, 0.1453347504645576271, 1.910168102697987313 ) ) ;
#16441=CARTESIAN_POINT ( 'NONE',  ( 6.408657466097477773, 0.6165391127177908270, 1.870651749748206916 ) ) ;
#16443=CARTESIAN_POINT ( 'NONE',  ( 0.9496594531581278309, -1.914679731917130479, 0.9119059213342151082 ) ) ;
#16445=CARTESIAN_POINT ( 'NONE',  ( 3.696050037196423332, -1.868490534004090931, -0.09263902202472777681 ) ) ;
#16446=CARTESIAN_POINT ( 'NONE',  ( 1.066719475142905216, -1.649486405746130258, -0.7827983987617056494 ) ) ;
#16447=CARTESIAN_POINT ( 'NONE',  ( 4.635508124736155366, -2.018492079602551392, 0.8926152185086615454 ) ) ;
#16450=EDGE_CURVE ( 'NONE', #21539, #150774, #121464, .T. ) ;
#16451=CARTESIAN_POINT ( 'NONE',  ( 1.697793086734213697, -1.492557772401803318, -1.423914585240863673 ) ) ;
#16459=CARTESIAN_POINT ( 'NONE',  ( 4.826661161267837841, -1.354893614093263254, 1.565527137264411728 ) ) ;
#16461=CARTESIAN_POINT ( 'NONE',  ( 0.9487563388480976245, 0.6265645459165304354, 2.068816658077163861 ) ) ;
#16463=CARTESIAN_POINT ( 'NONE',  ( 2.473312253293189489, -1.758384921082667862, -0.9933899200572825494 ) ) ;
#16470=CARTESIAN_POINT ( 'NONE',  ( -0.1882626618336727398, -1.244567986390752390, -1.587255334073833790 ) ) ;
#16471=CARTESIAN_POINT ( 'NONE',  ( 6.539320575229278454, 2.035006821797652687, 2.408631514295301645 ) ) ;
#16472=CARTESIAN_POINT ( 'NONE',  ( 5.407841436338867602, -0.9846607899807978681, -1.957994596084790206 ) ) ;
#16474=CARTESIAN_POINT ( 'NONE',  ( 3.480628297764537304, -1.280852673386581486, 1.420289963180096260 ) ) ;
#16478=CARTESIAN_POINT ( 'NONE',  ( 2.566029989117986077, -1.034146858587611906, 1.730878619409223163 ) ) ;
#16480=CARTESIAN_POINT ( 'NONE',  ( 0.2402843302407534631, 2.286812847775396840, 0.1605059593563825382 ) ) ;
#16482=CARTESIAN_POINT ( 'NONE',  ( 4.014446192991796281, 1.219382930577699309, -1.220076339321971570 ) ) ;
#16483=CARTESIAN_POINT ( 'NONE',  ( -0.1394461523061013564, 4.080274402048936544, -2.835111295649892060 ) ) ;
#16486=CARTESIAN_POINT ( 'NONE',  ( 0.6548940681232479077, -1.578012236938080015, -1.004313744925364071 ) ) ;
#16488=CARTESIAN_POINT ( 'NONE',  ( 0.07556134207193415664, 4.081186479400328082, -2.798928192855642649 ) ) ;
#16489=CARTESIAN_POINT ( 'NONE',  ( 0.3564121386029559524, -2.069725681613205026, -0.05427943458365809548 ) ) ;
#16491=CARTESIAN_POINT ( 'NONE',  ( 4.793523346383269157, 1.688353701584244915, -0.6568948891843768845 ) ) ;
#16494=CARTESIAN_POINT ( 'NONE',  ( -0.1104750535120269106, 7.629137130509076492, -2.703481013110929698 ) ) ;
#16495=CARTESIAN_POINT ( 'NONE',  ( 5.567019150587803722, -1.423986762948417972, 1.119560556780722083 ) ) ;
#16501=CARTESIAN_POINT ( 'NONE',  ( 6.777813018113469923, -1.804774468322063452, 0.4538611949938906043 ) ) ;
#16503=CARTESIAN_POINT ( 'NONE',  ( 3.796418445691573940, 1.352171417773648132, -1.357169225504866406 ) ) ;
#16508=CARTESIAN_POINT ( 'NONE',  ( 5.858642105998121963, -2.011370865819528397, -0.6617598028889163375 ) ) ;
#16509=CARTESIAN_POINT ( 'NONE',  ( 0.5148121308554790554, 1.489681748880047563, -1.566682057046256071 ) ) ;
#16512=CARTESIAN_POINT ( 'NONE',  ( 1.254616015376356586, -1.441780481750528420, 1.119729341354458452 ) ) ;
#16514=CARTESIAN_POINT ( 'NONE',  ( 3.522295995157863846, 1.158834602800838498, -1.410599190884161747 ) ) ;
#16516=CARTESIAN_POINT ( 'NONE',  ( 2.918110517850933672, -1.910018876965378309, 0.09814724848770939314 ) ) ;
#16518=CARTESIAN_POINT ( 'NONE',  ( 2.928127725102438461, 1.051234477803453027, 1.665338043752979447 ) ) ;
#16519=CARTESIAN_POINT ( 'NONE',  ( 4.897963269493502025, -0.6577025220009655726, -1.827417481390420928 ) ) ;
#16522=CARTESIAN_POINT ( 'NONE',  ( 5.010073305087408002, -0.7609581946756528437, 1.979555329295646260 ) ) ;
#16524=CARTESIAN_POINT ( 'NONE',  ( 2.965378323150099860, -1.564627974442783342, -1.099164922500090347 ) ) ;
#16526=CARTESIAN_POINT ( 'NONE',  ( 0.2331563151865729544, 2.882199166944008795, -2.434502449063076224 ) ) ;
#16530=CARTESIAN_POINT ( 'NONE',  ( 4.143230477514478594, 0.1011454402246019235, 2.010680395766785811 ) ) ;
#16532=CARTESIAN_POINT ( 'NONE',  ( 5.145057536039753465, -1.563975785779356587, 0.9416349707431559413 ) ) ;
#16533=CARTESIAN_POINT ( 'NONE',  ( 1.100149375694438714, 0.8407228983892693908, -1.892171374333020628 ) ) ;
#16537=CARTESIAN_POINT ( 'NONE',  ( 5.190257414508706368, -1.856628772771324210, -0.2281712211116558864 ) ) ;
#16547=CARTESIAN_POINT ( 'NONE',  ( 0.5497785174156321064, 1.531638494488884339, 1.392999266381978130 ) ) ;
#16548=CARTESIAN_POINT ( 'NONE',  ( 2.601287765717251510, -0.2046159961377100600, 2.107301599238825318 ) ) ;
#16551=CARTESIAN_POINT ( 'NONE',  ( 6.227406488038683463, 0.1581931229415085571, -2.064300627111630870 ) ) ;
#16556=CARTESIAN_POINT ( 'NONE',  ( 2.221020806870691366, 0.002245647979397680065, 2.292435215953308791 ) ) ;
#16559=CARTESIAN_POINT ( 'NONE',  ( 2.689602200614676697, 1.814610489020528350, -0.6038049036062518304 ) ) ;
#16563=CARTESIAN_POINT ( 'NONE',  ( 0.6154903249990024694, 1.648289601840571938, 1.155678142064648917 ) ) ;
#16564=CARTESIAN_POINT ( 'NONE',  ( 0.9011314981347726683, -1.685442764318560771, 1.003610994683441948 ) ) ;
#16568=CARTESIAN_POINT ( 'NONE',  ( 3.539087885488776397, -1.583190213782994515, -1.365486535101219534 ) ) ;
#16569=CARTESIAN_POINT ( 'NONE',  ( 2.113771285056417426, -0.8311870117129838142, -1.562508279020339064 ) ) ;
#16572=CARTESIAN_POINT ( 'NONE',  ( 5.701222307317492799, -0.5618967582242094805, 2.222226568792139645 ) ) ;
#16573=CARTESIAN_POINT ( 'NONE',  ( 4.048569170814999119, -1.448435850583905671, -0.9644227198624519826 ) ) ;
#16576=CARTESIAN_POINT ( 'NONE',  ( 3.040114402249920911, 1.647253858686392958, -0.5413168154804471888 ) ) ;
#16577=CARTESIAN_POINT ( 'NONE',  ( 4.264261594705793357, -2.165624863444326920, 0.1558643175220644772 ) ) ;
#16579=CARTESIAN_POINT ( 'NONE',  ( 5.401577436481666439, -1.966305606708594667, 0.4464985920552416720 ) ) ;
#16580=CARTESIAN_POINT ( 'NONE',  ( 0.3749999999841767684, 2.052068128807281955, -2.222409888604170519E-14 ) ) ;
#16583=CARTESIAN_POINT ( 'NONE',  ( 2.168856224914788466, -1.760356022852540114, -0.7827933968581005653 ) ) ;
#16585=CARTESIAN_POINT ( 'NONE',  ( 5.537407084817251857, -0.05464564937080264306, 2.220880467482534204 ) ) ;
#16587=CARTESIAN_POINT ( 'NONE',  ( 6.983263157960363010, 3.696136926403908340, 2.460428995873820579 ) ) ;
#16591=CARTESIAN_POINT ( 'NONE',  ( 1.594693315975799441, -1.184698573716694847, 1.878835628132907054 ) ) ;
#16599=CARTESIAN_POINT ( 'NONE',  ( 4.281722439037777050, -1.974808133235542495, 0.5956899724020509046 ) ) ;
#16604=CARTESIAN_POINT ( 'NONE',  ( 6.186763334926775215, -0.2743023915687745617, -1.850177433978140051 ) ) ;
#16605=CARTESIAN_POINT ( 'NONE',  ( 4.676219527341594073, 1.289314336954486384, 1.159937944992680547 ) ) ;
#16606=CARTESIAN_POINT ( 'NONE',  ( 4.669343813871559945, 1.007284801977660349, 1.419122490755047705 ) ) ;
#16608=CARTESIAN_POINT ( 'NONE',  ( 1.576131469712481303, -1.221787821332357860, 1.939473486982680628 ) ) ;
#16610=CARTESIAN_POINT ( 'NONE',  ( 6.251524270843968445, 2.085125267542327965, -0.1543399900023248728 ) ) ;
#16611=CARTESIAN_POINT ( 'NONE',  ( 1.693040327840355408, -0.6214066371539993527, 1.733238834403828754 ) ) ;
#16614=CARTESIAN_POINT ( 'NONE',  ( 1.793592486599729252, 1.492254607734722072, -1.356300734917381678 ) ) ;
#16615=CARTESIAN_POINT ( 'NONE',  ( 0.3049557181189037625, 1.908793570626087455, 1.076422248949958638 ) ) ;
#16618=CARTESIAN_POINT ( 'NONE',  ( 1.856005582152659317, -0.6995316168164237292, 1.948720873434762080 ) ) ;
#16621=CARTESIAN_POINT ( 'NONE',  ( 3.545663791850160784, -1.958584582392399742, 0.8131309587096480218 ) ) ;
#16623=CARTESIAN_POINT ( 'NONE',  ( 5.268108045213575785, 0.9031548532531764595, 1.586571422427636824 ) ) ;
#16630=CARTESIAN_POINT ( 'NONE',  ( 3.832289616293593770, -1.041828873002103917, -1.730228960026259255 ) ) ;
#16631=CARTESIAN_POINT ( 'NONE',  ( 0.4464868854077256866, 2.100361318156780399, 0.1544987475943972732 ) ) ;
#16634=CARTESIAN_POINT ( 'NONE',  ( 5.295690652966449363, -1.314428334581790203, -1.317609258728233756 ) ) ;
#16640=CARTESIAN_POINT ( 'NONE',  ( 0.2335756976950612018, -1.975703151049061024, 0.8776370805363906680 ) ) ;
#16644=CARTESIAN_POINT ( 'NONE',  ( 1.844673738135360175, -0.9321790797625574276, 1.461707330738234667 ) ) ;
#16645=CARTESIAN_POINT ( 'NONE',  ( 0.7963321702096434196, 1.420339700582837539, 1.005379078535458159 ) ) ;
#16646=CARTESIAN_POINT ( 'NONE',  ( 6.375599228498684212, 2.210405824868751701, -0.6629917143727501738 ) ) ;
#16649=CARTESIAN_POINT ( 'NONE',  ( 2.495449868850362574, 1.590812333473600626, 1.309970014422021212 ) ) ;
#16652=CARTESIAN_POINT ( 'NONE',  ( 0.8958609827393304581, 0.1455075039201655374, 2.010896580075637541 ) ) ;
#16655=CARTESIAN_POINT ( 'NONE',  ( 6.438356904408193415, 1.850619875698428674, 0.2722718653145329015 ) ) ;
#16656=CARTESIAN_POINT ( 'NONE',  ( 4.113462262696740979, 1.539102623358613586, 1.134910093507961237 ) ) ;
#16658=CARTESIAN_POINT ( 'NONE',  ( 6.568967528192747096, -2.015767819289843388, -0.8987472251835016968 ) ) ;
#16663=CARTESIAN_POINT ( 'NONE',  ( 0.5397205009909338269, -1.917025550485540908, 0.6358503350361620621 ) ) ;
#16666=CARTESIAN_POINT ( 'NONE',  ( 4.102763937057193999, -0.7201832649769298600, -2.192400882750038971 ) ) ;
#16667=CARTESIAN_POINT ( 'NONE',  ( 5.107842384611220865, 0.6171798735227496113, -1.862306164846748491 ) ) ;
#16668=CARTESIAN_POINT ( 'NONE',  ( 2.412880707699780025, -1.519673801815585312, 1.240645658979570909 ) ) ;
#16671=CARTESIAN_POINT ( 'NONE',  ( 0.6556431738361043760, 2.038855430691276727, -0.5708433468438726122 ) ) ;
#16674=CARTESIAN_POINT ( 'NONE',  ( 0.4625323210639306071, 0.1833022542275381528, -1.831979997761295165 ) ) ;
#16676=CARTESIAN_POINT ( 'NONE',  ( 4.680651438812245324, 1.340593046976858771, -1.707629433300766664 ) ) ;
#16678=CARTESIAN_POINT ( 'NONE',  ( 1.441811196653530747, -1.994930912159533332, 0.7194735443712959588 ) ) ;
#16683=CARTESIAN_POINT ( 'NONE',  ( 1.897801681018367548, -0.6972820500400818133, 1.939346266731331259 ) ) ;
#16687=CARTESIAN_POINT ( 'NONE',  ( 0.07735805125225460321, 2.008365972388022946, -2.502973720202539276 ) ) ;
#16689=CARTESIAN_POINT ( 'NONE',  ( 5.022078740994724733, -1.902695638548990820, 0.1913334245251183119 ) ) ;
#16691=CARTESIAN_POINT ( 'NONE',  ( 2.003560550249494199, 1.880309486893988913, 1.257863985149072938 ) ) ;
#16693=CARTESIAN_POINT ( 'NONE',  ( 1.353448696812571850, -1.313440895511051032, -1.247944760566013223 ) ) ;
#16694=CARTESIAN_POINT ( 'NONE',  ( 1.639701460626964868, 1.910339084310968660, -0.1447352371885517186 ) ) ;
#16696=CARTESIAN_POINT ( 'NONE',  ( 3.437997351728830697, 1.311287738946330439, 1.602184970737066116 ) ) ;
#16698=CARTESIAN_POINT ( 'NONE',  ( 0.9011734813738042638, 1.610450750236171125, 1.136898926478569383 ) ) ;
#16699=CARTESIAN_POINT ( 'NONE',  ( 5.057218277682078877, -1.628452160524866521, -1.029070375190293873 ) ) ;
#16700=CARTESIAN_POINT ( 'NONE',  ( 0.8917866929778429652, 2.032703844138737725, -1.092514170908296833 ) ) ;
#16703=CARTESIAN_POINT ( 'NONE',  ( 5.020015070024019366, 2.040704184028362178, -0.2994381943521097766 ) ) ;
#16707=CARTESIAN_POINT ( 'NONE',  ( 6.335009839202000670, 0.2025031609870796001, 2.096191850513532184 ) ) ;
#16710=CARTESIAN_POINT ( 'NONE',  ( 4.850933092205481856, -1.739298515662604405, 1.283314429840809234 ) ) ;
#16711=CARTESIAN_POINT ( 'NONE',  ( 5.039715841750210146, -1.917062458738912012, 0.6357382205050918778 ) ) ;
#16718=CARTESIAN_POINT ( 'NONE',  ( 3.397672961473942266, -1.985868886743065609, 0.3494831190506141883 ) ) ;
#16723=CARTESIAN_POINT ( 'NONE',  ( 5.418883921851007202, 1.995750516393671514, 0.8311057252617033431 ) ) ;
#16728=CARTESIAN_POINT ( 'NONE',  ( 5.659779856126235131, 1.203369751103126717, 1.617807692209995984 ) ) ;
#16730=CARTESIAN_POINT ( 'NONE',  ( 0.8731895615166852531, 1.663438651979048277, -0.4559567554138827528 ) ) ;
#16735=CARTESIAN_POINT ( 'NONE',  ( 0.2096995604969940641, -0.7494040810181783474, -1.602093636072899008 ) ) ;
#16736=CARTESIAN_POINT ( 'NONE',  ( 1.190090860395363492, 1.200783890555771283, 1.615600688039710020 ) ) ;
#16742=CARTESIAN_POINT ( 'NONE',  ( 2.631617588254760776, -0.2053842346896698201, 2.110501108333342035 ) ) ;
#16743=CARTESIAN_POINT ( 'NONE',  ( 1.810172953844836119, 1.158670025852935437, -1.650096248209936167 ) ) ;
#16744=CARTESIAN_POINT ( 'NONE',  ( 2.179683618226692321, 1.775955819808447966, -0.3565394459093262358 ) ) ;
#16747=CARTESIAN_POINT ( 'NONE',  ( 6.051685545382852638, 0.6321331830463626789, -2.067208725892249799 ) ) ;
#16751=CARTESIAN_POINT ( 'NONE',  ( 0.5146670378583360073, 0.1438656263933698054, 1.910404373559170477 ) ) ;
#16759=CARTESIAN_POINT ( 'NONE',  ( 4.311504812833309330, -0.3723461477018601418, 2.129241309423899775 ) ) ;
#16762=CARTESIAN_POINT ( 'NONE',  ( 2.373420902723611725, -1.847293605357634982, -1.041186957106011723 ) ) ;
#16764=CARTESIAN_POINT ( 'NONE',  ( 3.743400255998735382, -1.490684086824107357, -1.290067496309046158 ) ) ;
#16765=CARTESIAN_POINT ( 'NONE',  ( 5.730699431777452446, 1.279516236652695316, -1.421498520143074540 ) ) ;
#16768=CARTESIAN_POINT ( 'NONE',  ( 5.969198390587827419, 1.736284540159404033, 0.9297856951416498816 ) ) ;
#16769=CARTESIAN_POINT ( 'NONE',  ( 1.411946100005515126, 1.304364503314077162, -1.438846909250802053 ) ) ;
#16774=CARTESIAN_POINT ( 'NONE',  ( 2.044979492446592939, -1.679722130475280961, -1.244493991799436650 ) ) ;
#16778=CARTESIAN_POINT ( 'NONE',  ( 6.463533315534490065, -1.538886664202097965, -1.134999244291827747 ) ) ;
#16780=CARTESIAN_POINT ( 'NONE',  ( 4.758537496233657293, 0.8426522330295079799, 2.039869969286691731 ) ) ;
#16781=CARTESIAN_POINT ( 'NONE',  ( 2.274722540679521288, -1.357913018379176995, 1.739418515187239223 ) ) ;
#16783=CARTESIAN_POINT ( 'NONE',  ( 0.7856316122640573107, 1.842795011522216697, -0.5104879603500325214 ) ) ;
#16786=CARTESIAN_POINT ( 'NONE',  ( 3.912603064140641518, 0.7423916865902053797, 1.932869565047180327 ) ) ;
#16789=CARTESIAN_POINT ( 'NONE',  ( 1.920999885407469243, 2.016935458891587096, 0.7782144962657986387 ) ) ;
#16790=CARTESIAN_POINT ( 'NONE',  ( 3.544632465004614374, -1.790652189326558563, 1.263247045326252094 ) ) ;
#16796=CARTESIAN_POINT ( 'NONE',  ( 5.783786074351109363, 1.412321387942861328, -1.005976269456631211 ) ) ;
#16798=CARTESIAN_POINT ( 'NONE',  ( 4.715722526854881913, 0.4587184135333640111, -2.018627749927892179 ) ) ;
#16799=CARTESIAN_POINT ( 'NONE',  ( 5.220359425914078422, 2.086072958538415012, 0.3609885457144176302 ) ) ;
#16802=CARTESIAN_POINT ( 'NONE',  ( 2.588665490599820096, 1.909050991929973629, 0.4833708566103470661 ) ) ;
#16803=CARTESIAN_POINT ( 'NONE',  ( 5.701222307317492799, -0.5618967582242094805, 2.222226568792139645 ) ) ;
#16804=CARTESIAN_POINT ( 'NONE',  ( 2.508196354075361789, -0.6984789837382252564, -1.686990664346368796 ) ) ;
#16810=ORIENTED_EDGE ( 'NONE', *, *, #116226, .T. ) ;
#16812=CARTESIAN_POINT ( 'NONE',  ( 3.867443265902783534, -1.676145683993632618, -1.114854040202686969 ) ) ;
#16813=CARTESIAN_POINT ( 'NONE',  ( 4.785966450049039089, -1.203721183051874810, -1.548998264137561254 ) ) ;
#16817=CARTESIAN_POINT ( 'NONE',  ( 0.1696251593464107033, 1.207222248521317765, 1.706790159955206887 ) ) ;
#16818=CARTESIAN_POINT ( 'NONE',  ( 6.192257685097896314, -1.761771181780842577, -0.1690057029742654260 ) ) ;
#16820=CARTESIAN_POINT ( 'NONE',  ( 2.062683196291382082, -2.004346222996217897, -0.8864330828558324438 ) ) ;
#16821=CARTESIAN_POINT ( 'NONE',  ( 0.8545597497816240784, 0.3412253653619911065, -1.706464705969434670 ) ) ;
#16824=CARTESIAN_POINT ( 'NONE',  ( 0.2335667940002320309, 1.326312899344052276, -2.404742575607053734 ) ) ;
#16825=CARTESIAN_POINT ( 'NONE',  ( 0.4160739966224377140, 1.193427498895651029, -1.245624518738875697 ) ) ;
#16826=CARTESIAN_POINT ( 'NONE',  ( 0.8436309607196719185, -1.274966737007717343, 1.912178556870794521 ) ) ;
#16827=CARTESIAN_POINT ( 'NONE',  ( -0.04112450405316381286, -1.960553898366865555, -0.9795403211517728082 ) ) ;
#16829=CARTESIAN_POINT ( 'NONE',  ( 2.737190076726934151, 0.2709513247245790013, 2.190122135706531914 ) ) ;
#16830=CARTESIAN_POINT ( 'NONE',  ( 1.481551236908748237, -0.05589941666775917473, 2.170521761658677828 ) ) ;
#16831=CARTESIAN_POINT ( 'NONE',  ( -0.01727558406095473439, -0.1313277740116538805, -1.795991579427682616 ) ) ;
#16832=CARTESIAN_POINT ( 'NONE',  ( 2.624332661740484962, 2.101919520188862744, 0.2543673568942694252 ) ) ;
#16833=CARTESIAN_POINT ( 'NONE',  ( 6.827182134110222123, 4.687887262399931920, 2.751577338787388083 ) ) ;
#16834=CARTESIAN_POINT ( 'NONE',  ( 5.860362583224701716, 0.7811062513497173398, 1.761092865462327239 ) ) ;
#16837=CARTESIAN_POINT ( 'NONE',  ( 2.068323803795060645, -1.406806521851681424, 1.809881060044524093 ) ) ;
#16841=CARTESIAN_POINT ( 'NONE',  ( 4.828890449103202975, 1.532327986240004103, -1.608379539844583705 ) ) ;
#16848=CARTESIAN_POINT ( 'NONE',  ( 2.883435573726996548, -0.5880205015329244000, -1.928751729079546173 ) ) ;
#16850=CARTESIAN_POINT ( 'NONE',  ( 1.252863987647494515, -0.4972004349026898362, -2.001653351804733028 ) ) ;
#16857=CARTESIAN_POINT ( 'NONE',  ( 4.435597005726048536, 0.9382243502508281763, -1.980580373504265301 ) ) ;
#16858=CARTESIAN_POINT ( 'NONE',  ( 1.090470458312575053, -0.4872005951904456733, 1.956561897242928172 ) ) ;
#16859=CARTESIAN_POINT ( 'NONE',  ( 1.399689850468607277, -0.6632477835330424787, -1.717811453623831808 ) ) ;
#16860=CARTESIAN_POINT ( 'NONE',  ( 4.751808913491627706, 0.7073710267669359730, 1.700028372310140368 ) ) ;
#16864=CARTESIAN_POINT ( 'NONE',  ( 5.420859398437725574, 1.687492901312273474, 0.6969783729503381542 ) ) ;
#16865=CARTESIAN_POINT ( 'NONE',  ( 6.135388727473008785, 0.6351960432287793168, 1.913804721665197883 ) ) ;
#16867=CARTESIAN_POINT ( 'NONE',  ( 5.120128864776952504, -1.205885850527373293, -1.914207236704228654 ) ) ;
#16869=CARTESIAN_POINT ( 'NONE',  ( 0.5398470734442856189, -1.490880511344143011, -1.487817205855391789 ) ) ;
#16870=CARTESIAN_POINT ( 'NONE',  ( 4.932118098221458524, 1.189261692661430114, 1.694535115018414917 ) ) ;
#16879=CARTESIAN_POINT ( 'NONE',  ( 1.160570123509139906, 2.118417766304943495, 0.09849428607798524360 ) ) ;
#16880=CARTESIAN_POINT ( 'NONE',  ( 1.723182734256373916, 1.642088205692782132, -1.496221191757711066 ) ) ;
#16884=CARTESIAN_POINT ( 'NONE',  ( 2.840232074097197579, -1.010955899468408248, 1.681206195012739046 ) ) ;
#16891=CARTESIAN_POINT ( 'NONE',  ( 2.285534418239891785, 0.09939759515392716793, -2.118372479656557061 ) ) ;
#16893=CARTESIAN_POINT ( 'NONE',  ( 3.930091730393743710, 1.087902980620155891, 1.632394305395828304 ) ) ;
#16894=CARTESIAN_POINT ( 'NONE',  ( 3.538091169922503276, 0.9737216987566952309, -1.930062384640649054 ) ) ;
#16895=CARTESIAN_POINT ( 'NONE',  ( 2.454439063956286304, -1.602943312447857593, -0.9057913635923324769 ) ) ;
#16898=CARTESIAN_POINT ( 'NONE',  ( 4.470479574576804005, -0.003715868306445029284, -1.740516468156935836 ) ) ;
#16902=CARTESIAN_POINT ( 'NONE',  ( 2.395597313961893349, 1.670541196947441520, 1.371929806955954012 ) ) ;
#16903=CARTESIAN_POINT ( 'NONE',  ( 4.727888646976695419, -1.799647678597478206, -0.9090046787488814672 ) ) ;
#16906=CARTESIAN_POINT ( 'NONE',  ( 1.797963993548271411, -0.7283430984801853025, 2.035426966748521860 ) ) ;
#16907=CARTESIAN_POINT ( 'NONE',  ( 3.520352277729906998, 1.251605784994310300, -1.523194303571529185 ) ) ;
#16908=CARTESIAN_POINT ( 'NONE',  ( 2.934795777137487516, 0.2378783870938088740, 1.956871125110821952 ) ) ;
#16910=CARTESIAN_POINT ( 'NONE',  ( 3.913568440338021315, -1.001196544591560933, -1.663976088286099886 ) ) ;
#16918=CARTESIAN_POINT ( 'NONE',  ( 1.167327668269029228, -1.995579438226593894, -0.9423882379527288577 ) ) ;
#16920=CARTESIAN_POINT ( 'NONE',  ( 5.084793414397763556, 1.876112756342168675, 0.5732009990792874543 ) ) ;
#16922=CARTESIAN_POINT ( 'NONE',  ( 3.784452290478927505, -0.6679156082517538895, -2.009268603764336358 ) ) ;
#16924=CARTESIAN_POINT ( 'NONE',  ( 0.1745949693968510408, 0.7659234433113177865, -1.841618699378000601 ) ) ;
#16926=CARTESIAN_POINT ( 'NONE',  ( 3.960763856159645879, 0.2235175650571289141, -1.827449369368571386 ) ) ;
#16930=CARTESIAN_POINT ( 'NONE',  ( 5.027636390373714903, -0.3086946445357250379, 2.097867224209007730 ) ) ;
#16933=CARTESIAN_POINT ( 'NONE',  ( 5.501267734246070518, 1.682208477397129975, 1.190076826167464352 ) ) ;
#16936=CARTESIAN_POINT ( 'NONE',  ( 1.258004785490075994, -1.861241886096485221, -0.004951839839751126689 ) ) ;
#16937=CARTESIAN_POINT ( 'NONE',  ( 2.559893532628489954, -1.268187297466142338, 1.335118840784771166 ) ) ;
#16943=CARTESIAN_POINT ( 'NONE',  ( 2.596532132193625664, -2.201043451360765957, -0.1612727490639675743 ) ) ;
#16944=CARTESIAN_POINT ( 'NONE',  ( 5.184992917819648994, -0.2698046931138863846, -2.246192962944548732 ) ) ;
#16946=CARTESIAN_POINT ( 'NONE',  ( 5.132992444152020717, 1.676870426783064083, 0.6860526005390086279 ) ) ;
#16947=CARTESIAN_POINT ( 'NONE',  ( 5.049963001771692106, 0.9498492218114750196, 1.663612537209507858 ) ) ;
#16949=CARTESIAN_POINT ( 'NONE',  ( 4.908994958506140982, 1.627828031611065152, 0.9215782234750914403 ) ) ;
#16951=CARTESIAN_POINT ( 'NONE',  ( 4.562867621930529971, 1.439169320343157921, -1.179982364782502069 ) ) ;
#16953=CARTESIAN_POINT ( 'NONE',  ( 5.963686863811354932, 1.742942877579903405, -0.3063674984340163387 ) ) ;
#16954=CARTESIAN_POINT ( 'NONE',  ( -0.1882626618336727398, -1.244567986390752390, -1.587255334073833790 ) ) ;
#16956=CARTESIAN_POINT ( 'NONE',  ( 2.666745002694201450, -1.451881433263510601, 1.525875076051644408 ) ) ;
#16959=CARTESIAN_POINT ( 'NONE',  ( 0.07479286986305369589, 4.095183424177953668, -2.410510762676120411 ) ) ;
#16961=CARTESIAN_POINT ( 'NONE',  ( 1.529563250702131727, -0.2428666551740152890, 2.005035470024270960 ) ) ;
#16965=CARTESIAN_POINT ( 'NONE',  ( 2.056162960589353883, 2.155939639820044107, -0.1567802445739118478 ) ) ;
#16966=CARTESIAN_POINT ( 'NONE',  ( 6.890000000000004121, 6.033562824179531603, 2.874897443939719910 ) ) ;
#16973=CARTESIAN_POINT ( 'NONE',  ( 1.066276686178056377, -1.386418637449363889, 1.697306931840412370 ) ) ;
#16975=CARTESIAN_POINT ( 'NONE',  ( 1.903560677580185656, 1.881515123832262715, 1.256258119677531315 ) ) ;
#16984=CARTESIAN_POINT ( 'NONE',  ( 2.899370140885823233, -0.5591585085688542955, 1.679125488999051452 ) ) ;
#16985=CARTESIAN_POINT ( 'NONE',  ( 0.2004011508093841987, -2.105512755765154509, -0.05116925900590372361 ) ) ;
#16990=CARTESIAN_POINT ( 'NONE',  ( 4.956657736208940790, -1.899625167328807374, -0.6766988040120130998 ) ) ;
#16994=CARTESIAN_POINT ( 'NONE',  ( 2.500682550815761740, 1.503739811390795378, -1.112508705057350999 ) ) ;
#16996=CARTESIAN_POINT ( 'NONE',  ( 2.940353189855488658, -1.068159618217549234, 1.773299548953041871 ) ) ;
#16998=CARTESIAN_POINT ( 'NONE',  ( 1.599720133015330337, 1.321132142916726204, 1.382909031182079307 ) ) ;
#17004=CARTESIAN_POINT ( 'NONE',  ( 0.8262462788446512940, -0.8622288892402606431, -1.707089296137359158 ) ) ;
#17006=CARTESIAN_POINT ( 'NONE',  ( 3.068751266904270025, 1.422870340827029345, -1.350941015047700366 ) ) ;
#17009=CARTESIAN_POINT ( 'NONE',  ( 5.062787373817619674, 0.6179034821891696838, 2.028544477791139222 ) ) ;
#17012=CARTESIAN_POINT ( 'NONE',  ( 6.169206948603202179, 0.1476589778573663692, -1.965905794126821426 ) ) ;
#17014=CARTESIAN_POINT ( 'NONE',  ( 2.039316462420410758, 0.004210374635823382894, 2.013376229890501357 ) ) ;
#17016=CARTESIAN_POINT ( 'NONE',  ( 0.6325982246286944166, 0.6188553777890459795, 2.024753282845246805 ) ) ;
#17018=CARTESIAN_POINT ( 'NONE',  ( 2.506376218629560171, 2.069854378281150709, 0.05321039126485183068 ) ) ;
#17022=CARTESIAN_POINT ( 'NONE',  ( 5.736299646367586824, 0.4068676293152873602, 2.050479918790772960 ) ) ;
#17024=CARTESIAN_POINT ( 'NONE',  ( 4.049673113991675955, 0.6152068410551281286, -1.718917501701062278 ) ) ;
#17028=CARTESIAN_POINT ( 'NONE',  ( 4.893709131440695081, 1.632385321431808256, 1.485157849447714451 ) ) ;
#17031=CARTESIAN_POINT ( 'NONE',  ( 3.967365900211225593, -1.591558630706500832, -1.059764132600553355 ) ) ;
#17037=CARTESIAN_POINT ( 'NONE',  ( 6.515165533258342023, -2.126321577054360201, 0.5302794918828001025 ) ) ;
#17039=CARTESIAN_POINT ( 'NONE',  ( -0.04178991631376138827, -1.644041690304678616, -0.8291446804715857377 ) ) ;
#17041=CARTESIAN_POINT ( 'NONE',  ( 4.798043669735932326, -1.870115615568968881, -0.04763329477865811679 ) ) ;
#17046=CARTESIAN_POINT ( 'NONE',  ( 1.076931260867712625, 1.817606662292377218, 0.7587987759381797925 ) ) ;
#17047=CARTESIAN_POINT ( 'NONE',  ( 1.827750133516142128, 0.7691037069590834774, -1.864176919362303675 ) ) ;
#17051=CARTESIAN_POINT ( 'NONE',  ( 2.379091696419192381, 2.003018898301941686, -0.8894332929959417600 ) ) ;
#17052=CARTESIAN_POINT ( 'NONE',  ( 5.883392091387670497, 1.685093539698417242, -0.7030590484572999399 ) ) ;
#17054=CARTESIAN_POINT ( 'NONE',  ( 6.825078400183553384, 0.5907600490881077526, 1.908621492364571903 ) ) ;
#17063=CARTESIAN_POINT ( 'NONE',  ( 4.686955257832659427, 1.367739038236553517, 1.232883728221023212 ) ) ;
#17064=CARTESIAN_POINT ( 'NONE',  ( 0.7154901591317133214, 1.647040347281914396, 1.157252022262734714 ) ) ;
#17065=CARTESIAN_POINT ( 'NONE',  ( 2.829810162582825139, -1.586297295151902986, 1.663386555757565555 ) ) ;
#17067=CARTESIAN_POINT ( 'NONE',  ( 0.9009385260731802569, -1.599958946562014539, 0.9501217156336287939 ) ) ;
#17071=CARTESIAN_POINT ( 'NONE',  ( 4.131050151015442928, 1.750605847248308145, 0.7702136748066327199 ) ) ;
#17074=CARTESIAN_POINT ( 'NONE',  ( 4.019144481351099252, -2.000086177330139492, 0.6089195546459759134 ) ) ;
#17075=CARTESIAN_POINT ( 'NONE',  ( 2.834663617355744680, 0.2272019944037397543, 1.856728029318695627 ) ) ;
#17078=CARTESIAN_POINT ( 'NONE',  ( 5.759284750224211713, 1.812880138157666465, -0.3211251414683007899 ) ) ;
#17082=CARTESIAN_POINT ( 'NONE',  ( 5.162619097868246243, -1.245661315326980212, 1.193383824415847450 ) ) ;
#17084=CARTESIAN_POINT ( 'NONE',  ( 0.2813449273042024079, 1.443300801228193153, -0.9609375900588543740 ) ) ;
#17086=CARTESIAN_POINT ( 'NONE',  ( 5.049771808528761952, 1.604214368398539925, 1.463040072455735974 ) ) ;
#17087=CARTESIAN_POINT ( 'NONE',  ( 2.912524513316586461, 1.322148455168963510, -1.259233298254287536 ) ) ;
#17088=CARTESIAN_POINT ( 'NONE',  ( 0.5495624486224827132, 1.449728300881658383, 1.321815246172884040 ) ) ;
#17089=CARTESIAN_POINT ( 'NONE',  ( 5.788306078712673219, -0.7643476728274435361, -1.974717070840046107 ) ) ;
#17091=CARTESIAN_POINT ( 'NONE',  ( 6.374598633881160659, -0.1077809834691043772, -2.289980472931157252 ) ) ;
#17094=CARTESIAN_POINT ( 'NONE',  ( 1.664851754375612058, 0.6682523891239250391, 2.012492909199379731 ) ) ;
#17098=CARTESIAN_POINT ( 'NONE',  ( 6.245025782124020708, -0.3104734683975469145, -2.148636169971326559 ) ) ;
#17099=CARTESIAN_POINT ( 'NONE',  ( 6.983263157960368339, 1.232032666090671302, 2.265420076015733031 ) ) ;
#17101=CARTESIAN_POINT ( 'NONE',  ( 1.788022372910631486, 2.124507586210178989, -0.6485351029156469771 ) ) ;
#17103=CARTESIAN_POINT ( 'NONE',  ( 6.469375277500488686, -1.978045142091336306, -0.3906011616893814709 ) ) ;
#17105=CARTESIAN_POINT ( 'NONE',  ( 4.047761193102417110, 1.490534549623608873, 1.425871689066391168 ) ) ;
#17111=CARTESIAN_POINT ( 'NONE',  ( 0.1329588055935760349, 6.948069629093068578, -2.440977959956799115 ) ) ;
#17112=CARTESIAN_POINT ( 'NONE',  ( 0.7090669197488512765, -0.3047467688393705187, 2.068175119304823451 ) ) ;
#17113=CARTESIAN_POINT ( 'NONE',  ( 4.036529152626888717, -1.599951230533543267, 0.9111318136766360931 ) ) ;
#17115=CARTESIAN_POINT ( 'NONE',  ( 1.887319702290214840, 1.186364228098319762, 1.252193311579427482 ) ) ;
#17116=CARTESIAN_POINT ( 'NONE',  ( 0.1632964843477149597, 1.879801964727344732, -0.7303121171872913875 ) ) ;
#17118=CARTESIAN_POINT ( 'NONE',  ( 1.477568294945711180, -2.288151160537778672, -0.2198310841375460678 ) ) ;
#17120=CARTESIAN_POINT ( 'NONE',  ( 1.423510532338147394, -0.05571650319935492202, 2.261890015172054458 ) ) ;
#17121=CARTESIAN_POINT ( 'NONE',  ( 4.213572796808015219, -0.3603392467595716298, 2.074844637031019623 ) ) ;
#17123=CARTESIAN_POINT ( 'NONE',  ( 2.477515592860125349, 1.084993897938502760, 1.398054747847920609 ) ) ;
#17127=CARTESIAN_POINT ( 'NONE',  ( 6.375000000015829116, 2.052068128807268188, -3.630807684676397404E-13 ) ) ;
#17131=CARTESIAN_POINT ( 'NONE',  ( 4.693709758858874537, 2.072258576215581183, -0.8006532145865407069 ) ) ;
#17132=CARTESIAN_POINT ( 'NONE',  ( 3.047022719409075986, -1.791863632763015968, -1.261349808265788797 ) ) ;
#17135=CARTESIAN_POINT ( 'NONE',  ( 5.830757645730302308, 1.424217953154560012, -1.571192434731554677 ) ) ;
#17137=CARTESIAN_POINT ( 'NONE',  ( 6.890000000000004121, 6.033562824179531603, 2.874897443939719910 ) ) ;
#17139=CARTESIAN_POINT ( 'NONE',  ( 5.379186226027963258, -1.918017450862268714, -0.9047448674902383026 ) ) ;
#17143=CARTESIAN_POINT ( 'NONE',  ( 6.561405286136595905, 0.3748316153167965403, -2.128808860954830795 ) ) ;
#17145=CARTESIAN_POINT ( 'NONE',  ( 6.128435733830499998, 0.1874100934057248424, 1.831705376836203936 ) ) ;
#17148=CARTESIAN_POINT ( 'NONE',  ( 0.9424304438642245874, -1.370989592614113795, -1.072060877835380621 ) ) ;
#17154=CARTESIAN_POINT ( 'NONE',  ( 5.612251347527116963, -0.9680786960581324596, -1.932885698521320528 ) ) ;
#17158=CARTESIAN_POINT ( 'NONE',  ( 4.768538688506021472, -1.414568798902924307, 1.634688457493836289 ) ) ;
#17162=CARTESIAN_POINT ( 'NONE',  ( 5.448493488195655488, 0.5694873833897282633, 1.887333253073280703 ) ) ;
#17163=CARTESIAN_POINT ( 'NONE',  ( 4.991369361657826964, 1.659364262194364725, 0.5025568866975324012 ) ) ;
#17165=CARTESIAN_POINT ( 'NONE',  ( 1.593588134247824639, -0.7342643958434189599, 2.065040727587868830 ) ) ;
#17166=CARTESIAN_POINT ( 'NONE',  ( 1.923324260599985402, 2.153519634812319783, 0.8294600792757185204 ) ) ;
#17167=CARTESIAN_POINT ( 'NONE',  ( 4.253237527111143557, -1.711175411557999348, -1.148025453137695662 ) ) ;
#17168=CARTESIAN_POINT ( 'NONE',  ( 0.02324440041187331510, -1.194077796415137449, -1.532174088482601837 ) ) ;
#17172=CARTESIAN_POINT ( 'NONE',  ( 3.937823072884456099, -2.028283017459261650, 0.6187693826033290323 ) ) ;
#17174=CARTESIAN_POINT ( 'NONE',  ( 1.600232647554021392, -0.2440283035436350279, 2.001511509883910911 ) ) ;
#17176=CARTESIAN_POINT ( 'NONE',  ( 4.542132036680512464, 0.9468659437555368985, -1.993456357439137960 ) ) ;
#17178=CARTESIAN_POINT ( 'NONE',  ( -0.1290005225502675879, 2.860092606084875033, -2.662085506130333457 ) ) ;
#17184=CARTESIAN_POINT ( 'NONE',  ( 3.450122203709057533, 2.061077815303002936, 0.001625369314967386580 ) ) ;
#17187=CARTESIAN_POINT ( 'NONE',  ( 2.947920495102425154, -1.358134161044775245, -1.495000266999703564 ) ) ;
#17190=CARTESIAN_POINT ( 'NONE',  ( 1.639600518753115521, -1.491979387419887892, -1.421952917470001632 ) ) ;
#17194=CARTESIAN_POINT ( 'NONE',  ( -0.2409995289980246258, 2.020898751655671788, -2.415740196953279462 ) ) ;
#17195=CARTESIAN_POINT ( 'NONE',  ( 1.429379046243149931, 0.9088080074306194023, -1.601118750654044964 ) ) ;
#17196=CARTESIAN_POINT ( 'NONE',  ( 0.1886478520232073020, -1.081937125009281964, 2.038365869624358506 ) ) ;
#17198=CARTESIAN_POINT ( 'NONE',  ( 1.950665695202157046, 0.6760947502928333908, 2.053231632317173538 ) ) ;
#17200=CARTESIAN_POINT ( 'NONE',  ( 1.675017921984035096, 1.752138005693338441, -0.9981273289914743829 ) ) ;
#17201=CARTESIAN_POINT ( 'NONE',  ( 2.091588275066556868, 1.323615364194903554, -1.878831054484223495 ) ) ;
#17203=CARTESIAN_POINT ( 'NONE',  ( 0.08069323953814251660, -0.1329233695197447052, -1.840450602299897431 ) ) ;
#17205=CARTESIAN_POINT ( 'NONE',  ( 4.381683959536594841, 1.286834623079432083, 1.493660651562748853 ) ) ;
#17206=CARTESIAN_POINT ( 'NONE',  ( 3.046111529846948329, 0.9110102549910354952, 1.799122713138465279 ) ) ;
#17210=CARTESIAN_POINT ( 'NONE',  ( 6.358053323650514344, 2.100580423050825818, -0.1529390103112079069 ) ) ;
#17211=CARTESIAN_POINT ( 'NONE',  ( 5.178213324540339002, -1.104578422852561914, -1.750899486206449751 ) ) ;
#17214=CARTESIAN_POINT ( 'NONE',  ( 6.539320575229236709, 3.694699318329996540, 2.517509839998680832 ) ) ;
#17215=CARTESIAN_POINT ( 'NONE',  ( 5.660417604421997595, 2.017665076342503916, 0.09485465564632548918 ) ) ;
#17217=CARTESIAN_POINT ( 'NONE',  ( 3.405163318333865874, 1.819529416799025912, -1.419322092190724138 ) ) ;
#17218=CARTESIAN_POINT ( 'NONE',  ( 1.147418581349904265, 1.820775857560010369, -0.9689367605143526241 ) ) ;
#17225=CARTESIAN_POINT ( 'NONE',  ( 3.139314614211644816, -0.1572037376256547880, -2.165524352769617078 ) ) ;
#17229=CARTESIAN_POINT ( 'NONE',  ( 3.245484093776138668, 1.841430844176932480, -0.003062914905635482320 ) ) ;
#17231=CARTESIAN_POINT ( 'NONE',  ( 4.652002595327206613, 0.8389548150543740812, 2.024815518666116088 ) ) ;
#17233=CARTESIAN_POINT ( 'NONE',  ( 4.522535110384587220, 1.395170471642327437, -1.781064426588598426 ) ) ;
#17239=CARTESIAN_POINT ( 'NONE',  ( 6.010986587707961348, 1.561705629380090832, 0.8325338966498199156 ) ) ;
#17240=CARTESIAN_POINT ( 'NONE',  ( 4.318997845537309033, 1.554796018123940193, -1.278706705004019506 ) ) ;
#17242=CARTESIAN_POINT ( 'NONE',  ( 3.381953601626528361, 1.334784698733671560, 1.628938261321200232 ) ) ;
#17243=CARTESIAN_POINT ( 'NONE',  ( 0.4740638213791115718, -1.901237768712552345, -0.2334040896743785343 ) ) ;
#17245=CARTESIAN_POINT ( 'NONE',  ( 1.732793293511214472, -1.869146454778564559, -0.6209850235064825474 ) ) ;
#17246=CARTESIAN_POINT ( 'NONE',  ( 0.9537216069140028729, 1.868711056098860235, -0.08788249432020722729 ) ) ;
#17247=CARTESIAN_POINT ( 'NONE',  ( 1.135121963537696566, -0.04462593873827064989, -1.961518378280776354 ) ) ;
#17248=CARTESIAN_POINT ( 'NONE',  ( -0.01753026575586694516, -1.247696154478775021, 1.449428981083925150 ) ) ;
#17251=ADVANCED_FACE ( 'NONE', ( #196336 ), #97991, .F. ) ;
#17254=CARTESIAN_POINT ( 'NONE',  ( 6.174654088403855212, -1.776896415251895789, -0.5849557326117056366 ) ) ;
#17257=CARTESIAN_POINT ( 'NONE',  ( 6.684440181240522527, 1.196966437107028547, -1.688953195037292243 ) ) ;
#17259=CARTESIAN_POINT ( 'NONE',  ( 0.4673438449808891004, 1.800595422158430825, 1.021790579661909781 ) ) ;
#17264=CARTESIAN_POINT ( 'NONE',  ( 5.584674446412367210, -1.345185468269005424, 1.639207791927596247 ) ) ;
#17268=CARTESIAN_POINT ( 'NONE',  ( 6.391066755906244623, 0.1909826923555627554, 1.952524381009380861 ) ) ;
#17270=CARTESIAN_POINT ( 'NONE',  ( 3.145861080134567000, -0.1455099638626895786, -2.010896398064919488 ) ) ;
#17271=CARTESIAN_POINT ( 'NONE',  ( 3.801880972252824176, -0.9895533254376009946, -1.640229128645746215 ) ) ;
#17274=CARTESIAN_POINT ( 'NONE',  ( 1.839652601550560096, 0.8350199954420146620, -2.026445374841173930 ) ) ;
#17275=CARTESIAN_POINT ( 'NONE',  ( 0.2333690889706925564, 2.018283468528142777, -2.468684669820114586 ) ) ;
#17276=CARTESIAN_POINT ( 'NONE',  ( 3.128041797164154758, 1.042111378005972311, -1.553157497896196393 ) ) ;
#17280=CARTESIAN_POINT ( 'NONE',  ( 5.220359425914078422, 2.086072958538415012, 0.3609885457144176302 ) ) ;
#17282=CARTESIAN_POINT ( 'NONE',  ( 6.672334155782003506, -0.9722939650993901450, -1.827837255792996718 ) ) ;
#17283=CARTESIAN_POINT ( 'NONE',  ( 2.753556666441462131, 2.080443298914707917, -0.2074443561481206788 ) ) ;
#17285=CARTESIAN_POINT ( 'NONE',  ( 1.025878534523045449, 1.032422052977323590, -1.381481875464431797 ) ) ;
#17295=CARTESIAN_POINT ( 'NONE',  ( 0.4514444101613367955, -1.279852094280601760, -1.282217761895942720 ) ) ;
#17300=CARTESIAN_POINT ( 'NONE',  ( 6.539320575229228716, 1.281788455817688188, 2.013036689384885225 ) ) ;
#17306=CARTESIAN_POINT ( 'NONE',  ( 2.646735056387524043, -0.3148485976074810733, -1.834047879892097388 ) ) ;
#17307=CARTESIAN_POINT ( 'NONE',  ( 0.3158528693416655653, 0.9839445311579012587, -1.643420606830671815 ) ) ;
#17308=CARTESIAN_POINT ( 'NONE',  ( 0.1647065507319189492, -1.628042339203483957, -0.8261295386280396169 ) ) ;
#17314=CARTESIAN_POINT ( 'NONE',  ( 4.891434682365626507, -1.802310843600445800, 0.7943598514809721012 ) ) ;
#17315=CARTESIAN_POINT ( 'NONE',  ( 1.436355765274465623, -1.180822252328097344, -1.761085815303937929 ) ) ;
#17319=CARTESIAN_POINT ( 'NONE',  ( 5.771465802492605768, 1.302860414194568550, 1.761948869136241047 ) ) ;
#17320=CARTESIAN_POINT ( 'NONE',  ( 4.436495903120683870, 1.889097993355067562, 0.3764034397915373975 ) ) ;
#17323=CARTESIAN_POINT ( 'NONE',  ( 0.9618826090718561872, 0.4271145061440981272, -2.164990749644220447 ) ) ;
#17328=CARTESIAN_POINT ( 'NONE',  ( 5.752784996495730496, -0.4749413952093975433, -1.911207028377271522 ) ) ;
#17329=CARTESIAN_POINT ( 'NONE',  ( 1.610778572542032050, -0.2360344744354908597, 1.927585326284560585 ) ) ;
#17330=CARTESIAN_POINT ( 'NONE',  ( 6.468148293998644327, 1.905381763673856810, 1.285138856061205148 ) ) ;
#17332=CARTESIAN_POINT ( 'NONE',  ( 4.785918264633797214, -1.142728415277466159, -1.468712688171626812 ) ) ;
#17338=CARTESIAN_POINT ( 'NONE',  ( 0.4861908890553789941, -2.175720422541329580, -0.2624175912114696252 ) ) ;
#17343=CARTESIAN_POINT ( 'NONE',  ( 1.347985785199314668, 1.823511463271022093, 0.09156768404049858701 ) ) ;
#17345=CARTESIAN_POINT ( 'NONE',  ( 3.217127751380299383, 1.692560603008624875, 0.3766165182450386117 ) ) ;
#17347=CARTESIAN_POINT ( 'NONE',  ( 6.509000000000012776, 0.5843741663743782233, 2.053293374786519188 ) ) ;
#17348=CARTESIAN_POINT ( 'NONE',  ( 0.1331565106231363538, 0.2470099659030860484, -1.980838409567912572 ) ) ;
#17349=CARTESIAN_POINT ( 'NONE',  ( 0.3988885142760539293, 1.602443225120395720, -1.069099046168849876 ) ) ;
#17350=CARTESIAN_POINT ( 'NONE',  ( 4.100408672059585591, 1.951911038179511726, 0.1965976633130430695 ) ) ;
#17353=CARTESIAN_POINT ( 'NONE',  ( 4.987034407221377030, -1.996844880220369545, -0.7138980100366009163 ) ) ;
#17357=CARTESIAN_POINT ( 'NONE',  ( 2.957943426865859760, -0.6537446763684885420, 1.964363857337739105 ) ) ;
#17361=CARTESIAN_POINT ( 'NONE',  ( 2.901363961662834168, -1.135721475377445167, -1.998492394250019233 ) ) ;
#17369=CARTESIAN_POINT ( 'NONE',  ( 3.884940529579200774, -1.786240503712609895, -0.6835825222790415934 ) ) ;
#17371=CARTESIAN_POINT ( 'NONE',  ( 5.368053323270940425, 0.8530656342727646058, 1.498931087277301843 ) ) ;
#17372=CARTESIAN_POINT ( 'NONE',  ( 3.591030000661588062, 1.731995077137841843, 1.032480907900306111 ) ) ;
#17373=CARTESIAN_POINT ( 'NONE',  ( 5.555437251493606787, -1.460316692103363456, 1.775274546321881530 ) ) ;
#17375=CARTESIAN_POINT ( 'NONE',  ( 0.3466626200071438180, 2.201290530325435757, 0.1579762268871589825 ) ) ;
#17377=CARTESIAN_POINT ( 'NONE',  ( 6.274623264596165484, -1.681128386917314366, -0.5530667918781423387 ) ) ;
#17380=CARTESIAN_POINT ( 'NONE',  ( 1.676131343691760645, -1.223425685817343789, 1.938311714834321631 ) ) ;
#17381=CARTESIAN_POINT ( 'NONE',  ( 6.685540632719009224, -0.7820230359689305244, 1.665195522482863399 ) ) ;
#17383=CARTESIAN_POINT ( 'NONE',  ( 6.421842908546858908, 1.265077015623069290, -1.789241164368003068 ) ) ;
#17386=CARTESIAN_POINT ( 'NONE',  ( -0.02988540731103107514, 0.005807295984020740404, -1.726291166677936362 ) ) ;
#17387=CARTESIAN_POINT ( 'NONE',  ( 0.6960477194701603088, -1.535568182542995208, -1.535184517522319769 ) ) ;
#17388=CARTESIAN_POINT ( 'NONE',  ( 1.059780186608853203, 1.205045252304644210, 1.616690996016925563 ) ) ;
#17390=CARTESIAN_POINT ( 'NONE',  ( 5.707627890916790570, -0.4656921374228146226, 1.869253615786143685 ) ) ;
#17392=CARTESIAN_POINT ( 'NONE',  ( 2.356001076229676805, -1.649452400593539148, -1.488157709660995920 ) ) ;
#17398=CARTESIAN_POINT ( 'NONE',  ( 4.511116409865087995, -1.705632679577104849, 0.3454082310308664305 ) ) ;
#17399=CARTESIAN_POINT ( 'NONE',  ( 3.473055881322492322, 1.772541284497713976, 0.8411618914155661875 ) ) ;
#17404=CARTESIAN_POINT ( 'NONE',  ( 0.5552253240413919100, 1.715889405040219584, -1.144428160675447614 ) ) ;
#17408=CARTESIAN_POINT ( 'NONE',  ( 1.692605830730309791, -2.251738780704269249, -0.2206997258237669290 ) ) ;
#17411=CARTESIAN_POINT ( 'NONE',  ( 2.706148147531197701, -0.7121320899835179574, -1.729884524348634933 ) ) ;
#17412=CARTESIAN_POINT ( 'NONE',  ( 0.9669347054478127923, -1.691490974053434959, -0.3813910478582624441 ) ) ;
#17413=CARTESIAN_POINT ( 'NONE',  ( 5.759372899636661991, 2.159370146098410714, -0.3733810082120898044 ) ) ;
#17414=CARTESIAN_POINT ( 'NONE',  ( 6.545943480548680249, 0.8917086005404940563, -2.128542236993334669 ) ) ;
#17415=CARTESIAN_POINT ( 'NONE',  ( 1.569287236123186213, 0.1524497474049029966, -2.055318472165644117 ) ) ;
#17416=CARTESIAN_POINT ( 'NONE',  ( 3.486211078826762844, -0.3796756879693505837, -1.904310675543115394 ) ) ;
#17419=CARTESIAN_POINT ( 'NONE',  ( 6.151601556293980089, 0.5431611868166182910, -1.789914130245950474 ) ) ;
#17420=CARTESIAN_POINT ( 'NONE',  ( 0.7500000000000005551, 4.270513119278528127E-14, 2.052068128417952497 ) ) ;
#17422=CARTESIAN_POINT ( 'NONE',  ( 6.714220164357198151, -1.617572894677368422, -1.203167480739217643 ) ) ;
#17425=CARTESIAN_POINT ( 'NONE',  ( 4.781875055470904634, 1.674888562130649960, -1.122497055794105192 ) ) ;
#17429=CARTESIAN_POINT ( 'NONE',  ( 2.385134503015675200, 1.669401249834654433, -0.7394980648879890817 ) ) ;
#17433=ORIENTED_EDGE ( 'NONE', *, *, #118416, .F. ) ;
#17437=CARTESIAN_POINT ( 'NONE',  ( 6.621752733038558603, -0.4373435798001067965, 1.978785184894470639 ) ) ;
#17438=CARTESIAN_POINT ( 'NONE',  ( 0.5047332052380922862, -2.104974169346077506, -0.2554120829242333968 ) ) ;
#17443=CARTESIAN_POINT ( 'NONE',  ( 5.998915433584960155, 1.686223865786851128, -1.184587077384538167 ) ) ;
#17444=CARTESIAN_POINT ( 'NONE',  ( 5.063125043234593115, -1.117834493326537393, 1.678003986596336761 ) ) ;
#17448=CARTESIAN_POINT ( 'NONE',  ( -0.2108831679770924727, 4.091978752061476321, -2.452067053820900178 ) ) ;
#17453=CARTESIAN_POINT ( 'NONE',  ( 5.677111188754776272, -0.9039728708103295096, -1.802140534545144890 ) ) ;
#17454=CARTESIAN_POINT ( 'NONE',  ( 4.945164379994194448, 0.5744887182440976403, -1.749284230371531024 ) ) ;
#17456=CARTESIAN_POINT ( 'NONE',  ( 3.159088808783340419, -1.747439373373047333, 1.507377025801335702 ) ) ;
#17458=CARTESIAN_POINT ( 'NONE',  ( 4.921240491056324551, -0.1114908479964340365, 2.158860929761210912 ) ) ;
#17460=CARTESIAN_POINT ( 'NONE',  ( 0.6088030852571654217, -0.2837962540496056785, 1.921085339388538982 ) ) ;
#17466=CARTESIAN_POINT ( 'NONE',  ( 3.959713429720784106, 1.856571849420919795, -0.2284545790810637578 ) ) ;
#17467=CARTESIAN_POINT ( 'NONE',  ( 0.8614045922798494459, -1.509235727096858826, -1.174430983434850972 ) ) ;
#17470=CARTESIAN_POINT ( 'NONE',  ( 2.350463684150871035, 2.206416367115513477, 0.05273732197710182673 ) ) ;
#17476=CARTESIAN_POINT ( 'NONE',  ( 1.018749824907847934, 1.819822117139553885, 0.7584178161138422913 ) ) ;
#17477=CARTESIAN_POINT ( 'NONE',  ( 0.2535066641492569883, -1.850528970283831010, 1.378429844982787422 ) ) ;
#17478=CARTESIAN_POINT ( 'NONE',  ( 1.310910670669521272, -1.548711629584406113, 1.204245502051364936 ) ) ;
#17479=CARTESIAN_POINT ( 'NONE',  ( 4.434473652564925317, -1.191674006009019404, 1.683292407194038054 ) ) ;
#17484=DIRECTION ( 'NONE',  ( -1.000000000000000000, 0.000000000000000000, 0.000000000000000000 ) ) ;
#17486=CARTESIAN_POINT ( 'NONE',  ( 0.4444779246538512751, -1.024716592377757696, 1.914062593285012603 ) ) ;
#17488=CARTESIAN_POINT ( 'NONE',  ( 6.040549724581927293, -1.551790349881351450, 0.9907606852931831742 ) ) ;
#17491=CARTESIAN_POINT ( 'NONE',  ( 1.616246341788161622, 1.260175398906153266, -1.382505567627971388 ) ) ;
#17492=CARTESIAN_POINT ( 'NONE',  ( 5.167319818800252484, 0.2175342549677051207, -2.150644138106901693 ) ) ;
#17494=CARTESIAN_POINT ( 'NONE',  ( -0.02264175331115596268, 2.007280006360371960, -2.503048469261221598 ) ) ;
#17497=CARTESIAN_POINT ( 'NONE',  ( 1.559083858985313320, -1.614856622157490706, 1.023943737511850083 ) ) ;
#17498=CARTESIAN_POINT ( 'NONE',  ( 2.500565701108145689, 1.422975883020457077, -1.052153950563482265 ) ) ;
#17499=CARTESIAN_POINT ( 'NONE',  ( 1.084454188491505988, -1.212558158303609135, 1.478703618145213783 ) ) ;
#17501=CARTESIAN_POINT ( 'NONE',  ( 4.903869178324737454, -1.028422014321051403, -1.615943446245589943 ) ) ;
#17502=CARTESIAN_POINT ( 'NONE',  ( 5.090277013941287620, 1.014100869069594291, -1.688273828314874825 ) ) ;
#17503=CARTESIAN_POINT ( 'NONE',  ( 1.301209403646291118, -0.3165094942152619772, -2.096747597609450953 ) ) ;
#17505=CARTESIAN_POINT ( 'NONE',  ( 3.608139902456270143, -0.7572706533398064765, -1.710698989992056607 ) ) ;
#17506=CARTESIAN_POINT ( 'NONE',  ( 0.1701549220758866166, -1.195335944658926230, 1.380069390326914336 ) ) ;
#17508=CARTESIAN_POINT ( 'NONE',  ( 3.035963658818414235, -1.482449291622448095, -1.634993338104336891 ) ) ;
#17512=CARTESIAN_POINT ( 'NONE',  ( 1.715356188534086224, -1.767971037936959089, -1.062312629515406170 ) ) ;
#17517=CARTESIAN_POINT ( 'NONE',  ( 6.381121926128928479, -1.751337275642101510, -0.7685668267764720341 ) ) ;
#17519=CARTESIAN_POINT ( 'NONE',  ( 4.123533666479628046, 0.2564666318346648377, -2.054367117340555549 ) ) ;
#17521=CARTESIAN_POINT ( 'NONE',  ( 1.915512222264357467, -0.2666219456287990952, 2.145042957367573777 ) ) ;
#17523=CARTESIAN_POINT ( 'NONE',  ( 2.420574729456357765, -0.7750317791199374806, -1.865254733019072297 ) ) ;
#17528=CARTESIAN_POINT ( 'NONE',  ( 6.679064532090532857, -0.9478974852125362505, -1.779352858464311016 ) ) ;
#17529=CARTESIAN_POINT ( 'NONE',  ( 0.7785302072789467287, -0.4946362931835950327, -1.954778448132548752 ) ) ;
#17530=CARTESIAN_POINT ( 'NONE',  ( 5.056268342064010213, -1.587557771011731678, 1.511049258477934032 ) ) ;
#17532=CARTESIAN_POINT ( 'NONE',  ( 3.920094060441734030, -1.906919942518231936, 0.1457910263855527466 ) ) ;
#17536=CARTESIAN_POINT ( 'NONE',  ( 2.319935610374638468, 0.9480221781073931986, -1.779637559903464394 ) ) ;
#17538=CARTESIAN_POINT ( 'NONE',  ( 0.4160993436025617886, -1.233022138464324291, -1.932370275504050827 ) ) ;
#17540=CARTESIAN_POINT ( 'NONE',  ( 4.436358534413815669, 1.691719876958649227, 0.3350348670820638142 ) ) ;
#17541=CARTESIAN_POINT ( 'NONE',  ( -0.1399997263889612154, 1.357298622859518078, -2.254419820505838334 ) ) ;
#17544=CARTESIAN_POINT ( 'NONE',  ( 0.8890225878602634468, 0.1407106197201784259, 1.956863499422318631 ) ) ;
#17548=CARTESIAN_POINT ( 'NONE',  ( 0.07516593201273896740, 4.087024598281757015, -2.598925129725014660 ) ) ;
#17549=CARTESIAN_POINT ( 'NONE',  ( 0.4267348894952603944, -1.354911996285239395, 1.565345633960463889 ) ) ;
#17551=CARTESIAN_POINT ( 'NONE',  ( 3.984856247070994506, -1.691632632888851351, -0.6484230535298250997 ) ) ;
#17555=CARTESIAN_POINT ( 'NONE',  ( 4.547391301494094762, -1.654308909395687310, 0.7384720232115218330 ) ) ;
#17560=CARTESIAN_POINT ( 'NONE',  ( 6.531710587413017244, 1.780498168465095787, -0.5416703039235416517 ) ) ;
#17562=CARTESIAN_POINT ( 'NONE',  ( 4.024928501738918030, -1.664925135935046763, 0.9472863605698205181 ) ) ;
#17570=CARTESIAN_POINT ( 'NONE',  ( 5.331313699870084299, -1.671001674814942994, -1.300292098898154780 ) ) ;
#17571=CARTESIAN_POINT ( 'NONE',  ( 1.217891636700708435, -2.108894920778502602, 0.4742063263511315796 ) ) ;
#17574=CARTESIAN_POINT ( 'NONE',  ( 1.201864610381056853, -1.825762228264395048, -0.004348209057210283834 ) ) ;
#17576=CARTESIAN_POINT ( 'NONE',  ( 3.926616521958687045, 1.733384925006593136, 0.5729815612169064654 ) ) ;
#17578=CARTESIAN_POINT ( 'NONE',  ( 2.004032382285144021, -0.8144628449315849394, 1.730399521388835460 ) ) ;
#17580=CARTESIAN_POINT ( 'NONE',  ( 2.330458462945466547, -1.214122947426389709, 1.550707797581540204 ) ) ;
#17581=CARTESIAN_POINT ( 'NONE',  ( 4.880387366230515944, -0.2415804104359954019, -1.926931144411721641 ) ) ;
#17584=CARTESIAN_POINT ( 'NONE',  ( 5.361630242575341931, -1.673063676233761621, -1.302930760576012092 ) ) ;
#17586=CARTESIAN_POINT ( 'NONE',  ( 3.123589223026546957, -0.3706944625661895976, 1.875830702792554483 ) ) ;
#17588=CARTESIAN_POINT ( 'NONE',  ( 0.2331563151865486683, 0.2490001740663889407, -1.980811336351681273 ) ) ;
#17594=CARTESIAN_POINT ( 'NONE',  ( 5.004447790439923160, -0.6182884515001166870, -1.717943145347331502 ) ) ;
#17600=CARTESIAN_POINT ( 'NONE',  ( 5.875831987524620992, 1.115552982110395330, 1.501486808359139946 ) ) ;
#17609=CARTESIAN_POINT ( 'NONE',  ( 6.473493066963706966, -0.2743099562094972743, 2.153646047958713172 ) ) ;
#17610=CARTESIAN_POINT ( 'NONE',  ( 1.107202915679715405, -0.04781017987004822223, 2.116844178444466706 ) ) ;
#17613=CARTESIAN_POINT ( 'NONE',  ( 5.928598010555855780, -1.317819122799672504, 1.596621505246295314 ) ) ;
#17614=CARTESIAN_POINT ( 'NONE',  ( 1.540310226958538475, -1.555040833713853710, 0.9856339240054690087 ) ) ;
#17619=CARTESIAN_POINT ( 'NONE',  ( 1.377341666110833529, 2.116387791839238641, -0.8810097948994728423 ) ) ;
#17622=CARTESIAN_POINT ( 'NONE',  ( 2.461071540317420592, -1.587761714688111780, 1.065645112462119570 ) ) ;
#17625=CARTESIAN_POINT ( 'NONE',  ( 0.07056460990086978191, 0.7743322593966313061, 1.858523817361916963 ) ) ;
#17626=CARTESIAN_POINT ( 'NONE',  ( 1.481223165768187355, -0.05357505548480785695, 1.961209554040027170 ) ) ;
#17630=CARTESIAN_POINT ( 'NONE',  ( 4.048837805470763662, -1.738144455908509078, -1.161405209330027555 ) ) ;
#17631=CARTESIAN_POINT ( 'NONE',  ( 1.938023551401172773, 1.750023271871611996, 0.2632672158595899536 ) ) ;
#17635=CARTESIAN_POINT ( 'NONE',  ( 4.927800006241752406, 1.181458742244513971, -1.964204249851936090 ) ) ;
#17636=CARTESIAN_POINT ( 'NONE',  ( 3.222313301838835020, 0.04370593061932443596, 1.739952058630070519 ) ) ;
#17639=CARTESIAN_POINT ( 'NONE',  ( 3.567500862290486019, 1.367785175758473581, -1.065411925293987760 ) ) ;
#17641=CARTESIAN_POINT ( 'NONE',  ( 4.088457082891777894, 1.164728776245987918, -1.832164736925721682 ) ) ;
#17643=CARTESIAN_POINT ( 'NONE',  ( 5.454314652423888354, -1.275559214091715354, 1.561879324423600668 ) ) ;
#17644=CARTESIAN_POINT ( 'NONE',  ( 1.000000000000000666, -5.752119711681284071E-14, -2.052068128417952053 ) ) ;
#17647=CARTESIAN_POINT ( 'NONE',  ( 2.256748493264736588, -1.490592131378381646, 1.220310119380305203 ) ) ;
#17649=CARTESIAN_POINT ( 'NONE',  ( 5.361676289133297857, -1.751401506552331400, -1.366425036640180446 ) ) ;
#17651=CARTESIAN_POINT ( 'NONE',  ( -0.2108831679770959699, 2.036692374882024037, -2.313561348563981657 ) ) ;
#17657=CARTESIAN_POINT ( 'NONE',  ( 1.875925780897500950, 0.3759573520328520768, -2.189106109952672519 ) ) ;
#17658=CARTESIAN_POINT ( 'NONE',  ( 6.707479306934847507, -1.574971382793718178, -1.169550641929931079 ) ) ;
#17662=CARTESIAN_POINT ( 'NONE',  ( -0.06968618116158857567, -1.560424145883563929, -1.276814929289785239 ) ) ;
#17663=CARTESIAN_POINT ( 'NONE',  ( 4.035635273026453085, 1.943268055400270811, -0.6920256600186375229 ) ) ;
#17667=CARTESIAN_POINT ( 'NONE',  ( 6.221928862670094595, -1.039020359566013907, -1.555222851818117924 ) ) ;
#17668=CARTESIAN_POINT ( 'NONE',  ( 5.027816288645148290, -1.483603310789272323, 0.8976219912088311270 ) ) ;
#17669=CARTESIAN_POINT ( 'NONE',  ( 4.352889007613729433, 0.3757914745146764823, -1.699215345876355476 ) ) ;
#17671=CARTESIAN_POINT ( 'NONE',  ( 1.751946580633024331, 2.285858364093972028, -0.1737669427509143383 ) ) ;
#17673=CARTESIAN_POINT ( 'NONE',  ( 5.530836773642837656, -1.889722758269284375, 0.8948517497979097124 ) ) ;
#17674=CARTESIAN_POINT ( 'NONE',  ( 0.3922017905241963476, 1.532332584989907653, -1.020347975915262939 ) ) ;
#17676=CARTESIAN_POINT ( 'NONE',  ( 1.371720446232262081, -0.2986288616722633793, -1.994071132515719658 ) ) ;
#17677=CARTESIAN_POINT ( 'NONE',  ( 0.09403522832084068583, -2.191061582759439297, -0.04926842934906834615 ) ) ;
#17682=CARTESIAN_POINT ( 'NONE',  ( 3.756581929197760683, 2.110411401290826383, 0.2062832702387565331 ) ) ;
#17684=CARTESIAN_POINT ( 'NONE',  ( 5.637271085457097541, -1.648663388651723460, 0.7845467231081537651 ) ) ;
#17690=CARTESIAN_POINT ( 'NONE',  ( 3.533467377359212680, -0.1442520194480846618, 2.014668725452229303 ) ) ;
#17691=CARTESIAN_POINT ( 'NONE',  ( 0.1652458694026041341, -1.881425287724652673, -0.9463707761560661291 ) ) ;
#17693=CARTESIAN_POINT ( 'NONE',  ( 3.643253357272932647, 1.684219189441754416, -0.7917782423425399063 ) ) ;
#17698=CARTESIAN_POINT ( 'NONE',  ( 0.3214396764580421118, -0.1044536432763705502, 2.159311484102262479 ) ) ;
#17702=CARTESIAN_POINT ( 'NONE',  ( 1.159081676615776990, -0.4145447896758222561, -1.683414020171439818 ) ) ;
#17703=CARTESIAN_POINT ( 'NONE',  ( 1.552286559517775499, -1.491368903747305019, -0.8966978864634599367 ) ) ;
#17704=CARTESIAN_POINT ( 'NONE',  ( 6.621674845842873580, -2.240319515690874397, 0.5532079777821105049 ) ) ;
#17707=CARTESIAN_POINT ( 'NONE',  ( 1.932957488262206480, 0.1987776095667900533, 2.051143708757536821 ) ) ;
#17708=CARTESIAN_POINT ( 'NONE',  ( 0.2278875137335881207, -1.799627942332830965, -0.9090566646320766830 ) ) ;
#17712=CARTESIAN_POINT ( 'NONE',  ( 6.315307248462690204, -0.2269180964024133385, 1.856785020699961875 ) ) ;
#17713=CARTESIAN_POINT ( 'NONE',  ( 4.693567934957057375, 1.782326746607498791, -0.6936623114904352239 ) ) ;
#17715=CARTESIAN_POINT ( 'NONE',  ( 6.340462157465731607, 2.182225300935904055, 0.3281612982340698093 ) ) ;
#17719=CARTESIAN_POINT ( 'NONE',  ( 6.463548717370299457, -1.702720583769131490, -1.263627255760652046 ) ) ;
#17721=CARTESIAN_POINT ( 'NONE',  ( 3.979734726549417623, 2.174020839304124042, -0.7740601867209749853 ) ) ;
#17722=CARTESIAN_POINT ( 'NONE',  ( 4.387127823891323608, 0.09410986116351567621, 1.959716250186482434 ) ) ;
#17723=CARTESIAN_POINT ( 'NONE',  ( 2.219515905360454067, 0.3404028402014187549, -1.931851785523025944 ) ) ;
#17727=CARTESIAN_POINT ( 'NONE',  ( 0.6380961361360514283, 2.114605634092497688, -0.1105060169243020224 ) ) ;
#17729=CARTESIAN_POINT ( 'NONE',  ( 0.1285073612291263989, -1.684675954457705682, 0.7431698939026829542 ) ) ;
#17730=CARTESIAN_POINT ( 'NONE',  ( 4.733362013637422372, 0.006437197247223526778, -2.171239809022653677 ) ) ;
#17732=CARTESIAN_POINT ( 'NONE',  ( 2.004293344102888508, -0.9022931611136343344, 1.919180038594799687 ) ) ;
#17737=CARTESIAN_POINT ( 'NONE',  ( 2.108734400483037952, 1.529077776457531401, -1.381789073784354560 ) ) ;
#17740=CARTESIAN_POINT ( 'NONE',  ( 6.509000000000010999, 0.004788705324892603143, 2.000274819378269786 ) ) ;
#17742=CARTESIAN_POINT ( 'NONE',  ( 0.07735805125223117751, 5.721077998510399887, -2.682987299736539377 ) ) ;
#17745=CARTESIAN_POINT ( 'NONE',  ( 4.213462193461685601, 1.537813053725526569, 1.136448645172025262 ) ) ;
#17747=CARTESIAN_POINT ( 'NONE',  ( 1.142281600899584193, 0.9165754381605104584, -2.068608644781688710 ) ) ;
#17749=CARTESIAN_POINT ( 'NONE',  ( 0.7909136568654427935, -0.04542554662571558072, -1.811195533156365611 ) ) ;
#17751=CARTESIAN_POINT ( 'NONE',  ( 2.202218669689899322, 1.248139960717888908, -1.453441320886917243 ) ) ;
#17752=CARTESIAN_POINT ( 'NONE',  ( 3.613788337741298040, 0.5058112091442801272, -2.007490274132675445 ) ) ;
#17755=CARTESIAN_POINT ( 'NONE',  ( 0.5847652604651293329, -0.2391135408384200411, -1.956842742423828829 ) ) ;
#17756=CARTESIAN_POINT ( 'NONE',  ( 5.215425455482871619, -0.2808245750387359796, 1.905809792320038998 ) ) ;
#17757=CARTESIAN_POINT ( 'NONE',  ( 0.4875218067809834466, -0.2886260216827610803, -2.289518885299694606 ) ) ;
#17761=CARTESIAN_POINT ( 'NONE',  ( 5.090308526370699305, 1.063348096890677441, -1.767349029039886110 ) ) ;
#17765=CARTESIAN_POINT ( 'NONE',  ( 5.473694172853372564, 2.030421858957079273, -0.5587401243299906506 ) ) ;
#17767=CARTESIAN_POINT ( 'NONE',  ( 0.8366658991775147713, -1.206067806592339142, 1.805196218089277549 ) ) ;
#17769=CARTESIAN_POINT ( 'NONE',  ( 5.061884429210019576, 2.138887713127162638, -0.3115965683029159883 ) ) ;
#17770=CARTESIAN_POINT ( 'NONE',  ( 5.742833863956755103, 1.946992082993486584, 0.5367204025522700483 ) ) ;
#17772=EDGE_CURVE ( 'NONE', #97632, #77820, #13107, .T. ) ;
#17777=CARTESIAN_POINT ( 'NONE',  ( 3.081267818761534549, 1.592661989535900657, 1.236799713577160231 ) ) ;
#17782=CARTESIAN_POINT ( 'NONE',  ( 4.786082296487640164, -1.021991182799499409, 1.904868704497929333 ) ) ;
#17787=CARTESIAN_POINT ( 'NONE',  ( 5.870720304489429608, -0.2986452421533461465, -1.994069804803912049 ) ) ;
#17789=CARTESIAN_POINT ( 'NONE',  ( 0.2051046121598932848, -0.4657588872633237065, 1.660747436093058083 ) ) ;
#17794=CARTESIAN_POINT ( 'NONE',  ( 6.046149701670225696, 1.868418987705861234, 0.09211505606019491921 ) ) ;
#17795=CARTESIAN_POINT ( 'NONE',  ( -0.005209864377695229073, -1.953240142932886725, -0.4869125064202137199 ) ) ;
#17796=CARTESIAN_POINT ( 'NONE',  ( 6.539320575229257138, 4.699150603835311912, 2.459441311396874497 ) ) ;
#17803=CARTESIAN_POINT ( 'NONE',  ( 1.787894333202539654, 2.028250040683087008, -0.6185522307536188702 ) ) ;
#17804=CARTESIAN_POINT ( 'NONE',  ( 1.317982704262925298, 0.9913799330133238330, -1.755781447868165035 ) ) ;
#17806=CARTESIAN_POINT ( 'NONE',  ( 2.232397805642115873, 1.180933449141470026, -1.373882015996011452 ) ) ;
#17808=CARTESIAN_POINT ( 'NONE',  ( 6.016527291255574283, 1.455332790597754000, -1.598591904487467463 ) ) ;
#17811=CARTESIAN_POINT ( 'NONE',  ( 0.09280537598354164641, 1.668161973260675834, 0.9417010505823987243 ) ) ;
#17819=CARTESIAN_POINT ( 'NONE',  ( 3.959979445722985325, 2.145676688911036578, -0.2621329562078680842 ) ) ;
#17823=CARTESIAN_POINT ( 'NONE',  ( 2.197662576721173266, 1.936918166296027977, -0.8637449004969056654 ) ) ;
#17824=CARTESIAN_POINT ( 'NONE',  ( 6.686557121163758666, -1.791048715316777562, -0.3524728914669760793 ) ) ;
#17825=CARTESIAN_POINT ( 'NONE',  ( 2.811746400649973499, -1.950408978035414354, 0.2857507918755904930 ) ) ;
#17826=CARTESIAN_POINT ( 'NONE',  ( 5.695548698317931091, 1.764485844685494742, -0.7379451211212140205 ) ) ;
#17829=CARTESIAN_POINT ( 'NONE',  ( 5.547300264688804994, 1.737891114709901208, -0.9267001309954668864 ) ) ;
#17830=CARTESIAN_POINT ( 'NONE',  ( 1.025216207372595223, -1.231406509999972254, -1.501593997598904995 ) ) ;
#17838=CARTESIAN_POINT ( 'NONE',  ( 5.742805640131908973, 1.844151595126357179, 0.5056804652876015771 ) ) ;
#17840=CARTESIAN_POINT ( 'NONE',  ( 2.754729969050898841, 0.7443088323898851000, 2.077706851784946185 ) ) ;
#17841=CARTESIAN_POINT ( 'NONE',  ( 1.993488836774780060, 1.919990754028239488, -1.087721427556323617 ) ) ;
#17843=CARTESIAN_POINT ( 'NONE',  ( 0.6449871831117168774, 0.1410837285014763798, 1.907147727228817757 ) ) ;
#17846=CARTESIAN_POINT ( 'NONE',  ( 3.596198176508007105, 0.9334358170956689182, -1.848091447891623051 ) ) ;
#17850=CARTESIAN_POINT ( 'NONE',  ( 1.727627455807039691, -2.035446057602477321, 0.7283451284763039490 ) ) ;
#17851=CARTESIAN_POINT ( 'NONE',  ( 3.439196427729715566, -1.660734982795486481, -1.430121640581414111 ) ) ;
#17858=CARTESIAN_POINT ( 'NONE',  ( 6.504571816962987363, -1.679391772619584833, 0.4319377402999846627 ) ) ;
#17861=CARTESIAN_POINT ( 'NONE',  ( 3.221598570378156001, 0.3083542414583049784, -2.047064864394084971 ) ) ;
#17862=CARTESIAN_POINT ( 'NONE',  ( 5.870749427052773584, -0.3112397890362226249, -2.094129459642315005 ) ) ;
#17865=CARTESIAN_POINT ( 'NONE',  ( 3.256658344530354299, -0.5673638227334516504, -1.885978461452636479 ) ) ;
#17866=CARTESIAN_POINT ( 'NONE',  ( 1.336036003918249948, -1.064896177285217016, -1.588262137521757822 ) ) ;
#17867=CARTESIAN_POINT ( 'NONE',  ( 6.439416457043729558, 0.8834936782941483768, -2.115358923741214259 ) ) ;
#17868=CARTESIAN_POINT ( 'NONE',  ( 2.894927146036041510, 1.565677646668685696, -0.9388022922067614795 ) ) ;
#17874=CARTESIAN_POINT ( 'NONE',  ( 3.568611400213494989, 0.7284950617309441379, 1.876934371664749301 ) ) ;
#17875=CARTESIAN_POINT ( 'NONE',  ( 4.135565103414404753, 1.848670044762780407, -0.6568835154602686854 ) ) ;
#17879=CARTESIAN_POINT ( 'NONE',  ( 0.4157161284131759005, -1.121801286243618190, -1.764121917367883263 ) ) ;
#17880=CARTESIAN_POINT ( 'NONE',  ( 5.805463146582474643, -0.4265672176911333713, 1.717519531449087866 ) ) ;
#17882=CARTESIAN_POINT ( 'NONE',  ( 2.308753661914957345, 1.958203289975643191, 0.9839491227633669901 ) ) ;
#17883=CARTESIAN_POINT ( 'NONE',  ( 6.562468561866369399, -1.594522334811569131, -0.6977961348336658709 ) ) ;
#17887=CARTESIAN_POINT ( 'NONE',  ( 0.5215560022201523038, -0.9183498723843477318, -1.459886522650925000 ) ) ;
#17888=CARTESIAN_POINT ( 'NONE',  ( 1.019433853822170777, 2.295598214472119203, -0.1149376033552674814 ) ) ;
#17889=CARTESIAN_POINT ( 'NONE',  ( 0.8201894534925309177, 1.301127354658284663, -1.763390660798454634 ) ) ;
#17890=CARTESIAN_POINT ( 'NONE',  ( 3.369938178094655346, 2.153121441420174698, -0.4834393813165636100 ) ) ;
#17891=CARTESIAN_POINT ( 'NONE',  ( 0.7257146478014552260, 0.2145687282662836204, -2.160472036209131197 ) ) ;
#17893=CARTESIAN_POINT ( 'NONE',  ( 2.817688460867060485, -1.425471633543059724, -1.565750481055405263 ) ) ;
#17894=CARTESIAN_POINT ( 'NONE',  ( 6.620655732516651071, 1.241313378043694238, 2.288056600130850882 ) ) ;
#17895=CARTESIAN_POINT ( 'NONE',  ( 5.403319659429405952, 1.574929826682970990, 1.109050863186450853 ) ) ;
#17897=CARTESIAN_POINT ( 'NONE',  ( 2.085838899777220590, -0.9763249575661275825, 2.074189754910108263 ) ) ;
#17902=CARTESIAN_POINT ( 'NONE',  ( 4.617978872065289231, -0.5927926152728602016, 2.140694073679518805 ) ) ;
#17909=CARTESIAN_POINT ( 'NONE',  ( 3.305314717767214638, 1.277042846462652204, -1.560500556308255238 ) ) ;
#17911=CARTESIAN_POINT ( 'NONE',  ( 0.5849265108320426121, 1.972682758258193392, 0.6021488627185996867 ) ) ;
#17916=CARTESIAN_POINT ( 'NONE',  ( 3.591891977137162684, -2.188917585555647527, -0.1077332384093188100 ) ) ;
#17917=CARTESIAN_POINT ( 'NONE',  ( 1.389296306420295224, -0.7283806465635984662, -1.880434191983325398 ) ) ;
#17918=CARTESIAN_POINT ( 'NONE',  ( 1.276629239279066574, 1.701104413791530767, -0.7050613402737049284 ) ) ;
#17919=CARTESIAN_POINT ( 'NONE',  ( 4.950848118218736715, -1.935628577297190400, -1.227853487085520001 ) ) ;
#17920=CARTESIAN_POINT ( 'NONE',  ( 4.611176429654996412, -1.805050139478355353, 0.3618648703537508671 ) ) ;
#17924=CARTESIAN_POINT ( 'NONE',  ( 4.436427218767265757, 1.790408935156896586, 0.3557191534368231434 ) ) ;
#17925=CARTESIAN_POINT ( 'NONE',  ( 4.412732527109735514, -1.242725882911545510, -1.587838301257207041 ) ) ;
#17927=CARTESIAN_POINT ( 'NONE',  ( 5.137693465899466183, -1.596169073733178845, -1.603756505840604918 ) ) ;
#17929=CARTESIAN_POINT ( 'NONE',  ( 0.04767123857605212733, -1.629476508726154016, -1.334019646271035198 ) ) ;
#17930=CARTESIAN_POINT ( 'NONE',  ( 4.668459276380106715, -0.8822503692092443783, -1.873099891353036561 ) ) ;
#17935=CARTESIAN_POINT ( 'NONE',  ( 2.332535780611888043, 1.868688736674573247, 0.4679572130895108817 ) ) ;
#17937=CARTESIAN_POINT ( 'NONE',  ( 0.5198876536083548716, 1.948639688611382148, -0.2852860490613322031 ) ) ;
#17941=CARTESIAN_POINT ( 'NONE',  ( 0.5980879788009090259, 1.428637019467562830, 1.567290143595565066 ) ) ;
#17942=CARTESIAN_POINT ( 'NONE',  ( 1.494693441997055894, -1.183060725354843079, 1.879997432091018217 ) ) ;
#17943=CARTESIAN_POINT ( 'NONE',  ( 3.733512407637301855, -1.946585179706640467, 0.8041552576890409476 ) ) ;
#17946=CARTESIAN_POINT ( 'NONE',  ( 3.016010921186715432, 1.952665002612500533, -0.1895750030070641190 ) ) ;
#17953=CARTESIAN_POINT ( 'NONE',  ( 1.072698285844303934, 0.8645715524648779349, 1.936551149067309741 ) ) ;
#17956=CARTESIAN_POINT ( 'NONE',  ( 4.650807877244386823, -0.4278111053654386486, -1.914496481071884970 ) ) ;
#17957=CARTESIAN_POINT ( 'NONE',  ( 3.573254463033649131, 0.05508235185803719847, -2.161170636208443963 ) ) ;
#17958=CARTESIAN_POINT ( 'NONE',  ( 1.452429406588066740, -1.579491434881035827, -0.9459884711465746943 ) ) ;
#17962=CARTESIAN_POINT ( 'NONE',  ( 4.593551391122507432, -1.740074876368927104, -0.03866795590094784102 ) ) ;
#17966=CARTESIAN_POINT ( 'NONE',  ( 2.307699607974790901, -0.4742087202370263155, 2.108885336910087283 ) ) ;
#17967=ADVANCED_FACE ( 'NONE', ( #1985 ), #120176, .F. ) ;
#17968=CARTESIAN_POINT ( 'NONE',  ( 4.815779736370030761, -1.620933320526974031, 1.198678058543983571 ) ) ;
#17970=CARTESIAN_POINT ( 'NONE',  ( 1.692469166403000491, -2.151312531270420436, -0.2117842694067117448 ) ) ;
#17971=CARTESIAN_POINT ( 'NONE',  ( 3.907068546088189986, 1.690197745946390162, 1.014639218175046764 ) ) ;
#17973=CARTESIAN_POINT ( 'NONE',  ( 3.948723843360758323, -1.616405859212793894, -1.076207510925797139 ) ) ;
#17982=CARTESIAN_POINT ( 'NONE',  ( 0.2357703454196959370, -2.016519153289020760, 0.8967723332334791575 ) ) ;
#17984=CARTESIAN_POINT ( 'NONE',  ( 5.172687041346638814, 1.355624813549320740, -1.418227474788292364 ) ) ;
#17985=CARTESIAN_POINT ( 'NONE',  ( 1.389296306420295224, -0.7283806465635984662, -1.880434191983325398 ) ) ;
#17987=CARTESIAN_POINT ( 'NONE',  ( 3.889952640533121286, -2.111394073168832097, 0.1598612332101984890 ) ) ;
#17991=CARTESIAN_POINT ( 'NONE',  ( 4.206863059814883066, -0.3125640686512491384, 1.814249101404527220 ) ) ;
#17996=CARTESIAN_POINT ( 'NONE',  ( 4.640951271726033056, 2.030106984047326701, 0.6129599860185754867 ) ) ;
#17999=EDGE_CURVE ( 'NONE', #141519, #119587, #87926, .T. ) ;
#18000=CARTESIAN_POINT ( 'NONE',  ( 5.993449436079309578, 1.557461279572001756, 1.349564693925601189 ) ) ;
#18002=CARTESIAN_POINT ( 'NONE',  ( 1.222862307070234911, -1.680409034227359211, -0.8001750615637763797 ) ) ;
#18003=CARTESIAN_POINT ( 'NONE',  ( 2.858754248528099229, 0.2676582106064147593, -1.821554178878769470 ) ) ;
#18008=CARTESIAN_POINT ( 'NONE',  ( 1.664966938652842954, -1.558911317520403239, 1.562347339584921002 ) ) ;
#18009=CARTESIAN_POINT ( 'NONE',  ( 5.413438844936455219, -0.3396298981525199823, 2.236681904191807568 ) ) ;
#18010=CARTESIAN_POINT ( 'NONE',  ( 3.573454097414618946, 1.463926983822515293, 1.387100322000796027 ) ) ;
#18012=CARTESIAN_POINT ( 'NONE',  ( 4.359482725938978120, -1.404519563743265920, -1.144221460762798737 ) ) ;
#18013=CARTESIAN_POINT ( 'NONE',  ( 5.260912935490944520, -0.05370519216219872549, -1.915158585242337397 ) ) ;
#18015=CARTESIAN_POINT ( 'NONE',  ( 3.748864756286158340, -1.612500686720008236, 1.134000162313458793 ) ) ;
#18016=CARTESIAN_POINT ( 'NONE',  ( 5.278141497218024725, -1.038406966791558528, 1.555765341417144842 ) ) ;
#18017=CARTESIAN_POINT ( 'NONE',  ( 4.422197255734514165, 0.8761312318771010688, 1.641894029917531084 ) ) ;
#18020=CARTESIAN_POINT ( 'NONE',  ( 5.383597848809928088, 1.190821987996647513, 1.309499010278234898 ) ) ;
#18021=CARTESIAN_POINT ( 'NONE',  ( -0.2234322562767385167, -0.4468160588090731022, -1.973564571300358228 ) ) ;
#18023=CARTESIAN_POINT ( 'NONE',  ( 2.174573150871310201, -1.294977634586411908, 1.660803824364719405 ) ) ;
#18027=CARTESIAN_POINT ( 'NONE',  ( 3.199588043238619228, 1.915454767000431602, -0.9102714984489732597 ) ) ;
#18029=CARTESIAN_POINT ( 'NONE',  ( 2.250265822158686646, 0.9482326530925830887, -1.783330763309778577 ) ) ;
#18031=CARTESIAN_POINT ( 'NONE',  ( 6.620655732516649294, 0.5971256128398574337, 1.879834161342401666 ) ) ;
#18035=CARTESIAN_POINT ( 'NONE',  ( 1.915512222264357467, -0.2666219456287990952, 2.145042957367573777 ) ) ;
#18036=CARTESIAN_POINT ( 'NONE',  ( 6.890000000000010338, 2.965158640989657979, 2.452917560796507246 ) ) ;
#18043=CARTESIAN_POINT ( 'NONE',  ( 1.312353134292881141, 1.468346937154514364, -1.627112938194043235 ) ) ;
#18045=CARTESIAN_POINT ( 'NONE',  ( 1.833286743572108968, 0.2227676567047157941, 2.251508545315301646 ) ) ;
#18055=CARTESIAN_POINT ( 'NONE',  ( 3.620126565017945275, 1.124893713931356842, -1.366185836280229715 ) ) ;
#18056=CARTESIAN_POINT ( 'NONE',  ( 6.211994372536747022, -2.190858219723303080, 0.2640275128017176565 ) ) ;
#18059=CARTESIAN_POINT ( 'NONE',  ( 5.589470316598125876, -0.4871849528341637980, 1.956566939648955339 ) ) ;
#18061=CARTESIAN_POINT ( 'NONE',  ( 2.008475284031425723, 1.387998011844304491, -1.254312187223500796 ) ) ;
#18062=CARTESIAN_POINT ( 'NONE',  ( 2.413015750098276513, -1.603085927076562500, 1.310038033242977518 ) ) ;
#18064=CARTESIAN_POINT ( 'NONE',  ( 2.250135261179100343, 0.8981609309555339538, -1.688322754368525747 ) ) ;
#18070=CARTESIAN_POINT ( 'NONE',  ( 0.07037084582631887575, 0.7337836260858083826, 1.766209603411242668 ) ) ;
#18072=CARTESIAN_POINT ( 'NONE',  ( 1.152704166800899932, -0.4732522875653189520, -1.903817266927515961 ) ) ;
#18074=CARTESIAN_POINT ( 'NONE',  ( 0.2630457479233569984, -2.015603748724136945, -0.05229424383911692592 ) ) ;
#18076=CARTESIAN_POINT ( 'NONE',  ( 5.010073305087408002, -0.7609581946756528437, 1.979555329295646260 ) ) ;
#18078=CARTESIAN_POINT ( 'NONE',  ( 6.591095686763909001, 1.716256228956919871, -0.9697327587238188107 ) ) ;
#18080=CARTESIAN_POINT ( 'NONE',  ( 1.511978199970403836, -0.6742157057700901568, 1.897102442587648374 ) ) ;
#18082=CARTESIAN_POINT ( 'NONE',  ( 1.230240178466317724, 2.114980979692267393, 0.09988113581482771508 ) ) ;
#18084=CARTESIAN_POINT ( 'NONE',  ( 2.699741690289765295, -1.532448122638006671, -1.392287113214360827 ) ) ;
#18088=CARTESIAN_POINT ( 'NONE',  ( 5.402318495819277366, 1.583515501651384438, -1.365094957383119700 ) ) ;
#18090=CARTESIAN_POINT ( 'NONE',  ( 4.524309061075334704, 1.122661849025725189, -1.439470297551891154 ) ) ;
#18091=CARTESIAN_POINT ( 'NONE',  ( 2.631291878999729938, -0.1756591012599724722, 1.802909387868474766 ) ) ;
#18096=CARTESIAN_POINT ( 'NONE',  ( 5.473716482686670659, 2.128106746890707335, -0.5837492795209007213 ) ) ;
#18099=CARTESIAN_POINT ( 'NONE',  ( 3.686107007616833631, 1.064666855108999721, 1.588282736317746302 ) ) ;
#18107=CARTESIAN_POINT ( 'NONE',  ( -0.1237769027084348328, -0.1346504581853508187, -1.811164470923332104 ) ) ;
#18110=CARTESIAN_POINT ( 'NONE',  ( 3.883945074633635031, -0.9243716352356041721, 1.626130415258054018 ) ) ;
#18116=CARTESIAN_POINT ( 'NONE',  ( 6.455931442665615805, -0.7031469350025701948, 1.947301169641938223 ) ) ;
#18117=CARTESIAN_POINT ( 'NONE',  ( 2.689077551358230789, 1.704951624378052033, 1.076298511635757738 ) ) ;
#18120=DIRECTION ( 'NONE',  ( -0.9999980456341538426, 0.000000000000000000, -0.001977050295941298105 ) ) ;
#18121=CARTESIAN_POINT ( 'NONE',  ( 2.713028398602938651, -0.2137989841624072795, 2.180988865010752509 ) ) ;
#18122=CARTESIAN_POINT ( 'NONE',  ( 6.164658409365946667, -1.287482145768016117, 1.294691480910937553 ) ) ;
#18129=CARTESIAN_POINT ( 'NONE',  ( 3.843160323004328305, 0.6166970922517557296, -1.735048075492843456 ) ) ;
#18130=CARTESIAN_POINT ( 'NONE',  ( 0.2936080233231981862, 1.877589464902774674, -0.7265071302150533095 ) ) ;
#18131=CARTESIAN_POINT ( 'NONE',  ( 3.603114471349005754, 1.037088744013005659, -2.051189238963199379 ) ) ;
#18133=CARTESIAN_POINT ( 'NONE',  ( 1.182201811662712210, 1.114302846955270709, -1.490276101724023583 ) ) ;
#18137=CARTESIAN_POINT ( 'NONE',  ( 4.675980034926481288, 1.890745994642643479, -0.2862527531290667837 ) ) ;
#18142=CARTESIAN_POINT ( 'NONE',  ( 3.421503388043937832, -1.247306758965301521, -1.677755357943153447 ) ) ;
#18143=CARTESIAN_POINT ( 'NONE',  ( 2.219420098953532428, -1.815089452277141691, 0.4520615115926190919 ) ) ;
#18146=CARTESIAN_POINT ( 'NONE',  ( 5.864778394761136049, 0.1288883805774850844, -1.836796581567698539 ) ) ;
#18151=CARTESIAN_POINT ( 'NONE',  ( 3.387030231456603424, 1.558874866368621159, -0.7386201850746020314 ) ) ;
#18153=CARTESIAN_POINT ( 'NONE',  ( 6.410767893487317792, 1.638320036227768783, -1.478771730184471389 ) ) ;
#18154=CARTESIAN_POINT ( 'NONE',  ( 6.983263157960391432, 4.691677264508577139, 2.616375093613742209 ) ) ;
#18156=CARTESIAN_POINT ( 'NONE',  ( 5.278266929526361118, -1.155484533919543422, -1.837868763204909994 ) ) ;
#18157=CARTESIAN_POINT ( 'NONE',  ( 2.842213963582499670, 1.811911227886909614, 0.2232855069103783507 ) ) ;
#18159=CARTESIAN_POINT ( 'NONE',  ( 6.069547426979996274, 1.461697874074740389, 1.532048495917796016 ) ) ;
#18161=CARTESIAN_POINT ( 'NONE',  ( 6.093372230586791893, -0.7761969640797984349, 2.157113249652943932 ) ) ;
#18164=CARTESIAN_POINT ( 'NONE',  ( 1.172698094321134477, 0.8626872041959359194, 1.937259058979395654 ) ) ;
#18170=CARTESIAN_POINT ( 'NONE',  ( 6.842638762948665132, -2.127444276778973631, -0.4322993451541176091 ) ) ;
#18171=CARTESIAN_POINT ( 'NONE',  ( 6.883263157960350043, 2.968548739964393945, 2.406833999121655854 ) ) ;
#18173=CARTESIAN_POINT ( 'NONE',  ( 1.612303553688280600, -0.7442547213242669546, 2.093046284049724370 ) ) ;
#18175=CARTESIAN_POINT ( 'NONE',  ( 6.604150280000163242, -0.1430408514614608939, 1.983920101186954721 ) ) ;
#18177=CARTESIAN_POINT ( 'NONE',  ( 4.100476343641854093, 2.052162271747024924, 0.2072667206600986300 ) ) ;
#18183=CARTESIAN_POINT ( 'NONE',  ( -0.02340959012393610192, -0.1578203421408593821, -2.056509962333047614 ) ) ;
#18184=CARTESIAN_POINT ( 'NONE',  ( 4.412732527109735514, -1.242725882911545510, -1.587838301257207041 ) ) ;
#18185=CARTESIAN_POINT ( 'NONE',  ( 4.335397732480402055, 0.7831895168094182846, -1.666506522714307437 ) ) ;
#18188=CARTESIAN_POINT ( 'NONE',  ( 1.166562959395722077, -1.556812811267356711, -0.7427251802107991407 ) ) ;
#18189=CARTESIAN_POINT ( 'NONE',  ( 0.2336117360935245635, 0.6279853779636718203, -1.916355031878452797 ) ) ;
#18190=CARTESIAN_POINT ( 'NONE',  ( 1.372188323541504218, -0.3435771540031757332, -2.272792483656468576 ) ) ;
#18192=CARTESIAN_POINT ( 'NONE',  ( 0.9314073880264511773, 0.1673361042086803641, 2.256242939573564144 ) ) ;
#18193=CARTESIAN_POINT ( 'NONE',  ( 3.580784747083717523, -2.029690618531124091, -0.5617794247858574064 ) ) ;
#18197=CARTESIAN_POINT ( 'NONE',  ( 0.000000000000000000, 2.344942989059404237, -2.501676308668091764 ) ) ;
#18203=CARTESIAN_POINT ( 'NONE',  ( 5.010122972300034228, -0.7987708819462059351, 2.073016528135694703 ) ) ;
#18204=CARTESIAN_POINT ( 'NONE',  ( 4.031328258368102269, -1.510625130563835627, -1.587819133214096734 ) ) ;
#18209=CARTESIAN_POINT ( 'NONE',  ( 6.609999999999971010, 7.629137130509032971, 2.879999999999991456 ) ) ;
#18211=CARTESIAN_POINT ( 'NONE',  ( 5.502226937873657242, -0.9515977829631333540, 1.895136135177949877 ) ) ;
#18215=CARTESIAN_POINT ( 'NONE',  ( 6.262596564776618635, -1.532251275270900326, 1.525113613579494709 ) ) ;
#18217=CARTESIAN_POINT ( 'NONE',  ( 5.952668924537682038, -1.582617586749142102, -0.9407850039931386910 ) ) ;
#18219=CARTESIAN_POINT ( 'NONE',  ( 1.294060738426667134, 1.423250580516822072, -1.001416416642088469 ) ) ;
#18225=CARTESIAN_POINT ( 'NONE',  ( 4.803692121107413726, -0.5798474923815257753, 2.082409481564663434 ) ) ;
#18229=CARTESIAN_POINT ( 'NONE',  ( 4.627887939457571598, -1.327398817707679868, -1.706084338546076662 ) ) ;
#18231=CARTESIAN_POINT ( 'NONE',  ( 5.852796007109359877, -1.555770171409420977, 1.210649060634989560 ) ) ;
#18232=CARTESIAN_POINT ( 'NONE',  ( 4.657415279524609986, -0.3804069660688877974, -1.691394979786196684 ) ) ;
#18234=CARTESIAN_POINT ( 'NONE',  ( 1.927518781310177509, -1.434474475899261581, -1.656937093973806396 ) ) ;
#18235=CARTESIAN_POINT ( 'NONE',  ( 1.659631924955577098, -1.980043282969433882, -1.184870857304116898 ) ) ;
#18236=CARTESIAN_POINT ( 'NONE',  ( 5.307911771147946212, -2.051258671218537444, 0.1976249854395220606 ) ) ;
#18237=CARTESIAN_POINT ( 'NONE',  ( 0.05839466612742905127, -1.734069842965625385, -0.8743347890363247776 ) ) ;
#18241=CARTESIAN_POINT ( 'NONE',  ( 3.322626870553476941, -0.8629183168706102691, -1.937285153019531414 ) ) ;
#18243=CARTESIAN_POINT ( 'NONE',  ( 1.512342498431101134, -1.897697209584522815, 0.6819976561535444626 ) ) ;
#18245=CARTESIAN_POINT ( 'NONE',  ( 4.471826267013489620, 2.141383520707430321, -0.5327586567505787629 ) ) ;
#18247=CARTESIAN_POINT ( 'NONE',  ( 1.832617572280154539, -1.765004919984759058, -0.5899526775028116621 ) ) ;
#18248=CARTESIAN_POINT ( 'NONE',  ( -0.02880301295727759683, -0.006976478922920535501, -2.273770288744044521 ) ) ;
#18252=CARTESIAN_POINT ( 'NONE',  ( 6.925078400183578786, 0.5640289027524867382, 2.196098379985710114 ) ) ;
#18255=CARTESIAN_POINT ( 'NONE',  ( 3.748945967280458369, -1.685778541264292274, 1.185220002557571206 ) ) ;
#18259=CARTESIAN_POINT ( 'NONE',  ( 2.473312253293189489, -1.758384921082667862, -0.9933899200572825494 ) ) ;
#18262=CARTESIAN_POINT ( 'NONE',  ( 1.498976495884283056, 1.685333290510768744, -1.185852821821014702 ) ) ;
#18267=CARTESIAN_POINT ( 'NONE',  ( -0.1408020194049781904, -0.005144001661201018025, -2.100147592658160089 ) ) ;
#18268=CARTESIAN_POINT ( 'NONE',  ( 0.9898993202219902310, -0.4452471680344311511, -1.786356756097874587 ) ) ;
#18269=AXIS2_PLACEMENT_3D ( 'NONE', #199734, #84933, #212789 ) ;
#18270=CARTESIAN_POINT ( 'NONE',  ( 5.777994779145079640, 1.311685685134782231, 1.774619457157788904 ) ) ;
#18272=CARTESIAN_POINT ( 'NONE',  ( 1.827627302340195437, -2.036028831988645926, 0.7264203155534704193 ) ) ;
#18274=CARTESIAN_POINT ( 'NONE',  ( 2.009000277268524481, 0.004839059525654776373, 2.016708403978189956 ) ) ;
#18277=CARTESIAN_POINT ( 'NONE',  ( 4.891463287051191600, 1.460324016362057886, 1.324601213698357149 ) ) ;
#18278=CARTESIAN_POINT ( 'NONE',  ( 3.186732694495420848, 1.586669336078951664, -1.244385354607212335 ) ) ;
#18282=CARTESIAN_POINT ( 'NONE',  ( 6.639294477394681593, -1.882217795646949687, 0.9450163710809048601 ) ) ;
#18283=CARTESIAN_POINT ( 'NONE',  ( 5.705552448923417508, -1.629793913574303588, -1.276656259598766940 ) ) ;
#18287=CARTESIAN_POINT ( 'NONE',  ( 5.801037524829370184, -0.3003419868748377630, -1.997221587554024458 ) ) ;
#18289=CARTESIAN_POINT ( 'NONE',  ( 0.7958482667242804398, -1.455889974409400045, -1.461266501696573794 ) ) ;
#18298=CARTESIAN_POINT ( 'NONE',  ( 2.576841123524225452, 1.419588041764899611, -1.642854796848471244 ) ) ;
#18301=CARTESIAN_POINT ( 'NONE',  ( 2.542321706073047416, -1.529623444112483632, 1.024600984555257277 ) ) ;
#18303=CARTESIAN_POINT ( 'NONE',  ( 4.423480980095358284, -1.348712413769267426, -1.727291790683552541 ) ) ;
#18305=CARTESIAN_POINT ( 'NONE',  ( 4.469752058069711431, 2.195618827641317772, -0.5456854893412068641 ) ) ;
#18313=CARTESIAN_POINT ( 'NONE',  ( 0.1800360811037614583, -1.714963048871451790, -0.4369287763777151556 ) ) ;
#18314=CARTESIAN_POINT ( 'NONE',  ( 3.615888430654935259, -0.5820857220382947839, 1.927115488332105553 ) ) ;
#18317=CARTESIAN_POINT ( 'NONE',  ( 3.522586592847714471, 1.337535325648725459, -1.626654721158872885 ) ) ;
#18318=CARTESIAN_POINT ( 'NONE',  ( 0.6849900193761117029, 1.566649212177973149, 1.102054418794357948 ) ) ;
#18321=CARTESIAN_POINT ( 'NONE',  ( 2.295301284060722313, -1.760697607696968037, 0.8827641120334356328 ) ) ;
#18322=CARTESIAN_POINT ( 'NONE',  ( 0.8834254411415434216, 1.253375741028007084, 1.388844808110502038 ) ) ;
#18323=CARTESIAN_POINT ( 'NONE',  ( 0.6253529088778920775, 0.1960189665039281104, -1.952063659030291998 ) ) ;
#18324=CARTESIAN_POINT ( 'NONE',  ( 6.451413702892147661, -1.613775625804831693, 0.8233398690262339059 ) ) ;
#18328=CARTESIAN_POINT ( 'NONE',  ( 5.541831131927607679, 0.7570117910807551143, -1.710825945835430462 ) ) ;
#18332=CARTESIAN_POINT ( 'NONE',  ( 5.436411051413860385, -1.154718516627372127, 1.718110687276501958 ) ) ;
#18344=CARTESIAN_POINT ( 'NONE',  ( 5.652778587040098834, -0.4750822840141955550, -1.903360745478323679 ) ) ;
#18347=CARTESIAN_POINT ( 'NONE',  ( 2.847029653296664353, -1.038834691150035461, 1.727737368502464621 ) ) ;
#18348=CARTESIAN_POINT ( 'NONE',  ( 2.799894175352398484, -0.9483327596419667271, -1.664474063330185105 ) ) ;
#18351=CARTESIAN_POINT ( 'NONE',  ( 0.9607770615731696662, -1.983481723135366304, -0.9323335341336475013 ) ) ;
#18352=CARTESIAN_POINT ( 'NONE',  ( 0.2335667940003049725, 0.6933325534057503958, -2.235178663643789143 ) ) ;
#18353=CARTESIAN_POINT ( 'NONE',  ( 3.655401173194738007, 0.4573680094964555076, -1.813624142381641491 ) ) ;
#18357=CARTESIAN_POINT ( 'NONE',  ( 4.165693581912960575, 1.384238758890417031, 1.602101081018918904 ) ) ;
#18359=CARTESIAN_POINT ( 'NONE',  ( 5.723117673755029777, -1.870111591731966616, -0.8886290660751752224 ) ) ;
#18360=CARTESIAN_POINT ( 'NONE',  ( 2.261376066768826743, 2.049819659885134371, -0.4107522398083974791 ) ) ;
#18361=CARTESIAN_POINT ( 'NONE',  ( 6.620655732516659064, 2.000981103421325180, 2.575746817850287140 ) ) ;
#18362=CARTESIAN_POINT ( 'NONE',  ( 0.9204217893557011809, 1.591181625417271039, 0.6660807200309772913 ) ) ;
#18363=EDGE_LOOP ( 'NONE', ( #199280, #6005, #5034, #141782 ) ) ;
#18372=CARTESIAN_POINT ( 'NONE',  ( 0.1174177504974990710, -0.4853618992130321885, 1.745175170155540245 ) ) ;
#18380=CARTESIAN_POINT ( 'NONE',  ( 0.2279634046833027561, 1.910523547013969869, 0.1400250592105151126 ) ) ;
#18381=CARTESIAN_POINT ( 'NONE',  ( 0.4871770963560326240, -1.998059126451703138, -0.7104936405118513765 ) ) ;
#18388=CARTESIAN_POINT ( 'NONE',  ( 4.522284192717240359, 0.9245163773116799044, 1.738918859443546516 ) ) ;
#18389=CARTESIAN_POINT ( 'NONE',  ( 1.102369588802411426, -0.9501182663193027400, 1.895776817140030213 ) ) ;
#18393=CARTESIAN_POINT ( 'NONE',  ( 6.316381784907312280, 2.043361914081378128, 0.7923855730916644635 ) ) ;
#18395=CARTESIAN_POINT ( 'NONE',  ( 4.788067677947292822, -0.9085903742032475083, 1.698673095886160000 ) ) ;
#18397=CARTESIAN_POINT ( 'NONE',  ( -0.1409997244346088141, -0.002808977843308038680, -2.000147647483838220 ) ) ;
#18398=CARTESIAN_POINT ( 'NONE',  ( 1.295869073816724226, 1.673045085319382119, 1.439284050222865652 ) ) ;
#18399=PLANE ( 'NONE',  #62028 ) ;
#18404=CARTESIAN_POINT ( 'NONE',  ( 6.666861335811934630, 1.461617314166022474, -1.320220550599479070 ) ) ;
#18405=CARTESIAN_POINT ( 'NONE',  ( 0.4154419552040686248, -1.039972057064937783, -1.639973222157356636 ) ) ;
#18406=CARTESIAN_POINT ( 'NONE',  ( 6.802148291397191571, -2.057678525504004430, 1.024270743344313672 ) ) ;
#18408=CARTESIAN_POINT ( 'NONE',  ( 4.856225966575771658, -1.860502807761035715, -0.04838197303517684927 ) ) ;
#18414=CARTESIAN_POINT ( 'NONE',  ( 0.2577194443907256383, 2.166829308800602316, -0.3276212646995610989 ) ) ;
#18420=CARTESIAN_POINT ( 'NONE',  ( 0.7678472254676466102, 0.8974085622692473674, 1.589837017038860045 ) ) ;
#18423=CARTESIAN_POINT ( 'NONE',  ( 3.234723362560991244, 1.734343004352358664, -0.003563068559135627086 ) ) ;
#18428=CARTESIAN_POINT ( 'NONE',  ( 6.639283661800273961, -1.628176093627232479, 0.8261057939347238310 ) ) ;
#18429=CARTESIAN_POINT ( 'NONE',  ( 4.065250617491710905, 1.680331827152386159, 1.012218702928203706 ) ) ;
#18432=CARTESIAN_POINT ( 'NONE',  ( 5.197945112634200449, 1.424400718755761908, 1.570990128125760554 ) ) ;
#18436=CARTESIAN_POINT ( 'NONE',  ( 2.834898843300116766, -1.979765732921334731, -0.6052725283285932401 ) ) ;
#18440=CARTESIAN_POINT ( 'NONE',  ( 3.182589804937531852, 1.813683736837278460, 1.412227471172630588 ) ) ;
#18448=CARTESIAN_POINT ( 'NONE',  ( 4.570513122935188299, 0.7371126809179430195, 1.764830652192488580 ) ) ;
#18450=CARTESIAN_POINT ( 'NONE',  ( 5.315364200056264643, -0.2495996188201006494, 1.706489999720143480 ) ) ;
#18451=CARTESIAN_POINT ( 'NONE',  ( 3.028530041973789277, 0.4946322284519070744, 1.954779462066410956 ) ) ;
#18452=CARTESIAN_POINT ( 'NONE',  ( 5.186298777384058312, 1.878100352198919465, 1.325219426413627000 ) ) ;
#18454=CARTESIAN_POINT ( 'NONE',  ( 0.5048604690408053930, -0.7474223562033958101, -2.076596198196341003 ) ) ;
#18456=CARTESIAN_POINT ( 'NONE',  ( 5.817594836490700416, -1.726241941513080747, 0.3891773745644273030 ) ) ;
#18458=CARTESIAN_POINT ( 'NONE',  ( 2.080407636089614432, -2.248563537884174846, -0.4446712507181517782 ) ) ;
#18459=CARTESIAN_POINT ( 'NONE',  ( 0.3568325553494673397, 1.722114113718915984, -0.2502821355834724537 ) ) ;
#18464=CARTESIAN_POINT ( 'NONE',  ( 0.1862956123577602652, -1.336862347539343965, -1.711682565949741885 ) ) ;
#18465=CARTESIAN_POINT ( 'NONE',  ( 1.217982839071569012, 0.9896824804975331569, -1.756856037137774162 ) ) ;
#18467=CARTESIAN_POINT ( 'NONE',  ( 5.162690889178682241, -1.394081347390314640, 1.329872870702011545 ) ) ;
#18469=CARTESIAN_POINT ( 'NONE',  ( 2.637233524875877588, 2.093239256532848369, 0.7440790952397638991 ) ) ;
#18476=CARTESIAN_POINT ( 'NONE',  ( 4.317713577401066871, 1.066398661528572989, -1.375396103214795218 ) ) ;
#18477=CARTESIAN_POINT ( 'NONE',  ( 2.400770673373255448, 0.4268909467371252431, 1.914702609522442867 ) ) ;
#18485=CARTESIAN_POINT ( 'NONE',  ( 0.4673242579315056155, 1.793762616230053508, 1.018268840648499207 ) ) ;
#18488=CARTESIAN_POINT ( 'NONE',  ( 1.042281785820580176, 0.9147803334835495903, -2.069518175336809929 ) ) ;
#18491=CARTESIAN_POINT ( 'NONE',  ( 2.688565094423268853, -0.3157439183511835945, -1.843535313746543336 ) ) ;
#18492=CARTESIAN_POINT ( 'NONE',  ( 0.9142546942676577082, -1.099255453910731983, -1.341178637715144673 ) ) ;
#18494=CARTESIAN_POINT ( 'NONE',  ( 5.021103811603734535, -2.081066139062941023, 0.6872292908843835590 ) ) ;
#18495=CARTESIAN_POINT ( 'NONE',  ( 5.403480793235289070, 1.882684667239397758, 1.334102933689439663 ) ) ;
#18496=CARTESIAN_POINT ( 'NONE',  ( 1.815377929200719720, -0.2531822047686766441, 2.045215655110666830 ) ) ;
#18497=CARTESIAN_POINT ( 'NONE',  ( 3.117060223387691398, -1.871409496450952226, 0.5184039432134399661 ) ) ;
#18499=CARTESIAN_POINT ( 'NONE',  ( 5.536355731483205922, 1.842701317132239724, 0.3206550288221421963 ) ) ;
#18500=CARTESIAN_POINT ( 'NONE',  ( 1.593750000000000666, -1.895863743164122983, -0.7852924748298991675 ) ) ;
#18502=CARTESIAN_POINT ( 'NONE',  ( 0.1922019376490837483, -1.058930769078871403, -1.372993611190379104 ) ) ;
#18506=CARTESIAN_POINT ( 'NONE',  ( 4.254529844270301453, 1.955172953530256219, -0.4926405443339901269 ) ) ;
#18510=CARTESIAN_POINT ( 'NONE',  ( 1.857752496991037061, 1.820901040755190214, -0.1330985588276211995 ) ) ;
#18519=CARTESIAN_POINT ( 'NONE',  ( 0.1057309665696047341, 1.499486454312322525, 1.353398366655131246 ) ) ;
#18520=CARTESIAN_POINT ( 'NONE',  ( 0.5750489506927083383, -1.533040007955801531, 1.465245631482835043 ) ) ;
#18524=CARTESIAN_POINT ( 'NONE',  ( 4.944241404475337553, 2.055231674695843669, 0.1536075889326995458 ) ) ;
#18525=CARTESIAN_POINT ( 'NONE',  ( 5.520157785563180930, -1.821743191724470634, 0.8647220171385737730 ) ) ;
#18533=CARTESIAN_POINT ( 'NONE',  ( 4.745470142856022200, -1.954873481938533608, -0.4925652823710227612 ) ) ;
#18534=CARTESIAN_POINT ( 'NONE',  ( 4.488128036367874607, -0.4058819498431766037, -1.795677737744493019 ) ) ;
#18535=CARTESIAN_POINT ( 'NONE',  ( 0.07661050522433666965, 0.7707917844542893082, -1.796988219766264550 ) ) ;
#18536=CARTESIAN_POINT ( 'NONE',  ( 2.122082200655984074, -2.237848761721575208, 0.5630162806932179631 ) ) ;
#18538=CARTESIAN_POINT ( 'NONE',  ( 5.255217470067075070, -1.823004960263453489, -1.161262906855420329 ) ) ;
#18540=CARTESIAN_POINT ( 'NONE',  ( 0.2748124788713289246, 1.811699325429259488, -0.6999492020843509632 ) ) ;
#18542=CARTESIAN_POINT ( 'NONE',  ( 3.884340333706528092, -0.1737987063687232436, 2.291882653078499477 ) ) ;
#18545=CARTESIAN_POINT ( 'NONE',  ( 3.678450976403758066, -1.802590750232490491, -0.4997190347926713794 ) ) ;
#18546=CARTESIAN_POINT ( 'NONE',  ( 0.8086807686161383568, -0.4671638426185490967, -1.854305266343849734 ) ) ;
#18549=CARTESIAN_POINT ( 'NONE',  ( 2.789901687333019797, 1.561178712900921584, 1.560079944692857046 ) ) ;
#18555=CARTESIAN_POINT ( 'NONE',  ( 6.825078400183526739, -0.0002198122173602961866, 1.955566246027613531 ) ) ;
#18556=CARTESIAN_POINT ( 'NONE',  ( 0.4293363604773897113, 2.209526777583595170, 0.6654907822973181730 ) ) ;
#18557=CARTESIAN_POINT ( 'NONE',  ( 1.082386330805637398, 1.171445227557347923, -1.573568114121715933 ) ) ;
#18558=CARTESIAN_POINT ( 'NONE',  ( 3.959878945198321620, -0.6033026367360559972, 1.972334540003743530 ) ) ;
#18567=CARTESIAN_POINT ( 'NONE',  ( 6.074718851800529507, 1.462630930118626660, -1.604749943717192373 ) ) ;
#18572=CARTESIAN_POINT ( 'NONE',  ( 1.598681293450100904, 1.532267803987485077, -1.072633048482305007 ) ) ;
#18577=CARTESIAN_POINT ( 'NONE',  ( 0.8735180803765253410, 0.3724630581584260636, -1.875478908130092215 ) ) ;
#18579=CARTESIAN_POINT ( 'NONE',  ( 3.045496301383675330, 0.6385914081092295413, -1.650799995714345325 ) ) ;
#18580=CARTESIAN_POINT ( 'NONE',  ( 0.2582720099171370021, 1.907150531373353664, 0.1405958444523764117 ) ) ;
#18582=CARTESIAN_POINT ( 'NONE',  ( 4.446842608676645270, -1.712983832262956696, -0.8575701973691277624 ) ) ;
#18584=CARTESIAN_POINT ( 'NONE',  ( 5.881302004902690506, -0.04997076178031189392, 1.969097942535046331 ) ) ;
#18585=CARTESIAN_POINT ( 'NONE',  ( 0.6332531790259123827, 1.961634380476449335, 0.8060562103610890983 ) ) ;
#18587=CARTESIAN_POINT ( 'NONE',  ( 4.205816867194319464, -1.865656749788859647, 0.1373567816406878750 ) ) ;
#18588=CARTESIAN_POINT ( 'NONE',  ( 0.8733498553583609603, 1.760202786292342170, -0.4843115980177821744 ) ) ;
#18590=CARTESIAN_POINT ( 'NONE',  ( 3.563272299071856164, -1.946135509614330239, -1.040604674307284316 ) ) ;
#18593=CARTESIAN_POINT ( 'NONE',  ( 0.9419289695592079070, 1.383825781391546883, 1.529776408950918265 ) ) ;
#18601=CARTESIAN_POINT ( 'NONE',  ( 2.699741690289765295, -1.532448122638006671, -1.392287113214360827 ) ) ;
#18603=CARTESIAN_POINT ( 'NONE',  ( 1.054251131370760319, 2.159144779032458050, -0.1049546803274861440 ) ) ;
#18605=CARTESIAN_POINT ( 'NONE',  ( 1.875654870896212190, 0.3429857902390308078, -1.990162865174507800 ) ) ;
#18610=CARTESIAN_POINT ( 'NONE',  ( 6.415388720371407949, 0.6297814698452592896, 1.915305867393565897 ) ) ;
#18611=CARTESIAN_POINT ( 'NONE',  ( 0.7609543035823238544, -0.05432987398422234326, -2.015980609757315190 ) ) ;
#18613=CARTESIAN_POINT ( 'NONE',  ( 5.355090213057959403, 0.4282289882464126451, -2.149144931432686256 ) ) ;
#18615=CARTESIAN_POINT ( 'NONE',  ( 3.164218664783400747, 1.912571728330178855, -0.004505864839042527346 ) ) ;
#18620=CARTESIAN_POINT ( 'NONE',  ( 1.300407892936685572, 1.352140309104767013, -1.496066053310755262 ) ) ;
#18622=CARTESIAN_POINT ( 'NONE',  ( 0.1876184131640425135, 1.704306722208508873, 1.533282888375518960 ) ) ;
#18624=CARTESIAN_POINT ( 'NONE',  ( 4.366008003732903653, 0.8140541678068600184, 1.520548270592293028 ) ) ;
#18625=CARTESIAN_POINT ( 'NONE',  ( -0.1405533004718494683, 0.2440837993472090295, -1.754028569132993542 ) ) ;
#18628=CARTESIAN_POINT ( 'NONE',  ( 1.574581288703358339, 1.320057194528483135, -1.451483715152704246 ) ) ;
#18631=CARTESIAN_POINT ( 'NONE',  ( 0.1755611466353447780, 0.6788741266964171128, -2.325051092042058620 ) ) ;
#18634=CARTESIAN_POINT ( 'NONE',  ( 4.160681542540445754, 0.4872625442002316287, 1.744618836514327587 ) ) ;
#18638=CARTESIAN_POINT ( 'NONE',  ( 5.039644362999008642, -1.718302384056184851, 0.5736564087924463928 ) ) ;
#18640=PRESENTATION_STYLE_ASSIGNMENT (( #84719 ) ) ;
#18642=CARTESIAN_POINT ( 'NONE',  ( 5.881279174647062291, -0.04503291608629880066, 1.860690090596372137 ) ) ;
#18644=CARTESIAN_POINT ( 'NONE',  ( 3.778834734487185099, 1.616410871901182711, -1.027684692424314594 ) ) ;
#18652=CARTESIAN_POINT ( 'NONE',  ( 0.6378455412261313517, -1.529572671500577297, -1.527792216034072670 ) ) ;
#18655=CARTESIAN_POINT ( 'NONE',  ( 0.4459769555512117511, 1.820297760642339391, 0.1397589855641478973 ) ) ;
#18657=CARTESIAN_POINT ( 'NONE',  ( 3.979382468966369935, 1.719079831940514502, -0.6148086763930470378 ) ) ;
#18659=CARTESIAN_POINT ( 'NONE',  ( 2.285291272251275707, 0.09004542135446562401, -1.910373438827176251 ) ) ;
#18661=CARTESIAN_POINT ( 'NONE',  ( 2.154690271565715687, -0.5224902820043091367, -1.898924457017936662 ) ) ;
#18662=CARTESIAN_POINT ( 'NONE',  ( 4.774914120469089696, 1.810774457899359202, -0.7023516835302608952 ) ) ;
#18665=CARTESIAN_POINT ( 'NONE',  ( 4.324552338190708056, -0.9094542848507057853, -1.915842285305848769 ) ) ;
#18676=CARTESIAN_POINT ( 'NONE',  ( 5.443921307256319508, 0.7362202147598860824, -1.670853202368662860 ) ) ;
#18677=CARTESIAN_POINT ( 'NONE',  ( 0.2212536527127808295, -1.848710500310095872, -0.9322282823912150240 ) ) ;
#18680=CARTESIAN_POINT ( 'NONE',  ( 6.925078400183546812, 3.702220002068328242, 2.370079373711677206 ) ) ;
#18681=CARTESIAN_POINT ( 'NONE',  ( 5.805500895539822181, -0.4530025297027094888, 1.814837910242727226 ) ) ;
#18683=CARTESIAN_POINT ( 'NONE',  ( 3.527879399192564325, -1.148099800794393444, -1.546878348965428973 ) ) ;
#18688=CARTESIAN_POINT ( 'NONE',  ( 1.265409400557556907, 1.954659568096604350, -0.8140754496198910894 ) ) ;
#18692=CARTESIAN_POINT ( 'NONE',  ( 6.192251260771239885, 1.025525066348543568, -1.798363755310352197 ) ) ;
#18693=CARTESIAN_POINT ( 'NONE',  ( 2.050122339901743196, -1.422379512129726908, 1.169167124061460949 ) ) ;
#18698=CARTESIAN_POINT ( 'NONE',  ( 1.799181239640806007, 1.907565883177517740, 1.270813247315852879 ) ) ;
#18699=CARTESIAN_POINT ( 'NONE',  ( -0.02319159430949970652, 0.003959926571647092407, -1.810968101872318714 ) ) ;
#18702=CARTESIAN_POINT ( 'NONE',  ( 1.160403428290600392, 2.011073784072180182, 0.09471770850632241223 ) ) ;
#18703=CARTESIAN_POINT ( 'NONE',  ( 1.463640819124707004, -0.4818986642843925972, 1.901505326443528876 ) ) ;
#18708=CARTESIAN_POINT ( 'NONE',  ( 3.996100316046395484, -0.6559638842641742906, -1.985124821949519891 ) ) ;
#18709=CARTESIAN_POINT ( 'NONE',  ( 1.832500204630353124, 0.1694391671427826207, 1.761704050274701894 ) ) ;
#18711=CARTESIAN_POINT ( 'NONE',  ( 5.859400655334408015, 2.259312458388713196, -0.3864819027975390786 ) ) ;
#18712=CARTESIAN_POINT ( 'NONE',  ( 2.835604015501072439, 1.727201357243525637, 0.2126739171897980840 ) ) ;
#18715=CARTESIAN_POINT ( 'NONE',  ( 3.391645568799035892, 0.04004947218742663240, 1.733546134666413607 ) ) ;
#18716=CARTESIAN_POINT ( 'NONE',  ( 3.490846471615864921, 2.117612208401131735, 0.4786232489656114253 ) ) ;
#18718=CARTESIAN_POINT ( 'NONE',  ( 4.839077477813122918, -1.706110771555340744, -1.074664961451990308 ) ) ;
#18719=CARTESIAN_POINT ( 'NONE',  ( 0.4687500000003047007, 0.7852924748224731077, -1.895863743164100335 ) ) ;
#18721=CARTESIAN_POINT ( 'NONE',  ( 1.817283056450700318, -0.2383884500203499179, 1.911531453543861225 ) ) ;
#18723=CARTESIAN_POINT ( 'NONE',  ( 6.064703480017706205, 0.6958612881963457397, 2.109637055116654558 ) ) ;
#18725=CARTESIAN_POINT ( 'NONE',  ( -0.1110810684433038154, 7.629137130509058728, -2.396956819904518809 ) ) ;
#18730=CARTESIAN_POINT ( 'NONE',  ( 0.5752228765869402682, -1.604835199033414872, 1.536031695938171460 ) ) ;
#18731=CARTESIAN_POINT ( 'NONE',  ( 5.758247127753066685, -1.962046631956643195, -0.001586170976335121285 ) ) ;
#18735=CARTESIAN_POINT ( 'NONE',  ( 6.432949606591497727, 0.2122621168692347127, 2.252429721023613496 ) ) ;
#18738=CARTESIAN_POINT ( 'NONE',  ( 4.246570442813556667, -2.039787899008322469, -0.3057716575347816934 ) ) ;
#18742=CARTESIAN_POINT ( 'NONE',  ( 6.028550586359523678, 1.802609027081774951, 0.4991829554215552744 ) ) ;
#18743=CARTESIAN_POINT ( 'NONE',  ( 4.816919938037654170, 0.8852131329995099884, -1.491020713638806949 ) ) ;
#18744=CARTESIAN_POINT ( 'NONE',  ( 4.528681460942417303, -1.588859801488880175, 0.7108448094420779517 ) ) ;
#18746=CARTESIAN_POINT ( 'NONE',  ( 1.962814135067984411, -2.097685689255949448, -0.9248770880663819138 ) ) ;
#18748=CARTESIAN_POINT ( 'NONE',  ( 5.671452434703694756, 1.246268910035509991, 1.678523727997438986 ) ) ;
#18749=CARTESIAN_POINT ( 'NONE',  ( 0.2867153840934755782, 1.362228626754984573, 1.238794746348782505 ) ) ;
#18752=CARTESIAN_POINT ( 'NONE',  ( 1.301407962653992501, 1.352153127569672098, -1.496052916918483522 ) ) ;
#18753=CARTESIAN_POINT ( 'NONE',  ( -0.02900071798685524560, -0.004641455105012376459, -2.173770343569726649 ) ) ;
#18757=CARTESIAN_POINT ( 'NONE',  ( 3.563236855010095017, -1.732559338849114505, 1.222301536229251084 ) ) ;
#18759=CARTESIAN_POINT ( 'NONE',  ( 5.496661139185262002, -0.4475443406098400523, -1.769863040007889410 ) ) ;
#18766=CARTESIAN_POINT ( 'NONE',  ( 3.480727363932310414, -1.353466037422011992, 1.499425228245174102 ) ) ;
#18767=CARTESIAN_POINT ( 'NONE',  ( 6.317417574511640765, -0.2763070477263400715, 2.189352377801502936 ) ) ;
#18769=CARTESIAN_POINT ( 'NONE',  ( 3.801460577334394575, -1.406423387113703960, -1.218697170607488944 ) ) ;
#18777=CARTESIAN_POINT ( 'NONE',  ( 1.563399581876812716, 1.420944641023152322, -0.9932112465018216874 ) ) ;
#18778=CARTESIAN_POINT ( 'NONE',  ( 1.200653373194009443, -0.4260525342448440722, 1.687239105062097400 ) ) ;
#18779=CARTESIAN_POINT ( 'NONE',  ( 0.09532371275382427178, -0.5158531520006398585, -2.257940698305866967 ) ) ;
#18782=CARTESIAN_POINT ( 'NONE',  ( 0.8782832160191712534, -1.147062573054495216, 1.711818785435960111 ) ) ;
#18784=CARTESIAN_POINT ( 'NONE',  ( 6.884150280000160826, -0.1566355309425542519, 2.263600626914013869 ) ) ;
#18788=CARTESIAN_POINT ( 'NONE',  ( 0.3386658216258168763, 0.3346604457750371187, 1.942702894000091662 ) ) ;
#18790=CARTESIAN_POINT ( 'NONE',  ( 4.992401499097729456, -1.057410677138232780, 1.593263788312593743 ) ) ;
#18792=CARTESIAN_POINT ( 'NONE',  ( 6.147136880733683917, -1.866598994669689926, 1.177069016086537356 ) ) ;
#18797=CARTESIAN_POINT ( 'NONE',  ( 6.410795937096152919, -0.5649949523399040441, -2.043744576961013859 ) ) ;
#18799=CARTESIAN_POINT ( 'NONE',  ( 3.452467797911736636, 2.307758715189492271, 0.002325993833134780940 ) ) ;
#18800=CARTESIAN_POINT ( 'NONE',  ( 4.932062528313536198, 1.127988425013145779, 1.604980062286972542 ) ) ;
#18801=CARTESIAN_POINT ( 'NONE',  ( 0.7429250141685154185, -0.2344385519315282107, -1.947609053799495005 ) ) ;
#18804=CARTESIAN_POINT ( 'NONE',  ( 0.1107727185766090999, 2.028241449780379568, 0.6078911015285259900 ) ) ;
#18807=CARTESIAN_POINT ( 'NONE',  ( 2.870184708472456325, -2.148041568373111776, 0.3144570722862209955 ) ) ;
#18809=CARTESIAN_POINT ( 'NONE',  ( 0.1762450972803019933, 2.096614079038420897, -0.3174041833761130360 ) ) ;
#18814=CARTESIAN_POINT ( 'NONE',  ( 2.266935757080061897, -1.882882732336080167, -0.8380483592859179209 ) ) ;
#18818=CARTESIAN_POINT ( 'NONE',  ( 0.07775346131142897577, 1.984126704040774181, -2.702190870904349840 ) ) ;
#18822=CARTESIAN_POINT ( 'NONE',  ( 4.635362334195573197, -0.09024504784891505815, 1.910265517452471862 ) ) ;
#18824=CARTESIAN_POINT ( 'NONE',  ( 1.124742813458483814, 1.347236035482470839, -1.817372803150618221 ) ) ;
#18827=CARTESIAN_POINT ( 'NONE',  ( 1.212835290986268300, 1.479965279312319693, -1.044435387019273742 ) ) ;
#18828=CARTESIAN_POINT ( 'NONE',  ( 0.3740639818887542267, -1.901581053304630675, -0.2314239742453021165 ) ) ;
#18829=CARTESIAN_POINT ( 'NONE',  ( 1.662640112210824306, -0.7432673875312334477, -1.932532381715674097 ) ) ;
#18831=CARTESIAN_POINT ( 'NONE',  ( 0.6726557866889815163, -1.855577277548149828, -0.6663020492489196700 ) ) ;
#18832=CARTESIAN_POINT ( 'NONE',  ( 5.953728026056397837, 0.5566793334266966209, -1.844321365346488273 ) ) ;
#18833=CARTESIAN_POINT ( 'NONE',  ( 0.2062968637084483525, -0.6088960595307371104, 2.225859948526871079 ) ) ;
#18836=CARTESIAN_POINT ( 'NONE',  ( 4.000476411064065374, 2.052455503700638229, 0.2052804401120340017 ) ) ;
#18841=CARTESIAN_POINT ( 'NONE',  ( 5.631892205062830392, -1.333580992396019571, -1.629923671128389762 ) ) ;
#18844=CARTESIAN_POINT ( 'NONE',  ( 1.223348113247175961, -1.962646724111057672, -0.9287667758015824004 ) ) ;
#18846=CARTESIAN_POINT ( 'NONE',  ( 4.833375328034618335, -1.978455579520097762, 0.8711445904842631816 ) ) ;
#18847=CARTESIAN_POINT ( 'NONE',  ( 5.725262222419306823, 1.782257655895511661, 0.9500345275383536015 ) ) ;
#18854=CARTESIAN_POINT ( 'NONE',  ( 3.872279980006509970, -1.995268062538615883, -0.2910826752766728642 ) ) ;
#18858=CARTESIAN_POINT ( 'NONE',  ( 5.084929678302336775, -0.2608814864752464491, -2.145832476913120068 ) ) ;
#18863=CARTESIAN_POINT ( 'NONE',  ( 4.587517648402447357, -0.5350702435001615243, 1.944077497823355483 ) ) ;
#18865=CARTESIAN_POINT ( 'NONE',  ( 0.5215560022201523038, -0.9183498723843477318, -1.459886522650925000 ) ) ;
#18870=CARTESIAN_POINT ( 'NONE',  ( 5.114452126850835612, 1.290914414355217366, -1.353902443742838191 ) ) ;
#18871=CARTESIAN_POINT ( 'NONE',  ( 6.533470335063485734, -0.1341179537190802518, 1.982235210812468340 ) ) ;
#18877=CARTESIAN_POINT ( 'NONE',  ( 1.858217301831434964, 0.8087058978607818416, -1.960417502992222838 ) ) ;
#18878=CARTESIAN_POINT ( 'NONE',  ( 0.5797041155359907716, -0.7231210598357665775, 1.882482590253447663 ) ) ;
#18879=CARTESIAN_POINT ( 'NONE',  ( 1.371055822538247870, -1.554752094505476467, -0.9295159999406394924 ) ) ;
#18881=CARTESIAN_POINT ( 'NONE',  ( 6.034075718726629844, 1.069613854859407631, -1.878468107683453514 ) ) ;
#18884=CARTESIAN_POINT ( 'NONE',  ( -0.1005721928965920831, -1.878210221491773524, 0.3762452260359094303 ) ) ;
#18892=CARTESIAN_POINT ( 'NONE',  ( 3.731458613173586514, -1.998165266068991253, 0.8252760040215676440 ) ) ;
#18895=CARTESIAN_POINT ( 'NONE',  ( 2.180079139336263516, 2.078761533942363737, -0.4183221158333137457 ) ) ;
#18897=CARTESIAN_POINT ( 'NONE',  ( 2.003138245156708130, 1.636809484843353868, 1.098402624201348488 ) ) ;
#18898=CARTESIAN_POINT ( 'NONE',  ( 4.922078805074791674, -1.902621863305080430, 0.1933406509087298719 ) ) ;
#18901=CARTESIAN_POINT ( 'NONE',  ( 6.391062254520311292, 0.1913994329204322109, 1.960204640275018395 ) ) ;
#18902=CARTESIAN_POINT ( 'NONE',  ( 1.745936028080337765, 0.6089015219087092756, 1.844080840262368071 ) ) ;
#18909=CARTESIAN_POINT ( 'NONE',  ( 4.916621234345090130, -0.6478637630910142331, -1.799314785492410529 ) ) ;
#18911=CARTESIAN_POINT ( 'NONE',  ( 3.844505992619148937, 2.196175933995975438, 0.2170506636963928093 ) ) ;
#18912=CARTESIAN_POINT ( 'NONE',  ( 2.520803682403276902, 1.441976459853638204, -1.670562425240495363 ) ) ;
#18914=CARTESIAN_POINT ( 'NONE',  ( 0.1527893875182678718, 0.3269112364552365091, 1.883972597190447518 ) ) ;
#18918=CARTESIAN_POINT ( 'NONE',  ( 3.033707436314789785, 1.966763487489433970, -0.6469820378900912328 ) ) ;
#18922=CARTESIAN_POINT ( 'NONE',  ( 2.114359756454447847, -1.018641858927371135, -1.906637348776268004 ) ) ;
#18923=CARTESIAN_POINT ( 'NONE',  ( 3.509492838045696672, -2.158849082856160173, 0.3763758916049686487 ) ) ;
#18924=CARTESIAN_POINT ( 'NONE',  ( 0.02755585400013305097, 7.629137130509076492, -2.789001785468494976 ) ) ;
#18930=CARTESIAN_POINT ( 'NONE',  ( 5.484916526786003388, -1.734343006517705676, 0.008455456694493946809 ) ) ;
#18932=CARTESIAN_POINT ( 'NONE',  ( 3.573154620739454224, 1.869565233029608198, 0.8895530118792621677 ) ) ;
#18933=CARTESIAN_POINT ( 'NONE',  ( 5.062167955004798436, -1.175237403299607797, 1.760913580352542862 ) ) ;
#18937=CARTESIAN_POINT ( 'NONE',  ( 2.535944157116743369, 1.207843060446149197, 1.555523554018751309 ) ) ;
#18938=CARTESIAN_POINT ( 'NONE',  ( 1.019614524654769872, -0.4619345408787678964, 1.855657206939323789 ) ) ;
#18939=CARTESIAN_POINT ( 'NONE',  ( 5.209026396049201146, -0.3404489335739938061, 2.266724491853837620 ) ) ;
#18940=CARTESIAN_POINT ( 'NONE',  ( 3.035583632137848653, -1.226507576337819483, -1.352503160878690380 ) ) ;
#18946=CARTESIAN_POINT ( 'NONE',  ( 3.744393049878576463, 1.073438034848249290, -1.702967747733853843 ) ) ;
#18948=CARTESIAN_POINT ( 'NONE',  ( 4.434394140398959294, -1.132915509570767476, 1.601352629973289199 ) ) ;
#18951=CARTESIAN_POINT ( 'NONE',  ( 0.1753634416057498202, 0.7014533214223102053, -2.226873008360684913 ) ) ;
#18952=CARTESIAN_POINT ( 'NONE',  ( 0.2399332258718233080, 2.085444179493881389, 0.1495565104911322774 ) ) ;
#18953=CARTESIAN_POINT ( 'NONE',  ( 5.682415782506053503, -1.727394229680437876, -0.3844701117694647174 ) ) ;
#18955=CARTESIAN_POINT ( 'NONE',  ( 2.414256260463796711, 1.430409426244143134, -1.660321623440104810 ) ) ;
#18956=CARTESIAN_POINT ( 'NONE',  ( 6.650362500428334656, -1.339898832705511911, 1.110426912289312451 ) ) ;
#18958=CARTESIAN_POINT ( 'NONE',  ( 0.1335669894368343991, 7.629137130509040965, -2.753547149787978654 ) ) ;
#18959=CARTESIAN_POINT ( 'NONE',  ( 0.7149654600043838792, -0.2576282674517544335, 1.705390864826474839 ) ) ;
#18960=CARTESIAN_POINT ( 'NONE',  ( 1.054597461939084768, 2.025951976169305890, -1.085350914182762638 ) ) ;
#18961=CARTESIAN_POINT ( 'NONE',  ( 0.5389544483674936215, -1.876709678404146153, 1.131566444868239874 ) ) ;
#18962=CARTESIAN_POINT ( 'NONE',  ( 2.491098823239074278, -0.3784457004711218042, -2.174036671264235387 ) ) ;
#18963=FACE_OUTER_BOUND ( 'NONE', #25327, .T. ) ;
#18964=CARTESIAN_POINT ( 'NONE',  ( 6.883263157960365142, -0.007059606330772279746, 2.153658854459541416 ) ) ;
#18966=CARTESIAN_POINT ( 'NONE',  ( 1.622414240495053672, 2.095119945234637182, 0.3050691438145485268 ) ) ;
#18968=CARTESIAN_POINT ( 'NONE',  ( 6.620655732516647518, 3.684600858287550906, 2.687722323901103660 ) ) ;
#18969=CARTESIAN_POINT ( 'NONE',  ( 5.350583055395741638, 0.5590458624239265095, 1.843501136262601037 ) ) ;
#18971=CARTESIAN_POINT ( 'NONE',  ( 1.435548669473255323, -1.664339209632224481, -1.576619915386682447 ) ) ;
#18975=CARTESIAN_POINT ( 'NONE',  ( 5.162811894357514753, 0.6434298260243781487, 2.126049117748362249 ) ) ;
#18984=CARTESIAN_POINT ( 'NONE',  ( 2.901017702322743919, -0.9963018188003970321, -1.753030416019534021 ) ) ;
#18986=CARTESIAN_POINT ( 'NONE',  ( 1.270463096138880088, -0.9239429406890822261, -1.844087381150324001 ) ) ;
#18991=CARTESIAN_POINT ( 'NONE',  ( 4.013774469618203611, -1.125877316280783358, -1.879984707117538845 ) ) ;
#18992=CARTESIAN_POINT ( 'NONE',  ( 1.336564801266389990, 0.5826540126645517459, -1.930418273149013153 ) ) ;
#18993=CARTESIAN_POINT ( 'NONE',  ( 1.135996871135702024, 0.3593859243370273182, 1.805655672011026391 ) ) ;
#18994=CARTESIAN_POINT ( 'NONE',  ( 5.443040390997877509, -1.805468894110316080, -1.412473186189531438 ) ) ;
#18995=CARTESIAN_POINT ( 'NONE',  ( 2.976309490518674217, -0.1360139883382974202, -1.836174483004118674 ) ) ;
#18999=CARTESIAN_POINT ( 'NONE',  ( 3.803562306130504389, -0.5304149723801485639, 1.746809896627635084 ) ) ;
#19000=CARTESIAN_POINT ( 'NONE',  ( 4.904922738988922504, -1.081064280317966420, -1.701948707654332704 ) ) ;
#19002=CARTESIAN_POINT ( 'NONE',  ( 4.381858629716777642, 1.474804143916402355, 1.715883708886431158 ) ) ;
#19004=CARTESIAN_POINT ( 'NONE',  ( 6.405314555823123257, 1.748765893162683271, 1.173091541056320297 ) ) ;
#19006=CARTESIAN_POINT ( 'NONE',  ( 3.437997351728830697, 1.311287738946330439, 1.602184970737066116 ) ) ;
#19011=CARTESIAN_POINT ( 'NONE',  ( 1.682126184939515934, -1.031041751839639087, 1.627202258603721363 ) ) ;
#19014=CARTESIAN_POINT ( 'NONE',  ( 6.912958093653829295, -1.524444945649571004, 1.246696689375533795 ) ) ;
#19018=CARTESIAN_POINT ( 'NONE',  ( 1.459560619642571000, -1.873223059428649639, 1.193793739728800762 ) ) ;
#19019=CARTESIAN_POINT ( 'NONE',  ( 3.258910125681306891, -1.595695288142566337, 1.374458643164514937 ) ) ;
#19022=CARTESIAN_POINT ( 'NONE',  ( 0.6603357414211168397, -0.6217855776655777378, -1.754263843975149006 ) ) ;
#19027=CARTESIAN_POINT ( 'NONE',  ( 0.9848172835694012361, -1.340914915981223476, 1.642866500755429948 ) ) ;
#19030=CARTESIAN_POINT ( 'NONE',  ( 4.703538834289092030, -1.515240342570793430, -1.246145567450624991 ) ) ;
#19031=CARTESIAN_POINT ( 'NONE',  ( 3.327187652246216931, 0.05129554954072869377, 2.161254785723889515 ) ) ;
#19032=CARTESIAN_POINT ( 'NONE',  ( 1.944624168438695566, -1.479605912621816399, -1.095697124569312564 ) ) ;
#19037=CARTESIAN_POINT ( 'NONE',  ( 4.786887925959832479, 1.292461281945065599, 1.165648420485969394 ) ) ;
#19041=CARTESIAN_POINT ( 'NONE',  ( 2.219795081190904629, -2.096929600374438429, 0.5247480557022954351 ) ) ;
#19042=CARTESIAN_POINT ( 'NONE',  ( 3.567732365556259833, 1.591074578583808075, -1.238131541301431549 ) ) ;
#19044=CARTESIAN_POINT ( 'NONE',  ( 0.8136072859011161951, -0.3160970183575459447, 2.138355382504661506 ) ) ;
#19045=CARTESIAN_POINT ( 'NONE',  ( 3.168780698033875076, -1.820990468880798296, -0.7558852700480926945 ) ) ;
#19048=CARTESIAN_POINT ( 'NONE',  ( 3.280740747204694774, 1.754465757641409995, -0.8330476171748876224 ) ) ;
#19053=CARTESIAN_POINT ( 'NONE',  ( -0.2106854629475037044, 2.877407191259284680, -2.485613835449883346 ) ) ;
#19057=EDGE_LOOP ( 'NONE', ( #189662, #16217, #33632, #103582 ) ) ;
#19059=CARTESIAN_POINT ( 'NONE',  ( 0.07755575628183573877, -0.002876890934064984650, -2.188974970840869005 ) ) ;
#19061=CARTESIAN_POINT ( 'NONE',  ( 4.645332984504850771, 1.754159843842403976, -0.8783796436172899291 ) ) ;
#19062=CARTESIAN_POINT ( 'NONE',  ( 2.215470409936692420, 1.956561601830292485, 0.4872017847364697452 ) ) ;
#19064=CARTESIAN_POINT ( 'NONE',  ( 3.766910327102332978, -0.2117226681838789426, -2.106763584193247940 ) ) ;
#19066=CARTESIAN_POINT ( 'NONE',  ( 0.07479286986305545837, 0.7422478802248284602, -1.939684878352589070 ) ) ;
#19068=CARTESIAN_POINT ( 'NONE',  ( 3.380630241506640932, 1.664009615612583204, -0.7882418170854917916 ) ) ;
#19072=CARTESIAN_POINT ( 'NONE',  ( 4.781546299372162245, 0.2051969522943071500, -2.110614603223801122 ) ) ;
#19074=CARTESIAN_POINT ( 'NONE',  ( 6.825078400183545391, 0.005516643811322498661, 1.755566376062764000 ) ) ;
#19076=CARTESIAN_POINT ( 'NONE',  ( 5.940714679333914283, 0.3976391751681263576, 2.021873298595587176 ) ) ;
#19077=CARTESIAN_POINT ( 'NONE',  ( 1.310759002261387529, -1.470036769156491063, 1.141183394468782364 ) ) ;
#19078=CARTESIAN_POINT ( 'NONE',  ( 2.524749765808989466, -1.717266272480859834, 0.6646640004178904215 ) ) ;
#19083=CARTESIAN_POINT ( 'NONE',  ( 2.754729969050898841, 0.7443088323898851000, 2.077706851784946185 ) ) ;
#19084=CARTESIAN_POINT ( 'NONE',  ( 4.921284695982240720, -0.1178685990214298068, 2.259476483347002240 ) ) ;
#19085=CARTESIAN_POINT ( 'NONE',  ( 3.520720487665735643, 0.3006478860226591276, 1.993893439002386581 ) ) ;
#19087=CARTESIAN_POINT ( 'NONE',  ( 5.115404481452859642, 1.485474843905653985, 1.036646722175238011 ) ) ;
#19088=CARTESIAN_POINT ( 'NONE',  ( 4.715990674440117658, 0.9792849278024118309, -1.646335200727979897 ) ) ;
#19090=CARTESIAN_POINT ( 'NONE',  ( 4.293796034307355569, -0.7555264168055545460, 1.821139111365249308 ) ) ;
#19091=CARTESIAN_POINT ( 'NONE',  ( 5.418772907935071714, 1.728844841293469159, 0.7149302089985640762 ) ) ;
#19092=CARTESIAN_POINT ( 'NONE',  ( 4.896841239116665356, 0.3175000240179836619, 1.833586397851859839 ) ) ;
#19095=CARTESIAN_POINT ( 'NONE',  ( 0.7082206942033396624, 1.197301205363930254, -1.622488844446705381 ) ) ;
#19097=CARTESIAN_POINT ( 'NONE',  ( 1.242952776902699785, 0.4124841525564198474, 2.065099357090140586 ) ) ;
#19102=CARTESIAN_POINT ( 'NONE',  ( 3.392942708002244068, -2.044739723715986113, -0.5619712599038150236 ) ) ;
#19104=CARTESIAN_POINT ( 'NONE',  ( 1.845969175824228925, -1.322618866652914393, -1.526557775719493915 ) ) ;
#19109=CARTESIAN_POINT ( 'NONE',  ( 2.108864864398530159, 1.603267699958549342, -1.450045708023157687 ) ) ;
#19110=CARTESIAN_POINT ( 'NONE',  ( 6.890000000000009450, -0.01081285896028030651, 2.279840171838913854 ) ) ;
#19116=CARTESIAN_POINT ( 'NONE',  ( 1.452940684028160234, -1.882004992133184285, -1.122693704575933316 ) ) ;
#19118=CARTESIAN_POINT ( 'NONE',  ( 1.112636518468415270, -1.019398372879092962, -2.019907345245135932 ) ) ;
#19126=CARTESIAN_POINT ( 'NONE',  ( 3.879312468746206832, 1.623315624747388775, -0.5835212994509741957 ) ) ;
#19128=CARTESIAN_POINT ( 'NONE',  ( 1.563349520526525538, 1.744638119327382553, -0.2959517217632592900 ) ) ;
#19129=CARTESIAN_POINT ( 'NONE',  ( 4.999154358079874960, 1.837129776665728187, -1.222328095618854693 ) ) ;
#19131=ORIENTED_EDGE ( 'NONE', *, *, #151247, .T. ) ;
#19132=CARTESIAN_POINT ( 'NONE',  ( 4.429947715222688487, -1.979980911821906497, 0.3981057063161990706 ) ) ;
#19134=CARTESIAN_POINT ( 'NONE',  ( 4.728138764314923748, 2.011206665557175199, 0.1455158850461671372 ) ) ;
#19135=CARTESIAN_POINT ( 'NONE',  ( 4.570457401048643398, 0.6997940171077315918, 1.671178544893426654 ) ) ;
#19137=CARTESIAN_POINT ( 'NONE',  ( 2.553401164250346245, 0.5009360343536627402, -1.802255699741683870 ) ) ;
#19139=CARTESIAN_POINT ( 'NONE',  ( 6.621730190220365131, -1.769489810573118049, 0.4491385735008179836 ) ) ;
#19140=CARTESIAN_POINT ( 'NONE',  ( 1.582132296805271787, 0.9858968508435607125, 1.638552900098678045 ) ) ;
#19146=CARTESIAN_POINT ( 'NONE',  ( 0.2813230411330031600, 0.1852680230450229892, -1.903361379684164412 ) ) ;
#19149=CARTESIAN_POINT ( 'NONE',  ( 2.119516022818414669, 0.3384452847540948550, -1.932298432780136244 ) ) ;
#19153=CARTESIAN_POINT ( 'NONE',  ( 5.291314375706784645, -0.05428322906628547939, -2.120082430678168706 ) ) ;
#19156=CARTESIAN_POINT ( 'NONE',  ( 6.819606788702130551, -1.912791534441590668, 0.4766558377571166183 ) ) ;
#19158=CARTESIAN_POINT ( 'NONE',  ( 0.5451820649361303062, 0.1524121550021810545, 2.007518037476815564 ) ) ;
#19160=CARTESIAN_POINT ( 'NONE',  ( 1.124788838837559535, 0.4171406989393853793, 2.075574515046583191 ) ) ;
#19162=CARTESIAN_POINT ( 'NONE',  ( 2.734898984476673789, -1.980466496001157317, -0.6033880717724803278 ) ) ;
#19166=CARTESIAN_POINT ( 'NONE',  ( 4.822261998019022222, 2.000437409348213347, 0.6074620046824655839 ) ) ;
#19168=CARTESIAN_POINT ( 'NONE',  ( 2.537895388257872753, 0.8626947210231518115, -1.608888323311054691 ) ) ;
#19169=CARTESIAN_POINT ( 'NONE',  ( 2.965264322261091934, -1.482184020574893069, -1.041122702216127571 ) ) ;
#19171=CARTESIAN_POINT ( 'NONE',  ( 6.164705905600973423, -1.563586322211576674, 1.557672334054376773 ) ) ;
#19173=CARTESIAN_POINT ( 'NONE',  ( 5.631908123138919642, -1.395923778694251105, -1.709176034821748624 ) ) ;
#19176=CARTESIAN_POINT ( 'NONE',  ( 4.125576785117724299, -0.3237648511281773778, 1.884507068624697190 ) ) ;
#19179=CARTESIAN_POINT ( 'NONE',  ( 5.881320641815352523, -0.05461762546566178989, 2.069818975884097689 ) ) ;
#19182=CARTESIAN_POINT ( 'NONE',  ( 6.620655732516649294, -0.002413161512292843602, 2.173887093218459743 ) ) ;
#19188=CARTESIAN_POINT ( 'NONE',  ( 3.462029368274913477, 0.8381641302350505418, 1.672297462726477946 ) ) ;
#19193=CARTESIAN_POINT ( 'NONE',  ( 6.977413707831522593, -0.1558467299303326059, 2.036386162850227333 ) ) ;
#19194=CARTESIAN_POINT ( 'NONE',  ( 0.9312678054614745848, -1.591333336790928366, -1.238303555203337458 ) ) ;
#19198=CARTESIAN_POINT ( 'NONE',  ( 1.218978173989828884, -0.05078841826402366588, 2.191026318449231791 ) ) ;
#19199=CARTESIAN_POINT ( 'NONE',  ( 6.111906964637446649, -1.811269838261083232, 0.2284818145076653595 ) ) ;
#19206=CARTESIAN_POINT ( 'NONE',  ( 3.702549152423353807, 1.581054339307564449, 0.9433870219286569769 ) ) ;
#19207=CARTESIAN_POINT ( 'NONE',  ( 0.3287710483851979393, 1.386612999538240576, -1.459627859818838802 ) ) ;
#19208=CARTESIAN_POINT ( 'NONE',  ( 2.847332689139534523, -1.183592279326161290, 1.970102427710369808 ) ) ;
#19209=CARTESIAN_POINT ( 'NONE',  ( -0.1290005225502918740, 6.946858002156244716, -2.769053915224591211 ) ) ;
#19210=CARTESIAN_POINT ( 'NONE',  ( 0.6196752394443981737, 1.841814893205738102, -0.2651871859581377833 ) ) ;
#19214=CARTESIAN_POINT ( 'NONE',  ( 4.359561026920276916, -1.481784043772149229, -1.208992945495937610 ) ) ;
#19219=CARTESIAN_POINT ( 'NONE',  ( 3.333613130510120648, 0.9378223671878234136, -1.868666107883134142 ) ) ;
#19220=CARTESIAN_POINT ( 'NONE',  ( 2.360033908006432757, 0.7977434165707707470, 1.692156362554583460 ) ) ;
#19223=CARTESIAN_POINT ( 'NONE',  ( 3.245385237338119566, 1.740626721681370670, -0.003331538806947489072 ) ) ;
#19227=CARTESIAN_POINT ( 'NONE',  ( 4.002375702155434922, -0.5437682074083802775, -1.636994321040524447 ) ) ;
#19229=CARTESIAN_POINT ( 'NONE',  ( 3.931328349035985603, -1.512150646884598215, -1.586510368271301541 ) ) ;
#19232=CARTESIAN_POINT ( 'NONE',  ( 3.590846382830733763, 2.117060681034032221, 0.4805534470472500042 ) ) ;
#19233=CARTESIAN_POINT ( 'NONE',  ( 2.437895498511342574, 0.8609710149188254391, -1.609920059450341778 ) ) ;
#19235=CARTESIAN_POINT ( 'NONE',  ( 5.102788515576859751, 1.957488760995762300, 0.8075332785216599030 ) ) ;
#19238=CARTESIAN_POINT ( 'NONE',  ( 5.425394459833968064, -1.452027641166652172, -1.773832485185691032 ) ) ;
#19241=CARTESIAN_POINT ( 'NONE',  ( 1.330900338397854155, 1.421537331630345014, -1.573617108223644312 ) ) ;
#19247=CARTESIAN_POINT ( 'NONE',  ( 1.436510670779034937, -1.237796341723711002, -1.844280071174006164 ) ) ;
#19249=CARTESIAN_POINT ( 'NONE',  ( 5.889296118903345700, -0.7283762112263308941, -1.880435897373772258 ) ) ;
#19251=CARTESIAN_POINT ( 'NONE',  ( 3.907127581704954888, -1.689070986467123836, 1.183507789072274496 ) ) ;
#19253=CARTESIAN_POINT ( 'NONE',  ( -0.2409995289980003397, 2.873648158547074338, -2.488896373646624749 ) ) ;
#19256=CARTESIAN_POINT ( 'NONE',  ( 0.4981332788140432899, -0.7063641614380437028, -1.967824727186429978 ) ) ;
#19257=CARTESIAN_POINT ( 'NONE',  ( 4.693982515131527755, 1.755768268644173791, 0.9914009648221073778 ) ) ;
#19258=CARTESIAN_POINT ( 'NONE',  ( 4.124425300631988200, 0.09459923933386081563, 1.838956108544815171 ) ) ;
#19261=CARTESIAN_POINT ( 'NONE',  ( 1.236830563851202491, -1.561790747969876714, 0.7321873917187391445 ) ) ;
#19262=CARTESIAN_POINT ( 'NONE',  ( 0.5148617154710419808, 0.1531739628206352510, 2.010800830040265996 ) ) ;
#19263=CARTESIAN_POINT ( 'NONE',  ( 1.249136956142880894, 2.263619502511230230, -0.3993902815438779563 ) ) ;
#19265=CARTESIAN_POINT ( 'NONE',  ( 1.405971756114566595, -0.5497231165422427068, 2.194469222715933476 ) ) ;
#19266=CARTESIAN_POINT ( 'NONE',  ( 3.299542427861827498, 1.660325518240006071, 1.295591914420061830 ) ) ;
#19270=CARTESIAN_POINT ( 'NONE',  ( 6.625000595499368039, -2.052053476427456502, 3.646059517245236328E-13 ) ) ;
#19275=CARTESIAN_POINT ( 'NONE',  ( 5.150715375432683985, 2.188637957643671417, 0.3792565894785212000 ) ) ;
#19276=CARTESIAN_POINT ( 'NONE',  ( 3.082162360440068749, -2.159116730143955998, -0.3741398933536920213 ) ) ;
#19279=CARTESIAN_POINT ( 'NONE',  ( 5.564887814092526419, 1.486691789297951871, -1.280227714881218892 ) ) ;
#19281=CARTESIAN_POINT ( 'NONE',  ( 6.890000000000008562, 1.260399741928097672, 2.114076522472335462 ) ) ;
#19284=CARTESIAN_POINT ( 'NONE',  ( 4.693665235656380830, 1.977662049654808740, -0.7657889336421249693 ) ) ;
#19288=CARTESIAN_POINT ( 'NONE',  ( 6.649309733611729278, -1.732918351142084035, -1.292073167451508686 ) ) ;
#19290=CARTESIAN_POINT ( 'NONE',  ( 4.774869596704574448, 1.716175909155163382, -0.6674964387535023969 ) ) ;
#19293=CARTESIAN_POINT ( 'NONE',  ( 1.171013094284451439, 1.035884637911354877, 1.398405216058955514 ) ) ;
#19297=CARTESIAN_POINT ( 'NONE',  ( 5.717692609583751029, -2.109997883074541392, 0.4692839721026839661 ) ) ;
#19302=CARTESIAN_POINT ( 'NONE',  ( 4.610339536224768331, -0.9213992672730475508, -1.955631277330005968 ) ) ;
#19304=CARTESIAN_POINT ( 'NONE',  ( 5.360604507329317592, -1.429826957936894960, 1.357393395290319660 ) ) ;
#19305=CARTESIAN_POINT ( 'NONE',  ( 3.655360161107966022, -0.3364991752431121808, -1.700650080047048318 ) ) ;
#19307=CARTESIAN_POINT ( 'NONE',  ( 0.8904706703079521279, -0.5376514911656914419, -2.124458794526106864 ) ) ;
#19308=CARTESIAN_POINT ( 'NONE',  ( 2.134188411380482098, -1.507708438093162018, -1.747028958505469909 ) ) ;
#19309=CARTESIAN_POINT ( 'NONE',  ( 5.149710871190182893, 0.6505453885284390170, -1.955453191944044766 ) ) ;
#19310=CARTESIAN_POINT ( 'NONE',  ( 6.392136499528294102, -0.5222240449473265489, -1.870457282704639290 ) ) ;
#19317=CARTESIAN_POINT ( 'NONE',  ( 1.178361531996233280, 1.528742360773158282, 1.314995429398260196 ) ) ;
#19319=CARTESIAN_POINT ( 'NONE',  ( 3.487540646120320442, 1.995909124301387116, -0.9416478298167814120 ) ) ;
#19321=CARTESIAN_POINT ( 'NONE',  ( 1.287708147089029032, -1.175244795098003614, -1.442924398407473108 ) ) ;
#19325=CARTESIAN_POINT ( 'NONE',  ( 6.925078400183590333, 2.958959781645562170, 2.496897724761244497 ) ) ;
#19328=CARTESIAN_POINT ( 'NONE',  ( 2.975518139630950021, 1.957357868463033501, -0.6452315760040390202 ) ) ;
#19331=CARTESIAN_POINT ( 'NONE',  ( 2.666670786633594137, 0.6826474749901580985, 1.900933108274209360 ) ) ;
#19334=CARTESIAN_POINT ( 'NONE',  ( 2.377870294028866294, 1.267006343609432761, 1.625331576946090539 ) ) ;
#19338=CARTESIAN_POINT ( 'NONE',  ( -0.2408018239684642792, 7.629137130509051623, -2.700476273684692785 ) ) ;
#19339=CARTESIAN_POINT ( 'NONE',  ( 5.654950187766193181, -1.741821662664808867, 1.355018943897445149 ) ) ;
#19341=CARTESIAN_POINT ( 'NONE',  ( 1.071799524545346216, 2.083542002058445863, -0.5754571431841256635 ) ) ;
#19343=CARTESIAN_POINT ( 'NONE',  ( 1.464077725791514517, -1.074659653367866952, 1.706114136832518779 ) ) ;
#19344=CARTESIAN_POINT ( 'NONE',  ( 2.284880952019330280, -2.229702823797473865, 0.5573334316414603196 ) ) ;
#19348=CARTESIAN_POINT ( 'NONE',  ( 2.061206331123175861, 0.3224310286589862629, -1.842498087946140561 ) ) ;
#19349=CARTESIAN_POINT ( 'NONE',  ( 3.274625289317079524, -0.3981104328964027994, -1.976669913042613747 ) ) ;
#19353=CARTESIAN_POINT ( 'NONE',  ( 4.758481774355417748, 0.8053329972168337125, 1.946216683261194236 ) ) ;
#19357=CARTESIAN_POINT ( 'NONE',  ( 5.607677614632407881, 1.532089292189286356, 1.316289066716142431 ) ) ;
#19359=CARTESIAN_POINT ( 'NONE',  ( 0.4267248635717044158, -1.349908593859616257, 1.559510075185864153 ) ) ;
#19367=CARTESIAN_POINT ( 'NONE',  ( 3.262351433937484835, -2.168797558456833308, 0.1038475075719157148 ) ) ;
#19370=CARTESIAN_POINT ( 'NONE',  ( 2.155570461979210428, 0.7887370375637430264, 1.663910549085621415 ) ) ;
#19372=CARTESIAN_POINT ( 'NONE',  ( 3.861010967126535576, 0.2669419790740577558, -2.175157288012785184 ) ) ;
#19374=CARTESIAN_POINT ( 'NONE',  ( 4.891644337148946420, 1.673267685831375307, 1.523052275532793320 ) ) ;
#19381=CARTESIAN_POINT ( 'NONE',  ( 4.956192180792302615, 0.6771475221719803761, 1.635265836519818716 ) ) ;
#19382=CARTESIAN_POINT ( 'NONE',  ( 3.246742594617262334, 1.964541544574874621, 0.4388061624774098890 ) ) ;
#19384=CARTESIAN_POINT ( 'NONE',  ( 1.483573828499670899, 1.945989852495342065, -0.8055925053903155719 ) ) ;
#19387=CARTESIAN_POINT ( 'NONE',  ( 1.662492070209736994, -0.7059575147525645189, -1.838877744480153620 ) ) ;
#19388=CARTESIAN_POINT ( 'NONE',  ( 0.6724591444495706671, -1.759989063064151038, -0.6342292696241008665 ) ) ;
#19389=CARTESIAN_POINT ( 'NONE',  ( 0.4671467121175364445, 1.705069321186868159, 0.9702857188121425391 ) ) ;
#19390=CARTESIAN_POINT ( 'NONE',  ( -0.2049973002360427898, -0.1418364932926942379, -1.881151990943498387 ) ) ;
#19395=CARTESIAN_POINT ( 'NONE',  ( 5.770339134078734666, -1.185559297855027561, 1.446973003893243348 ) ) ;
#19398=CARTESIAN_POINT ( 'NONE',  ( 5.120015143727554729, 2.048507142264085701, -0.2983452141967629645 ) ) ;
#19411=CARTESIAN_POINT ( 'NONE',  ( 5.459412808053472510, 1.602871733476991079, 1.130958114227413436 ) ) ;
#19413=CARTESIAN_POINT ( 'NONE',  ( 3.321638586175166719, -1.528507173905558014, 1.314795459203411676 ) ) ;
#19414=CARTESIAN_POINT ( 'NONE',  ( 2.887788952342277948, -1.913322710806207194, 0.09880452340514658816 ) ) ;
#19416=CARTESIAN_POINT ( 'NONE',  ( 0.6443834720083198020, 0.6415979653194536780, 2.095529601600601755 ) ) ;
#19417=CARTESIAN_POINT ( 'NONE',  ( 0.1333692844072559003, 5.722267537706915874, -2.647605121726896105 ) ) ;
#19418=CARTESIAN_POINT ( 'NONE',  ( 3.796049943699483453, -1.868292110373217518, -0.09463876624429126694 ) ) ;
#19422=CARTESIAN_POINT ( 'NONE',  ( 4.218443861432810138, 2.076744001477859314, 0.4112613105302816430 ) ) ;
#19423=CARTESIAN_POINT ( 'NONE',  ( 6.549288556030710140, 1.803345607721940524, -1.016871928424132099 ) ) ;
#19424=CARTESIAN_POINT ( 'NONE',  ( 1.400065306692158229, -0.7557916345088554477, -1.949536834912476646 ) ) ;
#19425=CARTESIAN_POINT ( 'NONE',  ( 6.720655732516642722, 6.033109933379183332, 2.868628414513713309 ) ) ;
#19426=CARTESIAN_POINT ( 'NONE',  ( 6.827182134110196365, 0.003888933837258023128, 1.810856214465895508 ) ) ;
#19434=CARTESIAN_POINT ( 'NONE',  ( 0.09988412287174981696, -0.8557525428138833545, 1.596560661436140283 ) ) ;
#19445=CARTESIAN_POINT ( 'NONE',  ( 6.609000000000036401, 0.002801690667396730238, 2.000160786441218086 ) ) ;
#19446=CARTESIAN_POINT ( 'NONE',  ( 0.6102159345307588412, -0.7594153588383574238, 1.980023364433493915 ) ) ;
#19448=CARTESIAN_POINT ( 'NONE',  ( -0.1394461523060988861, 1.283499747810852520, -2.524650647122913316 ) ) ;
#19452=CARTESIAN_POINT ( 'NONE',  ( 3.168761922233914952, 1.429703897159577464, -1.354768240434875759 ) ) ;
#19453=CARTESIAN_POINT ( 'NONE',  ( 0.9441710812277158693, -1.348169866081018853, -1.636719737310005973 ) ) ;
#19456=CARTESIAN_POINT ( 'NONE',  ( 6.727182134110200273, 0.5640974741700152117, 2.241195997201197443 ) ) ;
#19458=CARTESIAN_POINT ( 'NONE',  ( 6.298795234281088895, 1.819837665574381091, 1.220625243075368127 ) ) ;
#19460=CARTESIAN_POINT ( 'NONE',  ( 3.821244781301834426, -0.1429285350797465659, 1.921155437072092242 ) ) ;
#19462=CARTESIAN_POINT ( 'NONE',  ( -0.1294898018152200736, 7.629137130509059617, -2.526516153123930852 ) ) ;
#19463=CARTESIAN_POINT ( 'NONE',  ( 1.401302286655212948, 1.802556353783949517, -1.272968949304439379 ) ) ;
#19467=CARTESIAN_POINT ( 'NONE',  ( 6.051603174176475086, 1.488812912110796249, 1.289293616420229549 ) ) ;
#19468=CARTESIAN_POINT ( 'NONE',  ( 0.4857531807862237594, -1.927505705540471403, -0.2366729787525098105 ) ) ;
#19469=CARTESIAN_POINT ( 'NONE',  ( 6.046309306592402955, 2.127046199546629435, -0.8712367593181246095 ) ) ;
#19471=CARTESIAN_POINT ( 'NONE',  ( 4.750749981963457991, -0.4049220142380467458, -1.816192249911535272 ) ) ;
#19478=CARTESIAN_POINT ( 'NONE',  ( 0.7674258922165803076, 2.110627382301712540, -0.5898035449652739848 ) ) ;
#19483=CARTESIAN_POINT ( 'NONE',  ( 0.4690313652776016418, 0.1822212253758948297, -1.816563760317004395 ) ) ;
#19486=CARTESIAN_POINT ( 'NONE',  ( 2.461176475124981611, -1.659910965455011267, -0.5019686038148748475 ) ) ;
#19490=CARTESIAN_POINT ( 'NONE',  ( 6.129513044595952032, -1.717388127611047421, 0.6198453807191862674 ) ) ;
#19491=CARTESIAN_POINT ( 'NONE',  ( 3.203904402660478379, 0.7104733393662396868, -1.828749470067204896 ) ) ;
#19495=CARTESIAN_POINT ( 'NONE',  ( 4.969442291489525765, -1.791676405564743169, -1.133875526122554156 ) ) ;
#19498=CARTESIAN_POINT ( 'NONE',  ( 2.817306709214098870, -1.799057772339835548, -1.024303335033532658 ) ) ;
#19501=CARTESIAN_POINT ( 'NONE',  ( 5.022253332556455341, -2.210719170837057934, 0.2167383629448139670 ) ) ;
#19503=CARTESIAN_POINT ( 'NONE',  ( 2.391599454647721945, -0.8833308501894185927, -2.122370812339502422 ) ) ;
#19511=CARTESIAN_POINT ( 'NONE',  ( 4.025576834063953946, -0.3218090080209669024, 1.884953445776993863 ) ) ;
#19513=CARTESIAN_POINT ( 'NONE',  ( 3.662884335446520367, -1.521034750653621481, -0.8131990640867832187 ) ) ;
#19514=CARTESIAN_POINT ( 'NONE',  ( 3.221888912838869690, 0.9023448338944944913, -1.803416113280359445 ) ) ;
#19515=CARTESIAN_POINT ( 'NONE',  ( 3.639517500262396954, 0.8282738168534724554, 2.144427848026169592 ) ) ;
#19517=CARTESIAN_POINT ( 'NONE',  ( 0.04788047853313340263, -1.708876078042343316, -1.396090968258607790 ) ) ;
#19520=CARTESIAN_POINT ( 'NONE',  ( 4.516719421352251906, 1.617689212748760985, 0.7181139158070405371 ) ) ;
#19523=CARTESIAN_POINT ( 'NONE',  ( 0.7094041017953250927, -0.3309814517665210509, 2.268137058596159328 ) ) ;
#19524=CARTESIAN_POINT ( 'NONE',  ( 6.474545096729185545, -0.09562278402284159207, -1.838781726270556804 ) ) ;
#19526=CARTESIAN_POINT ( 'NONE',  ( 6.650331627364351128, -1.696677047125955795, 1.386650686450926484 ) ) ;
#19531=CARTESIAN_POINT ( 'NONE',  ( 0.2741912710782665741, -2.129148944087058126, 0.4243047986705119068 ) ) ;
#19532=CARTESIAN_POINT ( 'NONE',  ( 1.182827746461931229, 1.645757370610765102, -1.164989914844760444 ) ) ;
#19534=CARTESIAN_POINT ( 'NONE',  ( 4.916589582839517192, 1.327171671461774061, -1.396654247447129960 ) ) ;
#19536=CARTESIAN_POINT ( 'NONE',  ( 1.108037262132562262, 1.686735864949813202, 1.445688421275423075 ) ) ;
#19545=CARTESIAN_POINT ( 'NONE',  ( 4.194663043249587275, 1.400965740628885126, 1.032472458625796286 ) ) ;
#19546=CARTESIAN_POINT ( 'NONE',  ( 2.049198471137442912, 1.708465938063120637, -0.9642302061752604514 ) ) ;
#19552=CARTESIAN_POINT ( 'NONE',  ( 6.285602425426498385, -1.847771260692541162, 0.6596951833430019230 ) ) ;
#19555=CARTESIAN_POINT ( 'NONE',  ( 5.208220363674559650, 1.197307938467083055, -1.622483861274232719 ) ) ;
#19557=CARTESIAN_POINT ( 'NONE',  ( 1.323510708689378479, -0.05371019744930016770, 2.262043349595239228 ) ) ;
#19560=CARTESIAN_POINT ( 'NONE',  ( 2.336979506217982117, -1.672866993182718698, 0.8370366242000035761 ) ) ;
#19561=CARTESIAN_POINT ( 'NONE',  ( 1.107607643408299314, -0.04344470770747606292, 1.733769432050970449 ) ) ;
#19562=B_SPLINE_CURVE_WITH_KNOTS ( 'NONE', 3,
 ( #22360, #171843, #102571, #86319, #39708, #184867, #136153, #200050, #170772, #202170, #87395, #117823, #168631, #54892, #138290, #71110, #3969, #118881, #204305, #150270, #103650, #119958, #183813, #121046, #203248, #185933, #5035, #35423, #154532, #169701, #38644, #153462, #167571, #19171, #201107, #137228, #187013, #45070, #156673, #89547, #8266, #74350, #140454, #190211, #206465, #205392, #90616, #91691, #177183, #58092, #111181, #109046, #41871, #191271, #176126, #77537, #155598, #125312, #124252, #209653, #7183, #107981, #106902, #60220, #174009, #26652, #159861, #25580, #157744, #76469, #40797, #142578, #24505, #172928, #9341, #75414, #141527, #192338, #11464, #175065, #207535, #59154, #42937, #110115, #143659, #189158, #92753, #93820, #61294, #158797, #73254, #27726, #10394, #127455, #208585, #126379, #123197, #43997, #139361, #193426, #57030, #194490, #33059, #12530, #82864, #147890, #32002, #144722, #30947, #66580, #47205, #165186, #81807, #16780, #15722, #148940, #50373, #14657, #163076, #78602, #132722, #49321, #113320, #179327, #146839, #210734, #115438, #116496, #129582, #97022, #513, #63430, #80751, #62360, #197677, #212858, #114383, #94883, #64495, #213906, #198727, #130637, #65529, #196629, #131675, #128521, #28799, #195569, #160935, #181429, #99137, #48270, #98083, #46132, #112249, #180378, #178260, #164138, #29873, #95957, #162011, #13600, #79674, #145789, #211792, #18911, #122674, #167325, #84995, #68723, #151086, #83924, #183559, #184615, #58643, #2650, #207012, #204858, #134845, #72744, #57580, #200848, #152142, #150014, #157222, #35166, #56514, #52498, #199800, #156156, #101242, #188637, #41352, #118630, #36233, #172402, #133792, #23990, #117564, #51445, #102311, #168385, #141005, #19981, #86065, #6668, #138842, #40267, #91166, #106378, #90092, #73823, #182485, #7737, #189699, #139918, #8821, #205948, #123738, #107461, #173487, #25064, #1584, #74896, #100185, #34113, #166250, #17840, #67645, #191820, #28275, #144210, #79150, #162555, #193963, #78086, #43485, #142061, #208075, #174554, #93303, #160409, #109603, #30420, #190757, #62897, #46673, #14126, #195039, #27197, #192888, #44546, #209133, #129067, #80219, #210206, #110661, #61842, #12012, #60771, #175609, #13071, #112793, #128010, #126931, #45611, #75958, #176662, #145266, #178805, #9883, #111726, #96505, #146318, #159339, #124796, #212333, #94367, #42420, #177734, #29347, #95442, #108525, #161492, #211274, #26130, #59701, #92243, #158292, #125863, #10935, #77011, #143138, #66064, #83404, #312, #181966, #15200, #149486, #134334, #67134, #198215, #47752, #167865, #19463, #49850, #82340, #35720, #117045, #165736, #18398, #132207, #115978, #113867, #184100, #213394, #166806, #179862, #148432, #85538, #63971, #33595, #183041, #51990, #199276, #99667, #180913, #200339, #101796, #17323, #1069, #48797, #133267, #50918, #151629, #196115, #34657, #81291, #118115, #163620, #130127, #84475, #150566, #2127, #131171, #31486, #97561, #197161, #147368, #114915, #65018, #32537, #98611, #164672, #16255, #68203, #100727, #187302, #154816, #203527, #137510, #189439, #5317, #23729, #87677, #21570, #121326, #185157, #89835, #24793, #103941, #153749, #41081, #37861, #55181, #53037, #172134, #38928, #88759, #69265, #71399, #205675, #138573, #105011, #120252, #139655, #107189 ),
 .UNSPECIFIED., .F., .F.,
 ( 4, 1, 1, 1, 1, 1, 1, 1, 1, 1, 1, 1, 1, 1, 1, 1, 1, 1, 1, 1, 1, 1, 1, 1, 1, 1, 1, 1, 1, 1, 1, 1, 1, 1, 1, 1, 1, 1, 1, 1, 1, 1, 1, 1, 1, 1, 1, 1, 1, 1, 1, 1, 1, 1, 1, 1, 1, 1, 1, 1, 1, 1, 1, 1, 1, 1, 1, 1, 1, 1, 1, 1, 1, 1, 1, 1, 1, 1, 1, 1, 1, 1, 1, 1, 1, 1, 1, 1, 1, 1, 1, 1, 1, 1, 1, 1, 1, 1, 1, 1, 1, 1, 1, 1, 1, 1, 1, 1, 1, 1, 1, 1, 1, 1, 1, 1, 1, 1, 1, 1, 1, 1, 1, 1, 1, 1, 1, 1, 1, 1, 1, 1, 1, 1, 1, 1, 1, 1, 1, 1, 1, 1, 1, 1, 1, 1, 1, 1, 1, 1, 1, 1, 1, 1, 1, 1, 1, 1, 1, 1, 1, 1, 1, 1, 1, 1, 1, 1, 1, 1, 1, 1, 1, 1, 1, 1, 1, 1, 1, 1, 1, 1, 1, 1, 1, 1, 1, 1, 1, 1, 1, 1, 1, 1, 1, 1, 1, 1, 1, 1, 1, 1, 1, 1, 1, 1, 1, 1, 1, 1, 1, 1, 1, 1, 1, 1, 1, 1, 1, 1, 1, 1, 1, 1, 1, 1, 1, 1, 1, 1, 1, 1, 1, 1, 1, 1, 1, 1, 1, 1, 1, 1, 1, 1, 1, 1, 1, 1, 1, 1, 1, 1, 1, 1, 1, 1, 1, 1, 1, 1, 1, 1, 1, 1, 1, 1, 1, 1, 1, 1, 1, 1, 1, 1, 1, 1, 1, 1, 1, 1, 1, 1, 1, 1, 1, 1, 1, 1, 1, 1, 1, 1, 1, 1, 1, 1, 1, 1, 1, 1, 1, 1, 1, 1, 1, 1, 1, 1, 1, 1, 1, 1, 1, 1, 1, 1, 1, 1, 1, 1, 1, 1, 1, 1, 1, 1, 1, 1, 1, 1, 1, 1, 1, 1, 1, 1, 1, 1, 1, 1, 1, 1, 1, 1, 1, 1, 1, 1, 1, 1, 1, 1, 1, 1, 1, 1, 1, 1, 1, 1, 1, 1, 1, 1, 1, 1, 1, 1, 1, 1, 1, 1, 1, 1, 1, 1, 1, 1, 1, 1, 1, 1, 1, 1, 4 ),
 ( 0.000000000000000000, 0.002599878613971510263, 0.005208762566300055921, 0.007813076245110234588, 0.01041697056762492211, 0.01302017924898362516, 0.01562522799165661294, 0.01822895742955179393, 0.02083332403451576206, 0.02343772221867868391, 0.02604143078293654281, 0.02864626161639613477, 0.03124961764961396021, 0.03385452714844047750, 0.03645799780571232912, 0.03906266225314121432, 0.04166671052383312535, 0.04427076094224517699, 0.04687542278318937439, 0.04947889361195772356, 0.05208380280015859759, 0.05468715921365963767, 0.05729198803509916865, 0.05989568673917144287, 0.06250009379223495087, 0.06510449848632135494, 0.06770819839843210397, 0.07031302545632363288, 0.07291638160390327694, 0.07552129054917994244, 0.07812475961953217751, 0.08072942239586503033, 0.08333346963797970408, 0.08593751866472883194, 0.08854217935802578821, 0.09114564884740632145, 0.09375055680876714925, 0.09635391199924973893, 0.09895873945611717570, 0.1015624370353711836, 0.1041668426700886191, 0.1067712463110160465, 0.1093749448896196713, 0.1119797708301935452, 0.1145831257515418783, 0.1171880334468678037, 0.1197915013940491491, 0.1223961628153678316, 0.1250002090321265524, 0.1276042567216372492, 0.1302089163955687523, 0.1328123846563000476, 0.1354172914881497103, 0.1380206455552074885, 0.1406254717515977581, 0.1432291683081768907, 0.1458335726268597532, 0.1484379753169847160, 0.1510416726638619811, 0.1536464975900906083, 0.1562498513865758776, 0.1588547579349887939, 0.1614582248604825021, 0.1640628850295551278, 0.1666669303230295940, 0.1692709767774011609, 0.1718756355346959253, 0.1744791026682601387, 0.1770840084736199360, 0.1796873615186004858, 0.1822921865574477218, 0.1848958821930496710, 0.1875002852981585977, 0.1901046871399069693, 0.1927083833567690418, 0.1953132073715553307, 0.1979165601445126987, 0.2005214656490191816, 0.2031249316542690642, 0.2057295906738217384, 0.2083336351460475244, 0.2109376804673406547, 0.2135423384106908962, 0.2161458045185324639, 0.2187507094003866837, 0.2213540615246011867, 0.2239588855088016361, 0.2265625803250888304, 0.2291669823190463362, 0.2317713834148095453, 0.2343750786033309830, 0.2369799018095430365, 0.2395832536602726381, 0.2421881582238437913, 0.2447916234102597566, 0.2473962813829825302, 0.2500003251359625422, 0.2526043694262022354, 0.2552090266582678346, 0.2578124918417971090, 0.2604173959030967600, 0.2630207472078238129, 0.2656255702402394725, 0.2682292643388430320, 0.2708336653240377978, 0.2734380657761767419, 0.2760417600379992398, 0.2786465825384744077, 0.2812499335682448476, 0.2838548372938197173, 0.2864583017627815864, 0.2890629587913320364, 0.2916670019270400371, 0.2942710452882197347, 0.2968757019116316509, 0.2994791662722288139, 0.3020840696158954564, 0.3046874202023847622, 0.3072922423858477359, 0.3098959358683710530, 0.3125003359471613118, 0.3151047358580104651, 0.3177084292947467969, 0.3203132511922952008, 0.3229166015023476888, 0.3255215044928377321, 0.3281249683456989308, 0.3307296245327063788, 0.3333336671530912065, 0.3359377096871765112, 0.3385423658045411677, 0.3411458294435600336, 0.3437507321724898035, 0.3463540821419661686, 0.3489589035792820537, 0.3515625965473047621, 0.3541669958220223235, 0.3567713952938928457, 0.3593750880071304721, 0.3619799094045394461, 0.3645832590960911834, 0.3671881614543835437, 0.3697916247924753486, 0.3723962802405443862, 0.3750003224475334518, 0.3776043642564660408, 0.3802090199703688222, 0.3828124829891406122, 0.3854173852062082184, 0.3880207346598750218, 0.3906255554538268782, 0.3932292480089087938, 0.3958336465818629857, 0.3984380457170473289, 0.4010417378083525053, 0.4036465588083897882, 0.4062499079826380477, 0.4088548098116001062, 0.4114582727362346981, 0.4140629275479489335, 0.4166669694434522730, 0.4192710106291533956, 0.4218756660421624782, 0.4244791285419997062, 0.4270840303500617607, 0.4296873793891050619, 0.4322921996424575197, 0.4348958918861421385, 0.4375002898596233591, 0.4401046887603987101, 0.4427083803313200949, 0.4453132010367379379, 0.4479165497948640051, 0.4505214511973463787, 0.4531249138098211726, 0.4557295680877478938, 0.4583336097736617210, 0.4609376504380365280, 0.4635423056527069874, 0.4661457677349071238, 0.4687506692368063055, 0.4713540179623986193, 0.4739588377779012651, 0.4765625298117197040, 0.4791669272880037522, 0.4817713260566358624, 0.4843750172087082362, 0.4869798377222476216, 0.4895831861654201811, 0.4921880872442612742, 0.4947915496458628049, 0.4973962034925555886, 0.5000002450707665691, 0.5026042853157074441, 0.5052089404345847523, 0.5078124022004342208, 0.5104173034990032720, 0.5130206520123070657, 0.5156254714926987726, 0.5182291634181735995, 0.5208335604995248946, 0.5234379592382720769, 0.5260416500730202838, 0.5286464704974140894, 0.5312498187267931105, 0.5338547195848227789, 0.5364581818768299204, 0.5390628353948335727, 0.5416668769672219330, 0.5442709168946127107, 0.5468755720202369552, 0.5494790335710144635, 0.5520839347690799093, 0.5546872831712518215, 0.5572921024192640793, 0.5598957943379132551, 0.5625001911265891108, 0.5651045899377058479, 0.5677082805566486812, 0.5703131009946261765, 0.5729164491113668545, 0.5755213498514099024, 0.5781248121350983649, 0.5807294654269519185, 0.5833335070953961088, 0.5859375468071157389, 0.5885422020420250089, 0.5911456634790059894, 0.5937505646793920233, 0.5963539130715860281, 0.5989587321899475514, 0.6015624242032879820, 0.6041668208015419372, 0.6067712197872831004, 0.6093749102919370220, 0.6119797308462270324, 0.6145830789514836745, 0.6171879796763642956, 0.6197914420530098445, 0.6223960952212510556, 0.6250001370876311357, 0.6276041766855571247, 0.6302088321322918407, 0.6328122935567517260, 0.6354171948622837629, 0.6380205433456558328, 0.6406253624370956690, 0.6432290546466469250, 0.6458334511567334069, 0.6484378504193577530, 0.6510415409112403351, 0.6536463616845760161, 0.6562497098795055939, 0.6588546106920506462, 0.6614580732629331550, 0.6640627264101022220, 0.6666667685763031370, 0.6692708081623160998, 0.6718754639234225667, 0.6744789254366408970, 0.6770838269501499029, 0.6796871756258610064, 0.6822919947931124218, 0.6848956873004010681, 0.6875000838245786117, 0.6901044834663523364, 0.6927081740469867022, 0.6953129951421085364, 0.6979163435278744609, 0.7005212445309179081, 0.7031247073973251327, 0.7057293606259679164, 0.7083334031938842701, 0.7109374428698714832, 0.7135420990479055536, 0.7161455607511696408, 0.7187504625754957965, 0.7213538115447158949, 0.7239586308905210377, 0.7265623237970838533, 0.7291667204376187650, 0.7317711205608201652, 0.7343748113317387638, 0.7369796328513985584, 0.7395829815291747877, 0.7421878828255610294, 0.7447913460887924941, 0.7473959995014650692, 0.7500000425730045661, 0.7526040824408628538, 0.7552087391383944803, 0.7578122011330034047, 0.7604171033709996586, 0.7630204527349119248, 0.7656252723620247114, 0.7682289657694127971, 0.7708333626285834850, 0.7734377633355060677, 0.7760414543982535607, 0.7786462764452187768, 0.7812496255161931469, 0.7838545272087811266, 0.7864579909701516769, 0.7890626446694239959, 0.7916666883465109938, 0.7942707285081521684, 0.7968753858277685120, 0.7994788482150362308, 0.8020837509695725176, 0.8046871008293766669, 0.8072919208405671121, 0.8098956148503495545, 0.8125000120304503026, 0.8151044134234068927, 0.8177081048795449281, 0.8203129275566022338, 0.8229162771219805661, 0.8255211793136476572, 0.8281246436744912343, 0.8307292977629509023, 0.8333333421475307423, 0.8359373827048843797, 0.8385420407491936956, 0.8411455036304537058, 0.8437504070044209437, 0.8463537574613370085, 0.8489585779593948889, 0.8515622726731627568, 0.8541666702765071673, 0.8567710724578335713, 0.8593747644089445581, 0.8619795878189033811, 0.8645829379799131464, 0.8671878407735589267, 0.8697913058352330085, 0.8723959604154888359, 0.8750000056095312839, 0.8776040466645483873, 0.8802087055361843548, 0.8828121690127931354, 0.8854170731091063340, 0.8880204242643787715, 0.8906252453521178447, 0.8932289408714879642, 0.8958333390004131758, 0.8984377420724726226, 0.9010414346201626179, 0.9036462588658594752, 0.9062496097237539017, 0.9088545132223035949, 0.9114579790861923048, 0.9140626342608790811, 0.9166666803663815477, 0.9192707220210388774, 0.9218753818226663732, 0.9244788459960084914, 0.9270837509176034219, 0.9296871028724987829, 0.9322919246527909820, 0.9348956210794385768, 0.9375000198362011261, 0.9401044239011964176, 0.9427081171475072408, 0.9453129423329229564, 0.9479162939871883520, 0.9505211982878988275, 0.9531246650646376661, 0.9557293209618126228, 0.9583333680330715643, 0.9609374102905526849, 0.9635420713365114853, 0.9661455366701111602, 0.9687504417289087844, 0.9713537931426093897, 0.9739586182492501187, 0.9765623229037746489, 0.9791667147516245340, 0.9817710778420317697, 0.9843748014325267581, 0.9869798465897002826, 0.9895830499482988207, 0.9921869381715581193, 0.9947912477285243416, 0.9974001254724073062, 1.000000000000000000 ),
 .UNSPECIFIED. ) ;
#19564=CARTESIAN_POINT ( 'NONE',  ( 4.845371438081495619, 0.6875289519675978900, -2.081009137124201658 ) ) ;
#19565=CARTESIAN_POINT ( 'NONE',  ( 5.983493387795983054, 2.135156284703492169, -0.8757408730279289122 ) ) ;
#19566=CARTESIAN_POINT ( 'NONE',  ( 1.340775744366573541, 0.4011420747369342510, 2.021288966927562214 ) ) ;
#19567=CARTESIAN_POINT ( 'NONE',  ( 3.521366475706534160, -1.157360712602263808, -1.559242563676524584 ) ) ;
#19569=CARTESIAN_POINT ( 'NONE',  ( 5.800035319642947051, -1.870726058474009079, -0.0005997126256013226653 ) ) ;
#19572=CARTESIAN_POINT ( 'NONE',  ( 0.4383029422423733168, 0.9912079340955775031, 1.422354019259955304 ) ) ;
#19575=CARTESIAN_POINT ( 'NONE',  ( 4.623672751230786027, 0.3474658942751900903, 1.986100912583692812 ) ) ;
#19579=CARTESIAN_POINT ( 'NONE',  ( 1.945663734523142230, 0.6997465788082489757, -1.686465609443507763 ) ) ;
#19588=CARTESIAN_POINT ( 'NONE',  ( 6.217445935018812264, 1.680332259792745475, 1.120195391490413472 ) ) ;
#19589=CARTESIAN_POINT ( 'NONE',  ( 6.410783699188008278, -0.5891560598917375824, -2.141663135048486044 ) ) ;
#19590=ORIENTED_EDGE ( 'NONE', *, *, #143420, .F. ) ;
#19593=CARTESIAN_POINT ( 'NONE',  ( 5.541890059496114240, 0.8373154222949423797, -1.883320703650725125 ) ) ;
#19594=CARTESIAN_POINT ( 'NONE',  ( 5.168592345394213972, 1.356298078840772803, 1.492257005506091971 ) ) ;
#19603=CARTESIAN_POINT ( 'NONE',  ( 5.395861176733054876, 0.1455124041884261754, 2.010896217931843921 ) ) ;
#19604=CARTESIAN_POINT ( 'NONE',  ( 3.011469152984513009, -0.9080073089506625061, -1.601583425259824001 ) ) ;
#19605=CARTESIAN_POINT ( 'NONE',  ( 0.07661050522431848975, 5.726661425590173771, -2.304854160881860903 ) ) ;
#19606=CARTESIAN_POINT ( 'NONE',  ( 2.543975960257907953, -1.711040505396358657, -1.548661362299937228 ) ) ;
#19608=CARTESIAN_POINT ( 'NONE',  ( 4.569695524216377258, 2.097929177840287540, -0.5203329012281321386 ) ) ;
#19610=CARTESIAN_POINT ( 'NONE',  ( 0.5209107642259405146, -1.843744896352221829, 0.6102272969235060796 ) ) ;
#19614=CARTESIAN_POINT ( 'NONE',  ( 3.168673215318769110, -1.727878594304608217, -0.7172629358194044791 ) ) ;
#19615=CARTESIAN_POINT ( 'NONE',  ( 0.5968690581132638506, 1.641441770537595435, -1.091469919712923176 ) ) ;
#19618=CARTESIAN_POINT ( 'NONE',  ( 1.260703874955213744, 0.8971468365699288849, 2.016480257658866737 ) ) ;
#19624=CARTESIAN_POINT ( 'NONE',  ( 6.754760782388981255, -1.524083220479439005, 1.250168222439652421 ) ) ;
#19625=CARTESIAN_POINT ( 'NONE',  ( 6.358097629954328589, 2.302029506726857466, -0.1628147022267756039 ) ) ;
#19626=CARTESIAN_POINT ( 'NONE',  ( 0.9066075625437097774, 0.5660373911110065936, 1.878450800843839419 ) ) ;
#19627=CARTESIAN_POINT ( 'NONE',  ( 3.977431857364383205, -0.1567958407116451236, 2.056696387209145716 ) ) ;
#19635=CARTESIAN_POINT ( 'NONE',  ( 6.496539221175353873, 2.146586416477539672, 0.3252249059467678394 ) ) ;
#19637=CARTESIAN_POINT ( 'NONE',  ( 6.093280168761200599, -0.6138376400152152357, 1.736067454429328416 ) ) ;
#19641=CARTESIAN_POINT ( 'NONE',  ( 0.8779421195594695471, -1.044212112285093585, 1.551753832453220294 ) ) ;
#19645=CARTESIAN_POINT ( 'NONE',  ( 1.488763880571320808, -1.816176428755595706, -0.5988469716494762007 ) ) ;
#19646=CARTESIAN_POINT ( 'NONE',  ( 2.676313443976061190, -1.692906749566702507, -0.5160995803213176414 ) ) ;
#19648=CARTESIAN_POINT ( 'NONE',  ( 1.119614361207950548, -0.4638517909370845071, 1.855054000551699778 ) ) ;
#19650=CARTESIAN_POINT ( 'NONE',  ( 4.147977739690055898, 0.9062469702798245930, 1.687694244345463224 ) ) ;
#19652=CARTESIAN_POINT ( 'NONE',  ( 5.266046268760843141, -1.960244874886694744, 0.1909964021715639393 ) ) ;
#19653=CARTESIAN_POINT ( 'NONE',  ( 1.055114822555893728, 0.4192091730233596381, 2.078585086915801128 ) ) ;
#19655=CARTESIAN_POINT ( 'NONE',  ( 4.434354141042872399, 1.834536173243521917, 0.3649259964926266364 ) ) ;
#19656=CARTESIAN_POINT ( 'NONE',  ( 5.900961842893762466, 1.406060569669766114, -0.9988219321918601068 ) ) ;
#19658=CARTESIAN_POINT ( 'NONE',  ( 3.000804911251079510, -0.6410980074830170405, -2.111705341948390657 ) ) ;
#19661=CARTESIAN_POINT ( 'NONE',  ( 0.9946673667629982729, 2.031838985545178389, 0.3545390999590279368 ) ) ;
#19668=CARTESIAN_POINT ( 'NONE',  ( 3.385274849524767316, 0.04804411014160993310, 2.069964801482151895 ) ) ;
#19672=CARTESIAN_POINT ( 'NONE',  ( 0.9440171659906453350, -1.283125807103436600, -1.559678575094858077 ) ) ;
#19674=CARTESIAN_POINT ( 'NONE',  ( 0.1745949693968874838, 0.2569705180060793404, -1.790672585839627740 ) ) ;
#19676=CARTESIAN_POINT ( 'NONE',  ( 6.556017512941495262, 1.755498886817616677, -0.9912500394320120645 ) ) ;
#19677=CARTESIAN_POINT ( 'NONE',  ( 6.034394305845959927, 0.6080466156053351279, 1.816710885969755163 ) ) ;
#19678=CARTESIAN_POINT ( 'NONE',  ( 6.639320575229281651, -0.0007625845807879281287, 2.103388539994067497 ) ) ;
#19679=CARTESIAN_POINT ( 'NONE',  ( 3.333693798916517625, 0.9835563995168915552, -1.958507884819527867 ) ) ;
#19683=CARTESIAN_POINT ( 'NONE',  ( 3.269685606991072468, 0.4601866041431811327, -1.856093204100267124 ) ) ;
#19687=CARTESIAN_POINT ( 'NONE',  ( 0.6675924852559199651, 1.356316336250670496, 1.492241973137248934 ) ) ;
#19689=CARTESIAN_POINT ( 'NONE',  ( -0.09359539843449991847, -0.9867227890145138236, -2.066685918926200571 ) ) ;
#19691=CARTESIAN_POINT ( 'NONE',  ( 4.541862270049739969, 0.7358753100316551832, -1.560062421326340987 ) ) ;
#19693=CARTESIAN_POINT ( 'NONE',  ( 0.1399997263885794929, 4.089933038008564559, -2.554595152914000078 ) ) ;
#19697=CARTESIAN_POINT ( 'NONE',  ( 1.680054527999317759, -1.087118939145682583, -1.632918184844594611 ) ) ;
#19700=CARTESIAN_POINT ( 'NONE',  ( 0.07536363704233400851, 2.864322694550157866, -2.632457840217194089 ) ) ;
#19704=CARTESIAN_POINT ( 'NONE',  ( 4.406777823604307365, -0.4013596350818599556, -1.766266891646672166 ) ) ;
#19708=CARTESIAN_POINT ( 'NONE',  ( 5.303285216261115487, 1.594816061929973827, -0.8590795265051922591 ) ) ;
#19713=CARTESIAN_POINT ( 'NONE',  ( 6.689920442068890694, -1.216917952458838270, -1.408172490277598721 ) ) ;
#19715=CARTESIAN_POINT ( 'NONE',  ( 2.601083430876732105, -0.1850255667073404386, 1.906624535778883578 ) ) ;
#19722=CARTESIAN_POINT ( 'NONE',  ( 0.8663662989462637132, 1.066309655776727539, 1.880320099339624296 ) ) ;
#19725=CARTESIAN_POINT ( 'NONE',  ( 0.9908991873810431006, 1.612194894691898250, -0.8564790819722142290 ) ) ;
#19727=CARTESIAN_POINT ( 'NONE',  ( 2.696107482849848580, -1.820545782403935720, -0.1364615833806467338 ) ) ;
#19730=CARTESIAN_POINT ( 'NONE',  ( 1.863391182279940494, -1.538030936729195552, -1.136358088520472931 ) ) ;
#19731=CARTESIAN_POINT ( 'NONE',  ( 3.156658437648862225, -0.5693117071641734528, -1.885488911330883255 ) ) ;
#19732=CARTESIAN_POINT ( 'NONE',  ( 3.298316653532318732, 1.529317551288728483, -1.196868631420761053 ) ) ;
#19735=CARTESIAN_POINT ( 'NONE',  ( 4.131183091185314460, 1.940096312829143299, 0.8565103500411813675 ) ) ;
#19742=CARTESIAN_POINT ( 'NONE',  ( 4.371595934376539816, 1.770262903079304451, -0.4459408992859363319 ) ) ;
#19748=CARTESIAN_POINT ( 'NONE',  ( 4.557402362779487959, 0.4096945884842878582, -1.825068887194372991 ) ) ;
#19750=CARTESIAN_POINT ( 'NONE',  ( 3.105993306306195301, -1.924270352051945299, 0.09518456514568535143 ) ) ;
#19751=CARTESIAN_POINT ( 'NONE',  ( 6.789906393989944888, -1.279003670332454989, -1.487618534420579897 ) ) ;
#19757=CARTESIAN_POINT ( 'NONE',  ( 1.423615893443540337, -1.536295912932123642, -1.457111741773434943 ) ) ;
#19760=CARTESIAN_POINT ( 'NONE',  ( 6.754741982670550371, -0.5462536098296210119, -1.996853278248729824 ) ) ;
#19761=CARTESIAN_POINT ( 'NONE',  ( 0.7492455685023796663, 1.839184785914184994, -0.09005233288367914257 ) ) ;
#19763=CARTESIAN_POINT ( 'NONE',  ( 0.2635768167446932986, -2.297931531924101822, -0.05306211189425556751 ) ) ;
#19766=CARTESIAN_POINT ( 'NONE',  ( 1.623385997035782013, -2.157220310706788435, 0.7755101668525423708 ) ) ;
#19770=CARTESIAN_POINT ( 'NONE',  ( 6.562452659285362699, -1.776534117310492711, -0.7846822752179910543 ) ) ;
#19774=CARTESIAN_POINT ( 'NONE',  ( 1.072522059793120652, 0.8197897455473095452, 1.838922316899212372 ) ) ;
#19775=CARTESIAN_POINT ( 'NONE',  ( 6.403528931544730796, -1.954801056786956259, 0.4946215565981848528 ) ) ;
#19779=CARTESIAN_POINT ( 'NONE',  ( 3.310569631373377231, 1.890246369116010960, 0.8934441069041214600 ) ) ;
#19780=CARTESIAN_POINT ( 'NONE',  ( 1.129378208368720271, -1.118813933885588474, -1.371354111526525754 ) ) ;
#19783=CARTESIAN_POINT ( 'NONE',  ( 5.578174268327147800, -2.235363620237617255, -0.5069547310770585735 ) ) ;
#19784=CARTESIAN_POINT ( 'NONE',  ( 3.275097224137039742, 1.105054647683247460, 1.344453793780414186 ) ) ;
#19787=CARTESIAN_POINT ( 'NONE',  ( 3.690549081386824248, -1.031632686913460883, -1.393354295182136715 ) ) ;
#19788=CARTESIAN_POINT ( 'NONE',  ( 3.139314614211644816, -0.1572037376256547880, -2.165524352769617078 ) ) ;
#19790=CARTESIAN_POINT ( 'NONE',  ( 4.153529959351897283, 1.954779968807466295, -0.4946301968136583849 ) ) ;
#19791=CARTESIAN_POINT ( 'NONE',  ( 1.437500000000001110, 1.451031289061064156, -1.451031289061176288 ) ) ;
#19793=CARTESIAN_POINT ( 'NONE',  ( 1.694233118518298165, -1.916858602850049609, -0.1915058630488040703 ) ) ;
#19795=CARTESIAN_POINT ( 'NONE',  ( 5.941669428368816952, -2.091911387875099670, 0.7476460515099275783 ) ) ;
#19797=CARTESIAN_POINT ( 'NONE',  ( -0.1106856583840878927, 5.722746153615347886, -2.590994828783958592 ) ) ;
#19802=CARTESIAN_POINT ( 'NONE',  ( 0.9443249964648057215, -1.413213925058560028, -1.713760899525147874 ) ) ;
#19803=CARTESIAN_POINT ( 'NONE',  ( 6.197705743426439540, -1.420020466879829302, -1.353909852041992767 ) ) ;
#19806=CARTESIAN_POINT ( 'NONE',  ( 0.3335754702045168330, -1.976410766185803691, 0.8757516042032786885 ) ) ;
#19809=CARTESIAN_POINT ( 'NONE',  ( 4.633292856664962933, 0.003200217577232782832, -2.062851381006901352 ) ) ;
#19813=CARTESIAN_POINT ( 'NONE',  ( 6.204356031920277736, -0.6731288877953770511, -1.745422550748019441 ) ) ;
#19814=CARTESIAN_POINT ( 'NONE',  ( 4.236742506082516790, 1.733672338021419179, -0.04812345329192367627 ) ) ;
#19815=CARTESIAN_POINT ( 'NONE',  ( 3.280519990774858119, 1.572054556770419387, -0.7471684773981291938 ) ) ;
#19818=CARTESIAN_POINT ( 'NONE',  ( 1.681587762198969216, 1.584507396495305587, 1.656812167128306035 ) ) ;
#19820=CARTESIAN_POINT ( 'NONE',  ( 5.407793395736015363, -0.9409669688741102433, -1.867122848840888416 ) ) ;
#19821=CARTESIAN_POINT ( 'NONE',  ( 0.1109373197970727615, -1.806229982939497658, 0.3559056038356380736 ) ) ;
#19823=CARTESIAN_POINT ( 'NONE',  ( 1.776017750421728270, 1.753029812786778940, -0.9963028777105964462 ) ) ;
#19824=CARTESIAN_POINT ( 'NONE',  ( 0.2170718473699268236, -0.1031819972749977166, 2.189145592210713698 ) ) ;
#19828=CARTESIAN_POINT ( 'NONE',  ( 2.526173596586390957, -2.097057114080549844, 0.3136139059176298871 ) ) ;
#19831=CARTESIAN_POINT ( 'NONE',  ( 5.514214477338500231, -0.8245889995748825196, -1.628937154514856545 ) ) ;
#19837=CARTESIAN_POINT ( 'NONE',  ( 2.250265822158686646, 0.9482326530925830887, -1.783330763309778577 ) ) ;
#19838=CARTESIAN_POINT ( 'NONE',  ( 6.229534195615700654, -2.079954537573494466, 0.7377168454194837910 ) ) ;
#19840=CARTESIAN_POINT ( 'NONE',  ( 4.610102165239228889, 1.860615736367857265, -0.04253844368732987574 ) ) ;
#19846=CARTESIAN_POINT ( 'NONE',  ( 5.514214477338500231, -0.8245889995748825196, -1.628937154514856545 ) ) ;
#19850=CARTESIAN_POINT ( 'NONE',  ( 1.422726403049366706, 0.6964842469411072212, 1.588000322196560399 ) ) ;
#19851=CARTESIAN_POINT ( 'NONE',  ( 0.2162406733101406298, -0.09061050886127393345, 1.738091409524551878 ) ) ;
#19852=CARTESIAN_POINT ( 'NONE',  ( 5.883493432195608719, 2.134490442297873880, -0.8776364701479767438 ) ) ;
#19855=CARTESIAN_POINT ( 'NONE',  ( 1.704443381354688203, -0.7389896827423731995, -1.923919429860524888 ) ) ;
#19857=CARTESIAN_POINT ( 'NONE',  ( 0.3157796101352361440, -1.620936768121715499, 1.198674607299075934 ) ) ;
#19861=CARTESIAN_POINT ( 'NONE',  ( 0.2331951027847931901, -1.803461566636242797, 0.7967608462288151561 ) ) ;
#19863=CARTESIAN_POINT ( 'NONE',  ( 3.340010735810138520, -1.142844047782382466, -1.533173144288489276 ) ) ;
#19865=CARTESIAN_POINT ( 'NONE',  ( 4.740968412965463230, 0.3751893352213676591, 2.174603215771487630 ) ) ;
#19870=CARTESIAN_POINT ( 'NONE',  ( 6.481110812017948142, -1.938455339442773706, -0.8599551062365148324 ) ) ;
#19872=CARTESIAN_POINT ( 'NONE',  ( 3.153680125570026416, -1.885591857120081372, -1.329971080218894874 ) ) ;
#19873=CARTESIAN_POINT ( 'NONE',  ( 4.949637131784443866, 1.452432516441283905, 1.319008059494260143 ) ) ;
#19874=CARTESIAN_POINT ( 'NONE',  ( 0.9187138386215136787, -1.424830647414500051, 1.348730089142296418 ) ) ;
#19878=CARTESIAN_POINT ( 'NONE',  ( 0.5677576367011258895, 1.426771234092726104, 1.564575111376417915 ) ) ;
#19880=CARTESIAN_POINT ( 'NONE',  ( -0.02377707250108065939, -0.1326659201078099481, -1.811169398030491928 ) ) ;
#19881=CARTESIAN_POINT ( 'NONE',  ( 3.133805249272236804, 2.063032676455050396, -0.6766426178266419234 ) ) ;
#19883=CARTESIAN_POINT ( 'NONE',  ( 0.5102161431939798986, -0.7575819503438313562, 1.980855387931411915 ) ) ;
#19888=CARTESIAN_POINT ( 'NONE',  ( 1.722021792205346902, -1.142311743720581196, -1.714993188781144928 ) ) ;
#19894=CARTESIAN_POINT ( 'NONE',  ( 3.984940423737866055, -1.785409543757199291, -0.6854135386504257577 ) ) ;
#19898=CARTESIAN_POINT ( 'NONE',  ( 0.8788404743438563704, -1.638286771785288254, -0.7734350870383081000 ) ) ;
#19900=CARTESIAN_POINT ( 'NONE',  ( 1.252998012795783822, 0.1371590870133630458, -1.910833894730893601 ) ) ;
#19901=CARTESIAN_POINT ( 'NONE',  ( 1.838419004579601834, -1.109345826794335688, 1.747895861591180156 ) ) ;
#19904=CARTESIAN_POINT ( 'NONE',  ( 1.041797052332312568, 0.8010751512182741063, -1.801556251716707413 ) ) ;
#19905=CARTESIAN_POINT ( 'NONE',  ( 5.426370213035293766, 1.145732239094964466, -1.548636736622555299 ) ) ;
#19906=CARTESIAN_POINT ( 'NONE',  ( 6.674453038267287752, -1.361800985140369402, 1.737325302230605883 ) ) ;
#19909=CARTESIAN_POINT ( 'NONE',  ( 4.193840287544727374, -1.420164769765386303, -1.496150262111215934 ) ) ;
#19914=CARTESIAN_POINT ( 'NONE',  ( 5.297925755477892906, -0.7609016685872365127, 1.963875245004148562 ) ) ;
#19916=CARTESIAN_POINT ( 'NONE',  ( 0.1335669894368500255, -0.0009366757763962055587, -2.153671288142432250 ) ) ;
#19918=CARTESIAN_POINT ( 'NONE',  ( 4.692742333269261934, -0.4685372120167423660, -2.110058259655919422 ) ) ;
#19919=CARTESIAN_POINT ( 'NONE',  ( 4.371743357251212103, 0.4404049503993580639, -1.970906944672585315 ) ) ;
#19925=CARTESIAN_POINT ( 'NONE',  ( 2.378138974734815392, -2.011451771401792321, -0.1435188914247695346 ) ) ;
#19933=CARTESIAN_POINT ( 'NONE',  ( 4.605092316430917876, -0.09611821078869468848, 2.014234682242924457 ) ) ;
#19935=CARTESIAN_POINT ( 'NONE',  ( 0.6973489402126078485, -0.6253137818992074992, 1.607738891190332753 ) ) ;
#19940=CARTESIAN_POINT ( 'NONE',  ( 5.817618194842751222, -1.825074353437942554, 0.4092329068215995180 ) ) ;
#19941=CARTESIAN_POINT ( 'NONE',  ( 0.2408851659233458842, 1.927091567462356547, 0.5821649069043339786 ) ) ;
#19945=CARTESIAN_POINT ( 'NONE',  ( 0.7906389332529573100, 1.525030349845598820, -1.319245847334844735 ) ) ;
#19946=CARTESIAN_POINT ( 'NONE',  ( 1.318313199092124188, -0.6538357601561273214, -1.689641652304620045 ) ) ;
#19948=CARTESIAN_POINT ( 'NONE',  ( 6.332923096303629151, 0.2067577541180857514, 2.151790036905242953 ) ) ;
#19954=CARTESIAN_POINT ( 'NONE',  ( 0.7607752342545861524, -0.05021853532924521607, -1.915246365852550037 ) ) ;
#19962=CARTESIAN_POINT ( 'NONE',  ( 3.643588467267334874, -1.635511012911139650, -1.413612897787956513 ) ) ;
#19965=CARTESIAN_POINT ( 'NONE',  ( 0.5629301599625028407, 0.6213668382478373386, 2.027498709647377773 ) ) ;
#19968=CARTESIAN_POINT ( 'NONE',  ( 2.284392081957301812, -1.932574240873608629, -0.3883164474826616419 ) ) ;
#19969=CARTESIAN_POINT ( 'NONE',  ( 5.080287894202283105, 0.9478536798121822704, 1.660923459347658282 ) ) ;
#19972=CARTESIAN_POINT ( 'NONE',  ( 5.810992205472774508, -1.553620646631387991, 1.210443464816546744 ) ) ;
#19973=CARTESIAN_POINT ( 'NONE',  ( 0.4978614556471228081, -0.6533520819593687801, -1.828864621591755002 ) ) ;
#19979=CARTESIAN_POINT ( 'NONE',  ( 5.514289750425454883, -1.912461473380810961, 0.004301308668797076962 ) ) ;
#19981=CARTESIAN_POINT ( 'NONE',  ( 3.176612885197922953, -1.314426786483071208, 1.772596291930063961 ) ) ;
#19982=CARTESIAN_POINT ( 'NONE',  ( 1.923171073188837843, 2.059116738528983692, 0.7940920450543451636 ) ) ;
#19984=CARTESIAN_POINT ( 'NONE',  ( 0.8207898099904624711, 1.447681275506585541, -1.249484660484905030 ) ) ;
#19988=CARTESIAN_POINT ( 'NONE',  ( 3.174344110969638866, -1.018096006688212096, -1.802650257252853772 ) ) ;
#19993=CARTESIAN_POINT ( 'NONE',  ( 0.7433210806352362754, -1.853469564684958382, 1.112228649290482263 ) ) ;
#19994=CARTESIAN_POINT ( 'NONE',  ( 2.454835928891830221, -1.908367152989149718, -1.077367144120815023 ) ) ;
#20000=CARTESIAN_POINT ( 'NONE',  ( 6.486931489777390425, -1.733547045345487758, 0.05303144115107599060 ) ) ;
#20003=CARTESIAN_POINT ( 'NONE',  ( 4.012602964903419611, 0.7404812365185129419, 1.933494928807255375 ) ) ;
#20004=CARTESIAN_POINT ( 'NONE',  ( 4.183301248788100501, 1.701634275673917784, 1.259637755991403374 ) ) ;
#20007=CARTESIAN_POINT ( 'NONE',  ( 3.203910658309446990, 0.7132968404394635087, -1.835904812064126590 ) ) ;
#20008=CARTESIAN_POINT ( 'NONE',  ( 0.5098338327763075606, -0.6861045072398126443, 1.785269576063217567 ) ) ;
#20009=CARTESIAN_POINT ( 'NONE',  ( 4.752058238528302780, 0.8743775744927633209, 2.119134945200305431 ) ) ;
#20010=CARTESIAN_POINT ( 'NONE',  ( 2.525780997283606499, -1.050937884436175418, -1.492673824175783093 ) ) ;
#20014=CARTESIAN_POINT ( 'NONE',  ( 3.972906070543721579, -1.488974544083881746, 1.355118003239277336 ) ) ;
#20015=CARTESIAN_POINT ( 'NONE',  ( 4.873855640358407904, -1.924671727690111966, 0.3787619532854279436 ) ) ;
#20018=CARTESIAN_POINT ( 'NONE',  ( 0.1751657365761547513, 0.002452341591364578209, -2.044164811867712483 ) ) ;
#20019=CARTESIAN_POINT ( 'NONE',  ( 6.714806893291140888, -0.1599574331335733013, 2.055667697375664016 ) ) ;
#20020=CARTESIAN_POINT ( 'NONE',  ( 6.244957947127046438, -1.492741346086885024, 0.9504933407481640506 ) ) ;
#20022=CARTESIAN_POINT ( 'NONE',  ( 1.377182423176852133, 2.023737929115625445, -0.8412682346608522099 ) ) ;
#20023=CARTESIAN_POINT ( 'NONE',  ( 0.1162408695623952659, -0.08860816971513819917, 1.738289989025374016 ) ) ;
#20025=CARTESIAN_POINT ( 'NONE',  ( 0.2335667940002684184, 0.001055507091213009818, -2.153566573614831281 ) ) ;
#20026=CARTESIAN_POINT ( 'NONE',  ( 0.8380132626705768528, 1.698558605200460869, 0.2991625477344951323 ) ) ;
#20027=CARTESIAN_POINT ( 'NONE',  ( 0.4569821463788895644, 1.705326812283548765, 1.541052590308614745 ) ) ;
#20028=CARTESIAN_POINT ( 'NONE',  ( 0.8904706703079521279, -0.5376514911656914419, -2.124458794526106864 ) ) ;
#20029=CARTESIAN_POINT ( 'NONE',  ( 6.432912826982137844, 0.8947389043411910770, 1.484938929457087164 ) ) ;
#20030=CARTESIAN_POINT ( 'NONE',  ( 3.071135375186518690, -2.039199700013223815, -0.8442704067812344393 ) ) ;
#20033=CARTESIAN_POINT ( 'NONE',  ( 0.5499837882529658994, 1.607816289776839991, 1.459057700483844311 ) ) ;
#20035=CARTESIAN_POINT ( 'NONE',  ( 0.9720387486300664515, -0.9465246498777776241, 1.894042457640370491 ) ) ;
#20036=CARTESIAN_POINT ( 'NONE',  ( 6.620655732516649294, 2.950034989283246478, 2.626075342966327497 ) ) ;
#20037=CARTESIAN_POINT ( 'NONE',  ( 5.719733624436385000, -1.879402930333987198, 0.4222299131634628111 ) ) ;
#20039=CARTESIAN_POINT ( 'NONE',  ( 1.470720204089857930, -2.178542539925924171, -0.7136519110988813752 ) ) ;
#20043=CARTESIAN_POINT ( 'NONE',  ( 3.651236063859903069, 0.3270389233705518484, 2.196992388787385231 ) ) ;
#20049=CARTESIAN_POINT ( 'NONE',  ( 2.233046271152541618, 2.016033844848092560, 0.04667593304989729741 ) ) ;
#20051=CARTESIAN_POINT ( 'NONE',  ( 1.551709131853472368, 1.559248165652558082, 1.350213067335771511 ) ) ;
#20053=CARTESIAN_POINT ( 'NONE',  ( 0.01093749962182561514, -1.805946196879631094, 0.3578947576599255664 ) ) ;
#20056=CARTESIAN_POINT ( 'NONE',  ( 1.723279953462612202, 1.994870059565261755, 0.2930690452552578429 ) ) ;
#20057=CARTESIAN_POINT ( 'NONE',  ( -0.02423404108400224743, -1.785672699080865788, -0.4486397487279417118 ) ) ;
#20058=CARTESIAN_POINT ( 'NONE',  ( 5.021132725759672510, -2.177342503763429082, 0.7171727232720275236 ) ) ;
#20059=CARTESIAN_POINT ( 'NONE',  ( 3.556447125109524876, -1.624355972047783148, -0.8667379164201680641 ) ) ;
#20062=CARTESIAN_POINT ( 'NONE',  ( 4.313378725478684395, -0.3118687524542098632, 1.798583714455632476 ) ) ;
#20063=CARTESIAN_POINT ( 'NONE',  ( 4.852185490356213826, 0.1948433276699329531, -2.006959737079899497 ) ) ;
#20065=CARTESIAN_POINT ( 'NONE',  ( 3.854571047428239527, 0.8115417623771915556, 2.112135835510853710 ) ) ;
#20067=CARTESIAN_POINT ( 'NONE',  ( 6.071333362910682041, 0.1583771919418910934, -2.100070647415654079 ) ) ;
#20069=CARTESIAN_POINT ( 'NONE',  ( 3.648938843998358106, -0.4010542052625790110, -2.030977206718207473 ) ) ;
#20074=CARTESIAN_POINT ( 'NONE',  ( 1.734862838405337060, 0.1885825406544305305, 1.917253122483292715 ) ) ;
#20077=CARTESIAN_POINT ( 'NONE',  ( 0.3441184698094986727, -0.9315698024882634876, 1.735327799219071210 ) ) ;
#20083=CARTESIAN_POINT ( 'NONE',  ( 2.039591900818237491, 0.005460781979979567602, 2.221583674558536892 ) ) ;
#20084=CARTESIAN_POINT ( 'NONE',  ( 3.610471823009605341, -0.8516972358460070947, -1.926234778997274244 ) ) ;
#20087=CARTESIAN_POINT ( 'NONE',  ( 0.5900176457281476328, 0.9615612750370464701, -1.593262740414502776 ) ) ;
#20093=CARTESIAN_POINT ( 'NONE',  ( 1.670341986359990205, 2.114562342887704283, -0.1611296783964668855 ) ) ;
#20096=CARTESIAN_POINT ( 'NONE',  ( 4.281663391851794565, -1.878042059144067633, 0.5673916069991248312 ) ) ;
#20097=CARTESIAN_POINT ( 'NONE',  ( 3.116266767097406909, -1.064116542966097922, -1.881565754655416756 ) ) ;
#20098=CARTESIAN_POINT ( 'NONE',  ( 1.997363575765517485, -1.840834563946552649, 0.04656924640939615057 ) ) ;
#20100=CARTESIAN_POINT ( 'NONE',  ( 5.138483783005516337, -1.490010379379594241, 0.8989716238894971401 ) ) ;
#20105=CARTESIAN_POINT ( 'NONE',  ( 2.342841879718413622, 0.4729757327756216601, 2.109170662781891359 ) ) ;
#20106=CARTESIAN_POINT ( 'NONE',  ( 3.778672575519220977, -1.986742196792599335, 0.3418835855632795795 ) ) ;
#20108=CARTESIAN_POINT ( 'NONE',  ( 1.376082401959723089, 1.288024388040419632, 1.735935173841046675 ) ) ;
#20110=CARTESIAN_POINT ( 'NONE',  ( 3.889495165534775811, 1.427134975246695969, 1.360358076685687978 ) ) ;
#20111=CARTESIAN_POINT ( 'NONE',  ( 6.609000000000047947, 7.629137130509099585, 2.499999999999994227 ) ) ;
#20112=CARTESIAN_POINT ( 'NONE',  ( 3.579573000355208645, -0.9547435552521261748, 1.691086383587044883 ) ) ;
#20117=CARTESIAN_POINT ( 'NONE',  ( -0.1108833634137010304, 0.2458664895051872190, -1.931623620491630611 ) ) ;
#20122=CARTESIAN_POINT ( 'NONE',  ( 0.08333923026508995024, -0.1592477204843331384, -2.171661519566956855 ) ) ;
#20124=CARTESIAN_POINT ( 'NONE',  ( 3.871884822249270108, -1.933460040528666379, 0.3310023857948928838 ) ) ;
#20126=CARTESIAN_POINT ( 'NONE',  ( 1.986954140179174155, -2.015912935764123670, 0.05229865529512293942 ) ) ;
#20128=CARTESIAN_POINT ( 'NONE',  ( 3.116528361068672481, 2.066776279341679956, 0.4593686614828630943 ) ) ;
#20132=CARTESIAN_POINT ( 'NONE',  ( 3.257574473681293270, 0.8286728953739975756, 1.644182576024610265 ) ) ;
#20136=CARTESIAN_POINT ( 'NONE',  ( 4.605793411009856619, 1.573235607984494688, 1.422142093439874522 ) ) ;
#20139=CARTESIAN_POINT ( 'NONE',  ( 5.237599208242285087, -1.454345255708370255, -1.460303020606460445 ) ) ;
#20141=CARTESIAN_POINT ( 'NONE',  ( 2.929072846782492245, -1.238530643895646488, -1.362589426554157157 ) ) ;
#20146=( BOUNDED_SURFACE ( )  B_SPLINE_SURFACE ( 3, 3, ( 
 ( #51132, #46081, #66274, #82551, #34856, #3415, #2341, #16471, #210683, #204, #164876 ),
 ( #112200, #99883, #53259, #144670, #135589, #134545, #119389, #169136, #52196, #185377, #118322 ),
 ( #62312, #194439, #83618, #178207, #184308, #35932, #102010, #116190, #69481, #36997, #29823 ),
 ( #165945, #149700, #148638, #168080, #198423, #50067, #98827, #1281, #67339, #133484, #19678 ),
 ( #85758, #23940, #106327, #38081, #107410, #170201, #121546, #172350, #6616, #190707, #140950 ),
 ( #73771, #90044, #156102, #7688, #58592, #87894, #205898, #57532, #203746, #72696, #153967 ),
 ( #138791, #187517, #204811, #123689, #139867, #189651, #41302, #155031, #124747, #42368, #56462 ) ),
 .UNSPECIFIED., .T., .F., .T. ) 
 B_SPLINE_SURFACE_WITH_KNOTS ( ( 4, 3, 4 ),
 ( 4, 1, 1, 1, 1, 1, 1, 1, 4 ),
 ( 0.000000000000000000, 0.5000000000000000000, 1.000000000000000000 ),
 ( 0.000000000000000000, 0.2256777920876190668, 0.3978457394851813711, 0.5256768607792676740, 0.6183602023682204241, 0.6850295134299612121, 0.7345374503969632762, 0.7752450576501028756, 1.000000000000000000 ),
 .UNSPECIFIED. ) 
 GEOMETRIC_REPRESENTATION_ITEM ( )  RATIONAL_B_SPLINE_SURFACE ( (
 ( 1.000000000000000000, 1.000000000000000000, 1.000000000000000000, 1.000000000000000222, 0.9999999999999997780, 1.000000000000000444, 0.9999999999999997780, 1.000000000000000222, 0.9999999999999996669, 1.000000000000000222, 1.000000000000000222),
 ( 0.3333333333333333703, 0.3333333333333334259, 0.3333333333333333703, 0.3333333333333334259, 0.3333333333333333703, 0.3333333333333334259, 0.3333333333333333703, 0.3333333333333334259, 0.3333333333333333148, 0.3333333333333334259, 0.3333333333333334259),
 ( 0.3333333333333333703, 0.3333333333333334259, 0.3333333333333333703, 0.3333333333333334259, 0.3333333333333333703, 0.3333333333333334259, 0.3333333333333333703, 0.3333333333333334259, 0.3333333333333333148, 0.3333333333333334259, 0.3333333333333334259),
 ( 1.000000000000000000, 1.000000000000000000, 1.000000000000000000, 1.000000000000000222, 0.9999999999999997780, 1.000000000000000444, 0.9999999999999997780, 1.000000000000000222, 0.9999999999999996669, 1.000000000000000222, 1.000000000000000222),
 ( 0.3333333333333333703, 0.3333333333333334259, 0.3333333333333333703, 0.3333333333333334259, 0.3333333333333333703, 0.3333333333333334259, 0.3333333333333333703, 0.3333333333333334259, 0.3333333333333333148, 0.3333333333333334259, 0.3333333333333334259),
 ( 0.3333333333333333703, 0.3333333333333334259, 0.3333333333333333703, 0.3333333333333334259, 0.3333333333333333703, 0.3333333333333334259, 0.3333333333333333703, 0.3333333333333334259, 0.3333333333333333148, 0.3333333333333334259, 0.3333333333333334259),
 ( 1.000000000000000000, 1.000000000000000000, 1.000000000000000000, 1.000000000000000222, 0.9999999999999997780, 1.000000000000000444, 0.9999999999999997780, 1.000000000000000222, 0.9999999999999996669, 1.000000000000000222, 1.000000000000000222) ) ) 
 REPRESENTATION_ITEM ( '' )  SURFACE ( )  );
#20148=CARTESIAN_POINT ( 'NONE',  ( 2.684424123961434816, -1.133677649706768431, 1.893296980138805097 ) ) ;
#20149=CARTESIAN_POINT ( 'NONE',  ( 4.763087504681410955, -2.017952330160921015, -1.023110994099560411 ) ) ;
#20151=CARTESIAN_POINT ( 'NONE',  ( 4.412255891540381114, -1.811360455869342578, -0.03765339742955660374 ) ) ;
#20152=CARTESIAN_POINT ( 'NONE',  ( 3.907376549751972572, -1.831493090834277249, 0.5616838290606884776 ) ) ;
#20154=CARTESIAN_POINT ( 'NONE',  ( 3.942224353883512222, 1.961846943226858597, 0.1946112770482635312 ) ) ;
#20155=CARTESIAN_POINT ( 'NONE',  ( 5.295714669793899709, -0.6724083694377264164, 1.745798414713333413 ) ) ;
#20156=CARTESIAN_POINT ( 'NONE',  ( 4.914427440023315441, 0.7117315627661743305, 1.719784830429422984 ) ) ;
#20158=CARTESIAN_POINT ( 'NONE',  ( -0.1531117392989979065, -1.803405091603600185, -0.9023890051431044945 ) ) ;
#20160=CARTESIAN_POINT ( 'NONE',  ( 2.121831256377606501, -2.042539606455844758, 0.5128510974094899755 ) ) ;
#20163=CARTESIAN_POINT ( 'NONE',  ( 0.07479286986305289098, 7.629137130509083597, -2.455503679634088776 ) ) ;
#20164=CARTESIAN_POINT ( 'NONE',  ( 2.988655875014298857, -1.259908772670719657, 1.705623289672608678 ) ) ;
#20166=CARTESIAN_POINT ( 'NONE',  ( 1.494405286683021306, -1.076835855708496936, 1.708581493997686662 ) ) ;
#20171=CARTESIAN_POINT ( 'NONE',  ( 2.231903258980330484, -1.410129017595105561, -1.638413920015222125 ) ) ;
#20179=CARTESIAN_POINT ( 'NONE',  ( 6.585487052573138378, -0.8941505307449393314, 1.888277625537030380 ) ) ;
#20181=CARTESIAN_POINT ( 'NONE',  ( 1.305971919559431704, -0.5478059591418303897, 2.195072679011981442 ) ) ;
#20188=CARTESIAN_POINT ( 'NONE',  ( 4.213312296666638979, -0.2916954692788272796, 1.699858598931931919 ) ) ;
#20190=CARTESIAN_POINT ( 'NONE',  ( 2.213771126746429729, -0.8293587345859743110, -1.563345763006577238 ) ) ;
#20191=B_SPLINE_CURVE_WITH_KNOTS ( 'NONE', 3,
 ( #43180, #141763, #209891, #157991, #90858, #159037, #189400, #76705, #191515, #110355, #106075 ),
 .UNSPECIFIED., .F., .F.,
 ( 4, 1, 1, 1, 1, 1, 1, 1, 4 ),
 ( 0.000000000000000000, 0.2256337125576066971, 0.3978389261578171299, 0.5257960283851228489, 0.6187025735204009225, 0.6856790771877526725, 0.7354782194756434022, 0.7762620033627533056, 0.9999999999999998890 ),
 .UNSPECIFIED. ) ;
#20192=CARTESIAN_POINT ( 'NONE',  ( 2.736979112881072762, 1.896321534115693819, 0.6760404272549996874 ) ) ;
#20193=CARTESIAN_POINT ( 'NONE',  ( 4.964015014492747291, 2.183396446337606989, -0.3195234977587738667 ) ) ;
#20195=CARTESIAN_POINT ( 'NONE',  ( 3.972919405334675691, -1.493746422221740699, 1.359666112553897355 ) ) ;
#20197=CARTESIAN_POINT ( 'NONE',  ( 4.429314653828757109, -1.560513098751922900, -1.277029310785951388 ) ) ;
#20198=CARTESIAN_POINT ( 'NONE',  ( 4.517698195727691157, -0.4766141805869225645, 1.747713001785702325 ) ) ;
#20203=CARTESIAN_POINT ( 'NONE',  ( 2.307302758404996545, -0.4121581357655336730, 1.824517092411604757 ) ) ;
#20205=CARTESIAN_POINT ( 'NONE',  ( 2.232540727315056373, 1.246330492051262784, -1.450604739030990187 ) ) ;
#20210=CARTESIAN_POINT ( 'NONE',  ( 0.1055216070770526038, 1.418477292093557329, 1.282857148695019989 ) ) ;
#20212=CARTESIAN_POINT ( 'NONE',  ( 1.416376618315864144, 0.7919773292732554815, 1.795081228748253377 ) ) ;
#20215=CARTESIAN_POINT ( 'NONE',  ( 4.500305224345508393, -0.9970752094022590217, 1.871535012320741265 ) ) ;
#20218=CARTESIAN_POINT ( 'NONE',  ( 5.061777102197771327, 1.950294035894485356, -0.2865203566276338654 ) ) ;
#20220=CARTESIAN_POINT ( 'NONE',  ( 1.037359019205979171, -0.04529029187893931357, 2.012842730658084278 ) ) ;
#20221=EDGE_LOOP ( 'NONE', ( #44618, #59558, #19590, #9328 ) ) ;
#20222=CARTESIAN_POINT ( 'NONE',  ( 1.212693198809017270, 2.041623912717607237, 0.5605823208302792571 ) ) ;
#20224=CARTESIAN_POINT ( 'NONE',  ( 2.383334800519558705, -0.002349189141126820958, 2.070544812199434315 ) ) ;
#20229=CARTESIAN_POINT ( 'NONE',  ( 4.804676392994963408, 1.818819718876990565, 1.030695182279812272 ) ) ;
#20231=CARTESIAN_POINT ( 'NONE',  ( 2.994927033977520470, 1.566606242385214731, -0.9370212210159312161 ) ) ;
#20232=CARTESIAN_POINT ( 'NONE',  ( 1.066738840199648042, -1.428349636637029407, 1.113955053652333493 ) ) ;
#20237=CARTESIAN_POINT ( 'NONE',  ( 5.790102700048296747, -0.9971039342967463748, 1.968745932239771568 ) ) ;
#20240=CARTESIAN_POINT ( 'NONE',  ( 4.512308969215598431, -1.911949174345693336, -0.04343532550177275214 ) ) ;
#20243=CARTESIAN_POINT ( 'NONE',  ( 6.742638474511262636, -2.029596885996234334, -0.4079607620106340260 ) ) ;
#20247=CARTESIAN_POINT ( 'NONE',  ( 5.706613541269077494, 1.932210019790636224, 1.034112652976440394 ) ) ;
#20253=CARTESIAN_POINT ( 'NONE',  ( 4.130043426961079511, 1.002751595458702738, -1.578879078160302818 ) ) ;
#20259=CARTESIAN_POINT ( 'NONE',  ( 6.772334134356085222, -0.9704686269969391432, -1.828672837219179392 ) ) ;
#20261=CARTESIAN_POINT ( 'NONE',  ( 0.7203276360899166786, 1.987051886588153682, 0.3419113104980234241 ) ) ;
#20265=CARTESIAN_POINT ( 'NONE',  ( 1.816621679704206516, 2.045545470589833492, 0.7867152234099920038 ) ) ;
#20266=CARTESIAN_POINT ( 'NONE',  ( 5.900976575431972293, 1.489821718068456979, -1.054992404821846863 ) ) ;
#20273=CARTESIAN_POINT ( 'NONE',  ( 3.315785976855676775, 1.165629053876730659, -1.425327459889616177 ) ) ;
#20274=CARTESIAN_POINT ( 'NONE',  ( 1.137358842852369545, -0.04729656459989117767, 2.012689239070045488 ) ) ;
#20275=CARTESIAN_POINT ( 'NONE',  ( 2.566106820329843163, 1.847058390165011721, -1.367687711909180148 ) ) ;
#20277=CARTESIAN_POINT ( 'NONE',  ( 1.516205985490867381, 0.7479433349990645130, 1.704208623783896259 ) ) ;
#20281=CARTESIAN_POINT ( 'NONE',  ( 4.043146078444789460, 0.09904687726844901841, 1.909973672635330910 ) ) ;
#20286=CARTESIAN_POINT ( 'NONE',  ( 3.456657222422593545, -1.844998171120499020, -0.9834188347317989187 ) ) ;
#20287=CARTESIAN_POINT ( 'NONE',  ( 2.518242125168220102, 1.223528130051700025, -1.415109699333151561 ) ) ;
#20290=CARTESIAN_POINT ( 'NONE',  ( 3.386022052710332186, -0.3430625053944387770, -1.706099273433875130 ) ) ;
#20294=CARTESIAN_POINT ( 'NONE',  ( 3.721100771531059781, -0.1247040890464539975, 1.720429258078775669 ) ) ;
#20295=CARTESIAN_POINT ( 'NONE',  ( 3.562233144267571650, -1.470601008620987749, 1.625073949779440419 ) ) ;
#20296=CARTESIAN_POINT ( 'NONE',  ( 6.059228469117068805, -1.890744221452178353, -1.137928576693452820 ) ) ;
#20297=CARTESIAN_POINT ( 'NONE',  ( 6.983263157960363898, 2.958708369276577876, 2.506372104999963657 ) ) ;
#20299=CARTESIAN_POINT ( 'NONE',  ( 3.379888771869215436, -2.093702847677909595, 0.5742949676477026033 ) ) ;
#20300=CARTESIAN_POINT ( 'NONE',  ( 1.822601884235462766, 1.703052241681313861, 0.6583118566880485911 ) ) ;
#20301=CARTESIAN_POINT ( 'NONE',  ( 0.3386216902839487841, -1.901412053528793722, -0.4823507731460881520 ) ) ;
#20302=CARTESIAN_POINT ( 'NONE',  ( 4.698512310153400762, 1.457641359173178275, -1.535954635999142948 ) ) ;
#20304=CARTESIAN_POINT ( 'NONE',  ( 5.319995955860258974, 1.367515572929053791, -1.839686415443070100 ) ) ;
#20306=CARTESIAN_POINT ( 'NONE',  ( 6.720655732516628511, 2.062125556784020652, 2.233254568942647733 ) ) ;
#20308=CARTESIAN_POINT ( 'NONE',  ( 0.2059360158346480729, 1.574223368660916611, 1.420867075595611650 ) ) ;
#20313=CARTESIAN_POINT ( 'NONE',  ( 6.883263157960365142, 1.273421409013283823, 2.069651443392322765 ) ) ;
#20316=CARTESIAN_POINT ( 'NONE',  ( 5.098279808040273586, -0.2930726886911338425, 1.994869512123042199 ) ) ;
#20318=CARTESIAN_POINT ( 'NONE',  ( 4.592669665391247769, 2.021776019120101520, 0.4074096221951555297 ) ) ;
#20324=CARTESIAN_POINT ( 'NONE',  ( 0.8496949173334772398, 2.088161746953997255, -0.1042977956757246832 ) ) ;
#20325=CARTESIAN_POINT ( 'NONE',  ( 4.254529844270301453, 1.955172953530256219, -0.4926405443339901269 ) ) ;
#20326=CARTESIAN_POINT ( 'NONE',  ( 4.370544011308346910, -0.004580445953385886559, -1.841430844414258861 ) ) ;
#20328=CARTESIAN_POINT ( 'NONE',  ( 0.8676543833149966689, 0.8442763457921966808, 1.503926039954103677 ) ) ;
#20330=CARTESIAN_POINT ( 'NONE',  ( 0.8448572530952251913, 0.4413087945813984336, -2.255810399402935484 ) ) ;
#20332=CARTESIAN_POINT ( 'NONE',  ( 0.7555949320777423095, -1.911880202960547948, -1.209378468041100607 ) ) ;
#20333=CARTESIAN_POINT ( 'NONE',  ( 2.719469050394443421, -0.2056238487441063856, 2.096000168696035448 ) ) ;
#20343=CARTESIAN_POINT ( 'NONE',  ( 5.467086432746695479, -1.751203904306109838, 1.366580491753234039 ) ) ;
#20344=CARTESIAN_POINT ( 'NONE',  ( 2.713028398602938651, -0.2137989841624072795, 2.180988865010752509 ) ) ;
#20348=CARTESIAN_POINT ( 'NONE',  ( 5.213317179658601752, -1.656387821537348426, -1.051046178410528942 ) ) ;
#20350=CARTESIAN_POINT ( 'NONE',  ( 6.890000000000009450, 0.5473178204696281801, 2.329866691457019190 ) ) ;
#20352=CARTESIAN_POINT ( 'NONE',  ( 4.359710196644346780, -1.641147893522959089, -1.343014508298406628 ) ) ;
#20358=CARTESIAN_POINT ( 'NONE',  ( 5.583513413114173041, -0.8223277247318347971, 1.647484189299788682 ) ) ;
#20362=CARTESIAN_POINT ( 'NONE',  ( 1.153398195617076682, 0.7042877955899041753, 1.591771711926233346 ) ) ;
#20365=CARTESIAN_POINT ( 'NONE',  ( 5.366167234668930419, 1.061923416652654550, 1.882811416686725359 ) ) ;
#20370=CARTESIAN_POINT ( 'NONE',  ( 4.293933718354110418, -0.8299404887524584051, 1.996233173270183681 ) ) ;
#20372=CARTESIAN_POINT ( 'NONE',  ( 5.255133876903111734, -1.663856106090171538, -1.057019077474026680 ) ) ;
#20373=CARTESIAN_POINT ( 'NONE',  ( 3.637800481086241433, 0.04416708034036923719, -1.733463101117929339 ) ) ;
#20374=CARTESIAN_POINT ( 'NONE',  ( 1.189316404147572337, 1.662717542896676504, 1.427817766309902314 ) ) ;
#20375=CARTESIAN_POINT ( 'NONE',  ( 1.940857006665818174, 2.282658722630509729, 0.3375727702036589450 ) ) ;
#20376=CARTESIAN_POINT ( 'NONE',  ( 3.585278813505449858, 1.864625933638365485, -0.8777486340088790362 ) ) ;
#20377=CARTESIAN_POINT ( 'NONE',  ( 0.3396542298245264213, 1.936664667523413152, 0.1439508268369827926 ) ) ;
#20384=CARTESIAN_POINT ( 'NONE',  ( 2.977765718515757332, 2.095881712254169305, -0.6909776239150815513 ) ) ;
#20386=CARTESIAN_POINT ( 'NONE',  ( 0.3911518402437937358, -1.704754640775848928, 0.7467128926999586636 ) ) ;
#20391=CARTESIAN_POINT ( 'NONE',  ( 6.925078400183553029, 2.941156041390875941, 2.696161060448130975 ) ) ;
#20392=CARTESIAN_POINT ( 'NONE',  ( 5.964778383650899407, 0.1308802983275309528, -1.836551591404868233 ) ) ;
#20394=CARTESIAN_POINT ( 'NONE',  ( 3.643480044026959241, -1.559369103033839465, -1.347540176210021423 ) ) ;
#20398=CARTESIAN_POINT ( 'NONE',  ( 2.578776193315842846, -1.391201028639722281, 1.464365899026105700 ) ) ;
#20402=CARTESIAN_POINT ( 'NONE',  ( 1.604443549136617575, -0.7409017435648653782, -1.923293390451373819 ) ) ;
#20406=CARTESIAN_POINT ( 'NONE',  ( 5.039771180630152614, -1.558841386063321455, -1.562417271110942307 ) ) ;
#20407=CARTESIAN_POINT ( 'NONE',  ( 1.001511639980020130, 1.766541945284912263, 1.245431700958275600 ) ) ;
#20410=CARTESIAN_POINT ( 'NONE',  ( 0.7257964430846426396, 0.8128130212789463904, -1.845628942776005088 ) ) ;
#20411=CARTESIAN_POINT ( 'NONE',  ( 1.880608668887576052, -0.2816854878555269392, 2.281025131504022863 ) ) ;
#20413=CARTESIAN_POINT ( 'NONE',  ( 6.287759715630294011, 1.828497742151834027, -0.5598019499635784602 ) ) ;
#20415=CARTESIAN_POINT ( 'NONE',  ( 1.621729638615863944, -1.036547396872866678, -1.557007864774778705 ) ) ;
#20416=CARTESIAN_POINT ( 'NONE',  ( 4.030482632556767975, 0.5424685788828055300, 1.942097399793737633 ) ) ;
#20420=CARTESIAN_POINT ( 'NONE',  ( 5.145193760806440864, -1.806914327231067929, 1.081695767794567775 ) ) ;
#20425=CARTESIAN_POINT ( 'NONE',  ( 5.713150811708690213, 1.648777711927760015, -1.166343465331370455 ) ) ;
#20427=CARTESIAN_POINT ( 'NONE',  ( 1.182570505923411952, 1.231668817017372408, -1.654277799056037335 ) ) ;
#20434=CARTESIAN_POINT ( 'NONE',  ( 2.945941647375094785, 1.533668492858210497, 1.537084210998492795 ) ) ;
#20437=CARTESIAN_POINT ( 'NONE',  ( 2.278628554356322500, 1.682734121078124812, -0.7478279864501293783 ) ) ;
#20440=CARTESIAN_POINT ( 'NONE',  ( 4.247736854543925133, 2.191053489037126045, -0.05455935714590579716 ) ) ;
#20441=CARTESIAN_POINT ( 'NONE',  ( 6.883263157960363365, 3.690127339433949327, 2.567897385111846731 ) ) ;
#20442=CARTESIAN_POINT ( 'NONE',  ( 5.032209928657234599, 1.167594373104458461, -1.937845176762391874 ) ) ;
#20449=CARTESIAN_POINT ( 'NONE',  ( 5.307753102408475421, -1.761140305208692913, 0.1738094965475830145 ) ) ;
#20451=CARTESIAN_POINT ( 'NONE',  ( 2.450341380362738075, 2.105475501793910631, 0.05272098179117353650 ) ) ;
#20454=CARTESIAN_POINT ( 'NONE',  ( 2.084365741702984387, 1.136530121079984301, -1.608336531363078414 ) ) ;
#20458=CARTESIAN_POINT ( 'NONE',  ( 5.888875516108613262, -1.723027129771546484, -0.5597982944235294633 ) ) ;
#20462=CARTESIAN_POINT ( 'NONE',  ( 5.489076674590072535, 1.649195787720953987, -0.8828566466120501000 ) ) ;
#20464=CARTESIAN_POINT ( 'NONE',  ( 5.471561611210747245, -0.3092806512635417060, 2.046926588373791933 ) ) ;
#20474=CARTESIAN_POINT ( 'NONE',  ( 5.512146440779991607, 1.959692598237902761, -0.09458084330612320789 ) ) ;
#20476=CARTESIAN_POINT ( 'NONE',  ( 3.391953724946985105, 0.04666865176591523945, 2.015725201127672506 ) ) ;
#20477=CARTESIAN_POINT ( 'NONE',  ( 3.028439059693835311, 0.4704065786719989761, 1.856910451861475631 ) ) ;
#20479=CARTESIAN_POINT ( 'NONE',  ( 0.1522426329377546128, 0.8445714516599597266, 2.022489037641273857 ) ) ;
#20480=CARTESIAN_POINT ( 'NONE',  ( 0.2335667940003048615, 2.868049447791064743, -2.641685461849890171 ) ) ;
#20481=CARTESIAN_POINT ( 'NONE',  ( 1.633845377418343237, 0.9265681688636999702, -1.624882239709434018 ) ) ;
#20483=CARTESIAN_POINT ( 'NONE',  ( 4.377201702235844927, -1.800125857882298508, -0.9014936589236545172 ) ) ;
#20486=CARTESIAN_POINT ( 'NONE',  ( 4.728176305778284849, 2.111628383735635328, 0.1544883665849701437 ) ) ;
#20488=CARTESIAN_POINT ( 'NONE',  ( 6.162566008723842081, -0.7415158119226210598, -1.933206815039355320 ) ) ;
#20489=CARTESIAN_POINT ( 'NONE',  ( 1.329752858235648150, 1.027315703197308361, -1.820849364048042318 ) ) ;
#20490=CARTESIAN_POINT ( 'NONE',  ( 6.620655732516652847, 2.941130357193070033, 2.725706755162327966 ) ) ;
#20491=CARTESIAN_POINT ( 'NONE',  ( 6.458013382736495167, 1.820430347099718293, -0.1376817787434730933 ) ) ;
#20500=CARTESIAN_POINT ( 'NONE',  ( 0.9436867518335406713, -1.148578278726499757, -1.400746029399003501 ) ) ;
#20509=CARTESIAN_POINT ( 'NONE',  ( 6.081657687927014777, -0.6766999560612970699, 1.899624756701682626 ) ) ;
#20510=CARTESIAN_POINT ( 'NONE',  ( 0.3816889160728509367, 0.2035859187828891470, -2.110680546376259681 ) ) ;
#20512=CARTESIAN_POINT ( 'NONE',  ( -0.1394461523061013564, 4.080274402048936544, -2.835111295649892060 ) ) ;
#20516=CARTESIAN_POINT ( 'NONE',  ( 3.907052821786443975, -1.612583007836394966, 1.130340192709837766 ) ) ;
#20519=CARTESIAN_POINT ( 'NONE',  ( 4.464470365011488973, -1.956567236562205325, -0.4871837624095613495 ) ) ;
#20522=CARTESIAN_POINT ( 'NONE',  ( 4.998067021457727854, -0.7363416341295281331, -2.064161796032103258 ) ) ;
#20524=CARTESIAN_POINT ( 'NONE',  ( 3.487250860276095210, 1.742034520097140771, -0.8226350277544016709 ) ) ;
#20527=CARTESIAN_POINT ( 'NONE',  ( -0.02968770228140016343, 0.003472272166151618711, -1.826291111852257343 ) ) ;
#20528=CARTESIAN_POINT ( 'NONE',  ( 0.1331565106231328566, 1.371277436080810208, -2.201942895618694607 ) ) ;
#20532=CARTESIAN_POINT ( 'NONE',  ( 5.313322838536244319, -1.661678602684885986, -1.056841482759300233 ) ) ;
#20533=CARTESIAN_POINT ( 'NONE',  ( 0.5736477084636192325, -1.077812090576779402, 1.615333711560530849 ) ) ;
#20534=CARTESIAN_POINT ( 'NONE',  ( 4.020185130887462321, -2.007537125943322120, 0.1504822817294942383 ) ) ;
#20535=CARTESIAN_POINT ( 'NONE',  ( 5.729893540575130118, -2.074111880986319711, -0.9905765078317919636 ) ) ;
#20537=CARTESIAN_POINT ( 'NONE',  ( 3.959670595502752022, -0.5440038360976228171, 1.779617975935204655 ) ) ;
#20542=CARTESIAN_POINT ( 'NONE',  ( 0.2401087780563165297, 2.186128513634697512, 0.1550312349237955856 ) ) ;
#20547=CARTESIAN_POINT ( 'NONE',  ( 0.4338677482375961070, 0.9413943332680120291, -1.564114433284753636 ) ) ;
#20549=CARTESIAN_POINT ( 'NONE',  ( 2.971044740931504613, -1.708945904174772989, -0.2933555621278273184 ) ) ;
#20550=CARTESIAN_POINT ( 'NONE',  ( 6.609000000000047947, 2.072800852438889230, 2.208748404276588584 ) ) ;
#20552=CARTESIAN_POINT ( 'NONE',  ( 5.777927443424748510, 1.091106472389313131, 1.463626628978510702 ) ) ;
#20553=CARTESIAN_POINT ( 'NONE',  ( 2.852341167582587378, -1.956174252073937359, -0.1491622203949396763 ) ) ;
#20559=CARTESIAN_POINT ( 'NONE',  ( 4.828832153679845973, 1.461785933843419150, -1.536352341152541046 ) ) ;
#20562=CARTESIAN_POINT ( 'NONE',  ( 1.498975721005956219, 0.3999860688887920679, 2.031077231357696355 ) ) ;
#20565=CARTESIAN_POINT ( 'NONE',  ( 4.934350062338543452, -1.187533444586796438, -1.877053939226761115 ) ) ;
#20567=CARTESIAN_POINT ( 'NONE',  ( 3.024404714233555946, -2.025920917938589749, 1.086156575756046294 ) ) ;
#20574=CARTESIAN_POINT ( 'NONE',  ( 3.076317393561965208, 0.8638369986560844316, 1.706277067364105893 ) ) ;
#20576=CARTESIAN_POINT ( 'NONE',  ( 3.996854971928843092, 1.456802638785438475, -0.9229968019349673591 ) ) ;
#20577=CARTESIAN_POINT ( 'NONE',  ( 3.292204118033771110, -0.8216723425069611952, -1.841733987974409237 ) ) ;
#20578=CARTESIAN_POINT ( 'NONE',  ( 4.430533913404213209, -1.776825693393409455, -1.458421372522151538 ) ) ;
#20580=CARTESIAN_POINT ( 'NONE',  ( 6.498663405296385420, -0.5599463640075187376, -2.030188946737851108 ) ) ;
#20582=CARTESIAN_POINT ( 'NONE',  ( 4.340886628629798238, -1.540457278443696509, 0.8709714020649069743 ) ) ;
#20584=CARTESIAN_POINT ( 'NONE',  ( 0.3754557147975129960, 2.136610487456944263, -0.8307393200860619942 ) ) ;
#20585=CARTESIAN_POINT ( 'NONE',  ( 6.351489326974223637, 1.835832825663574752, -0.1405570519043483624 ) ) ;
#20587=CARTESIAN_POINT ( 'NONE',  ( 5.718738293430368991, -0.05686238728638653983, 2.190873718245327506 ) ) ;
#20591=CARTESIAN_POINT ( 'NONE',  ( 0.2390591215055883068, -2.106223889411312999, -0.5266447289704286883 ) ) ;
#20592=CARTESIAN_POINT ( 'NONE',  ( 1.428923106112218067, -1.700960256238340573, 1.082842518468102089 ) ) ;
#20594=CARTESIAN_POINT ( 'NONE',  ( 4.512281715141372551, -0.8252044610495885557, -1.740951444232276657 ) ) ;
#20596=CARTESIAN_POINT ( 'NONE',  ( 0.9146621208586953600, -2.221583675102642097, 0.007239306818007660779 ) ) ;
#20604=CARTESIAN_POINT ( 'NONE',  ( 3.913389451132457619, -0.8987009378256786141, -1.490314472085547237 ) ) ;
#20605=CARTESIAN_POINT ( 'NONE',  ( 1.890992312513404716, 0.1891058464698439912, 1.952711869325058691 ) ) ;
#20609=CARTESIAN_POINT ( 'NONE',  ( 6.478960399985357554, 1.830089090633261417, 0.7073212282268787066 ) ) ;
#20612=CARTESIAN_POINT ( 'NONE',  ( 5.120327457147888950, 1.987497208294352280, 0.3399611521368098854 ) ) ;
#20613=CARTESIAN_POINT ( 'NONE',  ( 0.9192595896337816264, 2.091463038127399532, 0.8634530567685079205 ) ) ;
#20617=CARTESIAN_POINT ( 'NONE',  ( 1.299835797595794151, -1.870726058509405210, -0.005653028302576856845 ) ) ;
#20618=CARTESIAN_POINT ( 'NONE',  ( 0.03525962724756306205, -1.394606873943932346, 1.030409205853829668 ) ) ;
#20619=CARTESIAN_POINT ( 'NONE',  ( 3.755584314896889264, 2.174856280799509545, -0.2696606696684644700 ) ) ;
#20620=CARTESIAN_POINT ( 'NONE',  ( 6.018676637735699941, 1.555688181992231245, -1.704518584337791021 ) ) ;
#20621=CARTESIAN_POINT ( 'NONE',  ( 0.8837498274346058391, 1.383631269908250472, 1.527543229604712893 ) ) ;
#20622=CARTESIAN_POINT ( 'NONE',  ( 3.538947879116743689, -1.471199320522957876, -1.267674678009507394 ) ) ;
#20624=CARTESIAN_POINT ( 'NONE',  ( 5.958239543830242901, 0.7576973323653662939, 1.710380810381225691 ) ) ;
#20627=CARTESIAN_POINT ( 'NONE',  ( 4.131482539099665452, 0.5404898895830790861, 1.942541833525657680 ) ) ;
#20631=CARTESIAN_POINT ( 'NONE',  ( 1.594096589105632011, -1.816728215151931058, -0.1805768397986490248 ) ) ;
#20640=CARTESIAN_POINT ( 'NONE',  ( 6.006511931541290927, -2.010153113457528118, -0.1956843118748711474 ) ) ;
#20641=CARTESIAN_POINT ( 'NONE',  ( 0.08289510313583270396, -1.381697626658566547, 1.608636130391014163 ) ) ;
#20646=CARTESIAN_POINT ( 'NONE',  ( 5.770404196412942888, -1.309395467888567754, 1.591445708773833401 ) ) ;
#20647=CARTESIAN_POINT ( 'NONE',  ( 4.412732527109735514, -1.242725882911545288, -1.587838301257207263 ) ) ;
#20654=CARTESIAN_POINT ( 'NONE',  ( 4.147814418418220406, -0.1948115906579734602, -2.006652602119996853 ) ) ;
#20655=CARTESIAN_POINT ( 'NONE',  ( 3.855264089065893351, 1.827008581971893530, -0.2271198879545410221 ) ) ;
#20657=CARTESIAN_POINT ( 'NONE',  ( 2.297912027771050081, 1.785232721601331507, 1.462330537539487496 ) ) ;
#20659=CARTESIAN_POINT ( 'NONE',  ( 5.395850447034295172, -0.7835752172833524432, 2.014745138864987073 ) ) ;
#20661=CARTESIAN_POINT ( 'NONE',  ( -0.1294898018152357000, -0.0008549345193622873455, -1.926395771554180625 ) ) ;
#20667=CARTESIAN_POINT ( 'NONE',  ( 1.920565142479381038, 1.744437793965779582, 0.6759427408406930571 ) ) ;
#20669=CARTESIAN_POINT ( 'NONE',  ( 6.473508845062264427, 1.886732274579514756, -0.5718055884485659934 ) ) ;
#20672=CARTESIAN_POINT ( 'NONE',  ( 1.190363680384380229, -0.9894552095768920363, 1.972713631218452557 ) ) ;
#20678=CARTESIAN_POINT ( 'NONE',  ( 5.717641559312711230, -1.923570962979544330, 0.4312651734501466994 ) ) ;
#20679=CARTESIAN_POINT ( 'NONE',  ( 6.533790081910475500, -1.501629927769430273, -1.752384480091616847 ) ) ;
#20680=CARTESIAN_POINT ( 'NONE',  ( 6.865680895677650497, -0.4029405758906497437, 1.823372528724865438 ) ) ;
#20681=CARTESIAN_POINT ( 'NONE',  ( 3.942276525692486544, -1.021014944866809326, 1.792092113122957242 ) ) ;
#20689=CARTESIAN_POINT ( 'NONE',  ( 6.021977204206338641, 2.140098014189107278, -0.3652067468529682226 ) ) ;
#20691=CARTESIAN_POINT ( 'NONE',  ( 4.968220237687512864, -1.735557695065930606, -0.6152675618510683453 ) ) ;
#20694=CARTESIAN_POINT ( 'NONE',  ( 0.4209003391736841349, -0.09842406703440903515, 1.868101828653282226 ) ) ;
#20698=CARTESIAN_POINT ( 'NONE',  ( 0.6801455168885979230, 0.9429141125626202546, 1.663586755705208420 ) ) ;
#20699=CARTESIAN_POINT ( 'NONE',  ( 1.463349669262783870, 1.744408624272808073, -0.2979475530153224416 ) ) ;
#20700=CARTESIAN_POINT ( 'NONE',  ( 6.111982388360997831, -0.6759622889470856544, 1.896349411511048855 ) ) ;
#20702=CARTESIAN_POINT ( 'NONE',  ( 4.815990648786471873, 0.9809511849332609446, -1.645218558792021613 ) ) ;
#20703=CARTESIAN_POINT ( 'NONE',  ( -0.1409997244345879974, 2.021982482314553131, -2.415666835770650778 ) ) ;
#20704=CARTESIAN_POINT ( 'NONE',  ( 4.949637397294944563, 1.457986120030363431, 1.324331637980098675 ) ) ;
#20705=CARTESIAN_POINT ( 'NONE',  ( 6.117445925308827803, 1.681535965833020230, 1.118592408852390641 ) ) ;
#20707=CARTESIAN_POINT ( 'NONE',  ( 3.748781033766034998, -1.529746656882627454, 1.076398355447941491 ) ) ;
#20708=CARTESIAN_POINT ( 'NONE',  ( 5.725168984891365831, -0.03570264050535218447, 1.724697241110892509 ) ) ;
#20710=CARTESIAN_POINT ( 'NONE',  ( 3.686314334879085663, -1.088174899301070253, 1.919869060924610293 ) ) ;
#20714=CARTESIAN_POINT ( 'NONE',  ( 0.5903720789649337108, 1.061967407477812264, -1.768178413720230990 ) ) ;
#20720=CARTESIAN_POINT ( 'NONE',  ( 3.244645865714153032, -2.039272935636734285, -0.3565889006169955522 ) ) ;
#20724=CARTESIAN_POINT ( 'NONE',  ( 1.277996545170931197, 1.989402420072207800, -0.3474319251903742467 ) ) ;
#20727=CARTESIAN_POINT ( 'NONE',  ( 0.07479286986305544449, 2.888457405263197941, -2.344396930208477947 ) ) ;
#20729=CARTESIAN_POINT ( 'NONE',  ( 6.327499943094792023, -1.427716970705223520, 1.423745300580002482 ) ) ;
#20730=CARTESIAN_POINT ( 'NONE',  ( 5.383970194100923479, -1.915903400165029469, 0.006849619181082886032 ) ) ;
#20732=CARTESIAN_POINT ( 'NONE',  ( 4.124703146219878214, 0.1084699374758208573, 2.189010777610411740 ) ) ;
#20734=CARTESIAN_POINT ( 'NONE',  ( 2.074333847954575205, 0.8209984392052707136, 1.727357542596375861 ) ) ;
#20738=CARTESIAN_POINT ( 'NONE',  ( 1.317982704262925520, 0.9913799330133237220, -1.755781447868165257 ) ) ;
#20740=CARTESIAN_POINT ( 'NONE',  ( 6.198795224570643470, 1.821041368708445907, 1.219022265761634971 ) ) ;
#20742=CARTESIAN_POINT ( 'NONE',  ( 3.293694421395336303, -0.6999868571894217739, 1.576533365092074757 ) ) ;
#20744=CARTESIAN_POINT ( 'NONE',  ( 0.1394461523056772234, 0.2496508530322391062, -1.754170159799403717 ) ) ;
#20748=CARTESIAN_POINT ( 'NONE',  ( 1.099968687278202406, 0.7983322178258808188, -1.792280776234013828 ) ) ;
#20757=CARTESIAN_POINT ( 'NONE',  ( 3.527799351415283002, -1.784095038623861651, 0.3127521441018704107 ) ) ;
#20761=CARTESIAN_POINT ( 'NONE',  ( 4.670457322363490427, 0.6978976414240989357, 1.671844709466139722 ) ) ;
#20765=CARTESIAN_POINT ( 'NONE',  ( 4.580409787399508659, 1.145788356511275863, -1.466404039444089591 ) ) ;
#20767=CARTESIAN_POINT ( 'NONE',  ( 2.390125374076298659, -0.7353994070154221685, -1.769027144041198429 ) ) ;
#20774=CARTESIAN_POINT ( 'NONE',  ( 1.675843188381221038, -1.117204103763050016, 1.766894365349908069 ) ) ;
#20776=CARTESIAN_POINT ( 'NONE',  ( 0.08272424614634911466, -0.1293432359340887239, -1.795996506534849324 ) ) ;
#20779=CARTESIAN_POINT ( 'NONE',  ( 2.326929888710258965, -0.002694909042751796133, 1.825762228105472840 ) ) ;
#20781=CARTESIAN_POINT ( 'NONE',  ( 2.091926199050548441, 1.179367891222588005, 1.505316542580182659 ) ) ;
#20782=CARTESIAN_POINT ( 'NONE',  ( 1.363649640492822668, -0.4818474322187695780, 1.909556114072549882 ) ) ;
#20783=CARTESIAN_POINT ( 'NONE',  ( 3.860829347334773232, 0.2347576860389360420, -1.927744540433872888 ) ) ;
#20788=CARTESIAN_POINT ( 'NONE',  ( 3.972980863544761654, -1.569110274459505350, 1.426624754300914510 ) ) ;
#20796=CARTESIAN_POINT ( 'NONE',  ( 4.143042835627613663, -1.587387879459275286, 0.9017181768668989239 ) ) ;
#20801=CARTESIAN_POINT ( 'NONE',  ( 4.821099876132087125, -0.09137817997613774390, 1.868553921495450965 ) ) ;
#20803=CARTESIAN_POINT ( 'NONE',  ( 2.613793455771874719, -1.905494007693061098, 0.2829725131217008527 ) ) ;
#20804=CARTESIAN_POINT ( 'NONE',  ( 6.473494419632052299, -0.2434444386649399217, 1.946554233954982172 ) ) ;
#20811=CARTESIAN_POINT ( 'NONE',  ( 0.8611331728165865229, -0.05642918589183294059, -2.116647836221299261 ) ) ;
#20814=CARTESIAN_POINT ( 'NONE',  ( 6.332887962430945983, -1.963924782908726296, -0.6550794379977520343 ) ) ;
#20815=CARTESIAN_POINT ( 'NONE',  ( 0.5734669319550633748, -1.023298125840161887, 1.530493987491374330 ) ) ;
#20817=CARTESIAN_POINT ( 'NONE',  ( 6.117888908451988073, 0.2214900195740623634, 2.288030219478351057 ) ) ;
#20820=CARTESIAN_POINT ( 'NONE',  ( 1.043418098205237676, -1.810020423698131653, -1.406424589915030943 ) ) ;
#20823=CARTESIAN_POINT ( 'NONE',  ( 6.369087006730828726, 1.857646680926292815, -0.5659663566517159072 ) ) ;
#20826=CARTESIAN_POINT ( 'NONE',  ( 6.064708884584704585, 0.6063723501847050334, 1.813766235492550560 ) ) ;
#20831=CARTESIAN_POINT ( 'NONE',  ( 2.607466773009491146, -2.067780616408128935, 0.3074339443978144626 ) ) ;
#20832=CARTESIAN_POINT ( 'NONE',  ( 1.586397006687990885, -0.2552452650203296813, -1.751205042619798258 ) ) ;
#20835=CARTESIAN_POINT ( 'NONE',  ( 4.523529124507605914, -1.408076564469705527, -1.808723714663774240 ) ) ;
#20836=CARTESIAN_POINT ( 'NONE',  ( 3.556370828957751140, -1.535720284108733624, -0.8187001993567950553 ) ) ;
#20839=CARTESIAN_POINT ( 'NONE',  ( 3.092811855500672280, 0.9656183884470933565, -1.439801824928796048 ) ) ;
#20840=CARTESIAN_POINT ( 'NONE',  ( 3.859984642892180684, -0.6334943099049659132, 2.076686793900458294 ) ) ;
#20842=CARTESIAN_POINT ( 'NONE',  ( 4.716029918043215474, 1.032482702726954527, -1.731993998903176957 ) ) ;
#20843=CARTESIAN_POINT ( 'NONE',  ( 1.750000000000001332, 1.008799782768345906E-13, 2.052068128417951165 ) ) ;
#20845=CARTESIAN_POINT ( 'NONE',  ( 2.028227463090884974, 1.110962183858194452, -1.573585318204050676 ) ) ;
#20847=CARTESIAN_POINT ( 'NONE',  ( 4.025785557498418044, -0.3775041287265075152, 2.188942893082143293 ) ) ;
#20849=CARTESIAN_POINT ( 'NONE',  ( -0.1106856583840696712, 2.878213433396461962, -2.485464591233726317 ) ) ;
#20854=CARTESIAN_POINT ( 'NONE',  ( 0.5400543498376106921, -2.107395444675621121, 0.7023712877645065245 ) ) ;
#20855=CARTESIAN_POINT ( 'NONE',  ( 5.459412808053472510, 1.602871733476991079, 1.130958114227413436 ) ) ;
#20858=CARTESIAN_POINT ( 'NONE',  ( 0.5269342146079664113, 2.068330297753611546, 0.6279826202375409228 ) ) ;
#20861=CARTESIAN_POINT ( 'NONE',  ( 3.578633024105078331, 1.310608547571969540, -1.592757226543355165 ) ) ;
#20865=CARTESIAN_POINT ( 'NONE',  ( 5.272658424858247095, -1.760895560629770262, -0.6313210838888929644 ) ) ;
#20866=CARTESIAN_POINT ( 'NONE',  ( 3.744493841719060967, 1.720499418279351822, -0.2165549783500023973 ) ) ;
#20867=CARTESIAN_POINT ( 'NONE',  ( 3.807932448155851191, 1.227607710457185197, -1.234010206841095636 ) ) ;
#20868=CARTESIAN_POINT ( 'NONE',  ( 0.9609334056123096657, -2.075215392668391168, -0.9741618742916816620 ) ) ;
#20870=CARTESIAN_POINT ( 'NONE',  ( 5.355056023315875713, 0.4066876561409601964, -2.050628154503638889 ) ) ;
#20871=CARTESIAN_POINT ( 'NONE',  ( 6.281195871053392388, 1.340900550492612364, 1.404911987746715774 ) ) ;
#20873=CARTESIAN_POINT ( 'NONE',  ( 1.318982659667154334, 0.9913977828604101372, -1.755770081111128977 ) ) ;
#20874=CARTESIAN_POINT ( 'NONE',  ( 0.04132284026489921325, -1.696808583893465894, -1.386471574116483696 ) ) ;
#20878=CARTESIAN_POINT ( 'NONE',  ( 2.350376503035214615, 0.9972050307137376723, -1.871358364749615033 ) ) ;
#20880=CARTESIAN_POINT ( 'NONE',  ( 5.725187622324654946, -0.04035785615889506128, 1.825416780793003069 ) ) ;
#20887=CARTESIAN_POINT ( 'NONE',  ( 2.179950100978587990, 1.979969115219997189, -0.3981650194792104025 ) ) ;
#20888=CARTESIAN_POINT ( 'NONE',  ( 0.1125219251090440048, -0.9011682483198739657, -1.901734387108368063 ) ) ;
#20891=CARTESIAN_POINT ( 'NONE',  ( 4.188223417972539053, 0.9984873940180930552, -1.570204455898941420 ) ) ;
#20896=CARTESIAN_POINT ( 'NONE',  ( 4.846238042176662653, 1.821038859956089606, 0.1311717439725426648 ) ) ;
#20900=CARTESIAN_POINT ( 'NONE',  ( 2.125947893326819660, 0.3012468308378027371, -1.707275946889510676 ) ) ;
#20901=CARTESIAN_POINT ( 'NONE',  ( 0.2513753182956691146, 0.6612109069651134208, 1.610038921780505339 ) ) ;
#20902=CARTESIAN_POINT ( 'NONE',  ( 5.022255751415273473, -1.231121986244879452, -1.951710362602774307 ) ) ;
#20905=CARTESIAN_POINT ( 'NONE',  ( 1.809912028077927282, -2.045576594096469414, 0.2490995888081939946 ) ) ;
#20909=CARTESIAN_POINT ( 'NONE',  ( 0.4388270972612972609, 1.158508728638860230, 1.649830871073371119 ) ) ;
#20912=CARTESIAN_POINT ( 'NONE',  ( 6.491075539335432687, 1.626419376453295706, -0.9240138038444989377 ) ) ;
#20913=CARTESIAN_POINT ( 'NONE',  ( 3.568532368641282648, 0.6928216322696268969, 1.782650395559831180 ) ) ;
#20915=CARTESIAN_POINT ( 'NONE',  ( 4.688207069967821106, -1.042061291317699423, 1.945354640606362873 ) ) ;
#20920=CARTESIAN_POINT ( 'NONE',  ( 6.235037545507011281, 1.978399733989940401, 0.7636319146847592165 ) ) ;
#20922=CARTESIAN_POINT ( 'NONE',  ( 3.645846906810937149, -1.745625206895658810, -1.509303248858377966 ) ) ;
#20923=CARTESIAN_POINT ( 'NONE',  ( 4.105873170248697690, 0.6631157982108953908, -1.846516426336957784 ) ) ;
#20925=CARTESIAN_POINT ( 'NONE',  ( 0.3737810522974581717, -1.925036204310347943, 0.3769080146646397456 ) ) ;
#20928=CARTESIAN_POINT ( 'NONE',  ( 5.647672796105281279, 1.985869605424210649, -0.3494789899042491932 ) ) ;
#20932=CARTESIAN_POINT ( 'NONE',  ( 3.590846382830733763, 2.117060681034032221, 0.4805534470472500042 ) ) ;
#20934=CARTESIAN_POINT ( 'NONE',  ( 0.5980879788009090259, 1.428637019467562830, 1.567290143595565066 ) ) ;
#20939=ORIENTED_EDGE ( 'NONE', *, *, #137354, .T. ) ;
#20940=CARTESIAN_POINT ( 'NONE',  ( 1.423197193765327384, -0.05341811584172677374, 2.060271317188705709 ) ) ;
#20946=CARTESIAN_POINT ( 'NONE',  ( 4.705663775918221603, 1.419457463540532816, 1.281590252682027087 ) ) ;
#20949=CARTESIAN_POINT ( 'NONE',  ( 0.3163054335677130680, -0.6107064426322272865, -1.705642966030767260 ) ) ;
#20951=CARTESIAN_POINT ( 'NONE',  ( 0.8662487887013297083, -1.869732701101217476, -0.4164899194021577933 ) ) ;
#20952=CARTESIAN_POINT ( 'NONE',  ( 2.418496320782090869, 0.8830982243829659240, 1.872697815963566992 ) ) ;
#20954=CARTESIAN_POINT ( 'NONE',  ( 0.09253734621218495660, -0.4319466259074012937, -1.930967020758065589 ) ) ;
#20955=CARTESIAN_POINT ( 'NONE',  ( 3.105874302609371362, -1.823586186413633126, 0.09019715141062728536 ) ) ;
#20956=CARTESIAN_POINT ( 'NONE',  ( 0.4347317753056179623, 1.181035649988096958, -1.982462206444644437 ) ) ;
#20959=CARTESIAN_POINT ( 'NONE',  ( 4.457523014600942801, 1.654850327679569633, 1.231099151980449724 ) ) ;
#20965=CARTESIAN_POINT ( 'NONE',  ( 5.614326327132292072, -0.9438296153482359507, -1.882684210903639022 ) ) ;
#20967=CARTESIAN_POINT ( 'NONE',  ( 6.338344951546218908, -1.110931056888088353, 1.746890944850580052 ) ) ;
#20969=CARTESIAN_POINT ( 'NONE',  ( 3.233815116076131257, -1.449111151313630996, -1.604113057997895053 ) ) ;
#20970=CARTESIAN_POINT ( 'NONE',  ( 3.826823269871942657, 1.426704988148481901, -1.429811943454310397 ) ) ;
#20971=CARTESIAN_POINT ( 'NONE',  ( 6.620655732516625314, 7.629137130509059617, 2.773739711112707340 ) ) ;
#20977=CARTESIAN_POINT ( 'NONE',  ( 2.536342520008515233, 0.6839386381054488595, 1.897109991223707937 ) ) ;
#20985=CARTESIAN_POINT ( 'NONE',  ( 4.253529916566947122, 1.955168710539030075, -0.4926619687581067497 ) ) ;
#20988=CARTESIAN_POINT ( 'NONE',  ( 6.440463960111763697, 1.706863596762456581, 0.2470990609701722573 ) ) ;
#20994=CARTESIAN_POINT ( 'NONE',  ( 5.378141472655761923, -1.040010688794581029, 1.554561134376866161 ) ) ;
#20995=CARTESIAN_POINT ( 'NONE',  ( -0.1106856583841060310, -0.002128758811529348188, -1.996853503091333470 ) ) ;
#20999=CARTESIAN_POINT ( 'NONE',  ( 1.019157904985489305, -1.821734318179563106, 0.8647433871810316086 ) ) ;
#21000=CARTESIAN_POINT ( 'NONE',  ( 0.9139796618767962455, -1.811767225755844146, 0.001225010880583424656 ) ) ;
#21006=CARTESIAN_POINT ( 'NONE',  ( 6.257445408045815505, 1.831477697454777953, -0.5614084181123339956 ) ) ;
#21013=CARTESIAN_POINT ( 'NONE',  ( 3.063507763784904192, 0.3185916186679502715, -2.137983152197140413 ) ) ;
#21016=CARTESIAN_POINT ( 'NONE',  ( 0.4223351350958382544, -2.109807164369668087, 0.2139620856976830465 ) ) ;
#21018=CARTESIAN_POINT ( 'NONE',  ( 6.229513028222847026, -1.717969363144413952, 0.6179237509907066217 ) ) ;
#21019=CARTESIAN_POINT ( 'NONE',  ( 1.950399328871486704, 0.6145138020485548802, 1.873222726689319106 ) ) ;
#21020=CARTESIAN_POINT ( 'NONE',  ( 4.429883728109570207, -1.874397765517330061, 0.3784635845696313061 ) ) ;
#21024=CARTESIAN_POINT ( 'NONE',  ( 6.232857221494619182, -1.869652508273983882, -0.6194465747909986275 ) ) ;
#21025=CARTESIAN_POINT ( 'NONE',  ( 0.5330192132981932396, -1.372706249750287322, -1.373872859839823990 ) ) ;
#21031=CARTESIAN_POINT ( 'NONE',  ( 5.092401474535850348, -1.059014397921493433, 1.592059587274458510 ) ) ;
#21033=CARTESIAN_POINT ( 'NONE',  ( 0.9036964725192305758, 1.805054822729842190, 1.269220749904229839 ) ) ;
#21035=CARTESIAN_POINT ( 'NONE',  ( -0.02298948590537253436, -1.708053232816408196, -0.8599758793098393195 ) ) ;
#21040=CARTESIAN_POINT ( 'NONE',  ( 2.647004975520852454, -0.3514972095969396970, -2.040143077068845123 ) ) ;
#21045=CARTESIAN_POINT ( 'NONE',  ( 0.3214396764580421118, -0.1044536432763705502, 2.159311484102262479 ) ) ;
#21051=CARTESIAN_POINT ( 'NONE',  ( 5.924387396467542644, -1.262448726827345435, -1.189203582418095761 ) ) ;
#21054=CARTESIAN_POINT ( 'NONE',  ( 3.766520095694513959, -0.8345382577515870759, -1.894767260282135712 ) ) ;
#21055=CARTESIAN_POINT ( 'NONE',  ( 4.587589571003643840, -0.5631140419127963481, 2.040926637660822163 ) ) ;
#21058=CARTESIAN_POINT ( 'NONE',  ( 2.483201282919132336, -0.004963586128624993335, 1.969629312250702036 ) ) ;
#21059=CARTESIAN_POINT ( 'NONE',  ( 0.6153073421325053749, 1.564839666810373231, 1.099065937236625157 ) ) ;
#21060=CARTESIAN_POINT ( 'NONE',  ( 4.576316751016760165, -2.222806176453680393, -0.5595744876762742681 ) ) ;
#21061=CARTESIAN_POINT ( 'NONE',  ( 2.666400811807769777, -1.259032629953384719, 1.322343945743660543 ) ) ;
#21065=CARTESIAN_POINT ( 'NONE',  ( 3.902593620319398937, -1.991888969257959774, -0.2912845021679384971 ) ) ;
#21066=CARTESIAN_POINT ( 'NONE',  ( 3.731260466781026963, 0.05263058604075031982, -1.961233346245725429 ) ) ;
#21069=CARTESIAN_POINT ( 'NONE',  ( 0.07556134207192373442, 6.947017789483680872, -2.839293120204011256 ) ) ;
#21070=CARTESIAN_POINT ( 'NONE',  ( 6.281206920390010495, 1.440802673026912117, 1.515107276980606654 ) ) ;
#21071=CARTESIAN_POINT ( 'NONE',  ( 4.117836676938036788, -0.9100935957705791335, -1.517748890920249671 ) ) ;
#21072=CARTESIAN_POINT ( 'NONE',  ( 0.3401085955914601722, 2.185883683461706362, 0.1570275565265024931 ) ) ;
#21073=CARTESIAN_POINT ( 'NONE',  ( -0.05959145049940026140, -1.342969899416647905, -1.106900597494438143 ) ) ;
#21076=CARTESIAN_POINT ( 'NONE',  ( 0.3514386742532841779, -1.080868183629126067, 2.028406642177064345 ) ) ;
#21077=CARTESIAN_POINT ( 'NONE',  ( 0.08191350661116909848, -1.027414926483052326, 1.935800647029708443 ) ) ;
#21078=CARTESIAN_POINT ( 'NONE',  ( 6.555961055344926791, 1.506409351870329649, -0.8582156258899288348 ) ) ;
#21079=CARTESIAN_POINT ( 'NONE',  ( 3.246891520140795517, 0.5363302883765566076, 2.140594385818309409 ) ) ;
#21080=CARTESIAN_POINT ( 'NONE',  ( 0.6026744816367580748, 2.165159614417012879, 0.1613400170472640283 ) ) ;
#21082=CARTESIAN_POINT ( 'NONE',  ( 1.569685796324036264, 1.464237652897076414, 1.529633472619792656 ) ) ;
#21083=CARTESIAN_POINT ( 'NONE',  ( 3.125000000000001776, -2.052068128417947168, 1.787079010424618414E-13 ) ) ;
#21084=CARTESIAN_POINT ( 'NONE',  ( 6.727182134110193168, 3.677753830905213128, 2.802861976130672783 ) ) ;
#21085=CARTESIAN_POINT ( 'NONE',  ( 5.333004766823168374, 0.1418691241366967226, 1.921211455432366044 ) ) ;
#21087=CARTESIAN_POINT ( 'NONE',  ( 1.681587762198969216, 1.584507396495305587, 1.656812167128306035 ) ) ;
#21091=CARTESIAN_POINT ( 'NONE',  ( 3.545754021904829134, -2.051903114543842666, 0.8512574589945339776 ) ) ;
#21098=CARTESIAN_POINT ( 'NONE',  ( 2.110000207431836472, 0.002812218110825881467, 2.016597019944998959 ) ) ;
#21100=CARTESIAN_POINT ( 'NONE',  ( 6.672339319202143848, -0.9689918024566068766, -1.820889590527257740 ) ) ;
#21102=CARTESIAN_POINT ( 'NONE',  ( 6.497592319816168249, -1.739837010378456617, 0.05289828334312414448 ) ) ;
#21105=CARTESIAN_POINT ( 'NONE',  ( 2.899370140885823233, -0.5591585085688542955, 1.679125488999051452 ) ) ;
#21106=CARTESIAN_POINT ( 'NONE',  ( 1.477185633673218534, -2.006960102380969779, -0.1948397147320118372 ) ) ;
#21107=CARTESIAN_POINT ( 'NONE',  ( 6.515217664332146441, -1.685650512211306129, 0.4329046258050253670 ) ) ;
#21108=CARTESIAN_POINT ( 'NONE',  ( 4.968466765020612463, -2.157917790226408172, -0.7739415147586664601 ) ) ;
#21109=CARTESIAN_POINT ( 'NONE',  ( 3.573999110145977820, -1.774750109099573869, -0.4897004633943187191 ) ) ;
#21111=CARTESIAN_POINT ( 'NONE',  ( 4.541915102786819425, 0.7800907816924649296, -1.650662693317282770 ) ) ;
#21112=CARTESIAN_POINT ( 'NONE',  ( 4.992814645674492624, -2.006446365708704160, 0.2004330516618065550 ) ) ;
#21114=CARTESIAN_POINT ( 'NONE',  ( 3.063607368349754889, 0.3334396122402134011, -2.237705976790417939 ) ) ;
#21116=CARTESIAN_POINT ( 'NONE',  ( 6.264693295067493395, -1.491911088229242788, 1.486630704232002609 ) ) ;
#21118=CARTESIAN_POINT ( 'NONE',  ( 3.139188941651628539, -0.1496422021231707811, -2.064996656166856237 ) ) ;
#21121=CARTESIAN_POINT ( 'NONE',  ( 5.953796468794862129, -1.535729488331440074, -1.462440914314271811 ) ) ;
#21124=CARTESIAN_POINT ( 'NONE',  ( 1.717283182695702015, -0.2364092415704423800, 1.911874917900743931 ) ) ;
#21128=CARTESIAN_POINT ( 'NONE',  ( 0.1331715793776600265, 0.003733371859311259821, -1.953671397793784070 ) ) ;
#21133=CARTESIAN_POINT ( 'NONE',  ( 0.1061415085658158342, 1.651838695520141398, 1.485519503937395402 ) ) ;
#21134=CARTESIAN_POINT ( 'NONE',  ( 3.118299990072324057, -1.036503014707575332, -1.833135815837197535 ) ) ;
#21138=CARTESIAN_POINT ( 'NONE',  ( 0.9591554131188588794, 1.518337787816389284, 1.075887112759424280 ) ) ;
#21143=CARTESIAN_POINT ( 'NONE',  ( 0.7738737444688469358, 0.4079195088417563730, -2.080830740624163955 ) ) ;
#21146=CARTESIAN_POINT ( 'NONE',  ( 4.158614545834369736, -0.6132839004606009947, -1.863630207987923004 ) ) ;
#21147=CARTESIAN_POINT ( 'NONE',  ( 2.711983997553393699, -2.138339778157403615, 0.3160903847422363300 ) ) ;
#21148=CARTESIAN_POINT ( 'NONE',  ( 1.680954830071922812, 1.270413995023990106, 1.332975479855981416 ) ) ;
#21150=CARTESIAN_POINT ( 'NONE',  ( 3.204748380415303188, -0.3384778632026878564, 1.706898776778777993 ) ) ;
#21156=CARTESIAN_POINT ( 'NONE',  ( 0.4444780689869810564, 2.156031605563761833, 0.1575401717312311101 ) ) ;
#21157=CARTESIAN_POINT ( 'NONE',  ( 3.268907511149142575, -2.013924394373915128, 0.09611935726179518524 ) ) ;
#21159=CARTESIAN_POINT ( 'NONE',  ( 0.4093245661422850734, 1.881582470445356314, 1.064130679222355491 ) ) ;
#21160=CARTESIAN_POINT ( 'NONE',  ( 3.010573890873136094, 1.429054271512670615, -1.358355385302984164 ) ) ;
#21161=CARTESIAN_POINT ( 'NONE',  ( 6.609000000000029296, 3.690475914267136837, 2.614198802211770367 ) ) ;
#21162=CARTESIAN_POINT ( 'NONE',  ( 2.138135174613201350, 0.4275120379338535614, 1.894264587998186089 ) ) ;
#21163=CARTESIAN_POINT ( 'NONE',  ( 6.398695753475230674, -1.876852914212179035, -0.3660984893600614520 ) ) ;
#21167=CARTESIAN_POINT ( 'NONE',  ( -0.1110810684432986112, 0.7552414886912374170, -1.881935688996359213 ) ) ;
#21172=CARTESIAN_POINT ( 'NONE',  ( 6.774459802350780713, -1.427793189328768753, 1.813748355473641549 ) ) ;
#21175=CARTESIAN_POINT ( 'NONE',  ( 3.924618397835403893, -1.320764108826902428, 1.450678906977073579 ) ) ;
#21177=CARTESIAN_POINT ( 'NONE',  ( 2.022111496571117772, -1.799922141918413487, 0.9091460122201827643 ) ) ;
#21179=CARTESIAN_POINT ( 'NONE',  ( 2.835287003684193508, -1.733785568389034193, -1.215143187034111838 ) ) ;
#21184=CARTESIAN_POINT ( 'NONE',  ( 3.310337721246572773, 1.664907390794263531, 0.7863323413084821745 ) ) ;
#21187=CARTESIAN_POINT ( 'NONE',  ( 4.025719079702368752, -0.3592959752154977204, 2.089770972018199835 ) ) ;
#21190=CARTESIAN_POINT ( 'NONE',  ( 5.220021542613917376, -1.098816822949649774, -1.743189258048108314 ) ) ;
#21192=CARTESIAN_POINT ( 'NONE',  ( 2.595044651933966495, -0.5755060336137384214, 1.749081985381637061 ) ) ;
#21199=CARTESIAN_POINT ( 'NONE',  ( 1.840723031453334935, 2.183200880077686978, 0.3216222850719457349 ) ) ;
#21200=CARTESIAN_POINT ( 'NONE',  ( 4.060077147624012284, 2.245929291707829289, -0.2719227649434445282 ) ) ;
#21202=CARTESIAN_POINT ( 'NONE',  ( 3.076200346286896536, 0.8185659037078784062, 1.616202036402814901 ) ) ;
#21203=CARTESIAN_POINT ( 'NONE',  ( 4.733546111355320107, 0.5950593785610300834, -1.821060146467222918 ) ) ;
#21205=CARTESIAN_POINT ( 'NONE',  ( 4.223478185285460818, -1.886956702611849002, 0.5710618836329334203 ) ) ;
#21206=CARTESIAN_POINT ( 'NONE',  ( 1.149297380808786517, -1.516923518071541910, -1.187294353726556562 ) ) ;
#21207=CARTESIAN_POINT ( 'NONE',  ( 5.366025703835962446, 0.9229158262306772498, 1.627043297953718382 ) ) ;
#21208=CARTESIAN_POINT ( 'NONE',  ( 3.194261032343487461, -0.9352514745577229505, 2.109854200106716426 ) ) ;
#21209=CARTESIAN_POINT ( 'NONE',  ( 4.633164157742322153, 0.0009153448507570947738, -1.861241882716960561 ) ) ;
#21211=CARTESIAN_POINT ( 'NONE',  ( 0.5675926644314840397, 1.357872185771633156, 1.490966652548594285 ) ) ;
#21213=CARTESIAN_POINT ( 'NONE',  ( 1.559346616682453668, -1.807134503733454078, -1.081319387842846425 ) ) ;
#21217=CARTESIAN_POINT ( 'NONE',  ( 3.322626870553476941, -0.8629183168706102691, -1.937285153019531414 ) ) ;
#21219=CARTESIAN_POINT ( 'NONE',  ( 1.037374617392500031, -0.04523278242563041895, 2.019440925237799167 ) ) ;
#21224=CARTESIAN_POINT ( 'NONE',  ( 1.669428131952359839, 0.1607934374257547205, -2.155692497560882437 ) ) ;
#21228=CARTESIAN_POINT ( 'NONE',  ( 6.925078400183550364, 2.460400685555228950, 2.239421262742965268 ) ) ;
#21231=CARTESIAN_POINT ( 'NONE',  ( 6.245327377194020535, 0.3399632236478037917, -1.987496870419297013 ) ) ;
#21233=CARTESIAN_POINT ( 'NONE',  ( 0.3456114054924685486, 0.6817542107791437767, -2.082909237240769151 ) ) ;
#21235=CARTESIAN_POINT ( 'NONE',  ( 6.819229411136438657, -0.1619093195798972928, 2.126376854085454404 ) ) ;
#21242=CARTESIAN_POINT ( 'NONE',  ( 4.389066697632080682, 1.539216480442310075, -0.7786167122535156970 ) ) ;
#21244=CARTESIAN_POINT ( 'NONE',  ( 1.545802484126792109, 1.767419949743149532, 0.09338694931935660748 ) ) ;
#21246=CARTESIAN_POINT ( 'NONE',  ( 5.438574045396407541, 2.173287242562565780, 0.3821286992964008089 ) ) ;
#21248=CARTESIAN_POINT ( 'NONE',  ( 4.588152005245718534, 1.166368207181975869, 1.648760302449885584 ) ) ;
#21250=CARTESIAN_POINT ( 'NONE',  ( 3.809332071562030908, 1.790574611000576244, -1.135637872363919110 ) ) ;
#21251=CARTESIAN_POINT ( 'NONE',  ( 3.532827515057835654, -1.646827434736859441, 1.163287548526056980 ) ) ;
#21252=CARTESIAN_POINT ( 'NONE',  ( 4.095841850722721667, 1.188128187434208893, 1.367607970084052660 ) ) ;
#21256=CARTESIAN_POINT ( 'NONE',  ( 1.199835987674138460, -1.870836310881810682, -0.003643258294119822160 ) ) ;
#21259=CARTESIAN_POINT ( 'NONE',  ( 6.410821795378537580, -0.4906875946298261959, -1.743675775721682752 ) ) ;
#21264=CARTESIAN_POINT ( 'NONE',  ( -0.01753026575586694516, -1.247696154478775021, 1.449428981083925150 ) ) ;
#21267=CARTESIAN_POINT ( 'NONE',  ( 1.785527960060459440, -1.848404783191982315, 0.6579185095809261252 ) ) ;
#21270=CARTESIAN_POINT ( 'NONE',  ( 3.674183785563363447, 2.104178206457421485, -0.2630699042918820396 ) ) ;
#21273=CARTESIAN_POINT ( 'NONE',  ( 6.011001170722232168, 1.737326539053269059, 0.9316862151012759163 ) ) ;
#21275=CARTESIAN_POINT ( 'NONE',  ( 1.301040509920841526, -0.2996390532185671529, -1.990687865782204469 ) ) ;
#21277=CARTESIAN_POINT ( 'NONE',  ( 0.8435474745839615096, 0.4086855458026328880, -2.077256349191716200 ) ) ;
#21280=CARTESIAN_POINT ( 'NONE',  ( 2.752462066230080495, -2.064650614848703825, -0.1547973748374023295 ) ) ;
#21284=CARTESIAN_POINT ( 'NONE',  ( 5.050766879278534738, -1.765858898356540196, -1.118837652998798005 ) ) ;
#21286=CARTESIAN_POINT ( 'NONE',  ( 2.854317205943053271, 0.6132515345431620579, 1.719634925709014439 ) ) ;
#21287=CARTESIAN_POINT ( 'NONE',  ( 1.541375357114631806, -1.705629342057282560, 0.6104535550692562484 ) ) ;
#21292=CARTESIAN_POINT ( 'NONE',  ( 4.190592561755676293, -2.182319254149690302, -0.3268587364041104504 ) ) ;
#21296=CARTESIAN_POINT ( 'NONE',  ( 3.352119889487484183, 0.8575151890419380196, -1.709291564166728783 ) ) ;
#21299=CARTESIAN_POINT ( 'NONE',  ( 6.074686117427479104, 1.393331124738606874, -1.531503843499823159 ) ) ;
#21301=CARTESIAN_POINT ( 'NONE',  ( 6.146043800834426918, 0.6857851511376764631, 2.081541312870714311 ) ) ;
#21306=CARTESIAN_POINT ( 'NONE',  ( 3.778450875046265534, -1.801938340082277712, -0.5016190811713144848 ) ) ;
#21312=CARTESIAN_POINT ( 'NONE',  ( 0.4616802850961505555, -0.5308588990461468038, 1.896450293990773472 ) ) ;
#21313=CARTESIAN_POINT ( 'NONE',  ( 1.142204091441896718, 0.8197918422115093584, 1.842440257734210274 ) ) ;
#21317=CARTESIAN_POINT ( 'NONE',  ( 1.465048628566959055, 0.1585425061045864503, -2.185770122351132994 ) ) ;
#21318=CARTESIAN_POINT ( 'NONE',  ( 6.076747101522134820, -1.735163100867884500, -0.5679748894881069265 ) ) ;
#21324=VERTEX_POINT ( 'NONE', #132335 ) ;
#21325=CARTESIAN_POINT ( 'NONE',  ( 3.790429961727882713, 1.553415782126759792, -0.9881970032953185656 ) ) ;
#21326=CARTESIAN_POINT ( 'NONE',  ( 0.2408851659233458842, 1.927091567462356547, 0.5821649069043339786 ) ) ;
#21327=CARTESIAN_POINT ( 'NONE',  ( 1.845480572931688767, -1.229624162049542058, 1.941665159144045250 ) ) ;
#21329=CARTESIAN_POINT ( 'NONE',  ( 6.842638302680406071, -1.923265442670134329, -0.3857968560932593660 ) ) ;
#21333=CARTESIAN_POINT ( 'NONE',  ( 4.306835718904429733, -0.4242474483713705169, -1.864571660543254961 ) ) ;
#21337=CARTESIAN_POINT ( 'NONE',  ( 2.999644136165266595, -2.088248420355208523, 0.1050208477483879216 ) ) ;
#21338=CARTESIAN_POINT ( 'NONE',  ( 1.217418975555501826, -1.825842229346545498, 0.4062821374252246764 ) ) ;
#21341=CARTESIAN_POINT ( 'NONE',  ( 2.928976884739741493, -1.170936322307249089, -1.287801759770091925 ) ) ;
#21344=CARTESIAN_POINT ( 'NONE',  ( 3.879312468746206832, 1.623315624747388775, -0.5835212994509741957 ) ) ;
#21346=CARTESIAN_POINT ( 'NONE',  ( 3.720431430916489646, 2.081484170424623859, 0.6860852429351402826 ) ) ;
#21347=CARTESIAN_POINT ( 'NONE',  ( 5.830760709146560750, 2.125890151018691832, 0.5921790101122563765 ) ) ;
#21350=CARTESIAN_POINT ( 'NONE',  ( 3.151421466623941292, 1.864366918651944927, -1.112252681494025897 ) ) ;
#21351=CARTESIAN_POINT ( 'NONE',  ( 1.769861954154128725, 0.9373860217288846330, 1.566528536362868707 ) ) ;
#21353=CARTESIAN_POINT ( 'NONE',  ( 4.048151681910251654, 1.001636719310808887, 1.865476516996619649 ) ) ;
#21356=CARTESIAN_POINT ( 'NONE',  ( 5.249693134425458041, 2.289860626911474739, -0.1101728261837572470 ) ) ;
#21358=CARTESIAN_POINT ( 'NONE',  ( 6.620655732516673275, 1.290356161719278028, 1.942653802560645460 ) ) ;
#21360=CARTESIAN_POINT ( 'NONE',  ( 0.6453774867190856801, 0.1600191834128759094, 2.114519675249281416 ) ) ;
#21364=CARTESIAN_POINT ( 'NONE',  ( 6.883263157960358924, 4.692138088316172073, 2.616388454592593504 ) ) ;
#21367=CARTESIAN_POINT ( 'NONE',  ( 4.957657809308734898, -1.899617967926207740, -0.6767155953601932117 ) ) ;
#21369=CARTESIAN_POINT ( 'NONE',  ( 4.416881224320576393, -1.531859844946925397, 1.381376250335116795 ) ) ;
#21371=CARTESIAN_POINT ( 'NONE',  ( 6.883263157960399781, 2.970623603138924818, 2.399364662246627589 ) ) ;
#21375=CARTESIAN_POINT ( 'NONE',  ( 0.5508686287750690358, -1.767239575335936230, -1.116659500934626514 ) ) ;
#21376=CARTESIAN_POINT ( 'NONE',  ( 4.799454022740247794, 1.388487131293577592, -1.462444391756134943 ) ) ;
#21377=CARTESIAN_POINT ( 'NONE',  ( 3.649809678215182096, 0.6660801477775115664, 1.716721118343276453 ) ) ;
#21380=CARTESIAN_POINT ( 'NONE',  ( 0.8149653058732795330, -0.2595981955949409614, 1.704996164590016683 ) ) ;
#21382=CARTESIAN_POINT ( 'NONE',  ( 1.284255082537180570, 1.875723515222413207, -1.328569176028525645 ) ) ;
#21384=CARTESIAN_POINT ( 'NONE',  ( 0.3864610594027502732, -1.064975819449946126, 1.996106434226818216 ) ) ;
#21385=CARTESIAN_POINT ( 'NONE',  ( 2.614012881481563522, -2.083059734262616036, 0.3096129728813925008 ) ) ;
#21389=CARTESIAN_POINT ( 'NONE',  ( 5.843750000000004441, 1.895863743164205140, 0.7852924748296741253 ) ) ;
#21394=CARTESIAN_POINT ( 'NONE',  ( 3.480930870787651621, -1.489476591903232228, 1.648259452209248854 ) ) ;
#21395=CARTESIAN_POINT ( 'NONE',  ( 1.799034956846547795, 1.823213324544867397, 1.215573211712846158 ) ) ;
#21399=CARTESIAN_POINT ( 'NONE',  ( 5.652778587040098834, -0.4750822840141955550, -1.903360745478323679 ) ) ;
#21403=CARTESIAN_POINT ( 'NONE',  ( 4.851869265964163347, -1.501451181749386743, -1.497782127133556518 ) ) ;
#21407=CARTESIAN_POINT ( 'NONE',  ( 5.682550338946039226, -2.108058120380253087, -0.4779004524640489970 ) ) ;
#21409=CARTESIAN_POINT ( 'NONE',  ( 5.056134578334451568, -1.329838508726857382, 1.273713382018211382 ) ) ;
#21412=CARTESIAN_POINT ( 'NONE',  ( 6.456985410506528744, 0.2896317775202154610, -1.715898445072817413 ) ) ;
#21417=CARTESIAN_POINT ( 'NONE',  ( 5.401312781148373432, 1.764888628567516049, 1.247983453017486699 ) ) ;
#21420=CARTESIAN_POINT ( 'NONE',  ( 3.784175263432405956, -1.067420458145739826, 1.879713924940962677 ) ) ;
#21421=CARTESIAN_POINT ( 'NONE',  ( 4.727780648284140241, -1.210341919374293473, -1.556009220651358715 ) ) ;
#21422=CARTESIAN_POINT ( 'NONE',  ( 4.182719533963025427, -0.8905394866418876454, -1.487461311242815443 ) ) ;
#21423=CARTESIAN_POINT ( 'NONE',  ( 0.6971427418834205136, 1.794861059153027627, 1.257291590721874686 ) ) ;
#21424=CARTESIAN_POINT ( 'NONE',  ( 1.800300592175264613, -0.7760554750895022336, 2.173288546431056734 ) ) ;
#21425=CARTESIAN_POINT ( 'NONE',  ( 3.761055697714862589, -1.815786459315921642, -0.9745866149870155981 ) ) ;
#21426=CARTESIAN_POINT ( 'NONE',  ( 6.181195893160847277, 1.342424930544680928, 1.403604608442722057 ) ) ;
#21432=CARTESIAN_POINT ( 'NONE',  ( 3.891806949550260519, 1.596497936513015192, 1.523729906679156754 ) ) ;
#21435=CARTESIAN_POINT ( 'NONE',  ( 0.9185399124422718442, -1.353032588479759157, 1.277947871810279246 ) ) ;
#21441=CARTESIAN_POINT ( 'NONE',  ( -0.2104748580754166598, -0.006608320950483163522, -2.103482951484026753 ) ) ;
#21442=VERTEX_POINT ( 'NONE', #31612 ) ;
#21443=CARTESIAN_POINT ( 'NONE',  ( 3.397389285588784169, 1.623555618760182062, 1.269252347208242870 ) ) ;
#21449=CARTESIAN_POINT ( 'NONE',  ( 2.237249138949083171, -1.841491494976960075, 0.9254197329602343869 ) ) ;
#21455=CARTESIAN_POINT ( 'NONE',  ( 6.041676539500916654, -1.595688354349385607, -1.524751901930617715 ) ) ;
#21456=CARTESIAN_POINT ( 'NONE',  ( 6.661402789601885033, 0.3967159107356016401, -2.227235065690711835 ) ) ;
#21458=CARTESIAN_POINT ( 'NONE',  ( 0.9191581010105540628, -1.820984308097562954, 0.8666112775468015617 ) ) ;
#21459=CARTESIAN_POINT ( 'NONE',  ( 1.634533438177967923, 0.1689203749893586071, -2.292248917674902575 ) ) ;
#21462=CARTESIAN_POINT ( 'NONE',  ( 1.498681428038322050, 1.531199225506232553, -1.074333469806128427 ) ) ;
#21463=CARTESIAN_POINT ( 'NONE',  ( 3.257046257486408969, 0.04465439498414420366, -2.016188763087948033 ) ) ;
#21467=CARTESIAN_POINT ( 'NONE',  ( 5.567048526788405560, -1.903460050192711028, -0.9016015758830184801 ) ) ;
#21472=CARTESIAN_POINT ( 'NONE',  ( 3.568621913994294292, 0.7309530501433506577, 1.883054584751037819 ) ) ;
#21474=CARTESIAN_POINT ( 'NONE',  ( 0.8837254586576195337, -1.959797800638187093, 0.6432524670345032280 ) ) ;
#21476=CARTESIAN_POINT ( 'NONE',  ( 5.431013727915853906, 0.1530101862373678123, 2.156222312673663488 ) ) ;
#21482=CARTESIAN_POINT ( 'NONE',  ( 3.016274402391531773, 2.160936140102893255, -0.2104436154053441199 ) ) ;
#21485=CARTESIAN_POINT ( 'NONE',  ( 1.821575194732877545, 1.059174331173462935, -1.505913648122420900 ) ) ;
#21487=CARTESIAN_POINT ( 'NONE',  ( 3.439196427729715566, -1.660734982795486481, -1.430121640581414111 ) ) ;
#21488=CARTESIAN_POINT ( 'NONE',  ( 6.883263157960364254, 2.038911835798001171, 2.358809022084580764 ) ) ;
#21489=CARTESIAN_POINT ( 'NONE',  ( 4.417028899805944597, 2.066919071766720517, 0.9206345982136554529 ) ) ;
#21496=CARTESIAN_POINT ( 'NONE',  ( 5.782415762239879520, -1.726843194930051562, -0.3863986657466413899 ) ) ;
#21498=CARTESIAN_POINT ( 'NONE',  ( 3.457684585873057159, -1.525941150838805216, -1.313146537923309376 ) ) ;
#21500=CARTESIAN_POINT ( 'NONE',  ( 1.395691461817370804, 1.594359505120213960, 1.375974583626845993 ) ) ;
#21502=CARTESIAN_POINT ( 'NONE',  ( 2.453506318599480096, 1.520516184767862100, 1.251830903418025054 ) ) ;
#21504=CARTESIAN_POINT ( 'NONE',  ( 5.765820309002536170, 0.5175119463115984697, -1.736122601384345820 ) ) ;
#21508=CARTESIAN_POINT ( 'NONE',  ( 5.014452206985246185, 1.289541220462528504, -1.355370375751355105 ) ) ;
#21509=CARTESIAN_POINT ( 'NONE',  ( 5.594608825991118195, 2.038665915018455177, 0.3594684214384344378 ) ) ;
#21518=CARTESIAN_POINT ( 'NONE',  ( 4.844172697165038066, -0.9265620464425131653, 1.729294158640543699 ) ) ;
#21520=CARTESIAN_POINT ( 'NONE',  ( 2.934922540206804875, 1.076151813804010926, 1.704677747124828446 ) ) ;
#21521=CARTESIAN_POINT ( 'NONE',  ( 1.991283197800724825, -0.4156388933829333610, 1.869923353789121556 ) ) ;
#21523=CARTESIAN_POINT ( 'NONE',  ( 0.8025787753177977546, 1.655945718051672566, -1.435626523826734280 ) ) ;
#21526=CARTESIAN_POINT ( 'NONE',  ( 2.671000074538076863, 0.09590037325727870932, -1.868228684465601752 ) ) ;
#21528=CARTESIAN_POINT ( 'NONE',  ( 4.324480843662709795, -0.8647720088908043001, -1.818167814553457884 ) ) ;
#21532=CARTESIAN_POINT ( 'NONE',  ( 4.376635333690025220, -0.4654363970535125294, -2.065280895323940324 ) ) ;
#21535=CARTESIAN_POINT ( 'NONE',  ( 5.863751307568212390, -0.5067217619753560109, 2.007263066363853987 ) ) ;
#21536=CARTESIAN_POINT ( 'NONE',  ( 1.505537475160537264, -2.074567991729712180, 0.2591490344204059881 ) ) ;
#21538=CARTESIAN_POINT ( 'NONE',  ( 5.948246703923279810, 1.823645139926059144, 0.08696428134234018836 ) ) ;
#21539=VERTEX_POINT ( 'NONE', #213517 ) ;
#21545=CARTESIAN_POINT ( 'NONE',  ( 0.8557779741884026237, 0.7350315055517571139, -1.655818919202347361 ) ) ;
#21553=CARTESIAN_POINT ( 'NONE',  ( 5.694935465533643715, 1.779635825068434984, 0.9480254120717497290 ) ) ;
#21554=CARTESIAN_POINT ( 'NONE',  ( 0.6980877996264934771, 1.427081234210248573, 1.568565553304770877 ) ) ;
#21558=CARTESIAN_POINT ( 'NONE',  ( -0.1394461523061195918, 0.2309855492786689335, -2.314897844796594661 ) ) ;
#21562=CARTESIAN_POINT ( 'NONE',  ( 3.555474331475856786, 1.549626312082365898, 1.215309171139463684 ) ) ;
#21563=CARTESIAN_POINT ( 'NONE',  ( 4.499625164952708367, -1.976952908697379607, 0.3961224619316304763 ) ) ;
#21566=CARTESIAN_POINT ( 'NONE',  ( 4.312563266315373234, 2.003113633248252867, 0.8892094534625747393 ) ) ;
#21567=CARTESIAN_POINT ( 'NONE',  ( 3.153258193586833347, -1.574033464040735408, -1.110325110657943481 ) ) ;
#21569=CARTESIAN_POINT ( 'NONE',  ( -0.02968770228140017037, 2.049257630910449990, -2.243713227073070637 ) ) ;
#21570=CARTESIAN_POINT ( 'NONE',  ( 0.3291288957359936318, 2.113116833900237967, 0.6364493931270903682 ) ) ;
#21574=CARTESIAN_POINT ( 'NONE',  ( 4.838697515689712958, -1.909247481386136647, -0.4825833779809485802 ) ) ;
#21575=CARTESIAN_POINT ( 'NONE',  ( 0.3275467377269140057, 0.9974989819340736030, -1.666164454441501297 ) ) ;
#21576=CARTESIAN_POINT ( 'NONE',  ( 4.266274873615797603, 2.012593780953766842, -0.05172614775082911426 ) ) ;
#21577=CARTESIAN_POINT ( 'NONE',  ( 5.360842878201462547, -0.8341330746063200241, 2.141841041818067559 ) ) ;
#21579=CARTESIAN_POINT ( 'NONE',  ( 3.432308073483012922, -1.112138214925220803, 1.491878268611693814 ) ) ;
#21585=CARTESIAN_POINT ( 'NONE',  ( 0.5213437761196970666, -2.079166062760181788, 0.6930039600180630810 ) ) ;
#21591=CARTESIAN_POINT ( 'NONE',  ( 0.8908993799596062191, 1.611356928563783208, -0.8583080905386344384 ) ) ;
#21593=CARTESIAN_POINT ( 'NONE',  ( 2.338123177510130102, 0.4612838472501363252, -1.671594290515050041 ) ) ;
#21595=CARTESIAN_POINT ( 'NONE',  ( 6.509000000000012776, 0.5843741663743782233, 2.053293374786519188 ) ) ;
#21598=CARTESIAN_POINT ( 'NONE',  ( 0.3915760470782835845, -1.894197279051227811, 0.8358220917567968922 ) ) ;
#21599=CARTESIAN_POINT ( 'NONE',  ( 5.373610676068619973, 1.758448663713826132, -0.4906839848310071139 ) ) ;
#21600=CARTESIAN_POINT ( 'NONE',  ( 3.748837004188230182, -0.3782986639458625899, -1.924763881548184230 ) ) ;
#21604=CARTESIAN_POINT ( 'NONE',  ( 3.791739704763209318, 1.996120715041304061, -0.7158466834289513026 ) ) ;
#21605=CARTESIAN_POINT ( 'NONE',  ( 6.827182134110198142, 6.033542260787205791, 2.783941933017803905 ) ) ;
#21607=CARTESIAN_POINT ( 'NONE',  ( 1.323191598296684646, -1.869966582492128548, -0.8887066864657000576 ) ) ;
#21609=CARTESIAN_POINT ( 'NONE',  ( 4.811300260135710438, 1.847242992945047568, -1.233362022257722845 ) ) ;
#21611=CARTESIAN_POINT ( 'NONE',  ( 2.163060705912169812, 1.417378650759585357, 1.809622876518288681 ) ) ;
#21619=CARTESIAN_POINT ( 'NONE',  ( 2.654443970922310214, 1.898414275235399407, 0.2300336082040748686 ) ) ;
#21621=CARTESIAN_POINT ( 'NONE',  ( 3.750762392430748271, -1.410035727865316613, 0.9929894849482110430 ) ) ;
#21622=CARTESIAN_POINT ( 'NONE',  ( 2.360564879530482330, -1.931125380751706810, -0.5807522007576990664 ) ) ;
#21623=CARTESIAN_POINT ( 'NONE',  ( 4.043764476089898530, -1.703284420474758143, 1.543771250003633355 ) ) ;
#21624=CARTESIAN_POINT ( 'NONE',  ( 3.532755146446086680, 2.206387722723508915, 0.4996636332569806549 ) ) ;
#21625=CARTESIAN_POINT ( 'NONE',  ( 5.918611218600786650, 1.415673333675367296, -1.559471542009479350 ) ) ;
#21627=CARTESIAN_POINT ( 'NONE',  ( 4.639784515242838303, 0.7573303825321504590, -1.599664492173937358 ) ) ;
#21629=CARTESIAN_POINT ( 'NONE',  ( 1.060933235008169051, -2.074266264760935563, -0.9759354127518887756 ) ) ;
#21630=CARTESIAN_POINT ( 'NONE',  ( 5.384640740818634974, 1.621930891500168670, -0.8712783443201177480 ) ) ;
#21632=CARTESIAN_POINT ( 'NONE',  ( 5.841772037242090931, 2.188765561305112683, 0.1107676204459909497 ) ) ;
#21636=CARTESIAN_POINT ( 'NONE',  ( 6.355931484454268698, -0.7012994977402075003, 1.948090369817329526 ) ) ;
#21637=CARTESIAN_POINT ( 'NONE',  ( 1.727750297885573882, 0.7672897036171549834, -1.865047645237365215 ) ) ;
#21640=CARTESIAN_POINT ( 'NONE',  ( 4.055238279289786973, -1.602352113334176043, -1.069235405101864878 ) ) ;
#21642=CARTESIAN_POINT ( 'NONE',  ( 1.635333617853749200, 2.074933741853498770, 0.7937918740310870858 ) ) ;
#21652=CARTESIAN_POINT ( 'NONE',  ( 4.722041168748464912, 1.667336974042502584, 0.4991589302964939412 ) ) ;
#21653=CARTESIAN_POINT ( 'NONE',  ( 2.348037267531626338, -0.8415878996531295231, 1.772339229757218471 ) ) ;
#21659=CARTESIAN_POINT ( 'NONE',  ( 6.742638286788313451, -1.923764577213080029, -0.3838556375530403630 ) ) ;
#21662=CARTESIAN_POINT ( 'NONE',  ( 5.050017674172561755, 0.9981218692422781924, 1.752141108012375437 ) ) ;
#21663=CARTESIAN_POINT ( 'NONE',  ( 1.534417833908331863, 1.113959020207640593, -1.969227013157865303 ) ) ;
#21667=CARTESIAN_POINT ( 'NONE',  ( 1.493192106177696044, 1.412881632968411516, 1.225925835885120829 ) ) ;
#21668=CARTESIAN_POINT ( 'NONE',  ( 0.3340423123194468658, 0.5469568729883391711, -1.645723886551814452 ) ) ;
#21670=CARTESIAN_POINT ( 'NONE',  ( 3.825867475279482566, 1.171244075711602051, -1.852137614134836907 ) ) ;
#21671=CARTESIAN_POINT ( 'NONE',  ( 5.456226512670824036, 2.305251103711564387, -0.1065007851034898423 ) ) ;
#21672=CARTESIAN_POINT ( 'NONE',  ( 0.5849274615713345726, -0.2514902370338990001, -2.045404637917444646 ) ) ;
#21673=CARTESIAN_POINT ( 'NONE',  ( 3.134642302965468641, -1.712256071497103349, 0.9161664635699683368 ) ) ;
#21677=CARTESIAN_POINT ( 'NONE',  ( 3.885388821667290493, -0.6351983117205138862, -1.913803978180687482 ) ) ;
#21681=CARTESIAN_POINT ( 'NONE',  ( 0.8030139110496161692, 1.490934425176414502, 1.053415343471690857 ) ) ;
#21687=CARTESIAN_POINT ( 'NONE',  ( 6.737187473210400235, -1.842164534206979676, 0.9240717516781959961 ) ) ;
#21691=CARTESIAN_POINT ( 'NONE',  ( 5.971354884044596467, -1.733367664992270685, -1.036320259733174209 ) ) ;
#21692=CARTESIAN_POINT ( 'NONE',  ( 6.182328207180960433, 1.139467527619671294, 1.906663674214443382 ) ) ;
#21697=CARTESIAN_POINT ( 'NONE',  ( 5.278222320829740077, -1.146742738506721704, 1.712165125756033968 ) ) ;
#21698=CARTESIAN_POINT ( 'NONE',  ( 4.447888798048591497, -1.802416534049579910, -0.9041112711936499791 ) ) ;
#21705=CARTESIAN_POINT ( 'NONE',  ( 4.024767406304472495, 2.001204788683898617, -0.2439926020210633206 ) ) ;
#21706=CARTESIAN_POINT ( 'NONE',  ( 3.204851553285171573, -0.3583046703147829137, 1.805758307424263354 ) ) ;
#21709=CARTESIAN_POINT ( 'NONE',  ( 2.262750896497740527, 0.9887190084108381516, 2.085292768615305992 ) ) ;
#21711=CARTESIAN_POINT ( 'NONE',  ( 4.358765367649009903, -1.604958417591015207, 1.448176592534822005 ) ) ;
#21713=CARTESIAN_POINT ( 'NONE',  ( -0.07675543424010172755, -1.195724141806488561, -1.531021551883532172 ) ) ;
#21718=CARTESIAN_POINT ( 'NONE',  ( 2.553401164250346245, 0.5009360343536627402, -1.802255699741683870 ) ) ;
#21720=CARTESIAN_POINT ( 'NONE',  ( 6.561403051094389483, 0.3373947195176879021, -1.942235834477159084 ) ) ;
#21724=CARTESIAN_POINT ( 'NONE',  ( 1.963769682107346037, 0.3752889857368995608, -2.174583152744386627 ) ) ;
#21730=CARTESIAN_POINT ( 'NONE',  ( 5.946159419501746868, 1.969187058922382993, 0.09738397392708775246 ) ) ;
#21732=CARTESIAN_POINT ( 'NONE',  ( 5.479250216003205054, -0.05159697844352681417, -2.307286710698839727 ) ) ;
#21733=CARTESIAN_POINT ( 'NONE',  ( 0.2210476084268316321, -1.750679471464357650, -0.8856473702157914296 ) ) ;
#21734=CARTESIAN_POINT ( 'NONE',  ( 4.329007229187351591, -1.922695762783795947, -0.7470244877981512266 ) ) ;
#21741=CARTESIAN_POINT ( 'NONE',  ( 6.531686450800388677, 2.079676181002787061, -0.6237389289161490158 ) ) ;
#21744=CARTESIAN_POINT ( 'NONE',  ( 5.372543328820884589, -0.05112055865702340440, -1.840719716649619198 ) ) ;
#21746=CARTESIAN_POINT ( 'NONE',  ( 6.216381822182693639, 2.044192415450503120, 0.7905562269360306704 ) ) ;
#21747=CARTESIAN_POINT ( 'NONE',  ( 0.1806930697454533219, -0.1309388314422038346, -1.840455529407057256 ) ) ;
#21752=CARTESIAN_POINT ( 'NONE',  ( 0.4516295384478057895, -1.352486712789632950, -1.352142238705160704 ) ) ;
#21753=CARTESIAN_POINT ( 'NONE',  ( 2.078617942332625201, -0.08328603760934982780, -1.768007077409910588 ) ) ;
#21754=CARTESIAN_POINT ( 'NONE',  ( 6.358070405704149941, 0.7683137238208622710, -1.860897411154702530 ) ) ;
#21756=CARTESIAN_POINT ( 'NONE',  ( 4.095261013068919098, -0.3237038700398958690, 1.887879439767611744 ) ) ;
#21758=CARTESIAN_POINT ( 'NONE',  ( 5.705506402468259353, -1.551454039220935055, -1.213164361648248368 ) ) ;
#21759=CARTESIAN_POINT ( 'NONE',  ( 0.1938080739139167730, 1.976361990896974508, -0.7691651810952588875 ) ) ;
#21761=CARTESIAN_POINT ( 'NONE',  ( 2.377632874612686020, 1.149002834218125102, 1.476114537088555112 ) ) ;
#21762=CARTESIAN_POINT ( 'NONE',  ( 5.883370885758751001, 1.591107372635025330, -0.6665480857693687478 ) ) ;
#21764=CARTESIAN_POINT ( 'NONE',  ( 3.229339687698820072, 0.05429069646168545316, 2.206380697113208722 ) ) ;
#21767=CARTESIAN_POINT ( 'NONE',  ( 1.258340527071156956, -2.062851378465610175, -0.001992840727984764547 ) ) ;
#21772=VERTEX_POINT ( 'NONE', #37730 ) ;
#21773=CARTESIAN_POINT ( 'NONE',  ( 3.174344110969638866, -1.018096006688212096, -1.802650257252853772 ) ) ;
#21777=CARTESIAN_POINT ( 'NONE',  ( 1.119792439799172978, -0.4886160933238526405, 1.959555815251372568 ) ) ;
#21781=CARTESIAN_POINT ( 'NONE',  ( 0.07479286986302942364, 7.629137130509078268, -2.455503679634089220 ) ) ;
#21783=CARTESIAN_POINT ( 'NONE',  ( 6.222029796014385106, -1.727739227931901489, -1.038831587593692873 ) ) ;
#21784=CARTESIAN_POINT ( 'NONE',  ( 5.981633625760849782, -0.6386546108097415075, 1.806296054365429393 ) ) ;
#21786=CARTESIAN_POINT ( 'NONE',  ( 3.966501855323391723, -2.045284974426237579, -0.7877190255709336508 ) ) ;
#21788=CARTESIAN_POINT ( 'NONE',  ( 1.968876373762207477, -1.476028252698018406, 1.215921256797661609 ) ) ;
#21792=CARTESIAN_POINT ( 'NONE',  ( 0.8609541034889023337, -0.05231784723681161264, -2.015913592316537883 ) ) ;
#21794=EDGE_CURVE ( 'NONE', #11785, #88459, #15627, .T. ) ;
#21795=CARTESIAN_POINT ( 'NONE',  ( 5.706613541269077494, 1.932210019790636224, 1.034112652976440394 ) ) ;
#21797=CARTESIAN_POINT ( 'NONE',  ( 3.557352906045672114, 0.4196458916515317661, -1.672789571874600645 ) ) ;
#21798=EDGE_LOOP ( 'NONE', ( #200999, #34723, #34247, #207814 ) ) ;
#21799=CARTESIAN_POINT ( 'NONE',  ( 0.1394461523057136665, 2.058909413595513715, -2.136561586061051621 ) ) ;
#21803=CARTESIAN_POINT ( 'NONE',  ( 1.240593047436115759, -1.913272810121857237, -0.4332019784048374289 ) ) ;
#21811=CARTESIAN_POINT ( 'NONE',  ( 4.477109312160544974, -1.620259271022955305, -0.8101795318041657978 ) ) ;
#21812=ORIENTED_EDGE ( 'NONE', *, *, #78667, .T. ) ;
#21816=CARTESIAN_POINT ( 'NONE',  ( 4.494648839764849413, -1.758179434694202570, -0.4356380854809716041 ) ) ;
#21819=CARTESIAN_POINT ( 'NONE',  ( 5.670303652858919463, -0.8369403475225531963, -1.662290214344812833 ) ) ;
#21821=CARTESIAN_POINT ( 'NONE',  ( 2.284663151613754550, 1.537047112958013440, -1.143011353438025957 ) ) ;
#21829=CARTESIAN_POINT ( 'NONE',  ( 1.517645033149318978, -1.162591604200275963, -1.737351732476496657 ) ) ;
#21831=CARTESIAN_POINT ( 'NONE',  ( 6.563506682682211490, 0.3285509523427312950, -1.898022546839329472 ) ) ;
#21833=CARTESIAN_POINT ( 'NONE',  ( 2.660947563312371589, -1.587261545009664765, -0.9017329732442301848 ) ) ;
#21835=CARTESIAN_POINT ( 'NONE',  ( 1.880979024232478425, -1.749874716401520036, -0.7718601483891265325 ) ) ;
#21836=CARTESIAN_POINT ( 'NONE',  ( 1.838274926946784182, -1.056231965017372598, 1.662188548998255078 ) ) ;
#21837=CARTESIAN_POINT ( 'NONE',  ( 4.177243316516196181, 1.270932653052879502, 1.468510540936379671 ) ) ;
#21842=CARTESIAN_POINT ( 'NONE',  ( 3.744478000529617656, 1.131475959888720295, -1.793321066073015224 ) ) ;
#21851=CARTESIAN_POINT ( 'NONE',  ( 3.615676881913011176, -1.798418494116042821, 0.3134422064149794407 ) ) ;
#21856=CARTESIAN_POINT ( 'NONE',  ( 4.223419137798128276, -1.790188510885984297, 0.5427707113358354318 ) ) ;
#21858=CARTESIAN_POINT ( 'NONE',  ( 1.699704897782030377, -0.6493637136964022227, 1.813892859743936103 ) ) ;
#21859=CARTESIAN_POINT ( 'NONE',  ( 6.825062041929172985, -1.792332737533608666, -0.7979697884207545000 ) ) ;
#21867=CARTESIAN_POINT ( 'NONE',  ( 0.8786900280967164800, -0.5185874880111912555, -2.052613615991748297 ) ) ;
#21870=CARTESIAN_POINT ( 'NONE',  ( 5.401260523219934662, -1.778462342247935979, 1.059464396209061521 ) ) ;
#21871=CARTESIAN_POINT ( 'NONE',  ( 0.5910386730991653570, -0.6632029860377097741, 1.717849102829023922 ) ) ;
#21873=CARTESIAN_POINT ( 'NONE',  ( 5.397245865906225681, -1.031513598091776673, -2.054350403923683732 ) ) ;
#21877=CARTESIAN_POINT ( 'NONE',  ( 1.957357739143847919, 0.3891275796813770116, -2.258848713223185367 ) ) ;
#21880=CARTESIAN_POINT ( 'NONE',  ( 5.788998755281030029, 1.472039788614720290, 1.266697539889444446 ) ) ;
#21884=CARTESIAN_POINT ( 'NONE',  ( 5.941656858135131891, -1.798430535887390658, 0.6506349336675710804 ) ) ;
#21885=CARTESIAN_POINT ( 'NONE',  ( 5.647672796105281279, 1.985869605424210649, -0.3494789899042491932 ) ) ;
#21889=CARTESIAN_POINT ( 'NONE',  ( 2.800817752552913209, 1.766549217158249085, 1.117748608743725169 ) ) ;
#21890=CARTESIAN_POINT ( 'NONE',  ( 1.533702468213002712, 0.8761213712049474855, -1.537698828099523629 ) ) ;
#21892=CARTESIAN_POINT ( 'NONE',  ( 3.715000766203532034, -0.1696613574440029304, 2.286031353463747529 ) ) ;
#21893=CARTESIAN_POINT ( 'NONE',  ( 2.923474784230184920, 0.9664119506291848349, -1.447106689822146963 ) ) ;
#21897=CARTESIAN_POINT ( 'NONE',  ( 2.266548906626513649, -1.733607756391885912, 0.03760194650299571173 ) ) ;
#21898=CARTESIAN_POINT ( 'NONE',  ( 3.965408508876398841, 1.860285638359628235, 1.119340054616506874 ) ) ;
#21900=CARTESIAN_POINT ( 'NONE',  ( 4.856657812281613751, -1.900414607462055816, -0.6748505307947461063 ) ) ;
#21901=CARTESIAN_POINT ( 'NONE',  ( 2.156250000000001776, -1.895863743164040160, 0.7852924748301010061 ) ) ;
#21903=CARTESIAN_POINT ( 'NONE',  ( 0.7801460289126905812, -1.072782840069667509, 1.599849161009530674 ) ) ;
#21905=CARTESIAN_POINT ( 'NONE',  ( 4.641020947978182321, 2.126209183204033959, 0.6434571820467527292 ) ) ;
#21907=CARTESIAN_POINT ( 'NONE',  ( -0.1108833634137010027, 1.377173795795206157, -2.152720132533674668 ) ) ;
#21912=CARTESIAN_POINT ( 'NONE',  ( 0.8037664367953377687, 1.956346004370253633, -1.052120880887427390 ) ) ;
#21913=CARTESIAN_POINT ( 'NONE',  ( 5.846142468697441252, -0.8834969228576605715, 1.751761657833034613 ) ) ;
#21916=CARTESIAN_POINT ( 'NONE',  ( 0.5972264258897291844, 1.797487153981947916, -1.200333582630601637 ) ) ;
#21918=CARTESIAN_POINT ( 'NONE',  ( 3.613784930257180950, 0.5038104997578238820, -2.000076687661219044 ) ) ;
#21923=CARTESIAN_POINT ( 'NONE',  ( 4.481629103029507455, 1.220264704679861811, 1.417821649906551906 ) ) ;
#21924=CARTESIAN_POINT ( 'NONE',  ( 3.973097536218972436, -1.716008982208137468, -0.2490561736530460535 ) ) ;
#21925=CARTESIAN_POINT ( 'NONE',  ( 3.456370904947672074, -1.536751586138744852, -0.8169772437159742440 ) ) ;
#21926=CARTESIAN_POINT ( 'NONE',  ( 0.5566822826340491748, -1.655162342056889502, 1.586242259447123493 ) ) ;
#21928=CARTESIAN_POINT ( 'NONE',  ( 4.651946873442760477, 0.8016356570225026124, 1.931162265472508910 ) ) ;
#21929=CARTESIAN_POINT ( 'NONE',  ( 0.05820987927622478519, -1.643049995186950829, -0.8308948761173093889 ) ) ;
#21932=CARTESIAN_POINT ( 'NONE',  ( 0.3170300144729014669, 1.034162889623980286, -1.730867746391979933 ) ) ;
#21933=CARTESIAN_POINT ( 'NONE',  ( 0.8617730121942971389, -1.675286201960282995, -1.300076073212981242 ) ) ;
#21934=CARTESIAN_POINT ( 'NONE',  ( 6.925078400183550364, -0.007619068086212391067, 2.144148427808051594 ) ) ;
#21938=CARTESIAN_POINT ( 'NONE',  ( 2.367978261241600713, 0.5630001329197281690, -2.044326955284565539 ) ) ;
#21940=CARTESIAN_POINT ( 'NONE',  ( 4.582524934692378871, -1.771534430979417429, -0.4408631061849078714 ) ) ;
#21946=CARTESIAN_POINT ( 'NONE',  ( 2.338154391725711267, -1.166417678377267064, -1.648725491961404055 ) ) ;
#21947=CARTESIAN_POINT ( 'NONE',  ( 5.315527377757141458, -0.3284926246858720922, 2.182075488366498117 ) ) ;
#21949=CARTESIAN_POINT ( 'NONE',  ( 3.854231730816888302, -1.858662791824859051, -0.09517680055876918954 ) ) ;
#21957=CARTESIAN_POINT ( 'NONE',  ( 4.670415550810885996, -1.190324863180821646, 1.384379922071424351 ) ) ;
#21962=CARTESIAN_POINT ( 'NONE',  ( 0.9832555119714074809, 1.599142458273569600, 0.6705785602827417646 ) ) ;
#21963=CARTESIAN_POINT ( 'NONE',  ( 0.4271921415617612183, 0.8987490902026186168, -1.490136572063437637 ) ) ;
#21964=CARTESIAN_POINT ( 'NONE',  ( 5.953837893508783452, 0.6757001976828447276, -2.206575258351393565 ) ) ;
#21966=CARTESIAN_POINT ( 'NONE',  ( 1.001328657153805146, 1.683097017759589420, 1.188813969666648873 ) ) ;
#21968=CARTESIAN_POINT ( 'NONE',  ( 6.415373042369045820, 0.7112672321729663905, 2.185653275185605704 ) ) ;
#21971=CARTESIAN_POINT ( 'NONE',  ( 6.104356062600288624, -0.6750377415852754082, -1.744797942764392928 ) ) ;
#21972=CARTESIAN_POINT ( 'NONE',  ( 3.427896188528327226, -1.883279545317056547, 0.3315703044584616399 ) ) ;
#21975=CARTESIAN_POINT ( 'NONE',  ( 5.092482806099829062, -2.189899077852827780, -0.2726905915074183673 ) ) ;
#21980=CARTESIAN_POINT ( 'NONE',  ( 6.041668349913133618, -1.996727924239691587, 0.7141442534656232688 ) ) ;
#21982=CARTESIAN_POINT ( 'NONE',  ( 3.136059509142240742, -1.548504943098116593, -1.711042559064612334 ) ) ;
#21983=CARTESIAN_POINT ( 'NONE',  ( 4.088298575758734898, 1.051444423028622399, -1.656135347060924135 ) ) ;
#21985=CARTESIAN_POINT ( 'NONE',  ( 1.147228161472005681, 1.732707765124143817, -0.9198407203683529598 ) ) ;
#21989=CARTESIAN_POINT ( 'NONE',  ( 6.175017591530616023, 1.752142144017948100, -0.9981200475188132248 ) ) ;
#21993=CARTESIAN_POINT ( 'NONE',  ( 2.606498238493897279, 2.170487999849361138, 0.05724136673956359972 ) ) ;
#21995=CARTESIAN_POINT ( 'NONE',  ( 0.3695850531008069706, -1.794773754367712693, -1.129184308951653781 ) ) ;
#22000=CARTESIAN_POINT ( 'NONE',  ( 0.4388362695032248517, 0.3497011122354178325, 2.030714657000245893 ) ) ;
#22006=CARTESIAN_POINT ( 'NONE',  ( 3.193911838225035105, 1.215006091714765368, 1.476655219734591906 ) ) ;
#22007=( BOUNDED_SURFACE ( )  B_SPLINE_SURFACE ( 3, 3, ( 
 ( #12182, #123902, #43651, #176830, #42588, #140087, #58808, #108693, #59872, #174721 ),
 ( #26294, #175775, #29518, #206112, #28444, #189871, #107626, #94535, #91334, #144378 ),
 ( #92409, #10049, #210377, #158448, #8986, #76124, #93469, #159508, #95611, #73994 ),
 ( #11107, #62019, #77182, #143304, #111902, #157392, #128173, #15370, #115091, #81463 ),
 ( #129243, #149663, #195216, #112966, #212510, #97735, #213562, #180035, #65184, #198384 ),
 ( #50026, #33767, #147541, #67303, #17494, #64151, #148599, #178978, #181088, #130293 ),
 ( #199450, #168, #145444, #47929, #48974, #31657, #14300, #30592, #116149, #196282 ) ),
 .UNSPECIFIED., .T., .F., .T. ) 
 B_SPLINE_SURFACE_WITH_KNOTS ( ( 4, 3, 4 ),
 ( 4, 1, 1, 1, 1, 1, 1, 4 ),
 ( 0.000000000000000000, 0.5000000000000000000, 1.000000000000000000 ),
 ( 0.000000000000000000, 0.09090790722575105287, 0.1825853934691276381, 0.2551728700554835028, 0.3603391217242263855, 0.5205903519787860034, 0.7335386666926504429, 0.9999999999999998890 ),
 .UNSPECIFIED. ) 
 GEOMETRIC_REPRESENTATION_ITEM ( )  RATIONAL_B_SPLINE_SURFACE ( (
 ( 1.000000000000000222, 1.000000000000000222, 1.000000000000000222, 1.000000000000000222, 1.000000000000000222, 1.000000000000000444, 1.000000000000000222, 1.000000000000000222, 1.000000000000000222, 1.000000000000000222),
 ( 0.3333333333333334259, 0.3333333333333334259, 0.3333333333333334259, 0.3333333333333333148, 0.3333333333333334259, 0.3333333333333335369, 0.3333333333333334259, 0.3333333333333334814, 0.3333333333333334259, 0.3333333333333334259),
 ( 0.3333333333333334259, 0.3333333333333334259, 0.3333333333333334259, 0.3333333333333333148, 0.3333333333333334259, 0.3333333333333335369, 0.3333333333333334259, 0.3333333333333334814, 0.3333333333333334259, 0.3333333333333334259),
 ( 1.000000000000000222, 1.000000000000000222, 1.000000000000000222, 1.000000000000000222, 1.000000000000000222, 1.000000000000000444, 1.000000000000000222, 1.000000000000000222, 1.000000000000000222, 1.000000000000000222),
 ( 0.3333333333333334259, 0.3333333333333334259, 0.3333333333333334259, 0.3333333333333333148, 0.3333333333333334259, 0.3333333333333335369, 0.3333333333333334259, 0.3333333333333334814, 0.3333333333333334259, 0.3333333333333334259),
 ( 0.3333333333333334259, 0.3333333333333334259, 0.3333333333333334259, 0.3333333333333333148, 0.3333333333333334259, 0.3333333333333335369, 0.3333333333333334259, 0.3333333333333334814, 0.3333333333333334259, 0.3333333333333334259),
 ( 1.000000000000000222, 1.000000000000000222, 1.000000000000000222, 1.000000000000000222, 1.000000000000000222, 1.000000000000000444, 1.000000000000000222, 1.000000000000000222, 1.000000000000000222, 1.000000000000000222) ) ) 
 REPRESENTATION_ITEM ( '' )  SURFACE ( )  );
#22008=CARTESIAN_POINT ( 'NONE',  ( 5.559369761212399119, 0.3421458929979518948, -1.736264261622854743 ) ) ;
#22011=CARTESIAN_POINT ( 'NONE',  ( 0.5975729546051986585, 1.217269667385068477, 1.341803709015822132 ) ) ;
#22013=CARTESIAN_POINT ( 'NONE',  ( 0.7959256443332961561, -0.8641892358523853845, -1.709830222631677943 ) ) ;
#22014=CARTESIAN_POINT ( 'NONE',  ( 2.295452831283749440, -1.850383948470477602, 0.9288054807428181014 ) ) ;
#22016=CARTESIAN_POINT ( 'NONE',  ( 6.561405567229332547, 0.3174558530528898692, -1.843364171016811603 ) ) ;
#22017=CARTESIAN_POINT ( 'NONE',  ( 3.053144290054691901, -1.492835736363471888, -1.050712463094093385 ) ) ;
#22018=CARTESIAN_POINT ( 'NONE',  ( 0.1886478520232073020, -1.081937125009281964, 2.038365869624358506 ) ) ;
#22021=CARTESIAN_POINT ( 'NONE',  ( 4.615719743604500103, 0.4549637584481819319, -2.011722621177906678 ) ) ;
#22027=CARTESIAN_POINT ( 'NONE',  ( 6.127406499145813257, 0.1562011534181114436, -2.064545280851529885 ) ) ;
#22030=CARTESIAN_POINT ( 'NONE',  ( 3.198656860129048152, -0.6241516536032962748, -2.069545307505623821 ) ) ;
#22031=CARTESIAN_POINT ( 'NONE',  ( 4.160810511097835729, 0.5408905907967902493, 1.945810383981197544 ) ) ;
#22032=CARTESIAN_POINT ( 'NONE',  ( 6.720655732516636505, 1.219515403015670296, 2.385684514189966521 ) ) ;
#22037=CARTESIAN_POINT ( 'NONE',  ( 2.694546298722868549, 1.457235452327232395, -1.394086077981852911 ) ) ;
#22042=CARTESIAN_POINT ( 'NONE',  ( 5.519756697582540284, -0.4584384640409415734, 1.856529252577573397 ) ) ;
#22045=CARTESIAN_POINT ( 'NONE',  ( 4.921500000981174239, -1.427949280599305482, -1.423951169029838315 ) ) ;
#22048=CARTESIAN_POINT ( 'NONE',  ( 6.264645798839446833, -1.215808215430391304, 1.223651055087880080 ) ) ;
#22053=CARTESIAN_POINT ( 'NONE',  ( 5.079306140367803479, 1.745876537259077432, -0.6719496041647440299 ) ) ;
#22054=CARTESIAN_POINT ( 'NONE',  ( 6.152595719530761009, 1.991896818749523845, 0.2912318779872117847 ) ) ;
#22056=CARTESIAN_POINT ( 'NONE',  ( 2.202089267374872872, 0.7962392033929905910, -1.911209141678638090 ) ) ;
#22059=CARTESIAN_POINT ( 'NONE',  ( 1.036732716359071604, -1.587823911754655315, 1.242746109592095527 ) ) ;
#22060=CARTESIAN_POINT ( 'NONE',  ( 0.8612205622890884982, -1.428740940428592898, -1.113706988620609240 ) ) ;
#22066=CARTESIAN_POINT ( 'NONE',  ( 6.573869778094940663, -0.8146055380063941254, 1.732351315116484880 ) ) ;
#22074=CARTESIAN_POINT ( 'NONE',  ( 2.747127081003514881, -1.797865629537301668, 1.199965651887124896 ) ) ;
#22077=CARTESIAN_POINT ( 'NONE',  ( 0.7211286721200690364, 1.601891702520108485, -1.389630591760198541 ) ) ;
#22078=CARTESIAN_POINT ( 'NONE',  ( 5.930640623865814476, 1.760069778787749506, 0.4843501209313359479 ) ) ;
#22079=CARTESIAN_POINT ( 'NONE',  ( 2.442595505675814405, 0.4281495253689853175, 1.924161874619955359 ) ) ;
#22080=CARTESIAN_POINT ( 'NONE',  ( 4.324404969281474109, -0.8226261416362996570, -1.726585468271451651 ) ) ;
#22083=CARTESIAN_POINT ( 'NONE',  ( 4.545333244533083850, 1.760332640988309993, -0.8834868730601146414 ) ) ;
#22084=CARTESIAN_POINT ( 'NONE',  ( 0.04082682177056726897, -1.500436592000290670, -1.232479804542076618 ) ) ;
#22090=CARTESIAN_POINT ( 'NONE',  ( 4.969353466749234727, -1.617520173792227567, -1.019718193788564209 ) ) ;
#22093=CARTESIAN_POINT ( 'NONE',  ( 0.4466624375424713689, 2.201045718399210038, 0.1599725512250807224 ) ) ;
#22095=CARTESIAN_POINT ( 'NONE',  ( 5.848296790250511634, 0.9903421736442417078, -1.752559156024376508 ) ) ;
#22096=CARTESIAN_POINT ( 'NONE',  ( 0.07680821025391608436, 6.948789780205374633, -2.405840108717867132 ) ) ;
#22099=CARTESIAN_POINT ( 'NONE',  ( 3.227070907399377298, -1.911900318415656441, -0.7948586591664740242 ) ) ;
#22103=CARTESIAN_POINT ( 'NONE',  ( 0.6026772488060898603, -0.7295331166810551382, -2.035022307366324945 ) ) ;
#22109=CARTESIAN_POINT ( 'NONE',  ( 6.825078400183550720, 7.629137130509051623, 2.355651831298340326 ) ) ;
#22112=CARTESIAN_POINT ( 'NONE',  ( 4.307042110543488178, 1.062484115506344473, -1.370455642081182646 ) ) ;
#22115=CARTESIAN_POINT ( 'NONE',  ( 3.871986384844767315, -2.040452582458017083, 0.3490408808229996662 ) ) ;
#22116=CARTESIAN_POINT ( 'NONE',  ( 4.517270869736185190, -1.935087425045402654, 0.8595401143802297028 ) ) ;
#22119=CARTESIAN_POINT ( 'NONE',  ( 1.305442304231837714, -1.549127766076626056, -1.215949579239549161 ) ) ;
#22120=CARTESIAN_POINT ( 'NONE',  ( 0.4570967503451648373, -1.639016809899789040, 0.9851245988263114262 ) ) ;
#22121=CARTESIAN_POINT ( 'NONE',  ( 5.261813964552005451, 1.126222290254262015, 1.996463630829442337 ) ) ;
#22122=CARTESIAN_POINT ( 'NONE',  ( 1.822601884235462766, 1.703052241681313861, 0.6583118566880485911 ) ) ;
#22126=CARTESIAN_POINT ( 'NONE',  ( 3.164317521226766239, 2.013376229028215558, -0.004237188189804701709 ) ) ;
#22127=CARTESIAN_POINT ( 'NONE',  ( 3.186327686730246800, 1.093712407854827706, -1.628379936052851917 ) ) ;
#22130=CARTESIAN_POINT ( 'NONE',  ( 0.1753634416057740786, 1.334841368177059895, -2.397339160348281428 ) ) ;
#22131=CARTESIAN_POINT ( 'NONE',  ( 5.789036971029382528, 1.582348866732422810, 1.366464223246833809 ) ) ;
#22132=CARTESIAN_POINT ( 'NONE',  ( 4.381574371570028603, 1.156860168461280036, 1.339510341777202074 ) ) ;
#22134=CARTESIAN_POINT ( 'NONE',  ( 0.3225714733509216781, 2.098294765757203528, 0.6321472216322538973 ) ) ;
#22135=CARTESIAN_POINT ( 'NONE',  ( 0.2216635874392547945, 1.664573546290064598, 0.5083179512348577900 ) ) ;
#22138=CARTESIAN_POINT ( 'NONE',  ( 5.731119460814408484, 2.295830932937119595, 0.1164615576392889484 ) ) ;
#22140=CARTESIAN_POINT ( 'NONE',  ( 6.468101748929986350, 1.443884034049055298, 0.9595089302780019924 ) ) ;
#22141=CARTESIAN_POINT ( 'NONE',  ( 1.823171247573553311, 2.059948494222668014, 0.7922594597074559264 ) ) ;
#22142=CARTESIAN_POINT ( 'NONE',  ( 0.5851434883720012525, 2.077150299251043553, 0.6315224188822368134 ) ) ;
#22144=CARTESIAN_POINT ( 'NONE',  ( 1.130240340503264829, 2.115179321838219551, 0.09787962981822571906 ) ) ;
#22145=CARTESIAN_POINT ( 'NONE',  ( 4.156250000000002665, -1.895863743163992199, 0.7852924748302037017 ) ) ;
#22147=CARTESIAN_POINT ( 'NONE',  ( 4.752910067621118451, -1.547527511699481106, 1.147055677608086466 ) ) ;
#22149=CARTESIAN_POINT ( 'NONE',  ( 1.874976642369927005, -0.1173453557595251634, -2.289501271392534676 ) ) ;
#22153=CARTESIAN_POINT ( 'NONE',  ( 3.791809789012908549, 2.091298394358314550, -0.7490737107957652352 ) ) ;
#22161=CARTESIAN_POINT ( 'NONE',  ( 1.723279953462612202, 1.994870059565261755, 0.2930690452552578429 ) ) ;
#22163=CARTESIAN_POINT ( 'NONE',  ( 6.777782349474076540, -2.001779569883685106, 0.4972090909861492936 ) ) ;
#22167=CARTESIAN_POINT ( 'NONE',  ( 6.515217664332146441, -1.685650512211306129, 0.4329046258050253670 ) ) ;
#22170=CARTESIAN_POINT ( 'NONE',  ( 1.405125766016354305, -0.4367768486257683769, 1.714848201936822525 ) ) ;
#22171=CARTESIAN_POINT ( 'NONE',  ( 0.2994542103806375200, 1.388483683912977495, -1.462447666687356485 ) ) ;
#22172=CARTESIAN_POINT ( 'NONE',  ( 6.550362485727940332, -1.338708790221679656, 1.112040286498132025 ) ) ;
#22173=CARTESIAN_POINT ( 'NONE',  ( 4.634495141935854434, 0.3908333592176889137, 2.258673302944668837 ) ) ;
#22174=CARTESIAN_POINT ( 'NONE',  ( 3.450948914068392881, 0.4461466885457600062, -1.786139022923169506 ) ) ;
#22178=CARTESIAN_POINT ( 'NONE',  ( 4.032112419961201510, 0.9767663869549062516, -1.542106374223570775 ) ) ;
#22179=CARTESIAN_POINT ( 'NONE',  ( 5.414685466650038137, -1.281359335986744341, -1.556910257834144051 ) ) ;
#22181=CARTESIAN_POINT ( 'NONE',  ( 3.819400769403025198, -0.1694044215128273911, 2.256236840065691585 ) ) ;
#22183=CARTESIAN_POINT ( 'NONE',  ( 0.2058769709349675681, -0.5595275159893696726, 2.030311192619388638 ) ) ;
#22186=CARTESIAN_POINT ( 'NONE',  ( 4.018080225218490398, 2.055083638104511223, -0.2504045000601487492 ) ) ;
#22189=CARTESIAN_POINT ( 'NONE',  ( 5.531924462405465981, -2.068776410037334479, 0.4646945096876684556 ) ) ;
#22192=CARTESIAN_POINT ( 'NONE',  ( 2.156748612084181005, -1.489394325481137260, 1.221923121036755600 ) ) ;
#22195=CARTESIAN_POINT ( 'NONE',  ( 0.1859136753566691391, -1.208741973239912726, -1.555490313720475415 ) ) ;
#22200=CARTESIAN_POINT ( 'NONE',  ( 0.2291713999985908190, 1.525799623841477493, -1.614749986458098974 ) ) ;
#22201=CARTESIAN_POINT ( 'NONE',  ( 3.909285118862667829, 1.805215983022747439, 1.084321332058492571 ) ) ;
#22204=CARTESIAN_POINT ( 'NONE',  ( 0.2032580500000652490, -1.434579632348313982, -1.185340245312079377 ) ) ;
#22209=CARTESIAN_POINT ( 'NONE',  ( 1.635180430577408028, 1.980530345366804834, 0.7584260845197098311 ) ) ;
#22212=CARTESIAN_POINT ( 'NONE',  ( 3.279693232472491893, -1.891448704997201302, 0.5207070127687256633 ) ) ;
#22213=CARTESIAN_POINT ( 'NONE',  ( 2.254944280175336324, -1.671361177491991201, 1.370965666894090385 ) ) ;
#22214=CARTESIAN_POINT ( 'NONE',  ( 2.173174093899932657, 1.133995793187540180, 1.450494936146892622 ) ) ;
#22217=CARTESIAN_POINT ( 'NONE',  ( 3.749730547248275148, 0.6284987560769598192, 1.623061768561576468 ) ) ;
#22220=CARTESIAN_POINT ( 'NONE',  ( 0.9542513359644848592, 2.159166806557303531, -0.1069676271590186134 ) ) ;
#22221=CARTESIAN_POINT ( 'NONE',  ( 2.970077202574809228, 1.701686883299750264, 1.080900613174784475 ) ) ;
#22223=CARTESIAN_POINT ( 'NONE',  ( 0.3038912542124502236, -0.5749842496362895794, 2.083749421223294540 ) ) ;
#22224=CARTESIAN_POINT ( 'NONE',  ( 2.272288244244465627, -1.214158342444570327, 1.553133305774859974 ) ) ;
#22226=CARTESIAN_POINT ( 'NONE',  ( 6.509000000000014552, 2.444259026362519904, 2.383015625331697862 ) ) ;
#22227=CARTESIAN_POINT ( 'NONE',  ( 2.683070245604711523, 1.375115853580029635, 1.371619177916082011 ) ) ;
#22233=CARTESIAN_POINT ( 'NONE',  ( -0.2106854629475244378, -0.004120941679102134263, -1.996958217618934661 ) ) ;
#22240=CARTESIAN_POINT ( 'NONE',  ( 6.756845507909216231, -1.789895876690169585, 1.456048205946461005 ) ) ;
#22242=CARTESIAN_POINT ( 'NONE',  ( 3.942202469084721272, -0.9707516781715104237, 1.704694321266352786 ) ) ;
#22244=CARTESIAN_POINT ( 'NONE',  ( 1.565077508395201988, -1.076315722900993643, 1.704939445326451475 ) ) ;
#22246=CARTESIAN_POINT ( 'NONE',  ( 2.677094534585529928, 1.813448998079300489, -1.092781719356890946 ) ) ;
#22250=CARTESIAN_POINT ( 'NONE',  ( 2.782953997937851920, 1.302219384484751830, 1.301801165952347628 ) ) ;
#22254=CARTESIAN_POINT ( 'NONE',  ( 3.691739789689612472, 1.995538565534977549, -0.7177698711837015022 ) ) ;
#22255=CARTESIAN_POINT ( 'NONE',  ( 0.2691533882960769897, 1.057504993221158873, 1.506941669042777265 ) ) ;
#22258=CARTESIAN_POINT ( 'NONE',  ( 4.288392841435205938, -2.037809284099707074, -0.3060936983758227870 ) ) ;
#22261=CARTESIAN_POINT ( 'NONE',  ( 1.276629239279066574, 1.701104413791530767, -0.7050613402737049284 ) ) ;
#22265=CARTESIAN_POINT ( 'NONE',  ( 0.8212658843103730621, 2.040464674744349338, 0.8412164853940640175 ) ) ;
#22266=CARTESIAN_POINT ( 'NONE',  ( 4.218261219551087571, -1.158436920226207034, -1.943184041606202950 ) ) ;
#22268=CARTESIAN_POINT ( 'NONE',  ( 4.060681591697304249, 0.4892206165460743494, 1.744179128828279302 ) ) ;
#22269=CARTESIAN_POINT ( 'NONE',  ( 3.819475811356612738, -1.325201190313522792, -1.383632964731799531 ) ) ;
#22270=CARTESIAN_POINT ( 'NONE',  ( 5.635237798060349412, -0.04710594754482424346, -2.069988403558701062 ) ) ;
#22272=CARTESIAN_POINT ( 'NONE',  ( 3.590661340855735961, -0.3832702008734929500, -1.933690442540521470 ) ) ;
#22273=CARTESIAN_POINT ( 'NONE',  ( 1.430555067506549483, 1.855864167146383581, 0.5162276523679990570 ) ) ;
#22274=CARTESIAN_POINT ( 'NONE',  ( 3.572993900519233712, 0.04689164532409998559, -1.870237235490713079 ) ) ;
#22275=CARTESIAN_POINT ( 'NONE',  ( 3.000898454221593958, -0.6702494718498009929, -2.208213912191819617 ) ) ;
#22276=CARTESIAN_POINT ( 'NONE',  ( 3.472968545230222581, 1.681562272349636622, 0.7977436208898255332 ) ) ;
#22279=CARTESIAN_POINT ( 'NONE',  ( 1.998786363724443182, -0.5629491194198692483, -2.029361489363819882 ) ) ;
#22283=CARTESIAN_POINT ( 'NONE',  ( 3.340189922722580196, -1.266226476691566738, -1.700888996046201029 ) ) ;
#22285=CARTESIAN_POINT ( 'NONE',  ( 0.8264327134144221487, -0.9118592345104499231, -1.802339519251413780 ) ) ;
#22290=CARTESIAN_POINT ( 'NONE',  ( 0.7730135719010817752, -2.035059957909639561, -0.7290066412228360937 ) ) ;
#22293=CARTESIAN_POINT ( 'NONE',  ( 6.825078400183550720, 7.629137130509051623, 2.555651831298339616 ) ) ;
#22296=CARTESIAN_POINT ( 'NONE',  ( 5.981657729715996297, -0.6748525008196132324, 1.900413905137773529 ) ) ;
#22299=CARTESIAN_POINT ( 'NONE',  ( -0.02351032182101517320, -2.127384168920816165, -0.5261613093957145937 ) ) ;
#22302=CARTESIAN_POINT ( 'NONE',  ( 0.7962373781299083575, -0.8115885651059464578, 2.112105989495225877 ) ) ;
#22306=CARTESIAN_POINT ( 'NONE',  ( 0.8959254483255777446, -0.8623397379431455567, -1.710623486014851480 ) ) ;
#22310=CARTESIAN_POINT ( 'NONE',  ( 3.158550911874979938, -1.305529951647845355, 1.127390448682374924 ) ) ;
#22312=CARTESIAN_POINT ( 'NONE',  ( 2.020411781336392210, 1.649200945362235826, 0.6424177339450982682 ) ) ;
#22313=CARTESIAN_POINT ( 'NONE',  ( 2.543610208494262892, -1.877569574052952328, 0.7265587727790027150 ) ) ;
#22315=CARTESIAN_POINT ( 'NONE',  ( 5.139771110516938357, -1.557344429106276573, -1.563758303505815572 ) ) ;
#22317=CARTESIAN_POINT ( 'NONE',  ( 4.359631895039292715, -1.563893385546542003, -1.278231166955777764 ) ) ;
#22319=CARTESIAN_POINT ( 'NONE',  ( 4.196021508500130004, 1.385991406618786836, 1.604897850144955340 ) ) ;
#22320=CARTESIAN_POINT ( 'NONE',  ( 4.218375177057286152, 1.978055892313890229, 0.3905773888849966013 ) ) ;
#22321=CARTESIAN_POINT ( 'NONE',  ( 4.447391390197759975, -1.653601938829275975, 0.7403539279892316083 ) ) ;
#22325=CARTESIAN_POINT ( 'NONE',  ( 0.8834254411415434216, 1.253375741028007084, 1.388844808110502038 ) ) ;
#22327=CARTESIAN_POINT ( 'NONE',  ( 6.692070433991195166, -0.7751425012093198230, 1.651373049820707317 ) ) ;
#22328=CARTESIAN_POINT ( 'NONE',  ( -0.1583346312582509796, -1.114004300041637974, -1.428896152673633013 ) ) ;
#22334=CARTESIAN_POINT ( 'NONE',  ( 0.4219365929402639215, -1.902980170924161385, 0.1897552588234762416 ) ) ;
#22339=CARTESIAN_POINT ( 'NONE',  ( 4.711248855110969913, 1.761570823303935551, -1.180294879073326308 ) ) ;
#22340=CARTESIAN_POINT ( 'NONE',  ( -0.1294898018152200736, 7.629137130509059617, -2.526516153123930852 ) ) ;
#22343=CARTESIAN_POINT ( 'NONE',  ( 5.887953105907347329, -0.8888255776743571035, 1.759709591642463433 ) ) ;
#22346=CARTESIAN_POINT ( 'NONE',  ( 0.6154903249990024694, 1.648289601840571938, 1.155678142064648917 ) ) ;
#22348=CARTESIAN_POINT ( 'NONE',  ( 6.315624676198635434, -1.384492656466195681, -1.602007840318976584 ) ) ;
#22350=CARTESIAN_POINT ( 'NONE',  ( 2.031770498437397876, 1.981864486777328294, -0.5989037013024376410 ) ) ;
#22355=CARTESIAN_POINT ( 'NONE',  ( 4.470703160837229184, 0.0002547659985942945528, -2.090823719324691687 ) ) ;
#22357=CARTESIAN_POINT ( 'NONE',  ( 3.645350208285046634, -1.381898811119431691, -1.193016960613018096 ) ) ;
#22358=CARTESIAN_POINT ( 'NONE',  ( 1.699580558467077118, 1.249458034614457702, 1.311817296177042902 ) ) ;
#22360=CARTESIAN_POINT ( 'NONE',  ( 6.727182134110200273, -0.004969159814478123736, 2.189081792362323586 ) ) ;
#22362=CARTESIAN_POINT ( 'NONE',  ( 3.733602637680955905, -2.039903990487581087, 0.8422819887162477093 ) ) ;
#22365=CARTESIAN_POINT ( 'NONE',  ( 2.684119430630255820, 1.024705199231435993, 1.614373862881289590 ) ) ;
#22367=CARTESIAN_POINT ( 'NONE',  ( 6.197728532230423859, -1.496850047335227085, -1.430563974149069661 ) ) ;
#22370=CARTESIAN_POINT ( 'NONE',  ( 5.636325218313963603, 0.4264374063192889475, 2.149501299143250055 ) ) ;
#22377=CARTESIAN_POINT ( 'NONE',  ( 4.112460492241882370, 1.324567223757302514, -1.321038939096484066 ) ) ;
#22383=CARTESIAN_POINT ( 'NONE',  ( 0.2507523796677147421, -0.4231762011769435450, -1.930160340004604569 ) ) ;
#22385=CARTESIAN_POINT ( 'NONE',  ( 0.6500178175347063325, 0.9963223104369984817, 1.753020061881370051 ) ) ;
#22388=CARTESIAN_POINT ( 'NONE',  ( 1.254151665356119549, 0.8908215700371600043, 2.002402562943622844 ) ) ;
#22389=CARTESIAN_POINT ( 'NONE',  ( 4.652862234063231739, -1.464609733205827879, 1.089778014065109657 ) ) ;
#22399=CARTESIAN_POINT ( 'NONE',  ( 3.245484093776138668, 1.841430844176932480, -0.003062914905635482320 ) ) ;
#22400=CARTESIAN_POINT ( 'NONE',  ( 0.04752084976851479736, -1.839644132637440865, 0.8178810061007844023 ) ) ;
#22401=CARTESIAN_POINT ( 'NONE',  ( 1.634533438177967923, 0.1689203749893586071, -2.292248917674902575 ) ) ;
#22403=CARTESIAN_POINT ( 'NONE',  ( 0.2857036466711966316, -1.138303949996006148, -1.472634861895638636 ) ) ;
#22406=CARTESIAN_POINT ( 'NONE',  ( 3.199369407753744454, 1.726971514772487559, -0.8218122705464236954 ) ) ;
#22410=CARTESIAN_POINT ( 'NONE',  ( 2.683241491500857556, 1.480437668936212869, 1.476589516890645104 ) ) ;
#22411=CARTESIAN_POINT ( 'NONE',  ( 1.375632740723360836, 1.111493989511678881, 1.504490780774490499 ) ) ;
#22412=CARTESIAN_POINT ( 'NONE',  ( 2.477888549845189470, 1.799646572043178683, 0.9090068759892779848 ) ) ;
#22415=CARTESIAN_POINT ( 'NONE',  ( 3.509068237933731016, -1.713987098263862086, 0.3013083454645076875 ) ) ;
#22418=CARTESIAN_POINT ( 'NONE',  ( 3.861678741103656165, 1.711552447172806968, -0.2133835738165473228 ) ) ;
#22419=CARTESIAN_POINT ( 'NONE',  ( 3.948915171154475878, -1.822730400009948237, -1.216494452853926322 ) ) ;
#22420=CARTESIAN_POINT ( 'NONE',  ( 4.705825944637973990, -0.5905853116198942487, 2.126329296355852883 ) ) ;
#22422=CARTESIAN_POINT ( 'NONE',  ( 4.135715461124009451, 2.046248213957535089, -0.7259774245699932571 ) ) ;
#22423=CARTESIAN_POINT ( 'NONE',  ( 2.648829494986388422, -1.517897411861212076, 1.014145048410304284 ) ) ;
#22425=CARTESIAN_POINT ( 'NONE',  ( 4.645784029343587918, 2.093824292288968270, -0.3141051717527267861 ) ) ;
#22426=CARTESIAN_POINT ( 'NONE',  ( 6.639320575229255006, 4.696066290934245657, 2.559399261709224049 ) ) ;
#22428=CARTESIAN_POINT ( 'NONE',  ( 4.669621734427405357, 1.318897967798425608, 1.874777261101326920 ) ) ;
#22430=CARTESIAN_POINT ( 'NONE',  ( 6.720655732516647163, 0.6055996050860124047, 1.780393570709505546 ) ) ;
#22432=CARTESIAN_POINT ( 'NONE',  ( 0.7684181764250408442, 2.117871390293009526, -0.1079879263860619443 ) ) ;
#22436=CARTESIAN_POINT ( 'NONE',  ( 6.883263157960404222, 3.695221384915627905, 2.468000959490519897 ) ) ;
#22438=CARTESIAN_POINT ( 'NONE',  ( 5.748672702226536479, 1.986101125435947301, -0.3474646712962395911 ) ) ;
#22440=CARTESIAN_POINT ( 'NONE',  ( 3.625881544801349055, 2.013384979781565942, -0.4471371585693607598 ) ) ;
#22442=CARTESIAN_POINT ( 'NONE',  ( -0.1408020194049912077, 0.6951682901239358836, -2.180991432481160341 ) ) ;
#22446=CARTESIAN_POINT ( 'NONE',  ( 5.753911783233988331, 0.8852683131516884130, 2.004867968450708915 ) ) ;
#22447=CARTESIAN_POINT ( 'NONE',  ( 3.867814693791224112, -0.2004342644464084944, -2.006446243107910199 ) ) ;
#22448=CARTESIAN_POINT ( 'NONE',  ( 3.473999211503727036, -1.775402473473717935, -0.4878004006634574230 ) ) ;
#22452=CARTESIAN_POINT ( 'NONE',  ( 0.1996746939399509924, -1.724222465425511386, -0.05034706749046553159 ) ) ;
#22454=CARTESIAN_POINT ( 'NONE',  ( 1.407308937662318460, -1.282028150163934122, -1.907831638372993410 ) ) ;
#22456=CARTESIAN_POINT ( 'NONE',  ( 0.2810632938833834693, -2.195003449849114663, -0.5476492663787374537 ) ) ;
#22457=CARTESIAN_POINT ( 'NONE',  ( 2.684315897010148610, -1.081986827455215572, 1.806733699029156259 ) ) ;
#22466=CARTESIAN_POINT ( 'NONE',  ( 2.373420902723611725, -1.847293605357634982, -1.041186957106011723 ) ) ;
#22467=CARTESIAN_POINT ( 'NONE',  ( 3.990652734535464319, -1.277060150153148221, 1.817470393784472948 ) ) ;
#22468=CARTESIAN_POINT ( 'NONE',  ( 2.572451567087580493, -2.097416440861415321, -0.6350555677336400251 ) ) ;
#22471=CARTESIAN_POINT ( 'NONE',  ( 5.107842384611220865, 0.6171798735227496113, -1.862306164846748491 ) ) ;
#22476=CARTESIAN_POINT ( 'NONE',  ( 4.500305224345508393, -0.9970752094022590217, 1.871535012320741265 ) ) ;
#22479=CARTESIAN_POINT ( 'NONE',  ( 5.805597153138060129, -0.5296426447994294628, 2.095691122003799478 ) ) ;
#22481=CARTESIAN_POINT ( 'NONE',  ( 4.810013364240863787, 1.265987717737980134, -1.337210144835267345 ) ) ;
#22484=CARTESIAN_POINT ( 'NONE',  ( 0.1162408695623952659, -0.08860816971513819917, 1.738289989025374016 ) ) ;
#22485=CARTESIAN_POINT ( 'NONE',  ( 6.727182134110243794, 2.977085856046020051, 2.364561739503980853 ) ) ;
#22488=CARTESIAN_POINT ( 'NONE',  ( 3.766626874709140704, -1.453462046928340579, 1.600284095077113333 ) ) ;
#22491=CARTESIAN_POINT ( 'NONE',  ( 3.116266767097406909, -1.064116542966097922, -1.881565754655416756 ) ) ;
#22492=CARTESIAN_POINT ( 'NONE',  ( 4.710209360279286273, -0.8403073340159574744, -1.783404427212876842 ) ) ;
#22493=CARTESIAN_POINT ( 'NONE',  ( 4.340949964944015527, -0.9985633389030469376, 1.417159075928013046 ) ) ;
#22495=CARTESIAN_POINT ( 'NONE',  ( 1.171705676731093604, 1.309414992938146893, 1.757219779060022580 ) ) ;
#22496=CARTESIAN_POINT ( 'NONE',  ( 1.501454852758288494, 1.885366349659310048, -1.330307493247370410 ) ) ;
#22497=CARTESIAN_POINT ( 'NONE',  ( 4.007146649590315413, 1.765602988722612565, 1.062546815679512369 ) ) ;
#22498=CARTESIAN_POINT ( 'NONE',  ( 6.022988683830415191, -1.827201308531730017, 0.6583088893449047241 ) ) ;
#22505=ORIENTED_EDGE ( 'NONE', *, *, #49103, .F. ) ;
#22507=CARTESIAN_POINT ( 'NONE',  ( 3.364504783244476993, 0.9904720576699842516, 1.972067388187691339 ) ) ;
#22510=CARTESIAN_POINT ( 'NONE',  ( 0.6196752394443981737, 1.841814893205738102, -0.2651871859581377833 ) ) ;
#22511=CARTESIAN_POINT ( 'NONE',  ( -0.1290005225502433017, 7.629137130509076492, -2.773995091683974401 ) ) ;
#22514=CARTESIAN_POINT ( 'NONE',  ( 6.825078400183554272, 2.951006455646578264, 2.596623860847916188 ) ) ;
#22515=CARTESIAN_POINT ( 'NONE',  ( 6.333933918656591722, 1.821832875601756774, 0.2651207078676054429 ) ) ;
#22517=CARTESIAN_POINT ( 'NONE',  ( 2.430605206563386300, 1.998658846558550195, 0.5020661504441750189 ) ) ;
#22524=CARTESIAN_POINT ( 'NONE',  ( 0.8485939591743509869, 0.5976917523492016882, 1.972322469454860672 ) ) ;
#22531=CARTESIAN_POINT ( 'NONE',  ( 6.094375512030342001, -2.195847865938059140, -0.2203403561373064590 ) ) ;
#22532=CARTESIAN_POINT ( 'NONE',  ( 6.907534427287327361, -0.5096537312613695914, 2.212693016512882416 ) ) ;
#22534=CARTESIAN_POINT ( 'NONE',  ( 0.5098338327763075606, -0.6861045072398126443, 1.785269576063217567 ) ) ;
#22535=CARTESIAN_POINT ( 'NONE',  ( 0.7082206942033396624, 1.197301205363930254, -1.622488844446705381 ) ) ;
#22542=CARTESIAN_POINT ( 'NONE',  ( 1.445950363956361340, 1.868363765441739099, 0.09516058986362013750 ) ) ;
#22544=CARTESIAN_POINT ( 'NONE',  ( 2.800017839408690090, -0.9981255096969069429, -1.752139039461996006 ) ) ;
#22548=CARTESIAN_POINT ( 'NONE',  ( 5.356126594405285601, 2.103725632816171309, -0.1020696835895683885 ) ) ;
#22553=CARTESIAN_POINT ( 'NONE',  ( 4.359631895039292715, -1.563893385546542003, -1.278231166955777764 ) ) ;
#22556=CARTESIAN_POINT ( 'NONE',  ( 5.951645758832087907, 1.559603009536973284, 1.349993227703372156 ) ) ;
#22558=CARTESIAN_POINT ( 'NONE',  ( 6.063787883973515314, 2.130759124531961923, -0.3628933549372145295 ) ) ;
#22564=CARTESIAN_POINT ( 'NONE',  ( 1.592468369012179918, 1.070935286220242366, -1.888628467986789738 ) ) ;
#22567=CARTESIAN_POINT ( 'NONE',  ( 2.208333698829296310, 1.645431377724184463, 0.8263914577605266931 ) ) ;
#22569=CARTESIAN_POINT ( 'NONE',  ( 2.859115728684503477, 0.3189004193784421015, -2.168101852914063876 ) ) ;
#22570=CARTESIAN_POINT ( 'NONE',  ( 6.983263157960362122, 2.430545403621493072, 2.435370848939223620 ) ) ;
#22571=CARTESIAN_POINT ( 'NONE',  ( 3.520660345214459586, 1.437014610000959314, -1.747548891452437081 ) ) ;
#22577=CARTESIAN_POINT ( 'NONE',  ( 5.378098658424382172, -0.9825891054615911724, 1.471664417823245197 ) ) ;
#22579=CARTESIAN_POINT ( 'NONE',  ( 1.501149451381103672, 1.721883814275385616, -1.212229816669802895 ) ) ;
#22582=CARTESIAN_POINT ( 'NONE',  ( 1.398812336859527550, 0.3809602064741451355, 1.932172009363951837 ) ) ;
#22585=CARTESIAN_POINT ( 'NONE',  ( 6.310821775929002619, -0.4926439853468951857, -1.743236492463080767 ) ) ;
#22589=CARTESIAN_POINT ( 'NONE',  ( 4.469519713540137218, 1.814478506493341969, -0.4545110902946307152 ) ) ;
#22592=CARTESIAN_POINT ( 'NONE',  ( 5.805552407531882508, -1.628464769346991581, -1.278160613847306504 ) ) ;
#22595=CARTESIAN_POINT ( 'NONE',  ( 0.1509401653462701109, -0.4529219869476922011, -2.027634260368789576 ) ) ;
#22602=CARTESIAN_POINT ( 'NONE',  ( 4.598074495912658044, 0.8407358649686399454, -1.772743347989129692 ) ) ;
#22604=CARTESIAN_POINT ( 'NONE',  ( 2.196638537759632470, -1.314794530490107638, -1.528507974810841219 ) ) ;
#22606=CARTESIAN_POINT ( 'NONE',  ( 0.3631484714031462668, 0.2087870660046411420, -2.181583536649676525 ) ) ;
#22608=CARTESIAN_POINT ( 'NONE',  ( 2.073319367481298858, 1.791407343212477077, -0.5384048943791116537 ) ) ;
#22610=CARTESIAN_POINT ( 'NONE',  ( 3.691655806294301900, 1.894216563707728396, -0.6821535943304660732 ) ) ;
#22613=CARTESIAN_POINT ( 'NONE',  ( 3.286815299386883549, 1.667571603535710434, -1.304429798788673267 ) ) ;
#22615=CARTESIAN_POINT ( 'NONE',  ( 6.426242046702522082, 1.060841730010402495, 1.777776562702712226 ) ) ;
#22616=CARTESIAN_POINT ( 'NONE',  ( 0.7321124197560413549, 2.060462595713075995, 0.3535659584654736731 ) ) ;
#22617=CARTESIAN_POINT ( 'NONE',  ( 6.720655732516626735, 6.034942950145537388, 2.668627893128409756 ) ) ;
#22618=CARTESIAN_POINT ( 'NONE',  ( 6.739283625173963621, -1.628968703954777553, 0.8242606506234579911 ) ) ;
#22619=ORIENTED_EDGE ( 'NONE', *, *, #182631, .T. ) ;
#22625=CARTESIAN_POINT ( 'NONE',  ( 6.410809557875646547, -0.5148348048229570706, -1.841598127471068658 ) ) ;
#22633=CARTESIAN_POINT ( 'NONE',  ( 5.554314605481814660, -1.277030258849481736, 1.560512323070535112 ) ) ;
#22634=CARTESIAN_POINT ( 'NONE',  ( 0.6453774867190856801, 0.1600191834128759094, 2.114519675249281416 ) ) ;
#22641=CARTESIAN_POINT ( 'NONE',  ( 3.819166351039466001, -1.734870831597424612, -0.9322225710242746377 ) ) ;
#22642=CARTESIAN_POINT ( 'NONE',  ( 4.956657736208940790, -1.899625167328807374, -0.6766988040120130998 ) ) ;
#22645=CARTESIAN_POINT ( 'NONE',  ( 4.699289266375740404, -0.5861454505808120219, 2.111544493182772708 ) ) ;
#22646=CARTESIAN_POINT ( 'NONE',  ( 2.889578633693023590, 1.361086032938205070, 1.363490106525049317 ) ) ;
#22648=CARTESIAN_POINT ( 'NONE',  ( -0.02988540731096045455, 2.895077309840556445, -2.215427197800499570 ) ) ;
#22654=CARTESIAN_POINT ( 'NONE',  ( 5.225436369306192930, 0.1968503305618974075, -1.959608170402066696 ) ) ;
#22655=CARTESIAN_POINT ( 'NONE',  ( 0.2220789341932476180, 1.858810982918417620, 0.5625763381651854855 ) ) ;
#22656=CARTESIAN_POINT ( 'NONE',  ( 3.633450831153079541, -0.1460068579729571769, 2.007839618615501642 ) ) ;
#22657=CARTESIAN_POINT ( 'NONE',  ( 5.343244854357415363, -1.283103863925443955, 1.906741504182138502 ) ) ;
#22659=CARTESIAN_POINT ( 'NONE',  ( 3.748742453178009360, -0.3589989779783793744, -1.825800159725386118 ) ) ;
#22662=CARTESIAN_POINT ( 'NONE',  ( 6.363533315466952445, -1.540175188624912650, -1.133462061071670579 ) ) ;
#22665=CARTESIAN_POINT ( 'NONE',  ( 5.618719695961268634, -0.05021595884377753893, 2.090305304898040006 ) ) ;
#22669=CARTESIAN_POINT ( 'NONE',  ( 0.7326872660318053398, 0.1314506862302306234, 1.821024990000128518 ) ) ;
#22671=CARTESIAN_POINT ( 'NONE',  ( 3.058897358425614055, -1.030606816589432873, 1.394497854932384762 ) ) ;
#22676=CARTESIAN_POINT ( 'NONE',  ( 6.983263157960363010, -0.009046620988246899253, 2.153544821522495489 ) ) ;
#22677=CARTESIAN_POINT ( 'NONE',  ( 5.479063914364931343, -0.04889757770590653918, -1.825204647902956889 ) ) ;
#22678=CARTESIAN_POINT ( 'NONE',  ( 3.080854412065773928, 1.845568107317007822, 0.6654098317215583203 ) ) ;
#22682=CARTESIAN_POINT ( 'NONE',  ( 3.949941927655271190, -1.463281269271698770, -1.534908012577620440 ) ) ;
#22685=CARTESIAN_POINT ( 'NONE',  ( 2.342711862795249012, -2.029470198211943632, -0.4080651701656515251 ) ) ;
#22687=CARTESIAN_POINT ( 'NONE',  ( 4.108218931252209494, -0.8498058027226679245, 2.052504409502105442 ) ) ;
#22689=CARTESIAN_POINT ( 'NONE',  ( 2.180727191476996563, 1.779927251244978192, 1.454631630963822309 ) ) ;
#22691=CARTESIAN_POINT ( 'NONE',  ( 0.4440980561614649158, -0.9299495107331550159, 1.727370323332158897 ) ) ;
#22695=CARTESIAN_POINT ( 'NONE',  ( 6.497600353373155002, -1.840680978339729545, 0.05264081064878384231 ) ) ;
#22699=CARTESIAN_POINT ( 'NONE',  ( 3.181800181368432678, 1.864768544494728175, -0.4233684943922080834 ) ) ;
#22700=CARTESIAN_POINT ( 'NONE',  ( -0.1106727585415863135, 6.947232144882324434, -2.598525652753637782 ) ) ;
#22701=CARTESIAN_POINT ( 'NONE',  ( 3.574969364760666846, 0.04275877055364904478, -1.724416222950067690 ) ) ;
#22702=CARTESIAN_POINT ( 'NONE',  ( 2.712125330650519750, 1.116209241849321465, -1.679223868463100233 ) ) ;
#22703=CARTESIAN_POINT ( 'NONE',  ( 3.797728626882245884, 1.624942816722572125, -1.626123495085467496 ) ) ;
#22704=CARTESIAN_POINT ( 'NONE',  ( 3.515140014801207524, 2.043520737213794458, 0.9711500472536734874 ) ) ;
#22705=CARTESIAN_POINT ( 'NONE',  ( 6.059223728125719965, -1.805531155315470926, -1.083989359861557533 ) ) ;
#22708=CARTESIAN_POINT ( 'NONE',  ( 4.938602502702000407, 0.3022688342860947452, 1.743538433004296673 ) ) ;
#22710=CARTESIAN_POINT ( 'NONE',  ( 0.6918693526153978368, -0.8198495674218098106, 2.140808456117601732 ) ) ;
#22712=CARTESIAN_POINT ( 'NONE',  ( 6.122987604524110949, -1.732013368603693593, 0.6248225064409973495 ) ) ;
#22714=CARTESIAN_POINT ( 'NONE',  ( 5.472676780243426187, -0.05103125619924236966, -2.191024458042860168 ) ) ;
#22718=CARTESIAN_POINT ( 'NONE',  ( 6.250451049865752395, -2.060019788584551481, -0.2068627631737207651 ) ) ;
#22719=CARTESIAN_POINT ( 'NONE',  ( 0.3566581422463632189, -1.900417414521380133, -0.6748426577906708745 ) ) ;
#22721=CARTESIAN_POINT ( 'NONE',  ( 3.932187577746598883, 1.029727551008235320, -1.628035494724868970 ) ) ;
#22723=CARTESIAN_POINT ( 'NONE',  ( 0.8443251495477720470, -1.414827328263716266, -1.712562173056450643 ) ) ;
#22731=CARTESIAN_POINT ( 'NONE',  ( 2.558977423257744022, 1.577441344615847951, -1.166261179026031547 ) ) ;
#22735=CARTESIAN_POINT ( 'NONE',  ( 6.549272904993657995, 1.707534169505098953, -0.9658701945045378157 ) ) ;
#22738=CARTESIAN_POINT ( 'NONE',  ( 0.3919815047150644327, 1.678997099660347603, 1.516718289441946199 ) ) ;
#22740=EDGE_LOOP ( 'NONE', ( #120498, #27691 ) ) ;
#22742=CARTESIAN_POINT ( 'NONE',  ( 1.036156370570060270, 1.841834720703208639, 0.3256331921374157057 ) ) ;
#22743=CARTESIAN_POINT ( 'NONE',  ( 0.2813449273042024079, 1.443300801228193153, -0.9609375900588543740 ) ) ;
#22745=CARTESIAN_POINT ( 'NONE',  ( 4.300438532332786501, 1.693616701070689956, -1.390861761948622766 ) ) ;
#22746=CARTESIAN_POINT ( 'NONE',  ( 5.262836394871557744, -1.675821390925121168, 1.586616667910417888 ) ) ;
#22747=CARTESIAN_POINT ( 'NONE',  ( 0.6552379465495603572, -1.740689658905628878, -1.102993579323052753 ) ) ;
#22748=CARTESIAN_POINT ( 'NONE',  ( 2.150241637240562831, -1.501185980473922488, 1.231905181128474691 ) ) ;
#22753=CARTESIAN_POINT ( 'NONE',  ( 3.762342404062005041, 1.897698010425369786, -0.6819954029829021769 ) ) ;
#22758=CARTESIAN_POINT ( 'NONE',  ( 0.6447967512687136082, -1.567379569643694515, 0.9359695128687425258 ) ) ;
#22764=CARTESIAN_POINT ( 'NONE',  ( 5.594623806460828241, -0.4985412361782278201, -1.999555476978178703 ) ) ;
#22770=CARTESIAN_POINT ( 'NONE',  ( 5.197918162715867929, 1.358090353789550342, 1.495039904793266095 ) ) ;
#22771=CARTESIAN_POINT ( 'NONE',  ( 5.918639493159310483, -0.7970842504121906646, -2.073522590485813666 ) ) ;
#22774=CARTESIAN_POINT ( 'NONE',  ( 5.471578299931997513, 1.986755592664890324, -0.5475478416450995089 ) ) ;
#22775=CARTESIAN_POINT ( 'NONE',  ( 4.324842380567116784, 0.8596320953860696612, -1.824118450417112847 ) ) ;
#22782=CARTESIAN_POINT ( 'NONE',  ( 4.007185349139028574, 2.006139037694018690, 0.2004037502189442987 ) ) ;
#22783=CARTESIAN_POINT ( 'NONE',  ( 4.031074566243696644, -1.271087849624694233, -1.332192834049110486 ) ) ;
#22785=CARTESIAN_POINT ( 'NONE',  ( 2.139721691919532098, -2.060220725375282225, 1.039829281875967570 ) ) ;
#22787=CARTESIAN_POINT ( 'NONE',  ( 3.550220938608072085, 2.161773192003491495, 0.003901938047633223515 ) ) ;
#22790=CARTESIAN_POINT ( 'NONE',  ( 3.691010296293754323, -1.365721494773973754, -1.848513781679576251 ) ) ;
#22793=CARTESIAN_POINT ( 'NONE',  ( 2.166681600665042229, -1.709288833360942617, -0.7604731621856930524 ) ) ;
#22795=CARTESIAN_POINT ( 'NONE',  ( 6.420779677996255153, 1.839401344301737184, 0.7098503129845078474 ) ) ;
#22801=CARTESIAN_POINT ( 'NONE',  ( 1.594636444620714633, -2.196503929104542951, -0.2137616909994101977 ) ) ;
#22806=CARTESIAN_POINT ( 'NONE',  ( 6.403199630258991526, 1.638877779571865423, 1.095505698648422177 ) ) ;
#22807=CARTESIAN_POINT ( 'NONE',  ( 5.338606043529401823, 2.272755431710461238, 0.3992410602531944464 ) ) ;
#22808=CARTESIAN_POINT ( 'NONE',  ( 0.4495626703563436743, 1.451167377975391304, 1.320406988977901985 ) ) ;
#22809=CARTESIAN_POINT ( 'NONE',  ( 2.518489969072700507, 0.8780072382167501965, 1.866465334303254897 ) ) ;
#22817=CARTESIAN_POINT ( 'NONE',  ( 0.2687526973377635797, -0.9260139170579514412, -1.961338766822422919 ) ) ;
#22819=CARTESIAN_POINT ( 'NONE',  ( 5.354971380013192395, 0.3533838956982695567, -1.806849549699687696 ) ) ;
#22820=CARTESIAN_POINT ( 'NONE',  ( 6.620655732516683045, 6.038298567659169613, 2.521170675138622475 ) ) ;
#22821=CARTESIAN_POINT ( 'NONE',  ( 6.720655732516647163, -0.004400176169771369272, 2.173773060281408931 ) ) ;
#22822=CARTESIAN_POINT ( 'NONE',  ( 0.2626887844769665303, -1.667795467377327423, -0.8471929967568125885 ) ) ;
#22823=CARTESIAN_POINT ( 'NONE',  ( 6.543838037463636681, 0.8733170268561093463, -2.087377253365163110 ) ) ;
#22827=CARTESIAN_POINT ( 'NONE',  ( 0.4692111731946085884, -1.615589042895089200, -1.022764193708516789 ) ) ;
#22828=CARTESIAN_POINT ( 'NONE',  ( 1.586397006687990885, -0.2552452650203296813, -1.751205042619798258 ) ) ;
#22830=CARTESIAN_POINT ( 'NONE',  ( 6.322908177684296582, 1.490210921086480234, -1.353605025193492128 ) ) ;
#22832=CARTESIAN_POINT ( 'NONE',  ( 3.145994354733801845, 0.8638979756431870438, 1.709836580976647813 ) ) ;
#22834=CARTESIAN_POINT ( 'NONE',  ( 4.000420421810535032, 1.959860935258441517, 0.1952677912114946512 ) ) ;
#22835=CARTESIAN_POINT ( 'NONE',  ( 0.2113915902133572944, 1.759560880827226947, -1.183302968686468226 ) ) ;
#22837=CARTESIAN_POINT ( 'NONE',  ( 3.115926070338378207, -0.9207206926411042325, -1.628290677324291780 ) ) ;
#22838=CARTESIAN_POINT ( 'NONE',  ( 6.059189007909253633, -1.483166448586000774, -0.8803546789384365523 ) ) ;
#22840=CARTESIAN_POINT ( 'NONE',  ( 2.578998426009218470, -2.112161100990978202, -0.6396139477699357423 ) ) ;
#22843=CARTESIAN_POINT ( 'NONE',  ( 1.170463292146912915, -0.9257924050831314311, -1.843294045186917085 ) ) ;
#22851=CARTESIAN_POINT ( 'NONE',  ( 3.209495720308676248, -1.691010085789945716, -1.194244797349801157 ) ) ;
#22855=CARTESIAN_POINT ( 'NONE',  ( 0.5748750247985534578, -1.461244816878112029, 1.394459567027491076 ) ) ;
#22859=CARTESIAN_POINT ( 'NONE',  ( 0.07459516483344308391, 2.893589955008399883, -2.244599473808198020 ) ) ;
#22861=CARTESIAN_POINT ( 'NONE',  ( 5.202499893966790800, -1.423744420606623429, -1.427717849564233532 ) ) ;
#22862=CARTESIAN_POINT ( 'NONE',  ( 5.876186789644119557, -1.907177742178717716, -0.1804351137127818694 ) ) ;
#22864=CARTESIAN_POINT ( 'NONE',  ( 4.177398808104064720, 1.432170664236757540, 1.658919600136643524 ) ) ;
#22866=CARTESIAN_POINT ( 'NONE',  ( 2.056764645581514728, 0.4224895836346024280, 1.864965418913032913 ) ) ;
#22869=CARTESIAN_POINT ( 'NONE',  ( 0.9488424731869498086, -1.824129051820524205, -0.8596123018156722750 ) ) ;
#22871=CARTESIAN_POINT ( 'NONE',  ( 6.603104432341277530, -0.4828188497946246382, 2.145653685147373313 ) ) ;
#22873=CARTESIAN_POINT ( 'NONE',  ( 3.416762500535154068, 1.558979225792535006, 0.7381585831351898941 ) ) ;
#22886=CARTESIAN_POINT ( 'NONE',  ( 3.281707762122548555, 1.766655041338391907, -0.3996267988317265818 ) ) ;
#22890=CARTESIAN_POINT ( 'NONE',  ( 4.318897000252651885, 1.397372457865418083, -1.152701029936139099 ) ) ;
#22895=CARTESIAN_POINT ( 'NONE',  ( 4.808966763405270406, -1.495079835775798838, 1.108065441546413288 ) ) ;
#22897=CARTESIAN_POINT ( 'NONE',  ( 2.267068109148970834, 1.750504415394140922, -0.7784415599910772254 ) ) ;
#22902=CARTESIAN_POINT ( 'NONE',  ( 6.925078400183575233, 2.022016365062285104, 2.447829694591229899 ) ) ;
#22907=CARTESIAN_POINT ( 'NONE',  ( 1.552797837233742095, -1.793874147449931344, -1.073420256486889324 ) ) ;
#22909=CARTESIAN_POINT ( 'NONE',  ( 6.176777841581622575, -1.829441475422811436, -0.6035904912435466896 ) ) ;
#22911=CARTESIAN_POINT ( 'NONE',  ( 2.221465439867484903, -1.771451409125622600, 0.4407646962370226351 ) ) ;
#22913=CARTESIAN_POINT ( 'NONE',  ( 1.037202349414727109, -0.04413313863061394532, 1.912034500058952036 ) ) ;
#22914=CARTESIAN_POINT ( 'NONE',  ( 1.240603756995876772, -1.920774042053990494, -0.4348295819559512831 ) ) ;
#22915=CARTESIAN_POINT ( 'NONE',  ( 3.843253449720198667, 0.6512379428032251116, -1.829756300597375596 ) ) ;
#22917=ORIENTED_EDGE ( 'NONE', *, *, #185885, .T. ) ;
#22920=CARTESIAN_POINT ( 'NONE',  ( 0.2032580500000652490, -1.434579632348313982, -1.185340245312079377 ) ) ;
#22929=CARTESIAN_POINT ( 'NONE',  ( 3.984828715814022981, -0.1808549858164226476, -1.816707794649790708 ) ) ;
#22934=CARTESIAN_POINT ( 'NONE',  ( 4.381629165553334815, 1.221847395770376377, 1.416585496670008659 ) ) ;
#22936=CARTESIAN_POINT ( 'NONE',  ( 1.611812915071403784, -1.911997954552616008, 0.2354761707349817823 ) ) ;
#22938=CARTESIAN_POINT ( 'NONE',  ( 6.948121807170864805, -0.8414398651286276731, 1.770450887113049099 ) ) ;
#22944=CARTESIAN_POINT ( 'NONE',  ( 6.491443032814855130, -0.4656331456187530748, 2.073361762655197893 ) ) ;
#22948=CARTESIAN_POINT ( 'NONE',  ( 4.715722526854881913, 0.4587184135333640111, -2.018627749927892179 ) ) ;
#22949=CARTESIAN_POINT ( 'NONE',  ( 0.1339853816830008371, 0.3136495386693045062, 1.814181566856580607 ) ) ;
#22951=CARTESIAN_POINT ( 'NONE',  ( 5.414730038718025718, -1.455890720088355961, -1.778839290973016629 ) ) ;
#22955=CARTESIAN_POINT ( 'NONE',  ( 0.7797068561936998377, 1.543341569868655450, 1.695032692825575005 ) ) ;
#22958=CARTESIAN_POINT ( 'NONE',  ( 5.472584303614713264, -0.04973451981254246174, -1.941474127069875433 ) ) ;
#22962=CARTESIAN_POINT ( 'NONE',  ( 5.818603510220927255, -0.6945032022064903110, -1.782003016414166474 ) ) ;
#22963=CARTESIAN_POINT ( 'NONE',  ( 5.788296071918774821, -0.7303023681345042206, -1.879805717804765353 ) ) ;
#22967=CARTESIAN_POINT ( 'NONE',  ( 2.431682593473180276, 0.9845738105917539729, -1.844271946693208708 ) ) ;
#22968=CARTESIAN_POINT ( 'NONE',  ( 0.7250502862299773588, -1.682426168213309703, 0.5495948440489316633 ) ) ;
#22970=CARTESIAN_POINT ( 'NONE',  ( 3.925942518080671739, 1.227467849647005282, -1.935749465030587313 ) ) ;
#22971=CARTESIAN_POINT ( 'NONE',  ( 1.991783209624857331, -0.4627563367010344986, -1.677588981799936541 ) ) ;
#22974=CARTESIAN_POINT ( 'NONE',  ( 2.213800448916534158, -1.389428533404401422, -1.036884654713841725 ) ) ;
#22976=CARTESIAN_POINT ( 'NONE',  ( 2.013881029938934919, 1.856366682828480608, -0.1327402387825328822 ) ) ;
#22977=CARTESIAN_POINT ( 'NONE',  ( 1.996751263802678533, 2.147379752972265354, 0.3199099038852480370 ) ) ;
#22979=CARTESIAN_POINT ( 'NONE',  ( 4.311732611912100666, -1.244383703160652610, -1.586670621409623116 ) ) ;
#22980=CARTESIAN_POINT ( 'NONE',  ( 3.031250000000001776, -0.7852924748301450819, -1.895863743164018400 ) ) ;
#22982=CARTESIAN_POINT ( 'NONE',  ( 0.5692023642799119987, 0.1922812221162081003, -1.916781067358761748 ) ) ;
#22984=CARTESIAN_POINT ( 'NONE',  ( 4.711300293261502681, 1.846222065370630050, -1.235088439349934841 ) ) ;
#22990=CARTESIAN_POINT ( 'NONE',  ( 0.1182595804350913826, -0.5859369620430117109, 2.142582832819041716 ) ) ;
#22992=CARTESIAN_POINT ( 'NONE',  ( 5.881297811770386019, -0.04968318840743202180, 1.961410508136133712 ) ) ;
#22995=CARTESIAN_POINT ( 'NONE',  ( 6.292268727954291485, -2.250598158220047385, -0.2311834041341890578 ) ) ;
#22997=CARTESIAN_POINT ( 'NONE',  ( 3.016140967954855423, 2.052969616667064123, -0.1997095218184695709 ) ) ;
#23001=CARTESIAN_POINT ( 'NONE',  ( 4.446469999505775483, 0.4968273501132040026, 1.803309644091706021 ) ) ;
#23002=CARTESIAN_POINT ( 'NONE',  ( 3.480872026922664286, -1.732388960670039113, -0.08070120533314528721 ) ) ;
#23003=CARTESIAN_POINT ( 'NONE',  ( 3.702475415089864441, 1.494950309154385426, 0.8909294612347866682 ) ) ;
#23004=CARTESIAN_POINT ( 'NONE',  ( 1.330038945030669995, 1.124775647945252643, -1.997386028781794387 ) ) ;
#23006=CARTESIAN_POINT ( 'NONE',  ( 4.194928683902748645, 1.680244682056671879, 1.243991948001839543 ) ) ;
#23007=CARTESIAN_POINT ( 'NONE',  ( 6.193304230345664685, -0.6518728838521523627, 1.829399646200319252 ) ) ;
#23011=CARTESIAN_POINT ( 'NONE',  ( 0.8267963299631932994, 0.8146243292815741333, -1.844710905833810255 ) ) ;
#23012=CARTESIAN_POINT ( 'NONE',  ( 0.5102161431939798986, -0.7575819503438313562, 1.980855387931411915 ) ) ;
#23017=CARTESIAN_POINT ( 'NONE',  ( 2.192179715818479036, 1.306768369893403170, 1.669877806752372740 ) ) ;
#23019=CARTESIAN_POINT ( 'NONE',  ( 4.775911370473768791, 1.053640644303525331, 1.490772598166143048 ) ) ;
#23027=CARTESIAN_POINT ( 'NONE',  ( 2.461199802766162570, -1.676885983773316990, 1.125551603727361627 ) ) ;
#23028=CARTESIAN_POINT ( 'NONE',  ( 5.790102700048295858, -0.9971039342967463748, 1.968745932239771568 ) ) ;
#23030=CARTESIAN_POINT ( 'NONE',  ( 3.309261503611124144, -1.518638105539332317, -1.075258281928012094 ) ) ;
#23036=CARTESIAN_POINT ( 'NONE',  ( 5.373610676068619973, 1.758448663713826132, -0.4906839848310071139 ) ) ;
#23040=CARTESIAN_POINT ( 'NONE',  ( 0.8601780606121096628, -0.6315397308106798224, 1.614934579331471998 ) ) ;
#23041=CARTESIAN_POINT ( 'NONE',  ( 6.720655732516648939, 0.005566325962592238129, 1.826293863978686538 ) ) ;
#23042=CARTESIAN_POINT ( 'NONE',  ( 6.024106105913028308, -1.276746162841462695, -1.922164112325924989 ) ) ;
#23044=CARTESIAN_POINT ( 'NONE',  ( 0.4212572661226633985, -0.1035701926632242170, 2.058322702938982562 ) ) ;
#23046=CARTESIAN_POINT ( 'NONE',  ( 6.098996632684510644, 1.141130774408656068, -1.995064312872560697 ) ) ;
#23049=CARTESIAN_POINT ( 'NONE',  ( 5.875831987524620992, 1.115552982110395330, 1.501486808359139946 ) ) ;
#23050=CARTESIAN_POINT ( 'NONE',  ( 4.060738401289211374, 0.5150538496448524572, 1.841637258418599155 ) ) ;
#23052=CARTESIAN_POINT ( 'NONE',  ( 4.934293700819583073, 1.136511309699510308, -1.891595316245115788 ) ) ;
#23053=CARTESIAN_POINT ( 'NONE',  ( 4.136029606254186142, 2.116781002543933088, -0.05581379417103624063 ) ) ;
#23056=CARTESIAN_POINT ( 'NONE',  ( 6.983263157960404754, 7.052265632007776119, 2.644342174942279744 ) ) ;
#23059=CARTESIAN_POINT ( 'NONE',  ( 5.496778590849229040, -2.068848325035842706, -0.4644329061709790429 ) ) ;
#23061=CARTESIAN_POINT ( 'NONE',  ( 2.468180027558197320, 2.263118346622743360, -0.4500467933809069176 ) ) ;
#23062=CARTESIAN_POINT ( 'NONE',  ( 3.965250677406896962, 1.681448970545707855, 1.010551734412237446 ) ) ;
#23064=CARTESIAN_POINT ( 'NONE',  ( 0.8484012048698870156, -1.946262134508335739, -0.2457884297097159831 ) ) ;
#23068=CARTESIAN_POINT ( 'NONE',  ( 5.524625123954316486, 0.3981063221985549072, 1.976670730632006601 ) ) ;
#23072=CARTESIAN_POINT ( 'NONE',  ( 3.327178260015594802, -2.004142704238300876, -0.8352945444606455494 ) ) ;
#23074=CARTESIAN_POINT ( 'NONE',  ( 0.5277791401020451856, -0.3051165123582540994, 2.098401203810342786 ) ) ;
#23079=CARTESIAN_POINT ( 'NONE',  ( 0.9134385407369073340, -0.3049482027854091837, 2.037980195292460550 ) ) ;
#23085=CARTESIAN_POINT ( 'NONE',  ( 2.859904825981678833, 0.6862549603197342085, -1.785085608301796523 ) ) ;
#23086=CARTESIAN_POINT ( 'NONE',  ( 5.418734442855144273, 1.636401904928608042, 0.6746929113052438920 ) ) ;
#23089=CARTESIAN_POINT ( 'NONE',  ( 0.1229364404080907497, 1.576183056183463993, 0.8927909362536170512 ) ) ;
#23091=CARTESIAN_POINT ( 'NONE',  ( 0.3916159773660661259, -1.906239802237769787, 0.1905982916604181676 ) ) ;
#23092=CARTESIAN_POINT ( 'NONE',  ( 2.523957353938070192, 2.030885678308389952, -0.4015143504868187718 ) ) ;
#23094=CARTESIAN_POINT ( 'NONE',  ( 6.244977087980838171, -1.579202250953464670, 1.002420361074819688 ) ) ;
#23095=CARTESIAN_POINT ( 'NONE',  ( 2.894927146036041510, 1.565677646668685696, -0.9388022922067614795 ) ) ;
#23097=CARTESIAN_POINT ( 'NONE',  ( 6.217417563691929772, -0.2743312036321900460, 2.189694890431858276 ) ) ;
#23100=CARTESIAN_POINT ( 'NONE',  ( 4.545415624535277921, 1.843838458276589209, -0.9247144854665176883 ) ) ;
#23104=CARTESIAN_POINT ( 'NONE',  ( 0.9136071317731933039, -0.3180670004044767740, 2.137961049616762921 ) ) ;
#23106=CARTESIAN_POINT ( 'NONE',  ( 6.443811375169310907, 1.424792453395683500, 1.502365266013883538 ) ) ;
#23108=CARTESIAN_POINT ( 'NONE',  ( 4.147864318636265146, 0.7325676050485959712, -2.033789780341701547 ) ) ;
#23109=CARTESIAN_POINT ( 'NONE',  ( 4.547524150180999314, -1.845711718722802486, 0.8204608018674663938 ) ) ;
#23115=CARTESIAN_POINT ( 'NONE',  ( 2.079314900164643820, 1.561883299538204151, 1.275554356156020308 ) ) ;
#23119=CARTESIAN_POINT ( 'NONE',  ( 5.730699431777452446, 1.279516236652695316, -1.421498520143074540 ) ) ;
#23123=CARTESIAN_POINT ( 'NONE',  ( 4.165638788432171502, 1.319243065725501873, 1.525032742243138451 ) ) ;
#23126=CARTESIAN_POINT ( 'NONE',  ( 6.282236785375785892, -0.9178991178065436518, 1.460045492214437246 ) ) ;
#23129=CARTESIAN_POINT ( 'NONE',  ( 4.446469999505775483, 0.4968273501132040026, 1.803309644091706021 ) ) ;
#23132=CARTESIAN_POINT ( 'NONE',  ( 2.061466481998303735, 1.718891244229248105, 1.153550331455879707 ) ) ;
#23136=CARTESIAN_POINT ( 'NONE',  ( 0.5269705342763851830, -1.727990693721896287, 1.039014695730144933 ) ) ;
#23137=CARTESIAN_POINT ( 'NONE',  ( 1.617148605665112537, 1.507408818846365017, 1.004416837792695194 ) ) ;
#23146=CARTESIAN_POINT ( 'NONE',  ( 6.398046686924231174, -0.9077857338794625974, -1.686868998638735073 ) ) ;
#23155=CARTESIAN_POINT ( 'NONE',  ( 3.538091169922503276, 0.9737216987566952309, -1.930062384640649054 ) ) ;
#23159=CARTESIAN_POINT ( 'NONE',  ( 0.3344391967911933272, -1.139684030083350841, -1.788147294700337397 ) ) ;
#23160=CARTESIAN_POINT ( 'NONE',  ( 6.352569596097208837, 0.5757234290239590102, 1.732508359437078482 ) ) ;
#23161=CARTESIAN_POINT ( 'NONE',  ( 2.583225839741074115, 1.803852637447726392, -0.7955871043755156080 ) ) ;
#23162=CARTESIAN_POINT ( 'NONE',  ( 4.517770118113122457, -0.5046507728132009207, 1.844564425022446885 ) ) ;
#23164=CARTESIAN_POINT ( 'NONE',  ( 5.090277013941287620, 1.014100869069594291, -1.688273828314874825 ) ) ;
#23165=CARTESIAN_POINT ( 'NONE',  ( 0.07597880344310371792, -1.883441279811811642, -0.4727451468593062422 ) ) ;
#23172=CARTESIAN_POINT ( 'NONE',  ( 4.811142580195256535, 1.587781804131962682, -1.065416552848017284 ) ) ;
#23173=ORIENTED_EDGE ( 'NONE', *, *, #55279, .F. ) ;
#23174=CARTESIAN_POINT ( 'NONE',  ( 0.6927435329204565395, -2.190372518412486702, -0.2681103625320201411 ) ) ;
#23176=CARTESIAN_POINT ( 'NONE',  ( 6.621754286443582771, -0.4424289334611238300, 1.971349943050800801 ) ) ;
#23179=CARTESIAN_POINT ( 'NONE',  ( 2.031770498437397876, 1.981864486777328294, -0.5989037013024376410 ) ) ;
#23183=CARTESIAN_POINT ( 'NONE',  ( 0.4444780689869810564, 2.156031605563761833, 0.1575401717312311101 ) ) ;
#23188=CARTESIAN_POINT ( 'NONE',  ( -0.02319159430947624612, 7.629137130509076492, -2.410989586153564623 ) ) ;
#23190=CARTESIAN_POINT ( 'NONE',  ( 4.641094080744356809, 0.6698209448141523303, 1.599790421982680400 ) ) ;
#23192=CARTESIAN_POINT ( 'NONE',  ( 2.694261129275489886, 0.9798316074655871732, -1.823736424811234658 ) ) ;
#23194=CARTESIAN_POINT ( 'NONE',  ( 4.956716356600668227, -1.994036693836033658, -0.7120731657841266049 ) ) ;
#23198=CARTESIAN_POINT ( 'NONE',  ( 2.078894642590666031, 1.835759051837970945, 0.7136754054878727827 ) ) ;
#23200=CARTESIAN_POINT ( 'NONE',  ( -0.2049973002360427898, -0.1418364932926942379, -1.881151990943498387 ) ) ;
#23201=CARTESIAN_POINT ( 'NONE',  ( 4.382983890270373273, 2.048579214610211530, -1.028644635605566959 ) ) ;
#23202=CARTESIAN_POINT ( 'NONE',  ( 1.312830284664792790, 1.609138963534262778, 0.8624270714618911260 ) ) ;
#23207=CARTESIAN_POINT ( 'NONE',  ( 3.269792347016476697, 0.4849277011088357070, -1.953833955329455696 ) ) ;
#23208=( BOUNDED_CURVE ( )  B_SPLINE_CURVE ( 3, ( #87851, #23894, #55348, #138747 ),
 .UNSPECIFIED., .F., .T. ) 
 B_SPLINE_CURVE_WITH_KNOTS ( ( 4, 4 ),
 ( 0.4999999999999992784, 1.000000000000000000 ),
 .UNSPECIFIED. ) 
 CURVE ( )  GEOMETRIC_REPRESENTATION_ITEM ( )  RATIONAL_B_SPLINE_CURVE ( ( 1.000000000000000888, 0.3333333333333333148, 0.3333333333333323711, 1.000000000000000000 ) ) 
 REPRESENTATION_ITEM ( '' )  );
#23209=CARTESIAN_POINT ( 'NONE',  ( 3.432423435979839343, -1.172226468724973936, 1.572839002276872566 ) ) ;
#23213=CARTESIAN_POINT ( 'NONE',  ( 6.509723796436136745, -0.9841294377065135102, -1.844520550012812565 ) ) ;
#23214=CARTESIAN_POINT ( 'NONE',  ( 4.697990591988738807, -1.769527177957382680, -0.04185004791794690038 ) ) ;
#23216=CARTESIAN_POINT ( 'NONE',  ( 0.8850414913617115076, 1.931072968267994794, -1.036053359626129877 ) ) ;
#23217=CARTESIAN_POINT ( 'NONE',  ( 5.683501733545419654, -0.7767583057271000291, 1.557453612149447775 ) ) ;
#23220=CARTESIAN_POINT ( 'NONE',  ( 6.311202115008078373, 1.327223183623595704, -1.876690649992603044 ) ) ;
#23223=CARTESIAN_POINT ( 'NONE',  ( 5.202368031388965974, -1.227288160380139548, -1.225006654371106452 ) ) ;
#23224=CARTESIAN_POINT ( 'NONE',  ( 1.787996309160574837, 1.523479866092191548, 1.596893430481533649 ) ) ;
#23226=CARTESIAN_POINT ( 'NONE',  ( 5.881339278728036746, -0.05926448915108929044, 2.170540009233146606 ) ) ;
#23228=CARTESIAN_POINT ( 'NONE',  ( 0.6907973960054912821, 1.599150545848356364, -1.387813827701115610 ) ) ;
#23229=CARTESIAN_POINT ( 'NONE',  ( 2.718750000000001332, -0.7852924748298429902, 1.895863743164144744 ) ) ;
#23230=CARTESIAN_POINT ( 'NONE',  ( 6.727182134110181622, 6.034673098952469950, 2.683942742083842425 ) ) ;
#23231=CARTESIAN_POINT ( 'NONE',  ( 4.840804290916858932, 0.3290424097142484738, 1.897927756555679801 ) ) ;
#23232=CARTESIAN_POINT ( 'NONE',  ( 1.243189324034719823, 2.142110494306264101, 0.5876511989056328877 ) ) ;
#23234=CARTESIAN_POINT ( 'NONE',  ( 1.277341847617214476, 2.115720621435190907, -0.8829085993839781432 ) ) ;
#23238=CARTESIAN_POINT ( 'NONE',  ( 4.231244787023562992, 2.030907777374240997, 0.9001406952713184584 ) ) ;
#23244=CARTESIAN_POINT ( 'NONE',  ( 2.215470409936692420, 1.956561601830292485, 0.4872017847364697452 ) ) ;
#23246=CARTESIAN_POINT ( 'NONE',  ( 6.180145878880094479, -1.142753862412404509, -1.717008129757614077 ) ) ;
#23249=CARTESIAN_POINT ( 'NONE',  ( 6.269106929289325336, 1.662610211318481301, -0.5146825814001282362 ) ) ;
#23251=CARTESIAN_POINT ( 'NONE',  ( 1.159032429170350653, 0.3524738178620877571, -1.734097463706934183 ) ) ;
#23252=CARTESIAN_POINT ( 'NONE',  ( 0.7213275451133926985, 1.987047012402185731, 0.3419330716275259530 ) ) ;
#23253=CARTESIAN_POINT ( 'NONE',  ( 6.532745107981281940, -1.550057735787165214, 0.7916670675358824516 ) ) ;
#23254=CARTESIAN_POINT ( 'NONE',  ( 4.493851497812589635, -2.291808737193799406, -0.05710960328321466883 ) ) ;
#23255=CARTESIAN_POINT ( 'NONE',  ( 3.099365256270599112, -1.839010575856118823, 0.09107247011905240941 ) ) ;
#23258=CARTESIAN_POINT ( 'NONE',  ( 2.643341535394112984, -1.351257319430071657, -1.227710988083303478 ) ) ;
#23259=CARTESIAN_POINT ( 'NONE',  ( 4.043592392309851569, -1.492256208629010761, 1.356298961253152413 ) ) ;
#23261=CARTESIAN_POINT ( 'NONE',  ( 3.204270770158343939, -2.259979215032235977, 0.1094169825565076415 ) ) ;
#23263=CARTESIAN_POINT ( 'NONE',  ( 5.315496758875870142, -0.3119175628578441661, 2.082610458907033557 ) ) ;
#23265=CARTESIAN_POINT ( 'NONE',  ( 4.105968538015460467, 0.7004154448949986289, -1.948405661837959713 ) ) ;
#23268=CARTESIAN_POINT ( 'NONE',  ( 5.303433364654349447, 1.869980213031800398, -0.9998494819224086338 ) ) ;
#23271=CARTESIAN_POINT ( 'NONE',  ( 1.049297559255836010, -1.518254527582623359, -1.185787014772927916 ) ) ;
#23279=CARTESIAN_POINT ( 'NONE',  ( 0.5279477311770188752, -0.3182371573221299266, 2.198381937975202760 ) ) ;
#23280=CARTESIAN_POINT ( 'NONE',  ( 2.133940825901488481, -1.375048162780323935, -1.595187971101755364 ) ) ;
#23283=CARTESIAN_POINT ( 'NONE',  ( 6.526204204079649962, 0.9558936715202811518, 1.596491800297286545 ) ) ;
#23290=CARTESIAN_POINT ( 'NONE',  ( 0.2465380642357860586, 1.084720387836759725, -1.822023332652397354 ) ) ;
#23293=CARTESIAN_POINT ( 'NONE',  ( 3.297265573180406584, -1.731424309613574852, 0.9225008839797432802 ) ) ;
#23294=CARTESIAN_POINT ( 'NONE',  ( 1.657319961134783748, -1.854130675604428902, -1.111159678259740602 ) ) ;
#23295=CARTESIAN_POINT ( 'NONE',  ( 1.083273795380396143, -0.8277460070302902206, 1.644747122058511035 ) ) ;
#23298=CARTESIAN_POINT ( 'NONE',  ( 3.257457426684560620, 0.7833967258410595713, 1.554110229252920528 ) ) ;
#23302=CARTESIAN_POINT ( 'NONE',  ( 1.253037233087474611, -1.703760181015579134, 1.330383891403746688 ) ) ;
#23303=CARTESIAN_POINT ( 'NONE',  ( 2.266953675890924558, -2.015725231744563306, 0.04666741021024794350 ) ) ;
#23305=CARTESIAN_POINT ( 'NONE',  ( 0.1984014031938194922, -2.161264429664040421, -0.05129915172277095536 ) ) ;
#23306=CARTESIAN_POINT ( 'NONE',  ( 2.342595614570395668, 0.4301288016448929774, 1.923825502367804141 ) ) ;
#23307=CARTESIAN_POINT ( 'NONE',  ( 6.609000000000009756, 0.005669918681722520802, 1.900160851458796873 ) ) ;
#23308=CARTESIAN_POINT ( 'NONE',  ( 2.067823894287325714, -1.192992258377950865, 1.532381367046357523 ) ) ;
#23314=CARTESIAN_POINT ( 'NONE',  ( -0.1110810684432986112, 0.002541288824218449188, -1.796853612742685513 ) ) ;
#23319=CARTESIAN_POINT ( 'NONE',  ( 6.124106107054944736, -1.275020473110911157, -1.923184551904693507 ) ) ;
#23321=CARTESIAN_POINT ( 'NONE',  ( 3.625789200213443753, 1.914935786268581852, -0.4253726038727227432 ) ) ;
#23323=CARTESIAN_POINT ( 'NONE',  ( 0.4576579978108759050, -1.899619568183811058, -0.6767110947205197125 ) ) ;
#23325=CARTESIAN_POINT ( 'NONE',  ( 1.815762809344774187, -1.387149605378830586, -1.599721994570136197 ) ) ;
#23328=CARTESIAN_POINT ( 'NONE',  ( 3.398233898566359823, 1.450718870894672330, -1.133551952132209717 ) ) ;
#23331=CARTESIAN_POINT ( 'NONE',  ( 3.902672080109194752, -2.098000727953463151, -0.3078000538283761078 ) ) ;
#23332=CARTESIAN_POINT ( 'NONE',  ( 0.3922017905241963476, 1.532332584989907653, -1.020347975915262939 ) ) ;
#23336=CARTESIAN_POINT ( 'NONE',  ( 4.429017379523855880, 0.09708327650245980600, 2.058604088861961667 ) ) ;
#23338=CARTESIAN_POINT ( 'NONE',  ( 1.452429406588066740, -1.579491434881035827, -0.9459884711465746943 ) ) ;
#23343=CARTESIAN_POINT ( 'NONE',  ( 0.8739773845415178544, 2.125910683164092152, -0.5920798734769525673 ) ) ;
#23344=CARTESIAN_POINT ( 'NONE',  ( 3.638171750181828035, 1.021205778115843010, -2.018914226005202206 ) ) ;
#23346=CARTESIAN_POINT ( 'NONE',  ( 3.937629537800376500, -1.731762593766679403, 0.5317277010480087052 ) ) ;
#23347=CARTESIAN_POINT ( 'NONE',  ( 3.837047941109549054, -1.595840754823075303, -1.059516945425369450 ) ) ;
#23349=CARTESIAN_POINT ( 'NONE',  ( 5.494608840674215955, 2.039112051642687717, 0.3575134270455831986 ) ) ;
#23351=CARTESIAN_POINT ( 'NONE',  ( 2.940257707442377022, 1.956376729411358095, 0.2430245213203632293 ) ) ;
#23352=CARTESIAN_POINT ( 'NONE',  ( 1.184454412485607344, -1.878822398200689525, -0.4247803175085519412 ) ) ;
#23353=CARTESIAN_POINT ( 'NONE',  ( 3.977312496258199825, 1.761605600429091201, -0.6297503393934977822 ) ) ;
#23355=CARTESIAN_POINT ( 'NONE',  ( 2.948224681477436881, 0.8299853515197992415, -2.153443412361542020 ) ) ;
#23356=CARTESIAN_POINT ( 'NONE',  ( 4.158551126772993989, -0.5825245785200537929, -1.767622772031415490 ) ) ;
#23361=CARTESIAN_POINT ( 'NONE',  ( 0.4168064962662480499, 1.450752768847368257, -1.526948433937134197 ) ) ;
#23366=CARTESIAN_POINT ( 'NONE',  ( 1.775790443353560732, 0.3575140072833470906, -2.090081039791711337 ) ) ;
#23368=CARTESIAN_POINT ( 'NONE',  ( 0.5627676185161786249, 0.5905471060306236586, 1.931493850173772397 ) ) ;
#23373=CARTESIAN_POINT ( 'NONE',  ( 0.6851285477917113953, -0.2638797801631336259, -2.145333599305146333 ) ) ;
#23374=CARTESIAN_POINT ( 'NONE',  ( 6.610000000000006537, 0.6121396118998356783, 1.775466344933520846 ) ) ;
#23376=CARTESIAN_POINT ( 'NONE',  ( 6.825078400183590688, 2.971555572656236599, 2.408956600524428282 ) ) ;
#23379=CARTESIAN_POINT ( 'NONE',  ( 5.841029835422532734, -1.731992920607817288, -1.032484497598872064 ) ) ;
#23381=CARTESIAN_POINT ( 'NONE',  ( 0.1698123575781598782, 1.266975945507025081, 1.788028528876134393 ) ) ;
#23382=CARTESIAN_POINT ( 'NONE',  ( 6.684453901184132185, -2.118919246787358102, -0.4271090584619871566 ) ) ;
#23386=CARTESIAN_POINT ( 'NONE',  ( 1.089294787249419194, -0.4641297292061612456, 1.858405954227143386 ) ) ;
#23390=CARTESIAN_POINT ( 'NONE',  ( 2.560839114378242076, -1.500511350262800470, -0.8505237462590549136 ) ) ;
#23392=CARTESIAN_POINT ( 'NONE',  ( 2.002845679596281681, 1.468101958376843985, 0.9879206967360052438 ) ) ;
#23393=CARTESIAN_POINT ( 'NONE',  ( 4.928867898441261275, 2.110505041808665716, 0.6446608841527908806 ) ) ;
#23395=CARTESIAN_POINT ( 'NONE',  ( 4.219013726799848207, 1.558537513506755845, -1.284668789120123833 ) ) ;
#23397=CARTESIAN_POINT ( 'NONE',  ( 4.705793326368500118, 1.571798730262342181, 1.423547657546264000 ) ) ;
#23398=CARTESIAN_POINT ( 'NONE',  ( 3.673453983005552814, 1.462458373076291673, 1.388474078538141754 ) ) ;
#23399=CARTESIAN_POINT ( 'NONE',  ( 4.007922362044618048, -0.6876924770315288038, 1.676191166192544157 ) ) ;
#23403=CARTESIAN_POINT ( 'NONE',  ( 1.621729638615863944, -1.036547396872866678, -1.557007864774778705 ) ) ;
#23405=CARTESIAN_POINT ( 'NONE',  ( 6.305303276254960565, 1.572402219250234268, -0.8993151100721032964 ) ) ;
#23417=CARTESIAN_POINT ( 'NONE',  ( 4.060867369437678676, 0.5686956411946364476, 2.042824496258560441 ) ) ;
#23418=CARTESIAN_POINT ( 'NONE',  ( -0.1296875068448125334, 4.095146142119266308, -2.381513845672214913 ) ) ;
#23420=CARTESIAN_POINT ( 'NONE',  ( 5.395764264914824970, -0.7120431519804657494, 1.838431125455505688 ) ) ;
#23422=CARTESIAN_POINT ( 'NONE',  ( 0.4045417950784445105, -1.998468379361338698, -0.2424310749817460697 ) ) ;
#23424=CARTESIAN_POINT ( 'NONE',  ( 6.509000000000050967, 0.001920477310565076989, 2.100274754360692331 ) ) ;
#23426=CARTESIAN_POINT ( 'NONE',  ( 1.170471352854907776, -0.9292243337341490328, -1.850172451097586990 ) ) ;
#23430=CARTESIAN_POINT ( 'NONE',  ( 5.226549702048478352, 0.1529751191454275516, 2.085101625929087099 ) ) ;
#23433=CARTESIAN_POINT ( 'NONE',  ( 2.678497062878131718, -1.746332412481563567, -0.5319975912557314279 ) ) ;
#23434=CARTESIAN_POINT ( 'NONE',  ( 2.033590728242135715, -1.756817081591253604, 0.4409998202260062006 ) ) ;
#23438=CARTESIAN_POINT ( 'NONE',  ( 4.770673279661371780, -1.444480529215144804, 1.668407551275403300 ) ) ;
#23442=CARTESIAN_POINT ( 'NONE',  ( 3.387273370026026686, 0.04433669930821101945, -1.911926451916061476 ) ) ;
#23445=CARTESIAN_POINT ( 'NONE',  ( 6.180147188013234150, -1.146869210499700920, -1.723488058659912392 ) ) ;
#23447=CARTESIAN_POINT ( 'NONE',  ( 6.023007056224171762, -2.064090639567913499, 0.7368321019862942300 ) ) ;
#23457=CARTESIAN_POINT ( 'NONE',  ( 5.629760504653214426, 1.996728726787128538, -0.5467053113129491937 ) ) ;
#23458=CARTESIAN_POINT ( 'NONE',  ( 4.248602273900093707, 0.5149172349826669493, 1.856347322705960146 ) ) ;
#23459=CARTESIAN_POINT ( 'NONE',  ( 1.546500145565053108, -1.423948579484592747, 1.427951870166991544 ) ) ;
#23463=ADVANCED_FACE ( 'NONE', ( #8981 ), #189865, .T. ) ;
#23465=CARTESIAN_POINT ( 'NONE',  ( 1.060776890969020059, -1.982532595227912475, -0.9341070725938580566 ) ) ;
#23466=CARTESIAN_POINT ( 'NONE',  ( 5.162654993523497993, -1.319871331358621447, 1.261628347558926944 ) ) ;
#23475=ORIENTED_EDGE ( 'NONE', *, *, #191590, .F. ) ;
#23476=CARTESIAN_POINT ( 'NONE',  ( 2.507154105146496725, -1.820902139252629448, 0.2722148935128121394 ) ) ;
#23477=CARTESIAN_POINT ( 'NONE',  ( 6.521754290436940771, -0.4404898795188401106, 1.971875975034496742 ) ) ;
#23478=CARTESIAN_POINT ( 'NONE',  ( 2.091588275066556868, 1.323615364194903554, -1.878831054484223495 ) ) ;
#23479=CARTESIAN_POINT ( 'NONE',  ( 0.2329586101569866563, 0.008238550247445517935, -1.845944905557160398 ) ) ;
#23481=DIRECTION ( 'NONE',  ( -0.9999980456341537316, 0.000000000000000000, -0.001977050295949950038 ) ) ;
#23482=CARTESIAN_POINT ( 'NONE',  ( 3.322422747544371280, -0.7792853099402965444, -1.746611395919236642 ) ) ;
#23486=CARTESIAN_POINT ( 'NONE',  ( 2.120754239039924549, 0.003043923042475667976, 2.090933975095090158 ) ) ;
#23487=CARTESIAN_POINT ( 'NONE',  ( 1.516246529245099284, 1.258767711876613848, -1.383943980506313398 ) ) ;
#23488=CARTESIAN_POINT ( 'NONE',  ( 2.214220036344019871, -1.617569417291262690, -1.203170845901546215 ) ) ;
#23492=CARTESIAN_POINT ( 'NONE',  ( 2.630072014739594177, 0.2149344560898290013, 1.727053582138169618 ) ) ;
#23496=CARTESIAN_POINT ( 'NONE',  ( 2.490480453433571384, -0.2941264275767330183, -1.699438164531028583 ) ) ;
#23497=CARTESIAN_POINT ( 'NONE',  ( 2.806388347806953121, 1.585463108415147149, -1.513251884624075672 ) ) ;
#23498=CARTESIAN_POINT ( 'NONE',  ( 4.916741810085082598, 1.523553907054091328, -1.596827639139485777 ) ) ;
#23500=CARTESIAN_POINT ( 'NONE',  ( 3.907220266852969637, -1.778082601562074094, 1.245552836545896769 ) ) ;
#23501=CARTESIAN_POINT ( 'NONE',  ( 2.156629195875509719, -1.411784796728832392, 1.157573153174975111 ) ) ;
#23502=( NAMED_UNIT ( * ) PLANE_ANGLE_UNIT ( ) SI_UNIT ( $, .RADIAN. ) );
#23503=CARTESIAN_POINT ( 'NONE',  ( 4.540305813605725938, 0.8135460886731570307, 1.954998174167394520 ) ) ;
#23504=CARTESIAN_POINT ( 'NONE',  ( 6.639320575229236354, 1.260096212659385984, 2.110683211146132443 ) ) ;
#23507=CARTESIAN_POINT ( 'NONE',  ( 4.388395349243869425, -0.5016406811718626679, -2.236657869423730460 ) ) ;
#23511=CARTESIAN_POINT ( 'NONE',  ( 0.03014954708456181465, -2.078685333231004684, 0.4181070283913386199 ) ) ;
#23517=CARTESIAN_POINT ( 'NONE',  ( 4.975232503164924935, -2.001511053420693020, -0.2440319332882301961 ) ) ;
#23519=CARTESIAN_POINT ( 'NONE',  ( 3.063389470891558997, 1.739959455442946279, 1.107334787568447165 ) ) ;
#23521=CARTESIAN_POINT ( 'NONE',  ( -0.1409997244345879697, 0.2375178066936211585, -2.034344168881811132 ) ) ;
#23524=CARTESIAN_POINT ( 'NONE',  ( 5.736325210887869730, 0.4244523575273988492, 2.149783713274712404 ) ) ;
#23525=CARTESIAN_POINT ( 'NONE',  ( 3.358046224211252095, 0.04667712216412447934, -2.016033814150198999 ) ) ;
#23526=CARTESIAN_POINT ( 'NONE',  ( 3.122423488780329492, 0.04808623196613136253, 1.840796284283818585 ) ) ;
#23528=CARTESIAN_POINT ( 'NONE',  ( 6.651389018303578204, -1.468406013062272253, -1.084454090978362428 ) ) ;
#23530=CARTESIAN_POINT ( 'NONE',  ( 6.543838037463636681, 0.8733170268561093463, -2.087377253365163110 ) ) ;
#23531=CARTESIAN_POINT ( 'NONE',  ( 1.383574010005955701, 1.945322680536746063, -0.8074913105669545565 ) ) ;
#23539=CARTESIAN_POINT ( 'NONE',  ( 3.973042321754824524, -1.644474126697339944, 1.493583396047935219 ) ) ;
#23540=CARTESIAN_POINT ( 'NONE',  ( 2.853686581259745836, 2.180823047698337902, -0.2155538573413370296 ) ) ;
#23542=CARTESIAN_POINT ( 'NONE',  ( 6.883263157960393563, 1.268976584491373183, 2.060807272249213451 ) ) ;
#23544=CARTESIAN_POINT ( 'NONE',  ( 5.406682003534418079, 0.5678430586343993225, 1.877905798087247335 ) ) ;
#23552=CARTESIAN_POINT ( 'NONE',  ( 5.062787373817618786, 0.6179034821891697948, 2.028544477791139222 ) ) ;
#23555=CARTESIAN_POINT ( 'NONE',  ( 5.911032513020411550, 1.904272706209766630, 1.023102869888978583 ) ) ;
#23557=CARTESIAN_POINT ( 'NONE',  ( 4.546344060013487898, -1.475942220874026489, 1.100600019281534836 ) ) ;
#23560=CARTESIAN_POINT ( 'NONE',  ( 0.2744473674479709913, 1.625014162249105443, -0.6237133657705071776 ) ) ;
#23561=CARTESIAN_POINT ( 'NONE',  ( 6.727182134110196721, 3.701357331967893405, 2.425430364167603603 ) ) ;
#23564=CARTESIAN_POINT ( 'NONE',  ( 4.258765444007106105, -1.603684720688375975, 1.449730421305382544 ) ) ;
#23566=CARTESIAN_POINT ( 'NONE',  ( 6.854846703925610463, -0.8643618726141141240, 1.819651424301058640 ) ) ;
#23570=CARTESIAN_POINT ( 'NONE',  ( 3.819328725847204620, -0.1613130240520690706, 2.155748724213396361 ) ) ;
#23571=CARTESIAN_POINT ( 'NONE',  ( 4.341064969683814390, -1.716640784620737659, 0.9690559893368445588 ) ) ;
#23572=CARTESIAN_POINT ( 'NONE',  ( 3.444447550215405052, 1.098527548611628601, 1.341433071544478217 ) ) ;
#23573=CARTESIAN_POINT ( 'NONE',  ( 1.277182604683280598, 2.023070758711601691, -0.8431670391453591762 ) ) ;
#23574=CARTESIAN_POINT ( 'NONE',  ( 1.343279689680024536, 0.4525242940816387449, 2.262625540901804122 ) ) ;
#23575=CARTESIAN_POINT ( 'NONE',  ( 4.182927011504236070, -0.1980092267137799622, -2.051220347156012647 ) ) ;
#23576=CARTESIAN_POINT ( 'NONE',  ( 5.759312517635055251, 1.912593682650292060, -0.3362288579709416525 ) ) ;
#23584=CARTESIAN_POINT ( 'NONE',  ( 3.241465689944766915, -1.947025830926933043, 1.038692105600529159 ) ) ;
#23587=CARTESIAN_POINT ( 'NONE',  ( 0.5142147075538996415, 0.7048593813003102282, 1.722512033545370080 ) ) ;
#23588=CARTESIAN_POINT ( 'NONE',  ( -0.02919842301646497981, 5.720960850909259321, -2.667883601355185430 ) ) ;
#23592=CARTESIAN_POINT ( 'NONE',  ( 6.298766309436587996, 1.533505995929709487, 1.018591839899836371 ) ) ;
#23594=CARTESIAN_POINT ( 'NONE',  ( 2.026313557074521210, 1.187556641299570614, -1.684123726253353492 ) ) ;
#23601=CARTESIAN_POINT ( 'NONE',  ( 0.9892191112199534286, 1.817966452439750968, -0.9706697534878678812 ) ) ;
#23603=CARTESIAN_POINT ( 'NONE',  ( 5.108874002337426390, -0.2646564886703614006, 1.822002613180016883 ) ) ;
#23607=CARTESIAN_POINT ( 'NONE',  ( 4.442132104469964204, 0.9450947508268662256, -1.994404356956205326 ) ) ;
#23608=CARTESIAN_POINT ( 'NONE',  ( 0.7905619602705875604, -2.145198653374354336, -0.2653712149464776959 ) ) ;
#23610=CARTESIAN_POINT ( 'NONE',  ( 0.6153073421325053749, 1.564839666810373231, 1.099065937236625157 ) ) ;
#23611=CARTESIAN_POINT ( 'NONE',  ( 0.8664231474371618669, -1.968446048378743152, -0.4370742218882398000 ) ) ;
#23612=COLOUR_RGB ( '', 0.09019608, 0.27058824, 0.51372549) ;
#23615=CARTESIAN_POINT ( 'NONE',  ( 1.318156941596902998, -1.811358654967555104, 1.414711894558273730 ) ) ;
#23619=CARTESIAN_POINT ( 'NONE',  ( 1.727212824277712944, -1.762453432929488528, 0.6273722324065673650 ) ) ;
#23620=CARTESIAN_POINT ( 'NONE',  ( 2.764861550476094276, -0.1531697945360478985, -2.010801143277194392 ) ) ;
#23622=CARTESIAN_POINT ( 'NONE',  ( 6.639320575229257670, 2.427506520031021520, 2.484945200759064665 ) ) ;
#23624=CARTESIAN_POINT ( 'NONE',  ( 3.985071343692931034, -0.2060594512321256011, -2.095964026187596918 ) ) ;
#23630=CARTESIAN_POINT ( 'NONE',  ( 3.920179414529322504, -2.014104250368133453, 0.1526392722818684933 ) ) ;
#23632=CARTESIAN_POINT ( 'NONE',  ( 6.531690654341108626, 1.975040822251827644, -0.5949189890239890977 ) ) ;
#23634=CARTESIAN_POINT ( 'NONE',  ( 4.552137767457805850, 2.161219302129935738, -0.04802546048104232301 ) ) ;
#23640=CARTESIAN_POINT ( 'NONE',  ( 2.172564162468085147, -1.022266837292043595, -1.915435327925461229 ) ) ;
#23643=CARTESIAN_POINT ( 'NONE',  ( 1.311775528174640604, 1.236260529797410301, -1.364685630449238740 ) ) ;
#23645=CARTESIAN_POINT ( 'NONE',  ( 3.034921719543516971, -1.931671641359738567, 1.035203715903771915 ) ) ;
#23646=CARTESIAN_POINT ( 'NONE',  ( 6.983263157960365675, 7.629137130509066722, 2.753810918356710769 ) ) ;
#23647=CARTESIAN_POINT ( 'NONE',  ( 3.889755562772099662, 1.636703778197702075, 1.562332884182315196 ) ) ;
#23654=CARTESIAN_POINT ( 'NONE',  ( 5.044116495868207650, 1.765035602982415242, 0.1300806658623629153 ) ) ;
#23656=CARTESIAN_POINT ( 'NONE',  ( 1.852698501422584298, 0.6601115537133980249, 1.999908888789264649 ) ) ;
#23659=CARTESIAN_POINT ( 'NONE',  ( 0.8187300819318241718, -1.428952508342665517, 1.355707701654704112 ) ) ;
#23663=CARTESIAN_POINT ( 'NONE',  ( 5.343967111402722736, -1.155686419774919704, -1.395051459885946699 ) ) ;
#23666=CARTESIAN_POINT ( 'NONE',  ( 5.260568668178753349, -1.354309965608934352, 1.290672426560689035 ) ) ;
#23668=CARTESIAN_POINT ( 'NONE',  ( 4.469627305733424372, -0.3590069766891256231, 2.038746214588673666 ) ) ;
#23678=CARTESIAN_POINT ( 'NONE',  ( 3.455471728117681440, 1.544996161402897528, 1.208956721487665087 ) ) ;
#23680=CARTESIAN_POINT ( 'NONE',  ( 2.126327167286511166, 0.3474154575464418748, -1.985796285822030383 ) ) ;
#23685=CARTESIAN_POINT ( 'NONE',  ( 2.284254421533092216, -1.833544361078912388, -0.3693468884775341077 ) ) ;
#23687=CARTESIAN_POINT ( 'NONE',  ( 4.412362193956616885, -2.012844744014946841, -0.04520991500436136873 ) ) ;
#23690=CARTESIAN_POINT ( 'NONE',  ( 3.761412437133329068, 1.992871936191454418, -0.7152352101782408766 ) ) ;
#23692=CARTESIAN_POINT ( 'NONE',  ( 4.475093801846619535, 1.891600172242546840, 0.8420093967692193759 ) ) ;
#23694=CARTESIAN_POINT ( 'NONE',  ( 0.8551579053767807137, 0.4041549552570160575, -2.051131941465775821 ) ) ;
#23695=CARTESIAN_POINT ( 'NONE',  ( 6.620655732516651071, 4.689394895873098434, 2.736297475404291024 ) ) ;
#23696=CARTESIAN_POINT ( 'NONE',  ( 6.581069972421211389, -0.09314021972051110543, -1.823315219958022482 ) ) ;
#23704=CARTESIAN_POINT ( 'NONE',  ( -0.07596920688733227456, -0.7732221873907207943, -1.636987988057141852 ) ) ;
#23713=CARTESIAN_POINT ( 'NONE',  ( 6.415638736316127577, -1.319241173714128745, -1.525034172108488573 ) ) ;
#23716=CARTESIAN_POINT ( 'NONE',  ( -0.1405533004718676759, 7.629137130509054288, -2.320277334263821434 ) ) ;
#23719=CARTESIAN_POINT ( 'NONE',  ( 2.307411487444132270, -1.578694758215667404, -1.177220170345204098 ) ) ;
#23720=CARTESIAN_POINT ( 'NONE',  ( 4.780875152847498200, 1.674876996157638187, -1.122516304564516565 ) ) ;
#23724=CARTESIAN_POINT ( 'NONE',  ( 4.927760762764835434, 1.128268568998530563, -1.878541326455762661 ) ) ;
#23726=CARTESIAN_POINT ( 'NONE',  ( 2.713793335149127905, -1.905670363949378165, 0.2809714450454863233 ) ) ;
#23728=CARTESIAN_POINT ( 'NONE',  ( -0.1298852118744256712, 1.416581902219627542, -1.986715197202136185 ) ) ;
#23729=CARTESIAN_POINT ( 'NONE',  ( 0.3642759247451561322, 2.182245240920151375, -0.3280614795862640820 ) ) ;
#23735=CARTESIAN_POINT ( 'NONE',  ( 5.970224376651540155, -1.750504005202535796, -0.5711807346103907612 ) ) ;
#23736=CARTESIAN_POINT ( 'NONE',  ( 3.123692395903770347, -0.3905211382968387102, 1.974689860881967407 ) ) ;
#23737=CARTESIAN_POINT ( 'NONE',  ( 4.886215977948979550, -0.1196125283245419307, 2.295398719017431866 ) ) ;
#23739=CARTESIAN_POINT ( 'NONE',  ( 2.940123752802700885, -0.9609217279343595930, 1.593531096896059873 ) ) ;
#23745=CARTESIAN_POINT ( 'NONE',  ( 6.444877668667830406, -1.679477184941297496, -1.245029935506683838 ) ) ;
#23751=CARTESIAN_POINT ( 'NONE',  ( 6.428329371266205072, 0.9864720512241608175, -1.414751289540659318 ) ) ;
#23753=CARTESIAN_POINT ( 'NONE',  ( 2.056849044198369114, -1.066344721839644460, 1.367450411802049182 ) ) ;
#23758=CARTESIAN_POINT ( 'NONE',  ( 6.825048293896172957, -1.981324744236719004, -0.8880960284254543202 ) ) ;
#23759=CARTESIAN_POINT ( 'NONE',  ( 5.408770660633122063, 1.379882519126625295, -1.195542987486551301 ) ) ;
#23760=CARTESIAN_POINT ( 'NONE',  ( 2.905073028004667712, -1.633678134795817583, 1.085783093053994453 ) ) ;
#23764=CARTESIAN_POINT ( 'NONE',  ( 4.231183009085410340, 1.939187816756043237, 0.8583030597293441755 ) ) ;
#23765=CARTESIAN_POINT ( 'NONE',  ( 6.827182134110223011, 1.235230467647760566, 2.302354205009625954 ) ) ;
#23767=CARTESIAN_POINT ( 'NONE',  ( 1.762639944428091576, -0.7413553172891698129, -1.933158369416078770 ) ) ;
#23770=CARTESIAN_POINT ( 'NONE',  ( 3.211816561499138523, 1.752256602034316213, 1.365123760953767418 ) ) ;
#23772=CARTESIAN_POINT ( 'NONE',  ( 1.565480925793379274, -1.225038264044479686, 1.944918359529357543 ) ) ;
#23774=CARTESIAN_POINT ( 'NONE',  ( 0.2390249890181182224, -0.1369461163322066299, -1.930431041017650395 ) ) ;
#23778=CARTESIAN_POINT ( 'NONE',  ( 6.550350952284553330, -1.418464805562440922, 1.173678288350611609 ) ) ;
#23780=CARTESIAN_POINT ( 'NONE',  ( 2.882959773793275726, -1.768624019741386277, -0.7279546805132871556 ) ) ;
#23781=CARTESIAN_POINT ( 'NONE',  ( -0.2104748580754391973, 0.7011259924453935310, -2.185273273056092425 ) ) ;
#23782=CARTESIAN_POINT ( 'NONE',  ( 4.576996085227628797, -0.001753933126501586170, -1.724958192235986232 ) ) ;
#23783=CARTESIAN_POINT ( 'NONE',  ( 2.483611571103707227, -0.6279893487078170855, 1.916353726171161398 ) ) ;
#23784=CARTESIAN_POINT ( 'NONE',  ( 3.920743334446879835, -1.585418671752996334, -1.664648107385821030 ) ) ;
#23785=CARTESIAN_POINT ( 'NONE',  ( 3.655803326253406649, 0.5538646471104657909, -2.193435612772106413 ) ) ;
#23786=CARTESIAN_POINT ( 'NONE',  ( 5.883451020920152708, 1.946514763749309429, -0.8046133670899023871 ) ) ;
#23788=CARTESIAN_POINT ( 'NONE',  ( 5.132005351226563761, 0.9095619001311354701, -1.517971549226182715 ) ) ;
#23790=CARTESIAN_POINT ( 'NONE',  ( 0.8148889116572692881, 2.119938092393148565, 0.8724386107587696060 ) ) ;
#23791=CARTESIAN_POINT ( 'NONE',  ( 6.087831982560696353, -1.832735460234231617, -0.1757473516527594259 ) ) ;
#23795=CARTESIAN_POINT ( 'NONE',  ( 6.070311387754347088, -2.079788119406985825, -0.6908379657195939938 ) ) ;
#23798=CARTESIAN_POINT ( 'NONE',  ( 6.268043187460373922, -2.055199631210803624, 0.2494731385529954104 ) ) ;
#23799=CARTESIAN_POINT ( 'NONE',  ( 0.4445464637146989695, -1.457232572767804379, 1.394089106691732693 ) ) ;
#23801=CARTESIAN_POINT ( 'NONE',  ( 4.863854859025781074, 1.905264070129700782, -0.2845116402651908794 ) ) ;
#23804=CARTESIAN_POINT ( 'NONE',  ( 1.512303732575480675, -0.7424040314494853021, 2.093836701676012879 ) ) ;
#23809=CARTESIAN_POINT ( 'NONE',  ( -0.1108833634136767443, 0.0002062650063822807356, -1.896853557917008271 ) ) ;
#23814=CARTESIAN_POINT ( 'NONE',  ( 1.135121963537696566, -0.04462593873827064989, -1.961518378280776354 ) ) ;
#23817=CARTESIAN_POINT ( 'NONE',  ( 6.268018250734934682, -1.947192974725008963, 0.2387856323943157166 ) ) ;
#23820=CARTESIAN_POINT ( 'NONE',  ( 0.2337813496832439053, -2.066932786716439541, 0.9205801711329018033 ) ) ;
#23824=CARTESIAN_POINT ( 'NONE',  ( 0.9482695043977107385, 0.5371953702461745861, 1.791772314883005146 ) ) ;
#23825=CARTESIAN_POINT ( 'NONE',  ( 0.6681306116654138760, 1.163384174638517177, 1.286150249643343901 ) ) ;
#23827=CARTESIAN_POINT ( 'NONE',  ( 4.124703146219878214, 0.1084699374758208573, 2.189010777610411740 ) ) ;
#23828=CARTESIAN_POINT ( 'NONE',  ( 4.032480619008128819, 1.237564890788948269, -1.947499633988438061 ) ) ;
#23829=CARTESIAN_POINT ( 'NONE',  ( 0.5146158036630330557, 1.421672375139692246, -1.492246178604545115 ) ) ;
#23830=CARTESIAN_POINT ( 'NONE',  ( 2.466655979050590197, 0.09513121245676225968, -1.939734245173969640 ) ) ;
#23832=CARTESIAN_POINT ( 'NONE',  ( 5.642871316567687145, 2.044259226470702462, 0.5637153772257290640 ) ) ;
#23834=CARTESIAN_POINT ( 'NONE',  ( 3.199842427594956185, 1.824118962040650604, 0.8596310190432245868 ) ) ;
#23838=CARTESIAN_POINT ( 'NONE',  ( 1.066719475142905216, -1.649486405746130258, -0.7827983987617056494 ) ) ;
#23843=CARTESIAN_POINT ( 'NONE',  ( 5.963760128287220574, 2.030816783491296906, -0.3497918165830601334 ) ) ;
#23848=CARTESIAN_POINT ( 'NONE',  ( 5.320965550519270337, 1.527853097053995191, -1.320967980168601175 ) ) ;
#23849=CARTESIAN_POINT ( 'NONE',  ( 5.760436963792294307, 2.218610086356072930, 0.1113587401332209043 ) ) ;
#23853=CARTESIAN_POINT ( 'NONE',  ( 4.592684518728709975, -0.4495978358524716501, -2.011083796685923630 ) ) ;
#23854=CARTESIAN_POINT ( 'NONE',  ( 4.465470312728934132, -1.956561007648183192, -0.4872041746135646889 ) ) ;
#23861=CARTESIAN_POINT ( 'NONE',  ( 3.743517394402117837, -1.942243990624907823, -0.5404084370827856310 ) ) ;
#23862=CARTESIAN_POINT ( 'NONE',  ( 3.222423357234117436, 0.04607595322191247733, 1.840729346561786661 ) ) ;
#23864=CARTESIAN_POINT ( 'NONE',  ( 1.260874316716424470, 0.9392902264234997967, 2.108064829403846208 ) ) ;
#23866=CARTESIAN_POINT ( 'NONE',  ( 3.286554482555790191, -2.129011082553730727, -0.3730605165198074835 ) ) ;
#23871=CARTESIAN_POINT ( 'NONE',  ( 2.412791964582483129, 1.669947582624079274, 0.8431454209596804805 ) ) ;
#23873=CARTESIAN_POINT ( 'NONE',  ( 6.332890595682218127, 0.1930081403669886009, 1.961983401381848457 ) ) ;
#23877=CARTESIAN_POINT ( 'NONE',  ( 1.489210700298746692, -0.3264265768355456010, -2.182489157894373033 ) ) ;
#23882=CARTESIAN_POINT ( 'NONE',  ( 5.682488568729203493, -1.923295458312636264, -0.4324549907560610307 ) ) ;
#23883=CARTESIAN_POINT ( 'NONE',  ( 6.076872578159392191, -2.189301982996785245, -0.7299270095633101363 ) ) ;
#23884=CARTESIAN_POINT ( 'NONE',  ( 6.654761307663171976, -0.4979203083825957110, -1.793151784937331961 ) ) ;
#23885=CARTESIAN_POINT ( 'NONE',  ( 3.010651042449908221, 0.6904807078514271224, 1.943715162320960088 ) ) ;
#23887=ADVANCED_FACE ( 'NONE', ( #16427 ), #164379, .T. ) ;
#23893=CARTESIAN_POINT ( 'NONE',  ( 5.863789056686759871, -0.5331677977272324398, 2.104577851170267078 ) ) ;
#23894=CARTESIAN_POINT ( 'NONE',  ( 6.639320575229258559, 0.002292789353198345943, 1.996863816985874118 ) ) ;
#23895=CARTESIAN_POINT ( 'NONE',  ( 4.880324068823122197, -0.2306306682541107433, -1.826696389425507938 ) ) ;
#23898=CARTESIAN_POINT ( 'NONE',  ( 6.750000000000007994, 7.629137130509070275, 2.600000000000001421 ) ) ;
#23899=CARTESIAN_POINT ( 'NONE',  ( 0.2634263733268344398, -2.021796075192600295, -1.015562799429880814 ) ) ;
#23907=CARTESIAN_POINT ( 'NONE',  ( 1.551229123295729373, 0.5181449431543529993, -1.692289574110398931 ) ) ;
#23908=CARTESIAN_POINT ( 'NONE',  ( -0.02298948590537253436, -1.708053232816408196, -0.8599758793098393195 ) ) ;
#23910=CARTESIAN_POINT ( 'NONE',  ( 3.339363673285804079, 0.4624358396413058570, -1.858828564233159675 ) ) ;
#23912=CARTESIAN_POINT ( 'NONE',  ( 3.947672784279113500, 1.424866277981166052, 1.359976495918001627 ) ) ;
#23913=CARTESIAN_POINT ( 'NONE',  ( 6.381118777440311085, -1.848351591093103652, -0.8147283084726087976 ) ) ;
#23914=CARTESIAN_POINT ( 'NONE',  ( 2.535844406030359544, 0.8837261853790435717, -1.648756255988912400 ) ) ;
#23915=CARTESIAN_POINT ( 'NONE',  ( -0.02319159430949970999, 0.003959926571647092407, -1.810968101872318714 ) ) ;
#23917=CARTESIAN_POINT ( 'NONE',  ( 2.086817400036289794, -2.164668306305051804, -0.4287355390964405211 ) ) ;
#23920=CARTESIAN_POINT ( 'NONE',  ( 6.777797683793751915, -1.903277019102869616, 0.4755351429900215310 ) ) ;
#23928=CARTESIAN_POINT ( 'NONE',  ( 1.557173632797459684, 1.693725193156172315, -1.190412882225246438 ) ) ;
#23932=CARTESIAN_POINT ( 'NONE',  ( 1.330729578248716960, 1.354828421643257119, -1.498027418808007605 ) ) ;
#23936=CARTESIAN_POINT ( 'NONE',  ( 0.07459516483341446791, 5.726030365519781284, -2.349570391284861781 ) ) ;
#23938=CARTESIAN_POINT ( 'NONE',  ( 5.993517489292202960, 1.942244631591660164, 0.5404061186519912852 ) ) ;
#23939=CARTESIAN_POINT ( 'NONE',  ( 5.594928181924037069, 1.692849881775596366, 0.8967378362389683000 ) ) ;
#23940=CARTESIAN_POINT ( 'NONE',  ( 6.639320575229291421, 7.052573552169272730, 2.601414154538615353 ) ) ;
#23941=CARTESIAN_POINT ( 'NONE',  ( 3.667680160636753506, 1.218766932906123479, 1.821211977396507198 ) ) ;
#23943=CARTESIAN_POINT ( 'NONE',  ( 2.408343312057196872, -1.907530749141531423, -0.1368029246449145864 ) ) ;
#23947=CARTESIAN_POINT ( 'NONE',  ( 6.239883422132978197, 2.111550094393780608, -0.1561052605421053563 ) ) ;
#23950=CARTESIAN_POINT ( 'NONE',  ( 6.392125918040960642, -0.5824770489515176397, -2.112646119873210271 ) ) ;
#23952=CARTESIAN_POINT ( 'NONE',  ( 3.012419478190906830, 1.250452035320260835, -1.188195685136491875 ) ) ;
#23965=CARTESIAN_POINT ( 'NONE',  ( 3.141053669680595739, 0.04696373034178760036, 1.811039086309898627 ) ) ;
#23969=CARTESIAN_POINT ( 'NONE',  ( 4.354050602105923318, 0.7703955181818689102, -1.639620356061684436 ) ) ;
#23973=CARTESIAN_POINT ( 'NONE',  ( 5.406657457964442415, 0.5403815791694633885, 1.780887135367102303 ) ) ;
#23975=CARTESIAN_POINT ( 'NONE',  ( 2.144012975658988740, 0.8210224433658172005, 1.730898686554068311 ) ) ;
#23976=CARTESIAN_POINT ( 'NONE',  ( 1.360069071312763223, 0.7361036424862777983, 1.670779996689908398 ) ) ;
#23986=CARTESIAN_POINT ( 'NONE',  ( 0.8848510708264365476, 1.842997052242268508, -0.9869714196348714497 ) ) ;
#23987=CARTESIAN_POINT ( 'NONE',  ( 6.792047303494690880, -0.8216981310003536043, 1.740383667632472875 ) ) ;
#23989=CARTESIAN_POINT ( 'NONE',  ( 2.379681254797087586, 1.121034037677430595, 1.440765146680768272 ) ) ;
#23990=CARTESIAN_POINT ( 'NONE',  ( 3.282038605231399231, 1.400092287458438722, 1.705885466304429166 ) ) ;
#23992=CARTESIAN_POINT ( 'NONE',  ( 1.908593538011025492, 0.6150006609981206740, 1.871157805954210440 ) ) ;
#23993=CARTESIAN_POINT ( 'NONE',  ( 3.667467498987980967, 1.081383794499408468, 1.612947176984424802 ) ) ;
#23997=CARTESIAN_POINT ( 'NONE',  ( 6.438329693799461850, -0.9962124079390155540, 1.571646734037221105 ) ) ;
#24000=ADVANCED_FACE ( 'NONE', ( #77441 ), #112156, .T. ) ;
#24003=CARTESIAN_POINT ( 'NONE',  ( 2.384552795368581890, -0.3778730364575392797, -2.158588602542845347 ) ) ;
#24008=CARTESIAN_POINT ( 'NONE',  ( 4.055160972438559774, -1.518969423100406946, -1.012540670841777013 ) ) ;
#24015=CARTESIAN_POINT ( 'NONE',  ( 2.332535780611888043, 1.868688736674573247, 0.4679572130895108817 ) ) ;
#24022=CARTESIAN_POINT ( 'NONE',  ( 6.385961957380775544, -2.116826826188836552, 0.05405687909286471110 ) ) ;
#24024=CARTESIAN_POINT ( 'NONE',  ( 4.979381509686323426, -0.1069728651886258930, 2.067640925720988232 ) ) ;
#24025=CARTESIAN_POINT ( 'NONE',  ( 0.4855842612344652975, -1.827229208960782447, -0.2260576252584786672 ) ) ;
#24027=CARTESIAN_POINT ( 'NONE',  ( 5.555437251493606787, -1.460316692103363456, 1.775274546321881530 ) ) ;
#24031=CARTESIAN_POINT ( 'NONE',  ( 0.5688445697737016804, -2.160344153581617022, -0.7667740616737575010 ) ) ;
#24034=CARTESIAN_POINT ( 'NONE',  ( 4.576081071864527061, -1.884036987645235417, -0.4702585519323047025 ) ) ;
#24038=CARTESIAN_POINT ( 'NONE',  ( 6.398695753475230674, -1.876852914212179035, -0.3660984893600614520 ) ) ;
#24039=CARTESIAN_POINT ( 'NONE',  ( 0.3281590906380106865, 1.648959081962350304, 0.5061492587876709193 ) ) ;
#24040=CARTESIAN_POINT ( 'NONE',  ( 6.157435431667657610, 1.928259211291092123, -0.5899821858514133766 ) ) ;
#24043=CARTESIAN_POINT ( 'NONE',  ( 3.169954053886741008, -1.245012139812958996, 1.679338519663716500 ) ) ;
#24044=CARTESIAN_POINT ( 'NONE',  ( 1.604008636410862554, -0.6330215999658711512, -1.652955932040809595 ) ) ;
#24048=CARTESIAN_POINT ( 'NONE',  ( 4.506013928309719141, -0.9778350203078637337, -2.073373472838499598 ) ) ;
#24049=CARTESIAN_POINT ( 'NONE',  ( 2.150002804924430411, -1.345968700644652349, 1.103203096369822056 ) ) ;
#24052=CARTESIAN_POINT ( 'NONE',  ( 2.777707764728345907, 0.3069055913166895966, -2.098134212408508059 ) ) ;
#24054=CARTESIAN_POINT ( 'NONE',  ( 2.653305042933405300, -0.2923731341353021373, -1.708803492460549744 ) ) ;
#24056=CARTESIAN_POINT ( 'NONE',  ( 1.838117294476193431, -0.9991240133950601843, 1.569924424075196390 ) ) ;
#24057=CARTESIAN_POINT ( 'NONE',  ( 1.891327416536987105, 0.2117802020594385659, 2.160802721360413070 ) ) ;
#24059=CARTESIAN_POINT ( 'NONE',  ( 3.204314817619222211, 1.275555974797081049, -1.561881975048397209 ) ) ;
#24060=CARTESIAN_POINT ( 'NONE',  ( 2.718750000000001332, -0.7852924748298429902, 1.895863743164144744 ) ) ;
#24062=CARTESIAN_POINT ( 'NONE',  ( 1.342661396784496697, 0.3730742192328758144, 1.889760217127177455 ) ) ;
#24064=CARTESIAN_POINT ( 'NONE',  ( 5.045291550738682851, 0.1642389012704112972, 2.215424048113129540 ) ) ;
#24066=CARTESIAN_POINT ( 'NONE',  ( -0.2110808730067144090, 0.2462152545684419269, -1.831495465910786269 ) ) ;
#24070=CARTESIAN_POINT ( 'NONE',  ( 6.082328216444968128, 1.141246503175277205, 1.905736721132505140 ) ) ;
#24071=CARTESIAN_POINT ( 'NONE',  ( 4.756279191188107269, -1.961398630904508833, -0.05015466537350299348 ) ) ;
#24075=CARTESIAN_POINT ( 'NONE',  ( 5.518922325393873507, 2.087324940739025525, 0.8731552084927389767 ) ) ;
#24077=CARTESIAN_POINT ( 'NONE',  ( 3.033693852995589246, 1.959511903404848043, -0.6444255830786119743 ) ) ;
#24081=CARTESIAN_POINT ( 'NONE',  ( 4.885944009213345929, -0.8832235454491498272, 1.648918812636574804 ) ) ;
#24082=CARTESIAN_POINT ( 'NONE',  ( 3.955468362790943715, -1.619900715620861131, -0.6195580815930351593 ) ) ;
#24083=CARTESIAN_POINT ( 'NONE',  ( 2.876183954794831354, -0.1304463317927692101, -1.735623171917876073 ) ) ;
#24084=CARTESIAN_POINT ( 'NONE',  ( 0.8730959291491724450, -0.06322356207747076295, -2.291674109354911781 ) ) ;
#24085=CARTESIAN_POINT ( 'NONE',  ( 1.501302152069685425, 1.803625081967351829, -1.271268654958551014 ) ) ;
#24086=CARTESIAN_POINT ( 'NONE',  ( 5.056232447125663221, -1.513354532948107956, 1.442795048270538727 ) ) ;
#24087=CARTESIAN_POINT ( 'NONE',  ( 5.507742394360604088, -0.8750994344452074358, -1.733673826448577593 ) ) ;
#24090=CARTESIAN_POINT ( 'NONE',  ( 0.8443752267504719411, 0.3905955241953715795, -1.978051186352240309 ) ) ;
#24098=CARTESIAN_POINT ( 'NONE',  ( 3.932112477472641920, 0.9751300899686901058, -1.543267412809447681 ) ) ;
#24103=CARTESIAN_POINT ( 'NONE',  ( 1.722921806169195547, 1.493705621373665915, -1.359711205623759023 ) ) ;
#24104=CARTESIAN_POINT ( 'NONE',  ( 5.438574045396407541, 2.173287242562565780, 0.3821286992964008089 ) ) ;
#24106=CARTESIAN_POINT ( 'NONE',  ( 2.553354172538614630, 1.434905519572576171, 1.184926768776579431 ) ) ;
#24112=CARTESIAN_POINT ( 'NONE',  ( 4.547361323050268744, -1.413013347330991598, -1.156083184146582177 ) ) ;
#24116=CARTESIAN_POINT ( 'NONE',  ( 0.7371068013607602332, -1.629765380930665364, -0.5920680523868580014 ) ) ;
#24117=CARTESIAN_POINT ( 'NONE',  ( 0.1459185412583801633, -1.400943258209320863, 1.032289493613134823 ) ) ;
#24118=CARTESIAN_POINT ( 'NONE',  ( 5.250698995481407394, 0.6654115676409579905, 2.209675006967478428 ) ) ;
#24120=CARTESIAN_POINT ( 'NONE',  ( 0.4915707408097417797, 1.525207926881542830, 1.386002245639144981 ) ) ;
#24123=CARTESIAN_POINT ( 'NONE',  ( 6.063868583556772052, 1.884346855680006261, -1.315804018288849964 ) ) ;
#24126=CARTESIAN_POINT ( 'NONE',  ( 5.295714669793899709, -0.6724083694377264164, 1.745798414713333413 ) ) ;
#24127=CARTESIAN_POINT ( 'NONE',  ( 3.603681638446740720, 1.388520161702249567, 1.315275747533505069 ) ) ;
#24129=CARTESIAN_POINT ( 'NONE',  ( 5.285833163787800437, 1.479997892162682849, 1.637210856327932618 ) ) ;
#24130=CARTESIAN_POINT ( 'NONE',  ( 4.417270958439249107, -1.934380516720465959, 0.8614220525851381538 ) ) ;
#24135=CARTESIAN_POINT ( 'NONE',  ( 6.199870563505585963, 1.461971410283597894, 1.536153618249151309 ) ) ;
#24136=CARTESIAN_POINT ( 'NONE',  ( 2.802171680323842118, -0.7245931359087741663, 2.190924829087222303 ) ) ;
#24137=CARTESIAN_POINT ( 'NONE',  ( 3.666413850373055006, -0.7928392042928497085, -1.794698522912529182 ) ) ;
#24138=CARTESIAN_POINT ( 'NONE',  ( 5.998899845030374323, 0.3968100507469035643, 2.023884403326465797 ) ) ;
#24142=CARTESIAN_POINT ( 'NONE',  ( 5.348842313791752900, -1.825074749614737701, -0.8578464102408298597 ) ) ;
#24145=CARTESIAN_POINT ( 'NONE',  ( 2.114367463569406080, 2.165448829365283157, -0.1565315255437193243 ) ) ;
#24151=CARTESIAN_POINT ( 'NONE',  ( 1.511086176359067501, 1.816151333767004772, 0.9739060079534812564 ) ) ;
#24153=CARTESIAN_POINT ( 'NONE',  ( 6.727182134110222478, 3.706444386917655986, 2.325533714637216143 ) ) ;
#24155=CARTESIAN_POINT ( 'NONE',  ( -0.1608832656953863849, 7.629137130509072939, -2.497055476982701361 ) ) ;
#24157=CARTESIAN_POINT ( 'NONE',  ( 3.791585636498477463, 1.799617611794877670, -0.6470144256675299799 ) ) ;
#24158=CARTESIAN_POINT ( 'NONE',  ( 4.926482082969720899, 1.694141084728201907, 0.5120089106541975132 ) ) ;
#24161=CARTESIAN_POINT ( 'NONE',  ( 0.6327121402699478203, 1.674153623460835627, 0.6926115325788273491 ) ) ;
#24163=CARTESIAN_POINT ( 'NONE',  ( 0.004910489962322779275, -0.09121751714964576596, 1.913643331117439672 ) ) ;
#24164=CARTESIAN_POINT ( 'NONE',  ( 1.346235217667652417, -0.9325981557438846048, 1.848514419461377845 ) ) ;
#24166=CARTESIAN_POINT ( 'NONE',  ( 6.666881909320486521, -1.711340306973156977, -0.7558587634414122292 ) ) ;
#24167=CARTESIAN_POINT ( 'NONE',  ( 2.754317325142870754, 0.6151756178996542479, 1.719052816137212503 ) ) ;
#24168=CARTESIAN_POINT ( 'NONE',  ( 5.865903189996044098, 2.174886565178067777, -0.3735607071253948530 ) ) ;
#24171=CARTESIAN_POINT ( 'NONE',  ( 3.016140967954855423, 2.052969616667064123, -0.1997095218184695709 ) ) ;
#24177=CARTESIAN_POINT ( 'NONE',  ( 6.109843426155951107, 0.6047356833836557977, -1.980059631771100781 ) ) ;
#24179=CARTESIAN_POINT ( 'NONE',  ( 4.042369558984196587, 2.150769235480045616, 0.2162802025119994753 ) ) ;
#24180=CARTESIAN_POINT ( 'NONE',  ( 4.600263385724223220, -0.9500085478860437194, 1.782271578547896418 ) ) ;
#24181=CARTESIAN_POINT ( 'NONE',  ( 2.066782613880484565, 1.455849762852476248, -1.315278764014264912 ) ) ;
#24186=CARTESIAN_POINT ( 'NONE',  ( 2.149625371984189126, 1.976669504256656218, -0.3981124878784659815 ) ) ;
#24190=CARTESIAN_POINT ( 'NONE',  ( 6.117437049485344502, 1.593764408019750389, 1.056661447057717362 ) ) ;
#24194=CARTESIAN_POINT ( 'NONE',  ( 3.409779952838042583, -1.203371721269937744, -1.617806234278630573 ) ) ;
#24197=CARTESIAN_POINT ( 'NONE',  ( 5.965779495465724835, 1.698367018877691370, -0.2996015908335278310 ) ) ;
#24202=CARTESIAN_POINT ( 'NONE',  ( 3.936663633328242096, 0.2718032920513112627, 1.850550731861917653 ) ) ;
#24204=CARTESIAN_POINT ( 'NONE',  ( 1.657173498210939844, 1.694793865239911712, -1.188712540599102141 ) ) ;
#24209=CARTESIAN_POINT ( 'NONE',  ( 6.621734039712152686, -0.3858887922842542673, 1.776151629007856281 ) ) ;
#24216=CARTESIAN_POINT ( 'NONE',  ( 6.603150280507321668, -0.1401627607961895561, 1.883980500587930429 ) ) ;
#24224=CARTESIAN_POINT ( 'NONE',  ( 2.799875798528407511, -0.6792266858460673795, 2.052276964324008635 ) ) ;
#24227=CARTESIAN_POINT ( 'NONE',  ( 0.3520121086563637869, -1.504009422257305495, -1.495223887398588358 ) ) ;
#24228=CARTESIAN_POINT ( 'NONE',  ( 5.508770632382115728, 1.381118045931900573, -1.193960910464037850 ) ) ;
#24230=CARTESIAN_POINT ( 'NONE',  ( 1.247272744223869356, -1.551563771690873006, -1.215972028847669417 ) ) ;
#24231=CARTESIAN_POINT ( 'NONE',  ( 3.902528505893249733, -1.892296425594198750, -0.2755589300712790735 ) ) ;
#24234=CARTESIAN_POINT ( 'NONE',  ( 5.125436402459787821, 0.1948648891074710732, -1.959901157258244098 ) ) ;
#24235=CARTESIAN_POINT ( 'NONE',  ( 0.4099697989727095204, 1.339763683568921504, -1.405998798013205819 ) ) ;
#24239=CARTESIAN_POINT ( 'NONE',  ( 6.539320575229233157, 0.001224430076711413356, 2.103502572931112091 ) ) ;
#24242=CARTESIAN_POINT ( 'NONE',  ( 3.615784255950851289, -0.5524401208748200842, 1.830756043982272097 ) ) ;
#24244=CARTESIAN_POINT ( 'NONE',  ( 1.114635189304619356, -0.9934212416997322270, -1.970578525975318573 ) ) ;
#24246=CARTESIAN_POINT ( 'NONE',  ( 6.393232662110455600, -0.1012007143085277561, -2.010677637860050382 ) ) ;
#24249=CARTESIAN_POINT ( 'NONE',  ( 6.727182134110203826, 2.985950691969769810, 2.264927069331075238 ) ) ;
#24250=CARTESIAN_POINT ( 'NONE',  ( 2.172408243068229439, -0.9739482337229148357, -1.826950231780352762 ) ) ;
#24253=CARTESIAN_POINT ( 'NONE',  ( 0.7784641540938314064, -1.199969256800371697, 1.797863220954009966 ) ) ;
#24260=CARTESIAN_POINT ( 'NONE',  ( 6.925078400183577010, 7.053014648177382995, 2.453806744102948745 ) ) ;
#24262=CARTESIAN_POINT ( 'NONE',  ( 5.379468213355050210, -0.4295577260071090087, -1.679954900457746980 ) ) ;
#24265=CARTESIAN_POINT ( 'NONE',  ( 2.993098612437725681, 0.2488643248897918769, 2.055149816265568585 ) ) ;
#24266=CARTESIAN_POINT ( 'NONE',  ( 3.128620947210249970, 0.5168888077675163339, 2.053037424179054327 ) ) ;
#24269=CARTESIAN_POINT ( 'NONE',  ( 1.410928143256191092, -1.555772830594209788, 1.207522851012821308 ) ) ;
#24272=CARTESIAN_POINT ( 'NONE',  ( 3.451411174752341715, 0.5572527081592703047, -2.223385661236119581 ) ) ;
#24273=CARTESIAN_POINT ( 'NONE',  ( 1.980809073483770000, -0.08854697198140694392, -1.823669195971427071 ) ) ;
#24277=CARTESIAN_POINT ( 'NONE',  ( 3.375247105954663596, -1.777387065663883714, -0.9453995415899820731 ) ) ;
#24278=CARTESIAN_POINT ( 'NONE',  ( 3.028120845615460688, 1.045410262836780069, 1.659804706804830277 ) ) ;
#24281=CARTESIAN_POINT ( 'NONE',  ( 0.07536363704235481131, 0.6997989235110781969, -2.226667633679416447 ) ) ;
#24282=CARTESIAN_POINT ( 'NONE',  ( 6.492138175525482779, -0.5563555211482211771, -2.015168333173870785 ) ) ;
#24283=CARTESIAN_POINT ( 'NONE',  ( 5.067173336470212064, 0.1711322554274422036, -1.761558580727173862 ) ) ;
#24285=CARTESIAN_POINT ( 'NONE',  ( 0.5510472016944796270, -1.853416330350022179, -1.169031858332982177 ) ) ;
#24286=CARTESIAN_POINT ( 'NONE',  ( 6.017484387666114820, -0.9725936433230500944, -1.442976214814440716 ) ) ;
#24288=CARTESIAN_POINT ( 'NONE',  ( 0.1333692844072767447, 1.351132181276387678, -2.308013766563504987 ) ) ;
#24289=CARTESIAN_POINT ( 'NONE',  ( 6.082725252809636274, -0.7780705872160005310, 2.163147651226764889 ) ) ;
#24291=CARTESIAN_POINT ( 'NONE',  ( 5.149590220011600827, -0.2133714078210862675, -1.720544222028724146 ) ) ;
#24292=CARTESIAN_POINT ( 'NONE',  ( 1.840723031453334935, 2.183200880077686978, 0.3216222850719457349 ) ) ;
#24293=CARTESIAN_POINT ( 'NONE',  ( 6.421112215724263272, -1.799107166270615732, 0.9110519380226205222 ) ) ;
#24295=CARTESIAN_POINT ( 'NONE',  ( 5.600102540861260358, 0.8850759393619503923, -1.982774263332246489 ) ) ;
#24297=CARTESIAN_POINT ( 'NONE',  ( -0.1177638760072839408, -2.117013592363240271, -0.04492315971119444085 ) ) ;
#24298=CARTESIAN_POINT ( 'NONE',  ( 3.312500000000002220, 1.451031289061251339, 1.451031289060983998 ) ) ;
#24299=CARTESIAN_POINT ( 'NONE',  ( 6.827182134110199918, 0.5620517916639695688, 2.240906645742099190 ) ) ;
#24300=CARTESIAN_POINT ( 'NONE',  ( 4.102502470231626397, -0.6033306519132185519, -1.829551733875626862 ) ) ;
#24301=CARTESIAN_POINT ( 'NONE',  ( 1.577126836321657954, -1.567749618368704967, 1.573888218047289067 ) ) ;
#24306=CARTESIAN_POINT ( 'NONE',  ( 3.862163208519187929, 0.7476031731964963845, -2.091851990882629408 ) ) ;
#24312=CARTESIAN_POINT ( 'NONE',  ( 1.846327496167538884, 0.3419342931599393398, -1.987046799686801757 ) ) ;
#24314=CARTESIAN_POINT ( 'NONE',  ( 0.3388347341246043531, -1.999784422754165458, -0.5045462532434812353 ) ) ;
#24317=CARTESIAN_POINT ( 'NONE',  ( 0.02850758872123548837, -1.683968158181762043, 0.7450552726024004535 ) ) ;
#24320=CARTESIAN_POINT ( 'NONE',  ( 1.369957856843624366, -1.128201996292097498, 1.363478919461190708 ) ) ;
#24321=CARTESIAN_POINT ( 'NONE',  ( 0.6158615555539399544, 0.1511424999406512648, 2.010826230049263863 ) ) ;
#24322=CARTESIAN_POINT ( 'NONE',  ( 0.1515692981730529243, 0.7036590017722235135, 1.701685288394996665 ) ) ;
#24323=CARTESIAN_POINT ( 'NONE',  ( 3.931398753607476593, -1.581038262191627686, -1.660111252351449185 ) ) ;
#24324=CARTESIAN_POINT ( 'NONE',  ( 2.712652182946372559, -0.1802803596865458491, 1.832282175343015407 ) ) ;
#24327=CARTESIAN_POINT ( 'NONE',  ( 3.293790705515726280, -0.7410340593078695859, 1.668602820345471027 ) ) ;
#24328=CARTESIAN_POINT ( 'NONE',  ( 3.674454069786535548, 1.462445212485608437, 1.388486266691544957 ) ) ;
#24330=CARTESIAN_POINT ( 'NONE',  ( 3.292113192954935208, -0.9186832275986864804, 2.067785417532372438 ) ) ;
#24332=CARTESIAN_POINT ( 'NONE',  ( 5.473694172853372564, 2.030421858957079273, -0.5587401243299906506 ) ) ;
#24334=CARTESIAN_POINT ( 'NONE',  ( 1.961466609329724164, 1.720096886549182136, 1.151944459977225055 ) ) ;
#24337=CARTESIAN_POINT ( 'NONE',  ( 6.199870563505585963, 1.461971410283597894, 1.536153618249151309 ) ) ;
#24339=CARTESIAN_POINT ( 'NONE',  ( 0.7856181369204550125, 1.292946451617222436, 1.428335531958953464 ) ) ;
#24346=CARTESIAN_POINT ( 'NONE',  ( 0.7916362837351547110, -0.06200823681477837107, -2.220726283632424192 ) ) ;
#24347=CARTESIAN_POINT ( 'NONE',  ( 1.870285774507766119, 1.081916120455215902, 1.806640566525853808 ) ) ;
#24350=CARTESIAN_POINT ( 'NONE',  ( 6.578945215809504532, 1.736110340762307969, 0.6705269824554618285 ) ) ;
#24352=CARTESIAN_POINT ( 'NONE',  ( -0.02299388927988389730, 0.001624902753813084553, -1.910968047046639695 ) ) ;
#24355=CARTESIAN_POINT ( 'NONE',  ( 0.2816890862925770511, 0.2015970107726860194, -2.110973810222869229 ) ) ;
#24358=CARTESIAN_POINT ( 'NONE',  ( 3.367582429956605061, -0.3852447139683997657, 1.923494667983568718 ) ) ;
#24359=CARTESIAN_POINT ( 'NONE',  ( 2.360439101503517101, 0.9236781337260314695, 1.954550705658316456 ) ) ;
#24363=CARTESIAN_POINT ( 'NONE',  ( 3.415673062852276232, 1.103011313415346306, -1.346137666936922717 ) ) ;
#24367=CARTESIAN_POINT ( 'NONE',  ( 2.636092105226188309, 0.1017362925337349233, -2.013677536115268563 ) ) ;
#24368=CARTESIAN_POINT ( 'NONE',  ( 0.07536363704235565786, 7.629137130509072051, -2.744199452819145346 ) ) ;
#24369=CARTESIAN_POINT ( 'NONE',  ( 0.3390366800232989530, 0.3710982241871863541, 2.129449491308422537 ) ) ;
#24370=CARTESIAN_POINT ( 'NONE',  ( 2.500799400523348037, 1.584503739761052188, -1.172863459551294341 ) ) ;
#24378=CARTESIAN_POINT ( 'NONE',  ( 2.561199701127094830, -1.677907875943387639, 1.123823742627054312 ) ) ;
#24380=CARTESIAN_POINT ( 'NONE',  ( 5.807753868445137080, -0.5680028841938968842, 2.236484270104825089 ) ) ;
#24381=FACE_OUTER_BOUND ( 'NONE', #158071, .T. ) ;
#24382=CARTESIAN_POINT ( 'NONE',  ( 2.606241817087478374, 1.961221450604538008, 0.05310280016677935283 ) ) ;
#24384=CARTESIAN_POINT ( 'NONE',  ( 0.07093568767341934533, -0.9480374005119349690, 1.779628194860154222 ) ) ;
#24386=CARTESIAN_POINT ( 'NONE',  ( 2.554045646286424276, 1.136978842527110123, 1.786019645988563997 ) ) ;
#24389=CARTESIAN_POINT ( 'NONE',  ( 1.816098422328410900, 1.717562825535594140, 0.6636192267199734207 ) ) ;
#24393=CARTESIAN_POINT ( 'NONE',  ( 3.762070191281779774, 0.7111978290502696254, -1.997938288694045550 ) ) ;
#24394=CARTESIAN_POINT ( 'NONE',  ( 6.703083108286362446, -0.4264415456523527603, 1.901745634116110084 ) ) ;
#24398=CARTESIAN_POINT ( 'NONE',  ( 4.657529158609388986, 0.4554517582456064084, -2.009643979410648651 ) ) ;
#24400=CARTESIAN_POINT ( 'NONE',  ( 1.311775528174640604, 1.236260529797410301, -1.364685630449238740 ) ) ;
#24405=CARTESIAN_POINT ( 'NONE',  ( 0.5576012004645107822, -1.866542136390366036, -1.177153700605698461 ) ) ;
#24406=CARTESIAN_POINT ( 'NONE',  ( 3.339431287149054572, -1.996970876468142864, 1.063245685667679519 ) ) ;
#24408=CARTESIAN_POINT ( 'NONE',  ( 3.146531925530637430, 1.768428357263505557, 0.3923012617871086682 ) ) ;
#24409=EDGE_CURVE ( 'NONE', #90194, #190431, #186518, .T. ) ;
#24410=CARTESIAN_POINT ( 'NONE',  ( 2.729585477426241802, 0.6851132086851609015, -1.789222977413899462 ) ) ;
#24411=CARTESIAN_POINT ( 'NONE',  ( 3.859880467719906783, -0.6038372105774907350, 1.980330894321411517 ) ) ;
#24414=CARTESIAN_POINT ( 'NONE',  ( 2.957844615808038480, 1.962099266425470390, -0.1918489139557562340 ) ) ;
#24415=CARTESIAN_POINT ( 'NONE',  ( 0.8504600536136133204, 0.5560621936452102565, 1.844401357902447414 ) ) ;
#24416=CARTESIAN_POINT ( 'NONE',  ( 3.836663719693265584, 0.2738035037005565053, 1.850374562403465983 ) ) ;
#24417=CARTESIAN_POINT ( 'NONE',  ( 2.104549495715298590, -2.307096348898482585, 0.05917499873058817972 ) ) ;
#24418=CARTESIAN_POINT ( 'NONE',  ( 3.226847753617521963, -1.718569378881330989, -0.7146659259855172586 ) ) ;
#24423=CARTESIAN_POINT ( 'NONE',  ( 0.5925747745999773164, -2.090437052192719136, -0.2555399532009738350 ) ) ;
#24429=CARTESIAN_POINT ( 'NONE',  ( 2.092179824929023102, 1.308410154019133076, 1.668721082780571408 ) ) ;
#24431=CARTESIAN_POINT ( 'NONE',  ( 0.8791727066333665519, -1.827835516345464484, -0.8596444897858869227 ) ) ;
#24436=CARTESIAN_POINT ( 'NONE',  ( 1.317891493549529391, -2.109231647155560108, 0.4722262556789079135 ) ) ;
#24441=CARTESIAN_POINT ( 'NONE',  ( 6.175017591530616023, 1.752142144017948100, -0.9981200475188132248 ) ) ;
#24443=CARTESIAN_POINT ( 'NONE',  ( 6.603094310190187777, -0.4545541770063685760, 2.048106021177148683 ) ) ;
#24445=CARTESIAN_POINT ( 'NONE',  ( 0.7786449305766733886, -1.254482527970951056, 1.882701536962180677 ) ) ;
#24450=CARTESIAN_POINT ( 'NONE',  ( 1.071739250477701466, -0.8599075215434035524, 1.711803488807943197 ) ) ;
#24454=CARTESIAN_POINT ( 'NONE',  ( 2.402614999361089243, 1.385809671090399986, -1.026769200382530167 ) ) ;
#24457=CARTESIAN_POINT ( 'NONE',  ( 0.4030913312595973408, -0.4806107285681981423, 1.703151836983556988 ) ) ;
#24459=CARTESIAN_POINT ( 'NONE',  ( 1.770182950735105898, 2.007541250849652847, -0.1504272076729237795 ) ) ;
#24460=CARTESIAN_POINT ( 'NONE',  ( 4.524592175135637717, 1.360519573838222085, -1.737388959189074100 ) ) ;
#24465=CARTESIAN_POINT ( 'NONE',  ( 3.862070080935349203, 0.7130468835700142227, -1.997148454185311506 ) ) ;
#24466=CARTESIAN_POINT ( 'NONE',  ( 3.814077502958601595, 1.076299547611740293, -1.704950967544152984 ) ) ;
#24467=CARTESIAN_POINT ( 'NONE',  ( 3.691515636560299463, 1.703854809669336001, -0.6157217382992925536 ) ) ;
#24471=CARTESIAN_POINT ( 'NONE',  ( 1.129532124359374334, -1.183843481993757774, -1.448407549327054955 ) ) ;
#24472=CARTESIAN_POINT ( 'NONE',  ( 6.287720257080702702, 1.262826302610157381, 1.318732360701305062 ) ) ;
#24479=CARTESIAN_POINT ( 'NONE',  ( 4.188685576152741064, 1.555700494002542067, -1.282988152656767911 ) ) ;
#24483=CARTESIAN_POINT ( 'NONE',  ( 3.867525618572264623, -1.764951123045129577, -1.175235903013646332 ) ) ;
#24484=CARTESIAN_POINT ( 'NONE',  ( -0.02948999725178608200, 2.884818527723536530, -2.415019744152223868 ) ) ;
#24486=CARTESIAN_POINT ( 'NONE',  ( 4.481683897012714191, 1.285251931988955709, 1.494896804799286993 ) ) ;
#24489=CARTESIAN_POINT ( 'NONE',  ( 0.08813964471556486047, 1.162479488604960753, 1.643474645366525877 ) ) ;
#24490=EDGE_LOOP ( 'NONE', ( #100836, #134352, #95562, #79415 ) ) ;
#24491=CARTESIAN_POINT ( 'NONE',  ( 0.1228732512454956405, 0.3668972607131052999, 2.085061435120295847 ) ) ;
#24493=CARTESIAN_POINT ( 'NONE',  ( 1.434126425884488354, 1.231690216755284562, 1.664001042209894088 ) ) ;
#24498=CARTESIAN_POINT ( 'NONE',  ( 3.556657146437085970, -1.843967315269653628, -0.9851420625589295543 ) ) ;
#24502=CARTESIAN_POINT ( 'NONE',  ( 1.940199132888191791, 1.805219978825555627, 0.2711003711317952480 ) ) ;
#24503=CARTESIAN_POINT ( 'NONE',  ( 1.611653755202663518, -0.6102688749147866520, 1.705724428093706946 ) ) ;
#24505=CARTESIAN_POINT ( 'NONE',  ( 5.479209177496175087, -0.05098606815037013545, -2.206463706674952618 ) ) ;
#24507=CARTESIAN_POINT ( 'NONE',  ( 3.821466819111440927, -0.1649144712266135959, 2.200675313789305143 ) ) ;
#24510=( BOUNDED_SURFACE ( )  B_SPLINE_SURFACE ( 3, 3, ( 
 ( #98415, #35537, #117931, #183925, #65875, #165544, #198033, #214244, #180725, #148242, #877 ),
 ( #18209, #200159, #134150, #116852, #1948, #85363, #33408, #34472, #202286, #32350, #3018 ),
 ( #151445, #149296, #17137, #82150, #133083, #100544, #84293, #168746, #4083, #20350, #150378 ),
 ( #66943, #101614, #132023, #114727, #68010, #199081, #115786, #167681, #19281, #69086, #99486 ),
 ( #164479, #135207, #52864, #184976, #50727, #36601, #70154, #136266, #16066, #49663, #83214 ),
 ( #181774, #87511, #105934, #38755, #8375, #89657, #58203, #57136, #137337, #206575, #203354 ),
 ( #5145, #122231, #103762, #121157, #40906, #157856, #74458, #156789, #155710, #91799, #107012 ) ),
 .UNSPECIFIED., .T., .F., .F. ) 
 B_SPLINE_SURFACE_WITH_KNOTS ( ( 4, 3, 4 ),
 ( 4, 1, 1, 1, 1, 1, 1, 1, 4 ),
 ( 0.000000000000000000, 0.5000000000000000000, 1.000000000000000000 ),
 ( 0.000000000000000000, 0.2255619619413396781, 0.3975297875667437308, 0.5250373104567740423, 0.6172314665434700531, 0.6832587661106447330, 0.7322037845459880012, 0.7729093456892226488, 1.000000000000000000 ),
 .UNSPECIFIED. ) 
 GEOMETRIC_REPRESENTATION_ITEM ( )  RATIONAL_B_SPLINE_SURFACE ( (
 ( 1.000000000000000000, 1.000000000000000000, 1.000000000000000444, 0.9999999999999996669, 1.000000000000000222, 0.9999999999999996669, 1.000000000000000444, 1.000000000000000000, 1.000000000000000000, 1.000000000000000000, 1.000000000000000000),
 ( 0.3333333333333333703, 0.3333333333333333703, 0.3333333333333334814, 0.3333333333333332038, 0.3333333333333333703, 0.3333333333333332593, 0.3333333333333334814, 0.3333333333333333703, 0.3333333333333334814, 0.3333333333333333703, 0.3333333333333333703),
 ( 0.3333333333333333703, 0.3333333333333333703, 0.3333333333333334814, 0.3333333333333332038, 0.3333333333333333703, 0.3333333333333332593, 0.3333333333333334814, 0.3333333333333333703, 0.3333333333333334814, 0.3333333333333333703, 0.3333333333333333703),
 ( 1.000000000000000000, 1.000000000000000000, 1.000000000000000444, 0.9999999999999996669, 1.000000000000000222, 0.9999999999999996669, 1.000000000000000444, 1.000000000000000000, 1.000000000000000000, 1.000000000000000000, 1.000000000000000000),
 ( 0.3333333333333333703, 0.3333333333333333703, 0.3333333333333334814, 0.3333333333333332038, 0.3333333333333333703, 0.3333333333333332593, 0.3333333333333334814, 0.3333333333333333703, 0.3333333333333334814, 0.3333333333333333703, 0.3333333333333333703),
 ( 0.3333333333333333703, 0.3333333333333333703, 0.3333333333333334814, 0.3333333333333332038, 0.3333333333333333703, 0.3333333333333332593, 0.3333333333333334814, 0.3333333333333333703, 0.3333333333333334814, 0.3333333333333333703, 0.3333333333333333703),
 ( 1.000000000000000000, 1.000000000000000000, 1.000000000000000444, 0.9999999999999996669, 1.000000000000000222, 0.9999999999999996669, 1.000000000000000444, 1.000000000000000000, 1.000000000000000000, 1.000000000000000000, 1.000000000000000000) ) ) 
 REPRESENTATION_ITEM ( '' )  SURFACE ( )  );
#24511=CARTESIAN_POINT ( 'NONE',  ( 3.316961667764028121, 1.505919282548912719, -1.178437403786938731 ) ) ;
#24513=CARTESIAN_POINT ( 'NONE',  ( 5.143061708805018561, -0.2499388813127951525, -2.055141626981969338 ) ) ;
#24516=CARTESIAN_POINT ( 'NONE',  ( 5.530878137806295669, -1.981686641427220286, 0.9361944923952856268 ) ) ;
#24527=CARTESIAN_POINT ( 'NONE',  ( 5.278213287142951238, -1.102824678039602269, -1.751873656341627505 ) ) ;
#24528=CARTESIAN_POINT ( 'NONE',  ( 4.318917837333097864, 1.761897194459721927, 0.7795765077616281236 ) ) ;
#24529=CARTESIAN_POINT ( 'NONE',  ( 6.538674910786447469, -1.636584463124007627, 1.342808005693174156 ) ) ;
#24534=CARTESIAN_POINT ( 'NONE',  ( 0.07648947921621782053, -2.126777779243053779, -0.5280787695999613618 ) ) ;
#24535=CARTESIAN_POINT ( 'NONE',  ( 5.549374350267230582, -1.441814640532925074, -1.119852386600270311 ) ) ;
#24542=CARTESIAN_POINT ( 'NONE',  ( 2.471991059931688106, -1.762569054296094340, -0.5325411743367302053 ) ) ;
#24543=CARTESIAN_POINT ( 'NONE',  ( 5.888937080504050847, -1.913070152547487579, -0.6273127349021755395 ) ) ;
#24544=CARTESIAN_POINT ( 'NONE',  ( 1.001802975355575054, 2.264736134964080438, 0.3911735967057332064 ) ) ;
#24545=CARTESIAN_POINT ( 'NONE',  ( 6.596542563702321615, 1.939940506139478327, 0.2910815776849539627 ) ) ;
#24547=DIRECTION ( 'NONE',  ( 2.949029909160572061E-17, 1.000000000000000000, -8.673600428462429131E-15 ) ) ;
#24549=CARTESIAN_POINT ( 'NONE',  ( 0.8364851226981102617, -1.151554295457988930, 1.720357586142134076 ) ) ;
#24551=CARTESIAN_POINT ( 'NONE',  ( 2.525039811729863359, -1.949768895325499463, 0.7551890176837258162 ) ) ;
#24552=CARTESIAN_POINT ( 'NONE',  ( 1.445950363956361340, 1.868363765441739099, 0.09516058986362013750 ) ) ;
#24553=CARTESIAN_POINT ( 'NONE',  ( 1.511092056569414366, 2.013677475703846476, 0.1017375232199163593 ) ) ;
#24557=CARTESIAN_POINT ( 'NONE',  ( 1.663200723894017852, 0.8946008992836312901, 1.492777717291964512 ) ) ;
#24562=CARTESIAN_POINT ( 'NONE',  ( 3.211258912624019857, -0.3355696072399985685, 1.691725950409156631 ) ) ;
#24563=CARTESIAN_POINT ( 'NONE',  ( 2.788834510562918645, 1.878274557074947948, -1.128960604485473862 ) ) ;
#24564=CARTESIAN_POINT ( 'NONE',  ( 5.496761087669068679, -0.5331231007881258588, -2.141394884921154151 ) ) ;
#24567=CARTESIAN_POINT ( 'NONE',  ( 2.096751143937364947, 2.146985459555655673, 0.3218790139906148040 ) ) ;
#24568=CARTESIAN_POINT ( 'NONE',  ( 0.5217476098421744979, -0.9739702522407606144, -1.544006022310390192 ) ) ;
#24570=CARTESIAN_POINT ( 'NONE',  ( 4.259064461820570635, -0.003692207519963904699, -2.117513409117043999 ) ) ;
#24571=CARTESIAN_POINT ( 'NONE',  ( 6.539320575229256249, 4.699150603835311912, 2.459441311396874941 ) ) ;
#24573=CARTESIAN_POINT ( 'NONE',  ( 4.353268756680241047, 0.5026898720560546430, -2.236438357558430123 ) ) ;
#24577=CARTESIAN_POINT ( 'NONE',  ( 0.4871770963560326240, -1.998059126451703138, -0.7104936405118513765 ) ) ;
#24584=CARTESIAN_POINT ( 'NONE',  ( 4.729138786257041538, 2.011204126674607462, 0.1455352507326590494 ) ) ;
#24586=CARTESIAN_POINT ( 'NONE',  ( 3.450102088163331082, -0.8403066601648312428, 1.883826651212586745 ) ) ;
#24588=CARTESIAN_POINT ( 'NONE',  ( -0.1409997244346088141, 7.629137130509076492, -2.600278764091648487 ) ) ;
#24592=CARTESIAN_POINT ( 'NONE',  ( 6.474583112218436298, -0.1034247314782872212, -2.189140632845664403 ) ) ;
#24593=CARTESIAN_POINT ( 'NONE',  ( 3.076796235938107138, -0.8146265060355701859, 1.844709937164576097 ) ) ;
#24594=CARTESIAN_POINT ( 'NONE',  ( 3.333393596924072444, 0.8250370302015205271, -1.646115572170883112 ) ) ;
#24596=CARTESIAN_POINT ( 'NONE',  ( 6.334959139596201716, 0.1821375521317940283, 1.816452708017932238 ) ) ;
#24597=CARTESIAN_POINT ( 'NONE',  ( 0.1417928296247125686, 0.8878553654741733192, 2.120496703859587662 ) ) ;
#24599=CARTESIAN_POINT ( 'NONE',  ( 0.5271418889439123401, 2.165442452462429834, 0.6551351998097357798 ) ) ;
#24600=CARTESIAN_POINT ( 'NONE',  ( 1.559346616682453668, -1.807134503733454078, -1.081319387842846425 ) ) ;
#24609=CARTESIAN_POINT ( 'NONE',  ( 2.232824136269210502, 1.381628265877183903, -1.608862310199298928 ) ) ;
#24610=CARTESIAN_POINT ( 'NONE',  ( 4.078556047614148028, 1.049247773278503049, 1.958029639119197585 ) ) ;
#24611=CARTESIAN_POINT ( 'NONE',  ( 1.992365796559266267, -0.5863786240636534863, -2.111471653062434672 ) ) ;
#24612=CARTESIAN_POINT ( 'NONE',  ( 0.5752038918783763943, -2.079344756725898691, -0.7397341299467049547 ) ) ;
#24614=CARTESIAN_POINT ( 'NONE',  ( 4.264078424595136418, -1.956757550135434620, 0.1421211968542570592 ) ) ;
#24620=ORIENTED_EDGE ( 'NONE', *, *, #1218, .T. ) ;
#24622=CARTESIAN_POINT ( 'NONE',  ( 3.076547362214879566, 0.9570632234598417387, 1.892448740577145738 ) ) ;
#24624=CARTESIAN_POINT ( 'NONE',  ( 5.032170685167933755, 1.114402916724830161, -1.852182961850391774 ) ) ;
#24625=CARTESIAN_POINT ( 'NONE',  ( 4.229911503591711863, 1.806553461410321582, 0.3548724298726435022 ) ) ;
#24628=CARTESIAN_POINT ( 'NONE',  ( -0.07713737713477014646, -1.067615817814296042, -1.374817276609247907 ) ) ;
#24629=CARTESIAN_POINT ( 'NONE',  ( 6.827182134110177714, 4.703275060517408512, 2.273677308227497917 ) ) ;
#24632=CARTESIAN_POINT ( 'NONE',  ( 3.889662759143839299, 1.564074849111227516, 1.492423382767386730 ) ) ;
#24634=CARTESIAN_POINT ( 'NONE',  ( 5.132185397524263060, 0.2004025303571632666, -2.006139158026089220 ) ) ;
#24636=CARTESIAN_POINT ( 'NONE',  ( 4.030267251519312310, 1.158562084521784108, -1.824840551714689507 ) ) ;
#24637=CARTESIAN_POINT ( 'NONE',  ( 4.059811131046401123, 1.956822991617146457, -0.2382644796226577599 ) ) ;
#24639=CARTESIAN_POINT ( 'NONE',  ( 1.536587678696316184, 1.135727589777148605, -2.008695742776007709 ) ) ;
#24640=CARTESIAN_POINT ( 'NONE',  ( 3.514965343742028736, 1.861552560010207191, 0.8843320499443955152 ) ) ;
#24641=CARTESIAN_POINT ( 'NONE',  ( 5.249535210367334948, 1.939651965044559390, -0.09935550175556999430 ) ) ;
#24650=CARTESIAN_POINT ( 'NONE',  ( 2.573496151666111231, 0.1090403232480302298, -2.204208057042057245 ) ) ;
#24653=CARTESIAN_POINT ( 'NONE',  ( 1.041598845562411890, 1.244476351500271472, 1.383831004058704961 ) ) ;
#24654=CARTESIAN_POINT ( 'NONE',  ( 6.539320575229274901, 4.692178491785949923, 2.665866134390063813 ) ) ;
#24659=CARTESIAN_POINT ( 'NONE',  ( 5.384640740818634086, 1.621930891500168226, -0.8712783443201176370 ) ) ;
#24661=CARTESIAN_POINT ( 'NONE',  ( 2.202092877552201067, -2.060466153685360791, 0.04932271190436626068 ) ) ;
#24667=CARTESIAN_POINT ( 'NONE',  ( 0.6552379465495603572, -1.740689658905628878, -1.102993579323052753 ) ) ;
#24670=CARTESIAN_POINT ( 'NONE',  ( 4.739718475747470627, 1.836682745182907972, 0.1304020654292817605 ) ) ;
#24675=CARTESIAN_POINT ( 'NONE',  ( 3.932405576212230525, 1.181341412803040614, -1.863887651898883613 ) ) ;
#24676=CARTESIAN_POINT ( 'NONE',  ( 0.5620833348847533717, 2.138143771118843350, -0.3165822943479515983 ) ) ;
#24678=CARTESIAN_POINT ( 'NONE',  ( 0.7207899753199145110, 1.446443371814851941, -1.251069288267861346 ) ) ;
#24679=CARTESIAN_POINT ( 'NONE',  ( 1.200408080392855181, 1.350732740426639822, -1.497504596960941958 ) ) ;
#24681=CARTESIAN_POINT ( 'NONE',  ( 1.581885565347431966, 1.542867095709683056, -1.703685752350136751 ) ) ;
#24683=CARTESIAN_POINT ( 'NONE',  ( 6.393217174440144035, -0.09883813596619006603, -1.909861267343159863 ) ) ;
#24685=CARTESIAN_POINT ( 'NONE',  ( 0.2505829665140328899, -1.505242420826727656, 1.110479572284161831 ) ) ;
#24686=CARTESIAN_POINT ( 'NONE',  ( 2.009000277268524481, 0.004839059525654776373, 2.016708403978189956 ) ) ;
#24690=CARTESIAN_POINT ( 'NONE',  ( 3.703829026103040434, -0.6115302605771840705, 2.015330080423376913 ) ) ;
#24696=CARTESIAN_POINT ( 'NONE',  ( 3.691669705439902138, 1.900360886217996370, -0.6845428438169256502 ) ) ;
#24700=CARTESIAN_POINT ( 'NONE',  ( 4.516967039858135635, 1.974289957696921949, 0.8805908171375662619 ) ) ;
#24706=CARTESIAN_POINT ( 'NONE',  ( 1.522189222387077656, 2.139176736804601298, -0.3705008953195278454 ) ) ;
#24707=CARTESIAN_POINT ( 'NONE',  ( 6.727182134110201162, 7.629137130509070275, 2.410944104600750038 ) ) ;
#24709=CARTESIAN_POINT ( 'NONE',  ( 1.030510548812729965, -1.664561007783531332, 0.7873658874757857307 ) ) ;
#24711=CARTESIAN_POINT ( 'NONE',  ( 3.404031855413204966, -0.8899279105200922357, -2.002928011436304612 ) ) ;
#24713=CARTESIAN_POINT ( 'NONE',  ( 4.135799973978175892, -1.557659423114423847, -1.641163307807387950 ) ) ;
#24720=CARTESIAN_POINT ( 'NONE',  ( 3.813518172763687986, -1.743905005666521291, 0.3001630661942331080 ) ) ;
#24722=CARTESIAN_POINT ( 'NONE',  ( 0.4816451290811329389, 1.964891932219949844, -0.7582931990086133611 ) ) ;
#24725=CARTESIAN_POINT ( 'NONE',  ( 1.240603756995876772, -1.920774042053990494, -0.4348295819559512831 ) ) ;
#24728=CARTESIAN_POINT ( 'NONE',  ( 6.345981700719151242, -1.190820116993321243, -1.365292378351635083 ) ) ;
#24733=CARTESIAN_POINT ( 'NONE',  ( 4.416781281874038179, 1.710313510141375115, 0.7581657270378170388 ) ) ;
#24736=CARTESIAN_POINT ( 'NONE',  ( 4.276279003695676373, -1.059865903354087813, -1.778221194881628220 ) ) ;
#24746=CARTESIAN_POINT ( 'NONE',  ( 3.912515228517557286, 0.7039278570535618673, 1.831416474553926310 ) ) ;
#24747=CARTESIAN_POINT ( 'NONE',  ( 2.407577179044288584, 0.4389615990625857500, 1.967586618684707522 ) ) ;
#24751=CARTESIAN_POINT ( 'NONE',  ( 2.020564968092851021, 1.743606242109306148, 0.6777753874912318954 ) ) ;
#24753=CARTESIAN_POINT ( 'NONE',  ( 3.603774441610514412, 1.461153639754816824, 1.385179026781646394 ) ) ;
#24755=CARTESIAN_POINT ( 'NONE',  ( 2.794651083563943761, 1.531546425470770245, -1.462076589042210495 ) ) ;
#24757=CARTESIAN_POINT ( 'NONE',  ( 4.457524453155742528, 1.660904245173303373, 1.235824716467534889 ) ) ;
#24759=CARTESIAN_POINT ( 'NONE',  ( 6.685487044060022477, -0.8959250478542144513, 1.887356362924677233 ) ) ;
#24760=CARTESIAN_POINT ( 'NONE',  ( 6.620655732516651071, 2.021119449029490589, 2.477762541108457839 ) ) ;
#24761=CARTESIAN_POINT ( 'NONE',  ( 5.139593076133685656, -1.292025762983131099, -1.289991942498528665 ) ) ;
#24769=CARTESIAN_POINT ( 'NONE',  ( 5.777967262743825216, 1.883199444611630691, -0.3313529498064629597 ) ) ;
#24779=CARTESIAN_POINT ( 'NONE',  ( 5.501577430365036214, -1.966641501487207622, 0.4445218866586594930 ) ) ;
#24781=CARTESIAN_POINT ( 'NONE',  ( 6.620655732516627090, 7.629137130509076492, 2.426260288887295502 ) ) ;
#24782=CARTESIAN_POINT ( 'NONE',  ( -0.1405533004718312329, 0.7798934913714054007, -1.807795836271476331 ) ) ;
#24785=CARTESIAN_POINT ( 'NONE',  ( 2.166797266485945617, 1.462705959888461971, -1.319016900598804831 ) ) ;
#24786=CARTESIAN_POINT ( 'NONE',  ( 4.921500000981174239, -1.427949280599305482, -1.423951169029838315 ) ) ;
#24788=CARTESIAN_POINT ( 'NONE',  ( 6.727182134110201162, 1.237345558575110083, 2.302850971298702198 ) ) ;
#24789=CARTESIAN_POINT ( 'NONE',  ( 4.628971764384363752, -2.004251508290517680, 0.8866568735110615940 ) ) ;
#24790=CARTESIAN_POINT ( 'NONE',  ( 2.836843495735667187, 0.2342426253194809793, 1.912026175940540140 ) ) ;
#24793=CARTESIAN_POINT ( 'NONE',  ( 0.2587985324217951244, 0.8487602207661277820, 2.037339956011213093 ) ) ;
#24799=ORIENTED_EDGE ( 'NONE', *, *, #81110, .F. ) ;
#24800=CARTESIAN_POINT ( 'NONE',  ( 6.409700764581637067, -0.8744420883355051854, -1.620376909479949390 ) ) ;
#24801=CARTESIAN_POINT ( 'NONE',  ( 2.983067126429808091, -1.860865636787402577, -0.7683904602088088565 ) ) ;
#24802=CARTESIAN_POINT ( 'NONE',  ( 5.272985406448559509, -2.287992931341980896, 0.2183071761258491283 ) ) ;
#24804=CARTESIAN_POINT ( 'NONE',  ( 2.817075279929776688, -1.616631405580427838, -0.9216590669160623639 ) ) ;
#24810=CARTESIAN_POINT ( 'NONE',  ( 5.864805775728457071, 0.1527762835577218814, -2.085202849681159876 ) ) ;
#24816=CARTESIAN_POINT ( 'NONE',  ( 5.883370885758751001, 1.591107372635025330, -0.6665480857693687478 ) ) ;
#24818=CARTESIAN_POINT ( 'NONE',  ( 1.002125825150332883, -1.692058386710117990, 0.3787823561424672469 ) ) ;
#24822=CARTESIAN_POINT ( 'NONE',  ( 5.436453865645980876, -1.212139536413152197, 1.801006579369943239 ) ) ;
#24823=CARTESIAN_POINT ( 'NONE',  ( 4.547361323050268744, -1.413013347330991598, -1.156083184146582177 ) ) ;
#24824=CARTESIAN_POINT ( 'NONE',  ( 2.114041031776827673, 1.956853317873577414, -0.1391692324632237410 ) ) ;
#24830=CARTESIAN_POINT ( 'NONE',  ( 4.090573159264241809, -1.219870178150096462, 1.734285844867427651 ) ) ;
#24831=CARTESIAN_POINT ( 'NONE',  ( 6.827182134110194589, 2.412578537245218868, 2.569476350730160785 ) ) ;
#24832=ADVANCED_FACE ( 'NONE', ( #207185 ), #89764, .F. ) ;
#24835=CARTESIAN_POINT ( 'NONE',  ( 1.516557075436252733, 0.8353943144701718726, 1.894387172633307692 ) ) ;
#24838=CARTESIAN_POINT ( 'NONE',  ( 3.352378926113183777, 0.9974692666060747115, -1.984802063203878086 ) ) ;
#24840=CARTESIAN_POINT ( 'NONE',  ( 2.022535828336795127, -2.051039051814534719, 1.038070753253451439 ) ) ;
#24842=CARTESIAN_POINT ( 'NONE',  ( 0.2858946156298440844, -1.202361161835348025, -1.550730028719159215 ) ) ;
#24846=CARTESIAN_POINT ( 'NONE',  ( 6.409700764581637067, -0.8744420883355051854, -1.620376909479949390 ) ) ;
#24848=CARTESIAN_POINT ( 'NONE',  ( 2.696000938853719830, -1.719994558248700844, -0.1292177092697097962 ) ) ;
#24849=CARTESIAN_POINT ( 'NONE',  ( 1.973842561262352469, -0.8578407463649927456, 1.825077436249371354 ) ) ;
#24850=CARTESIAN_POINT ( 'NONE',  ( 2.743178873131403961, 2.287300171779807378, -0.2288005476599272447 ) ) ;
#24851=CARTESIAN_POINT ( 'NONE',  ( 3.339431287149054572, -1.996970876468142864, 1.063245685667679519 ) ) ;
#24852=CARTESIAN_POINT ( 'NONE',  ( 5.268238656634978589, 1.036954370284940419, 1.833022835974008613 ) ) ;
#24854=CARTESIAN_POINT ( 'NONE',  ( 3.092752268530512438, 1.519777622694931773, -0.9064811718217934411 ) ) ;
#24856=CARTESIAN_POINT ( 'NONE',  ( 6.392113680008942644, -0.6066422732131382389, -2.210563551359717938 ) ) ;
#24857=CARTESIAN_POINT ( 'NONE',  ( 5.613187951484799321, -1.795345830453990654, 0.4073638586896133340 ) ) ;
#24861=CARTESIAN_POINT ( 'NONE',  ( 5.437503290160631941, 0.8905978969957989433, -2.002497223260243153 ) ) ;
#24864=CARTESIAN_POINT ( 'NONE',  ( 5.529760519541640384, 1.996289034380031913, -0.5486624943154896350 ) ) ;
#24865=CARTESIAN_POINT ( 'NONE',  ( 0.5851731681005939434, 1.651346252830317551, 1.157095189655330314 ) ) ;
#24867=CARTESIAN_POINT ( 'NONE',  ( 4.582597182753257670, -1.869065293654921023, -0.4664472792492486697 ) ) ;
#24870=CARTESIAN_POINT ( 'NONE',  ( 6.293239850429793947, -0.1054838202379469042, -2.118119863012501991 ) ) ;
#24879=CARTESIAN_POINT ( 'NONE',  ( 0.8890225878602634468, 0.1407106197201784259, 1.956863499422318631 ) ) ;
#24882=CARTESIAN_POINT ( 'NONE',  ( 5.230891786122516152, -1.846674803186045821, -0.6626716404555529349 ) ) ;
#24885=CARTESIAN_POINT ( 'NONE',  ( 6.526263005029544928, 1.249015235541932167, -1.764162671312206498 ) ) ;
#24889=CARTESIAN_POINT ( 'NONE',  ( 1.721729502718066795, -1.034818790731323990, -1.558030248997283040 ) ) ;
#24890=CARTESIAN_POINT ( 'NONE',  ( 0.4219819185556292207, -1.224561070735529444, -1.228170329033271724 ) ) ;
#24892=CARTESIAN_POINT ( 'NONE',  ( 3.790727848299980440, 1.850687065220711469, -1.173560875862532660 ) ) ;
#24893=CARTESIAN_POINT ( 'NONE',  ( 4.471882758057180496, 2.239461445850467580, -0.5561450820626266944 ) ) ;
#24894=CARTESIAN_POINT ( 'NONE',  ( 0.4443025167278572551, 2.055347410954794451, 0.1520637142833832778 ) ) ;
#24895=CARTESIAN_POINT ( 'NONE',  ( 2.290873232013816541, 1.501373485850267198, 1.231690586011934041 ) ) ;
#24899=CARTESIAN_POINT ( 'NONE',  ( 5.449516625918088053, -1.916229881892789866, 0.9086369058012438993 ) ) ;
#24901=CARTESIAN_POINT ( 'NONE',  ( 3.797500137148449362, 1.423962148579031917, -1.427936706820939872 ) ) ;
#24905=CARTESIAN_POINT ( 'NONE',  ( 1.435882461153328515, 0.9014729512111450127, -1.587519582607027635 ) ) ;
#24910=CARTESIAN_POINT ( 'NONE',  ( 5.489158015974754612, 1.818697853212094095, -0.9693054586683967910 ) ) ;
#24912=MANIFOLD_SOLID_BREP ( 'Sweep1[9]', #108812 ) ;
#24917=CARTESIAN_POINT ( 'NONE',  ( 4.547524150180999314, -1.845711718722802486, 0.8204608018674663938 ) ) ;
#24918=CARTESIAN_POINT ( 'NONE',  ( 5.162811894357514753, 0.6434298260243781487, 2.126049117748362249 ) ) ;
#24922=CARTESIAN_POINT ( 'NONE',  ( 3.995036845513312951, 1.742007986889832161, -1.100897373992800299 ) ) ;
#24923=CARTESIAN_POINT ( 'NONE',  ( 4.360000113718985659, -0.002809843368253156070, -2.016597020062675050 ) ) ;
#24932=CARTESIAN_POINT ( 'NONE',  ( 3.532577226125938274, 1.967586357134976094, -0.4389627639644277934 ) ) ;
#24933=CARTESIAN_POINT ( 'NONE',  ( 2.853255899669316697, 1.832232481769331844, -0.1808706098178694266 ) ) ;
#24935=CARTESIAN_POINT ( 'NONE',  ( 0.8566255916394946990, 2.304767657353411270, -0.1186049529825431298 ) ) ;
#24937=CARTESIAN_POINT ( 'NONE',  ( 3.479894426560462328, 1.368377867093536482, 1.673357603396708360 ) ) ;
#24939=CARTESIAN_POINT ( 'NONE',  ( 3.480086682454126557, 2.076208366568982555, 0.9861560518420305899 ) ) ;
#24940=EDGE_LOOP ( 'NONE', ( #104737, #27394, #55937, #69684 ) ) ;
#24942=CARTESIAN_POINT ( 'NONE',  ( 2.447944060942487621, 1.870205405844455049, 0.04815357881200743595 ) ) ;
#24943=CARTESIAN_POINT ( 'NONE',  ( 5.946159419501746868, 1.969187058922382993, 0.09738397392708775246 ) ) ;
#24947=CARTESIAN_POINT ( 'NONE',  ( 0.4345545588612038657, 1.130843733186673639, -1.894998796914903139 ) ) ;
#24954=CARTESIAN_POINT ( 'NONE',  ( 6.631714602856194851, -1.287423518921044341, -1.493153376739835947 ) ) ;
#24955=CARTESIAN_POINT ( 'NONE',  ( 5.602268381685036935, -2.307868969066428022, -0.005371834822459965395 ) ) ;
#24956=CARTESIAN_POINT ( 'NONE',  ( 0.1331565106231328843, 0.003911343561965873426, -1.946049565259087455 ) ) ;
#24958=CARTESIAN_POINT ( 'NONE',  ( 2.940340207046471921, -1.064325496585982078, 1.766646112275678693 ) ) ;
#24965=CARTESIAN_POINT ( 'NONE',  ( 5.635278836315742446, -0.04772081403418790974, -2.170810874590335171 ) ) ;
#24967=CARTESIAN_POINT ( 'NONE',  ( 5.724118993814841794, 1.776208094789998304, 0.4848738846057951135 ) ) ;
#24969=CARTESIAN_POINT ( 'NONE',  ( 6.720655732516646275, 4.698042323276835575, 2.488944259588221186 ) ) ;
#24972=CARTESIAN_POINT ( 'NONE',  ( 6.702048742255109381, -2.262191126150433274, 0.04724482429044154358 ) ) ;
#24977=CARTESIAN_POINT ( 'NONE',  ( 0.1176276963383571517, -0.5100272734060510293, 1.842954807014775653 ) ) ;
#24978=CARTESIAN_POINT ( 'NONE',  ( 2.201683042903946230, -1.769559083619182349, 0.04015057502057895605 ) ) ;
#24979=CARTESIAN_POINT ( 'NONE',  ( 5.936195100277483760, -1.120233448768311435, -1.672418650214458014 ) ) ;
#24981=CARTESIAN_POINT ( 'NONE',  ( 4.946364073002400552, 2.100128792357182750, 0.1576013620808654481 ) ) ;
#24983=CARTESIAN_POINT ( 'NONE',  ( 3.163600654563469838, 1.217692022474494262, 1.478743580268084390 ) ) ;
#24985=CARTESIAN_POINT ( 'NONE',  ( 3.807052887859848855, -1.611515334864065840, 1.132039114057415308 ) ) ;
#24986=CARTESIAN_POINT ( 'NONE',  ( 6.416272379866970965, -2.019260422740985828, 0.05364450914858465147 ) ) ;
#24988=CARTESIAN_POINT ( 'NONE',  ( 3.168673215318769110, -1.727878594304608217, -0.7172629358194044791 ) ) ;
#24989=CARTESIAN_POINT ( 'NONE',  ( 5.268053373232242542, 0.8548693298336268453, 1.498049451945895116 ) ) ;
#24991=CARTESIAN_POINT ( 'NONE',  ( 2.702037527177497012, -0.6914408288211832954, 2.095836555436859872 ) ) ;
#24994=CARTESIAN_POINT ( 'NONE',  ( 0.1860857499333635756, -1.268064657576525978, -1.627672589050175089 ) ) ;
#25002=CARTESIAN_POINT ( 'NONE',  ( 2.207561477879273593, -1.661462528888792090, -1.235070534849058266 ) ) ;
#25006=CARTESIAN_POINT ( 'NONE',  ( 6.358074577831472673, 0.8120454629646983724, -1.959034198684066697 ) ) ;
#25011=CARTESIAN_POINT ( 'NONE',  ( 5.835314490094169138, -1.281163661392352493, 1.556671411349755285 ) ) ;
#25012=CARTESIAN_POINT ( 'NONE',  ( 5.296063324668989658, -0.8673027158061608066, -1.708257925969633551 ) ) ;
#25014=CARTESIAN_POINT ( 'NONE',  ( 2.630644284709309666, 0.2711686948545319886, 2.174668582101045633 ) ) ;
#25016=CARTESIAN_POINT ( 'NONE',  ( 1.916128293556786044, -1.911906470838855343, 0.05044092668918254141 ) ) ;
#25020=CARTESIAN_POINT ( 'NONE',  ( 6.380470236391142080, -0.5646626916907444560, -2.040458243955853401 ) ) ;
#25022=CARTESIAN_POINT ( 'NONE',  ( 3.597287555019304861, -0.6049611382589085151, 2.001324503170316849 ) ) ;
#25024=CARTESIAN_POINT ( 'NONE',  ( 2.942113945249478668, 1.711507881387188013, 0.2129122850730424121 ) ) ;
#25037=CARTESIAN_POINT ( 'NONE',  ( 2.859786144356114779, 0.6500800702718724233, -1.690994707955698617 ) ) ;
#25041=CARTESIAN_POINT ( 'NONE',  ( 4.090334381980924583, -1.039670344891037601, 1.483205724144847748 ) ) ;
#25046=CARTESIAN_POINT ( 'NONE',  ( 4.668306603206507255, -0.7948602423475581435, -1.682893250223691517 ) ) ;
#25048=CARTESIAN_POINT ( 'NONE',  ( 1.599098272587581748, -0.2325377738172547115, 1.901345697680896007 ) ) ;
#25049=CARTESIAN_POINT ( 'NONE',  ( 1.447985623159939284, 1.823312892812560593, 0.09356915273009414058 ) ) ;
#25055=CARTESIAN_POINT ( 'NONE',  ( 6.925078400183550364, -0.007619068086212391067, 2.144148427808051594 ) ) ;
#25057=CARTESIAN_POINT ( 'NONE',  ( 6.086760365903021608, 1.896989206666617633, 0.5289026096024685986 ) ) ;
#25060=CARTESIAN_POINT ( 'NONE',  ( 1.570382428225084226, -1.985578813138744403, -0.6546124938694962703 ) ) ;
#25061=CARTESIAN_POINT ( 'NONE',  ( 0.2350025537052654601, -1.671451849548213797, 0.7345932495873632728 ) ) ;
#25063=CARTESIAN_POINT ( 'NONE',  ( 1.412830140145465263, 1.608106816955911178, 0.8641515426408912237 ) ) ;
#25064=CARTESIAN_POINT ( 'NONE',  ( 2.860232119962682784, 2.196193069775736362, -0.2169517147150926140 ) ) ;
#25065=CARTESIAN_POINT ( 'NONE',  ( 1.441514601552947417, -1.799640695080907182, 0.6472408003148700795 ) ) ;
#25067=CARTESIAN_POINT ( 'NONE',  ( 1.504289420374326447, 1.967163215448018088, 0.09980459116839916767 ) ) ;
#25068=CARTESIAN_POINT ( 'NONE',  ( 2.770961567126817737, 1.843342918492569149, -0.6114499264749191365 ) ) ;
#25072=CARTESIAN_POINT ( 'NONE',  ( 6.877813048773076865, -1.805165420234026818, 0.4518952398848713470 ) ) ;
#25076=CARTESIAN_POINT ( 'NONE',  ( 2.261505105119133052, 2.148611799745976381, -0.4309092228176118478 ) ) ;
#25077=FACE_OUTER_BOUND ( 'NONE', #40861, .T. ) ;
#25079=CARTESIAN_POINT ( 'NONE',  ( 2.894927146036041510, 1.565677646668685696, -0.9388022922067614795 ) ) ;
#25086=CARTESIAN_POINT ( 'NONE',  ( 2.262220261732431403, 0.8237980678013016034, 1.741618625116077235 ) ) ;
#25087=CARTESIAN_POINT ( 'NONE',  ( 5.559412779221331924, 1.601624451964112739, 1.132529127964493121 ) ) ;
#25096=CARTESIAN_POINT ( 'NONE',  ( 5.577033793921920335, 1.910671465402475677, 0.7975372692515869666 ) ) ;
#25099=CARTESIAN_POINT ( 'NONE',  ( 5.362068906036296490, -0.05402111011005260310, -2.298215290733228500 ) ) ;
#25103=CARTESIAN_POINT ( 'NONE',  ( 0.1820931442207155415, -1.074843934555272273, 2.024655709774853207 ) ) ;
#25106=CARTESIAN_POINT ( 'NONE',  ( 4.523342001410900259, -1.195735706813789045, -1.530077746507539027 ) ) ;
#25110=ORIENTED_EDGE ( 'NONE', *, *, #191848, .T. ) ;
#25111=CARTESIAN_POINT ( 'NONE',  ( 5.959226163113887864, -1.611951592244726950, 1.028742869173946861 ) ) ;
#25112=CARTESIAN_POINT ( 'NONE',  ( 6.159189016523521687, -1.482050057771692186, -0.8820200739605223994 ) ) ;
#25113=CARTESIAN_POINT ( 'NONE',  ( 5.594935472981866553, 1.780666063871166882, 0.9463038388278844915 ) ) ;
#25117=CARTESIAN_POINT ( 'NONE',  ( 1.587951679898065294, -2.080713178594826296, -0.2033740637906420179 ) ) ;
#25118=CARTESIAN_POINT ( 'NONE',  ( 0.3909914118310651165, 1.306912223127455919, 1.193654972778479539 ) ) ;
#25121=CARTESIAN_POINT ( 'NONE',  ( 3.451411174752341715, 0.5572527081592703047, -2.223385661236119581 ) ) ;
#25122=CARTESIAN_POINT ( 'NONE',  ( 2.079653994411820417, -1.706432041406182654, -0.3408243062450431182 ) ) ;
#25123=CARTESIAN_POINT ( 'NONE',  ( 2.760144723603759065, 0.7592700852765141839, -1.980205354017528840 ) ) ;
#25125=CARTESIAN_POINT ( 'NONE',  ( 2.477566078851959563, 1.547001316009195548, 0.7831083592614047628 ) ) ;
#25127=CARTESIAN_POINT ( 'NONE',  ( 1.908444903620472477, 0.5799682436128813512, 1.768463464005122443 ) ) ;
#25128=CARTESIAN_POINT ( 'NONE',  ( 2.647136220323087485, -0.3691774202370365354, -2.139407045683580755 ) ) ;
#25130=CARTESIAN_POINT ( 'NONE',  ( 3.714077560468319827, 1.074663192196689376, -1.706111893292367343 ) ) ;
#25131=CARTESIAN_POINT ( 'NONE',  ( 4.718750000000002665, -0.7852924748297362978, 1.895863743164184045 ) ) ;
#25133=CARTESIAN_POINT ( 'NONE',  ( 0.8680396935916842027, 0.9469273490957976769, 1.677514697326354387 ) ) ;
#25135=CARTESIAN_POINT ( 'NONE',  ( 4.183969649472300212, 2.154223736155444602, -0.5416631952432825470 ) ) ;
#25141=CARTESIAN_POINT ( 'NONE',  ( 6.539320575229294441, -0.001643797937642132567, 2.203502507913539521 ) ) ;
#25142=CARTESIAN_POINT ( 'NONE',  ( 5.178158156489047315, -1.047961880893449882, -1.658324637040713867 ) ) ;
#25146=CARTESIAN_POINT ( 'NONE',  ( 5.764971491839249396, -2.041691765312734663, -0.9750072289948004123 ) ) ;
#25149=CARTESIAN_POINT ( 'NONE',  ( 2.928243574330684496, 1.101304876339922467, 1.743887257993762763 ) ) ;
#25154=CARTESIAN_POINT ( 'NONE',  ( 4.622238261848357510, 1.152259890254858421, -1.473394524551620011 ) ) ;
#25155=CARTESIAN_POINT ( 'NONE',  ( 4.025767975679870325, -1.506360102045413596, 0.8590090823815172971 ) ) ;
#25156=CARTESIAN_POINT ( 'NONE',  ( 2.419155098189431641, -1.003372571555812831, -1.421874531148322740 ) ) ;
#25157=CARTESIAN_POINT ( 'NONE',  ( 0.5918695612782381987, -0.8180161699140885423, 2.141640516796620375 ) ) ;
#25158=CARTESIAN_POINT ( 'NONE',  ( 1.184930176456780115, -2.153272645635353033, -0.4822455307981614592 ) ) ;
#25159=CARTESIAN_POINT ( 'NONE',  ( 4.845306142872277455, 0.6545843485197681000, -1.985720288498250774 ) ) ;
#25160=CARTESIAN_POINT ( 'NONE',  ( 5.894467665742915585, 1.586334124781592969, -1.119885764912365467 ) ) ;
#25164=CARTESIAN_POINT ( 'NONE',  ( 0.9674229098759130618, -1.967888300253183953, -0.4390273639364171698 ) ) ;
#25165=EDGE_CURVE ( 'NONE', #89693, #175232, #16323, .T. ) ;
#25172=CARTESIAN_POINT ( 'NONE',  ( 4.828627627824715773, 1.747987318788373656, 0.5269492854979712648 ) ) ;
#25173=CARTESIAN_POINT ( 'NONE',  ( 1.694636308673210801, -2.196210861363355082, -0.2157497520150277459 ) ) ;
#25179=CARTESIAN_POINT ( 'NONE',  ( 1.213155585027906325, 1.648708085711389160, -1.166442415167892932 ) ) ;
#25183=CARTESIAN_POINT ( 'NONE',  ( 2.658860470891976302, 1.497794124733292431, -1.104231377384189861 ) ) ;
#25188=CARTESIAN_POINT ( 'NONE',  ( 4.248545464119923842, 0.4890907236730773766, 1.758887239191930796 ) ) ;
#25192=CARTESIAN_POINT ( 'NONE',  ( 1.106332979110283610, 0.7092076354480534306, -1.582373438193741322 ) ) ;
#25193=CARTESIAN_POINT ( 'NONE',  ( 6.122987604524110949, -1.732013368603693593, 0.6248225064409973495 ) ) ;
#25194=CARTESIAN_POINT ( 'NONE',  ( 4.547712581667567200, -1.782031661950409962, -1.466240793230636275 ) ) ;
#25196=CARTESIAN_POINT ( 'NONE',  ( 0.3685255395303523307, -1.348100972195030334, 1.558720748697209224 ) ) ;
#25197=CARTESIAN_POINT ( 'NONE',  ( 5.396019846235262207, 0.1618137187183350256, 2.292739235009821908 ) ) ;
#25200=CARTESIAN_POINT ( 'NONE',  ( 6.157094445334826638, -1.605393284960114242, -0.9600186418455139981 ) ) ;
#25202=CARTESIAN_POINT ( 'NONE',  ( 2.654443970922310214, 1.898414275235399407, 0.2300336082040748686 ) ) ;
#25204=CARTESIAN_POINT ( 'NONE',  ( 3.703933201646680828, -0.6411959742554216302, 2.111683309420588905 ) ) ;
#25205=CARTESIAN_POINT ( 'NONE',  ( 5.137957784024314911, 2.114781318005181099, -0.1070058694263714694 ) ) ;
#25208=CARTESIAN_POINT ( 'NONE',  ( 6.883263157960335832, 7.629137130509037412, 2.646189081643287810 ) ) ;
#25209=CARTESIAN_POINT ( 'NONE',  ( -0.2110808730067273986, 0.0005491059566040295322, -1.796958327270286704 ) ) ;
#25212=CARTESIAN_POINT ( 'NONE',  ( 2.450585703787050651, 2.307050653106942573, 0.05676454813420374335 ) ) ;
#25213=CARTESIAN_POINT ( 'NONE',  ( 3.191801227909254912, -1.315628469008291557, -1.455533501494077342 ) ) ;
#25215=CARTESIAN_POINT ( 'NONE',  ( 6.895384927792009400, -1.844987169530726723, 0.9222207602926129066 ) ) ;
#25219=CARTESIAN_POINT ( 'NONE',  ( 5.366422816783521732, -1.968444216653497003, -0.4370823996120917765 ) ) ;
#25225=CARTESIAN_POINT ( 'NONE',  ( 1.534277631021633059, 1.291084678180357104, 1.745351423456573015 ) ) ;
#25230=CARTESIAN_POINT ( 'NONE',  ( 1.177107960601676551, -0.04769765464058715876, -2.060389331245067179 ) ) ;
#25232=CARTESIAN_POINT ( 'NONE',  ( 6.727182134110196721, 3.701357331967893405, 2.425430364167603603 ) ) ;
#25236=CARTESIAN_POINT ( 'NONE',  ( 3.246637215680724164, 1.866209232881730573, 0.4165188312477489663 ) ) ;
#25238=CARTESIAN_POINT ( 'NONE',  ( 4.873781607783202574, 1.020544065373253817, 1.445763320596996193 ) ) ;
#25243=CARTESIAN_POINT ( 'NONE',  ( 0.1982580178685423022, 1.319089833320963079, -1.389493073782912091 ) ) ;
#25245=CARTESIAN_POINT ( 'NONE',  ( 0.4321921490204432281, 1.190796696626210682, 1.693455153822187587 ) ) ;
#25247=CARTESIAN_POINT ( 'NONE',  ( 6.614126560844452385, -0.8839695271746010885, -1.648598838400926692 ) ) ;
#25248=CARTESIAN_POINT ( 'NONE',  ( 3.351995281737112364, 1.825872481133209879, -0.0009662468829912954560 ) ) ;
#25249=CARTESIAN_POINT ( 'NONE',  ( 5.795608111622330583, 1.668732747960173235, 1.444295198399044855 ) ) ;
#25252=CARTESIAN_POINT ( 'NONE',  ( 2.629405133799759486, 0.1038056934173016560, -2.060197576267445818 ) ) ;
#25257=CARTESIAN_POINT ( 'NONE',  ( 0.5444778865218367070, 2.155786741090206959, 0.1595364878888144988 ) ) ;
#25259=CARTESIAN_POINT ( 'NONE',  ( 5.213363469605923228, -1.747142239327776903, -1.110534646669825376 ) ) ;
#25261=CARTESIAN_POINT ( 'NONE',  ( 3.356853517036356038, -1.639235867460669294, 1.409173823127254144 ) ) ;
#25263=CARTESIAN_POINT ( 'NONE',  ( 2.895180478094826704, -0.1506588039767979559, -2.014126839200135688 ) ) ;
#25264=CARTESIAN_POINT ( 'NONE',  ( 1.908577322519442454, 0.6123880975643315461, 1.863924812142327525 ) ) ;
#25270=CARTESIAN_POINT ( 'NONE',  ( 1.165250339122084533, 1.861343190080061882, -0.7762330495894869120 ) ) ;
#25272=CARTESIAN_POINT ( 'NONE',  ( 6.040607902356621040, -1.852314659301614874, 1.170993205287726768 ) ) ;
#25274=CARTESIAN_POINT ( 'NONE',  ( 6.170165192347925043, 1.906784905861274249, -0.1475879885542986658 ) ) ;
#25278=CARTESIAN_POINT ( 'NONE',  ( 3.392203995056555232, -0.8197896108859267228, -1.842441248588816860 ) ) ;
#25281=CARTESIAN_POINT ( 'NONE',  ( 6.581054485068423610, -0.09077197429533871709, -1.722499283940544634 ) ) ;
#25286=CARTESIAN_POINT ( 'NONE',  ( 4.674985431947434655, 0.001863223488791227334, -1.870726058175266715 ) ) ;
#25289=CARTESIAN_POINT ( 'NONE',  ( 2.518496159030516601, 0.8812310945605882351, 1.873447404777649261 ) ) ;
#25293=CARTESIAN_POINT ( 'NONE',  ( 0.2108110590392465178, 1.506053368259860248, -1.006445417241896845 ) ) ;
#25298=CARTESIAN_POINT ( 'NONE',  ( 1.504273306027693602, 1.959471947749168663, 0.09963418240711149898 ) ) ;
#25301=CARTESIAN_POINT ( 'NONE',  ( 5.554270809058080793, -1.211575977211576172, 1.483806794280813302 ) ) ;
#25307=CARTESIAN_POINT ( 'NONE',  ( 2.711983997553392811, -2.138339778157403615, 0.3160903847422362745 ) ) ;
#25311=CARTESIAN_POINT ( 'NONE',  ( 6.317409609008932669, -0.2203418483949574069, 1.812181760327068680 ) ) ;
#25314=CARTESIAN_POINT ( 'NONE',  ( 1.264844077314925652, -1.780367465076490019, -0.8468111885079774304 ) ) ;
#25315=CARTESIAN_POINT ( 'NONE',  ( 3.392734571251673881, -1.844325299564765652, -0.5055192353106837677 ) ) ;
#25318=CARTESIAN_POINT ( 'NONE',  ( 5.142998410927586583, -0.2390059684120172390, -1.954905448695958059 ) ) ;
#25320=CARTESIAN_POINT ( 'NONE',  ( 6.251511512115349056, 1.936530502255621622, -0.1475284815631947022 ) ) ;
#25324=CARTESIAN_POINT ( 'NONE',  ( 6.345950370838200350, -1.386202306585911925, -1.604841549997563455 ) ) ;
#25326=CARTESIAN_POINT ( 'NONE',  ( 4.389254143344611947, -0.003399479254035177832, -1.912461472815998320 ) ) ;
#25327=EDGE_LOOP ( 'NONE', ( #122261, #35315, #87118, #208741 ) ) ;
#25329=CARTESIAN_POINT ( 'NONE',  ( 0.7455094363101981703, -1.891729906373079029, 1.136061337225414913 ) ) ;
#25331=CARTESIAN_POINT ( 'NONE',  ( 6.147140879040452255, 0.1997598139246952731, 2.003170966399501651 ) ) ;
#25333=CARTESIAN_POINT ( 'NONE',  ( 5.953692858212231265, 0.5253669772854427933, -1.748464709795935157 ) ) ;
#25334=CARTESIAN_POINT ( 'NONE',  ( 2.313015868914463091, -1.601887806243259771, 1.311650804931147274 ) ) ;
#25338=CARTESIAN_POINT ( 'NONE',  ( 6.719622092096638966, -1.813896567892055112, 0.4569536213836836169 ) ) ;
#25343=DIRECTION ( 'NONE',  ( -1.000000000000000000, 1.014813233446432150E-15, 1.972152263052529514E-31 ) ) ;
#25345=CARTESIAN_POINT ( 'NONE',  ( 6.925078400183515726, -0.002206826874838820583, 1.955452213090567160 ) ) ;
#25347=CARTESIAN_POINT ( 'NONE',  ( 5.098194074801078557, -0.2466363661708069477, 1.716370243172520516 ) ) ;
#25349=CARTESIAN_POINT ( 'NONE',  ( 2.395452669547156077, -1.851176756146424074, 0.9269567275110508486 ) ) ;
#25350=CARTESIAN_POINT ( 'NONE',  ( 3.462624114536147157, -2.041159069107215007, -0.5622701121768166610 ) ) ;
#25353=CARTESIAN_POINT ( 'NONE',  ( 2.201947278869041291, 0.7584239558163529127, -1.817761916770490149 ) ) ;
#25357=CARTESIAN_POINT ( 'NONE',  ( 4.101757505036166762, -2.286240945789700607, 0.1669829803510776423 ) ) ;
#25358=CARTESIAN_POINT ( 'NONE',  ( 2.033574986395149775, -1.191784744093337123, -1.383114941912518159 ) ) ;
#25363=CARTESIAN_POINT ( 'NONE',  ( 3.410405542056849981, -2.011076457950426555, -0.09466423678533388009 ) ) ;
#25364=CARTESIAN_POINT ( 'NONE',  ( 2.483191118468269565, -0.005009705968514814069, 1.961936380092830223 ) ) ;
#25368=CARTESIAN_POINT ( 'NONE',  ( 5.841762345275034463, 2.088193589346263312, 0.1035180442379990684 ) ) ;
#25369=CARTESIAN_POINT ( 'NONE',  ( 4.803428869931958722, -0.4704684023625771983, 1.706073424435787134 ) ) ;
#25371=CARTESIAN_POINT ( 'NONE',  ( 0.5686479265839607944, -2.064760635122906418, -0.7346842419702694915 ) ) ;
#25372=CARTESIAN_POINT ( 'NONE',  ( 5.859256971114414014, 1.713395515214741538, -0.3040290152411839752 ) ) ;
#25375=CARTESIAN_POINT ( 'NONE',  ( 6.557281991921043662, -1.419039031320767474, 1.809608378690949149 ) ) ;
#25377=CARTESIAN_POINT ( 'NONE',  ( 5.044171318280882055, 1.617313383883935529, -0.6254187727454744161 ) ) ;
#25379=CARTESIAN_POINT ( 'NONE',  ( 5.617690636765501289, 0.4290425436993560715, -2.128212118068722347 ) ) ;
#25381=CARTESIAN_POINT ( 'NONE',  ( 0.2689693067343159605, -0.2660441693766130711, -2.100534484541769498 ) ) ;
#25382=CARTESIAN_POINT ( 'NONE',  ( 3.718750000000002220, -0.7852924748297895885, 1.895863743164163617 ) ) ;
#25385=CARTESIAN_POINT ( 'NONE',  ( 4.032187520235196665, 1.031363847994439142, -1.626874456138996949 ) ) ;
#25387=CARTESIAN_POINT ( 'NONE',  ( 0.6982527715983916083, 1.495984496936525021, 1.642170479989105480 ) ) ;
#25388=ORIENTED_EDGE ( 'NONE', *, *, #104171, .F. ) ;
#25392=CARTESIAN_POINT ( 'NONE',  ( 2.209928731909744481, 1.719286606775907611, 1.406518386542881638 ) ) ;
#25398=CARTESIAN_POINT ( 'NONE',  ( 0.6861729220449981348, 1.650083401500940239, 1.158686392676591570 ) ) ;
#25400=CARTESIAN_POINT ( 'NONE',  ( 6.391093295415360309, 0.1985076180841711668, 2.053089703019762791 ) ) ;
#25403=CARTESIAN_POINT ( 'NONE',  ( 0.8953273879380260203, -0.6444125412686675380, 1.648433012593934155 ) ) ;
#25404=CARTESIAN_POINT ( 'NONE',  ( 0.2818752512256904597, 1.674885806461807958, -1.122501178855893400 ) ) ;
#25405=CARTESIAN_POINT ( 'NONE',  ( 5.970193594734433340, -1.655480682217812083, -0.5374289683400793605 ) ) ;
#25406=CARTESIAN_POINT ( 'NONE',  ( 4.652058317211603011, 0.8762739730861779375, 2.118468771859642441 ) ) ;
#25408=CARTESIAN_POINT ( 'NONE',  ( 2.027068592762204080, -1.202062398780713748, -1.394650109237540070 ) ) ;
#25410=CARTESIAN_POINT ( 'NONE',  ( 3.223480179809079971, -1.759765543241718966, 0.4855387900214308550 ) ) ;
#25411=CARTESIAN_POINT ( 'NONE',  ( 3.604138833494671346, -0.1455340571130462057, 2.011204217620660817 ) ) ;
#25413=CARTESIAN_POINT ( 'NONE',  ( 1.833286743572108968, 0.2227676567047157941, 2.251508545315301646 ) ) ;
#25415=CARTESIAN_POINT ( 'NONE',  ( 5.297925755477892906, -0.7609016685872365127, 1.963875245004148562 ) ) ;
#25417=CARTESIAN_POINT ( 'NONE',  ( 2.998552181135270001, 2.054425100943928051, 0.2560010573490826835 ) ) ;
#25420=CARTESIAN_POINT ( 'NONE',  ( 4.987034407221377030, -1.996844880220369545, -0.7138980100366009163 ) ) ;
#25422=CARTESIAN_POINT ( 'NONE',  ( 0.7504602152685091454, 0.5580118324238073635, 1.843911685078497120 ) ) ;
#25429=CARTESIAN_POINT ( 'NONE',  ( 5.941668366282724101, -1.996146358238064522, 0.7160658055916299114 ) ) ;
#25430=CARTESIAN_POINT ( 'NONE',  ( 1.694499644457616583, -2.095784359944006248, -0.2068371402374687973 ) ) ;
#25433=CARTESIAN_POINT ( 'NONE',  ( 6.455886261557550299, -0.6278800607443285609, 1.751925260802848827 ) ) ;
#25441=CARTESIAN_POINT ( 'NONE',  ( 2.840232074097197579, -1.010955899468408248, 1.681206195012739046 ) ) ;
#25442=CARTESIAN_POINT ( 'NONE',  ( 2.518638242371186386, 1.412657066830936392, -1.636333507658905173 ) ) ;
#25446=CARTESIAN_POINT ( 'NONE',  ( 3.644249385861945800, -1.421566135898670646, 1.003629588703761621 ) ) ;
#25451=CARTESIAN_POINT ( 'NONE',  ( 2.723982329760873178, -1.752761823190003287, -0.9961495992579154635 ) ) ;
#25452=CARTESIAN_POINT ( 'NONE',  ( 6.825078400183575589, -0.005632053428735600553, 2.144262460745151255 ) ) ;
#25453=CARTESIAN_POINT ( 'NONE',  ( 0.2335756976950612018, -1.975703151049061024, 0.8776370805363906680 ) ) ;
#25455=CARTESIAN_POINT ( 'NONE',  ( 1.867985033921132798, 1.011920226373051346, 1.691812110196472041 ) ) ;
#25458=CARTESIAN_POINT ( 'NONE',  ( 6.170165192347925931, 1.906784905861274693, -0.1475879885542986936 ) ) ;
#25463=CARTESIAN_POINT ( 'NONE',  ( 1.858075313305072473, 0.7708903827231723405, -1.866970155298973921 ) ) ;
#25465=CARTESIAN_POINT ( 'NONE',  ( 5.262836394871557744, -1.675821390925121168, 1.586616667910417888 ) ) ;
#25467=CARTESIAN_POINT ( 'NONE',  ( 2.518345088137901477, 0.8342845254802437882, 1.775630740545742992 ) ) ;
#25469=CARTESIAN_POINT ( 'NONE',  ( 0.4049229342097167006, -1.081068455937021611, -1.701946057285643965 ) ) ;
#25470=B_SPLINE_CURVE_WITH_KNOTS ( 'NONE', 3,
 ( #6293, #54004, #120142, #106008, #172029, #3084, #23622, #37753, #103827, #169875, #87574 ),
 .UNSPECIFIED., .F., .F.,
 ( 4, 1, 1, 1, 1, 1, 1, 1, 4 ),
 ( 0.000000000000000000, 0.2256777920876190668, 0.3978457394851813711, 0.5256768607792676740, 0.6183602023682204241, 0.6850295134299612121, 0.7345374503969632762, 0.7752450576501028756, 1.000000000000000000 ),
 .UNSPECIFIED. ) ;
#25472=CARTESIAN_POINT ( 'NONE',  ( 1.798220840057991543, -1.003180963283013982, -1.864648404631663148 ) ) ;
#25475=CARTESIAN_POINT ( 'NONE',  ( 1.956743257466783570, 0.3155556147324266036, -1.813728304320901596 ) ) ;
#25479=CARTESIAN_POINT ( 'NONE',  ( 3.094099843433151253, 1.348383549611749332, 1.636666742212993686 ) ) ;
#25481=CARTESIAN_POINT ( 'NONE',  ( 0.5328340850149284602, -1.300071877079148841, -1.303948673260245439 ) ) ;
#25485=CARTESIAN_POINT ( 'NONE',  ( 4.165347332011271497, 0.2559277237221342371, -2.044777286818760142 ) ) ;
#25487=CARTESIAN_POINT ( 'NONE',  ( 0.8723036553972834950, -0.04505207493780280514, -1.840872848514919502 ) ) ;
#25489=CARTESIAN_POINT ( 'NONE',  ( -0.02224634325198419221, -0.007204097619508199532, -2.289079630542793620 ) ) ;
#25492=CARTESIAN_POINT ( 'NONE',  ( 1.084930333755677045, -2.153824616689365978, -0.4803136671489223741 ) ) ;
#25493=CARTESIAN_POINT ( 'NONE',  ( 3.813984095001612395, -2.229740912845196377, 0.3821933647679372492 ) ) ;
#25495=CARTESIAN_POINT ( 'NONE',  ( 3.322321318109163979, -0.7387318680696324247, -1.654322230785286063 ) ) ;
#25496=CARTESIAN_POINT ( 'NONE',  ( 2.676846564686267804, 1.640678131122888406, -0.9888057999517668728 ) ) ;
#25497=CARTESIAN_POINT ( 'NONE',  ( 4.457524453155742528, 1.660904245173303373, 1.235824716467534889 ) ) ;
#25499=CARTESIAN_POINT ( 'NONE',  ( 2.922686454756417085, 1.855838157306726632, 0.6655703372969791198 ) ) ;
#25500=CARTESIAN_POINT ( 'NONE',  ( 0.7801460289126905812, -1.072782840069667509, 1.599849161009530674 ) ) ;
#25501=CARTESIAN_POINT ( 'NONE',  ( 4.416781281874038179, 1.710313510141375115, 0.7581657270378170388 ) ) ;
#25502=CARTESIAN_POINT ( 'NONE',  ( 2.262750896497740527, 0.9887190084108381516, 2.085292768615305992 ) ) ;
#25503=CARTESIAN_POINT ( 'NONE',  ( 3.631172916894987779, 0.04772338994715261129, -1.860622308654858559 ) ) ;
#25509=CARTESIAN_POINT ( 'NONE',  ( 1.172648168047723649, -1.334858166028422222, 1.629009436104215558 ) ) ;
#25513=CARTESIAN_POINT ( 'NONE',  ( 2.637105894733019262, 1.998242115483703341, 0.7103459930332192140 ) ) ;
#25514=CARTESIAN_POINT ( 'NONE',  ( 6.569012466128139494, -1.559778377529440929, 1.282785893457456750 ) ) ;
#25518=CARTESIAN_POINT ( 'NONE',  ( 1.089409339093825979, 1.906878951332368954, -1.017924135055588541 ) ) ;
#25520=CARTESIAN_POINT ( 'NONE',  ( 6.825078400183582694, 7.052760558784821221, 2.553807217019073761 ) ) ;
#25523=CARTESIAN_POINT ( 'NONE',  ( 6.192592252150040721, 1.490973663936447258, -1.357864438797616868 ) ) ;
#25527=CARTESIAN_POINT ( 'NONE',  ( 0.1107634673921135821, -0.9696846621911526798, -2.041722876818732324 ) ) ;
#25531=CARTESIAN_POINT ( 'NONE',  ( -0.01814341541641998484, -1.915199053885572988, -0.04638162876333290496 ) ) ;
#25535=CARTESIAN_POINT ( 'NONE',  ( 2.982692045960423588, -0.1271664282922572997, -1.720251185527998272 ) ) ;
#25538=CARTESIAN_POINT ( 'NONE',  ( 1.106321208856683613, 1.344927736385517658, -1.150416400790694960 ) ) ;
#25540=CARTESIAN_POINT ( 'NONE',  ( 1.436190773529995468, -1.120142249841639348, -1.672479584328613988 ) ) ;
#25541=CARTESIAN_POINT ( 'NONE',  ( 6.883263157960391787, -0.001104538646235289417, 1.946037152736757925 ) ) ;
#25542=CARTESIAN_POINT ( 'NONE',  ( 4.383934217864794647, 1.438874268414831015, 1.673263306058408340 ) ) ;
#25545=CARTESIAN_POINT ( 'NONE',  ( 3.774183692772983267, 2.104302197123971485, -0.2610650231627819062 ) ) ;
#25546=CARTESIAN_POINT ( 'NONE',  ( 3.163685574146878565, 1.281377625384312324, 1.556896677758594416 ) ) ;
#25547=CARTESIAN_POINT ( 'NONE',  ( 3.656362025717549535, 1.803379273073001388, 0.1719060212231597329 ) ) ;
#25550=CARTESIAN_POINT ( 'NONE',  ( 1.885419139999934934, 1.287927767047766903, 1.356919574424742203 ) ) ;
#25552=CARTESIAN_POINT ( 'NONE',  ( 5.953692858212231265, 0.5253669772854427933, -1.748464709795935157 ) ) ;
#25554=CARTESIAN_POINT ( 'NONE',  ( 2.571384127028350175, 1.358050290760448364, 1.351446277617992076 ) ) ;
#25563=CARTESIAN_POINT ( 'NONE',  ( 3.217144136595586179, 1.669276650691432495, -1.307696563879121143 ) ) ;
#25564=CARTESIAN_POINT ( 'NONE',  ( -0.02988540731095785247, 0.7668091516429014209, -1.812018377701756888 ) ) ;
#25566=CARTESIAN_POINT ( 'NONE',  ( 4.938727034960622930, 0.3341968672867478007, 1.942665651468850951 ) ) ;
#25567=CARTESIAN_POINT ( 'NONE',  ( 0.2814942100668381131, 0.1933317163467423994, -2.003872996790170724 ) ) ;
#25569=CARTESIAN_POINT ( 'NONE',  ( 0.4041146219485808877, -1.136702437883057470, -1.786057295064005013 ) ) ;
#25571=CARTESIAN_POINT ( 'NONE',  ( 1.504437137538238600, 2.067909592606699487, 0.1035681241481553605 ) ) ;
#25572=CARTESIAN_POINT ( 'NONE',  ( 2.326030237553232016, 1.883725225384206281, 0.4715086074991140519 ) ) ;
#25575=CARTESIAN_POINT ( 'NONE',  ( 4.031257853796605062, -1.441737515256842572, -1.514218249133948868 ) ) ;
#25578=CARTESIAN_POINT ( 'NONE',  ( 0.3811517019768875802, 0.1791931900220759266, -1.802556192996515705 ) ) ;
#25580=CARTESIAN_POINT ( 'NONE',  ( 5.567066847960510323, -1.993696164035433371, -0.9465883713010987410 ) ) ;
#25582=CARTESIAN_POINT ( 'NONE',  ( 4.419099417909471583, 2.016199240759775524, 0.8975180220924662278 ) ) ;
#25585=CARTESIAN_POINT ( 'NONE',  ( 2.631394046745598736, -0.1854624247320437458, 1.903247139735386284 ) ) ;
#25587=CARTESIAN_POINT ( 'NONE',  ( 4.949704645232673172, 1.531818663031824013, 1.392983054852282132 ) ) ;
#25589=CARTESIAN_POINT ( 'NONE',  ( 2.764712544972968811, -1.491509591961351910, 1.564943835847030229 ) ) ;
#25590=CARTESIAN_POINT ( 'NONE',  ( 4.388337494309430653, -0.4807229498768311182, -2.138019847805587403 ) ) ;
#25600=CARTESIAN_POINT ( 'NONE',  ( 5.506714918851105089, 0.5956099481174789156, 1.982760374633622424 ) ) ;
#25601=CARTESIAN_POINT ( 'NONE',  ( 4.406810040222974401, 1.488408744443140863, -1.223127719473691588 ) ) ;
#25602=CARTESIAN_POINT ( 'NONE',  ( 0.1226730236999207246, 0.3474926252081366185, 1.986097365194151809 ) ) ;
#25607=CARTESIAN_POINT ( 'NONE',  ( 0.7092355107721182161, -0.3178641103029449799, 2.168156088950490723 ) ) ;
#25608=CARTESIAN_POINT ( 'NONE',  ( 5.619710272201024814, -1.780234218580947436, 0.4041525643716862848 ) ) ;
#25615=CARTESIAN_POINT ( 'NONE',  ( 2.348939331405873077, 0.4892633877765646400, -1.774999737812533063 ) ) ;
#25616=CARTESIAN_POINT ( 'NONE',  ( 6.170187344554162401, 2.007508049254663529, -0.1525455265532823512 ) ) ;
#25617=CARTESIAN_POINT ( 'NONE',  ( 0.6503308509665306492, -0.2843267121918050533, -2.280655268134044622 ) ) ;
#25618=CARTESIAN_POINT ( 'NONE',  ( 6.666857073735664052, 1.455856877570886887, -1.315125143065517532 ) ) ;
#25622=CARTESIAN_POINT ( 'NONE',  ( 0.7310241076574041097, -1.948878508384953356, -0.6990896207654460071 ) ) ;
#25624=CARTESIAN_POINT ( 'NONE',  ( 2.489882245090881963, -2.085347646507927699, -0.1508444384941027561 ) ) ;
#25625=CARTESIAN_POINT ( 'NONE',  ( 0.7955152940811484052, -0.6771210053572243037, 1.743984199989514927 ) ) ;
#25626=CARTESIAN_POINT ( 'NONE',  ( 1.809922493048341297, -1.704678386728165185, 1.076150803433255865 ) ) ;
#25629=CARTESIAN_POINT ( 'NONE',  ( 2.173056921186319546, 1.071630648972416333, 1.371277206274525096 ) ) ;
#25633=CARTESIAN_POINT ( 'NONE',  ( 2.578358533787118212, -1.650418691300073570, -0.5013113332296408320 ) ) ;
#25634=CARTESIAN_POINT ( 'NONE',  ( 3.034921719543516971, -1.931671641359738567, 1.035203715903771915 ) ) ;
#25635=CARTESIAN_POINT ( 'NONE',  ( 5.444034239667132624, 0.8972360612293399651, -2.016436982482258333 ) ) ;
#25637=CARTESIAN_POINT ( 'NONE',  ( 2.659224658930594121, 1.746150167319389990, -1.290005652201154263 ) ) ;
#25638=CARTESIAN_POINT ( 'NONE',  ( 1.312830284664792790, 1.609138963534262778, 0.8624270714618911260 ) ) ;
#25639=CARTESIAN_POINT ( 'NONE',  ( 3.960252432329254724, -1.215859836287141116, 1.733281388416860525 ) ) ;
#25643=CARTESIAN_POINT ( 'NONE',  ( 3.738036193864560541, 2.281383974799616521, 0.2239769770701737495 ) ) ;
#25647=CARTESIAN_POINT ( 'NONE',  ( 5.637407045567618624, -0.05664847855723317838, 2.220727194027871665 ) ) ;
#25654=CARTESIAN_POINT ( 'NONE',  ( 4.606092368833686557, -0.09613688574180989654, 2.014232646917232916 ) ) ;
#25656=CARTESIAN_POINT ( 'NONE',  ( 3.748931555198372845, -0.3975983499134613242, -2.023727603370987449 ) ) ;
#25661=CARTESIAN_POINT ( 'NONE',  ( 5.947271710577298087, 0.6394180277670692414, -2.096098967930816848 ) ) ;
#25662=CARTESIAN_POINT ( 'NONE',  ( 3.445935549842124690, -1.779626424299302956, -0.9480406757386842242 ) ) ;
#25663=CARTESIAN_POINT ( 'NONE',  ( 3.684953445348177148, 1.336164438771630714, 1.267087564277062484 ) ) ;
#25667=CARTESIAN_POINT ( 'NONE',  ( 6.422862827026682098, 1.704596635199370880, 0.6539724957527744964 ) ) ;
#25668=CARTESIAN_POINT ( 'NONE',  ( 0.1769827672329090662, 1.709356359883105636, 1.537109589704383827 ) ) ;
#25670=CARTESIAN_POINT ( 'NONE',  ( 0.5095019425028306514, 1.969206903598280212, 1.113800330609107103 ) ) ;
#25671=CARTESIAN_POINT ( 'NONE',  ( 1.541775746491366395, -1.526411702840410722, -1.451317155924846336 ) ) ;
#25675=SHAPE_REPRESENTATION_RELATIONSHIP ( 'NONE' , 'NONE' ,  #149737, #47143 ) ;
#25681=CARTESIAN_POINT ( 'NONE',  ( 3.586370468055916305, 1.236567345028506182, 1.845233891176313756 ) ) ;
#25682=CARTESIAN_POINT ( 'NONE',  ( 1.377182423176852133, 2.023737929115625445, -0.8412682346608522099 ) ) ;
#25683=CARTESIAN_POINT ( 'NONE',  ( 0.2412292383832773390, 0.3817025157030576321, 2.173470055567463088 ) ) ;
#25686=CARTESIAN_POINT ( 'NONE',  ( 4.896903505236655185, 0.3334610245491422265, 1.933150054703360432 ) ) ;
#25694=CARTESIAN_POINT ( 'NONE',  ( 3.656581996618038843, 2.110704406498860486, 0.2042969539849878724 ) ) ;
#25696=CARTESIAN_POINT ( 'NONE',  ( 5.506754051192107369, 1.639644015412666800, -1.408845030788405506 ) ) ;
#25697=CARTESIAN_POINT ( 'NONE',  ( 4.036529152626888717, -1.599951230533543045, 0.9111318136766359821 ) ) ;
#25698=CARTESIAN_POINT ( 'NONE',  ( 5.419157771004846857, -1.820987890746316173, 0.8666037247077316152 ) ) ;
#25701=CARTESIAN_POINT ( 'NONE',  ( -0.1298852118744100725, 0.003815113116375101580, -1.726395881205537330 ) ) ;
#25702=CARTESIAN_POINT ( 'NONE',  ( 6.827182134110205247, 0.5943742033862747798, 1.864010940340610212 ) ) ;
#25705=CARTESIAN_POINT ( 'NONE',  ( 3.959979445722985325, 2.145676688911036578, -0.2621329562078680842 ) ) ;
#25707=CARTESIAN_POINT ( 'NONE',  ( 5.958361200765043719, 1.524811557412728114, 1.319025083221535333 ) ) ;
#25709=CARTESIAN_POINT ( 'NONE',  ( 3.995124980148881288, 1.827535992889782523, -1.154293374375232828 ) ) ;
#25710=CARTESIAN_POINT ( 'NONE',  ( 3.479716606839049930, 1.247861786229450543, 1.526166498753677825 ) ) ;
#25712=CARTESIAN_POINT ( 'NONE',  ( 0.9917865004017255570, 2.033541294120873033, -1.090684920485317733 ) ) ;
#25713=CARTESIAN_POINT ( 'NONE',  ( 2.671226777604285729, 0.1043416919609811144, -2.058284026376159925 ) ) ;
#25714=CARTESIAN_POINT ( 'NONE',  ( 5.425317942119275649, -1.235012148030777412, -1.498765763798795891 ) ) ;
#25716=ORIENTED_EDGE ( 'NONE', *, *, #8288, .F. ) ;
#25722=CARTESIAN_POINT ( 'NONE',  ( 2.784424029790978139, -1.135345490304447091, 1.892179603154810597 ) ) ;
#25724=CARTESIAN_POINT ( 'NONE',  ( 6.631700630569578259, 1.878258136613653040, -0.5663492180864730940 ) ) ;
#25725=CARTESIAN_POINT ( 'NONE',  ( -0.1291982275798625457, 6.946856551170387029, -2.669038260222480918 ) ) ;
#25729=CARTESIAN_POINT ( 'NONE',  ( 4.839718430358881385, 1.836437689789902405, 0.1323948491315785347 ) ) ;
#25731=CARTESIAN_POINT ( 'NONE',  ( 2.131779597171743923, -1.345384690298248698, -1.561254108789570827 ) ) ;
#25739=CARTESIAN_POINT ( 'NONE',  ( 1.164996006578455923, -1.862832630767555120, -0.8818606138344189382 ) ) ;
#25740=CARTESIAN_POINT ( 'NONE',  ( 4.458453498679889826, -1.646799808365447149, -0.8236825204945982248 ) ) ;
#25744=CARTESIAN_POINT ( 'NONE',  ( 6.610000000000022524, 3.695490760540712127, 2.514297579034238783 ) ) ;
#25746=CARTESIAN_POINT ( 'NONE',  ( 4.951907052881864502, 0.6945806438464275923, -2.094803410698709900 ) ) ;
#25747=CARTESIAN_POINT ( 'NONE',  ( 6.802048716365778347, -2.262122309816359422, 0.04523717395405778968 ) ) ;
#25749=CARTESIAN_POINT ( 'NONE',  ( 0.1582721923853447621, 1.907395734848855051, 0.1385995803297388196 ) ) ;
#25750=CARTESIAN_POINT ( 'NONE',  ( 6.350803879971770982, -1.754615558991738267, -0.7693843322766678039 ) ) ;
#25752=CARTESIAN_POINT ( 'NONE',  ( 0.07536363704235565786, 7.629137130509072051, -2.744199452819145346 ) ) ;
#25754=CARTESIAN_POINT ( 'NONE',  ( 5.865855438783554199, 0.5507134639845880919, -1.831277125143706774 ) ) ;
#25756=CARTESIAN_POINT ( 'NONE',  ( 0.4263524580605422276, 1.788790299270696993, 0.5473224044415525569 ) ) ;
#25757=CARTESIAN_POINT ( 'NONE',  ( 2.747280062631300535, 0.2910806042949847239, -1.995268371848608835 ) ) ;
#25759=CARTESIAN_POINT ( 'NONE',  ( 3.914754834457169874, 1.489469167258972382, -1.489228550157334574 ) ) ;
#25765=CARTESIAN_POINT ( 'NONE',  ( 3.621357264417348620, 1.734514936435461507, 1.034602781942542515 ) ) ;
#25769=CARTESIAN_POINT ( 'NONE',  ( 4.235729478701364847, -1.487246874726022128, -1.568870776130903089 ) ) ;
#25774=CARTESIAN_POINT ( 'NONE',  ( 2.190095119440739424, -1.416971674389384761, -1.645159614449900776 ) ) ;
#25778=CARTESIAN_POINT ( 'NONE',  ( 0.8195642880178370948, 1.096917009463085790, -1.478703137254427924 ) ) ;
#25780=CARTESIAN_POINT ( 'NONE',  ( 3.544632465004614374, -1.790652189326558563, 1.263247045326252094 ) ) ;
#25782=CARTESIAN_POINT ( 'NONE',  ( 3.485499699327331502, 2.046305154993263375, -0.9654624412855338234 ) ) ;
#25784=CARTESIAN_POINT ( 'NONE',  ( 4.592982591267942283, 1.756852934926198317, 0.9896879400849432074 ) ) ;
#25790=CARTESIAN_POINT ( 'NONE',  ( 4.446413189832159496, 0.4709973186826624802, 1.705850592114676489 ) ) ;
#25792=CARTESIAN_POINT ( 'NONE',  ( 0.8683613728089655259, 1.037855563948440363, 1.832367646046024534 ) ) ;
#25796=CARTESIAN_POINT ( 'NONE',  ( 0.8538788329778913555, -0.7122206123622039087, 1.836445260119154543 ) ) ;
#25798=CARTESIAN_POINT ( 'NONE',  ( 6.151970292378349470, 1.039009440890667824, 1.727993850779283580 ) ) ;
#25802=CARTESIAN_POINT ( 'NONE',  ( 4.328871119428026049, 0.09166491666120352155, 1.868520897946590598 ) ) ;
#25803=CARTESIAN_POINT ( 'NONE',  ( 4.399325512199628641, -1.803763729973751451, 1.015883459259236954 ) ) ;
#25812=CARTESIAN_POINT ( 'NONE',  ( 4.088298575758734898, 1.051444423028622399, -1.656135347060924135 ) ) ;
#25813=CARTESIAN_POINT ( 'NONE',  ( 1.827499746633702182, -1.427720486614523221, 1.423741782973136694 ) ) ;
#25816=CARTESIAN_POINT ( 'NONE',  ( 1.264687732342294701, -1.688641954842164283, -0.8049673154429252131 ) ) ;
#25818=CARTESIAN_POINT ( 'NONE',  ( 2.707291822170342144, 1.724471752635655664, -1.038662168513148965 ) ) ;
#25820=CARTESIAN_POINT ( 'NONE',  ( 3.673546786387419605, 1.535089753090538078, 1.458380203637131833 ) ) ;
#25822=CARTESIAN_POINT ( 'NONE',  ( 5.195788487752976081, -1.461605715988937515, -1.466586839339318882 ) ) ;
#25824=CARTESIAN_POINT ( 'NONE',  ( -0.1116087887279961222, -0.4605761454780517572, -2.046466910313152532 ) ) ;
#25825=CARTESIAN_POINT ( 'NONE',  ( 6.720655732516665815, 7.629137130509056064, 2.773739711112707340 ) ) ;
#25826=CARTESIAN_POINT ( 'NONE',  ( 5.420859398437725574, 1.687492901312273474, 0.6969783729503381542 ) ) ;
#25833=CARTESIAN_POINT ( 'NONE',  ( 6.428373272941257710, -0.9058926715965059939, -1.684108486221975953 ) ) ;
#25835=( BOUNDED_CURVE ( )  B_SPLINE_CURVE ( 3, ( #160689, #142342, #188911, #176941 ),
 .UNSPECIFIED., .F., .T. ) 
 B_SPLINE_CURVE_WITH_KNOTS ( ( 4, 4 ),
 ( 0.5000000000000001110, 1.000000000000000000 ),
 .UNSPECIFIED. ) 
 CURVE ( )  GEOMETRIC_REPRESENTATION_ITEM ( )  RATIONAL_B_SPLINE_CURVE ( ( 0.9999999999999998890, 0.3333333333333333703, 0.3333333333333335369, 1.000000000000000000 ) ) 
 REPRESENTATION_ITEM ( '' )  );
#25844=CARTESIAN_POINT ( 'NONE',  ( 5.167592292328679449, 1.356312711205298172, 1.492245250866150785 ) ) ;
#25850=CARTESIAN_POINT ( 'NONE',  ( 2.729305274051788022, 0.1014009245450513547, -1.966985261555218800 ) ) ;
#25851=CARTESIAN_POINT ( 'NONE',  ( 3.937125189161301719, -1.678018027730580286, -1.117815418662113425 ) ) ;
#25853=CARTESIAN_POINT ( 'NONE',  ( 6.727182134110242906, 2.956326135258012577, 2.541581140702349195 ) ) ;
#25854=CARTESIAN_POINT ( 'NONE',  ( 3.293114190187882429, 1.727671002657789057, 1.348082825637614279 ) ) ;
#25856=CARTESIAN_POINT ( 'NONE',  ( 2.239170187357332420, -1.721643101494104044, 0.8643732543716446948 ) ) ;
#25858=CARTESIAN_POINT ( 'NONE',  ( 0.1333542156527660338, 2.021264325465597977, -2.461897275464264290 ) ) ;
#25866=CARTESIAN_POINT ( 'NONE',  ( 5.917501325027624048, -1.028386522942719816, -1.527094029191010893 ) ) ;
#25867=CARTESIAN_POINT ( 'NONE',  ( 2.402991782874515092, -0.3463731968284866625, -1.982927098142922784 ) ) ;
#25868=CARTESIAN_POINT ( 'NONE',  ( 4.675370021169432455, -0.9774931845568238797, -2.080278028362152032 ) ) ;
#25869=CARTESIAN_POINT ( 'NONE',  ( -0.02919842301648319441, 0.2290444945237135044, -2.107092690553781456 ) ) ;
#25870=CARTESIAN_POINT ( 'NONE',  ( 2.711566728334329213, 0.5015729494155155566, -1.791976956261555953 ) ) ;
#25876=CARTESIAN_POINT ( 'NONE',  ( 5.636299653793654940, 0.4088526781071535887, 2.050197504659311942 ) ) ;
#25881=CARTESIAN_POINT ( 'NONE',  ( 6.305283062370508063, 1.438394668203015092, 0.9516435707833100777 ) ) ;
#25883=CARTESIAN_POINT ( 'NONE',  ( 1.248208839261849112, 1.708581046602712039, -0.2955488178391346143 ) ) ;
#25887=CARTESIAN_POINT ( 'NONE',  ( 5.963789030284865511, -0.5350816163755196531, 2.103975319158644552 ) ) ;
#25888=CARTESIAN_POINT ( 'NONE',  ( 4.793472150574508817, 1.354911484294840429, 1.223852735664505698 ) ) ;
#25889=CARTESIAN_POINT ( 'NONE',  ( 2.307404798597446849, -1.572557994556064154, -1.172606125687980061 ) ) ;
#25893=CARTESIAN_POINT ( 'NONE',  ( 3.158948766716848766, 0.5171890032967979556, 2.056314737185329644 ) ) ;
#25898=CARTESIAN_POINT ( 'NONE',  ( 1.041946221393402539, 1.387617377995558288, 1.536584593769604323 ) ) ;
#25902=CARTESIAN_POINT ( 'NONE',  ( 3.528187740469524769, -2.188240134182100949, 0.3810097408954765119 ) ) ;
#25904=CARTESIAN_POINT ( 'NONE',  ( 1.583111924021431305, -0.7688449931826674133, 2.166437542035759556 ) ) ;
#25906=CARTESIAN_POINT ( 'NONE',  ( 6.280145880020024052, -1.141028152120068917, -1.718028578259041872 ) ) ;
#25909=EDGE_CURVE ( 'NONE', #119587, #190223, #38499, .T. ) ;
#25915=CARTESIAN_POINT ( 'NONE',  ( -0.2106725631050176961, 2.017899180269961956, -2.418275446281520136 ) ) ;
#25916=CARTESIAN_POINT ( 'NONE',  ( 2.555303990735880770, 0.4627875540959677236, -1.661435987504814360 ) ) ;
#25917=CARTESIAN_POINT ( 'NONE',  ( 2.536342520008515233, 0.6839386381054488595, 1.897109991223707937 ) ) ;
#25918=CARTESIAN_POINT ( 'NONE',  ( 2.936492027000091376, -1.880918663215241926, -1.321213444053377373 ) ) ;
#25919=CARTESIAN_POINT ( 'NONE',  ( 4.060077147624012284, 2.245929291707829289, -0.2719227649434445282 ) ) ;
#25920=CARTESIAN_POINT ( 'NONE',  ( 5.584633104594088238, -2.054432100182907561, -0.4627632117069883089 ) ) ;
#25922=CARTESIAN_POINT ( 'NONE',  ( 3.743183411477500222, -1.338374212114415762, -1.157953421578450381 ) ) ;
#25924=CARTESIAN_POINT ( 'NONE',  ( 5.847306917912500346, 0.6688746937079934618, -2.192647164702413498 ) ) ;
#25925=CARTESIAN_POINT ( 'NONE',  ( 5.173706384855800700, -1.019854773079221344, 1.532662130498331887 ) ) ;
#25930=CARTESIAN_POINT ( 'NONE',  ( 4.435597005726048536, 0.9382243502508281763, -1.980580373504265301 ) ) ;
#25933=CARTESIAN_POINT ( 'NONE',  ( 6.021949436824264978, 2.040384406434097464, -0.3501103912618847014 ) ) ;
#25936=CARTESIAN_POINT ( 'NONE',  ( 3.439987180796261423, 0.8656686944604700118, -1.721121497068250017 ) ) ;
#25940=CARTESIAN_POINT ( 'NONE',  ( 0.3521972369381949908, -1.576644756679127513, -1.565149006781616725 ) ) ;
#25949=CARTESIAN_POINT ( 'NONE',  ( 0.8187140321147531319, -1.423520202335259999, 1.350257566363553208 ) ) ;
#25952=CARTESIAN_POINT ( 'NONE',  ( 6.074655751228532630, 1.318658252384183438, -1.452748870126779890 ) ) ;
#25956=CARTESIAN_POINT ( 'NONE',  ( 0.4974159974337259427, 1.879172763871908902, -1.259763710243780865 ) ) ;
#25960=CARTESIAN_POINT ( 'NONE',  ( 0.3505827959322353471, -1.506356567903786470, 1.108807183729618062 ) ) ;
#25961=CARTESIAN_POINT ( 'NONE',  ( 6.468101748929986350, 1.443884034049055298, 0.9595089302780019924 ) ) ;
#25963=CARTESIAN_POINT ( 'NONE',  ( 3.386445149735781257, -0.4294187885149694517, -2.148908265708626697 ) ) ;
#25964=CARTESIAN_POINT ( 'NONE',  ( 4.665214083390394784, -2.058938813511351551, -1.042142520334616185 ) ) ;
#25965=CARTESIAN_POINT ( 'NONE',  ( 0.6903932018771785639, -2.045263458338997253, -0.2527981509174073715 ) ) ;
#25966=CARTESIAN_POINT ( 'NONE',  ( 2.642442020880403586, -1.614326438788242557, 1.079121087018119152 ) ) ;
#25969=CARTESIAN_POINT ( 'NONE',  ( 5.326475955075804514, -0.9554483686352827077, -1.893264085526874974 ) ) ;
#25971=CARTESIAN_POINT ( 'NONE',  ( 3.920546200773936896, -1.392545040883992336, -1.458557299768625581 ) ) ;
#25975=CARTESIAN_POINT ( 'NONE',  ( 1.506192966688112422, -0.6554880476431452774, -1.704135612709246184 ) ) ;
#25980=CARTESIAN_POINT ( 'NONE',  ( 5.541890059496114240, 0.8373154222949423797, -1.883320703650725125 ) ) ;
#25985=CARTESIAN_POINT ( 'NONE',  ( 4.600263385724223220, -0.9500085478860437194, 1.782271578547896418 ) ) ;
#25986=CARTESIAN_POINT ( 'NONE',  ( 6.235052692738393354, 2.071546745583602522, 0.8022605484305275203 ) ) ;
#25991=CARTESIAN_POINT ( 'NONE',  ( 3.907146709503729110, 1.766719954806586612, 1.060879741047163316 ) ) ;
#25992=CARTESIAN_POINT ( 'NONE',  ( 3.041638857185970046, -1.525043868314728934, 1.319228477497782936 ) ) ;
#25998=CARTESIAN_POINT ( 'NONE',  ( 3.040388574052850235, 1.915307028720541371, -0.6297779509270851062 ) ) ;
#25999=CARTESIAN_POINT ( 'NONE',  ( 2.044624030687072214, -1.478315374303545315, -1.097237131862264903 ) ) ;
#26000=CARTESIAN_POINT ( 'NONE',  ( 0.8741376776274005778, 2.222666731570396959, -0.6204599517294244748 ) ) ;
#26002=CARTESIAN_POINT ( 'NONE',  ( 4.147864318636265146, 0.7325676050485960822, -2.033789780341701547 ) ) ;
#26004=CARTESIAN_POINT ( 'NONE',  ( 3.444923099841538772, 1.455166840473320233, 1.779090439993118888 ) ) ;
#26008=CARTESIAN_POINT ( 'NONE',  ( 1.147088892781012781, -1.472398045354219365, -1.153743250124287689 ) ) ;
#26010=CARTESIAN_POINT ( 'NONE',  ( 5.787953125587765868, -0.8870788200928159117, 1.760698262704742723 ) ) ;
#26014=CARTESIAN_POINT ( 'NONE',  ( 0.8739773845415178544, 2.125910683164092152, -0.5920798734769525673 ) ) ;
#26018=CARTESIAN_POINT ( 'NONE',  ( 6.639320575229256782, 2.033582276073117701, 2.408309898857839304 ) ) ;
#26019=CARTESIAN_POINT ( 'NONE',  ( 5.366080375918201639, 0.9711980517450971018, 1.715566965677978173 ) ) ;
#26020=CARTESIAN_POINT ( 'NONE',  ( 5.250698995481407394, 0.6654115676409579905, 2.209675006967478428 ) ) ;
#26021=CARTESIAN_POINT ( 'NONE',  ( 5.758217292028081857, -1.861241882002647285, 0.0004304118630827496474 ) ) ;
#26022=CARTESIAN_POINT ( 'NONE',  ( 2.957939313049274599, -0.6512127342562739063, 1.957104789517728483 ) ) ;
#26029=CARTESIAN_POINT ( 'NONE',  ( 4.897030219210679824, 0.3665305452156160659, 2.139867649710110786 ) ) ;
#26031=CARTESIAN_POINT ( 'NONE',  ( 4.247483403459266782, 1.840758003770435414, -0.04960325993209198370 ) ) ;
#26034=CARTESIAN_POINT ( 'NONE',  ( 6.304242050522723240, 1.625252681175231029, -1.470355468214133543 ) ) ;
#26036=CARTESIAN_POINT ( 'NONE',  ( 0.5798237426192736077, 2.110460337659907371, -0.8156065903286384700 ) ) ;
#26041=CARTESIAN_POINT ( 'NONE',  ( 0.1000639402851908749, -0.9014739813196898099, 1.686438745833309660 ) ) ;
#26042=CARTESIAN_POINT ( 'NONE',  ( 1.269958040854075154, -1.126728106645444205, 1.364847948389063870 ) ) ;
#26043=CARTESIAN_POINT ( 'NONE',  ( 5.250644345176154637, 1.983683461502975254, 0.3419521592970317103 ) ) ;
#26045=CARTESIAN_POINT ( 'NONE',  ( 3.733512407637301855, -1.946585179706640467, 0.8041552576890409476 ) ) ;
#26046=CARTESIAN_POINT ( 'NONE',  ( 2.882342042720618558, -0.5589011775578194285, -1.832234547041192929 ) ) ;
#26048=CARTESIAN_POINT ( 'NONE',  ( 4.211352281912852824, -1.636193967830642748, -1.096030559421146133 ) ) ;
#26049=CARTESIAN_POINT ( 'NONE',  ( 5.062762828692743966, 0.5904309321736100902, 1.931528952932992427 ) ) ;
#26051=CARTESIAN_POINT ( 'NONE',  ( 3.221420234344949840, -1.803205065257794004, 0.4975683872451354683 ) ) ;
#26052=CARTESIAN_POINT ( 'NONE',  ( 5.303229652072571021, 1.413297086782526302, 0.9885393367406664078 ) ) ;
#26053=CARTESIAN_POINT ( 'NONE',  ( 0.7559434568639655794, 0.7726834774516875282, -1.749509110286852742 ) ) ;
#26055=CARTESIAN_POINT ( 'NONE',  ( 2.737190076726934151, 0.2709513247245790013, 2.190122135706531914 ) ) ;
#26058=CARTESIAN_POINT ( 'NONE',  ( 6.865691018405424728, -0.4312029709039078007, 1.920920986087648163 ) ) ;
#26066=CARTESIAN_POINT ( 'NONE',  ( 1.838419004579601834, -1.109345826794335688, 1.747895861591180156 ) ) ;
#26072=CARTESIAN_POINT ( 'NONE',  ( 0.3112020186443940628, 1.677875239561373855, -1.123872588032665210 ) ) ;
#26076=CARTESIAN_POINT ( 'NONE',  ( 0.07479286986303290696, 5.725009232006174287, -2.449550298930736059 ) ) ;
#26078=CARTESIAN_POINT ( 'NONE',  ( 5.413435409655408925, 0.5825687168248098180, 1.930121546480124461 ) ) ;
#26079=CARTESIAN_POINT ( 'NONE',  ( 5.032410968829077014, 0.5625187028349203366, 1.831241071522809127 ) ) ;
#26080=CARTESIAN_POINT ( 'NONE',  ( 2.243918346939121733, 2.191141468336772036, 0.05030144379260944459 ) ) ;
#26083=CARTESIAN_POINT ( 'NONE',  ( 5.695569903961543723, 1.858472494656268958, -0.7744561248179144819 ) ) ;
#26084=CARTESIAN_POINT ( 'NONE',  ( 1.476665317443916381, -1.350161712199383413, 1.354623164920423672 ) ) ;
#26086=CARTESIAN_POINT ( 'NONE',  ( 0.4566579290818244541, -1.899626807963299635, -0.6766942018802262204 ) ) ;
#26089=CARTESIAN_POINT ( 'NONE',  ( 2.946908815893133138, -1.710673590971498292, -1.201729372296795662 ) ) ;
#26091=CARTESIAN_POINT ( 'NONE',  ( 1.922448523189672853, 1.607815062812420370, 0.6247884732281087095 ) ) ;
#26093=CARTESIAN_POINT ( 'NONE',  ( 6.275647701495586261, 0.3610785225884837191, -2.089460823871174266 ) ) ;
#26096=CARTESIAN_POINT ( 'NONE',  ( 0.3440982351944205653, -0.9282241650855774795, 1.728402704573737125 ) ) ;
#26102=CARTESIAN_POINT ( 'NONE',  ( 2.947712979364258690, -1.218347856841961452, -1.340696891046004868 ) ) ;
#26107=CARTESIAN_POINT ( 'NONE',  ( 4.213381321868588714, 1.457370398675205569, 1.075660112967236737 ) ) ;
#26111=CARTESIAN_POINT ( 'NONE',  ( 3.648742529127374734, -0.3609857515115758586, -1.825517407628447053 ) ) ;
#26112=CARTESIAN_POINT ( 'NONE',  ( 1.757307594529472272, 1.832486779838927937, -0.5580655975847663708 ) ) ;
#26113=CARTESIAN_POINT ( 'NONE',  ( 0.8854529848611718545, 1.222500307375608886, 1.355994775097228766 ) ) ;
#26120=CARTESIAN_POINT ( 'NONE',  ( 6.925078400183550364, 3.684205305355064297, 2.658256427561227486 ) ) ;
#26122=CARTESIAN_POINT ( 'NONE',  ( 5.260591308972474067, -0.6599101888420509932, -1.855755260766891235 ) ) ;
#26126=CARTESIAN_POINT ( 'NONE',  ( 6.492125937493531396, -0.5805207454109837517, -2.113085764653479082 ) ) ;
#26127=CARTESIAN_POINT ( 'NONE',  ( 4.999011269523485623, 1.601735033023284904, -1.069960431631542752 ) ) ;
#26129=CARTESIAN_POINT ( 'NONE',  ( 0.8854529848611718545, 1.222500307375608886, 1.355994775097228766 ) ) ;
#26130=CARTESIAN_POINT ( 'NONE',  ( 1.735297346119796691, 0.2185962045802778420, 2.196029071591873993 ) ) ;
#26133=CARTESIAN_POINT ( 'NONE',  ( 0.8789968191965717992, -1.730013457311157188, -0.8152767527440167861 ) ) ;
#26135=CARTESIAN_POINT ( 'NONE',  ( 0.8890313061419883311, 0.1412731933134198092, 1.964529561086136189 ) ) ;
#26136=CARTESIAN_POINT ( 'NONE',  ( 2.190873381757904692, 1.502741926987064325, 1.230217333823523163 ) ) ;
#26138=CARTESIAN_POINT ( 'NONE',  ( 1.247422469434919412, -1.966343046301596509, -0.4444367004674750210 ) ) ;
#26140=CARTESIAN_POINT ( 'NONE',  ( 6.649252725998297642, 1.619456339520190413, -0.9165514639192672286 ) ) ;
#26145=CARTESIAN_POINT ( 'NONE',  ( 2.876726420669137863, -0.1638259704515396820, -2.185508879517850112 ) ) ;
#26149=CARTESIAN_POINT ( 'NONE',  ( 2.666400811807769777, -1.259032629953384719, 1.322343945743660543 ) ) ;
#26156=CARTESIAN_POINT ( 'NONE',  ( 1.225083325515680555, -0.04812572341393595021, 1.926057772195179485 ) ) ;
#26157=CARTESIAN_POINT ( 'NONE',  ( 5.893401036868160858, -1.775023410133094615, 0.8355650083611900758 ) ) ;
#26161=CARTESIAN_POINT ( 'NONE',  ( 4.546525781634036534, -1.759932548463913671, 1.305750774140898685 ) ) ;
#26163=CARTESIAN_POINT ( 'NONE',  ( 4.873920291170623642, -2.031351322358550870, 0.3986081187722507746 ) ) ;
#26165=CARTESIAN_POINT ( 'NONE',  ( 5.467524615204178318, -2.242144116172717361, -0.5062228086629757540 ) ) ;
#26169=CARTESIAN_POINT ( 'NONE',  ( 0.7445458516137266614, 0.6704725750066173884, 2.192023251310899923 ) ) ;
#26174=CARTESIAN_POINT ( 'NONE',  ( 4.699130951095971120, -0.5162677480817599029, 1.872006234571305772 ) ) ;
#26179=CARTESIAN_POINT ( 'NONE',  ( 5.308822938259078583, -0.4706598425541131947, -1.853433239416848455 ) ) ;
#26180=CARTESIAN_POINT ( 'NONE',  ( 6.264645798839446833, -1.215808215430391304, 1.223651055087880080 ) ) ;
#26181=CARTESIAN_POINT ( 'NONE',  ( 5.630092293170263495, 2.014432788975322630, 0.09412139267171715229 ) ) ;
#26185=CARTESIAN_POINT ( 'NONE',  ( 1.095779546523030668, -2.090823718873015657, 0.001679924440483454573 ) ) ;
#26186=CARTESIAN_POINT ( 'NONE',  ( 0.5140565032336151807, 1.225199188247323878, -1.277449566202024656 ) ) ;
#26187=CARTESIAN_POINT ( 'NONE',  ( 5.397111353752316987, -0.9091427841607623295, -1.799923777076550824 ) ) ;
#26189=CARTESIAN_POINT ( 'NONE',  ( 3.398623556838876514, 1.807253594820698250, -1.409964679536945598 ) ) ;
#26190=CARTESIAN_POINT ( 'NONE',  ( 1.815945235625218590, 1.623157326234461628, 0.6282625412417954802 ) ) ;
#26191=CARTESIAN_POINT ( 'NONE',  ( 2.865608904542978674, -1.736054085904148669, -1.217558864107195715 ) ) ;
#26193=CARTESIAN_POINT ( 'NONE',  ( 1.633743589071215974, 0.1333172958793479579, -1.728787957231948447 ) ) ;
#26195=CARTESIAN_POINT ( 'NONE',  ( 1.925991809680915878, 0.9530580284189617002, 1.598336604343030931 ) ) ;
#26196=CARTESIAN_POINT ( 'NONE',  ( 2.049520782779357120, 1.889653518395111753, -1.069053457954100006 ) ) ;
#26197=CARTESIAN_POINT ( 'NONE',  ( 3.169157936054858293, 1.820986098869777470, -0.8666075021629695563 ) ) ;
#26198=CARTESIAN_POINT ( 'NONE',  ( 4.625000000000002665, -2.052068128417944504, 2.503915141160646116E-13 ) ) ;
#26200=CARTESIAN_POINT ( 'NONE',  ( 0.7274102002729305738, -1.830281784476958773, 0.6011100631785198933 ) ) ;
#26202=CARTESIAN_POINT ( 'NONE',  ( 3.603960747418310184, 1.611073206568460758, 1.529666071269941474 ) ) ;
#26204=CARTESIAN_POINT ( 'NONE',  ( -0.2108831679771168421, 7.629137130509075604, -2.497154329497493386 ) ) ;
#26208=CARTESIAN_POINT ( 'NONE',  ( 6.521772982575972044, -0.4919494239215887466, 2.174507958589830370 ) ) ;
#26209=CARTESIAN_POINT ( 'NONE',  ( 4.439869198996494681, 1.279870211898268550, 1.486999339763886097 ) ) ;
#26213=CARTESIAN_POINT ( 'NONE',  ( 5.641944544108610238, 0.9243782401199867049, -2.065144452299176425 ) ) ;
#26215=CARTESIAN_POINT ( 'NONE',  ( 2.242701489527811454, -2.022432087814116652, -0.4046766347945063846 ) ) ;
#26220=CARTESIAN_POINT ( 'NONE',  ( 4.182764291190976813, -0.1809548918480126112, -1.861743760598027597 ) ) ;
#26221=CARTESIAN_POINT ( 'NONE',  ( 2.320625381698769640, 0.8157257908444032202, -1.530271591396751729 ) ) ;
#26222=CARTESIAN_POINT ( 'NONE',  ( 0.2051334325893399424, 1.998568519175287328, 1.122693669494337909 ) ) ;
#26223=CARTESIAN_POINT ( 'NONE',  ( 0.5170026063063514199, 1.520138765826519300, -1.599913083071627273 ) ) ;
#26225=CARTESIAN_POINT ( 'NONE',  ( 5.701106494887172360, -0.4696333794993942101, 1.884192904834626869 ) ) ;
#26227=CARTESIAN_POINT ( 'NONE',  ( 0.3346115673153668424, 0.6298721381652396811, -1.915601020889952322 ) ) ;
#26230=CARTESIAN_POINT ( 'NONE',  ( 6.574846728087075931, -0.8593996854794653251, 1.822268861383633531 ) ) ;
#26234=CARTESIAN_POINT ( 'NONE',  ( 3.826616632296374831, 1.734130841282412128, 0.5711148077138239465 ) ) ;
#26235=CARTESIAN_POINT ( 'NONE',  ( 2.186817281270125424, -2.164169025584137263, -0.4306803264119417607 ) ) ;
#26240=CARTESIAN_POINT ( 'NONE',  ( 1.090109951703751801, 1.206612241219229942, 1.619577932830415623 ) ) ;
#26243=CARTESIAN_POINT ( 'NONE',  ( 3.098338563049109151, 1.846317948315750357, 0.2325098740301386746 ) ) ;
#26249=CARTESIAN_POINT ( 'NONE',  ( 4.037589748876240670, -1.260430739550026269, -1.321009972365666307 ) ) ;
#26254=CARTESIAN_POINT ( 'NONE',  ( 1.036033436886945047, 1.672847207165208072, -0.4555716438836182602 ) ) ;
#26255=CARTESIAN_POINT ( 'NONE',  ( 5.560457619783242933, -1.666209093894938764, -0.7835883864039174806 ) ) ;
#26257=CARTESIAN_POINT ( 'NONE',  ( 4.055530604549876017, -1.917597210323931378, -1.283581016687604270 ) ) ;
#26259=CARTESIAN_POINT ( 'NONE',  ( 0.8255485222598609729, -1.957653584835903349, 0.6440290526678188465 ) ) ;
#26261=CARTESIAN_POINT ( 'NONE',  ( 6.134147193249257946, 0.1786779444946043904, -2.291516319396588397 ) ) ;
#26265=CARTESIAN_POINT ( 'NONE',  ( 5.471519871388384360, 1.802534880541529994, -0.5000026934619330454 ) ) ;
#26268=CARTESIAN_POINT ( 'NONE',  ( 2.074333847954575205, 0.8209984392052707136, 1.727357542596375861 ) ) ;
#26270=CARTESIAN_POINT ( 'NONE',  ( 3.440233207309027375, 0.9924059104887033023, -1.971224004288201881 ) ) ;
#26276=CARTESIAN_POINT ( 'NONE',  ( 1.800300592175264613, -0.7760554750895022336, 2.173288546431056734 ) ) ;
#26277=CARTESIAN_POINT ( 'NONE',  ( 2.576550507925364109, 1.283677811227203147, -1.483670167215108693 ) ) ;
#26280=CARTESIAN_POINT ( 'NONE',  ( 6.209847231236663490, 0.6040719066883664112, -1.972102366942799945 ) ) ;
#26282=CARTESIAN_POINT ( 'NONE',  ( 3.819546216251490822, -1.394084564108012403, -1.457236891723237449 ) ) ;
#26285=CARTESIAN_POINT ( 'NONE',  ( 4.417204035549080920, -1.841734835922325120, 0.8216704330437707426 ) ) ;
#26289=CARTESIAN_POINT ( 'NONE',  ( 2.184662588793543136, 1.252765144364040850, -1.772974741507940211 ) ) ;
#26292=CARTESIAN_POINT ( 'NONE',  ( 2.477632765499269141, 1.147360842229189437, 1.477270975257204633 ) ) ;
#26293=CARTESIAN_POINT ( 'NONE',  ( 6.169229141836320096, 0.1658205177522271700, -2.155315574850395155 ) ) ;
#26294=CARTESIAN_POINT ( 'NONE',  ( -0.02224634325198419221, -0.007204097619508199532, -2.289079630542793620 ) ) ;
#26295=CARTESIAN_POINT ( 'NONE',  ( 6.727182134110203826, 0.5859025467632031914, 1.963451964196837984 ) ) ;
#26299=CARTESIAN_POINT ( 'NONE',  ( 2.930216680654484485, -0.9444820207657660394, -1.662695861641521278 ) ) ;
#26300=CARTESIAN_POINT ( 'NONE',  ( 3.977242411272710942, 1.666424048269627534, -0.5965368118019414023 ) ) ;
#26301=CARTESIAN_POINT ( 'NONE',  ( 1.436035868020806738, -1.063167577064242142, -1.589284522738307448 ) ) ;
#26304=CARTESIAN_POINT ( 'NONE',  ( -0.01269188720853537365, -0.5084903737302053361, 1.846954624685708923 ) ) ;
#26306=CARTESIAN_POINT ( 'NONE',  ( 0.6958625912084138720, -1.462932864358768459, -1.465259690088885014 ) ) ;
#26309=CARTESIAN_POINT ( 'NONE',  ( 5.717618200960680852, -1.824738551054584379, 0.4112096411929695439 ) ) ;
#26310=CARTESIAN_POINT ( 'NONE',  ( 1.488595654847742145, -0.2661386877833261111, -1.806066791206423439 ) ) ;
#26311=CARTESIAN_POINT ( 'NONE',  ( 6.041676539500916654, -1.595688354349385607, -1.524751901930617715 ) ) ;
#26314=CARTESIAN_POINT ( 'NONE',  ( 2.611848684353266226, 0.5523815846302374544, -1.987258587729407999 ) ) ;
#26319=CARTESIAN_POINT ( 'NONE',  ( 0.2632415847364302786, -1.930764589519979424, -0.9721467891136772455 ) ) ;
#26321=CARTESIAN_POINT ( 'NONE',  ( 4.896967953096117654, 0.3505727482827174502, 2.040303948762006492 ) ) ;
#26323=CARTESIAN_POINT ( 'NONE',  ( 3.040462492942562545, 2.144887288335277198, 0.2678724578094940356 ) ) ;
#26325=CARTESIAN_POINT ( 'NONE',  ( 3.352217588874096599, 0.9059935441126705236, -1.805122612331450105 ) ) ;
#26326=CARTESIAN_POINT ( 'NONE',  ( 2.277722772326017608, -1.903703133612335119, 0.4737097981617058862 ) ) ;
#26334=CARTESIAN_POINT ( 'NONE',  ( 1.464077725791514517, -1.074659653367866952, 1.706114136832518779 ) ) ;
#26336=CARTESIAN_POINT ( 'NONE',  ( 5.935146830689759234, -1.586316731616247200, -1.512381816529739353 ) ) ;
#26338=CARTESIAN_POINT ( 'NONE',  ( 5.677967274442059953, 1.882970570262190613, -0.3333453579756897600 ) ) ;
#26343=CARTESIAN_POINT ( 'NONE',  ( 3.093375225471244772, -0.3905761854139707667, 1.978056131710544063 ) ) ;
#26345=CARTESIAN_POINT ( 'NONE',  ( 5.332891432879703686, 0.1301960547291525494, 1.719897333435776776 ) ) ;
#26349=CARTESIAN_POINT ( 'NONE',  ( 4.499188554602613799, 1.501106652244098116, 1.115835331622745841 ) ) ;
#26350=CARTESIAN_POINT ( 'NONE',  ( 1.041946221393402539, 1.387617377995558066, 1.536584593769604101 ) ) ;
#26354=CARTESIAN_POINT ( 'NONE',  ( 0.06993570063764525946, -0.9480199632962028611, 1.779638758220257522 ) ) ;
#26355=CARTESIAN_POINT ( 'NONE',  ( 0.7557781591117664899, 0.7332364915693561080, -1.656728582389139781 ) ) ;
#26358=ORIENTED_EDGE ( 'NONE', *, *, #37732, .T. ) ;
#26361=CARTESIAN_POINT ( 'NONE',  ( 0.7308173252688826560, -1.846041318942293286, -0.6644482084196751126 ) ) ;
#26363=CARTESIAN_POINT ( 'NONE',  ( 4.974201611368001430, -1.901669438865726924, -0.2299391999119395624 ) ) ;
#26364=CARTESIAN_POINT ( 'NONE',  ( 0.07479286986305370977, 0.004866263145587856019, -1.855573292446038414 ) ) ;
#26372=CARTESIAN_POINT ( 'NONE',  ( 2.325270847726228496, -0.0006328605136555341855, 2.161883445422786654 ) ) ;
#26376=CARTESIAN_POINT ( 'NONE',  ( 4.647361241834577328, -1.411646026218037253, -1.157555111390089264 ) ) ;
#26379=CARTESIAN_POINT ( 'NONE',  ( 1.229685887263828770, -1.247259403286736124, -1.526659406866498481 ) ) ;
#26380=CARTESIAN_POINT ( 'NONE',  ( 3.744317949583543470, 1.018843395500759197, -1.618198357137661469 ) ) ;
#26383=CARTESIAN_POINT ( 'NONE',  ( 4.967230218399325103, 1.712698785223613740, 0.9724057732015491951 ) ) ;
#26385=CARTESIAN_POINT ( 'NONE',  ( 5.671417317124205937, 1.160065345341480647, 1.557364503162941061 ) ) ;
#26386=ORIENTED_EDGE ( 'NONE', *, *, #159892, .F. ) ;
#26389=CARTESIAN_POINT ( 'NONE',  ( 6.222909436229170588, 1.570324008046734221, -1.425282903188800798 ) ) ;
#26391=CARTESIAN_POINT ( 'NONE',  ( 4.231050068913538631, 1.749697241329374098, 0.7720063087622434095 ) ) ;
#26396=CARTESIAN_POINT ( 'NONE',  ( 5.145186220991746495, 0.1505098195577254938, 2.007535063509538809 ) ) ;
#26398=CARTESIAN_POINT ( 'NONE',  ( 6.059193749186201572, -1.568369423792463024, -0.9343120793870243190 ) ) ;
#26399=CARTESIAN_POINT ( 'NONE',  ( 6.727182134110199385, 2.469373133786161301, 2.195552656936059055 ) ) ;
#26400=CARTESIAN_POINT ( 'NONE',  ( 1.504437137538238600, 2.067909592606699487, 0.1035681241481553605 ) ) ;
#26404=CARTESIAN_POINT ( 'NONE',  ( 6.368025811218641863, 0.9635043244729593059, 1.603280169136585220 ) ) ;
#26413=CARTESIAN_POINT ( 'NONE',  ( 5.186046676097956443, 1.422060760911178390, 0.9921614550853893322 ) ) ;
#26415=CARTESIAN_POINT ( 'NONE',  ( 2.413015750098276513, -1.603085927076562500, 1.310038033242977518 ) ) ;
#26416=CARTESIAN_POINT ( 'NONE',  ( 3.040728130433269616, -1.601530262690466389, 1.384902248896832333 ) ) ;
#26419=CARTESIAN_POINT ( 'NONE',  ( 1.709744157921966101, 0.5768405975999196800, -1.883039948965541610 ) ) ;
#26424=CARTESIAN_POINT ( 'NONE',  ( 4.136908408643169111, -1.995281682711878668, 1.128303315244700178 ) ) ;
#26425=CARTESIAN_POINT ( 'NONE',  ( 0.5569169099325712580, -1.540613122784354916, -0.9793164655157863274 ) ) ;
#26431=CARTESIAN_POINT ( 'NONE',  ( 2.461191956773252087, -1.671442449460639468, 1.121892926246186306 ) ) ;
#26432=CARTESIAN_POINT ( 'NONE',  ( 2.219515905360454067, 0.3404028402014187549, -1.931851785523025944 ) ) ;
#26435=CARTESIAN_POINT ( 'NONE',  ( 0.07536363704237906969, 4.084105538841027894, -2.698926661290324880 ) ) ;
#26437=CARTESIAN_POINT ( 'NONE',  ( 5.138659532522440010, -1.793477146331866612, 1.074093663348500760 ) ) ;
#26438=CARTESIAN_POINT ( 'NONE',  ( 2.992752380588555638, 1.518849080061919654, -0.9082622674112093009 ) ) ;
#26440=CARTESIAN_POINT ( 'NONE',  ( 6.474598600699414064, -0.1057723710937721190, -2.289958182497778161 ) ) ;
#26441=CARTESIAN_POINT ( 'NONE',  ( 5.490116972639333071, -0.4286210177542044697, -1.686591927243533240 ) ) ;
#26443=CARTESIAN_POINT ( 'NONE',  ( 5.783868576693856234, 1.881360230585613413, -1.320557073901595047 ) ) ;
#26445=CARTESIAN_POINT ( 'NONE',  ( 5.237493459246572947, -1.633055164623600897, -0.5828427842848020735 ) ) ;
#26447=CARTESIAN_POINT ( 'NONE',  ( 6.109878594781020134, 0.6360665949224998394, -2.075910194261113784 ) ) ;
#26449=CARTESIAN_POINT ( 'NONE',  ( 6.503150282362620160, -0.1410805869419759218, 1.984311032119711715 ) ) ;
#26450=CARTESIAN_POINT ( 'NONE',  ( 6.031250000000003553, -0.7852924748303007352, -1.895863743163946680 ) ) ;
#26451=CARTESIAN_POINT ( 'NONE',  ( 6.727182134110196721, 6.033756510516266935, 2.783943001041962795 ) ) ;
#26452=CARTESIAN_POINT ( 'NONE',  ( 4.717753586115435382, -1.889304338648789106, 0.3753660715558500005 ) ) ;
#26454=CARTESIAN_POINT ( 'NONE',  ( 6.486594595706023370, -1.368296875179885852, 1.750867008312809059 ) ) ;
#26459=CARTESIAN_POINT ( 'NONE',  ( 3.106314965395097438, -0.8985160938580877277, 2.031629072759451926 ) ) ;
#26465=CARTESIAN_POINT ( 'NONE',  ( 0.4049229342097167006, -1.081068455937021611, -1.701946057285643743 ) ) ;
#26467=CARTESIAN_POINT ( 'NONE',  ( 4.984863162817260829, 1.972918577937707196, 0.6018043753471848945 ) ) ;
#26472=CARTESIAN_POINT ( 'NONE',  ( 0.3855647087021807362, -0.8419519913594010196, 1.556653678627561543 ) ) ;
#26473=CARTESIAN_POINT ( 'NONE',  ( -0.08726289061519039436, -1.242903867559573161, -1.588418431006669351 ) ) ;
#26474=CARTESIAN_POINT ( 'NONE',  ( 5.987833318177087527, -1.732952516383274855, -0.1613439405771869561 ) ) ;
#26475=CARTESIAN_POINT ( 'NONE',  ( 4.370831947049586219, 0.0005328150827835219676, -2.292545470631628390 ) ) ;
#26477=CARTESIAN_POINT ( 'NONE',  ( 2.695044507329581673, -0.5773736025265225891, 1.748335772842606106 ) ) ;
#26480=CARTESIAN_POINT ( 'NONE',  ( 3.557459645987316232, 0.4443818804308434789, -1.770531947851671006 ) ) ;
#26481=CARTESIAN_POINT ( 'NONE',  ( 3.498672800139957406, -1.986100699840901651, 0.3474671148789992836 ) ) ;
#26484=CARTESIAN_POINT ( 'NONE',  ( 4.963951390035996170, 2.083465175373377498, -0.3060735771123861970 ) ) ;
#26486=CARTESIAN_POINT ( 'NONE',  ( 3.033707436314789785, 1.966763487489433970, -0.6469820378900912328 ) ) ;
#26489=CARTESIAN_POINT ( 'NONE',  ( 5.180389117862056914, 1.045492054797515946, 1.844774357600783121 ) ) ;
#26493=CARTESIAN_POINT ( 'NONE',  ( 0.4516242601883875274, 0.6054225165459875546, -1.828971364544299538 ) ) ;
#26499=CARTESIAN_POINT ( 'NONE',  ( 0.0006278483607258588750, -1.039594266688011137, 1.963129682597685166 ) ) ;
#26500=CARTESIAN_POINT ( 'NONE',  ( 1.887856735188620627, 1.451798466554796718, 1.525807353268118227 ) ) ;
#26503=CARTESIAN_POINT ( 'NONE',  ( 6.121894333209238148, 1.833584433263518942, -0.3168336897404684382 ) ) ;
#26508=CARTESIAN_POINT ( 'NONE',  ( 0.05319811239242258627, 0.3688592364489845510, 2.088132107045739705 ) ) ;
#26511=CARTESIAN_POINT ( 'NONE',  ( 3.420314466093795414, 0.8798059112791326575, 1.753580237611163994 ) ) ;
#26512=CARTESIAN_POINT ( 'NONE',  ( 0.4796413896344040029, 2.016494124141111399, -0.7793912508547717888 ) ) ;
#26517=CARTESIAN_POINT ( 'NONE',  ( 2.273056812072488775, 1.069988629298643579, 1.372433606717870846 ) ) ;
#26521=CARTESIAN_POINT ( 'NONE',  ( 2.759138561942891421, -2.010518527590241966, -0.1511176148010634768 ) ) ;
#26522=CARTESIAN_POINT ( 'NONE',  ( 6.825078400183545391, 2.405270491081310968, 2.624368679222242484 ) ) ;
#26524=CARTESIAN_POINT ( 'NONE',  ( 2.096496217048297694, -0.5238668508756593178, -1.900535169118612755 ) ) ;
#26526=CARTESIAN_POINT ( 'NONE',  ( 6.187759705938407073, 1.828009178079874841, -0.5617473972939349691 ) ) ;
#26531=CARTESIAN_POINT ( 'NONE',  ( 0.7506560300556723853, 1.990167900158135605, 0.3429568431373567483 ) ) ;
#26533=CARTESIAN_POINT ( 'NONE',  ( 5.157380949817064852, -1.946147191792221953, -1.239698497533547661 ) ) ;
#26534=CARTESIAN_POINT ( 'NONE',  ( 6.180128940399614912, -1.088687182605744042, -1.631870318916525120 ) ) ;
#26535=CARTESIAN_POINT ( 'NONE',  ( 3.555471618195928496, 1.543666060651678551, 1.210462546525910010 ) ) ;
#26537=CARTESIAN_POINT ( 'NONE',  ( 0.8971115437808926396, -0.9091470795906559932, -1.799921601489597123 ) ) ;
#26539=CARTESIAN_POINT ( 'NONE',  ( 0.7435476276109568294, 0.4067398897551637305, -2.077755800567067546 ) ) ;
#26542=CARTESIAN_POINT ( 'NONE',  ( 2.150122221082468865, -1.423577340559305071, 1.167554138749152148 ) ) ;
#26543=VERTEX_POINT ( 'NONE', #186189 ) ;
#26545=CARTESIAN_POINT ( 'NONE',  ( 2.918346969001627045, -2.117983955170518851, 0.1081942149789016649 ) ) ;
#26549=CARTESIAN_POINT ( 'NONE',  ( 4.850885224688990860, -1.657504552092460504, 1.224352689660711535 ) ) ;
#26551=CARTESIAN_POINT ( 'NONE',  ( 1.048114208743459619, -1.451426956872736262, 1.132798186660122441 ) ) ;
#26556=CARTESIAN_POINT ( 'NONE',  ( 1.137671262558290763, -1.993743905544292927, 0.9465009238469668240 ) ) ;
#26557=CARTESIAN_POINT ( 'NONE',  ( 2.232027051843707532, -1.476457111770380415, -1.714336117487671007 ) ) ;
#26559=CARTESIAN_POINT ( 'NONE',  ( 2.742218629285391174, 1.002941080561991161, -1.508394886552874237 ) ) ;
#26560=CARTESIAN_POINT ( 'NONE',  ( 2.940549639715861030, -1.447296733178250250, 1.255168957218324666 ) ) ;
#26561=CARTESIAN_POINT ( 'NONE',  ( 4.141125838365485201, -0.1998502692034490602, -2.060677327190631569 ) ) ;
#26564=CARTESIAN_POINT ( 'NONE',  ( 3.221511537501456690, -1.900432112322864464, 0.5242411554721800870 ) ) ;
#26566=CARTESIAN_POINT ( 'NONE',  ( 6.340456170274588743, 1.905924810476855580, 0.2800546826549690782 ) ) ;
#26567=CARTESIAN_POINT ( 'NONE',  ( 4.258574955689950592, -1.386304660245713860, 1.256184814050688603 ) ) ;
#26568=CARTESIAN_POINT ( 'NONE',  ( 1.752963477315866658, 0.7269187894614470569, 2.190284518487267906 ) ) ;
#26570=CARTESIAN_POINT ( 'NONE',  ( 3.367479257110431945, -0.3654178573793941398, 1.824635806631241808 ) ) ;
#26577=CARTESIAN_POINT ( 'NONE',  ( 0.5750072486576313091, -1.983761410860336527, -0.7076436626956124076 ) ) ;
#26579=CARTESIAN_POINT ( 'NONE',  ( 6.380167732536218494, -1.162327630155314484, 1.822330041786710098 ) ) ;
#26580=CARTESIAN_POINT ( 'NONE',  ( 2.285534418239891785, 0.09939759515392716793, -2.118372479656557061 ) ) ;
#26581=CARTESIAN_POINT ( 'NONE',  ( 6.111974619354628935, -0.6785462737385530296, 1.902425049502977528 ) ) ;
#26590=CARTESIAN_POINT ( 'NONE',  ( 5.137907791644652278, 2.014008302827663854, -0.1037760698975112861 ) ) ;
#26594=CARTESIAN_POINT ( 'NONE',  ( 6.157120911006636277, -1.851533521339579380, -1.115484332758958974 ) ) ;
#26598=CARTESIAN_POINT ( 'NONE',  ( 6.503528962204017994, -1.955192063461574259, 0.4926555484118036454 ) ) ;
#26602=CARTESIAN_POINT ( 'NONE',  ( 2.754212737529265986, 0.5811417601193774596, 1.624163882408189652 ) ) ;
#26606=CARTESIAN_POINT ( 'NONE',  ( 1.035986422354659320, 1.742213337529074035, 0.3100009841157587154 ) ) ;
#26607=CARTESIAN_POINT ( 'NONE',  ( 1.875641098811844154, 0.3420332329174725072, -1.983669356598726674 ) ) ;
#26610=CARTESIAN_POINT ( 'NONE',  ( 4.014836333542094238, 1.562590183666902943, -1.558512549626612342 ) ) ;
#26611=CARTESIAN_POINT ( 'NONE',  ( 5.120078768083678789, 2.148437930330206136, -0.3118015998682179823 ) ) ;
#26615=CARTESIAN_POINT ( 'NONE',  ( 3.457788318579996467, -1.606868461378293755, -1.383752881913953292 ) ) ;
#26616=CARTESIAN_POINT ( 'NONE',  ( 2.601185598297011570, -0.1948207814224910128, 2.006963067508853005 ) ) ;
#26617=CARTESIAN_POINT ( 'NONE',  ( 3.621195883455626596, 1.556580008595293219, 0.9264731596013916493 ) ) ;
#26621=CARTESIAN_POINT ( 'NONE',  ( 0.5142528298564854605, 1.293200884458247657, -1.351890787750304135 ) ) ;
#26622=CARTESIAN_POINT ( 'NONE',  ( 5.936143289257818978, 0.8957264799932495025, -1.590785280889392528 ) ) ;
#26624=CARTESIAN_POINT ( 'NONE',  ( 1.252998012795783822, 0.1371590870133630458, -1.910833894730893601 ) ) ;
#26632=CARTESIAN_POINT ( 'NONE',  ( 2.496466685713152334, -1.086271176545396067, 1.821091972856798913 ) ) ;
#26633=CARTESIAN_POINT ( 'NONE',  ( -0.1296875068447916890, 6.948706544289747988, -2.421546651465163347 ) ) ;
#26636=CARTESIAN_POINT ( 'NONE',  ( 4.323478126428228485, -1.887445700180546915, 0.5691147572158322676 ) ) ;
#26637=CARTESIAN_POINT ( 'NONE',  ( 6.152599605923961157, 1.892562589925715466, 0.2737767527046449101 ) ) ;
#26640=CARTESIAN_POINT ( 'NONE',  ( 6.122275928298587466, 2.094602363090028785, 0.3085360351358697462 ) ) ;
#26642=CARTESIAN_POINT ( 'NONE',  ( 1.152881054890652957, -0.5012615762394446728, -2.008655542368184221 ) ) ;
#26643=CARTESIAN_POINT ( 'NONE',  ( 3.064326467805338350, -1.794528509343394473, -0.7426413790867588682 ) ) ;
#26644=ORIENTED_EDGE ( 'NONE', *, *, #42750, .T. ) ;
#26647=CARTESIAN_POINT ( 'NONE',  ( 3.609396000958647210, -2.059664220577660743, 0.3575658041875314219 ) ) ;
#26650=CARTESIAN_POINT ( 'NONE',  ( 0.4865836442241474602, -1.705128007267729506, -0.6119416708995157883 ) ) ;
#26652=CARTESIAN_POINT ( 'NONE',  ( 5.602238545945851023, -2.207063162045197924, -0.003355105161521874588 ) ) ;
#26654=CARTESIAN_POINT ( 'NONE',  ( 2.889901548669851383, 1.559680528474843841, 1.561422205034967314 ) ) ;
#26656=CARTESIAN_POINT ( 'NONE',  ( 1.506358462150747091, -1.903157483220425883, -0.1863595701613318389 ) ) ;
#26658=CARTESIAN_POINT ( 'NONE',  ( 4.809070886388271404, -1.664838503569150419, 1.230558894880565246 ) ) ;
#26660=CARTESIAN_POINT ( 'NONE',  ( 2.377987466095924152, 1.329388817951412394, 1.704534938537699995 ) ) ;
#26661=CARTESIAN_POINT ( 'NONE',  ( 4.915667883426772633, -1.172277214026868464, -1.851500752446763709 ) ) ;
#26672=CARTESIAN_POINT ( 'NONE',  ( 5.963751281166302043, -0.5086355806236466659, 2.006660534352236347 ) ) ;
#26673=CARTESIAN_POINT ( 'NONE',  ( 4.213445252184796708, -0.3281303603181011108, 1.898201707710310826 ) ) ;
#26675=CARTESIAN_POINT ( 'NONE',  ( 0.06993570063764525946, -0.9480199632962028611, 1.779638758220257522 ) ) ;
#26679=CARTESIAN_POINT ( 'NONE',  ( 5.084792200464717915, 1.883391756629303471, 0.5756752826196751549 ) ) ;
#26680=CARTESIAN_POINT ( 'NONE',  ( 6.650320093084655326, -1.776417932240816011, 1.448308594842239838 ) ) ;
#26681=CARTESIAN_POINT ( 'NONE',  ( 5.285714101943871590, 1.228958891529348785, 1.350286652578087665 ) ) ;
#26687=CARTESIAN_POINT ( 'NONE',  ( 2.120424178990498731, 0.001545453418709194504, 1.841430844159386293 ) ) ;
#26688=CARTESIAN_POINT ( 'NONE',  ( 5.941657920834610529, -1.894198565178412119, 0.6822040374353780523 ) ) ;
#26689=CARTESIAN_POINT ( 'NONE',  ( 0.9666848095895408388, 1.880238891319021111, 1.321614243928259880 ) ) ;
#26690=CARTESIAN_POINT ( 'NONE',  ( 5.207842308544940124, 0.6190457291245822224, -1.861560318597937913 ) ) ;
#26694=CARTESIAN_POINT ( 'NONE',  ( 0.6255436495894195481, 0.2045281481408110225, -2.060252820462626477 ) ) ;
#26697=CARTESIAN_POINT ( 'NONE',  ( 1.013356050919094198, -2.038958350640528661, 0.4616950316734638737 ) ) ;
#26698=CARTESIAN_POINT ( 'NONE',  ( 0.1450994221751950586, -1.442925249786636943, -1.190247126510869613 ) ) ;
#26701=CARTESIAN_POINT ( 'NONE',  ( 2.155425581425034487, 0.7450078602235529202, 1.573079536267004030 ) ) ;
#26705=CARTESIAN_POINT ( 'NONE',  ( 3.053030289171186684, -1.410389792183571966, -0.9926723171444253868 ) ) ;
#26706=CARTESIAN_POINT ( 'NONE',  ( 2.454835928891830221, -1.908367152989149718, -1.077367144120815023 ) ) ;
#26707=CARTESIAN_POINT ( 'NONE',  ( 5.777994779145079640, 1.311685685134782231, 1.774619457157788904 ) ) ;
#26710=CARTESIAN_POINT ( 'NONE',  ( 2.219799714087321796, 0.3745715905324221162, -2.138378345340052444 ) ) ;
#26711=CARTESIAN_POINT ( 'NONE',  ( 0.7151340513122245168, -0.2707656271505008982, 1.805370379145049275 ) ) ;
#26712=CARTESIAN_POINT ( 'NONE',  ( 3.696581757058306383, 1.494387559712303526, -1.500228622805776624 ) ) ;
#26713=CARTESIAN_POINT ( 'NONE',  ( 6.539320575229274901, 7.053161517996441532, 2.494893549996656912 ) ) ;
#26715=CARTESIAN_POINT ( 'NONE',  ( 3.263489799031735750, 2.236134436263835568, -0.5039766086074470852 ) ) ;
#26720=CARTESIAN_POINT ( 'NONE',  ( 6.129551335524713096, -0.2748284885467215943, 2.204153950570774345 ) ) ;
#26726=CARTESIAN_POINT ( 'NONE',  ( 4.588517629802620235, -0.5350896943857390564, 1.944070981013111155 ) ) ;
#26728=CARTESIAN_POINT ( 'NONE',  ( 3.168856051829985532, 1.497182195067780386, -1.418930203433153903 ) ) ;
#26733=CARTESIAN_POINT ( 'NONE',  ( 5.929655999079199269, 1.083026401007038952, -1.905042663481799403 ) ) ;
#26734=CARTESIAN_POINT ( 'NONE',  ( 3.955704058034177351, -1.882473782773282700, -0.7231407674024927790 ) ) ;
#26735=CARTESIAN_POINT ( 'NONE',  ( 2.700538275128167687, 1.556679782967337999, 0.9830204120172959525 ) ) ;
#26738=CARTESIAN_POINT ( 'NONE',  ( 6.352569596097208837, 0.5757234290239590102, 1.732508359437078482 ) ) ;
#26740=CARTESIAN_POINT ( 'NONE',  ( 5.928679764299940480, 2.178688510132809064, 0.6099592146414765104 ) ) ;
#26742=CARTESIAN_POINT ( 'NONE',  ( 1.612088513325710126, -2.090005036333367539, 0.2590644908504329824 ) ) ;
#26753=CARTESIAN_POINT ( 'NONE',  ( 2.918465973627711652, -2.218669909917521998, 0.1131645065166643205 ) ) ;
#26754=CARTESIAN_POINT ( 'NONE',  ( 0.03028722099337673168, -1.361824662662258767, -1.737358624739212543 ) ) ;
#26757=CARTESIAN_POINT ( 'NONE',  ( 4.070719198475009293, 1.388998261151509039, -1.385754695631277844 ) ) ;
#26765=CARTESIAN_POINT ( 'NONE',  ( 4.025719079702368752, -0.3592959752154977204, 2.089770972018199835 ) ) ;
#26767=CARTESIAN_POINT ( 'NONE',  ( 4.293933718354110418, -0.8299404887524584051, 1.996233173270183681 ) ) ;
#26768=CARTESIAN_POINT ( 'NONE',  ( 3.808014051635350672, 1.299385917162833692, -1.304790556973287163 ) ) ;
#26769=CARTESIAN_POINT ( 'NONE',  ( 4.839077477813122918, -1.706110771555340744, -1.074664961451990308 ) ) ;
#26772=CARTESIAN_POINT ( 'NONE',  ( 6.298757997817161502, 1.451094931915532404, 0.9604431249435537721 ) ) ;
#26775=CARTESIAN_POINT ( 'NONE',  ( 3.467792127863758456, 2.109446376165153847, -0.4717452660116944196 ) ) ;
#26776=CARTESIAN_POINT ( 'NONE',  ( 5.975935433960425591, 1.776740614516297390, 0.9528632009266968517 ) ) ;
#26778=CARTESIAN_POINT ( 'NONE',  ( 2.887745953747706373, 1.527789104365802286, 1.529575784674996886 ) ) ;
#26779=CARTESIAN_POINT ( 'NONE',  ( 3.268780567936521830, -1.820120084945201500, -0.7576984602858954920 ) ) ;
#26780=CARTESIAN_POINT ( 'NONE',  ( 0.7105614292102403473, -2.296071549169254489, 0.2300874200455073904 ) ) ;
#26781=CARTESIAN_POINT ( 'NONE',  ( 5.003436869212060323, -1.932333990966347503, 0.1943045992871711702 ) ) ;
#26790=CARTESIAN_POINT ( 'NONE',  ( 2.450463542074859724, 2.206263077450395738, 0.05474276496272853509 ) ) ;
#26792=CARTESIAN_POINT ( 'NONE',  ( 6.561383603009730336, 1.629167342741120406, 1.092533971175007723 ) ) ;
#26796=CARTESIAN_POINT ( 'NONE',  ( 0.1749903794560228876, 5.724274800596795387, -2.549334106949477263 ) ) ;
#26799=CARTESIAN_POINT ( 'NONE',  ( 5.788959344212086577, 1.397023377451442228, 1.199316859253784839 ) ) ;
#26806=CARTESIAN_POINT ( 'NONE',  ( 6.187751663909415001, 2.028806014889028120, -0.6170373231123224000 ) ) ;
#26809=CARTESIAN_POINT ( 'NONE',  ( 0.3564142383026321914, 0.7882222137287850927, 1.904402214580179331 ) ) ;
#26811=CARTESIAN_POINT ( 'NONE',  ( 2.049040314030759369, 1.621234533420016888, -0.9136741289750174300 ) ) ;
#26812=CARTESIAN_POINT ( 'NONE',  ( 4.493604616018744835, -1.840970053361364656, -0.04044509776383875543 ) ) ;
#26816=ORIENTED_EDGE ( 'NONE', *, *, #176013, .F. ) ;
#26817=CARTESIAN_POINT ( 'NONE',  ( 4.740968412965463230, 0.3751893352213676591, 2.174603215771487630 ) ) ;
#26818=CARTESIAN_POINT ( 'NONE',  ( 6.257125660641059461, -1.935629482380639033, -1.171090987803388606 ) ) ;
#26820=CARTESIAN_POINT ( 'NONE',  ( 6.521734044569575062, -0.3839667898355834663, 1.776778520094610903 ) ) ;
#26821=CARTESIAN_POINT ( 'NONE',  ( 6.315652784560811916, -1.257152391787072387, -1.445590397462018117 ) ) ;
#26825=CARTESIAN_POINT ( 'NONE',  ( 5.338497774373327509, 1.135723818413657549, -1.538349510941657838 ) ) ;
#26827=CARTESIAN_POINT ( 'NONE',  ( 1.252583056964752029, -1.476889893665521925, 1.148006582770304096 ) ) ;
#26829=CARTESIAN_POINT ( 'NONE',  ( 2.096888995370162156, 1.803417055948232761, 0.9023429676050932491 ) ) ;
#26831=CARTESIAN_POINT ( 'NONE',  ( 3.738982163358902877, 0.3088429966837880070, 2.083174605729753992 ) ) ;
#26836=CARTESIAN_POINT ( 'NONE',  ( 3.111586589114573975, 1.594763109418888991, 1.239388640070989478 ) ) ;
#26839=CARTESIAN_POINT ( 'NONE',  ( 3.989662644735529451, 1.562606173494068829, 1.493797087085822595 ) ) ;
#26844=CARTESIAN_POINT ( 'NONE',  ( 1.733130889747940495, -2.061367544037566280, -0.6818780404978814769 ) ) ;
#26847=CARTESIAN_POINT ( 'NONE',  ( 0.8723036553972834950, -0.04505207493780280514, -1.840872848514919502 ) ) ;
#26849=CARTESIAN_POINT ( 'NONE',  ( 2.542740116143254792, -1.820367712357463974, 1.220030464664762393 ) ) ;
#26851=CARTESIAN_POINT ( 'NONE',  ( 3.169090989670137581, -2.089828869452925009, -0.8673982956902188679 ) ) ;
#26857=CARTESIAN_POINT ( 'NONE',  ( 4.305725593384774896, -1.765090080884828661, 0.1286423764911871492 ) ) ;
#26860=CARTESIAN_POINT ( 'NONE',  ( 1.114449138222296742, -0.9466070430152218051, -1.881282081674582995 ) ) ;
#26865=CARTESIAN_POINT ( 'NONE',  ( 6.362907676916636390, -0.1017654035869921675, -2.013986322929907757 ) ) ;
#26870=CARTESIAN_POINT ( 'NONE',  ( 3.625732356982212412, -1.113523340526129335, -1.502988901547596567 ) ) ;
#26871=CARTESIAN_POINT ( 'NONE',  ( 4.065334711822697678, 1.773058433220272789, 1.068561072119569744 ) ) ;
#26880=CARTESIAN_POINT ( 'NONE',  ( 3.754310534785664899, -1.959519245081872585, -0.09869234604030494018 ) ) ;
#26881=CARTESIAN_POINT ( 'NONE',  ( 2.372422516638694745, -0.4444355326964634090, 1.966343308868031103 ) ) ;
#26883=CARTESIAN_POINT ( 'NONE',  ( 6.639320575229253230, 6.038193673056964528, 2.491643636677738360 ) ) ;
#26884=CARTESIAN_POINT ( 'NONE',  ( 0.7548939078372005618, -1.576849831105286537, -1.005952255950369301 ) ) ;
#26886=CARTESIAN_POINT ( 'NONE',  ( 3.217044422572811424, 1.584514289383936347, -1.241758421991135064 ) ) ;
#26888=CARTESIAN_POINT ( 'NONE',  ( 3.251669871774115705, 2.065089526129770814, -0.4662906127247400945 ) ) ;
#26890=CARTESIAN_POINT ( 'NONE',  ( 5.371561628297467195, -0.3073141173523045167, 2.047320497149993646 ) ) ;
#26892=CARTESIAN_POINT ( 'NONE',  ( 0.2575178465553956686, 2.067414111102347185, -0.3107122069949171395 ) ) ;
#26894=CARTESIAN_POINT ( 'NONE',  ( 5.403274641334286699, 1.493489847867332854, 1.049580640413529276 ) ) ;
#26901=CARTESIAN_POINT ( 'NONE',  ( -0.04078422793344065045, -1.398654746659812043, -1.150989216800960335 ) ) ;
#26911=PRESENTATION_STYLE_ASSIGNMENT (( #123463 ) ) ;
#26912=CARTESIAN_POINT ( 'NONE',  ( 0.1399997263885795207, 2.876830203203218694, -2.488333633689450597 ) ) ;
#26915=CARTESIAN_POINT ( 'NONE',  ( 2.342574202377019521, -1.930441307185966515, -0.3890957575964202886 ) ) ;
#26916=CARTESIAN_POINT ( 'NONE',  ( 3.638296137631126914, 0.7283958097016438593, 1.880429543521966007 ) ) ;
#26918=CARTESIAN_POINT ( 'NONE',  ( 6.827182134110235445, 0.5726250382554041174, 2.141766166723162002 ) ) ;
#26919=CARTESIAN_POINT ( 'NONE',  ( 3.539196308827243787, -1.659330947522210886, -1.431560661003590695 ) ) ;
#26921=CARTESIAN_POINT ( 'NONE',  ( 1.975490806028988633, 1.844176287694970995, -0.5568081592420818238 ) ) ;
#26924=CARTESIAN_POINT ( 'NONE',  ( 0.2329586101569346424, 2.887341434808698981, -2.334705299551639079 ) ) ;
#26931=CARTESIAN_POINT ( 'NONE',  ( 5.952668924537682038, -1.582617586749142102, -0.9407850039931386910 ) ) ;
#26932=CARTESIAN_POINT ( 'NONE',  ( 2.596342214666306880, -1.033070880159161264, 1.727660946855133606 ) ) ;
#26933=CARTESIAN_POINT ( 'NONE',  ( 4.112918304081806475, 0.7786346584819616723, -2.162581562504022337 ) ) ;
#26934=CARTESIAN_POINT ( 'NONE',  ( -0.02900071798683095947, 1.997299723774683455, -2.587491137808914488 ) ) ;
#26935=CARTESIAN_POINT ( 'NONE',  ( 2.078732565759545903, 1.734175166166322501, 0.6755533923482255343 ) ) ;
#26940=EDGE_CURVE ( 'NONE', #59934, #15524, #20191, .T. ) ;
#26942=CARTESIAN_POINT ( 'NONE',  ( 5.407793395736015363, -0.9409669688741102433, -1.867122848840888416 ) ) ;
#26943=CARTESIAN_POINT ( 'NONE',  ( 3.994877460428855276, 1.580554378303768992, -1.000287695324620252 ) ) ;
#26945=ORIENTED_EDGE ( 'NONE', *, *, #55426, .F. ) ;
#26948=CARTESIAN_POINT ( 'NONE',  ( 6.727182134110236689, 0.008744176509112643741, 1.710970312420513562 ) ) ;
#26950=CARTESIAN_POINT ( 'NONE',  ( 1.177864744846460754, 1.312336027064511690, 1.133722492108141244 ) ) ;
#26954=CARTESIAN_POINT ( 'NONE',  ( 5.559503684912662003, 1.770657277210012204, 1.256059096652543783 ) ) ;
#26955=CARTESIAN_POINT ( 'NONE',  ( 3.967279163243800255, 0.2216459979678051528, -1.812115712870238537 ) ) ;
#26956=CARTESIAN_POINT ( 'NONE',  ( 2.729291793292155432, 0.1011638768560127188, -1.959297240552673403 ) ) ;
#26959=CARTESIAN_POINT ( 'NONE',  ( 2.772263606761758759, 2.110060413066455975, -0.2101530891244970389 ) ) ;
#26965=CARTESIAN_POINT ( 'NONE',  ( 0.6728209460903146200, 1.430239379376567976, -1.496996390900617646 ) ) ;
#26969=CARTESIAN_POINT ( 'NONE',  ( 3.176664282717697851, 1.000473465829452735, 1.983322933999843052 ) ) ;
#26971=CARTESIAN_POINT ( 'NONE',  ( 0.7042444638330731532, 2.126757524241583486, 0.8727403922216511178 ) ) ;
#26973=CARTESIAN_POINT ( 'NONE',  ( 0.2331563151865486683, 0.005903526429595904942, -1.945944850731482934 ) ) ;
#26976=CARTESIAN_POINT ( 'NONE',  ( 0.1331565106231363538, 2.033293680964400885, -2.362282156872722805 ) ) ;
#26977=CARTESIAN_POINT ( 'NONE',  ( 5.706567001488551227, 1.626822141722890303, 0.8623401093873286349 ) ) ;
#26979=CARTESIAN_POINT ( 'NONE',  ( -0.1102773484824015326, 7.629137130509110243, -2.803480817674379288 ) ) ;
#26980=CARTESIAN_POINT ( 'NONE',  ( 2.502614896622682661, 1.386922750403916105, -1.025098202461205865 ) ) ;
#26981=CARTESIAN_POINT ( 'NONE',  ( 1.270720652900014791, -0.3006520276036573902, -1.993892820393451615 ) ) ;
#26982=CARTESIAN_POINT ( 'NONE',  ( 1.845381457188604690, -1.911753278855784943, 1.209540087214598270 ) ) ;
#26983=CARTESIAN_POINT ( 'NONE',  ( 4.969407589744497145, 0.2071734034183834172, -2.095845648730967792 ) ) ;
#26985=CARTESIAN_POINT ( 'NONE',  ( 4.165142103487808889, 0.2181862141000940336, -1.756177202920036429 ) ) ;
#26987=CARTESIAN_POINT ( 'NONE',  ( 6.532792773074245218, -2.049936377808206700, 1.026291560346163534 ) ) ;
#26988=CARTESIAN_POINT ( 'NONE',  ( 4.646344025792163990, -1.477054284018078256, 1.098930429567553047 ) ) ;
#26992=CARTESIAN_POINT ( 'NONE',  ( 4.453197812796324762, 0.4814713343750369190, -2.137748681182355170 ) ) ;
#26995=CARTESIAN_POINT ( 'NONE',  ( 4.475093801846619535, 1.891600172242546840, 0.8420093967692193759 ) ) ;
#26996=CARTESIAN_POINT ( 'NONE',  ( 0.1281391398850126040, 2.011452084832816123, 0.1435147193784985509 ) ) ;
#26999=CARTESIAN_POINT ( 'NONE',  ( 3.615773638797363798, -1.897832126884700932, 0.3302691188315133863 ) ) ;
#27002=CARTESIAN_POINT ( 'NONE',  ( 6.381110825713084189, -1.939362502171553482, -0.8581636585355473246 ) ) ;
#27005=CARTESIAN_POINT ( 'NONE',  ( 6.875078400183573635, 7.629137130509068498, 2.744348168701661095 ) ) ;
#27012=CARTESIAN_POINT ( 'NONE',  ( 1.187862215860764126, -1.241893603568875681, -1.518774446641702580 ) ) ;
#27015=CARTESIAN_POINT ( 'NONE',  ( 5.600043156098196917, 0.7966083592686534764, -1.793046234938546757 ) ) ;
#27018=CARTESIAN_POINT ( 'NONE',  ( 6.455963997168007396, 2.156291961557708525, -0.1537611777119098910 ) ) ;
#27022=CARTESIAN_POINT ( 'NONE',  ( 6.643826690903999577, 0.7566192825128185140, -1.820567107441137589 ) ) ;
#27023=CARTESIAN_POINT ( 'NONE',  ( 6.503290690126083184, 1.715628873550764988, 0.2497197086974659863 ) ) ;
#27025=CARTESIAN_POINT ( 'NONE',  ( 2.683357600500847262, 1.551837136583393839, 1.547750905674146971 ) ) ;
#27026=CARTESIAN_POINT ( 'NONE',  ( 4.225798673374229431, -2.209433879803673673, 0.6658836873896284425 ) ) ;
#27027=CARTESIAN_POINT ( 'NONE',  ( 5.975869988448771153, 1.224042345451004765, 1.657734310933855815 ) ) ;
#27028=CARTESIAN_POINT ( 'NONE',  ( 1.781094086345108130, 1.339032250488644937, 1.406688339355038009 ) ) ;
#27031=CARTESIAN_POINT ( 'NONE',  ( 4.974906307097914926, -1.534222593358970821, 1.464151343314526121 ) ) ;
#27033=CARTESIAN_POINT ( 'NONE',  ( 2.092422861153935276, -0.4390285686692517175, 1.967888031366466395 ) ) ;
#27037=CARTESIAN_POINT ( 'NONE',  ( 0.3459771380207553593, 1.820543102168985961, 0.1377627428671979182 ) ) ;
#27043=CARTESIAN_POINT ( 'NONE',  ( 5.682513945847499137, -2.010110750271485447, -0.4539000206328601683 ) ) ;
#27049=CARTESIAN_POINT ( 'NONE',  ( 5.074870355641393438, -1.461326316769593348, 1.394373881654621394 ) ) ;
#27056=CARTESIAN_POINT ( 'NONE',  ( 4.750885258907265651, -1.656392207783722315, 1.226022070186979063 ) ) ;
#27057=CARTESIAN_POINT ( 'NONE',  ( 2.338517726396415863, 0.5350873343827439177, -1.944071628254496087 ) ) ;
#27065=CARTESIAN_POINT ( 'NONE',  ( 3.268907511149142575, -2.013924394373915128, 0.09611935726179518524 ) ) ;
#27066=CARTESIAN_POINT ( 'NONE',  ( 1.974305314296275649, -0.08955604370030831318, -1.839086841257123073 ) ) ;
#27067=CARTESIAN_POINT ( 'NONE',  ( 0.5754005350990994971, -2.174928102591418888, -0.7718245971977951703 ) ) ;
#27070=CARTESIAN_POINT ( 'NONE',  ( 3.075615952314793233, 2.053625483174918553, -0.6748976972978243394 ) ) ;
#27073=CARTESIAN_POINT ( 'NONE',  ( 2.407932310410058285, 0.5022953597978959683, 2.242707597164790734 ) ) ;
#27077=CARTESIAN_POINT ( 'NONE',  ( 1.445950363956361340, 1.868363765441739099, 0.09516058986362013750 ) ) ;
#27078=CARTESIAN_POINT ( 'NONE',  ( 5.453970954872065846, 1.969229766360120149, -0.09616449669870225092 ) ) ;
#27082=CARTESIAN_POINT ( 'NONE',  ( 0.8915962724085277902, 1.944627461026976034, -1.043433064090833140 ) ) ;
#27086=CARTESIAN_POINT ( 'NONE',  ( 6.539320575229251808, 6.034535422585679321, 2.798157489527762554 ) ) ;
#27087=CARTESIAN_POINT ( 'NONE',  ( 4.944191625186433292, 1.966121618969366214, 0.1460544362237597982 ) ) ;
#27088=CARTESIAN_POINT ( 'NONE',  ( 0.1059362375676886209, 1.575662574916199210, 1.419458935296296520 ) ) ;
#27089=CARTESIAN_POINT ( 'NONE',  ( 4.336755680664809098, 2.262710760593138470, 0.4526611301470875870 ) ) ;
#27091=CARTESIAN_POINT ( 'NONE',  ( 2.817292378285217502, -1.792290562959488742, -1.020665671854523060 ) ) ;
#27098=CARTESIAN_POINT ( 'NONE',  ( 5.705598495378635171, -1.708133787927707647, -1.340148157549289953 ) ) ;
#27100=CARTESIAN_POINT ( 'NONE',  ( 4.089279031174639201, -0.7008038172400687937, 1.702867937621636463 ) ) ;
#27103=CARTESIAN_POINT ( 'NONE',  ( 5.196902890030515643, 1.791362914573800369, 1.262263373074036688 ) ) ;
#27105=CARTESIAN_POINT ( 'NONE',  ( 0.5974158272751062260, 1.880195615759198136, -1.258034406164424635 ) ) ;
#27110=CARTESIAN_POINT ( 'NONE',  ( 1.217257651388839346, -1.727774110360464244, 0.3828142623626716867 ) ) ;
#27113=CARTESIAN_POINT ( 'NONE',  ( 5.268231569329090647, 2.010679013512342017, -0.1011730594673541789 ) ) ;
#27115=CARTESIAN_POINT ( 'NONE',  ( 3.680784645728672810, -2.029037780879865416, -0.5636793167548505012 ) ) ;
#27116=CARTESIAN_POINT ( 'NONE',  ( 2.741684679331716890, 1.906140283219289966, -0.1903247725174895544 ) ) ;
#27118=CARTESIAN_POINT ( 'NONE',  ( 4.492606276566666779, 1.931098607525572497, 0.3863565733641035616 ) ) ;
#27119=CARTESIAN_POINT ( 'NONE',  ( 5.519787823685118333, -0.4868164491665989413, 1.960129884169951708 ) ) ;
#27120=CARTESIAN_POINT ( 'NONE',  ( 1.779943879855113709, -1.003247456797161652, 1.578688272967261996 ) ) ;
#27121=CARTESIAN_POINT ( 'NONE',  ( 4.811038506879902421, 1.503007855926122405, 0.8461308117306536314 ) ) ;
#27122=CARTESIAN_POINT ( 'NONE',  ( 1.687617486097678476, 1.829050272730630144, -0.5582976189952293389 ) ) ;
#27124=CARTESIAN_POINT ( 'NONE',  ( 1.840723031453334935, 2.183200880077686978, 0.3216222850719457349 ) ) ;
#27127=CARTESIAN_POINT ( 'NONE',  ( 6.602011099637477010, 0.7519813002578833450, -1.812223124677159181 ) ) ;
#27134=CARTESIAN_POINT ( 'NONE',  ( 1.732962091629593804, -1.965256999408044436, -0.6514315320021792921 ) ) ;
#27139=CARTESIAN_POINT ( 'NONE',  ( 0.02995210924121824436, -1.980234168275105455, 0.3962368897427023806 ) ) ;
#27146=CARTESIAN_POINT ( 'NONE',  ( 5.343124974464078747, -1.122324884721880078, 1.674632237393176792 ) ) ;
#27147=CARTESIAN_POINT ( 'NONE',  ( 4.417137112658839015, -1.749089155124187389, 0.7819188135024003339 ) ) ;
#27149=CARTESIAN_POINT ( 'NONE',  ( 3.017305944477025825, -2.111434807548946857, 0.5868732223921411251 ) ) ;
#27150=CARTESIAN_POINT ( 'NONE',  ( 0.1335669894368317900, 1.324834237272943360, -2.404533294357531048 ) ) ;
#27152=CARTESIAN_POINT ( 'NONE',  ( 5.607686816480834224, 1.527379804643314687, 1.311666717936723403 ) ) ;
#27153=CARTESIAN_POINT ( 'NONE',  ( 1.687617486097678476, 1.829050272730630144, -0.5582976189952293389 ) ) ;
#27156=CARTESIAN_POINT ( 'NONE',  ( 0.1754079408978586052, 1.496066871905444629, 1.352139405095334590 ) ) ;
#27158=CARTESIAN_POINT ( 'NONE',  ( 3.421503388043937832, -1.247306758965301521, -1.677755357943153447 ) ) ;
#27160=CARTESIAN_POINT ( 'NONE',  ( 1.658790106635851469, -1.476843439067159425, -0.8906862264850596844 ) ) ;
#27162=CARTESIAN_POINT ( 'NONE',  ( 6.533471381225442798, -0.1521382079053348602, 2.086446650026114735 ) ) ;
#27169=CARTESIAN_POINT ( 'NONE',  ( 2.543383136322028282, -1.689629589678593558, 0.6535807426650240837 ) ) ;
#27174=CARTESIAN_POINT ( 'NONE',  ( 3.281707762122548555, 1.766655041338391907, -0.3996267988317265818 ) ) ;
#27175=CARTESIAN_POINT ( 'NONE',  ( 6.539320575229216281, 4.696526872534390940, 2.559412612844500057 ) ) ;
#27179=CARTESIAN_POINT ( 'NONE',  ( 3.930005801358939621, 1.032382326871328804, 1.548228005463901491 ) ) ;
#27180=CARTESIAN_POINT ( 'NONE',  ( 1.897908843228306663, -0.9047085692259320133, -1.688519222619834892 ) ) ;
#27181=CARTESIAN_POINT ( 'NONE',  ( 0.4635302585514287088, 1.806487598472360956, -0.2625014351145052438 ) ) ;
#27189=CARTESIAN_POINT ( 'NONE',  ( 5.612145322048014862, 1.967363499941950034, -0.09270071294615632451 ) ) ;
#27192=CARTESIAN_POINT ( 'NONE',  ( 0.6036074345479571779, -2.080388865039545454, 0.2067186989125231189 ) ) ;
#27194=CARTESIAN_POINT ( 'NONE',  ( 5.948256396973989446, 1.924214498663083139, 0.09423418586224258098 ) ) ;
#27196=CARTESIAN_POINT ( 'NONE',  ( 1.078802750678783395, -0.04027803099338270881, -1.825304540826321542 ) ) ;
#27197=CARTESIAN_POINT ( 'NONE',  ( 2.368051099418837069, 2.164043333312406503, -0.4318774905316472013 ) ) ;
#27199=CARTESIAN_POINT ( 'NONE',  ( 1.089939655121434203, 1.141396045679959004, 1.534244836814010693 ) ) ;
#27200=CARTESIAN_POINT ( 'NONE',  ( 0.7484202955074462649, -1.954263247020354477, -0.2444711731117015785 ) ) ;
#27201=CARTESIAN_POINT ( 'NONE',  ( 2.102980028956519476, -0.4233231936755370572, 1.895218400837359818 ) ) ;
#27203=CARTESIAN_POINT ( 'NONE',  ( 0.4564073884281876214, 1.492024165150519055, 1.356095248386236074 ) ) ;
#27205=CARTESIAN_POINT ( 'NONE',  ( 6.508657375787280763, 0.5831478024676381988, 1.767317905175052051 ) ) ;
#27211=CARTESIAN_POINT ( 'NONE',  ( 2.050558489324630251, -1.691691439650149897, 1.393213601605561180 ) ) ;
#27215=CARTESIAN_POINT ( 'NONE',  ( 3.316849939159485228, 1.650902842016691130, 0.7798126646740562995 ) ) ;
#27219=CARTESIAN_POINT ( 'NONE',  ( 6.925078400183573457, 0.5887076473912872254, 1.908330883025354030 ) ) ;
#27221=CARTESIAN_POINT ( 'NONE',  ( 0.9965603196819513565, -0.4670424642401714288, -1.868911657674779958 ) ) ;
#27222=CARTESIAN_POINT ( 'NONE',  ( 5.910985094894211755, -1.548708053515185812, 1.204094020389692377 ) ) ;
#27227=CARTESIAN_POINT ( 'NONE',  ( 5.284801750429747536, 1.933107837519608685, -1.032524723389722787 ) ) ;
#27229=CARTESIAN_POINT ( 'NONE',  ( 4.592674910654532816, 2.029287475768901228, 0.4089837765668055680 ) ) ;
#27232=CARTESIAN_POINT ( 'NONE',  ( 4.395370282159323239, -0.9827166871091972400, -2.078181120130776272 ) ) ;
#27237=CARTESIAN_POINT ( 'NONE',  ( 6.620655732516659064, 6.039214117936751336, 2.421170424969817603 ) ) ;
#27239=CARTESIAN_POINT ( 'NONE',  ( 5.191327941051770978, -0.6971716684453888035, 1.812662890818200756 ) ) ;
#27244=CARTESIAN_POINT ( 'NONE',  ( 4.640819915729988310, 1.831716588661407963, 0.5496940206762624959 ) ) ;
#27245=CARTESIAN_POINT ( 'NONE',  ( 6.124008131756068174, -0.9624739961165188484, -1.431025375277717115 ) ) ;
#27246=CARTESIAN_POINT ( 'NONE',  ( 4.048064755690682581, 0.9548552675892291175, 1.776167154503265566 ) ) ;
#27249=CARTESIAN_POINT ( 'NONE',  ( 1.763735852432495754, 1.075751846022491964, 1.792481376920366687 ) ) ;
#27250=CARTESIAN_POINT ( 'NONE',  ( 0.1976571007769452604, -1.769309276362411643, -0.05040135802934773979 ) ) ;
#27251=CARTESIAN_POINT ( 'NONE',  ( 6.135388727473008785, 0.6351960432287793168, 1.913804721665197883 ) ) ;
#27253=CARTESIAN_POINT ( 'NONE',  ( 3.345926335499046722, 2.292435215394402093, 0.0001471259066659902901 ) ) ;
#27254=CARTESIAN_POINT ( 'NONE',  ( 1.921426573741076727, 1.003422016191083399, -1.421716384592019544 ) ) ;
#27255=CARTESIAN_POINT ( 'NONE',  ( 2.742561299210785286, 1.174483946500170184, -1.765453564165630596 ) ) ;
#27257=CARTESIAN_POINT ( 'NONE',  ( 0.5789038866980666942, 1.201919051685101270, -1.249903294292388667 ) ) ;
#27259=CARTESIAN_POINT ( 'NONE',  ( 1.398636348511049565, 0.3583461405318502102, 1.826042456754966681 ) ) ;
#27260=CARTESIAN_POINT ( 'NONE',  ( 2.576841123524225452, 1.419588041764899611, -1.642854796848471244 ) ) ;
#27261=CARTESIAN_POINT ( 'NONE',  ( 3.327361509216096191, -1.530157842762596143, -1.313544516083162028 ) ) ;
#27262=CARTESIAN_POINT ( 'NONE',  ( 4.562500000000002665, -1.451031289061298857, -1.451031289060931595 ) ) ;
#27265=CARTESIAN_POINT ( 'NONE',  ( 6.234985708453399944, 0.1916802727454213762, 1.916943350541326030 ) ) ;
#27267=CARTESIAN_POINT ( 'NONE',  ( 2.971146563671855034, -1.679565462486251048, 1.453923022682623856 ) ) ;
#27273=CARTESIAN_POINT ( 'NONE',  ( -0.1044638861024569515, -0.1585131741546479955, -2.186235582987208659 ) ) ;
#27274=CARTESIAN_POINT ( 'NONE',  ( 4.351973852746993110, -0.7528527933186466292, 1.811862133468461922 ) ) ;
#27279=CARTESIAN_POINT ( 'NONE',  ( 5.395900114300756556, -0.8213888976819706533, 2.108206106441696370 ) ) ;
#27281=CARTESIAN_POINT ( 'NONE',  ( 2.348159106025033083, -0.8842165242596754515, 1.863692774951962727 ) ) ;
#27285=CARTESIAN_POINT ( 'NONE',  ( 3.690566713891149320, -0.3619836066245524786, -1.835009008997898761 ) ) ;
#27286=CARTESIAN_POINT ( 'NONE',  ( 2.672175078814063909, 1.228020439816409848, 1.224710958539473094 ) ) ;
#27287=CARTESIAN_POINT ( 'NONE',  ( 6.181208317857348256, 1.509947553572440704, 1.588605474358975478 ) ) ;
#27288=CARTESIAN_POINT ( 'NONE',  ( 0.9739772326014315418, 2.126351460888118883, -0.5901193814053447007 ) ) ;
#27289=CARTESIAN_POINT ( 'NONE',  ( 4.469695567000064429, 2.097540297429688838, -0.5223010940857697459 ) ) ;
#27290=CARTESIAN_POINT ( 'NONE',  ( 5.665949523032352886, -1.230194547739250854, 1.502597557546548446 ) ) ;
#27294=CARTESIAN_POINT ( 'NONE',  ( -0.06985027309261250539, -2.078401542846250116, 0.4200961532789050379 ) ) ;
#27300=CARTESIAN_POINT ( 'NONE',  ( 3.457459740917231628, 0.4424662778084071935, -1.771134634090239190 ) ) ;
#27302=CARTESIAN_POINT ( 'NONE',  ( 2.345003271878861373, 0.4830727525354863716, 2.153096645625157457 ) ) ;
#27308=CARTESIAN_POINT ( 'NONE',  ( 0.8791727066333665519, -1.827835516345464484, -0.8596444897858869227 ) ) ;
#27309=CARTESIAN_POINT ( 'NONE',  ( 0.6629299983115041206, 0.6194173074674096391, 2.027988828570789437 ) ) ;
#27313=CARTESIAN_POINT ( 'NONE',  ( 2.623689330893996363, 1.826062842344724269, -0.3576783775682371158 ) ) ;
#27316=CARTESIAN_POINT ( 'NONE',  ( 0.6730137850648570952, -2.035850703004048246, -0.7271551459356735414 ) ) ;
#27322=CARTESIAN_POINT ( 'NONE',  ( 3.633261591126951018, -1.686358373764598406, 0.7000054678709469735 ) ) ;
#27326=CARTESIAN_POINT ( 'NONE',  ( 6.802112138117927920, -1.802125342305498146, 0.9040232568291312054 ) ) ;
#27327=CARTESIAN_POINT ( 'NONE',  ( 5.648353745280480176, -1.448853643138726000, 1.135948691490688667 ) ) ;
#27328=CARTESIAN_POINT ( 'NONE',  ( -0.02319159430947541692, 2.051704324979522820, -2.228571760951563618 ) ) ;
#27329=CARTESIAN_POINT ( 'NONE',  ( 4.125798732227327292, -2.208944405816467338, 0.6678306985251744043 ) ) ;
#27331=CARTESIAN_POINT ( 'NONE',  ( 0.8079727292511580394, -2.051105382888893658, 0.1991618667988598601 ) ) ;
#27333=CARTESIAN_POINT ( 'NONE',  ( 1.874458991091961568, -0.09742729390963811298, -1.939748921942837878 ) ) ;
#27335=CARTESIAN_POINT ( 'NONE',  ( 5.589350027729360626, 1.375356176494828553, -1.841343765151080003 ) ) ;
#27338=CARTESIAN_POINT ( 'NONE',  ( 4.574985519202336981, -0.0001439422951596270033, -1.870836309977530920 ) ) ;
#27340=CARTESIAN_POINT ( 'NONE',  ( 2.197387184563174944, 1.746976956643018442, -0.7784620831182070821 ) ) ;
#27343=CARTESIAN_POINT ( 'NONE',  ( 3.897267319706390065, 1.864829029706360330, -1.179861312946443697 ) ) ;
#27345=CARTESIAN_POINT ( 'NONE',  ( 6.883263157960364254, 2.447565407927353220, 2.329071302269662080 ) ) ;
#27346=CARTESIAN_POINT ( 'NONE',  ( -0.2108831679771168421, 6.948330828014878335, -2.492181822431015270 ) ) ;
#27349=CARTESIAN_POINT ( 'NONE',  ( 1.809780422520257170, -1.956919260803160032, 0.2374922769308157044 ) ) ;
#27350=CARTESIAN_POINT ( 'NONE',  ( 2.186954941700581134, -2.263197366206463279, -0.4496495349725088686 ) ) ;
#27351=CARTESIAN_POINT ( 'NONE',  ( 2.224987305166142626, -1.792472147789250236, -0.7979012372742313453 ) ) ;
#27354=CARTESIAN_POINT ( 'NONE',  ( 5.981316409642544407, -0.05633626937831189702, 2.061977559458886056 ) ) ;
#27356=CARTESIAN_POINT ( 'NONE',  ( 3.854704076794239764, -1.883312302057647880, -0.7212934815618715634 ) ) ;
#27362=CARTESIAN_POINT ( 'NONE',  ( 2.096751143937364947, 2.146985459555655673, 0.3218790139906148040 ) ) ;
#27366=CARTESIAN_POINT ( 'NONE',  ( 1.967826412060974084, 0.9573937279930484490, 1.606809688844474726 ) ) ;
#27368=CARTESIAN_POINT ( 'NONE',  ( 6.327428285124779173, -2.037722512857220725, 0.7216720553550812767 ) ) ;
#27370=CARTESIAN_POINT ( 'NONE',  ( 6.827182134110231893, 2.454327069706051745, 2.294502690501096787 ) ) ;
#27373=CARTESIAN_POINT ( 'NONE',  ( 2.666550042863625958, 0.6461651886627232111, 1.799920402468312197 ) ) ;
#27374=CARTESIAN_POINT ( 'NONE',  ( 4.346413238989558003, 0.4729554063761501892, 1.705410949051559877 ) ) ;
#27375=CARTESIAN_POINT ( 'NONE',  ( 1.664566505720616929, 0.6010121217654046388, 1.815428919054395518 ) ) ;
#27377=CARTESIAN_POINT ( 'NONE',  ( 6.573869778094940663, -0.8146055380063941254, 1.732351315116484880 ) ) ;
#27379=CARTESIAN_POINT ( 'NONE',  ( 0.7837444799244470683, -1.966470238067185905, 0.6478734989143407619 ) ) ;
#27381=CARTESIAN_POINT ( 'NONE',  ( 5.102362337376947998, -0.6309395149336484154, -1.761181640970375106 ) ) ;
#27382=CARTESIAN_POINT ( 'NONE',  ( 1.892912435568369744, 1.589020553905008626, -0.8988452475950716725 ) ) ;
#27383=CARTESIAN_POINT ( 'NONE',  ( 6.235036409211808461, 0.2120174297785166195, 2.196685143856290878 ) ) ;
#27387=CARTESIAN_POINT ( 'NONE',  ( 2.541531169099729759, 1.886825176844410645, -0.8337591773379445792 ) ) ;
#27394=ORIENTED_EDGE ( 'NONE', *, *, #85738, .T. ) ;
#27395=CARTESIAN_POINT ( 'NONE',  ( 5.037584538744971141, 1.933038169019934527, -0.7419538039311265321 ) ) ;
#27397=CARTESIAN_POINT ( 'NONE',  ( 2.530746307392011563, 2.096003997654236173, 0.5278882200696957128 ) ) ;
#27399=CARTESIAN_POINT ( 'NONE',  ( 3.510419912045096069, -2.017469964673058946, -0.09679370177045029666 ) ) ;
#27401=CARTESIAN_POINT ( 'NONE',  ( 6.720655732516679137, 7.052218778754904882, 2.671889809988809983 ) ) ;
#27407=CARTESIAN_POINT ( 'NONE',  ( 0.9191581010105540628, -1.820984308097562954, 0.8666112775468015617 ) ) ;
#27409=CARTESIAN_POINT ( 'NONE',  ( 6.374583145400191775, -0.1054333438532777389, -2.189162923280890904 ) ) ;
#27411=CARTESIAN_POINT ( 'NONE',  ( 4.324404969281474109, -0.8226261416362996570, -1.726585468271451651 ) ) ;
#27415=CARTESIAN_POINT ( 'NONE',  ( 3.585564690064909854, -0.5826378547920657569, 1.930424337232887977 ) ) ;
#27417=CARTESIAN_POINT ( 'NONE',  ( 5.280183324938524159, -0.9553487854751692154, 1.435786287184135368 ) ) ;
#27421=CARTESIAN_POINT ( 'NONE',  ( 3.866346082213562685, -1.258301477641217803, 1.384200088751494251 ) ) ;
#27423=CARTESIAN_POINT ( 'NONE',  ( 1.305626334525695986, -1.629615561912756805, -1.276682400165381148 ) ) ;
#27427=CARTESIAN_POINT ( 'NONE',  ( 6.059207019112636594, -1.526464042762348594, 0.9750640111952106892 ) ) ;
#27430=CARTESIAN_POINT ( 'NONE',  ( 0.2986855335190057859, -0.2218818089524568216, -1.797891974444510765 ) ) ;
#27434=CARTESIAN_POINT ( 'NONE',  ( 0.7484013653801385724, -1.946605496936428370, -0.2438083268051088881 ) ) ;
#27436=CARTESIAN_POINT ( 'NONE',  ( 4.798395639560619763, 1.317935440718048135, -1.390428439694970431 ) ) ;
#27439=CARTESIAN_POINT ( 'NONE',  ( 6.827182134110222123, -0.006956174471953178659, 2.188967759425272330 ) ) ;
#27443=CARTESIAN_POINT ( 'NONE',  ( 1.903414394802248166, 1.797162532295241366, 1.201017911493490020 ) ) ;
#27447=CARTESIAN_POINT ( 'NONE',  ( 4.998959831394860664, 1.517082468864182632, -1.015166198912627049 ) ) ;
#27449=CARTESIAN_POINT ( 'NONE',  ( 0.7199194774221047144, -1.050951492028269874, -1.667678589039832904 ) ) ;
#27450=CARTESIAN_POINT ( 'NONE',  ( 3.199369407753744454, 1.726971514772487559, -0.8218122705464236954 ) ) ;
#27453=CARTESIAN_POINT ( 'NONE',  ( 3.789471415310685654, -1.820739144500636231, 0.7515243927636706678 ) ) ;
#27455=CARTESIAN_POINT ( 'NONE',  ( 6.110880135979408045, -0.2334805506369178330, 1.927903797987507106 ) ) ;
#27459=CARTESIAN_POINT ( 'NONE',  ( 6.310795917644286490, -0.5669512758468171487, -2.043305014803979525 ) ) ;
#27461=CARTESIAN_POINT ( 'NONE',  ( 3.826736342760712173, 1.350229473097919630, -1.354399478966497261 ) ) ;
#27467=CARTESIAN_POINT ( 'NONE',  ( 5.303390062791992321, 1.774253655011595709, -0.9511161165304935494 ) ) ;
#27469=CARTESIAN_POINT ( 'NONE',  ( 6.270122753791413928, 0.9430518052575274091, 1.563124558401955300 ) ) ;
#27470=CARTESIAN_POINT ( 'NONE',  ( 2.207561477879273593, -1.661462528888792090, -1.235070534849058044 ) ) ;
#27475=CARTESIAN_POINT ( 'NONE',  ( 6.508674657442179878, 1.384610780642284711, -1.258058027910214927 ) ) ;
#27482=SURFACE_STYLE_USAGE ( .BOTH. , #175891 ) ;
#27485=CARTESIAN_POINT ( 'NONE',  ( 4.236742506082516790, 1.733672338021419179, -0.04812345329192367627 ) ) ;
#27487=CARTESIAN_POINT ( 'NONE',  ( 0.8310238944931707117, -1.948087850137161459, -0.7009411469260096172 ) ) ;
#27488=CARTESIAN_POINT ( 'NONE',  ( 3.321969493568678988, 0.9498371968033242352, -1.892263307760349900 ) ) ;
#27491=CARTESIAN_POINT ( 'NONE',  ( 6.930528400284448054, -1.278709912597691511, 1.628784411136071197 ) ) ;
#27495=CARTESIAN_POINT ( 'NONE',  ( 0.05278957052760185897, 0.3289079202175131389, 1.883742972368242174 ) ) ;
#27496=CARTESIAN_POINT ( 'NONE',  ( 3.345926335499046722, 2.292435215394402093, 0.0001471259066659902901 ) ) ;
#27497=CARTESIAN_POINT ( 'NONE',  ( 0.9788029507734037349, -0.04229004422508231970, -1.825371421953936757 ) ) ;
#27498=CARTESIAN_POINT ( 'NONE',  ( 3.744317949583543470, 1.018843395500759197, -1.618198357137661469 ) ) ;
#27502=CARTESIAN_POINT ( 'NONE',  ( 2.250246052928657203, 0.9454230575737303521, -1.777374461261713279 ) ) ;
#27503=CARTESIAN_POINT ( 'NONE',  ( 2.324987154519737143, -1.791562868964852395, -0.7996954790665599111 ) ) ;
#27507=CARTESIAN_POINT ( 'NONE',  ( 4.734370563723459213, 0.3569306294452011530, 2.059774728693287038 ) ) ;
#27508=CARTESIAN_POINT ( 'NONE',  ( 3.027930095613054817, 0.9845384034416431174, -1.470494568931050905 ) ) ;
#27510=CARTESIAN_POINT ( 'NONE',  ( 6.281209671116547710, 1.576043917979405684, 1.664718807710400705 ) ) ;
#27511=CARTESIAN_POINT ( 'NONE',  ( 5.085792842222247145, -1.727793525551263087, -0.2079256833047369302 ) ) ;
#27515=CARTESIAN_POINT ( 'NONE',  ( 6.063786081214013635, 1.415308013037285484, -1.001223213843880799 ) ) ;
#27516=CARTESIAN_POINT ( 'NONE',  ( 6.403528931544730796, -1.954801056786956259, 0.4946215565981848528 ) ) ;
#27517=CARTESIAN_POINT ( 'NONE',  ( 5.652828992512394457, -0.5219723807755486389, -2.107401415877676598 ) ) ;
#27519=CARTESIAN_POINT ( 'NONE',  ( 0.3392563814038212500, -1.792290195912203954, -1.127034558586788249 ) ) ;
#27520=CARTESIAN_POINT ( 'NONE',  ( 5.156250000000004441, -1.895863743163967108, 0.7852924748302536617 ) ) ;
#27522=CARTESIAN_POINT ( 'NONE',  ( 3.469672154888691296, 1.879743449303279634, -0.4207095485242727806 ) ) ;
#27524=CARTESIAN_POINT ( 'NONE',  ( -0.1102773484824119410, -0.006951161900758255283, -2.203378182130751206 ) ) ;
#27530=CARTESIAN_POINT ( 'NONE',  ( 2.719623178692368359, 1.877883874979644263, 1.186199984364836313 ) ) ;
#27532=CARTESIAN_POINT ( 'NONE',  ( -0.02900071798685525254, 1.326456003635017922, -2.425894103910302135 ) ) ;
#27537=CARTESIAN_POINT ( 'NONE',  ( 0.5455463417442986129, -1.458554840210561476, 1.392547631435703037 ) ) ;
#27539=CARTESIAN_POINT ( 'NONE',  ( 5.934046607644717142, 1.225649100846971651, 1.658920436798372311 ) ) ;
#27544=CARTESIAN_POINT ( 'NONE',  ( 6.907498162232361238, -0.4094499450241483318, 1.831839262316947270 ) ) ;
#27545=CARTESIAN_POINT ( 'NONE',  ( 5.818968308277153056, 0.8464176696867716787, -1.513466976307031642 ) ) ;
#27546=CARTESIAN_POINT ( 'NONE',  ( 5.442807971621070884, -1.376865196755885146, -1.064510927867247769 ) ) ;
#27547=CARTESIAN_POINT ( 'NONE',  ( 2.648291651658631007, 0.7751803744074429181, 2.157441745960963164 ) ) ;
#27549=CARTESIAN_POINT ( 'NONE',  ( 1.728195974063054141, 0.1793598003074353686, 1.832383557197496460 ) ) ;
#27552=CARTESIAN_POINT ( 'NONE',  ( 2.502731746374619259, 1.467688513602287470, -1.085450786651315225 ) ) ;
#27553=CARTESIAN_POINT ( 'NONE',  ( 3.656875104409584853, 1.122498086849915921, 1.674887873639265390 ) ) ;
#27556=CARTESIAN_POINT ( 'NONE',  ( 4.928798221971478988, 2.014404525830254311, 0.6141583887315901213 ) ) ;
#27559=CARTESIAN_POINT ( 'NONE',  ( 3.016144355299533952, 2.060630728401948275, -0.2003171163396169074 ) ) ;
#27562=CARTESIAN_POINT ( 'NONE',  ( 4.934296419935966682, -1.134874685878878520, -1.791058398909770588 ) ) ;
#27563=CARTESIAN_POINT ( 'NONE',  ( 0.7328819429333592872, 0.1407736501095498138, 1.921419779381093207 ) ) ;
#27570=CARTESIAN_POINT ( 'NONE',  ( 5.713165544288242970, 1.732532623411761286, -1.222520872474173848 ) ) ;
#27571=CARTESIAN_POINT ( 'NONE',  ( 1.430846025165666280, 2.029450977514839938, 0.5621798225463514598 ) ) ;
#27574=CARTESIAN_POINT ( 'NONE',  ( 6.649252725998297642, 1.619456339520190413, -0.9165514639192672286 ) ) ;
#27580=CARTESIAN_POINT ( 'NONE',  ( -0.1577409392781377873, -1.310076727147227560, -1.668215054097483385 ) ) ;
#27583=CARTESIAN_POINT ( 'NONE',  ( 2.400770673373255448, 0.4268909467371252431, 1.914702609522442867 ) ) ;
#27584=CARTESIAN_POINT ( 'NONE',  ( 1.534274790466340299, 1.065227450066742687, -1.880959520452238465 ) ) ;
#27588=CARTESIAN_POINT ( 'NONE',  ( 2.952174690553764691, 1.223825555390768871, 1.228469256970601498 ) ) ;
#27589=CARTESIAN_POINT ( 'NONE',  ( 2.114833760799132989, -1.688328753782810221, 0.4216566245275765179 ) ) ;
#27592=CARTESIAN_POINT ( 'NONE',  ( 1.774767310740913207, -2.001205085354029301, 0.2439901982170673833 ) ) ;
#27593=CARTESIAN_POINT ( 'NONE',  ( 6.825078400183511640, 3.690008145721306310, 2.558400262806997283 ) ) ;
#27595=CARTESIAN_POINT ( 'NONE',  ( 1.551575459862795325, 0.5740822587161975576, -1.886020533208163430 ) ) ;
#27596=CARTESIAN_POINT ( 'NONE',  ( 5.379139070037473935, -1.731557697741787916, -0.8120211572784155063 ) ) ;
#27601=CARTESIAN_POINT ( 'NONE',  ( 1.190109814708179670, 1.204940744830071075, 1.620691797242173937 ) ) ;
#27603=CARTESIAN_POINT ( 'NONE',  ( 5.772612788190349953, -1.469667252935745960, 1.779063562929294129 ) ) ;
#27604=CARTESIAN_POINT ( 'NONE',  ( 6.232861002365865488, -1.862453515449840724, -0.6167318247369477646 ) ) ;
#27606=CARTESIAN_POINT ( 'NONE',  ( 3.133595828963112950, 1.864314371477162169, -0.6108997337519045390 ) ) ;
#27608=CARTESIAN_POINT ( 'NONE',  ( 0.4752326960846975923, -2.001511663014220677, -0.2440270837566413387 ) ) ;
#27610=CARTESIAN_POINT ( 'NONE',  ( 1.763061546204633290, -0.1096309319212440264, -2.114649557665876145 ) ) ;
#27613=CARTESIAN_POINT ( 'NONE',  ( 1.991909005812149358, -0.4902695928585449892, -1.774584731258487036 ) ) ;
#27616=CARTESIAN_POINT ( 'NONE',  ( 2.971057270251746818, -1.603071526910588629, 1.388259434452358665 ) ) ;
#27620=CARTESIAN_POINT ( 'NONE',  ( 3.268875894143012939, -1.902732241629549348, -0.7919657925325486181 ) ) ;
#27623=CARTESIAN_POINT ( 'NONE',  ( 0.5734669319550633748, -1.023298125840161887, 1.530493987491374330 ) ) ;
#27625=CARTESIAN_POINT ( 'NONE',  ( -0.02244404828157658613, -0.004869073801674199918, -2.189079685368473527 ) ) ;
#27627=CARTESIAN_POINT ( 'NONE',  ( 0.4873205249028254027, -0.2742316277877173691, -2.189713876267186166 ) ) ;
#27628=CARTESIAN_POINT ( 'NONE',  ( 3.128476345081227628, 1.259638568860393493, -1.879123747193896632 ) ) ;
#27630=CARTESIAN_POINT ( 'NONE',  ( 2.179683618226692321, 1.775955819808447966, -0.3565394459093262358 ) ) ;
#27631=CARTESIAN_POINT ( 'NONE',  ( 3.415159944131008096, -1.768026670962073110, 0.7381028802780668086 ) ) ;
#27632=CARTESIAN_POINT ( 'NONE',  ( 3.789561645344252661, -1.914057400617325433, 0.7896510022299551013 ) ) ;
#27634=CARTESIAN_POINT ( 'NONE',  ( 2.887526864075397715, 1.393042391738574137, 1.395278474455765805 ) ) ;
#27635=CARTESIAN_POINT ( 'NONE',  ( 0.09454951164026764721, -0.4206464163897213893, -1.887090839307656864 ) ) ;
#27636=CARTESIAN_POINT ( 'NONE',  ( 2.465516990510143280, 1.834972510290140191, -0.3627323784974947340 ) ) ;
#27638=CARTESIAN_POINT ( 'NONE',  ( 2.737322364211117520, 0.2836107604972230578, 2.290143083710040717 ) ) ;
#27640=CARTESIAN_POINT ( 'NONE',  ( 2.488518357381704238, 1.804271297518467820, 0.4556280478851971183 ) ) ;
#27642=CARTESIAN_POINT ( 'NONE',  ( 6.373490837812130216, -0.2564121905142978664, 2.046633738985944806 ) ) ;
#27647=CARTESIAN_POINT ( 'NONE',  ( 0.2586047683651994666, 0.8082109201883975746, 1.945024607815620366 ) ) ;
#27649=CARTESIAN_POINT ( 'NONE',  ( 6.503215372615936296, 1.793156143535659330, 1.206815395834538451 ) ) ;
#27651=CARTESIAN_POINT ( 'NONE',  ( -0.01731643392406666954, -1.316173432332496507, 1.532187831819804780 ) ) ;
#27657=CARTESIAN_POINT ( 'NONE',  ( 6.925078400183531713, 7.629137130509067610, 2.355651831298340326 ) ) ;
#27660=CARTESIAN_POINT ( 'NONE',  ( 4.311732611912100666, -1.244383703160652610, -1.586670621409623116 ) ) ;
#27665=CARTESIAN_POINT ( 'NONE',  ( 5.840740251263128791, 0.4172088472891195554, 2.120894824392767664 ) ) ;
#27670=CARTESIAN_POINT ( 'NONE',  ( -0.1411974294642202310, -0.0004739540254597266757, -1.900147702309512132 ) ) ;
#27674=CARTESIAN_POINT ( 'NONE',  ( 1.400563108759992792, 1.411875272319111696, -0.9905557981151734692 ) ) ;
#27678=CARTESIAN_POINT ( 'NONE',  ( 0.4909911900966601461, 1.305473228555413812, 1.195063304280475025 ) ) ;
#27679=CARTESIAN_POINT ( 'NONE',  ( 2.156891369321057628, 0.4431265858878992159, 1.963560470019373172 ) ) ;
#27681=CARTESIAN_POINT ( 'NONE',  ( 4.735508036034060453, -2.019198892066270457, 0.8907332283012432406 ) ) ;
#27682=CARTESIAN_POINT ( 'NONE',  ( 5.331008558256671748, -2.041869270619638854, -0.7380826535893101337 ) ) ;
#27686=CARTESIAN_POINT ( 'NONE',  ( 3.246849895443252532, 2.069243461727567013, 0.4626693848822636124 ) ) ;
#27687=CARTESIAN_POINT ( 'NONE',  ( 2.513296185832504470, -1.880429104915388727, 0.7283969491318904588 ) ) ;
#27688=CARTESIAN_POINT ( 'NONE',  ( 3.638735373827857167, 1.721918111813141916, 0.5631709482423822299 ) ) ;
#27691=ORIENTED_EDGE ( 'NONE', *, *, #73601, .T. ) ;
#27696=CARTESIAN_POINT ( 'NONE',  ( 6.551389018236878137, -1.469694460105780642, -1.082916835497591324 ) ) ;
#27698=CARTESIAN_POINT ( 'NONE',  ( 1.692462117551472911, 1.416773270106906235, -1.289619884002331407 ) ) ;
#27705=CARTESIAN_POINT ( 'NONE',  ( 5.348557406608104969, 0.6236849695623291057, 2.069784783864880851 ) ) ;
#27708=CARTESIAN_POINT ( 'NONE',  ( 2.935903058640790597, -2.042584291827519660, 0.5695675404085094318 ) ) ;
#27709=CARTESIAN_POINT ( 'NONE',  ( -0.1298852118744257267, 5.725805934370246320, -2.320586200942467148 ) ) ;
#27711=CARTESIAN_POINT ( 'NONE',  ( 4.094965523422711584, 1.667053662060855812, -1.051937181705852931 ) ) ;
#27712=CARTESIAN_POINT ( 'NONE',  ( -0.01731850797281712928, -1.311767784893268285, 1.527291784361783922 ) ) ;
#27714=CARTESIAN_POINT ( 'NONE',  ( 5.225823379661913570, 0.8554599082026111967, -1.936989086107894664 ) ) ;
#27716=CARTESIAN_POINT ( 'NONE',  ( 0.1392002015415672034, -0.1474423581745692435, -2.037351525059682977 ) ) ;
#27717=CARTESIAN_POINT ( 'NONE',  ( 2.818227900350485982, 1.828750386608999356, 0.6536940613037258707 ) ) ;
#27721=CARTESIAN_POINT ( 'NONE',  ( 4.013684974745008738, -1.074646439955847965, -1.793145193944564175 ) ) ;
#27724=CARTESIAN_POINT ( 'NONE',  ( 0.1877650794145177826, 1.041282258498995361, 1.482055844031314518 ) ) ;
#27726=CARTESIAN_POINT ( 'NONE',  ( 5.145248760827346501, -1.894204247122273088, 1.132176536499051700 ) ) ;
#27728=CARTESIAN_POINT ( 'NONE',  ( 2.591098708763440062, -0.3764507303484417311, -2.174265822884546395 ) ) ;
#27731=CARTESIAN_POINT ( 'NONE',  ( 1.330556988563241561, 1.283596529665396169, -1.417643162000304935 ) ) ;
#27734=CARTESIAN_POINT ( 'NONE',  ( 5.125469573878929097, 0.2063957376101481500, -2.060066405364005426 ) ) ;
#27736=CARTESIAN_POINT ( 'NONE',  ( 2.905317003618158367, 1.825515667692039878, 1.157497049167732550 ) ) ;
#27737=CARTESIAN_POINT ( 'NONE',  ( 4.599289333468261631, -0.5842463895667610041, 2.112197083089427885 ) ) ;
#27745=CARTESIAN_POINT ( 'NONE',  ( 0.3521856818783953846, 0.1948384997633167970, -2.006960225185448810 ) ) ;
#27748=CARTESIAN_POINT ( 'NONE',  ( 5.735237735067806319, -0.04509738862551111033, -2.069921269439451539 ) ) ;
#27749=CARTESIAN_POINT ( 'NONE',  ( 4.266181944680371707, 0.9094715277466745018, 1.698315803094905041 ) ) ;
#27750=CARTESIAN_POINT ( 'NONE',  ( 6.591443028821331040, -0.4675721919094841250, 2.072835713318227135 ) ) ;
#27754=CARTESIAN_POINT ( 'NONE',  ( 5.067230186376567858, 1.711625542863755012, 0.9741009975822639833 ) ) ;
#27755=CARTESIAN_POINT ( 'NONE',  ( 0.7619990552875830492, 1.083242598816274382, 1.904929396514772444 ) ) ;
#27756=CARTESIAN_POINT ( 'NONE',  ( 3.914527900857078357, 1.289819402409349669, -1.292354223553587644 ) ) ;
#27762=CARTESIAN_POINT ( 'NONE',  ( 2.454439063956286304, -1.602943312447857593, -0.9057913635923324769 ) ) ;
#27763=CARTESIAN_POINT ( 'NONE',  ( 4.974862723197266412, -1.455255168294814272, 1.391337642457886270 ) ) ;
#27764=CARTESIAN_POINT ( 'NONE',  ( 1.230279809073684172, -2.078304686880276808, -0.9817359432500573080 ) ) ;
#27765=CARTESIAN_POINT ( 'NONE',  ( 5.559412779221331924, 1.601624451964112739, 1.132529127964493121 ) ) ;
#27767=CARTESIAN_POINT ( 'NONE',  ( 0.2333690889706925564, 0.2409277441041447754, -2.087868073146467829 ) ) ;
#27769=CARTESIAN_POINT ( 'NONE',  ( 0.1333692844072559280, 0.001398348041498076455, -2.053671342968105051 ) ) ;
#27771=CARTESIAN_POINT ( 'NONE',  ( 0.9957797365991372107, -2.090933974770115444, 0.003689723154384760839 ) ) ;
#27772=CARTESIAN_POINT ( 'NONE',  ( 6.819227944281511355, -0.1297537616256147774, 1.740395163524804945 ) ) ;
#27775=CARTESIAN_POINT ( 'NONE',  ( 1.944474315927123387, -1.398120440366573680, -1.036317219087657504 ) ) ;
#27777=DIRECTION ( 'NONE',  ( 1.040834085586084257E-15, 1.000000000000000000, -4.622230424712076367E-32 ) ) ;
#27779=CARTESIAN_POINT ( 'NONE',  ( 3.123388959964632949, -1.662097631915793183, 0.4608284732507839654 ) ) ;
#27780=CARTESIAN_POINT ( 'NONE',  ( 3.210657068901449307, 1.982179491636561819, 0.9350799695589939731 ) ) ;
#27781=CARTESIAN_POINT ( 'NONE',  ( 4.477303810882872881, 0.001702072213635372200, -2.207063162522747479 ) ) ;
#27783=B_SPLINE_CURVE_WITH_KNOTS ( 'NONE', 3,
 ( #46806, #84606, #130244, #14251, #165862, #133396, #17448, #150695, #83531, #1196 ),
 .UNSPECIFIED., .F., .F.,
 ( 4, 1, 1, 1, 1, 1, 1, 4 ),
 ( 0.000000000000000000, 0.09705918685507786137, 0.1907419858981972138, 0.2602182418918835838, 0.3625179829595637226, 0.5215049497019805802, 0.7338397267804015467, 1.000000000000000000 ),
 .UNSPECIFIED. ) ;
#27784=CARTESIAN_POINT ( 'NONE',  ( 2.588947950494639993, 2.104950400290429791, 0.5311738530254602741 ) ) ;
#27785=CARTESIAN_POINT ( 'NONE',  ( 0.6096330727367264002, -1.817201089070449971, 0.1759225495863714350 ) ) ;
#27786=CARTESIAN_POINT ( 'NONE',  ( 3.661412522060889074, 1.992289893316813609, -0.7171584230975246443 ) ) ;
#27787=CARTESIAN_POINT ( 'NONE',  ( 6.639320575229256782, 2.986994467643698137, 2.250762793112503157 ) ) ;
#27789=CARTESIAN_POINT ( 'NONE',  ( 4.212625126225740146, 2.095743129530680537, 0.9292526312315220194 ) ) ;
#27794=CARTESIAN_POINT ( 'NONE',  ( 5.672587799981195111, 0.8983335965149964464, 2.031727793752806210 ) ) ;
#27798=CARTESIAN_POINT ( 'NONE',  ( 6.825078400183548055, 3.702925343214446663, 2.370119418288775925 ) ) ;
#27800=CARTESIAN_POINT ( 'NONE',  ( 4.465470312728934132, -1.956561007648183192, -0.4872041746135646889 ) ) ;
#27802=CARTESIAN_POINT ( 'NONE',  ( 2.623947407551871169, 2.023649216642096960, -0.3979924315659318923 ) ) ;
#27807=CARTESIAN_POINT ( 'NONE',  ( 5.560537033210596114, -1.979929515673630513, -0.9395970221138388867 ) ) ;
#27808=CARTESIAN_POINT ( 'NONE',  ( 2.777970385693105726, 1.728001979019553325, -1.038993764437286416 ) ) ;
#27809=CARTESIAN_POINT ( 'NONE',  ( 1.768857366986800184, 1.761637791510446860, -0.5354853023365884201 ) ) ;
#27812=CARTESIAN_POINT ( 'NONE',  ( 6.475623784153278883, 1.746001614453606576, -0.5331787911772439825 ) ) ;
#27813=CARTESIAN_POINT ( 'NONE',  ( -0.05159450770049476415, -2.057278634402651907, -1.025749021234131364 ) ) ;
#27815=CARTESIAN_POINT ( 'NONE',  ( 6.016560025881092066, 1.524636124814653382, -1.671835012792993735 ) ) ;
#27817=CARTESIAN_POINT ( 'NONE',  ( 2.420660912963272349, 1.375124471020009231, -1.595256772795665023 ) ) ;
#27826=CARTESIAN_POINT ( 'NONE',  ( 1.969135536805465492, -1.636093909763213228, 1.349083368969570262 ) ) ;
#27827=CARTESIAN_POINT ( 'NONE',  ( 3.059039825962418746, 0.5433887813283566626, 2.153793114424791710 ) ) ;
#27832=CARTESIAN_POINT ( 'NONE',  ( 4.369553226407375313, -0.3375162941181614751, 1.932460123137308861 ) ) ;
#27840=CARTESIAN_POINT ( 'NONE',  ( 3.129257641292593650, 1.918792544363761454, 0.9031103230835100248 ) ) ;
#27842=CARTESIAN_POINT ( 'NONE',  ( 3.959979445722985325, 2.145676688911036578, -0.2621329562078680842 ) ) ;
#27843=CARTESIAN_POINT ( 'NONE',  ( 3.509164994824386596, -1.813400730843343966, 0.3181347684400454012 ) ) ;
#27846=CARTESIAN_POINT ( 'NONE',  ( 5.577983363897286218, -1.699187140184825751, -0.3753857801653339710 ) ) ;
#27851=CARTESIAN_POINT ( 'NONE',  ( 3.415052781332720055, 1.953485055394106107, 0.9259690932504063277 ) ) ;
#27852=CARTESIAN_POINT ( 'NONE',  ( 5.448592227559037049, 1.351948914259465173, 1.495821383734573073 ) ) ;
#27854=CARTESIAN_POINT ( 'NONE',  ( 2.272554088390315030, -1.330374092946192688, 1.703740541667747133 ) ) ;
#27855=CARTESIAN_POINT ( 'NONE',  ( 3.866447834861338695, -1.326295688514609550, 1.458626262776492544 ) ) ;
#27856=CARTESIAN_POINT ( 'NONE',  ( -0.1114211809780316365, -0.4883405756051837354, -2.144353428667714390 ) ) ;
#27857=CARTESIAN_POINT ( 'NONE',  ( 4.212401414637350072, 1.776917926058638963, 0.7840673734914437309 ) ) ;
#27866=CARTESIAN_POINT ( 'NONE',  ( 1.782535857997105566, -1.180187651135233384, 1.864495428577646274 ) ) ;
#27869=CARTESIAN_POINT ( 'NONE',  ( 6.702011072381410806, 0.7537920952922130269, -1.811353739714548272 ) ) ;
#27875=CARTESIAN_POINT ( 'NONE',  ( 5.753808258465379133, 0.7501079416377672837, 1.681592913607635964 ) ) ;
#27880=CARTESIAN_POINT ( 'NONE',  ( 6.240501835383900797, 1.219778281852833546, -1.734492557903525523 ) ) ;
#27883=CARTESIAN_POINT ( 'NONE',  ( 0.1454761644432709389, -1.592655978506152703, -1.307672486379028332 ) ) ;
#27885=CARTESIAN_POINT ( 'NONE',  ( 2.224856516622634395, -1.700045390792026989, -0.7576570785256631080 ) ) ;
#27886=CARTESIAN_POINT ( 'NONE',  ( 4.089279031174639201, -0.7008038172400687937, 1.702867937621636463 ) ) ;
#27894=CARTESIAN_POINT ( 'NONE',  ( 4.723365791888975096, -0.1103408873950258995, 2.204240794804641190 ) ) ;
#27895=CARTESIAN_POINT ( 'NONE',  ( 6.555986116969920730, 2.257040928323080564, -0.1566935481548906162 ) ) ;
#27897=CARTESIAN_POINT ( 'NONE',  ( 5.502179438505619302, -0.8068474266363240277, 1.622048611428918319 ) ) ;
#27898=CARTESIAN_POINT ( 'NONE',  ( 6.421099303836709460, -1.707838190419972424, 0.8681067396549295712 ) ) ;
#27900=CARTESIAN_POINT ( 'NONE',  ( 5.629731426258720361, -1.187751674602673058, -1.445209747047627946 ) ) ;
#27901=CARTESIAN_POINT ( 'NONE',  ( 5.162724115531082347, 0.5589384127702141658, 1.828758346017298697 ) ) ;
#27903=CARTESIAN_POINT ( 'NONE',  ( 0.8834254411415434216, 1.253375741028007084, 1.388844808110502038 ) ) ;
#27904=CARTESIAN_POINT ( 'NONE',  ( 0.7785302072789467287, -0.4946362931835950327, -1.954778448132548752 ) ) ;
#27906=CARTESIAN_POINT ( 'NONE',  ( 4.072956574305106159, -1.964985935830084740, -0.7583447493727160094 ) ) ;
#27911=CARTESIAN_POINT ( 'NONE',  ( 3.006122514718052585, -0.8146449015280079475, 1.848388696978587875 ) ) ;
#27915=CARTESIAN_POINT ( 'NONE',  ( 4.692742333269261934, -0.4685372120167423660, -2.110058259655919422 ) ) ;
#27920=( BOUNDED_CURVE ( )  B_SPLINE_CURVE ( 3, ( #197847, #149104, #49479, #115599 ),
 .UNSPECIFIED., .F., .T. ) 
 B_SPLINE_CURVE_WITH_KNOTS ( ( 4, 4 ),
 ( 0.4999999999999984457, 1.000000000000000000 ),
 .UNSPECIFIED. ) 
 CURVE ( )  GEOMETRIC_REPRESENTATION_ITEM ( )  RATIONAL_B_SPLINE_CURVE ( ( 1.000000000000001998, 0.3333333333333333703, 0.3333333333333313164, 1.000000000000000000 ) ) 
 REPRESENTATION_ITEM ( '' )  );
#27922=CARTESIAN_POINT ( 'NONE',  ( 1.188188303608740615, -1.377055334905618933, -1.678633986682298573 ) ) ;
#27927=CARTESIAN_POINT ( 'NONE',  ( 1.734175692058033347, 2.168326105380265378, 0.3173973903456903112 ) ) ;
#27928=CARTESIAN_POINT ( 'NONE',  ( 6.883263157960366030, 0.5727201817382967519, 2.105997115537924902 ) ) ;
#27929=CARTESIAN_POINT ( 'NONE',  ( 2.764839853141934256, -1.560785778453818828, 1.638175023747280523 ) ) ;
#27931=CARTESIAN_POINT ( 'NONE',  ( 4.680875185974167074, 1.673856063443099895, -1.124242729735332347 ) ) ;
#27936=CARTESIAN_POINT ( 'NONE',  ( 4.323360031453548302, -1.693909316728856806, 0.5125324126216290743 ) ) ;
#27938=CARTESIAN_POINT ( 'NONE',  ( 0.3761801408644695477, 1.212865950663596371, 1.721436218156185305 ) ) ;
#27942=CARTESIAN_POINT ( 'NONE',  ( 5.888296041240274725, -0.7283935311428509918, -1.880430420734761965 ) ) ;
#27945=CARTESIAN_POINT ( 'NONE',  ( 3.924554409752772699, 1.776107677202539925, 0.5873546117282566481 ) ) ;
#27946=CARTESIAN_POINT ( 'NONE',  ( 4.838769763947080804, -2.006773940031422399, -0.5081810985937407210 ) ) ;
#27956=CARTESIAN_POINT ( 'NONE',  ( 3.596105239937871456, 0.8843387906064968940, -1.751336483779348585 ) ) ;
#27957=CARTESIAN_POINT ( 'NONE',  ( 0.9485920322965734064, 1.351945250224910744, 1.495824703658617638 ) ) ;
#27960=CARTESIAN_POINT ( 'NONE',  ( 6.639320575229280763, 7.629137130509070275, 2.496737603865983424 ) ) ;
#27961=CARTESIAN_POINT ( 'NONE',  ( 1.352582913587907942, -1.478046865151939615, 1.146363905606573086 ) ) ;
#27963=CARTESIAN_POINT ( 'NONE',  ( 2.935794159824364868, -1.939102465223912830, 0.5408614042671439082 ) ) ;
#27965=CARTESIAN_POINT ( 'NONE',  ( 2.337658655405081110, 0.5614262474852428353, -2.041391482465891194 ) ) ;
#27967=CARTESIAN_POINT ( 'NONE',  ( 4.334477209444560053, -1.194628513295314942, 1.690740121169509447 ) ) ;
#27969=CARTESIAN_POINT ( 'NONE',  ( 0.4508687890585044711, -1.768401812538191287, -1.115020903081758608 ) ) ;
#27971=CARTESIAN_POINT ( 'NONE',  ( 4.788025880137685597, -0.8597811773201522456, 1.610451283527076116 ) ) ;
#27977=CARTESIAN_POINT ( 'NONE',  ( 6.001041448284401447, 1.807427358944500684, -1.265864663738118345 ) ) ;
#27979=CARTESIAN_POINT ( 'NONE',  ( 5.496708366351358066, -1.866603419165157041, -0.4147590543357379533 ) ) ;
#27988=CARTESIAN_POINT ( 'NONE',  ( 0.07680821025393690105, 0.005952109439256307241, -1.810863387344714193 ) ) ;
#27994=CARTESIAN_POINT ( 'NONE',  ( 2.852355409199380798, -1.963852837454314271, -0.1495663577412101042 ) ) ;
#27995=CARTESIAN_POINT ( 'NONE',  ( 3.128529964930275131, 0.4926631579876327716, 1.955168413974050834 ) ) ;
#27998=CARTESIAN_POINT ( 'NONE',  ( 6.827182134110199030, -0.004087946457608306570, 2.088967824442849341 ) ) ;
#27999=CARTESIAN_POINT ( 'NONE',  ( 3.170069416559752273, -1.305109287949431929, 1.760291797049506446 ) ) ;
#28001=CARTESIAN_POINT ( 'NONE',  ( 2.080962409574789174, -0.09239518442967499523, -1.924287757472051164 ) ) ;
#28004=CARTESIAN_POINT ( 'NONE',  ( 0.2329586101569527945, 4.095490909754247788, -2.400670182941808672 ) ) ;
#28010=CARTESIAN_POINT ( 'NONE',  ( 6.286648950733226826, 1.598451336667701339, -0.9137711784916457969 ) ) ;
#28011=CARTESIAN_POINT ( 'NONE',  ( 1.682290626080079621, 1.036857497476886936, 1.725414394560653042 ) ) ;
#28012=CARTESIAN_POINT ( 'NONE',  ( 4.429307823785958220, 1.078883539000154324, 2.029420160895245129 ) ) ;
#28013=CARTESIAN_POINT ( 'NONE',  ( -0.02919842301641034990, 1.352617229779122132, -2.329362550481127947 ) ) ;
#28014=CARTESIAN_POINT ( 'NONE',  ( 2.518200207203071805, 0.7905618127436510045, 1.684796146788158699 ) ) ;
#28017=CARTESIAN_POINT ( 'NONE',  ( 5.203337695038355193, 1.683698669361912259, -0.9069238330124268499 ) ) ;
#28021=CARTESIAN_POINT ( 'NONE',  ( 4.810148555269133652, 1.440736570533694527, -1.515338330687252988 ) ) ;
#28022=CARTESIAN_POINT ( 'NONE',  ( 3.608139902456270143, -0.7572706533398064765, -1.710698989992056607 ) ) ;
#28027=CARTESIAN_POINT ( 'NONE',  ( 5.654863297658344834, -1.355735166614827625, 1.066293663406183256 ) ) ;
#28029=CARTESIAN_POINT ( 'NONE',  ( 1.898628203569406203, -0.8177110325628260679, -1.529257715385720307 ) ) ;
#28032=CARTESIAN_POINT ( 'NONE',  ( 6.280482454654814362, -0.5424645211669875122, -1.942098458069536848 ) ) ;
#28035=CARTESIAN_POINT ( 'NONE',  ( 6.245025782124020708, -0.3104734683975469145, -2.148636169971326559 ) ) ;
#28036=CARTESIAN_POINT ( 'NONE',  ( 4.037589748876240670, -1.260430739550026269, -1.321009972365666307 ) ) ;
#28037=CARTESIAN_POINT ( 'NONE',  ( 2.342563710341159400, -1.922903400459201828, -0.3876519335672747313 ) ) ;
#28038=CARTESIAN_POINT ( 'NONE',  ( -0.08807185805374209697, -1.306980724784766013, -1.666505321573110265 ) ) ;
#28044=CARTESIAN_POINT ( 'NONE',  ( 2.315225504062240702, 1.701464259299827919, -1.265282535349021575 ) ) ;
#28048=CARTESIAN_POINT ( 'NONE',  ( 6.948074912775242140, -0.9353680688231647000, 1.957065181168372581 ) ) ;
#28051=CARTESIAN_POINT ( 'NONE',  ( 3.616091037371416572, -0.6436381315554053906, 2.126022720447027670 ) ) ;
#28053=CARTESIAN_POINT ( 'NONE',  ( 1.038157343047078296, -1.808118644657311203, 1.419311033984706816 ) ) ;
#28055=CARTESIAN_POINT ( 'NONE',  ( 5.664908073332702187, 1.565568307794177327, -1.342975779555633187 ) ) ;
#28058=CARTESIAN_POINT ( 'NONE',  ( 0.2329586101569527945, 4.095490909754247788, -2.400670182941808672 ) ) ;
#28059=CARTESIAN_POINT ( 'NONE',  ( 5.214338956685347526, 1.703448749313410282, 0.6994016148276983591 ) ) ;
#28062=CARTESIAN_POINT ( 'NONE',  ( 2.414726000362901637, 1.539333419754819854, 0.7781589270328890251 ) ) ;
#28063=CARTESIAN_POINT ( 'NONE',  ( 1.147673126774436225, 1.985868168208399842, -0.3494872464938902357 ) ) ;
#28064=CARTESIAN_POINT ( 'NONE',  ( 2.901363961662834168, -1.135721475377445167, -1.998492394250019233 ) ) ;
#28065=CARTESIAN_POINT ( 'NONE',  ( 2.091474534086060544, 1.969063197997424686, -1.113951356575371365 ) ) ;
#28066=CARTESIAN_POINT ( 'NONE',  ( 4.986996339425863844, -0.2567466434181593371, -2.090293495131962942 ) ) ;
#28068=CARTESIAN_POINT ( 'NONE',  ( 3.637761035129345455, 0.7980134727624802471, -1.579695959945091044 ) ) ;
#28070=CARTESIAN_POINT ( 'NONE',  ( 0.04153208042980033321, -1.776208762584199574, -1.448543121555950774 ) ) ;
#28071=CARTESIAN_POINT ( 'NONE',  ( 4.347483306186128438, 1.840691044367316120, -0.04759384897683878457 ) ) ;
#28076=CARTESIAN_POINT ( 'NONE',  ( 4.839868765920234850, 2.185429510258177110, 0.1630863781024796955 ) ) ;
#28080=CARTESIAN_POINT ( 'NONE',  ( 3.000521647167487593, -0.5595019940488660248, -1.843462078654713343 ) ) ;
#28083=CARTESIAN_POINT ( 'NONE',  ( 0.08853117554794007193, 1.285972019905703201, 1.811169930398129013 ) ) ;
#28092=CARTESIAN_POINT ( 'NONE',  ( 1.328483007144948935, -1.247240240105648379, 1.514344512384787622 ) ) ;
#28094=CARTESIAN_POINT ( 'NONE',  ( 6.819229411136438657, -0.1619093195798972928, 2.126376854085454404 ) ) ;
#28095=CARTESIAN_POINT ( 'NONE',  ( 6.039501783790233169, 1.813256598412491982, -0.7494862575098264479 ) ) ;
#28097=AXIS2_PLACEMENT_3D ( 'NONE', #67295, #133434, #17484 ) ;
#28099=CARTESIAN_POINT ( 'NONE',  ( 5.700121470611750674, -2.161883445634639411, -0.004416275431240455560 ) ) ;
#28103=CARTESIAN_POINT ( 'NONE',  ( 0.5439545674776785633, 1.865077268347898665, 0.1441030193207945287 ) ) ;
#28104=CARTESIAN_POINT ( 'NONE',  ( 6.063786081214013635, 1.415308013037285484, -1.001223213843880799 ) ) ;
#28106=CARTESIAN_POINT ( 'NONE',  ( 2.947022816757136621, -1.793111998972513277, -1.259777465452505796 ) ) ;
#28107=CARTESIAN_POINT ( 'NONE',  ( 4.928937574911031128, 2.206605557787114869, 0.6751633795739877542 ) ) ;
#28108=CARTESIAN_POINT ( 'NONE',  ( 6.063760116591036642, 2.031045510622536909, -0.3477994121598385613 ) ) ;
#28109=CARTESIAN_POINT ( 'NONE',  ( 1.658044662407763381, -1.373417096361102097, 1.373162012216273320 ) ) ;
#28113=CARTESIAN_POINT ( 'NONE',  ( 5.678019686890188211, 2.088907387943875982, -0.3644037002746222664 ) ) ;
#28115=CARTESIAN_POINT ( 'NONE',  ( 1.969375177810539945, -1.978050944945686673, -0.3905967402937361443 ) ) ;
#28117=CARTESIAN_POINT ( 'NONE',  ( 5.754950181447250124, -1.742976869204535983, 1.353379275444612562 ) ) ;
#28120=CARTESIAN_POINT ( 'NONE',  ( -0.02319159430949970999, 0.003959926571647092407, -1.810968101872318714 ) ) ;
#28126=CARTESIAN_POINT ( 'NONE',  ( 4.311438335051980708, -0.3541389166773502573, 2.030069380940119572 ) ) ;
#28128=CARTESIAN_POINT ( 'NONE',  ( 0.1331565106231328843, 0.003911343561965873426, -1.946049565259087455 ) ) ;
#28131=CARTESIAN_POINT ( 'NONE',  ( 4.758466132964124462, 2.014421802844321707, 0.1462751549737814905 ) ) ;
#28137=CARTESIAN_POINT ( 'NONE',  ( 4.627839754413318296, -1.266395719900258232, -1.625807017514354191 ) ) ;
#28138=CARTESIAN_POINT ( 'NONE',  ( 3.147111449167848019, 0.9091449406319618287, 1.799922684605055556 ) ) ;
#28140=CARTESIAN_POINT ( 'NONE',  ( 6.727182134110200273, -0.004969159814478123736, 2.189081792362323586 ) ) ;
#28144=CARTESIAN_POINT ( 'NONE',  ( 2.847029653296664353, -1.038834691150035461, 1.727737368502464621 ) ) ;
#28145=CARTESIAN_POINT ( 'NONE',  ( 2.554438963407625884, -1.601868926591401232, -0.9074879233003438905 ) ) ;
#28146=CARTESIAN_POINT ( 'NONE',  ( 1.085104692462773412, -2.252536170888468359, -0.5009029511823160918 ) ) ;
#28148=CARTESIAN_POINT ( 'NONE',  ( 3.110779230992101407, 1.568002374463087989, -1.488160049990403078 ) ) ;
#28150=( GEOMETRIC_REPRESENTATION_CONTEXT ( 3 ) GLOBAL_UNCERTAINTY_ASSIGNED_CONTEXT ( ( #102735 ) ) GLOBAL_UNIT_ASSIGNED_CONTEXT ( ( #68448, #86857, #188616 ) ) REPRESENTATION_CONTEXT ( 'NONE', 'WORKASPACE' ) );
#28153=CARTESIAN_POINT ( 'NONE',  ( 0.9537216069140028729, 1.868711056098860235, -0.08788249432020722729 ) ) ;
#28154=CARTESIAN_POINT ( 'NONE',  ( 6.139525842074132100, -1.427670353879314957, -1.359795004109279004 ) ) ;
#28158=CARTESIAN_POINT ( 'NONE',  ( 0.9970219447392356660, -0.5395372827587068265, -2.139793933917451874 ) ) ;
#28159=CARTESIAN_POINT ( 'NONE',  ( 6.584440175795505112, 1.195396180001909059, -1.690200020538407566 ) ) ;
#28162=CARTESIAN_POINT ( 'NONE',  ( 6.639320575229256782, 3.683803431435454190, 2.717262547424610375 ) ) ;
#28163=CARTESIAN_POINT ( 'NONE',  ( 4.926621433916460902, 1.886357061574754690, 0.5729670753305516895 ) ) ;
#28164=CARTESIAN_POINT ( 'NONE',  ( 6.504167520383483669, -0.8605252283936345448, 1.825738368183300153 ) ) ;
#28166=CARTESIAN_POINT ( 'NONE',  ( 4.916800105644766994, 1.594097815661306816, -1.668853466001555486 ) ) ;
#28167=CARTESIAN_POINT ( 'NONE',  ( 2.219651360329556233, 0.3568934070868194919, -2.031323280462021152 ) ) ;
#28174=CARTESIAN_POINT ( 'NONE',  ( 4.949771893170417769, 1.605651206033286815, 1.461634471724428064 ) ) ;
#28176=CARTESIAN_POINT ( 'NONE',  ( 4.300242120186610784, 1.420457692841030850, -1.171515996850613694 ) ) ;
#28179=CARTESIAN_POINT ( 'NONE',  ( 6.620655732516644854, 2.103946135090263514, 2.037628900882877847 ) ) ;
#28180=CARTESIAN_POINT ( 'NONE',  ( 6.005464345382193869, -2.175231771021503668, 0.2666438670960933344 ) ) ;
#28182=CARTESIAN_POINT ( 'NONE',  ( 6.473497647428577473, 2.167417048064937291, -0.6491153028224846411 ) ) ;
#28188=CARTESIAN_POINT ( 'NONE',  ( 0.4086181399716379281, 1.536643064871806574, 0.8779792868154213670 ) ) ;
#28190=CARTESIAN_POINT ( 'NONE',  ( 4.969394074578011633, -1.701821450762316612, -1.075051190359946895 ) ) ;
#28193=CARTESIAN_POINT ( 'NONE',  ( 4.471769775969771210, 2.043305595564361088, -0.5093722314385378258 ) ) ;
#28194=CARTESIAN_POINT ( 'NONE',  ( 2.214329231836575040, 1.858617268789555466, 0.4632827458446056035 ) ) ;
#28197=CARTESIAN_POINT ( 'NONE',  ( 3.332427603156477680, -1.175354876789212799, 1.580226413267592500 ) ) ;
#28198=CARTESIAN_POINT ( 'NONE',  ( 5.203380996274193038, 1.779418458119955915, -0.9556711282029080046 ) ) ;
#28199=CARTESIAN_POINT ( 'NONE',  ( 1.973319494866377699, 1.790917844098998124, -0.5403536831049270406 ) ) ;
#28200=CARTESIAN_POINT ( 'NONE',  ( 5.215364217145412873, -0.2476331258763775356, 1.706884187403294728 ) ) ;
#28201=CARTESIAN_POINT ( 'NONE',  ( 1.054777118923880597, 0.3758132965740559883, 1.874924941132802836 ) ) ;
#28203=CARTESIAN_POINT ( 'NONE',  ( 1.155211076828046579, -1.737760091701185505, 1.360235214042208263 ) ) ;
#28213=CARTESIAN_POINT ( 'NONE',  ( 2.436061438456170958, 1.271862942251865691, 1.633573898902056731 ) ) ;
#28218=CARTESIAN_POINT ( 'NONE',  ( 6.129554906816851556, -0.2598956320666659381, 2.104415924757463419 ) ) ;
#28223=CARTESIAN_POINT ( 'NONE',  ( 3.954453749441131816, 1.458333106491338960, 1.392332789497241263 ) ) ;
#28224=CARTESIAN_POINT ( 'NONE',  ( 4.680823747822191017, 1.589204433792507087, -1.069448900409355030 ) ) ;
#28226=CARTESIAN_POINT ( 'NONE',  ( 2.402122600552298870, -0.8417629408748151798, -2.023652355447075557 ) ) ;
#28227=CARTESIAN_POINT ( 'NONE',  ( 0.1333692844072767447, 1.351132181276387678, -2.308013766563504987 ) ) ;
#28229=CARTESIAN_POINT ( 'NONE',  ( 5.185796262198086204, 1.939088309008336397, -0.5409127675100529054 ) ) ;
#28232=CARTESIAN_POINT ( 'NONE',  ( 0.03478015955125923070, -1.617804660175032661, 1.203375172262765913 ) ) ;
#28234=CARTESIAN_POINT ( 'NONE',  ( 3.105106965723201551, -0.4054212715494521224, 2.050880055191468543 ) ) ;
#28236=CARTESIAN_POINT ( 'NONE',  ( 2.361930338997704659, 0.7344707938763440636, 1.560707491107244715 ) ) ;
#28238=CARTESIAN_POINT ( 'NONE',  ( 5.713165544288242970, 1.732532623411761286, -1.222520872474173848 ) ) ;
#28247=CARTESIAN_POINT ( 'NONE',  ( 1.383166562764587271, 0.1333312229490003775, -1.806600723499194538 ) ) ;
#28253=CARTESIAN_POINT ( 'NONE',  ( 2.807043740381453656, 1.552634882062135624, -0.9328946631028020020 ) ) ;
#28254=CARTESIAN_POINT ( 'NONE',  ( 6.639320575229259447, 0.002292789353198348111, 1.996863816985874118 ) ) ;
#28257=CARTESIAN_POINT ( 'NONE',  ( 4.527703488433511225, 1.805393378231552326, -0.4512502670087223944 ) ) ;
#28258=CARTESIAN_POINT ( 'NONE',  ( 1.142033650006045731, 0.7776438622074226537, 1.750858609485239192 ) ) ;
#28259=CARTESIAN_POINT ( 'NONE',  ( 1.324926479183065497, -0.04897172810776688479, 1.825096452545173609 ) ) ;
#28267=CARTESIAN_POINT ( 'NONE',  ( 6.051603174176475086, 1.488812912110796249, 1.289293616420229549 ) ) ;
#28270=CARTESIAN_POINT ( 'NONE',  ( 0.7618063994256699667, 1.031939465966443814, 1.818122583218291677 ) ) ;
#28272=CARTESIAN_POINT ( 'NONE',  ( 5.192375284248013756, -1.911820684568351192, -0.2360692857661383648 ) ) ;
#28274=CARTESIAN_POINT ( 'NONE',  ( 0.8502975112493587062, 0.5252643332615304361, 1.748389446526978031 ) ) ;
#28275=CARTESIAN_POINT ( 'NONE',  ( 2.702037527177497012, -0.6914408288211832954, 2.095836555436859872 ) ) ;
#28276=CARTESIAN_POINT ( 'NONE',  ( -0.08783152977152529350, -1.912005390248720627, -0.04503566501021933483 ) ) ;
#28277=CARTESIAN_POINT ( 'NONE',  ( 0.9241884870439884825, 0.9676023207046909880, 1.715383555584276909 ) ) ;
#28278=CARTESIAN_POINT ( 'NONE',  ( 2.612754452619329371, -0.1881026344860724786, 1.932912858947251511 ) ) ;
#28279=CARTESIAN_POINT ( 'NONE',  ( 0.8431247865267020858, -1.122328847578180078, 1.674629589540656216 ) ) ;
#28281=CARTESIAN_POINT ( 'NONE',  ( 5.084723738625635647, 1.780007044882421008, 0.5427147737909858716 ) ) ;
#28287=CARTESIAN_POINT ( 'NONE',  ( 1.154151856878969928, 0.8927059368322427524, 2.001694687108931170 ) ) ;
#28292=CARTESIAN_POINT ( 'NONE',  ( 3.141029808440584326, -1.609794727316344209, 0.8612202190056221784 ) ) ;
#28295=DIRECTION ( 'NONE',  ( -0.9999980456341537316, 0.000000000000000000, -0.001977050295958555567 ) ) ;
#28297=CARTESIAN_POINT ( 'NONE',  ( 1.365712245162364225, 1.898099017218597195, -0.3287360691993664874 ) ) ;
#28298=CARTESIAN_POINT ( 'NONE',  ( 5.084793414397763556, 1.876112756342168675, 0.5732009990792874543 ) ) ;
#28303=CARTESIAN_POINT ( 'NONE',  ( 5.407841436338867602, -0.9846607899807978681, -1.957994596084790206 ) ) ;
#28305=CARTESIAN_POINT ( 'NONE',  ( 3.485274717979901293, 0.04603381543630095940, 2.069897711131869933 ) ) ;
#28309=CARTESIAN_POINT ( 'NONE',  ( 3.639517500262396954, 0.8282738168534724554, 2.144427848026169592 ) ) ;
#28316=CARTESIAN_POINT ( 'NONE',  ( 3.591681417399609888, -1.939766604489696622, -0.09448766823863874453 ) ) ;
#28320=CARTESIAN_POINT ( 'NONE',  ( 5.256085721135645095, 0.7693902824621422498, -1.750971482026221437 ) ) ;
#28321=CARTESIAN_POINT ( 'NONE',  ( 6.141572722362285575, -1.252861708448499201, -1.185644778512841002 ) ) ;
#28322=CARTESIAN_POINT ( 'NONE',  ( 5.067592334412735156, 1.357865985192594049, 1.490972259599516070 ) ) ;
#28324=CARTESIAN_POINT ( 'NONE',  ( 2.157103830005083100, -1.704838622333640030, 1.401371054633032909 ) ) ;
#28327=CARTESIAN_POINT ( 'NONE',  ( 1.921934154048171584, 1.202774473455773041, -1.709796194579858319 ) ) ;
#28328=CARTESIAN_POINT ( 'NONE',  ( 0.6195364366361589825, -0.9414703481081601044, -1.498462015107356882 ) ) ;
#28329=CARTESIAN_POINT ( 'NONE',  ( 5.801407773674092105, 1.352156682446105984, -1.496049708713815374 ) ) ;
#28331=CARTESIAN_POINT ( 'NONE',  ( 3.293229231460121031, 1.807080150709074129, 1.410200864199236293 ) ) ;
#28332=CARTESIAN_POINT ( 'NONE',  ( 0.5854151811709865649, -1.726609166672494311, -0.2174223460936832719 ) ) ;
#28333=CARTESIAN_POINT ( 'NONE',  ( 2.848016566918720294, -1.427295477286108394, -1.568503593382633454 ) ) ;
#28335=CARTESIAN_POINT ( 'NONE',  ( 1.457864220016273693, 1.308402020977760261, 1.137755859488085886 ) ) ;
#28338=( BOUNDED_CURVE ( )  B_SPLINE_CURVE ( 3, ( #191291, #124271, #61313, #90633 ),
 .UNSPECIFIED., .F., .T. ) 
 B_SPLINE_CURVE_WITH_KNOTS ( ( 4, 4 ),
 ( 0.000000000000000000, 0.4999999999999948930 ),
 .UNSPECIFIED. ) 
 CURVE ( )  GEOMETRIC_REPRESENTATION_ITEM ( )  RATIONAL_B_SPLINE_CURVE ( ( 1.000000000000000444, 0.3333333333333403092, 0.3333333333333334814, 0.9999999999999936717 ) ) 
 REPRESENTATION_ITEM ( '' )  );
#28339=CARTESIAN_POINT ( 'NONE',  ( 0.8542542287434266024, -0.7813174834335520069, 2.025881038206469587 ) ) ;
#28340=CARTESIAN_POINT ( 'NONE',  ( 3.309780021317248355, -1.205041885261768808, -1.616693488061982098 ) ) ;
#28341=CARTESIAN_POINT ( 'NONE',  ( 5.343750000000003553, 1.895863743164196258, 0.7852924748297027691 ) ) ;
#28344=CARTESIAN_POINT ( 'NONE',  ( 6.252564000042572623, 0.6067452241035797833, 1.828529084590237774 ) ) ;
#28346=CARTESIAN_POINT ( 'NONE',  ( 3.691809873939347675, 2.090716244852005357, -0.7509968985505171002 ) ) ;
#28352=CARTESIAN_POINT ( 'NONE',  ( 4.897892112245933127, -0.5929259483795108476, -1.636466244661118452 ) ) ;
#28353=CARTESIAN_POINT ( 'NONE',  ( 4.932062528313535310, 1.127988425013145779, 1.604980062286972542 ) ) ;
#28357=CARTESIAN_POINT ( 'NONE',  ( 5.009165025557245521, 1.964990322317389015, 1.121224042300600576 ) ) ;
#28358=CARTESIAN_POINT ( 'NONE',  ( 1.961455461422195068, 1.713676499688887800, 1.147740006246004585 ) ) ;
#28363=CARTESIAN_POINT ( 'NONE',  ( 4.042156614576187579, 1.861303109871172312, 0.1859210194900539903 ) ) ;
#28364=CARTESIAN_POINT ( 'NONE',  ( 2.953449220662739183, -1.603453536992532902, -0.6609773998737851208 ) ) ;
#28365=CARTESIAN_POINT ( 'NONE',  ( 6.216381822182693639, 2.044192415450503120, 0.7905562269360306704 ) ) ;
#28366=CARTESIAN_POINT ( 'NONE',  ( 0.9915960798324228165, 1.945464911009102460, -1.041603813667857370 ) ) ;
#28367=CARTESIAN_POINT ( 'NONE',  ( 3.661132068870280420, -1.905464569931826446, -1.020879743040298271 ) ) ;
#28368=CARTESIAN_POINT ( 'NONE',  ( 4.874914055504836696, 1.811399353594527639, -0.7004420144864877962 ) ) ;
#28372=CARTESIAN_POINT ( 'NONE',  ( -0.08726289061519039436, -1.242903867559573161, -1.588418431006669351 ) ) ;
#28375=CARTESIAN_POINT ( 'NONE',  ( 6.258435431136967431, 1.928752767684217106, -0.5880170417187426946 ) ) ;
#28379=CARTESIAN_POINT ( 'NONE',  ( 3.123480263227970344, -1.759325740769552393, 0.4874977319994436287 ) ) ;
#28380=CARTESIAN_POINT ( 'NONE',  ( 2.573496151666111231, 0.1090403232480302298, -2.204208057042057245 ) ) ;
#28385=CARTESIAN_POINT ( 'NONE',  ( 0.6682303662221461549, 2.017294962401328107, -0.1032846847020176678 ) ) ;
#28386=CARTESIAN_POINT ( 'NONE',  ( 0.8035760164417544704, 1.868272328500224289, -1.003034915376184388 ) ) ;
#28388=EDGE_LOOP ( 'NONE', ( #159563, #111733, #30659, #133270 ) ) ;
#28390=CARTESIAN_POINT ( 'NONE',  ( 2.166652004499136197, 1.382927810177040584, -1.245475062859234372 ) ) ;
#28393=CARTESIAN_POINT ( 'NONE',  ( 1.024558638192473170, 1.287004556549703693, -1.736669753874709343 ) ) ;
#28394=CARTESIAN_POINT ( 'NONE',  ( 5.695935454815424848, 1.779625283580280382, 0.9480427965274510482 ) ) ;
#28398=CARTESIAN_POINT ( 'NONE',  ( 3.580510235063854019, -1.759844519496515325, -0.4856381957471164745 ) ) ;
#28403=CARTESIAN_POINT ( 'NONE',  ( 5.870470189955956819, -0.4925641237488035395, 1.954873771647095415 ) ) ;
#28404=CARTESIAN_POINT ( 'NONE',  ( 6.105383947169263692, -1.826632712061267094, 0.2301338403083788009 ) ) ;
#28405=CARTESIAN_POINT ( 'NONE',  ( -0.02319159430947542386, 5.725354828811364705, -2.405035539666657840 ) ) ;
#28406=CARTESIAN_POINT ( 'NONE',  ( 4.477368160356545168, 0.002844634383740093052, -2.307868969966973438 ) ) ;
#28408=CARTESIAN_POINT ( 'NONE',  ( 6.503215372615936296, 1.793156143535659108, 1.206815395834538451 ) ) ;
#28410=CARTESIAN_POINT ( 'NONE',  ( 2.753386078659710190, 1.932462020465589125, -0.1930240951200749566 ) ) ;
#28412=CARTESIAN_POINT ( 'NONE',  ( 4.675370021169432455, -0.9774931845568238797, -2.080278028362152032 ) ) ;
#28413=CARTESIAN_POINT ( 'NONE',  ( 0.1751657365761550289, 0.002452341591364583847, -2.044164811867712483 ) ) ;
#28416=CARTESIAN_POINT ( 'NONE',  ( 4.223419137798128276, -1.790188510885984297, 0.5427707113358354318 ) ) ;
#28418=CARTESIAN_POINT ( 'NONE',  ( 2.232540727315056373, 1.246330492051262784, -1.450604739030990187 ) ) ;
#28421=CARTESIAN_POINT ( 'NONE',  ( 3.721466898765386500, -0.1629207441977159332, 2.200919931280575170 ) ) ;
#28422=CARTESIAN_POINT ( 'NONE',  ( 6.883263157960418432, 2.078485899884211285, 2.154856264959764012 ) ) ;
#28423=CARTESIAN_POINT ( 'NONE',  ( -0.2108831679771168421, 7.629137130509075604, -2.497154329497493386 ) ) ;
#28426=CARTESIAN_POINT ( 'NONE',  ( 1.300003668391478406, -1.971530339922975550, -0.004173579811568225127 ) ) ;
#28427=CARTESIAN_POINT ( 'NONE',  ( 1.325685429717119446, -0.05423940138811130657, 2.307114084963398870 ) ) ;
#28428=CARTESIAN_POINT ( 'NONE',  ( 2.717183929654675811, -1.705535211757349456, -0.9694657131227711888 ) ) ;
#28430=CARTESIAN_POINT ( 'NONE',  ( 5.893442400364165223, -1.866981718288396763, 0.8769185494091299438 ) ) ;
#28437=CARTESIAN_POINT ( 'NONE',  ( 1.674930785650229792, 1.460053457903678131, -1.606915656648603141 ) ) ;
#28441=CARTESIAN_POINT ( 'NONE',  ( 3.040157689216971715, 1.855973101128991054, 0.2326549598439253685 ) ) ;
#28442=CARTESIAN_POINT ( 'NONE',  ( 6.239563118392394969, -1.560868990211834895, -1.495623836407403262 ) ) ;
#28444=CARTESIAN_POINT ( 'NONE',  ( -0.02224634325197898804, 1.983040877609225872, -2.702260234736663325 ) ) ;
#28445=CARTESIAN_POINT ( 'NONE',  ( 6.727182134110222478, 0.005875948494733079785, 1.810970247402940547 ) ) ;
#28448=CARTESIAN_POINT ( 'NONE',  ( 2.262237773093742188, 1.911903731097279513, 0.04523801603947830152 ) ) ;
#28449=CARTESIAN_POINT ( 'NONE',  ( 4.610057705051894494, -0.7578761767026606089, -1.599493228202266470 ) ) ;
#28450=CARTESIAN_POINT ( 'NONE',  ( 1.875505643822904300, 0.3255412885708880433, -1.884197853084010443 ) ) ;
#28452=CARTESIAN_POINT ( 'NONE',  ( 0.05764063133973944958, 1.105241252117078909, 1.564514492536345891 ) ) ;
#28454=CARTESIAN_POINT ( 'NONE',  ( 0.6079806153083644471, 0.6509857562557037625, -1.965403638620793147 ) ) ;
#28457=CARTESIAN_POINT ( 'NONE',  ( 5.401189721097995111, 1.529905263132097071, 1.076157610686766075 ) ) ;
#28458=CARTESIAN_POINT ( 'NONE',  ( 1.752308680507021155, 0.5713779359179693706, 1.734036872924920702 ) ) ;
#28459=CARTESIAN_POINT ( 'NONE',  ( 4.283934280384479543, 1.440456688004333019, 1.672026782002330458 ) ) ;
#28462=CARTESIAN_POINT ( 'NONE',  ( 3.455586768955606125, 1.624414792841613941, 1.271063249801159145 ) ) ;
#28470=CARTESIAN_POINT ( 'NONE',  ( 5.266107318980479235, -2.060723932065291031, 0.1993833602659672022 ) ) ;
#28472=CARTESIAN_POINT ( 'NONE',  ( 3.128364550451453230, 1.203671540783244565, -1.795256801906938815 ) ) ;
#28474=CARTESIAN_POINT ( 'NONE',  ( 2.736978119973699108, 1.902454848370996210, 0.6784627630139413723 ) ) ;
#28475=CARTESIAN_POINT ( 'NONE',  ( 6.720655732516647163, 2.019696082639847567, 2.477441386028636394 ) ) ;
#28481=CARTESIAN_POINT ( 'NONE',  ( 1.288296401830712368, -0.7303101666344159471, -1.879802715551846859 ) ) ;
#28483=CARTESIAN_POINT ( 'NONE',  ( 6.023007056224171762, -2.064090639567913499, 0.7368321019862942300 ) ) ;
#28485=CARTESIAN_POINT ( 'NONE',  ( 4.763870730211980487, 0.5944114921396548290, -1.817767169311027997 ) ) ;
#28489=CARTESIAN_POINT ( 'NONE',  ( 3.110954007106698338, 0.05231540665236523308, 2.015913653835194719 ) ) ;
#28492=CARTESIAN_POINT ( 'NONE',  ( 5.069259022003644866, 0.1660796517843898534, -1.716765078168249969 ) ) ;
#28497=CARTESIAN_POINT ( 'NONE',  ( 0.6376584384039893916, 1.932990051301992418, -0.7417924570976215382 ) ) ;
#28499=CARTESIAN_POINT ( 'NONE',  ( 6.883263157960362477, -0.004191378316371896506, 2.053658919477070910 ) ) ;
#28501=CARTESIAN_POINT ( 'NONE',  ( 6.463521484642490655, -1.459484751789320134, -1.072804587801470921 ) ) ;
#28505=CARTESIAN_POINT ( 'NONE',  ( 0.7909136568654427935, -0.04542554662571558072, -1.811195533156365611 ) ) ;
#28508=CARTESIAN_POINT ( 'NONE',  ( 3.117305861062225958, -2.111875107304355570, 0.5849144002756587746 ) ) ;
#28510=ADVANCED_FACE ( 'NONE', ( #136955 ), #202981, .T. ) ;
#28511=CARTESIAN_POINT ( 'NONE',  ( 0.4319881149899909567, 1.126445828788334991, 1.606065282034954578 ) ) ;
#28513=CARTESIAN_POINT ( 'NONE',  ( 5.220295459014530515, 1.888029131402849670, 0.3228437444452412763 ) ) ;
#28522=CARTESIAN_POINT ( 'NONE',  ( 2.096749907087645415, -0.5762017740289017143, -2.083436276955972222 ) ) ;
#28525=CARTESIAN_POINT ( 'NONE',  ( 1.606192798902779328, -0.6535759462080005244, -1.704761432720684144 ) ) ;
#28526=CARTESIAN_POINT ( 'NONE',  ( 0.1059362375676886209, 1.575662574916199210, 1.419458935296296520 ) ) ;
#28527=CARTESIAN_POINT ( 'NONE',  ( 4.401258566127845384, 1.466438172381477223, 1.087111955044787859 ) ) ;
#28531=CARTESIAN_POINT ( 'NONE',  ( 3.560960244297206589, 1.554118163632215444, -1.209804376587125807 ) ) ;
#28533=CARTESIAN_POINT ( 'NONE',  ( 6.304245038521663957, 1.436082020041820506, -1.307557180447990186 ) ) ;
#28539=CARTESIAN_POINT ( 'NONE',  ( 3.633378786761193968, -0.1378984027537045187, 1.907353237798288470 ) ) ;
#28540=EDGE_LOOP ( 'NONE', ( #68633, #118952, #15431, #194700 ) ) ;
#28546=CARTESIAN_POINT ( 'NONE',  ( 5.074862666803740652, -1.456563189067984876, 1.389812660683345191 ) ) ;
#28547=CARTESIAN_POINT ( 'NONE',  ( 0.1333542156527477984, 0.001576319744088546491, -2.046049510433407548 ) ) ;
#28548=CARTESIAN_POINT ( 'NONE',  ( 5.848246728868278232, 1.823843535133644389, 0.08496628090458313576 ) ) ;
#28549=CARTESIAN_POINT ( 'NONE',  ( 0.6079806153083644471, 0.6509857562557037625, -1.965403638620793147 ) ) ;
#28553=CARTESIAN_POINT ( 'NONE',  ( 6.473518811298506925, 1.789458955665638618, -0.5451884755478533240 ) ) ;
#28561=CARTESIAN_POINT ( 'NONE',  ( 4.201623210320468260, 1.587898197979008774, 0.6974748919710629380 ) ) ;
#28565=CARTESIAN_POINT ( 'NONE',  ( 1.129834432590616000, 1.996231214973245516, -0.5485114149718294252 ) ) ;
#28566=CARTESIAN_POINT ( 'NONE',  ( 3.708711176059620751, 2.011172256762243649, 0.6619615953592747903 ) ) ;
#28570=CARTESIAN_POINT ( 'NONE',  ( 0.8308272516417656295, -1.852502698908803591, -0.6688572162713811720 ) ) ;
#28575=CARTESIAN_POINT ( 'NONE',  ( 3.187719515414323190, -0.9288583595017800842, 2.095805606604860039 ) ) ;
#28576=CARTESIAN_POINT ( 'NONE',  ( 0.8381832108898427114, 1.798179982845280467, 0.3147962740308178353 ) ) ;
#28577=CARTESIAN_POINT ( 'NONE',  ( 3.252119977711815491, 0.8557668478980616777, -1.710280963351323846 ) ) ;
#28582=CARTESIAN_POINT ( 'NONE',  ( 2.109637220322407192, 1.559014694980038085, 1.273805747723085746 ) ) ;
#28583=CARTESIAN_POINT ( 'NONE',  ( 1.938261246079517219, -1.053878627966830184, 1.654468565904606558 ) ) ;
#28587=CARTESIAN_POINT ( 'NONE',  ( 5.542948256250054051, -1.647469546829454234, -1.286982348046373570 ) ) ;
#28588=CARTESIAN_POINT ( 'NONE',  ( 3.819032205515503708, -0.1302183858614604506, 1.765120429581680916 ) ) ;
#28590=( NAMED_UNIT ( * ) SI_UNIT ( $, .STERADIAN. ) SOLID_ANGLE_UNIT ( ) );
#28591=CARTESIAN_POINT ( 'NONE',  ( 0.1116237293282626442, -2.148295633857814746, 0.4319020730012904097 ) ) ;
#28592=CARTESIAN_POINT ( 'NONE',  ( 4.751753191611454596, 0.6700524488352653796, 1.606376638082593455 ) ) ;
#28596=CARTESIAN_POINT ( 'NONE',  ( 4.604694260812782325, 0.7408162341489711311, -1.567766963475358599 ) ) ;
#28597=CARTESIAN_POINT ( 'NONE',  ( 4.352125359537689420, -0.8347222424532302343, 2.004499096949263759 ) ) ;
#28599=CARTESIAN_POINT ( 'NONE',  ( 0.5502106600992883179, 1.049441996780882125, 1.838938355043976847 ) ) ;
#28600=CARTESIAN_POINT ( 'NONE',  ( 5.937500000000004441, 1.451031289060873863, -1.451031289061349927 ) ) ;
#28602=CARTESIAN_POINT ( 'NONE',  ( 2.889578633693023590, 1.361086032938205070, 1.363490106525049317 ) ) ;
#28604=CARTESIAN_POINT ( 'NONE',  ( 0.1182595804350913826, -0.5859369620430117109, 2.142582832819041716 ) ) ;
#28606=CARTESIAN_POINT ( 'NONE',  ( -0.2411972340275865823, -0.002466136893032512371, -1.900252416837118208 ) ) ;
#28609=CARTESIAN_POINT ( 'NONE',  ( 2.473529351063200377, -1.934054200746947227, -1.092377531094531173 ) ) ;
#28613=CARTESIAN_POINT ( 'NONE',  ( 0.3346115673153668424, 0.6298721381652396811, -1.915601020889952322 ) ) ;
#28615=CARTESIAN_POINT ( 'NONE',  ( 5.213357787468869020, -1.740689653174596563, -1.106377904087485486 ) ) ;
#28621=CARTESIAN_POINT ( 'NONE',  ( 6.919227945209173392, -0.1346273106918663420, 1.840389347376285345 ) ) ;
#28622=CARTESIAN_POINT ( 'NONE',  ( 5.502511934227880097, -1.689919030931926969, 0.3883318411201929776 ) ) ;
#28623=CARTESIAN_POINT ( 'NONE',  ( 5.407646374456077432, -0.7895141955979433357, -1.551160667784831748 ) ) ;
#28624=CARTESIAN_POINT ( 'NONE',  ( 3.052548088455210973, -1.734419513972422555, 1.498989523525402934 ) ) ;
#28626=CARTESIAN_POINT ( 'NONE',  ( 2.747807751077631977, 0.6205313035267927546, 1.733543155639664990 ) ) ;
#28630=CARTESIAN_POINT ( 'NONE',  ( 2.151128115021032627, -1.464471472660273665, -1.089769533225225073 ) ) ;
#28631=CARTESIAN_POINT ( 'NONE',  ( 2.215470409936692420, 1.956561601830292485, 0.4872017847364697452 ) ) ;
#28634=CARTESIAN_POINT ( 'NONE',  ( 4.717860591023939953, -2.065837571889141078, 0.4082076317219375250 ) ) ;
#28637=CARTESIAN_POINT ( 'NONE',  ( 2.699741690289765295, -1.532448122638006671, -1.392287113214360827 ) ) ;
#28640=CARTESIAN_POINT ( 'NONE',  ( 5.215537505735290402, 1.733765862324820439, 1.220609238144418240 ) ) ;
#28641=CARTESIAN_POINT ( 'NONE',  ( 6.252569598636129378, 0.5776572744066664766, 1.731972519516040032 ) ) ;
#28648=CARTESIAN_POINT ( 'NONE',  ( 6.504144398916748671, -0.9053081408615070158, 1.915699539216948688 ) ) ;
#28649=CARTESIAN_POINT ( 'NONE',  ( 0.9035134896902213830, 1.721610636892715984, 1.212602220121623775 ) ) ;
#28652=CARTESIAN_POINT ( 'NONE',  ( 5.119887769377023723, 1.841019424034021412, -0.2705144023524996277 ) ) ;
#28661=CARTESIAN_POINT ( 'NONE',  ( 2.330453122711079850, -1.209328770571056921, 1.544706564130463811 ) ) ;
#28662=CARTESIAN_POINT ( 'NONE',  ( 0.8136072859011161951, -0.3160970183575459447, 2.138355382504661506 ) ) ;
#28667=CARTESIAN_POINT ( 'NONE',  ( 2.829097238278361459, -1.198370081129100262, 1.253277946039689450 ) ) ;
#28668=CARTESIAN_POINT ( 'NONE',  ( 1.903882329689795094, 1.290680248512179551, -1.167607185883823728 ) ) ;
#28671=CARTESIAN_POINT ( 'NONE',  ( 0.9661724576192336489, 1.646585359754201061, 1.163093122096101162 ) ) ;
#28672=CARTESIAN_POINT ( 'NONE',  ( 6.825078400183588023, 2.959908325773926041, 2.496992193004472504 ) ) ;
#28674=CARTESIAN_POINT ( 'NONE',  ( 1.393369717069929514, 1.491581312685308580, 1.289216981855696664 ) ) ;
#28675=CARTESIAN_POINT ( 'NONE',  ( 5.924064563541377559, -1.897137492723115049, 0.2407653536913647030 ) ) ;
#28680=CARTESIAN_POINT ( 'NONE',  ( 1.137374441040917672, -0.04723908312853628000, 2.019287564836816262 ) ) ;
#28682=CARTESIAN_POINT ( 'NONE',  ( 4.067613405475267285, 0.2862205578705340203, -2.289715105617713409 ) ) ;
#28683=CARTESIAN_POINT ( 'NONE',  ( 6.039501783790233169, 1.813256598412491982, -0.7494862575098264479 ) ) ;
#28684=CARTESIAN_POINT ( 'NONE',  ( 2.782025223480470544, -1.125517505138178942, -1.606590762409945583 ) ) ;
#28688=CARTESIAN_POINT ( 'NONE',  ( 1.024788983299034451, 0.4191291695722613730, 2.075291419971446061 ) ) ;
#28691=CARTESIAN_POINT ( 'NONE',  ( 2.325889007780062023, 1.785771638016835361, 0.4476198290149570602 ) ) ;
#28694=CARTESIAN_POINT ( 'NONE',  ( 2.724977724663907530, 1.532976055022855499, -1.465462182430438798 ) ) ;
#28698=CARTESIAN_POINT ( 'NONE',  ( 3.514965343742028736, 1.861552560010207191, 0.8843320499443955152 ) ) ;
#28701=CARTESIAN_POINT ( 'NONE',  ( 0.2043192855987647494, 1.601443664334546213, 0.9084302959305108338 ) ) ;
#28703=CARTESIAN_POINT ( 'NONE',  ( -0.02224634325196597762, 7.629137130509080045, -2.889100442546748582 ) ) ;
#28706=CARTESIAN_POINT ( 'NONE',  ( 2.284789498180723744, -2.218439058979736700, -0.4430748376489759832 ) ) ;
#28708=CARTESIAN_POINT ( 'NONE',  ( 2.689504281738527514, 1.718874962283756691, -0.5722189708131807384 ) ) ;
#28709=CARTESIAN_POINT ( 'NONE',  ( 2.817496537900533671, -1.290266535947793392, -1.416188432289398058 ) ) ;
#28710=CARTESIAN_POINT ( 'NONE',  ( 4.176279081494421952, -1.061646348645030713, -1.777293304589353085 ) ) ;
#28712=CARTESIAN_POINT ( 'NONE',  ( 2.131653300961271924, -1.286245803994587877, -1.494167145092902160 ) ) ;
#28713=CARTESIAN_POINT ( 'NONE',  ( 0.2879446430137333479, -0.9113367411649232475, 1.697199823463049428 ) ) ;
#28714=CARTESIAN_POINT ( 'NONE',  ( 2.834663617355744680, 0.2272019944037397543, 1.856728029318695627 ) ) ;
#28715=CARTESIAN_POINT ( 'NONE',  ( 2.666999619196269045, -1.590435880060107499, 1.672335932400937253 ) ) ;
#28717=CARTESIAN_POINT ( 'NONE',  ( 2.963170385688845609, 1.570644928931948181, 0.9979875196418576122 ) ) ;
#28719=CARTESIAN_POINT ( 'NONE',  ( 6.074688485276667826, 1.387953460639863801, -1.525998863508086778 ) ) ;
#28724=CARTESIAN_POINT ( 'NONE',  ( 6.581095821095639842, -0.09928302661296910248, -2.103742297734310984 ) ) ;
#28726=CARTESIAN_POINT ( 'NONE',  ( 6.063787883973515314, 2.130759124531961923, -0.3628933549372145295 ) ) ;
#28727=CARTESIAN_POINT ( 'NONE',  ( 6.270176981224262924, 2.014133449145325105, -0.1505704652167982327 ) ) ;
#28732=CARTESIAN_POINT ( 'NONE',  ( 6.825078400183572036, 7.053423702906556514, 2.353807037893948628 ) ) ;
#28735=CARTESIAN_POINT ( 'NONE',  ( 4.997279897388729353, -0.2910847460899004258, 1.995267753224789997 ) ) ;
#28740=CARTESIAN_POINT ( 'NONE',  ( 5.541917325712655717, 0.8799508658935292216, -1.974686638939105343 ) ) ;
#28745=CARTESIAN_POINT ( 'NONE',  ( -0.05329673158829557195, -1.711387015114009369, -0.8607133870397830622 ) ) ;
#28749=CARTESIAN_POINT ( 'NONE',  ( 1.523609404914439969, -0.9557964113278711871, -1.435619824176268100 ) ) ;
#28753=CARTESIAN_POINT ( 'NONE',  ( 1.176598488244801954, -0.03600270464337343435, -1.769546047349578100 ) ) ;
#28754=CARTESIAN_POINT ( 'NONE',  ( 1.893228294049788207, -0.1010902060475794423, -2.010683160356161014 ) ) ;
#28756=CARTESIAN_POINT ( 'NONE',  ( 3.768774344222697970, -1.483932802477351487, 1.633493490917396151 ) ) ;
#28757=CARTESIAN_POINT ( 'NONE',  ( 5.489208499878581726, 0.1525156608223678933, 2.165750181564994215 ) ) ;
#28761=CARTESIAN_POINT ( 'NONE',  ( 3.299587915756982515, 1.916203934664402198, -0.9084051299479002362 ) ) ;
#28762=CARTESIAN_POINT ( 'NONE',  ( 3.269157808572686896, 1.821735364950356484, -0.8647411805496332260 ) ) ;
#28763=CARTESIAN_POINT ( 'NONE',  ( 3.076200346286896536, 0.8185659037078784062, 1.616202036402814901 ) ) ;
#28768=CARTESIAN_POINT ( 'NONE',  ( 0.4439547499465161251, 1.865322535695708606, 0.1421067652795371117 ) ) ;
#28772=CARTESIAN_POINT ( 'NONE',  ( 1.850665572125685721, -1.753200486404655090, -0.7725721188126480898 ) ) ;
#28773=CARTESIAN_POINT ( 'NONE',  ( 0.1745949693968694705, 0.009193469831055359198, -1.755468632744116242 ) ) ;
#28778=CARTESIAN_POINT ( 'NONE',  ( 5.594645800149128156, -0.5210773734287167391, -2.097845705497362712 ) ) ;
#28781=CARTESIAN_POINT ( 'NONE',  ( 3.041385797112206912, 0.05609166564453024750, 2.120036961950934273 ) ) ;
#28784=CARTESIAN_POINT ( 'NONE',  ( 4.921144022694462272, -0.09977086410491335655, 1.968969177566483042 ) ) ;
#28787=CARTESIAN_POINT ( 'NONE',  ( 5.559793223943660934, 1.263291928365728012, 1.699014672817029892 ) ) ;
#28789=CARTESIAN_POINT ( 'NONE',  ( 6.883263157960362477, -0.001323150302089473379, 1.953658984494692330 ) ) ;
#28790=CARTESIAN_POINT ( 'NONE',  ( 2.554547512858021729, -1.689694153139981392, -0.9569994400411386826 ) ) ;
#28794=CARTESIAN_POINT ( 'NONE',  ( 2.660199397079235695, -1.441175001385604393, 1.514759066650630093 ) ) ;
#28797=CARTESIAN_POINT ( 'NONE',  ( -0.005635951793048382327, -1.756493610686832740, -0.4425278525194314971 ) ) ;
#28799=CARTESIAN_POINT ( 'NONE',  ( 4.178501018151202118, -1.271701901513167421, 1.803451139310302986 ) ) ;
#28800=CARTESIAN_POINT ( 'NONE',  ( 2.784424029790978139, -1.135345490304447091, 1.892179603154810819 ) ) ;
#28803=CARTESIAN_POINT ( 'NONE',  ( 1.418461073652961257, -0.6892283116659430053, -1.783923526276688154 ) ) ;
#28805=CARTESIAN_POINT ( 'NONE',  ( 5.230950013807261989, -1.948248037745937022, -0.7008574099531189594 ) ) ;
#28808=CARTESIAN_POINT ( 'NONE',  ( 3.204151765443470357, -2.159293047372488950, 0.1044485798024074874 ) ) ;
#28809=CARTESIAN_POINT ( 'NONE',  ( 4.546525781634036534, -1.759932548463913671, 1.305750774140898685 ) ) ;
#28817=CARTESIAN_POINT ( 'NONE',  ( 0.7389079861009685279, 2.013985778099684154, -0.1017531103126300962 ) ) ;
#28820=CARTESIAN_POINT ( 'NONE',  ( 4.750872686184268723, -0.4484009487188305165, -2.020967519627144604 ) ) ;
#28821=CARTESIAN_POINT ( 'NONE',  ( 2.824735624865559735, 1.814154213653540237, 0.6486305857245775464 ) ) ;
#28822=CARTESIAN_POINT ( 'NONE',  ( 0.08751785467620704084, -0.5350655163729299835, 1.944078888069140865 ) ) ;
#28824=CARTESIAN_POINT ( 'NONE',  ( 3.573067284968055812, 1.778583338327298646, 0.8461400097728142278 ) ) ;
#28825=CARTESIAN_POINT ( 'NONE',  ( 0.2698121887318750689, 1.265274936352598134, 1.789097752032620114 ) ) ;
#28826=CARTESIAN_POINT ( 'NONE',  ( 4.441915170580639227, 0.7783198120194650960, -1.651611053696280695 ) ) ;
#28833=CARTESIAN_POINT ( 'NONE',  ( 1.241482983173985533, 1.839155304979672501, 0.08999620058360720265 ) ) ;
#28834=CARTESIAN_POINT ( 'NONE',  ( 4.799092303436800933, -0.2508153390233992530, -1.997484173059483892 ) ) ;
#28835=CARTESIAN_POINT ( 'NONE',  ( 0.4569821463788895644, 1.705326812283548765, 1.541052590308614745 ) ) ;
#28836=CARTESIAN_POINT ( 'NONE',  ( 4.979329090789969214, -0.1002203015587413149, 1.959344625532564610 ) ) ;
#28842=CARTESIAN_POINT ( 'NONE',  ( 1.347338520094189862, 0.6037249722931283813, -2.001697839036377324 ) ) ;
#28843=CARTESIAN_POINT ( 'NONE',  ( 6.438360790777991838, 1.751285973423050368, 0.2548140705225035441 ) ) ;
#28845=CARTESIAN_POINT ( 'NONE',  ( -0.1104750535120268828, 5.720715034752038797, -2.697548938405624597 ) ) ;
#28846=CARTESIAN_POINT ( 'NONE',  ( 2.260927701655718103, 1.706565837815830822, -0.3407169315452397984 ) ) ;
#28850=CARTESIAN_POINT ( 'NONE',  ( 1.892754278755165664, 1.501794282950255965, -0.8482797957840328973 ) ) ;
#28851=CARTESIAN_POINT ( 'NONE',  ( 1.558417602779540889, -1.546676288433556756, 1.552911753681482487 ) ) ;
#28853=CARTESIAN_POINT ( 'NONE',  ( 4.196070124731249074, -0.8457972711899945928, 2.038567251995755836 ) ) ;
#28855=CARTESIAN_POINT ( 'NONE',  ( 2.114367463569406080, 2.165448829365283157, -0.1565315255437193243 ) ) ;
#28856=CARTESIAN_POINT ( 'NONE',  ( 0.5920835508136900183, -1.811502216344462735, -0.2265648652611390590 ) ) ;
#28857=CARTESIAN_POINT ( 'NONE',  ( 3.345011933649364444, -1.869310496227539531, -0.9943253416123465360 ) ) ;
#28858=CARTESIAN_POINT ( 'NONE',  ( 6.639320575229278099, 0.5905802482995252678, 1.949996947996739172 ) ) ;
#28860=CARTESIAN_POINT ( 'NONE',  ( 3.948992478018618080, -1.906111675684089901, -1.273188117731700597 ) ) ;
#28864=CARTESIAN_POINT ( 'NONE',  ( 5.988988838570013407, -2.108473666775429134, -0.6992015888120094447 ) ) ;
#28872=CARTESIAN_POINT ( 'NONE',  ( 4.518204034511161815, -1.842447959940773705, 0.8197716922626956393 ) ) ;
#28874=CARTESIAN_POINT ( 'NONE',  ( 2.079038939659454854, 1.922984332675440777, 0.7462749415493277194 ) ) ;
#28877=AXIS2_PLACEMENT_3D ( 'NONE', #59612, #125768, #11921 ) ;
#28881=CARTESIAN_POINT ( 'NONE',  ( 5.419949545929089396, 1.307550890958172785, -1.758484179531449421 ) ) ;
#28882=CARTESIAN_POINT ( 'NONE',  ( 2.813125141109920069, 1.117832431973438734, -1.678005364621336426 ) ) ;
#28883=CARTESIAN_POINT ( 'NONE',  ( 2.436835438956724165, -1.365703447793526371, -1.235134912642745775 ) ) ;
#28886=CARTESIAN_POINT ( 'NONE',  ( 5.385714059857480862, 1.227405483141888132, 1.351559456777707835 ) ) ;
#28888=CARTESIAN_POINT ( 'NONE',  ( 6.065077313367789102, -1.076319894221990259, 1.704936797084610101 ) ) ;
#28890=CARTESIAN_POINT ( 'NONE',  ( 6.034080775264698993, 1.121385855563570288, -1.965008656891243044 ) ) ;
#28892=CARTESIAN_POINT ( 'NONE',  ( 0.4343773424168140274, 1.080651816385242547, -1.807535387385241776 ) ) ;
#28902=CARTESIAN_POINT ( 'NONE',  ( 1.600013431492643745, 1.466117565985028515, 1.532352819790145482 ) ) ;
#28903=CARTESIAN_POINT ( 'NONE',  ( 2.865722905416301369, -1.818493784693291815, -1.275605581943892730 ) ) ;
#28907=CARTESIAN_POINT ( 'NONE',  ( 3.877359892829432386, -0.1466975079335990917, 1.956454564409334296 ) ) ;
#28914=CARTESIAN_POINT ( 'NONE',  ( 3.498385214435925317, -1.041973313016024472, 1.846846941210858351 ) ) ;
#28916=CARTESIAN_POINT ( 'NONE',  ( 4.329101982860062314, 0.1031891237209987822, 2.159356164053369387 ) ) ;
#28917=CARTESIAN_POINT ( 'NONE',  ( 3.438839575862782549, -1.396446551253815782, -1.200180114512699792 ) ) ;
#28920=CARTESIAN_POINT ( 'NONE',  ( 5.261534320672216936, 0.8623632012556389226, 1.511560460804670880 ) ) ;
#28924=CARTESIAN_POINT ( 'NONE',  ( 3.538091169922503276, 0.9737216987566952309, -1.930062384640649054 ) ) ;
#28925=CARTESIAN_POINT ( 'NONE',  ( 6.186875009713125984, -1.117664052418202658, -1.677746505241828334 ) ) ;
#28927=CARTESIAN_POINT ( 'NONE',  ( 2.219795081190904629, -2.096929600374438429, 0.5247480557022954351 ) ) ;
#28929=CARTESIAN_POINT ( 'NONE',  ( 3.971915101536928283, 1.092440305464415840, 1.640793377567103528 ) ) ;
#28931=CARTESIAN_POINT ( 'NONE',  ( 4.704598389810739079, 1.691404259434112767, 0.9541841752371772456 ) ) ;
#28940=CARTESIAN_POINT ( 'NONE',  ( 2.749284697512776710, -1.835294401387000285, 1.225074929180599792 ) ) ;
#28942=CARTESIAN_POINT ( 'NONE',  ( 5.963715375765575644, -0.4800653121489819042, 1.901962685674676301 ) ) ;
#28946=CARTESIAN_POINT ( 'NONE',  ( 0.07479286986305544449, 2.046156589154801253, -2.272744413733415403 ) ) ;
#28947=CARTESIAN_POINT ( 'NONE',  ( 5.824118960990139371, 1.775556191179916699, 0.4867722729226392486 ) ) ;
#28952=CARTESIAN_POINT ( 'NONE',  ( 6.099870585610251084, 1.463495690422533579, 1.534846084132005961 ) ) ;
#28955=CARTESIAN_POINT ( 'NONE',  ( 6.555941810938458403, 2.055592219362284201, -0.1468124517445909549 ) ) ;
#28957=CARTESIAN_POINT ( 'NONE',  ( 1.750234856725553900, -1.851685525784763975, -0.1866200871585097509 ) ) ;
#28958=CARTESIAN_POINT ( 'NONE',  ( 3.843160323004328305, 0.6166970922517557296, -1.735048075492843456 ) ) ;
#28964=ORIENTED_EDGE ( 'NONE', *, *, #32928, .T. ) ;
#28966=CARTESIAN_POINT ( 'NONE',  ( 3.580891165198408110, -2.126768340858419926, -0.5889919780145411732 ) ) ;
#28967=CARTESIAN_POINT ( 'NONE',  ( 5.694667785318580755, -0.5416461603767928068, -2.196524604246933521 ) ) ;
#28969=CARTESIAN_POINT ( 'NONE',  ( 5.379120748016958053, -1.641329381114923658, -0.7670206631310432233 ) ) ;
#28970=CARTESIAN_POINT ( 'NONE',  ( 6.192599819808762618, 1.414433556397393543, -1.292206900294754490 ) ) ;
#28972=CARTESIAN_POINT ( 'NONE',  ( 5.998880656844745474, 1.528293836345222312, -1.078463600801618405 ) ) ;
#28973=CARTESIAN_POINT ( 'NONE',  ( 5.654919265238161685, 0.3773621422162172223, 1.874504418562010999 ) ) ;
#28975=CARTESIAN_POINT ( 'NONE',  ( 1.094370286708164386, -0.4508366001288487412, -1.815394955969009239 ) ) ;
#28977=CARTESIAN_POINT ( 'NONE',  ( 1.745327705122714956, 0.3399549603602426417, -1.987498286102694411 ) ) ;
#28979=CARTESIAN_POINT ( 'NONE',  ( 3.299542427861827498, 1.660325518240006071, 1.295591914420061830 ) ) ;
#28984=CARTESIAN_POINT ( 'NONE',  ( 2.724872815078176913, 1.459976238909798996, -1.395942890215768895 ) ) ;
#28987=CARTESIAN_POINT ( 'NONE',  ( 3.321700061091820366, -2.084211496276411779, 0.5730272365244913901 ) ) ;
#28993=CARTESIAN_POINT ( 'NONE',  ( 0.3269468692386565678, -1.417551234153333395, 1.644607001386617418 ) ) ;
#28997=CARTESIAN_POINT ( 'NONE',  ( 1.681448347407452193, 1.514353137444489406, 1.584415833815432162 ) ) ;
#28999=CARTESIAN_POINT ( 'NONE',  ( 3.010884265427976825, 1.639692042162781194, -1.559206548184206564 ) ) ;
#29006=CARTESIAN_POINT ( 'NONE',  ( 4.534285406439878763, 1.735348426437629765, 0.3461848140887160974 ) ) ;
#29009=CARTESIAN_POINT ( 'NONE',  ( 0.8156195060344322290, -0.3088407994138153700, 2.083069475825300110 ) ) ;
#29013=CARTESIAN_POINT ( 'NONE',  ( 5.027533431531807651, -0.2580777524966316738, 1.792966082415799800 ) ) ;
#29017=CARTESIAN_POINT ( 'NONE',  ( 3.221420234344949840, -1.803205065257794004, 0.4975683872451354683 ) ) ;
#29018=CARTESIAN_POINT ( 'NONE',  ( 3.256751887857904926, -0.5965066610371800859, -1.982489643792232137 ) ) ;
#29026=CARTESIAN_POINT ( 'NONE',  ( 6.819229411136438657, -0.1619093195798972928, 2.126376854085454404 ) ) ;
#29028=CARTESIAN_POINT ( 'NONE',  ( 2.418345249890076154, 0.8361516037145629854, 1.774881043358336630 ) ) ;
#29029=CARTESIAN_POINT ( 'NONE',  ( 1.405624810022429338, 0.3905361843517704545, 1.977748161624799161 ) ) ;
#29034=CARTESIAN_POINT ( 'NONE',  ( 1.422894040683621464, -0.05142188859055819850, 1.870020055627517497 ) ) ;
#29036=CARTESIAN_POINT ( 'NONE',  ( 3.304942742240731590, -0.3968801077466362903, -1.973537420673168397 ) ) ;
#29038=CARTESIAN_POINT ( 'NONE',  ( 2.671616206378808478, 1.499349897650571695, 1.495110359788552223 ) ) ;
#29040=CARTESIAN_POINT ( 'NONE',  ( 3.543477799061961253, 1.872898848466747479, -0.8826743078152868849 ) ) ;
#29042=CARTESIAN_POINT ( 'NONE',  ( 6.421832395068366672, 1.204883778905677216, -1.708312069947721668 ) ) ;
#29044=CARTESIAN_POINT ( 'NONE',  ( 5.315394819225006451, -0.2661953434012730435, 1.805952802178517613 ) ) ;
#29051=CARTESIAN_POINT ( 'NONE',  ( 5.584596538761583240, -1.209766832763665034, 1.480987728393488245 ) ) ;
#29057=ORIENTED_EDGE ( 'NONE', *, *, #178523, .F. ) ;
#29059=CARTESIAN_POINT ( 'NONE',  ( 4.903500725120335524, -0.5004011548357701900, 1.802273645872286334 ) ) ;
#29060=CARTESIAN_POINT ( 'NONE',  ( -0.02319159430949970999, 2.891346550825595774, -2.299931007135449512 ) ) ;
#29066=CARTESIAN_POINT ( 'NONE',  ( 1.041781249306489965, 1.318715992218882693, 1.462978117936466926 ) ) ;
#29067=CARTESIAN_POINT ( 'NONE',  ( 3.110954007106698338, 0.05231540665236523308, 2.015913653835194719 ) ) ;
#29070=CARTESIAN_POINT ( 'NONE',  ( 6.727182134110203826, 2.399899341769623273, 2.668786705202597531 ) ) ;
#29071=CARTESIAN_POINT ( 'NONE',  ( 3.433693710695666201, 0.9853049363134911420, -1.957518807868402044 ) ) ;
#29073=CARTESIAN_POINT ( 'NONE',  ( 2.432535651424679646, 1.868085840533942221, 0.4698736581597633966 ) ) ;
#29076=CARTESIAN_POINT ( 'NONE',  ( 0.1331565106231571705, 4.092041177288479048, -2.500854978060399691 ) ) ;
#29084=CARTESIAN_POINT ( 'NONE',  ( 4.581507094455529838, -0.8636776874328588871, 1.626104626046148249 ) ) ;
#29085=CARTESIAN_POINT ( 'NONE',  ( 2.174478567003877316, 0.8628565524405201748, 1.818940509527650295 ) ) ;
#29086=CARTESIAN_POINT ( 'NONE',  ( 4.464446571738351466, 1.842799458866357210, 1.373389552433499139 ) ) ;
#29087=CARTESIAN_POINT ( 'NONE',  ( -0.02900071798685524560, 2.860900941590225344, -2.661937258840251008 ) ) ;
#29088=CARTESIAN_POINT ( 'NONE',  ( 2.025991663365491746, 0.9512761431412205537, 1.599265494891942030 ) ) ;
#29091=CARTESIAN_POINT ( 'NONE',  ( 5.677967274442059953, 1.882970570262190835, -0.3333453579756898155 ) ) ;
#29094=CARTESIAN_POINT ( 'NONE',  ( 5.337476071801405375, 0.8461711052811745626, -1.912038999733718825 ) ) ;
#29095=CARTESIAN_POINT ( 'NONE',  ( 3.028041890241763401, 1.040506211802554981, -1.554362669439563360 ) ) ;
#29099=CARTESIAN_POINT ( 'NONE',  ( 5.514166437991733005, -0.7808720426115691726, -1.538077146617151669 ) ) ;
#29101=CARTESIAN_POINT ( 'NONE',  ( 0.9317525018172129192, -1.365947654462830618, -1.068275208499162909 ) ) ;
#29105=CARTESIAN_POINT ( 'NONE',  ( 6.034065736706932803, 1.286768452391522377, 1.748546487445822750 ) ) ;
#29106=CARTESIAN_POINT ( 'NONE',  ( 3.914527900857078357, 1.289819402409349669, -1.292354223553587644 ) ) ;
#29107=CARTESIAN_POINT ( 'NONE',  ( 2.764445781119912127, -0.7462812867886668977, -1.814464804917370166 ) ) ;
#29108=CARTESIAN_POINT ( 'NONE',  ( 6.315624676198635434, -1.384492656466195681, -1.602007840318976584 ) ) ;
#29112=CARTESIAN_POINT ( 'NONE',  ( 2.614065066921432479, -0.6628553294307990562, 2.014303955012682223 ) ) ;
#29116=CARTESIAN_POINT ( 'NONE',  ( 0.9013344411078340057, -1.777497804657724334, 1.061070337243313455 ) ) ;
#29118=CARTESIAN_POINT ( 'NONE',  ( 2.473529351063200377, -1.934054200746947227, -1.092377531094531173 ) ) ;
#29119=EDGE_LOOP ( 'NONE', ( #171994, #88858 ) ) ;
#29120=CARTESIAN_POINT ( 'NONE',  ( 0.2824055751470951892, 1.906470811695348599, -1.284064767653005257 ) ) ;
#29122=CARTESIAN_POINT ( 'NONE',  ( 5.893442400364165223, -1.866981718288396763, 0.8769185494091299438 ) ) ;
#29127=CARTESIAN_POINT ( 'NONE',  ( 5.038538826285253514, -1.576363729006284187, 0.9512496309353533075 ) ) ;
#29129=CARTESIAN_POINT ( 'NONE',  ( -0.2104748580754409182, 6.947232144882289795, -2.698723162346649662 ) ) ;
#29130=CARTESIAN_POINT ( 'NONE',  ( 3.240908261985251837, -1.521742930289736728, 0.8118271961824756744 ) ) ;
#29131=CARTESIAN_POINT ( 'NONE',  ( 0.7433754753295095385, 0.3886281223182270761, -1.978556061772406505 ) ) ;
#29133=CARTESIAN_POINT ( 'NONE',  ( 2.442968603456824095, 0.4936193734879111283, 2.207763252559187261 ) ) ;
#29134=CARTESIAN_POINT ( 'NONE',  ( 3.686240278715931851, -1.037925599752804739, 1.832463683143903399 ) ) ;
#29136=CARTESIAN_POINT ( 'NONE',  ( 3.989309445023786704, 1.280397443517577782, 1.221928027103141634 ) ) ;
#29140=CARTESIAN_POINT ( 'NONE',  ( 0.1645876019286318381, -1.492192613954560265, 1.740154187221523818 ) ) ;
#29141=CARTESIAN_POINT ( 'NONE',  ( 4.523293815724619193, -1.134750198001058585, -1.449786353205910538 ) ) ;
#29145=CARTESIAN_POINT ( 'NONE',  ( 4.242245924764226572, 0.5834501570099770440, 2.112278566661344392 ) ) ;
#29150=CARTESIAN_POINT ( 'NONE',  ( 3.053258290938072772, -1.575281680543440643, -1.108752609043755832 ) ) ;
#29153=CARTESIAN_POINT ( 'NONE',  ( 0.1588220795745398928, 2.216043539545629937, 0.1551192601621682043 ) ) ;
#29161=CARTESIAN_POINT ( 'NONE',  ( 2.682838027602444164, 1.232319236757819292, 1.229298679657732762 ) ) ;
#29166=CARTESIAN_POINT ( 'NONE',  ( 5.858325616802108726, 0.8718737102157668728, 1.978260574764856283 ) ) ;
#29171=CARTESIAN_POINT ( 'NONE',  ( 5.787991602622606813, -0.9759734195362681497, 1.928925553883020338 ) ) ;
#29172=CARTESIAN_POINT ( 'NONE',  ( -0.2106725631050020975, 7.629137130509112907, -2.603678913577145426 ) ) ;
#29175=CARTESIAN_POINT ( 'NONE',  ( 6.749300054864300513, -1.582014061365591751, -1.175997427595596445 ) ) ;
#29176=CARTESIAN_POINT ( 'NONE',  ( 6.608738931450677256, 0.6592670866186548517, -1.603827835538347291 ) ) ;
#29179=CARTESIAN_POINT ( 'NONE',  ( 3.597391730528697540, -0.6346259394694170330, 2.097678010650514402 ) ) ;
#29180=CARTESIAN_POINT ( 'NONE',  ( 3.382123439733915493, 1.462175888237092547, 1.785228103979496384 ) ) ;
#29181=CARTESIAN_POINT ( 'NONE',  ( 5.870404149471736943, -1.310866377807779593, 1.590078559457400287 ) ) ;
#29182=CARTESIAN_POINT ( 'NONE',  ( 0.7088029311262042942, -0.2857661853880436031, 1.920690660100693226 ) ) ;
#29186=CARTESIAN_POINT ( 'NONE',  ( 4.500305224345508393, -0.9970752094022590217, 1.871535012320741265 ) ) ;
#29188=CARTESIAN_POINT ( 'NONE',  ( 2.883435573726996548, -0.5880205015329244000, -1.928751729079546173 ) ) ;
#29190=CARTESIAN_POINT ( 'NONE',  ( 5.403435775159438847, 1.801252639416499379, 1.274624607731331905 ) ) ;
#29191=CARTESIAN_POINT ( 'NONE',  ( 6.750000000000007994, 7.629137130509070275, 2.600000000000001421 ) ) ;
#29200=CARTESIAN_POINT ( 'NONE',  ( 4.170816135027268778, -1.922254079802641069, -0.7435701193346122562 ) ) ;
#29205=CARTESIAN_POINT ( 'NONE',  ( 3.879560801468981523, 0.2449043481074340001, -2.004685163654993385 ) ) ;
#29210=CARTESIAN_POINT ( 'NONE',  ( 3.573166805712838734, 0.05218571934602388163, -2.060405206736420247 ) ) ;
#29211=CARTESIAN_POINT ( 'NONE',  ( 2.725232599228684993, 2.001511357256777313, 0.2440295182731533341 ) ) ;
#29217=CARTESIAN_POINT ( 'NONE',  ( 3.198592129611950607, -1.351947076146834403, -1.495823048609262518 ) ) ;
#29218=CARTESIAN_POINT ( 'NONE',  ( 2.624749632297512569, -1.717891791495285592, 0.6627527109525217508 ) ) ;
#29219=CARTESIAN_POINT ( 'NONE',  ( 0.3116875490984937214, 2.011018277352360606, 1.131832386414432179 ) ) ;
#29221=CARTESIAN_POINT ( 'NONE',  ( 2.935029080331118756, 0.2613785356864756770, 2.145644965459513109 ) ) ;
#29223=CARTESIAN_POINT ( 'NONE',  ( 4.874263506423556436, -2.101702868649154343, -0.2561063476108938475 ) ) ;
#29226=CARTESIAN_POINT ( 'NONE',  ( 1.621729638615863944, -1.036547396872866678, -1.557007864774778705 ) ) ;
#29227=CARTESIAN_POINT ( 'NONE',  ( 6.174684870424203886, -1.871919000353940099, -0.6187097519457245287 ) ) ;
#29232=CARTESIAN_POINT ( 'NONE',  ( 0.1533209562146371774, -1.769702838771534559, 1.318327933512997152 ) ) ;
#29233=CARTESIAN_POINT ( 'NONE',  ( 6.004363041306050697, 2.067815565686380364, 0.1054426792976848049 ) ) ;
#29236=CARTESIAN_POINT ( 'NONE',  ( 6.639320575229256782, 4.691717626494606996, 2.665852771288126366 ) ) ;
#29237=CARTESIAN_POINT ( 'NONE',  ( 5.119980909927547508, -1.054019455064346689, -1.665871061098343819 ) ) ;
#29238=CARTESIAN_POINT ( 'NONE',  ( -0.08743476694611679312, -2.120266877281291595, -0.04547849331201780226 ) ) ;
#29240=CARTESIAN_POINT ( 'NONE',  ( 4.459805605305016130, 0.5082999457236726526, -2.250878628046268037 ) ) ;
#29242=CARTESIAN_POINT ( 'NONE',  ( 2.360284975695529752, -2.062195451902974597, 0.04632573159841534699 ) ) ;
#29249=CARTESIAN_POINT ( 'NONE',  ( 4.422458135217792297, 1.019899284492602698, 1.916704820016806199 ) ) ;
#29251=CARTESIAN_POINT ( 'NONE',  ( 3.755264181858387840, 1.826884192416846631, -0.2291247506851084581 ) ) ;
#29252=DIRECTION ( 'NONE',  ( 2.949029909160572061E-17, 1.000000000000000000, -8.673600428462391266E-15 ) ) ;
#29253=CARTESIAN_POINT ( 'NONE',  ( 6.720655732516669367, 7.629137130509068498, 2.426260288887295058 ) ) ;
#29254=CARTESIAN_POINT ( 'NONE',  ( 5.618738332679400038, -0.05485954975367920983, 2.191026952110195491 ) ) ;
#29256=CARTESIAN_POINT ( 'NONE',  ( 6.403223674518304875, 1.876769595090790554, 1.263360297164903168 ) ) ;
#29262=CARTESIAN_POINT ( 'NONE',  ( 0.8129392405988710157, -0.2653805273100506290, 1.749707594005883937 ) ) ;
#29263=CARTESIAN_POINT ( 'NONE',  ( 5.672526239869847053, 0.8180066501249063649, 1.839585422649665958 ) ) ;
#29265=CARTESIAN_POINT ( 'NONE',  ( 4.260836881943074417, -1.562014524604074861, 1.412707936923715879 ) ) ;
#29266=CARTESIAN_POINT ( 'NONE',  ( 2.161615495643732565, 1.180369796089770995, 1.508615382416353290 ) ) ;
#29268=CARTESIAN_POINT ( 'NONE',  ( 2.752355523121536862, -1.964097686037095336, -0.1475717908260633926 ) ) ;
#29269=CARTESIAN_POINT ( 'NONE',  ( 5.027605771429075610, -0.2921156310390393140, 1.998402611621821423 ) ) ;
#29270=CARTESIAN_POINT ( 'NONE',  ( 1.305301652190330675, -0.4579020413679709689, 1.813615928118620380 ) ) ;
#29271=CARTESIAN_POINT ( 'NONE',  ( 5.180183349501196410, -0.9537450585986576579, 1.436990496349071833 ) ) ;
#29272=CARTESIAN_POINT ( 'NONE',  ( 1.318461241437279607, -0.6911404020932455650, -1.783297644634279200 ) ) ;
#29274=CARTESIAN_POINT ( 'NONE',  ( 1.260703874955213744, 0.8971468365699288849, 2.016480257658866737 ) ) ;
#29282=CARTESIAN_POINT ( 'NONE',  ( 1.188034388246852480, -1.312013912954514971, -1.601590607232979524 ) ) ;
#29287=CARTESIAN_POINT ( 'NONE',  ( 5.250683377293950294, 2.089169806880130320, 0.3621421040747307973 ) ) ;
#29292=CARTESIAN_POINT ( 'NONE',  ( 6.812952578306354035, -1.517200236233799071, 1.243500037895750143 ) ) ;
#29294=CARTESIAN_POINT ( 'NONE',  ( 4.182970119252515495, -1.034007530860373336, -1.730600854597413418 ) ) ;
#29295=CARTESIAN_POINT ( 'NONE',  ( 4.698395719694191897, 1.316562313306284038, -1.391896452211606849 ) ) ;
#29296=CARTESIAN_POINT ( 'NONE',  ( 2.700927432832851860, 1.852951201923001223, 1.169960570980829839 ) ) ;
#29299=CARTESIAN_POINT ( 'NONE',  ( 4.886981372429439752, -1.897129443012405936, -0.6741400253723847102 ) ) ;
#29302=CARTESIAN_POINT ( 'NONE',  ( 5.360994948850416719, -0.05292929278505505153, -2.116735950649220932 ) ) ;
#29304=CARTESIAN_POINT ( 'NONE',  ( 3.280887763456251882, 1.889169395226503401, -0.8960188238960642426 ) ) ;
#29306=CARTESIAN_POINT ( 'NONE',  ( 1.412684849630441386, 1.518645404226389051, 0.8176530575639671117 ) ) ;
#29308=CARTESIAN_POINT ( 'NONE',  ( 5.361630242575341931, -1.673063676233761621, -1.302930760576012092 ) ) ;
#29317=CARTESIAN_POINT ( 'NONE',  ( 1.506221797076849889, -1.802732806890252837, -0.1774259793663693907 ) ) ;
#29323=CARTESIAN_POINT ( 'NONE',  ( 2.525776224529495906, -1.791516492901791713, 0.2672755921442840354 ) ) ;
#29324=CARTESIAN_POINT ( 'NONE',  ( 6.639320575229253230, 6.038193673056963640, 2.491643636677738360 ) ) ;
#29328=CARTESIAN_POINT ( 'NONE',  ( 4.422197255734514165, 0.8761312318771010688, 1.641894029917531084 ) ) ;
#29329=CARTESIAN_POINT ( 'NONE',  ( 1.950665421479770067, -1.752291233380006474, -0.7743663792006536539 ) ) ;
#29330=CARTESIAN_POINT ( 'NONE',  ( 6.141620278036529434, -1.395723430145169752, -1.327979989909616521 ) ) ;
#29339=CARTESIAN_POINT ( 'NONE',  ( 5.787944378201490103, -1.246615054290018065, -1.524717904608218877 ) ) ;
#29342=CARTESIAN_POINT ( 'NONE',  ( 0.1290073198303761104, -1.910558061381230521, 0.8492679875119947264 ) ) ;
#29344=CARTESIAN_POINT ( 'NONE',  ( 5.719733624436385000, -1.879402930333987198, 0.4222299131634628111 ) ) ;
#29346=CARTESIAN_POINT ( 'NONE',  ( 0.7623938366894518204, -1.325735992016435105, 1.255310662410371592 ) ) ;
#29347=CARTESIAN_POINT ( 'NONE',  ( 1.823171247573553311, 2.059948494222668458, 0.7922594597074559264 ) ) ;
#29349=CARTESIAN_POINT ( 'NONE',  ( 0.03522015555855115276, -0.09184495783944729430, 1.910282976853895587 ) ) ;
#29350=VERTEX_POINT ( 'NONE', #51984 ) ;
#29352=CARTESIAN_POINT ( 'NONE',  ( 0.2737963954951051493, -1.932246063674218473, 0.3805649573235761474 ) ) ;
#29353=CARTESIAN_POINT ( 'NONE',  ( 1.276788482218065734, 1.793752796627584578, -0.7448022267775021854 ) ) ;
#29355=CARTESIAN_POINT ( 'NONE',  ( 0.5794536021234627521, 1.392335491182377316, -1.458330535474762213 ) ) ;
#29357=CARTESIAN_POINT ( 'NONE',  ( 5.102340918953698790, 1.855823733615385551, 0.1392438295388219172 ) ) ;
#29360=CARTESIAN_POINT ( 'NONE',  ( 6.509000000000037645, 2.054060622569788386, 2.307050226316338382 ) ) ;
#29363=CARTESIAN_POINT ( 'NONE',  ( 1.945129482973105839, -1.762486321751283835, -1.302348873264857820 ) ) ;
#29367=CARTESIAN_POINT ( 'NONE',  ( 3.088313589057069208, -1.798746773638896457, -0.3115406389907551810 ) ) ;
#29374=CARTESIAN_POINT ( 'NONE',  ( 1.084454569787800304, -1.879374161238209773, -0.4228483607967240543 ) ) ;
#29375=CARTESIAN_POINT ( 'NONE',  ( 5.787936641206399280, -1.241742415844361291, -1.518776266119965745 ) ) ;
#29378=CARTESIAN_POINT ( 'NONE',  ( 5.196902890030515643, 1.791362914573800369, 1.262263373074036688 ) ) ;
#29381=CARTESIAN_POINT ( 'NONE',  ( 3.924723049676182018, -1.394041313093749457, 1.530695986988837021 ) ) ;
#29386=CARTESIAN_POINT ( 'NONE',  ( 4.324990310505356206, 0.9834070133523404866, -2.077815080336536280 ) ) ;
#29393=CARTESIAN_POINT ( 'NONE',  ( 3.644416830925560014, -1.587075459539259992, 1.118831915631451013 ) ) ;
#29398=CARTESIAN_POINT ( 'NONE',  ( 4.763870730211980487, 0.5944114921396548290, -1.817767169311027997 ) ) ;
#29400=CARTESIAN_POINT ( 'NONE',  ( 6.352575194690796678, 0.5466354793271388512, 1.635951794362877187 ) ) ;
#29401=CARTESIAN_POINT ( 'NONE',  ( 4.241422899474024177, 0.4370803545316758743, -1.968444674787086734 ) ) ;
#29403=CARTESIAN_POINT ( 'NONE',  ( 2.385638622766753425, 2.017150886971270651, -0.8956362484653990208 ) ) ;
#29406=CARTESIAN_POINT ( 'NONE',  ( 1.816468492311611893, 1.951142502984483107, 0.7513475392508098816 ) ) ;
#29407=CARTESIAN_POINT ( 'NONE',  ( 6.626229037604012717, 1.016508351997437165, -1.448449474740549858 ) ) ;
#29408=CARTESIAN_POINT ( 'NONE',  ( 5.977185442992979603, -2.006959616289708315, -0.1948445219252663840 ) ) ;
#29411=CARTESIAN_POINT ( 'NONE',  ( 2.730776445121200435, 0.2818232878892740212, 2.274813446668845884 ) ) ;
#29412=CARTESIAN_POINT ( 'NONE',  ( 1.095196197045473774, -1.740516465796032586, -0.003461242977918776564 ) ) ;
#29414=CARTESIAN_POINT ( 'NONE',  ( 1.211752002169782738, -1.362220228754877027, -1.072495211514002289 ) ) ;
#29417=CARTESIAN_POINT ( 'NONE',  ( 1.768284035615394600, -2.154879749829127444, 0.2648707735025003229 ) ) ;
#29418=CARTESIAN_POINT ( 'NONE',  ( 1.868375392651611122, -1.978555653031977446, -0.3886301775877995524 ) ) ;
#29419=CARTESIAN_POINT ( 'NONE',  ( 4.687500000000003553, -1.451031289060926488, 1.451031289061301521 ) ) ;
#29421=CARTESIAN_POINT ( 'NONE',  ( 0.08292192553204823235, -0.1316706149618769306, -1.895886810074402185 ) ) ;
#29423=CARTESIAN_POINT ( 'NONE',  ( 3.744553100839841608, 1.186064971860462114, -1.878093021827110354 ) ) ;
#29429=CARTESIAN_POINT ( 'NONE',  ( 5.513164599239865460, -1.696177307367072506, 0.3892859123911066588 ) ) ;
#29430=CARTESIAN_POINT ( 'NONE',  ( 4.105873170248697690, 0.6631157982108953908, -1.846516426336957784 ) ) ;
#29434=CARTESIAN_POINT ( 'NONE',  ( 4.306154650063803935, -2.256721687276264099, 0.1609511959119753199 ) ) ;
#29435=CARTESIAN_POINT ( 'NONE',  ( 2.119651477787509730, 0.3549358516394903740, -2.031769927719127455 ) ) ;
#29438=CARTESIAN_POINT ( 'NONE',  ( 2.817521562391828827, -0.2228243041610066255, 2.251526839675880520 ) ) ;
#29441=CARTESIAN_POINT ( 'NONE',  ( 3.497188413392815498, 1.472618687456558773, 1.153256759092120554 ) ) ;
#29442=CARTESIAN_POINT ( 'NONE',  ( 2.408496482339622879, -0.9999731500247920346, -1.416544738438466400 ) ) ;
#29443=CARTESIAN_POINT ( 'NONE',  ( 6.040607902356621928, -1.852314659301615096, 1.170993205287726990 ) ) ;
#29444=CARTESIAN_POINT ( 'NONE',  ( 6.827182134110238110, -0.009824402486291110986, 2.288967694407697984 ) ) ;
#29445=CARTESIAN_POINT ( 'NONE',  ( 3.485389320157119997, 1.955090977548096687, -0.9225387301767663528 ) ) ;
#29446=CARTESIAN_POINT ( 'NONE',  ( 4.910071578948462800, 1.337895470842176193, -1.407775065355970412 ) ) ;
#29448=CARTESIAN_POINT ( 'NONE',  ( 6.432864026670258362, 0.1834693771665257822, 1.861492386831371748 ) ) ;
#29453=CARTESIAN_POINT ( 'NONE',  ( 5.274064633610318076, 1.777012466945230962, -0.9530095070046653571 ) ) ;
#29457=CARTESIAN_POINT ( 'NONE',  ( 3.158640206316553289, -1.382037546686708973, 1.193037399656725395 ) ) ;
#29458=CARTESIAN_POINT ( 'NONE',  ( 2.116530880626496192, -1.040147864624408003, -1.946245422063937802 ) ) ;
#29463=CARTESIAN_POINT ( 'NONE',  ( 1.230729765704338563, 1.353420925896263061, -1.499466043412321703 ) ) ;
#29464=CARTESIAN_POINT ( 'NONE',  ( 1.313308151137903224, 1.731519532738003297, -1.223779428986125462 ) ) ;
#29466=CARTESIAN_POINT ( 'NONE',  ( 2.113880859634624354, 1.856391821545114951, -0.1307286092924550835 ) ) ;
#29468=CARTESIAN_POINT ( 'NONE',  ( 6.578986920187222864, -0.09832028258810160404, -2.058664976587327722 ) ) ;
#29469=CARTESIAN_POINT ( 'NONE',  ( 6.047500043413473136, -1.423963828944514010, 1.427935028000301809 ) ) ;
#29474=CARTESIAN_POINT ( 'NONE',  ( 4.424309136736732206, 1.121156565774838354, -1.440799707636587712 ) ) ;
#29478=CARTESIAN_POINT ( 'NONE',  ( 6.520861224751243412, 2.010896128390584625, -0.1455136175190149816 ) ) ;
#29479=CARTESIAN_POINT ( 'NONE',  ( 6.333933918656591722, 1.821832875601756774, 0.2651207078676054429 ) ) ;
#29481=CARTESIAN_POINT ( 'NONE',  ( 4.248838534556359292, 0.6131519058680062750, 2.224680453567278171 ) ) ;
#29483=CARTESIAN_POINT ( 'NONE',  ( 6.063787883973515314, 2.130759124531961923, -0.3628933549372145295 ) ) ;
#29484=CARTESIAN_POINT ( 'NONE',  ( 0.8724827243445825165, -0.04916951280507049493, -1.941606035699546151 ) ) ;
#29486=CARTESIAN_POINT ( 'NONE',  ( 4.481968937923656249, 2.098976780363570604, 0.9367997793626892111 ) ) ;
#29490=CARTESIAN_POINT ( 'NONE',  ( 4.996879044411707937, 1.554903924810165705, -1.039696167511289238 ) ) ;
#29492=CARTESIAN_POINT ( 'NONE',  ( 1.916128293556786044, -1.911906470838855343, 0.05044092668918254141 ) ) ;
#29495=CARTESIAN_POINT ( 'NONE',  ( 4.283934280384479543, 1.440456688004333019, 1.672026782002330458 ) ) ;
#29496=CARTESIAN_POINT ( 'NONE',  ( 6.883263157960401557, 3.701933627517115966, 2.360572570571787043 ) ) ;
#29501=CARTESIAN_POINT ( 'NONE',  ( 1.141796867408477967, 0.8028701493673767731, -1.800646566474963572 ) ) ;
#29502=CARTESIAN_POINT ( 'NONE',  ( 0.9390046912478089425, 2.274041295854188238, 0.3912414073941206105 ) ) ;
#29503=CARTESIAN_POINT ( 'NONE',  ( 2.207404936347991065, -1.573848641742966459, -1.171066219227391070 ) ) ;
#29505=CARTESIAN_POINT ( 'NONE',  ( 5.805554948619430000, -1.622591123950654746, -1.273203187973567241 ) ) ;
#29512=CARTESIAN_POINT ( 'NONE',  ( 0.6730172731169652423, 1.498246551899045098, -1.571433807820749706 ) ) ;
#29516=CARTESIAN_POINT ( 'NONE',  ( 2.512791842090915218, 1.668957736969980621, 0.8448945032545759348 ) ) ;
#29517=CARTESIAN_POINT ( 'NONE',  ( 0.3685255395303523307, -1.348100972195030334, 1.558720748697209224 ) ) ;
#29518=CARTESIAN_POINT ( 'NONE',  ( -0.02224634325200240681, 0.6689394325187210111, -2.369055395299427769 ) ) ;
#29519=CARTESIAN_POINT ( 'NONE',  ( 6.827182134110203471, 2.976138737189625516, 2.364467684523130497 ) ) ;
#29521=CARTESIAN_POINT ( 'NONE',  ( 2.789602095257078584, 1.815147277589121533, -0.6018686165152677958 ) ) ;
#29522=CARTESIAN_POINT ( 'NONE',  ( 4.065142161210800076, 0.2162087174472343276, -1.756520380257739822 ) ) ;
#29524=CARTESIAN_POINT ( 'NONE',  ( 2.209489775926488431, 1.479274643242427301, 1.211860329591994745 ) ) ;
#29527=CARTESIAN_POINT ( 'NONE',  ( 5.290618452874795707, 1.447395081947447704, -1.254909122497225971 ) ) ;
#29529=CARTESIAN_POINT ( 'NONE',  ( 6.514111218838506190, 1.964378047669375293, -0.1432920118879192073 ) ) ;
#29532=CARTESIAN_POINT ( 'NONE',  ( 4.944154083221365070, 1.865701114312174225, 0.1370711555178441010 ) ) ;
#29533=CARTESIAN_POINT ( 'NONE',  ( 1.435882461153328515, 0.9014729512111450127, -1.587519582607027635 ) ) ;
#29535=CARTESIAN_POINT ( 'NONE',  ( 4.934293700819583073, 1.136511309699510308, -1.891595316245115788 ) ) ;
#29539=CARTESIAN_POINT ( 'NONE',  ( 1.750508186522087062, -2.052535545683041196, -0.2044793282457678107 ) ) ;
#29546=CARTESIAN_POINT ( 'NONE',  ( 4.984861949208964305, 1.980195279717174905, 0.6042863919064264122 ) ) ;
#29548=CARTESIAN_POINT ( 'NONE',  ( 2.144033130777025065, 0.8294244109963678779, -1.996327601563187670 ) ) ;
#29550=CARTESIAN_POINT ( 'NONE',  ( 2.912765130361310018, -0.5885411476599323732, -1.932001019476004888 ) ) ;
#29551=CARTESIAN_POINT ( 'NONE',  ( 6.720655732516624070, 2.949086357957014570, 2.625980845328681923 ) ) ;
#29553=AXIS2_PLACEMENT_3D ( 'NONE', #122154, #24547, #23481 ) ;
#29558=CARTESIAN_POINT ( 'NONE',  ( 1.323454262349360144, -1.463929862531298198, -1.387097294446784090 ) ) ;
#29559=CARTESIAN_POINT ( 'NONE',  ( 6.058177568126345669, -1.550975213528119623, 1.548612826651605712 ) ) ;
#29561=CARTESIAN_POINT ( 'NONE',  ( 4.834190613173367623, -1.027981871586785889, -1.612434056610718480 ) ) ;
#29565=CARTESIAN_POINT ( 'NONE',  ( 2.003530013310977242, -1.955168117277843898, 0.4926643476272293820 ) ) ;
#29568=CARTESIAN_POINT ( 'NONE',  ( 5.543893992536840010, 0.6953672157433439249, -1.578584939873737047 ) ) ;
#29575=CARTESIAN_POINT ( 'NONE',  ( 1.393514648303464387, -1.873246724434135313, 0.8816542684770899418 ) ) ;
#29577=CARTESIAN_POINT ( 'NONE',  ( 4.688045340743730804, 1.047092163662701525, 1.477968688824328858 ) ) ;
#29581=CARTESIAN_POINT ( 'NONE',  ( 6.393201686769759640, -0.09647555762395694512, -1.809044896826275783 ) ) ;
#29584=CARTESIAN_POINT ( 'NONE',  ( 3.451304434523004172, 0.5324976444292061073, -2.125649318046138880 ) ) ;
#29586=CARTESIAN_POINT ( 'NONE',  ( 0.7659737006216191801, -1.952758744216346765, 0.1886366088557633325 ) ) ;
#29589=CARTESIAN_POINT ( 'NONE',  ( 5.009359837557266992, -1.817519814519794830, 0.6052834035694378834 ) ) ;
#29591=ADVANCED_FACE ( 'NONE', ( #172128 ), #67560, .F. ) ;
#29597=CARTESIAN_POINT ( 'NONE',  ( 2.377987466095924152, 1.329388817951412394, 1.704534938537699995 ) ) ;
#29600=CARTESIAN_POINT ( 'NONE',  ( 1.465546361252961560, 1.799214786004127209, -0.3081908958329632742 ) ) ;
#29602=CARTESIAN_POINT ( 'NONE',  ( 4.278209411971904075, -1.050932907216840295, 1.492538610026641344 ) ) ;
#29605=CARTESIAN_POINT ( 'NONE',  ( 4.369560876907440772, -0.3388413995694672387, 1.940020671193002810 ) ) ;
#29607=CARTESIAN_POINT ( 'NONE',  ( 6.480031042553710208, -1.905489079494159910, -0.3742900760800580984 ) ) ;
#29612=CARTESIAN_POINT ( 'NONE',  ( 5.168275554957600271, 2.118074532352266282, -0.1063875075708180934 ) ) ;
#29620=CARTESIAN_POINT ( 'NONE',  ( 5.654944829759325664, 0.3949471196958070918, 1.973809479704929704 ) ) ;
#29623=CARTESIAN_POINT ( 'NONE',  ( 6.287720257080702702, 1.262826302610157381, 1.318732360701305062 ) ) ;
#29624=CARTESIAN_POINT ( 'NONE',  ( 1.117730493923989599, 0.4056601665377961852, -2.030061024271647252 ) ) ;
#29630=PRESENTATION_STYLE_ASSIGNMENT (( #144482 ) ) ;
#29636=CARTESIAN_POINT ( 'NONE',  ( 3.603937110245566178, -0.1228517400825197836, 1.729840182746833266 ) ) ;
#29638=CARTESIAN_POINT ( 'NONE',  ( 1.551716534671506498, 1.565040117424065347, 1.355267069636761912 ) ) ;
#29639=CARTESIAN_POINT ( 'NONE',  ( 2.232168359954420200, 2.116822148135434567, 0.04868514642705767947 ) ) ;
#29644=CARTESIAN_POINT ( 'NONE',  ( 0.8659821450925162534, -1.960479642884611629, 0.1873741036552133976 ) ) ;
#29649=CARTESIAN_POINT ( 'NONE',  ( 2.625266749315146253, -2.138330473123546405, 0.8262727722977771805 ) ) ;
#29650=CARTESIAN_POINT ( 'NONE',  ( 0.5217476098421744979, -0.9739702522407606144, -1.544006022310390192 ) ) ;
#29651=CARTESIAN_POINT ( 'NONE',  ( 3.550944491985886575, 0.2853618425060593378, 1.890879049853078087 ) ) ;
#29654=CARTESIAN_POINT ( 'NONE',  ( 1.951433385020440836, -1.796364150513751312, 0.9090842167202308755 ) ) ;
#29655=CARTESIAN_POINT ( 'NONE',  ( 2.149198318390078910, 1.709348667602617722, -0.9624241554767107854 ) ) ;
#29659=CARTESIAN_POINT ( 'NONE',  ( 5.173812367756161379, -1.161941297927127525, 1.737786252440294055 ) ) ;
#29660=CARTESIAN_POINT ( 'NONE',  ( 3.678344558940789266, -1.705506331563589661, -0.4725282708486245875 ) ) ;
#29664=CARTESIAN_POINT ( 'NONE',  ( 6.580031643469963498, -2.246689805010111396, -0.4540597329640746471 ) ) ;
#29665=CARTESIAN_POINT ( 'NONE',  ( 4.118918040174416539, -1.664481161445837687, 0.5081549729096886958 ) ) ;
#29667=CARTESIAN_POINT ( 'NONE',  ( -0.1104750535120268828, 2.006893987364383403, -2.517811492722863864 ) ) ;
#29668=CARTESIAN_POINT ( 'NONE',  ( 4.130049176863603400, 0.2125952495928511154, -1.720681531008328768 ) ) ;
#29669=CARTESIAN_POINT ( 'NONE',  ( 5.213404077426219807, -1.831445439253748031, -1.165863444158367290 ) ) ;
#29671=CARTESIAN_POINT ( 'NONE',  ( 5.507046092540283766, -0.04465857163906890998, 2.016188657829049991 ) ) ;
#29672=CARTESIAN_POINT ( 'NONE',  ( 5.343750000000003553, 1.895863743164196258, 0.7852924748297027691 ) ) ;
#29674=CARTESIAN_POINT ( 'NONE',  ( 2.748949809783503451, -1.602600522849004339, 1.068665135549841771 ) ) ;
#29676=CARTESIAN_POINT ( 'NONE',  ( 6.345936316318473658, -1.449877878406122145, -1.683046035897132420 ) ) ;
#29678=CARTESIAN_POINT ( 'NONE',  ( 6.883263157960405998, 2.961743250487959056, 2.498998094365055600 ) ) ;
#29681=CARTESIAN_POINT ( 'NONE',  ( 2.596574818557799258, -1.139633321999042659, 1.906535983277869661 ) ) ;
#29687=CARTESIAN_POINT ( 'NONE',  ( 1.108046318188542489, -0.04667474159409169127, 2.016033875899234662 ) ) ;
#29689=CARTESIAN_POINT ( 'NONE',  ( 5.600070422683368854, 0.8392489243487236683, -1.884408887491027196 ) ) ;
#29695=CARTESIAN_POINT ( 'NONE',  ( 6.714126539417144102, -0.8821443205445091973, -1.649434700640100226 ) ) ;
#29696=CARTESIAN_POINT ( 'NONE',  ( 5.467320813769629417, -1.693630324315539726, -0.3718415804769247268 ) ) ;
#29697=CARTESIAN_POINT ( 'NONE',  ( 5.899919523139840472, -0.6348737135929006792, -1.620717943835482844 ) ) ;
#29698=CARTESIAN_POINT ( 'NONE',  ( 3.193229341380324549, 1.808410471145019960, 1.408695239656273301 ) ) ;
#29700=CARTESIAN_POINT ( 'NONE',  ( 0.9371597039556851527, 0.7481776565299683712, -1.682445429299509909 ) ) ;
#29704=CARTESIAN_POINT ( 'NONE',  ( 1.553431815599433108, 0.5335803070953272220, -1.745854899344486233 ) ) ;
#29705=CARTESIAN_POINT ( 'NONE',  ( 2.795546247670523954, 1.458556481301529706, -1.392545902517070111 ) ) ;
#29706=CARTESIAN_POINT ( 'NONE',  ( 0.8498829323080080433, 2.188760582993890313, -0.1110106097068005726 ) ) ;
#29708=CARTESIAN_POINT ( 'NONE',  ( 4.840906100885360885, 0.3572417793257404717, 2.075268335340733739 ) ) ;
#29711=CARTESIAN_POINT ( 'NONE',  ( 1.926316106172959230, 1.062450747350886848, 1.776810178100460824 ) ) ;
#29714=CARTESIAN_POINT ( 'NONE',  ( 4.266349992362879817, 2.119992548681798095, -0.05317809935000831351 ) ) ;
#29715=CARTESIAN_POINT ( 'NONE',  ( 6.604126001430527637, -1.825160783932573860, 0.05055279568313279792 ) ) ;
#29722=CARTESIAN_POINT ( 'NONE',  ( -0.2102771530458277249, -0.008943344768331040057, -2.203482896658352175 ) ) ;
#29723=CARTESIAN_POINT ( 'NONE',  ( 1.114449138222296742, -0.9466070430152218051, -1.881282081674582995 ) ) ;
#29726=CARTESIAN_POINT ( 'NONE',  ( 4.645250437676715194, 1.663689067502411412, -0.8338919413633429922 ) ) ;
#29732=CARTESIAN_POINT ( 'NONE',  ( 2.752341281506097470, -1.956419249932477955, -0.1471676765215298721 ) ) ;
#29733=CARTESIAN_POINT ( 'NONE',  ( 1.411231610350563992, 1.906656261001705488, 1.018656936289302539 ) ) ;
#29737=CARTESIAN_POINT ( 'NONE',  ( 2.424751807388926039, 0.7370815838836901612, 1.569499502796549262 ) ) ;
#29738=CARTESIAN_POINT ( 'NONE',  ( 2.765247366594007605, 0.9310170973755277357, 1.470147560556547273 ) ) ;
#29741=CARTESIAN_POINT ( 'NONE',  ( 2.003267984693514858, 1.711604303819891593, 1.147383568780909302 ) ) ;
#29743=CARTESIAN_POINT ( 'NONE',  ( 1.546249734355091388, 1.863884247081739609, -0.7690006294575402190 ) ) ;
#29744=CARTESIAN_POINT ( 'NONE',  ( 6.825078400183551608, 4.689370880799383912, 2.706890346843467299 ) ) ;
#29746=CARTESIAN_POINT ( 'NONE',  ( 1.059376886711576260, 0.3867523390363221125, -1.932997803022660666 ) ) ;
#29747=CARTESIAN_POINT ( 'NONE',  ( 5.818603510220927255, -0.6945032022064903110, -1.782003016414166474 ) ) ;
#29752=CARTESIAN_POINT ( 'NONE',  ( 0.8385427299653764877, 1.201306043029852777, -1.623412603403198373 ) ) ;
#29754=CARTESIAN_POINT ( 'NONE',  ( 4.454349891636342207, 2.307156057683857675, -0.05211387993751984832 ) ) ;
#29755=CARTESIAN_POINT ( 'NONE',  ( 5.635196431686764207, -0.04651148872366302894, -1.961470878453225763 ) ) ;
#29756=CARTESIAN_POINT ( 'NONE',  ( 2.026150138982992566, 1.004015975608811173, 1.685199498757394831 ) ) ;
#29760=CARTESIAN_POINT ( 'NONE',  ( 1.464221803445309167, -1.127774752583620366, 1.791820951956924812 ) ) ;
#29763=CARTESIAN_POINT ( 'NONE',  ( 0.6910384644343778859, -0.6650364481293036256, 1.717017257891314097 ) ) ;
#29765=CARTESIAN_POINT ( 'NONE',  ( 4.539989016966003099, 1.413352768409949389, 1.648148102320112329 ) ) ;
#29767=CARTESIAN_POINT ( 'NONE',  ( 3.041385797112206912, 0.05609166564453024750, 2.120036961950934273 ) ) ;
#29772=CARTESIAN_POINT ( 'NONE',  ( 3.479809507395460244, 1.304684485917747994, 1.595210877418812956 ) ) ;
#29774=CARTESIAN_POINT ( 'NONE',  ( 0.09881949811249221560, -0.4921898920670075839, 1.774194203830472993 ) ) ;
#29776=CARTESIAN_POINT ( 'NONE',  ( -0.02224634325196857970, 4.078913133451218087, -2.843768138527980049 ) ) ;
#29779=CARTESIAN_POINT ( 'NONE',  ( 2.214515517796631805, -1.065126590517451843, -1.995962479041712534 ) ) ;
#29781=CARTESIAN_POINT ( 'NONE',  ( 1.933590839544163664, -1.756428034162808904, 0.4429697619106263695 ) ) ;
#29783=CARTESIAN_POINT ( 'NONE',  ( 2.219824929201766217, 0.8990433841352833966, -1.691613514901336490 ) ) ;
#29784=CARTESIAN_POINT ( 'NONE',  ( 2.611853368047814872, 0.5545374748289233491, -1.994631108499920646 ) ) ;
#29786=CARTESIAN_POINT ( 'NONE',  ( 1.867985033921132798, 1.011920226373051346, 1.691812110196472041 ) ) ;
#29787=CARTESIAN_POINT ( 'NONE',  ( 0.4285742275551830960, 1.842496385298073580, 0.5622912056609475906 ) ) ;
#29788=CARTESIAN_POINT ( 'NONE',  ( 3.362029495745801899, 0.8400119854848131506, 1.671504782411597612 ) ) ;
#29789=CARTESIAN_POINT ( 'NONE',  ( 1.682680061667326088, -1.231660274741898320, 1.951365989292063174 ) ) ;
#29791=CARTESIAN_POINT ( 'NONE',  ( 2.576407586095734725, 1.218277932339612901, -1.406949740073556887 ) ) ;
#29794=CARTESIAN_POINT ( 'NONE',  ( 5.846154128119951388, -0.9308047640707247661, 1.840808156992862932 ) ) ;
#29798=CARTESIAN_POINT ( 'NONE',  ( 6.739294440770141392, -1.883009798889522024, 0.9431707147840006078 ) ) ;
#29800=CARTESIAN_POINT ( 'NONE',  ( 6.468072252983536607, 1.105043713804385153, 1.857642994352682653 ) ) ;
#29801=CARTESIAN_POINT ( 'NONE',  ( 0.08815677907929740653, 1.166467155405017442, 1.648690671293622012 ) ) ;
#29810=CARTESIAN_POINT ( 'NONE',  ( 4.592982591267942283, 1.756852934926198317, 0.9896879400849432074 ) ) ;
#29816=CARTESIAN_POINT ( 'NONE',  ( 6.403215362905616992, 1.794359850238020693, 1.205212418099836480 ) ) ;
#29821=CARTESIAN_POINT ( 'NONE',  ( 6.327749939939702806, 0.7691082200134463642, -1.864175038933603146 ) ) ;
#29823=CARTESIAN_POINT ( 'NONE',  ( 6.639320575229294086, -0.003630812595115453199, 2.203388474976493594 ) ) ;
#29824=CARTESIAN_POINT ( 'NONE',  ( 1.945521746005531627, 0.6619316864419527713, -1.593019548489343240 ) ) ;
#29828=CARTESIAN_POINT ( 'NONE',  ( 6.274654046616443992, -1.776150972019393093, -0.5868208112121618969 ) ) ;
#29829=CARTESIAN_POINT ( 'NONE',  ( 1.154940503102233729, 0.3948395466160973255, 1.973830874585213113 ) ) ;
#29831=CARTESIAN_POINT ( 'NONE',  ( 3.294164632606086940, -0.8960083017303889230, 2.016869484631748310 ) ) ;
#29832=CARTESIAN_POINT ( 'NONE',  ( 5.858309005574939832, -2.171239809575730817, -0.007779773244297875576 ) ) ;
#29836=CARTESIAN_POINT ( 'NONE',  ( 3.633539341399088407, -0.1543397204060332761, 2.114911865293423787 ) ) ;
#29837=CARTESIAN_POINT ( 'NONE',  ( 2.847279977023515318, 0.2930488483154705670, -1.994874153863256172 ) ) ;
#29838=CARTESIAN_POINT ( 'NONE',  ( 1.863241329703895888, -1.456548260382009685, -1.076974786960547048 ) ) ;
#29845=CARTESIAN_POINT ( 'NONE',  ( 0.9892949506953198080, -0.4622125203353181222, 1.859009271263431184 ) ) ;
#29853=CARTESIAN_POINT ( 'NONE',  ( 4.856408821558930278, 0.8241108818672329139, 1.998647875481096126 ) ) ;
#29857=CARTESIAN_POINT ( 'NONE',  ( 2.566775492539817627, 0.7186216927172992541, 1.995234744298620910 ) ) ;
#29859=CARTESIAN_POINT ( 'NONE',  ( 3.286357016390834218, -1.941589536447934972, -0.3404988550089679267 ) ) ;
#29862=CARTESIAN_POINT ( 'NONE',  ( 0.9419464005683108043, 1.389173191389100337, 1.535309223701806447 ) ) ;
#29863=CARTESIAN_POINT ( 'NONE',  ( 2.941277052067638120, 0.6983745205926906729, -1.812199837690719129 ) ) ;
#29868=CARTESIAN_POINT ( 'NONE',  ( 2.255913092623571092, 0.8947350874906587759, 1.889642235345281307 ) ) ;
#29871=CARTESIAN_POINT ( 'NONE',  ( -0.09351100681491937572, -0.3904691765420374439, -1.774915231904458990 ) ) ;
#29873=CARTESIAN_POINT ( 'NONE',  ( 3.967548030458594610, 0.2710504330169677401, -2.190103208553782821 ) ) ;
#29874=CARTESIAN_POINT ( 'NONE',  ( 3.241465689944766915, -1.947025830926933043, 1.038692105600529159 ) ) ;
#29877=CARTESIAN_POINT ( 'NONE',  ( 1.365713085969634477, 0.5541664655046051324, -1.830235057661818487 ) ) ;
#29879=CARTESIAN_POINT ( 'NONE',  ( 3.947765587739564097, 1.497496809916948779, 1.429883829622953462 ) ) ;
#29881=CARTESIAN_POINT ( 'NONE',  ( 2.624079441566569582, -1.243859440641072123, -1.767801033134681843 ) ) ;
#29882=CARTESIAN_POINT ( 'NONE',  ( 4.757479570170550787, 2.167726397749652367, -0.3216086267831194112 ) ) ;
#29889=CARTESIAN_POINT ( 'NONE',  ( 0.5631252389872200004, -1.117830369828230808, 1.678006741548984770 ) ) ;
#29891=CARTESIAN_POINT ( 'NONE',  ( 4.645415698524104187, 1.851598927129451955, -0.9261206523473937136 ) ) ;
#29892=CARTESIAN_POINT ( 'NONE',  ( 3.211465258343335627, -0.3752234067680487728, 1.889445157240315254 ) ) ;
#29893=CARTESIAN_POINT ( 'NONE',  ( 6.046512527486515687, -1.496967179435993778, 1.497493072882298382 ) ) ;
#29896=CARTESIAN_POINT ( 'NONE',  ( 3.924621296410530480, -1.326038130087652922, 1.456277141313151224 ) ) ;
#29897=CARTESIAN_POINT ( 'NONE',  ( 6.404234474585668302, 1.703059896339639057, -1.534467582428314270 ) ) ;
#29898=CARTESIAN_POINT ( 'NONE',  ( 4.019992336727182369, -0.9402185374879183932, -1.564826772493657536 ) ) ;
#29905=CARTESIAN_POINT ( 'NONE',  ( 2.014959344526063845, -1.785600367564584179, 0.4486904387498573676 ) ) ;
#29906=CARTESIAN_POINT ( 'NONE',  ( 5.326436552476821795, -0.9091558477445594866, -1.796327993944699219 ) ) ;
#29907=CARTESIAN_POINT ( 'NONE',  ( 6.311202115008078373, 1.327223183623595704, -1.876690649992603044 ) ) ;
#29908=CARTESIAN_POINT ( 'NONE',  ( 5.998874280538830206, 0.3792253423284037139, 1.924579554046601970 ) ) ;
#29915=CARTESIAN_POINT ( 'NONE',  ( 2.015285228526709549, -2.027172053905087701, 0.5110949307850811696 ) ) ;
#29916=CARTESIAN_POINT ( 'NONE',  ( 6.455894400631252417, 1.764744506579400962, -0.1349141608881914423 ) ) ;
#29918=CARTESIAN_POINT ( 'NONE',  ( -0.1104750535120268828, 7.629137130509074716, -2.703481013110929254 ) ) ;
#29919=CARTESIAN_POINT ( 'NONE',  ( 1.487455728203713745, -1.732000560005091616, -0.1708635279896036641 ) ) ;
#29923=CARTESIAN_POINT ( 'NONE',  ( 1.804884324593715839, 1.432779585713826576, 0.9600471282974596399 ) ) ;
#29924=CARTESIAN_POINT ( 'NONE',  ( 2.015410700679621137, -2.124826835150806392, 0.5361769018528695918 ) ) ;
#29925=CARTESIAN_POINT ( 'NONE',  ( -0.08779760418278770295, -1.063538860511966444, -1.369745729481768759 ) ) ;
#29926=CARTESIAN_POINT ( 'NONE',  ( 3.932405576212230525, 1.181341412803040614, -1.863887651898883613 ) ) ;
#29928=CARTESIAN_POINT ( 'NONE',  ( 1.551893958816989993, 1.642325835523240629, 1.420010234424383455 ) ) ;
#29929=CARTESIAN_POINT ( 'NONE',  ( -0.02319159430949970999, 0.003959926571647092407, -1.810968101872318714 ) ) ;
#29930=CARTESIAN_POINT ( 'NONE',  ( 3.362624215892480173, -2.041811681064845896, -0.5603701389207839112 ) ) ;
#29931=CARTESIAN_POINT ( 'NONE',  ( 6.639320575229249677, 4.701313753536039641, 2.359456658813867236 ) ) ;
#29933=CARTESIAN_POINT ( 'NONE',  ( 3.333774467322860868, 1.029290431845871989, -2.048349661755991313 ) ) ;
#29937=CARTESIAN_POINT ( 'NONE',  ( 5.690131909746282801, 1.321361375537116967, 1.785392519086197671 ) ) ;
#29944=CARTESIAN_POINT ( 'NONE',  ( 3.762342404062005041, 1.897698010425369786, -0.6819954029829021769 ) ) ;
#29946=CARTESIAN_POINT ( 'NONE',  ( 2.746997431529357492, -0.3482204723163102034, -2.032804898803519222 ) ) ;
#29951=CARTESIAN_POINT ( 'NONE',  ( 4.945371362016417471, 0.6893947036107104243, -2.080263006054481334 ) ) ;
#29952=CARTESIAN_POINT ( 'NONE',  ( 2.918592439375994552, -1.356299846568160827, -1.492255409411530120 ) ) ;
#29953=CARTESIAN_POINT ( 'NONE',  ( 1.751249726499287673, 1.836263021919124050, -0.1365115386888632321 ) ) ;
#29955=CARTESIAN_POINT ( 'NONE',  ( 5.491160184941096922, 1.609068807629027820, -0.8623064814072267659 ) ) ;
#29956=CARTESIAN_POINT ( 'NONE',  ( 5.924453975591452703, -1.462443569488897754, -1.388487997949397368 ) ) ;
#29958=CARTESIAN_POINT ( 'NONE',  ( 5.401357799220028788, 1.846321421614788516, 1.307461012187713933 ) ) ;
#29960=CARTESIAN_POINT ( 'NONE',  ( 1.137491875146545039, -1.903277616399126293, 0.9019996372539202945 ) ) ;
#29970=CARTESIAN_POINT ( 'NONE',  ( 1.828540510153942922, -1.004066958311781832, -1.867862179375394005 ) ) ;
#29971=CARTESIAN_POINT ( 'NONE',  ( 2.584490447655915624, 1.192291587189574065, 1.874175285706691341 ) ) ;
#29975=CARTESIAN_POINT ( 'NONE',  ( 3.455471728117681440, 1.544996161402897528, 1.208956721487665087 ) ) ;
#29982=CARTESIAN_POINT ( 'NONE',  ( 2.267978396857213585, 0.5610993688725562922, -2.044979925899123252 ) ) ;
#29984=CARTESIAN_POINT ( 'NONE',  ( 3.977527890101069996, 2.036293384626610248, -0.7259696361804208742 ) ) ;
#29985=CARTESIAN_POINT ( 'NONE',  ( 2.296224312773272658, 1.477747569344042500, -1.098160524033331642 ) ) ;
#29988=CARTESIAN_POINT ( 'NONE',  ( 5.859256971114414014, 1.713395515214741538, -0.3040290152411839752 ) ) ;
#29992=CARTESIAN_POINT ( 'NONE',  ( 2.852577672069932735, 0.7271573612388192442, 2.035869728763760378 ) ) ;
#29994=CARTESIAN_POINT ( 'NONE',  ( 4.376327261493318410, -0.3474131038204917310, 1.985796694155849362 ) ) ;
#29996=CARTESIAN_POINT ( 'NONE',  ( 2.325270847726228940, -0.0006328605136555342939, 2.161883445422786654 ) ) ;
#29997=CARTESIAN_POINT ( 'NONE',  ( 2.565645918639497314, 1.934049084626581205, -0.3809019065194594877 ) ) ;
#29998=CARTESIAN_POINT ( 'NONE',  ( 2.923064838257955156, -1.776166165677966591, 0.9548571111624851726 ) ) ;
#29999=FACE_OUTER_BOUND ( 'NONE', #87328, .T. ) ;
#30000=CARTESIAN_POINT ( 'NONE',  ( 4.511236532831874868, -1.903902423773628838, 0.3822933785788319438 ) ) ;
#30003=VERTEX_POINT ( 'NONE', #81012 ) ;
#30010=CARTESIAN_POINT ( 'NONE',  ( 1.483733071427257411, 2.038639745401783721, -0.8453341458589253010 ) ) ;
#30012=CARTESIAN_POINT ( 'NONE',  ( 5.735196368693616265, -0.04450293679344322767, -1.961403813732150780 ) ) ;
#30016=CARTESIAN_POINT ( 'NONE',  ( 3.820104440490858622, 1.748809976318686177, 0.5759312369505511509 ) ) ;
#30021=FACE_OUTER_BOUND ( 'NONE', #97888, .T. ) ;
#30023=CARTESIAN_POINT ( 'NONE',  ( 0.09275324736048547181, -0.4491109574935348014, -2.018345435551980316 ) ) ;
#30026=CARTESIAN_POINT ( 'NONE',  ( 1.732617751151921404, -1.765751579927745007, -0.5880843478397956847 ) ) ;
#30027=CARTESIAN_POINT ( 'NONE',  ( 3.350949008998193257, 0.4442310927498266948, -1.786741727165648497 ) ) ;
#30032=CARTESIAN_POINT ( 'NONE',  ( 3.000804911251079510, -0.6410980074830170405, -2.111705341948390657 ) ) ;
#30033=CARTESIAN_POINT ( 'NONE',  ( 6.450461099754450700, 0.7004171410973459855, 2.151357330220986963 ) ) ;
#30035=CARTESIAN_POINT ( 'NONE',  ( 5.818593503215891971, -0.6604613111419742610, -1.687090931240011527 ) ) ;
#30036=CARTESIAN_POINT ( 'NONE',  ( 6.227746030346171580, 0.7262518248569529433, -1.772935525165220128 ) ) ;
#30038=CARTESIAN_POINT ( 'NONE',  ( 6.473518811298506925, 1.789458955665638618, -0.5451884755478533240 ) ) ;
#30039=CARTESIAN_POINT ( 'NONE',  ( 6.373497979817693171, -0.2265250974912805249, 1.847160380126455559 ) ) ;
#30041=CARTESIAN_POINT ( 'NONE',  ( 6.280137008050575176, -0.9429096061123897199, 1.497559920798942512 ) ) ;
#30042=CARTESIAN_POINT ( 'NONE',  ( 1.639861632979456418, 2.010800986640928656, -0.1531718788195315928 ) ) ;
#30044=CARTESIAN_POINT ( 'NONE',  ( 2.543703448412675261, -1.561038821359970408, -1.413940773279374508 ) ) ;
#30048=CARTESIAN_POINT ( 'NONE',  ( 6.983263157960366563, 7.629137130509066722, 2.653810918356712900 ) ) ;
#30049=CARTESIAN_POINT ( 'NONE',  ( 2.443623115440888061, -1.883043647339300186, 0.7309814453849405869 ) ) ;
#30053=CARTESIAN_POINT ( 'NONE',  ( 3.813887338145681927, -2.130327034543195275, 0.3653767458386343314 ) ) ;
#30058=CARTESIAN_POINT ( 'NONE',  ( 1.135490968158389791, -0.05309211241652118246, -2.170675730929682246 ) ) ;
#30063=CARTESIAN_POINT ( 'NONE',  ( 2.577880719133851084, -1.123996537731044354, 1.881222605751430521 ) ) ;
#30065=CARTESIAN_POINT ( 'NONE',  ( 2.676973543053912330, -2.164909235287615807, -0.6573374913001366338 ) ) ;
#30073=CARTESIAN_POINT ( 'NONE',  ( 2.758786678070863196, -1.537680025927037786, -0.8759604286991302668 ) ) ;
#30075=CARTESIAN_POINT ( 'NONE',  ( 6.053802686139254874, 0.6462426183462595120, -2.110027337871730690 ) ) ;
#30080=CARTESIAN_POINT ( 'NONE',  ( 3.590566789841375339, -0.3639703897368729568, -1.834726254853453087 ) ) ;
#30081=CARTESIAN_POINT ( 'NONE',  ( 3.678634981485491728, 1.317094234756083893, -1.597214816249421743 ) ) ;
#30086=SURFACE_SIDE_STYLE ('',( #46348 ) ) ;
#30089=CARTESIAN_POINT ( 'NONE',  ( 2.945700582358207864, 1.385421296276163838, 1.389331660621349274 ) ) ;
#30091=CARTESIAN_POINT ( 'NONE',  ( 0.4036724312478366938, 0.3418800534340654118, 1.986742826083332858 ) ) ;
#30094=CARTESIAN_POINT ( 'NONE',  ( 0.9131076777311696313, -0.2804849920042574718, 1.849292663789033009 ) ) ;
#30096=CARTESIAN_POINT ( 'NONE',  ( 2.619392002094393490, 1.702953528017937090, 1.073460467912157101 ) ) ;
#30098=CARTESIAN_POINT ( 'NONE',  ( 2.636446987817195886, 0.7160595562910974099, 1.992577970932450704 ) ) ;
#30100=CARTESIAN_POINT ( 'NONE',  ( 3.596198176508007105, 0.9334358170956689182, -1.848091447891623051 ) ) ;
#30102=CARTESIAN_POINT ( 'NONE',  ( 5.507793336809221785, -0.9391204764703815489, -1.867914344430561702 ) ) ;
#30104=CARTESIAN_POINT ( 'NONE',  ( 4.418855976699648025, 1.669273799801282765, 0.7395231729718022562 ) ) ;
#30107=CARTESIAN_POINT ( 'NONE',  ( 6.639320575229292309, -0.003630812595115444526, 2.203388474976493594 ) ) ;
#30109=CARTESIAN_POINT ( 'NONE',  ( 6.510767885691055135, 1.639592601025055885, -1.477219212978691409 ) ) ;
#30111=CARTESIAN_POINT ( 'NONE',  ( 5.391234928627540945, -0.05113397888981999206, -1.911771334517261778 ) ) ;
#30118=CARTESIAN_POINT ( 'NONE',  ( 0.7492455685023796663, 1.839184785914184994, -0.09005233288367914257 ) ) ;
#30122=CARTESIAN_POINT ( 'NONE',  ( 4.587079231881330266, 1.671727914585485530, -0.8392916717318498199 ) ) ;
#30129=CARTESIAN_POINT ( 'NONE',  ( 1.024188300031657617, 0.9657954515097492143, 1.716266578800438536 ) ) ;
#30130=CARTESIAN_POINT ( 'NONE',  ( 3.462517696756307384, -1.944077823024586538, -0.5350690621670484148 ) ) ;
#30135=CARTESIAN_POINT ( 'NONE',  ( 4.171962795014371395, -1.262591954434747921, 1.790989659139609724 ) ) ;
#30139=CARTESIAN_POINT ( 'NONE',  ( 0.2331563151865729544, 2.882199166944008795, -2.434502449063076224 ) ) ;
#30145=CARTESIAN_POINT ( 'NONE',  ( 4.458453498679889826, -1.646799808365447149, -0.8236825204945982248 ) ) ;
#30146=CARTESIAN_POINT ( 'NONE',  ( 2.279941584743001126, 1.973825526184776580, -0.3948664393432794184 ) ) ;
#30147=CARTESIAN_POINT ( 'NONE',  ( 3.954713598875368774, 1.661701185475419118, 1.588069724787332992 ) ) ;
#30148=CARTESIAN_POINT ( 'NONE',  ( -0.1291982275798807533, 2.865258409039960430, -2.562285117308207294 ) ) ;
#30149=CARTESIAN_POINT ( 'NONE',  ( 1.692022144237431469, 0.9228297918665344657, -1.615966242530289199 ) ) ;
#30152=CARTESIAN_POINT ( 'NONE',  ( 6.099862406061942188, 1.323743610676546334, 1.380425988546908567 ) ) ;
#30155=CARTESIAN_POINT ( 'NONE',  ( 5.232010533483211212, 2.060019964192044917, 0.3561100859283144460 ) ) ;
#30156=CARTESIAN_POINT ( 'NONE',  ( 2.922558825391399662, 1.760836971185793187, 0.6318509464167121337 ) ) ;
#30158=CARTESIAN_POINT ( 'NONE',  ( 6.427308110136687347, -1.208249125052461181, -1.389453836245766016 ) ) ;
#30161=CARTESIAN_POINT ( 'NONE',  ( 5.408750372623219782, 1.302234988713904640, -1.131221429639968745 ) ) ;
#30163=CARTESIAN_POINT ( 'NONE',  ( 0.3692042219665427893, -0.2092721526018372635, -1.721406745681583583 ) ) ;
#30165=( LENGTH_UNIT ( ) NAMED_UNIT ( * ) SI_UNIT ( .MILLI., .METRE. ) );
#30166=CARTESIAN_POINT ( 'NONE',  ( 4.803694799390169301, -1.674174935400191799, -1.382237342716886586 ) ) ;
#30167=CARTESIAN_POINT ( 'NONE',  ( 3.545350327189537687, -1.383302465072188792, -1.191577590537174158 ) ) ;
#30168=CARTESIAN_POINT ( 'NONE',  ( 1.569116724355507975, 1.727593668635756918, 0.9295332132536607839 ) ) ;
#30169=CARTESIAN_POINT ( 'NONE',  ( 0.3162073025194310771, 1.084344979787469354, -1.818339158833045976 ) ) ;
#30170=CARTESIAN_POINT ( 'NONE',  ( 0.6040055286682350921, -2.280654241543427663, 0.2304348961432670095 ) ) ;
#30174=CARTESIAN_POINT ( 'NONE',  ( 3.106218681870171139, -0.8574772492565514437, 1.939554460742904274 ) ) ;
#30179=CARTESIAN_POINT ( 'NONE',  ( 0.7782871991188352601, -1.104406889285912907, -1.750870654829151274 ) ) ;
#30180=CARTESIAN_POINT ( 'NONE',  ( 6.883263157960421097, 0.5621630953002605402, 2.205140871664055702 ) ) ;
#30183=CARTESIAN_POINT ( 'NONE',  ( 2.368119171756615238, 0.5893650439614643854, -2.141638343492527685 ) ) ;
#30185=CARTESIAN_POINT ( 'NONE',  ( 0.2121463357745425049, 2.202340261784305753, 0.6586529460593565366 ) ) ;
#30187=CARTESIAN_POINT ( 'NONE',  ( 5.172745336439665387, 1.426162745032448109, -1.490257803364034128 ) ) ;
#30191=FACE_OUTER_BOUND ( 'NONE', #51033, .T. ) ;
#30192=CARTESIAN_POINT ( 'NONE',  ( 5.724118993814841794, 1.776208094789998304, 0.4848738846057951135 ) ) ;
#30196=CARTESIAN_POINT ( 'NONE',  ( 2.397083457474056267, 1.331176160016230847, 1.096701253500545148 ) ) ;
#30197=CARTESIAN_POINT ( 'NONE',  ( 1.341030165941111241, -1.731997234073547220, -1.032477317303444053 ) ) ;
#30198=CARTESIAN_POINT ( 'NONE',  ( 1.829147786997789016, 0.8750025983248543859, -2.125820487401499204 ) ) ;
#30201=CARTESIAN_POINT ( 'NONE',  ( 2.056323133375201007, 2.256402538945650349, -0.1652075827990733270 ) ) ;
#30202=CARTESIAN_POINT ( 'NONE',  ( 4.248724916491292802, 0.5614479688690295900, 2.029775142636090379 ) ) ;
#30204=CARTESIAN_POINT ( 'NONE',  ( 2.231405582217013794, -1.152036887248751862, -1.343533879150171861 ) ) ;
#30208=CARTESIAN_POINT ( 'NONE',  ( 5.267208303392540536, 2.209927380382335826, -0.6089511437187348220 ) ) ;
#30212=EDGE_CURVE ( 'NONE', #21772, #111149, #115036, .T. ) ;
#30213=CARTESIAN_POINT ( 'NONE',  ( 4.787173061057010237, 1.622617466453496471, 1.473133629693437197 ) ) ;
#30219=CARTESIAN_POINT ( 'NONE',  ( 2.789578772358902281, 1.362584191422511415, 1.362147869459982230 ) ) ;
#30222=CARTESIAN_POINT ( 'NONE',  ( 5.220985865760717992, 1.604251394084664550, -1.386888226476624242 ) ) ;
#30228=CARTESIAN_POINT ( 'NONE',  ( 5.724118993814841794, 1.776208094789998304, 0.4848738846057951135 ) ) ;
#30231=CARTESIAN_POINT ( 'NONE',  ( 2.542201289624079319, -1.445942355291447434, 0.9683529963873671598 ) ) ;
#30233=CARTESIAN_POINT ( 'NONE',  ( 0.2034672893990868703, -1.513989045467616146, -1.247398002513319781 ) ) ;
#30237=CARTESIAN_POINT ( 'NONE',  ( 5.875883356151954118, 1.283970044810868849, 1.738936680771227206 ) ) ;
#30241=CARTESIAN_POINT ( 'NONE',  ( 6.297764839082774735, -0.7330946318361495351, 2.033732118066629457 ) ) ;
#30245=CARTESIAN_POINT ( 'NONE',  ( 6.257099195183372764, -1.689481296825417811, -1.015638971094455556 ) ) ;
#30246=CARTESIAN_POINT ( 'NONE',  ( 5.887993837006205489, -0.03927123031851989521, 1.733586367271770179 ) ) ;
#30248=CARTESIAN_POINT ( 'NONE',  ( 2.823975127348025804, 1.215230906543849354, -1.823574674616668556 ) ) ;
#30249=CARTESIAN_POINT ( 'NONE',  ( 3.716130297413534844, -2.273962828982917017, 0.3916390033968617512 ) ) ;
#30250=CARTESIAN_POINT ( 'NONE',  ( 5.641890011675567251, 0.8391073529228080252, -1.882412581722334943 ) ) ;
#30251=CARTESIAN_POINT ( 'NONE',  ( 1.499837725185527049, -0.6986378101729547874, -1.812093905146118233 ) ) ;
#30255=CARTESIAN_POINT ( 'NONE',  ( 4.166350089634453191, 2.120059694336435374, -0.05518752902338577848 ) ) ;
#30256=CARTESIAN_POINT ( 'NONE',  ( 2.303361484738715159, 1.314996338066702242, -1.528741580717301263 ) ) ;
#30258=CARTESIAN_POINT ( 'NONE',  ( 3.979664642534729513, 2.078844338038158934, -0.7408291028327750327 ) ) ;
#30264=CARTESIAN_POINT ( 'NONE',  ( 6.825078400183518745, 0.5555073798480349989, 2.295529415773037929 ) ) ;
#30266=EDGE_LOOP ( 'NONE', ( #107547, #15169, #204639, #135350 ) ) ;
#30267=CARTESIAN_POINT ( 'NONE',  ( 4.065347389730957772, 0.2539501645208458447, -2.045120066754711363 ) ) ;
#30273=CARTESIAN_POINT ( 'NONE',  ( 3.897132395768299951, -0.2000006916238558641, -2.009757592718981911 ) ) ;
#30278=CARTESIAN_POINT ( 'NONE',  ( 2.834896919975951057, 0.2507222237850720847, 2.045500233692464587 ) ) ;
#30279=CARTESIAN_POINT ( 'NONE',  ( 2.514296259408643319, -1.880434619097739013, 0.7283795345095490648 ) ) ;
#30286=CARTESIAN_POINT ( 'NONE',  ( 1.253568445147245525, 0.7445567558202557112, 1.684058134371092752 ) ) ;
#30287=CARTESIAN_POINT ( 'NONE',  ( 6.727182134110200273, -0.004969159814478123736, 2.189081792362323586 ) ) ;
#30289=CARTESIAN_POINT ( 'NONE',  ( 3.128364550451453230, 1.203671540783244565, -1.795256801906938815 ) ) ;
#30291=CARTESIAN_POINT ( 'NONE',  ( 4.294233728257051297, -0.9087460953031538669, -1.912572187454407047 ) ) ;
#30294=CARTESIAN_POINT ( 'NONE',  ( 0.6724591444495706671, -1.759989063064151038, -0.6342292696241008665 ) ) ;
#30295=CARTESIAN_POINT ( 'NONE',  ( 4.944191625186433292, 1.966121618969366214, 0.1460544362237597982 ) ) ;
#30296=CARTESIAN_POINT ( 'NONE',  ( 4.645720405014278853, 1.993893748393640086, -0.3006458143828410479 ) ) ;
#30300=CARTESIAN_POINT ( 'NONE',  ( 6.656868561830338038, -1.629224735911166233, 1.334343933791133141 ) ) ;
#30301=CARTESIAN_POINT ( 'NONE',  ( 6.742638474511262636, -2.029596885996234334, -0.4079607620106340260 ) ) ;
#30305=CARTESIAN_POINT ( 'NONE',  ( 6.639320575229291421, 7.052573552169272730, 2.601414154538615353 ) ) ;
#30306=CARTESIAN_POINT ( 'NONE',  ( 4.698096894549816049, -1.971010956759836397, -0.04940921540304286930 ) ) ;
#30307=CARTESIAN_POINT ( 'NONE',  ( 5.959241620951676310, -1.704104911329520800, 1.083944116985413819 ) ) ;
#30309=CARTESIAN_POINT ( 'NONE',  ( 4.670747285963097184, -1.509779504925019999, 1.745381082733918676 ) ) ;
#30310=CARTESIAN_POINT ( 'NONE',  ( 2.254800304804779110, -0.5458148477457210879, -1.989007103235032048 ) ) ;
#30318=CARTESIAN_POINT ( 'NONE',  ( 3.912682095371947444, 0.7780703539225676257, 2.027152283489948026 ) ) ;
#30321=CARTESIAN_POINT ( 'NONE',  ( 3.913478945735289205, -0.9499487412085620974, -1.577145280185827447 ) ) ;
#30323=CARTESIAN_POINT ( 'NONE',  ( 6.720655732516701342, 6.039000170257122768, 2.421169367564251385 ) ) ;
#30325=CARTESIAN_POINT ( 'NONE',  ( 5.706613541269077494, 1.932210019790636224, 1.034112652976440394 ) ) ;
#30327=CARTESIAN_POINT ( 'NONE',  ( 5.875896723904014962, 1.342229061679913071, 1.821250878268846352 ) ) ;
#30333=CARTESIAN_POINT ( 'NONE',  ( 0.4437791967034719343, 1.764639887404760188, 0.1366099650685937694 ) ) ;
#30334=CARTESIAN_POINT ( 'NONE',  ( 4.248693477488805215, 1.974695210492120045, 0.3904942472512766827 ) ) ;
#30336=CARTESIAN_POINT ( 'NONE',  ( 2.960101939890079858, 2.095960298449873971, -0.2048252169620876917 ) ) ;
#30337=CARTESIAN_POINT ( 'NONE',  ( 1.581495747622517323, -0.6437907056052544208, 1.804334155150161267 ) ) ;
#30339=CARTESIAN_POINT ( 'NONE',  ( 3.016014308207531247, 1.960325316701009735, -0.1901906172739661061 ) ) ;
#30340=CARTESIAN_POINT ( 'NONE',  ( 6.082287225941254150, 1.041776932085249907, 1.730260143339139134 ) ) ;
#30341=CARTESIAN_POINT ( 'NONE',  ( 1.867826558377215118, 0.9591755677602131769, 1.605880698980370225 ) ) ;
#30342=CARTESIAN_POINT ( 'NONE',  ( 1.732786548908150870, -1.861864252656076912, -0.6185235971247133868 ) ) ;
#30343=CARTESIAN_POINT ( 'NONE',  ( 3.808989599770518097, 1.480563749658039052, 0.8846867361136273589 ) ) ;
#30344=CARTESIAN_POINT ( 'NONE',  ( 1.652457426684301955, 1.892030339952909035, 0.2773405859870237133 ) ) ;
#30346=CARTESIAN_POINT ( 'NONE',  ( 1.137671262558290763, -1.993743905544292927, 0.9465009238469668240 ) ) ;
#30354=CARTESIAN_POINT ( 'NONE',  ( 1.029834584532058672, 1.995790600324919506, -0.5504719462680053299 ) ) ;
#30359=CARTESIAN_POINT ( 'NONE',  ( 5.953796468794862129, -1.535729488331440074, -1.462440914314271811 ) ) ;
#30364=CARTESIAN_POINT ( 'NONE',  ( 5.670351692713981429, -0.8806477319739226539, -1.753155087565357428 ) ) ;
#30366=CARTESIAN_POINT ( 'NONE',  ( 4.692732413458527319, -1.238132498367883860, -1.591073831703953445 ) ) ;
#30367=CARTESIAN_POINT ( 'NONE',  ( 3.837047941109549054, -1.595840754823075303, -1.059516945425369450 ) ) ;
#30369=CARTESIAN_POINT ( 'NONE',  ( 1.329895901633147748, 1.076045675571284166, -1.909117696414885934 ) ) ;
#30370=CARTESIAN_POINT ( 'NONE',  ( 0.1335669894368500255, -0.0009366757763962055587, -2.153671288142432250 ) ) ;
#30372=CARTESIAN_POINT ( 'NONE',  ( 5.467046525086633579, -1.584481552701553220, 1.241800460852604759 ) ) ;
#30376=CARTESIAN_POINT ( 'NONE',  ( 5.642236307234618664, 0.8587400236706268508, 1.935442681345787452 ) ) ;
#30378=CARTESIAN_POINT ( 'NONE',  ( 2.085595224044423102, -0.8910886986466991511, 1.891471387866516585 ) ) ;
#30380=CARTESIAN_POINT ( 'NONE',  ( 1.623609269016149437, -0.9540678014761799774, -1.436642212298586907 ) ) ;
#30391=CARTESIAN_POINT ( 'NONE',  ( 2.103910407274149907, -0.7736040573625382333, 1.638098421638082947 ) ) ;
#30398=CARTESIAN_POINT ( 'NONE',  ( 2.244508708441519840, 1.757319924227723762, 0.4390839574351864671 ) ) ;
#30399=CARTESIAN_POINT ( 'NONE',  ( 6.639320575229291421, 7.053415594291638335, 2.394893074302415936 ) ) ;
#30402=CARTESIAN_POINT ( 'NONE',  ( 2.980726927023560346, 1.751358449955683350, 0.6298351686941299210 ) ) ;
#30403=CARTESIAN_POINT ( 'NONE',  ( 0.4916157762205043413, -1.906313760269543911, 0.1885876022650559980 ) ) ;
#30404=CARTESIAN_POINT ( 'NONE',  ( 0.3229203692996869823, -0.09522068211164493035, 1.823229820405058099 ) ) ;
#30413=CARTESIAN_POINT ( 'NONE',  ( 4.276189508915988036, -1.008629908464111269, -1.691384299763159182 ) ) ;
#30416=CARTESIAN_POINT ( 'NONE',  ( 6.632779825423476439, -1.959453823303359377, 0.9815127000676395763 ) ) ;
#30417=CARTESIAN_POINT ( 'NONE',  ( 5.860362583224701716, 0.7811062513497173398, 1.761092865462327239 ) ) ;
#30419=CARTESIAN_POINT ( 'NONE',  ( -0.2409995289980038091, -0.004801160710915519658, -2.000252362011435636 ) ) ;
#30420=CARTESIAN_POINT ( 'NONE',  ( 2.473496279428960776, 0.1070396533628548558, -2.204406164007084445 ) ) ;
#30422=CARTESIAN_POINT ( 'NONE',  ( -0.1933232215488022709, -0.4202133615931051835, -1.872389726556406897 ) ) ;
#30425=CARTESIAN_POINT ( 'NONE',  ( 0.6077773097897182231, 0.6213696771984353884, -1.869019927991413921 ) ) ;
#30426=CARTESIAN_POINT ( 'NONE',  ( 1.153739077726954498, 0.7885942357991974072, 1.774928408438203098 ) ) ;
#30427=CARTESIAN_POINT ( 'NONE',  ( 1.229842044428463010, -1.821462008879136896, -0.8645945014377558469 ) ) ;
#30429=CARTESIAN_POINT ( 'NONE',  ( 4.979284885303652430, -0.09383206328643842187, 1.858730327737258436 ) ) ;
#30435=CARTESIAN_POINT ( 'NONE',  ( 1.769323484426460480, 2.095969018468134770, -0.6401429536977767398 ) ) ;
#30440=CARTESIAN_POINT ( 'NONE',  ( 1.945663734523142230, 0.6997465788082489757, -1.686465609443507763 ) ) ;
#30444=CARTESIAN_POINT ( 'NONE',  ( 6.609000000000047947, 3.700659725723095761, 2.414405743007182359 ) ) ;
#30446=CARTESIAN_POINT ( 'NONE',  ( 0.6449897232218603227, -1.652859335204670543, 0.9894661712252955654 ) ) ;
#30447=CARTESIAN_POINT ( 'NONE',  ( 4.223457129239616137, 0.2443821477370981265, -1.946437379933690481 ) ) ;
#30451=CARTESIAN_POINT ( 'NONE',  ( 4.933237592207079025, -1.549687834843778811, -1.549900206446311657 ) ) ;
#30452=CARTESIAN_POINT ( 'NONE',  ( 6.609000000000038177, 0.002801690667396730672, 2.000160786441218530 ) ) ;
#30453=CARTESIAN_POINT ( 'NONE',  ( 4.135645376760338721, 1.951069878921590783, -0.6927527371542248069 ) ) ;
#30456=CARTESIAN_POINT ( 'NONE',  ( 4.307493173298723832, 1.414159744579394307, -1.812179591053430627 ) ) ;
#30463=CARTESIAN_POINT ( 'NONE',  ( 4.224509699451983735, 0.09670237001900212903, 1.939662488567380993 ) ) ;
#30466=CARTESIAN_POINT ( 'NONE',  ( 5.572493885891085519, 0.7809320506734825917, 1.745880147543739325 ) ) ;
#30468=CARTESIAN_POINT ( 'NONE',  ( 5.280183324938524159, -0.9553487854751692154, 1.435786287184135368 ) ) ;
#30469=CARTESIAN_POINT ( 'NONE',  ( 4.346888830327386266, -1.803415170841724979, -0.9023466997552240798 ) ) ;
#30471=CARTESIAN_POINT ( 'NONE',  ( 5.203857780826313117, 2.123009612837105209, 0.8817886472500915396 ) ) ;
#30472=CARTESIAN_POINT ( 'NONE',  ( 0.5576012004645107822, -1.866542136390366036, -1.177153700605698461 ) ) ;
#30475=CARTESIAN_POINT ( 'NONE',  ( 5.729715491186369469, -1.123817246201250786, -1.367138390065870457 ) ) ;
#30476=CARTESIAN_POINT ( 'NONE',  ( 5.203750078570229753, 1.864167652161516031, 0.7691231355932278690 ) ) ;
#30478=CARTESIAN_POINT ( 'NONE',  ( 2.484683925703546237, -0.3935552064166462083, -2.258081804418234473 ) ) ;
#30479=CARTESIAN_POINT ( 'NONE',  ( 1.446757823190962577, 0.5079132294574678630, -1.664563843253030750 ) ) ;
#30482=CARTESIAN_POINT ( 'NONE',  ( 1.194254265631944367, -1.094737682603286189, -1.344534739289292569 ) ) ;
#30485=CARTESIAN_POINT ( 'NONE',  ( 1.276089585440323138, -2.118389508516528519, 0.4752255978458518881 ) ) ;
#30486=CARTESIAN_POINT ( 'NONE',  ( 2.342982756445275427, -1.756855002775299379, -0.9896843009072553432 ) ) ;
#30487=CARTESIAN_POINT ( 'NONE',  ( 5.531250000000004441, -0.7852924748302730906, -1.895863743163958226 ) ) ;
#30489=CARTESIAN_POINT ( 'NONE',  ( 6.604134034941783860, -1.926004669841055339, 0.05029594667986003048 ) ) ;
#30491=CARTESIAN_POINT ( 'NONE',  ( 2.127449211838834398, 1.986592753075850037, 0.9941332784057993477 ) ) ;
#30499=CARTESIAN_POINT ( 'NONE',  ( 5.319757424029775805, 1.030549729363830158, -1.402388650165889095 ) ) ;
#30500=CARTESIAN_POINT ( 'NONE',  ( 3.367582429956605061, -0.3852447139683997657, 1.923494667983568718 ) ) ;
#30505=CARTESIAN_POINT ( 'NONE',  ( 4.727936083913598431, -1.386761530526101405, -1.787517356406182811 ) ) ;
#30506=CARTESIAN_POINT ( 'NONE',  ( 1.592308366680051490, 1.018618965756763473, -1.793563681512408525 ) ) ;
#30508=CARTESIAN_POINT ( 'NONE',  ( 2.272703622300107362, -1.391801132404853147, 1.783687758696401504 ) ) ;
#30511=CARTESIAN_POINT ( 'NONE',  ( 4.059713336928523653, 1.856696190431494475, -0.2264497139414511362 ) ) ;
#30512=CARTESIAN_POINT ( 'NONE',  ( 1.986549370914699963, -1.733795460411426959, 0.04323319158786724514 ) ) ;
#30513=CARTESIAN_POINT ( 'NONE',  ( 6.304242050522723240, 1.625252681175231029, -1.470355468214133543 ) ) ;
#30514=CARTESIAN_POINT ( 'NONE',  ( 6.422925328166578574, 2.149888460833260684, 0.8388895797235284002 ) ) ;
#30515=CARTESIAN_POINT ( 'NONE',  ( 3.643588467267334874, -1.635511012911139650, -1.413612897787956513 ) ) ;
#30516=CARTESIAN_POINT ( 'NONE',  ( 4.382716955277085269, 1.733964400234957459, -0.8745241987923138005 ) ) ;
#30518=CARTESIAN_POINT ( 'NONE',  ( 6.309813054293936574, -1.856383540575656799, 0.2289572138471432372 ) ) ;
#30524=CARTESIAN_POINT ( 'NONE',  ( 6.240861317752083970, 2.010826688392798101, -0.1511364921914087889 ) ) ;
#30528=CARTESIAN_POINT ( 'NONE',  ( 3.035583632137848653, -1.226507576337819483, -1.352503160878690380 ) ) ;
#30535=CARTESIAN_POINT ( 'NONE',  ( 6.305333282589566934, 1.756257216537491450, -0.9971998561906397773 ) ) ;
#30536=CARTESIAN_POINT ( 'NONE',  ( 1.207859650372544280, 1.608047128250057689, 1.382383069919224106 ) ) ;
#30539=CARTESIAN_POINT ( 'NONE',  ( 2.219380450391433168, 0.3239122733160957890, -1.832380290584040505 ) ) ;
#30541=CARTESIAN_POINT ( 'NONE',  ( 6.069226122992825267, 0.1539936439061925788, -2.055202734049704105 ) ) ;
#30542=CARTESIAN_POINT ( 'NONE',  ( 6.363907750917786821, -0.1017471579566435469, -2.013986097687201049 ) ) ;
#30549=CARTESIAN_POINT ( 'NONE',  ( 0.07680821025396293578, 0.7488618828427398011, -1.895266105024134839 ) ) ;
#30551=CARTESIAN_POINT ( 'NONE',  ( 5.905624997962407363, 0.3905408587613137805, 1.977747231101577352 ) ) ;
#30552=CARTESIAN_POINT ( 'NONE',  ( 4.910013284106277354, 1.267360923890372693, -1.335742228452965863 ) ) ;
#30553=CARTESIAN_POINT ( 'NONE',  ( 0.07700591528354748527, 7.629137130509112907, -2.510791685687420838 ) ) ;
#30554=CARTESIAN_POINT ( 'NONE',  ( 3.282123524285113003, 1.463787882210180191, 1.784030387633539938 ) ) ;
#30556=CARTESIAN_POINT ( 'NONE',  ( 6.380167732536218494, -1.162327630155314484, 1.822330041786710098 ) ) ;
#30558=CARTESIAN_POINT ( 'NONE',  ( 0.7670095293261131042, 1.871311197688549699, -0.5191222856946677844 ) ) ;
#30561=CARTESIAN_POINT ( 'NONE',  ( 4.517165314107184138, 2.297965829929650372, -0.05084271438157876577 ) ) ;
#30564=CARTESIAN_POINT ( 'NONE',  ( 4.346470048663173102, 0.4987854378066917116, 1.802870001028591407 ) ) ;
#30566=CARTESIAN_POINT ( 'NONE',  ( 1.511816067030671729, -0.6413169068853613597, 1.801808535584384252 ) ) ;
#30569=CARTESIAN_POINT ( 'NONE',  ( 2.930518499080053907, 1.225513248159842083, -1.835134156090315605 ) ) ;
#30570=CARTESIAN_POINT ( 'NONE',  ( -0.1399997263889594112, -0.002789056014654289761, -2.000146600338557956 ) ) ;
#30575=CARTESIAN_POINT ( 'NONE',  ( 1.475783946021753446, 1.170879755915053666, 1.585848323755238320 ) ) ;
#30576=CARTESIAN_POINT ( 'NONE',  ( 1.712421914926518518, -2.289955115012487052, 0.2841115493098354539 ) ) ;
#30577=CARTESIAN_POINT ( 'NONE',  ( 2.418345249890076154, 0.8361516037145629854, 1.774881043358336630 ) ) ;
#30578=CARTESIAN_POINT ( 'NONE',  ( 5.735237406732953680, -0.04512126716067199617, -2.062225806692425945 ) ) ;
#30585=CARTESIAN_POINT ( 'NONE',  ( 1.059715561420447205, 1.773747297294786307, 1.251667063311131312 ) ) ;
#30590=CARTESIAN_POINT ( 'NONE',  ( 3.004993591039197831, 1.578202713744047303, 1.003818400984110681 ) ) ;
#30591=CARTESIAN_POINT ( 'NONE',  ( 6.380167732536218494, -1.162327630155314484, 1.822330041786710098 ) ) ;
#30592=CARTESIAN_POINT ( 'NONE',  ( -0.02244404828157658613, 5.719765766439059540, -2.783169749654360814 ) ) ;
#30593=CARTESIAN_POINT ( 'NONE',  ( 6.827182134110198142, 0.003888933837258023996, 1.810856214465889069 ) ) ;
#30595=CARTESIAN_POINT ( 'NONE',  ( 2.227084300891319035, 1.708885092217244051, 0.8583199515034346527 ) ) ;
#30596=CARTESIAN_POINT ( 'NONE',  ( 3.660817930519409291, -1.560716028760079421, -0.8345783561882027524 ) ) ;
#30597=CARTESIAN_POINT ( 'NONE',  ( 1.840342752298686380, 1.099902316243700939, -1.564109231055022864 ) ) ;
#30600=CARTESIAN_POINT ( 'NONE',  ( 5.062082326478217098, -1.060395474731326448, 1.595121111449711693 ) ) ;
#30601=CARTESIAN_POINT ( 'NONE',  ( 6.689911425329987615, -1.285551722473629477, -1.492250998650017202 ) ) ;
#30604=CARTESIAN_POINT ( 'NONE',  ( 1.846092968827160119, -1.388944967848893430, -1.602481653760478020 ) ) ;
#30605=CARTESIAN_POINT ( 'NONE',  ( 5.471519871388384360, 1.802534880541529994, -0.5000026934619330454 ) ) ;
#30606=CARTESIAN_POINT ( 'NONE',  ( 0.02954982209854748257, -1.120125052174587577, -1.442194003765177257 ) ) ;
#30608=CARTESIAN_POINT ( 'NONE',  ( 4.723365791888975096, -0.1103408873950258995, 2.204240794804641190 ) ) ;
#30611=CARTESIAN_POINT ( 'NONE',  ( 2.436046450607622926, 1.266989887546982052, 1.627633791282004250 ) ) ;
#30617=CARTESIAN_POINT ( 'NONE',  ( 0.1753634416057497647, 0.2329791690731698173, -2.177930625204091086 ) ) ;
#30619=CARTESIAN_POINT ( 'NONE',  ( 4.229010956685672618, -1.930657356216297860, -0.7480826485904977785 ) ) ;
#30621=CARTESIAN_POINT ( 'NONE',  ( 2.354944161360218224, -1.672559397656541824, 1.369352967626968898 ) ) ;
#30623=CARTESIAN_POINT ( 'NONE',  ( 2.455728411619819251, -1.498007593246965419, -1.354850333784217709 ) ) ;
#30628=FACE_OUTER_BOUND ( 'NONE', #79279, .T. ) ;
#30631=CARTESIAN_POINT ( 'NONE',  ( 0.005092704479254389627, -0.09411098085002241043, 2.014433268766747887 ) ) ;
#30632=CARTESIAN_POINT ( 'NONE',  ( 5.179302069984247581, 1.471482994053765925, 1.624232740060495228 ) ) ;
#30635=CARTESIAN_POINT ( 'NONE',  ( 5.185773951807310489, 1.841398108398510480, -0.5159224025059681029 ) ) ;
#30640=CARTESIAN_POINT ( 'NONE',  ( 2.583611426500437069, -0.6298568260672477992, 1.915607262459443794 ) ) ;
#30643=CARTESIAN_POINT ( 'NONE',  ( 5.262619041473771020, -1.246969283750315460, 1.191858809209481285 ) ) ;
#30648=ORIENTED_EDGE ( 'NONE', *, *, #144753, .T. ) ;
#30649=CARTESIAN_POINT ( 'NONE',  ( 0.7255434793691470929, 0.2065170452952343472, -2.059959488672699290 ) ) ;
#30651=CARTESIAN_POINT ( 'NONE',  ( 4.529823624924778969, -1.775545877285337193, 0.3580350944670795399 ) ) ;
#30654=CARTESIAN_POINT ( 'NONE',  ( 6.498695496729308907, -1.778006411731817060, -0.3456425897902185018 ) ) ;
#30658=CARTESIAN_POINT ( 'NONE',  ( 2.994263412949605296, -0.6367403190770392074, -2.096898073876966251 ) ) ;
#30659=ORIENTED_EDGE ( 'NONE', *, *, #187807, .T. ) ;
#30660=CARTESIAN_POINT ( 'NONE',  ( 0.5901948623465642640, 1.011764341257429978, -1.680720577067334354 ) ) ;
#30662=CARTESIAN_POINT ( 'NONE',  ( 4.939036846723444008, -1.620647644904899654, -1.020970555301304206 ) ) ;
#30669=CARTESIAN_POINT ( 'NONE',  ( 2.044033295145482043, 0.8276103948961744949, -1.997198329219296742 ) ) ;
#30672=CARTESIAN_POINT ( 'NONE',  ( 2.502731746374619259, 1.467688513602287470, -1.085450786651315225 ) ) ;
#30674=CARTESIAN_POINT ( 'NONE',  ( 4.541915102786819425, 0.7800907816924649296, -1.650662693317282770 ) ) ;
#30676=CARTESIAN_POINT ( 'NONE',  ( 2.636851627972558454, 1.802111047976437508, 0.6404684511054498097 ) ) ;
#30678=CARTESIAN_POINT ( 'NONE',  ( 4.158625497742932886, -0.6157697831138170264, -1.870904811771924470 ) ) ;
#30680=CARTESIAN_POINT ( 'NONE',  ( 4.669442277103274641, 1.121057080241712578, 1.585637770727834850 ) ) ;
#30684=CARTESIAN_POINT ( 'NONE',  ( 5.678019686890188211, 2.088907387943875982, -0.3644037002746222664 ) ) ;
#30686=CARTESIAN_POINT ( 'NONE',  ( 3.334525359879161766, 1.211162569113528598, -1.479845612687477496 ) ) ;
#30690=CARTESIAN_POINT ( 'NONE',  ( 6.983263157960362122, 3.696136926403908340, 2.460428995873820135 ) ) ;
#30693=CARTESIAN_POINT ( 'NONE',  ( 5.356112940025661295, 0.8138243144468767509, -1.841424879227879119 ) ) ;
#30695=CARTESIAN_POINT ( 'NONE',  ( 4.775911370473768791, 1.053640644303525331, 1.490772598166143048 ) ) ;
#30696=CARTESIAN_POINT ( 'NONE',  ( 0.5903903138861701372, 1.065687334306382184, -1.774900233272216798 ) ) ;
#30701=CARTESIAN_POINT ( 'NONE',  ( 5.735183426005796115, -1.690533149647139410, 0.8011652756413772947 ) ) ;
#30710=CARTESIAN_POINT ( 'NONE',  ( 1.832961912758425349, -1.964510197511709189, -0.6532998099852762586 ) ) ;
#30711=CARTESIAN_POINT ( 'NONE',  ( 2.302504360600155842, 1.380385731239835323, -1.605472654339132887 ) ) ;
#30714=CARTESIAN_POINT ( 'NONE',  ( 0.2507523796677147421, -0.4231762011769435450, -1.930160340004604569 ) ) ;
#30719=CARTESIAN_POINT ( 'NONE',  ( 2.836170770286027043, 2.275064633363361732, 0.2797384389828549978 ) ) ;
#30720=CARTESIAN_POINT ( 'NONE',  ( 1.031563979315492485, -1.156294252604734396, -1.412831148817683680 ) ) ;
#30721=CARTESIAN_POINT ( 'NONE',  ( 2.390748813209525814, -1.831196095803063528, -0.5514187292172747501 ) ) ;
#30725=CARTESIAN_POINT ( 'NONE',  ( 1.582290772395946066, 1.038639357175192401, 1.724485448976780688 ) ) ;
#30726=CARTESIAN_POINT ( 'NONE',  ( 0.6901946996495964548, 1.013433542811643440, -1.679602092450118489 ) ) ;
#30730=CARTESIAN_POINT ( 'NONE',  ( 4.259774723613071856, 0.9852665271268057356, 1.843911019796584450 ) ) ;
#30731=CARTESIAN_POINT ( 'NONE',  ( 3.924454612484959082, 1.680539001619888229, 0.5552615287828834845 ) ) ;
#30734=CARTESIAN_POINT ( 'NONE',  ( 0.09403522832084068583, -2.191061582759439297, -0.04926842934906834615 ) ) ;
#30735=CARTESIAN_POINT ( 'NONE',  ( 4.540767487494163035, -1.347652659646558115, -1.101159657664248170 ) ) ;
#30739=CARTESIAN_POINT ( 'NONE',  ( 4.973871655188280450, 1.509253006592145452, 0.8532917887605420137 ) ) ;
#30740=CARTESIAN_POINT ( 'NONE',  ( 5.020078820186387070, 2.148262114505914866, -0.3138009609788168230 ) ) ;
#30742=CARTESIAN_POINT ( 'NONE',  ( 5.366422816783521732, -1.968444216653497003, -0.4370823996120917765 ) ) ;
#30743=CARTESIAN_POINT ( 'NONE',  ( 6.187500000000010658, -1.451031289060719320, 1.451031289061361473 ) ) ;
#30745=CARTESIAN_POINT ( 'NONE',  ( 2.696214026845968448, -1.921097006559132625, -0.1437054574915888616 ) ) ;
#30747=CARTESIAN_POINT ( 'NONE',  ( 6.416288448142412726, -2.220950948806613034, 0.05311210701240512422 ) ) ;
#30749=CARTESIAN_POINT ( 'NONE',  ( 6.883263157960366918, 2.433703524355503411, 2.428201320676713237 ) ) ;
#30752=CARTESIAN_POINT ( 'NONE',  ( 1.770501988737150922, 2.215049892327343173, -0.1675478377428234744 ) ) ;
#30753=CARTESIAN_POINT ( 'NONE',  ( 6.549272904993657995, 1.707534169505098953, -0.9658701945045379267 ) ) ;
#30761=CARTESIAN_POINT ( 'NONE',  ( 5.055161771162819839, 1.716784339331741682, -1.143088790766825236 ) ) ;
#30766=CARTESIAN_POINT ( 'NONE',  ( 6.626239551081194001, 1.076695052409048614, -1.529385127534782951 ) ) ;
#30767=CARTESIAN_POINT ( 'NONE',  ( 5.432138663567621428, -1.371958567392589146, -1.060553414760868618 ) ) ;
#30768=CARTESIAN_POINT ( 'NONE',  ( 4.493551464656197147, -1.740228352261258049, -0.03666429755099299970 ) ) ;
#30771=CARTESIAN_POINT ( 'NONE',  ( 2.912002956782848262, -1.132189443809348273, -1.993217883792548495 ) ) ;
#30773=CARTESIAN_POINT ( 'NONE',  ( 1.060217833243476182, -1.663605802054025418, -0.7890760572396152694 ) ) ;
#30776=CARTESIAN_POINT ( 'NONE',  ( 2.326929888710258965, -0.002694909042751796133, 1.825762228105472840 ) ) ;
#30777=CARTESIAN_POINT ( 'NONE',  ( 3.111954093273407107, 0.05229746705895028935, 2.015912966248374349 ) ) ;
#30778=CARTESIAN_POINT ( 'NONE',  ( 1.342011898504836820, 2.189069585219292957, 0.1046993245200772138 ) ) ;
#30780=CARTESIAN_POINT ( 'NONE',  ( 4.383879424978657902, 1.373869114255725776, 1.596202613037283502 ) ) ;
#30783=CARTESIAN_POINT ( 'NONE',  ( 1.469279758060073160, 1.824989553406907383, 0.9776941847434923449 ) ) ;
#30786=CARTESIAN_POINT ( 'NONE',  ( 3.721430941620011534, 1.819509361161365524, 1.088713516244857571 ) ) ;
#30787=CARTESIAN_POINT ( 'NONE',  ( 6.164658409365947556, -1.287482145768016339, 1.294691480910937775 ) ) ;
#30794=CARTESIAN_POINT ( 'NONE',  ( 3.111586589114573975, 1.594763109418888991, 1.239388640070989478 ) ) ;
#30795=CARTESIAN_POINT ( 'NONE',  ( 0.7980485993467776318, -0.7579980429349441051, 1.964993406121709807 ) ) ;
#30798=CARTESIAN_POINT ( 'NONE',  ( 5.049569799528213387, 1.377159375265882391, 1.251766951177714526 ) ) ;
#30804=CARTESIAN_POINT ( 'NONE',  ( 2.084357000244409175, 1.132115006494602394, -1.602057852124554316 ) ) ;
#30805=CARTESIAN_POINT ( 'NONE',  ( 0.7784641540938314064, -1.199969256800371697, 1.797863220954009966 ) ) ;
#30809=CARTESIAN_POINT ( 'NONE',  ( 2.811537702714523856, -1.443443483380968173, 0.9601682615991720127 ) ) ;
#30810=CARTESIAN_POINT ( 'NONE',  ( 1.921426573741076727, 1.003422016191083399, -1.421716384592019544 ) ) ;
#30812=CARTESIAN_POINT ( 'NONE',  ( 0.2359759974720798681, -2.107749471535870445, 0.9397143452993106383 ) ) ;
#30815=CARTESIAN_POINT ( 'NONE',  ( 2.970052003254409545, 1.099468894914462647, 1.742775920482849905 ) ) ;
#30817=CARTESIAN_POINT ( 'NONE',  ( 1.124374798274978104, 0.3960433595797500095, -1.976652716225081097 ) ) ;
#30818=CARTESIAN_POINT ( 'NONE',  ( 6.925078400183553029, 0.5745968962584145912, 2.096956839219825230 ) ) ;
#30820=CARTESIAN_POINT ( 'NONE',  ( 1.639464495141579770, -1.426599704724445861, -1.360921036830293307 ) ) ;
#30822=CARTESIAN_POINT ( 'NONE',  ( 4.535362393419643645, -0.08824616237496611670, 1.910463848342447202 ) ) ;
#30828=CARTESIAN_POINT ( 'NONE',  ( 1.067063705314938771, -1.590654782179411031, 1.244411004956039291 ) ) ;
#30830=CARTESIAN_POINT ( 'NONE',  ( 4.542184868284099508, 0.9910628492805847456, -2.084066998532303483 ) ) ;
#30831=CARTESIAN_POINT ( 'NONE',  ( 6.303176765056641706, -1.658072099422291057, 1.048360225930293321 ) ) ;
#30832=CARTESIAN_POINT ( 'NONE',  ( 2.324987154519737143, -1.791562868964852395, -0.7996954790665599111 ) ) ;
#30836=CARTESIAN_POINT ( 'NONE',  ( 0.8841682305550628840, -2.117513412274423690, 0.006320426156874307463 ) ) ;
#30839=CARTESIAN_POINT ( 'NONE',  ( 1.025062291269123405, -1.166378923895025510, -1.424538887614942739 ) ) ;
#30841=CARTESIAN_POINT ( 'NONE',  ( 4.575155497752975364, 1.982410897724752319, 0.8856408146403412784 ) ) ;
#30843=CARTESIAN_POINT ( 'NONE',  ( 1.617596980227502756, 1.765956010477184535, 1.173731981927571555 ) ) ;
#30847=CARTESIAN_POINT ( 'NONE',  ( 3.022786435837477637, 1.939216523002813997, 0.6976457746366692136 ) ) ;
#30849=CARTESIAN_POINT ( 'NONE',  ( 0.5910386730991653570, -0.6632029860377097741, 1.717849102829023922 ) ) ;
#30851=CARTESIAN_POINT ( 'NONE',  ( -0.02244404828160087226, 1.995160441984781041, -2.602654351998904492 ) ) ;
#30855=CARTESIAN_POINT ( 'NONE',  ( 1.827766392559232012, -2.130618655838847353, 0.7612957800654009954 ) ) ;
#30857=CARTESIAN_POINT ( 'NONE',  ( 3.005918303229858424, -0.7299923727487073188, 1.658169170237313583 ) ) ;
#30858=CARTESIAN_POINT ( 'NONE',  ( 2.413182783470344983, -1.785834301256707723, 0.6938157933340273198 ) ) ;
#30859=CARTESIAN_POINT ( 'NONE',  ( 3.596198176508007105, 0.9334358170956689182, -1.848091447891623051 ) ) ;
#30861=CARTESIAN_POINT ( 'NONE',  ( 1.832829291326312005, 0.1914625595707402927, 1.962137882790424559 ) ) ;
#30862=CARTESIAN_POINT ( 'NONE',  ( 6.568979851886898480, -1.762530817088540758, -0.7781539781668064260 ) ) ;
#30863=CARTESIAN_POINT ( 'NONE',  ( 2.922558825391399662, 1.760836971185793187, 0.6318509464167121337 ) ) ;
#30864=CARTESIAN_POINT ( 'NONE',  ( 0.8390048429645606820, 2.274487955075610301, 0.3892829850337137243 ) ) ;
#30866=CARTESIAN_POINT ( 'NONE',  ( 2.295144308211858331, -1.664110045376477443, 0.8333370299275147941 ) ) ;
#30868=CARTESIAN_POINT ( 'NONE',  ( 5.617653825673187384, 0.4058615334493093085, -2.022196393678155957 ) ) ;
#30872=CARTESIAN_POINT ( 'NONE',  ( 6.510775453876758156, 1.563058401041140133, -1.411553977168745977 ) ) ;
#30874=CARTESIAN_POINT ( 'NONE',  ( 6.292270065666691892, -2.150519007954437622, -0.2187886337903441336 ) ) ;
#30875=CARTESIAN_POINT ( 'NONE',  ( 0.6437974683802077935, 0.5340323341261629109, 1.762076181610471526 ) ) ;
#30876=CARTESIAN_POINT ( 'NONE',  ( 5.320965550519270337, 1.527853097053995191, -1.320967980168601175 ) ) ;
#30883=CARTESIAN_POINT ( 'NONE',  ( 4.979703994296570180, -0.7212954316567052881, 1.883311551353183511 ) ) ;
#30889=CARTESIAN_POINT ( 'NONE',  ( 5.489210439962995736, 1.908424935776025455, -1.015307555102950010 ) ) ;
#30895=CARTESIAN_POINT ( 'NONE',  ( 5.976185453469534892, -2.006962702346287930, -0.1948244327795861652 ) ) ;
#30897=CARTESIAN_POINT ( 'NONE',  ( 2.191662871657253486, -0.7386692205221119245, 1.558845181661876467 ) ) ;
#30903=CARTESIAN_POINT ( 'NONE',  ( 6.919227945209173392, -0.1346273106918663420, 1.840389347376285345 ) ) ;
#30905=CARTESIAN_POINT ( 'NONE',  ( 1.383448652483735941, 0.1460618955802815977, -2.007835497447094664 ) ) ;
#30907=CARTESIAN_POINT ( 'NONE',  ( 2.802037382575186975, -0.6933082239683820980, 2.095089865402133267 ) ) ;
#30909=CARTESIAN_POINT ( 'NONE',  ( 4.979425714853139340, -0.1133551455631234828, 2.168255935233906584 ) ) ;
#30912=CARTESIAN_POINT ( 'NONE',  ( 3.053504691927158898, -1.869126254513186591, 1.001442229663196182 ) ) ;
#30913=CARTESIAN_POINT ( 'NONE',  ( 1.458611474731505986, -1.915607644094442064, -0.6298556652749933704 ) ) ;
#30914=CARTESIAN_POINT ( 'NONE',  ( 2.126969254794884634, 1.619647995875729496, 0.8116002879420233240 ) ) ;
#30919=CARTESIAN_POINT ( 'NONE',  ( 1.129944905810562839, 1.913687095308055808, 0.09034645858918381733 ) ) ;
#30926=CARTESIAN_POINT ( 'NONE',  ( 4.786082296487640164, -1.021991182799499409, 1.904868704497929333 ) ) ;
#30929=CARTESIAN_POINT ( 'NONE',  ( 2.127334043950947606, 1.896359100603739911, 0.9491756072362851349 ) ) ;
#30932=CARTESIAN_POINT ( 'NONE',  ( 3.620352162249322880, 1.253078330817010588, -1.521826374184510389 ) ) ;
#30933=CARTESIAN_POINT ( 'NONE',  ( 5.308822938259078583, -0.4706598425541131947, -1.853433239416848455 ) ) ;
#30936=CARTESIAN_POINT ( 'NONE',  ( 0.7134375191242479097, -1.748147108003229810, -1.108949491591210146 ) ) ;
#30937=CARTESIAN_POINT ( 'NONE',  ( 2.009616874778739071, -0.9155987108000520625, -1.712560621339030309 ) ) ;
#30942=CARTESIAN_POINT ( 'NONE',  ( 2.484421436082083101, -0.3582009261528392163, -2.059553721446294894 ) ) ;
#30945=CARTESIAN_POINT ( 'NONE',  ( 5.760397938718036848, 1.910310778393434106, 0.08934430699411573251 ) ) ;
#30947=CARTESIAN_POINT ( 'NONE',  ( 4.846401659255799466, 2.200796399388889935, 0.1645688927329121420 ) ) ;
#30949=CARTESIAN_POINT ( 'NONE',  ( 2.643839551151895506, -1.634601560588926583, -1.482707865360691990 ) ) ;
#30952=CARTESIAN_POINT ( 'NONE',  ( 1.541514448083292965, -1.800223203088219481, 0.6453159242577054533 ) ) ;
#30955=CARTESIAN_POINT ( 'NONE',  ( 4.369627354678314646, -0.3570511267821044332, 2.039192500141631115 ) ) ;
#30957=CARTESIAN_POINT ( 'NONE',  ( 1.358524781292804517, 0.8764843271744371389, 1.976213614152767750 ) ) ;
#30958=CARTESIAN_POINT ( 'NONE',  ( 3.210657068901449307, 1.982179491636561819, 0.9350799695589939731 ) ) ;
#30966=CARTESIAN_POINT ( 'NONE',  ( -0.1341500063891595818, -0.1486117279969369209, -1.983907055413631992 ) ) ;
#30968=CARTESIAN_POINT ( 'NONE',  ( 4.592674910654532816, 2.029287475768901228, 0.4089837765668055680 ) ) ;
#30969=CARTESIAN_POINT ( 'NONE',  ( 3.123571566491334384, -1.856553849623356234, 0.5141669907481066781 ) ) ;
#30970=CARTESIAN_POINT ( 'NONE',  ( 6.222275945484236459, 2.094208529755392068, 0.3105017025616888526 ) ) ;
#30973=CARTESIAN_POINT ( 'NONE',  ( 4.065260974683176265, 1.686948271169801616, 1.016115061114295504 ) ) ;
#30974=CARTESIAN_POINT ( 'NONE',  ( 5.718756930148481743, -0.06150597819632765140, 2.291595365457484323 ) ) ;
#30975=CARTESIAN_POINT ( 'NONE',  ( 4.107882937833263526, -1.820653182827164596, 0.1363937739093170898 ) ) ;
#30981=CARTESIAN_POINT ( 'NONE',  ( 1.698526806778306586, 1.531337151408303621, 1.022036240780115346 ) ) ;
#30982=CARTESIAN_POINT ( 'NONE',  ( 5.027594669734884114, -0.2912581947275821315, 1.991892893239319617 ) ) ;
#30983=CARTESIAN_POINT ( 'NONE',  ( 6.258407524398033495, 2.201109419358293628, -0.6625764064998507230 ) ) ;
#30984=CARTESIAN_POINT ( 'NONE',  ( 5.594571816639393624, 1.932094781187740917, 0.3390067100078468232 ) ) ;
#30989=CARTESIAN_POINT ( 'NONE',  ( 1.206708187092224716, 1.845608279032302512, 0.9822807542516975854 ) ) ;
#30990=CARTESIAN_POINT ( 'NONE',  ( 0.5845639792326964290, -0.2246964894469481722, -1.857040431621145959 ) ) ;
#30992=CARTESIAN_POINT ( 'NONE',  ( 5.665949523032352886, -1.230194547739250854, 1.502597557546548446 ) ) ;
#30993=CARTESIAN_POINT ( 'NONE',  ( -0.1102773484823937195, 1.994803768489497031, -2.617422746694163749 ) ) ;
#30994=CARTESIAN_POINT ( 'NONE',  ( 1.452286687950472999, -1.492487064643189809, -0.8950295028009451759 ) ) ;
#30997=CARTESIAN_POINT ( 'NONE',  ( 1.365380774817010368, 1.699871498885496379, -0.2916373863959387802 ) ) ;
#30998=CARTESIAN_POINT ( 'NONE',  ( 1.892365914234435120, -0.5883382831698009685, -2.111031122750434808 ) ) ;
#30999=CARTESIAN_POINT ( 'NONE',  ( 4.424592250794217030, 1.359014646446855767, -1.738718759629574118 ) ) ;
#31002=CARTESIAN_POINT ( 'NONE',  ( 1.253040875654364505, -0.5252153140962511069, -2.106489908942406952 ) ) ;
#31003=CARTESIAN_POINT ( 'NONE',  ( 0.2932112110246976044, 1.350478442433366677, 1.228755397233910696 ) ) ;
#31004=CARTESIAN_POINT ( 'NONE',  ( 2.536447107014605962, 0.7179835868570243473, 1.991995636484017673 ) ) ;
#31007=CARTESIAN_POINT ( 'NONE',  ( 2.472590379642979563, -2.194723544211283350, -0.6619992606377905764 ) ) ;
#31011=CARTESIAN_POINT ( 'NONE',  ( 4.494933454782477078, -2.154585855983886411, -0.5399016382821394400 ) ) ;
#31018=CARTESIAN_POINT ( 'NONE',  ( 2.461564753630896440, -1.930417925741171103, -0.5826551686555282439 ) ) ;
#31020=CARTESIAN_POINT ( 'NONE',  ( 1.938405323705337135, -1.106995438288145950, 1.740174596247965555 ) ) ;
#31025=CARTESIAN_POINT ( 'NONE',  ( 5.578137875217415775, -2.137416510240647494, -0.4829537091169676666 ) ) ;
#31026=CARTESIAN_POINT ( 'NONE',  ( 2.145157927413956944, 0.8647252629472859109, 1.821741647932619390 ) ) ;
#31027=CARTESIAN_POINT ( 'NONE',  ( 1.645803748337611783, 0.5784278848013635344, 1.748079663633335334 ) ) ;
#31031=CARTESIAN_POINT ( 'NONE',  ( 5.719710266082651096, -1.780569991979109590, 0.4021758204828808081 ) ) ;
#31032=CARTESIAN_POINT ( 'NONE',  ( 5.520157785563180930, -1.821743191724470634, 0.8647220171385738841 ) ) ;
#31034=CARTESIAN_POINT ( 'NONE',  ( 5.647450836711301214, -1.779752484188871886, -1.396855495411459147 ) ) ;
#31036=CARTESIAN_POINT ( 'NONE',  ( 0.6453166446471610973, -1.805311040884694185, 1.084365637629558954 ) ) ;
#31038=CARTESIAN_POINT ( 'NONE',  ( 4.281733463571851139, -1.982135700070002615, 0.5980053909793592304 ) ) ;
#31046=CARTESIAN_POINT ( 'NONE',  ( 1.635180430577408028, 1.980530345366804834, 0.7584260845197098311 ) ) ;
#31047=CARTESIAN_POINT ( 'NONE',  ( 3.322728300399055534, -0.9034660432867666069, -2.029577789741637162 ) ) ;
#31051=CARTESIAN_POINT ( 'NONE',  ( 2.682025323810240280, -1.127217178123595565, -1.605522638798158264 ) ) ;
#31057=CARTESIAN_POINT ( 'NONE',  ( 1.881254504445781794, -1.940830296247602949, -0.8548571619346673200 ) ) ;
#31059=CARTESIAN_POINT ( 'NONE',  ( 4.188458007013862172, -2.137797052781073237, -0.3198388112101158143 ) ) ;
#31060=CARTESIAN_POINT ( 'NONE',  ( 3.386116603743833497, -0.3623624896987760469, -1.805063595765175499 ) ) ;
#31064=CARTESIAN_POINT ( 'NONE',  ( 5.701030997009290502, -0.4167664840721523878, 1.689554919747728423 ) ) ;
#31065=CARTESIAN_POINT ( 'NONE',  ( 6.727182134110193168, 4.701113012587437190, 2.373661997258198486 ) ) ;
#31067=CARTESIAN_POINT ( 'NONE',  ( 2.588937169860201504, -0.3686131662095324946, -2.129881858774537395 ) ) ;
#31069=CARTESIAN_POINT ( 'NONE',  ( 4.077499844852236599, 1.427718728413525318, -1.423743541103118737 ) ) ;
#31071=CARTESIAN_POINT ( 'NONE',  ( 2.870174731959000525, 1.155358403710282866, 1.826860881501219280 ) ) ;
#31072=CARTESIAN_POINT ( 'NONE',  ( 2.882053135459626159, -1.016639628983921684, 1.688880165396142718 ) ) ;
#31073=CARTESIAN_POINT ( 'NONE',  ( 2.940638933469359895, -1.523795050681177710, 1.320827213682006285 ) ) ;
#31075=CARTESIAN_POINT ( 'NONE',  ( 6.509000000000011887, 2.430396405248925529, 2.482145556523357222 ) ) ;
#31076=CARTESIAN_POINT ( 'NONE',  ( 4.476081132534933893, -1.884639481945263872, -0.4683437986269470277 ) ) ;
#31084=ORIENTED_EDGE ( 'NONE', *, *, #4355, .F. ) ;
#31086=CARTESIAN_POINT ( 'NONE',  ( 1.272829778695073299, -1.399090282553701270, 1.706552004499435560 ) ) ;
#31088=CARTESIAN_POINT ( 'NONE',  ( 5.559412779221331924, 1.601624451964112739, 1.132529127964493121 ) ) ;
#31093=CARTESIAN_POINT ( 'NONE',  ( 0.07499057489264349119, 0.2503043380940940810, -1.990932473338621778 ) ) ;
#31094=CARTESIAN_POINT ( 'NONE',  ( 4.716662652015527257, -0.08744826293657045890, 1.839185557975311580 ) ) ;
#31099=CARTESIAN_POINT ( 'NONE',  ( 4.992489932941452935, -1.175987964647656536, 1.764448611491518548 ) ) ;
#31102=CARTESIAN_POINT ( 'NONE',  ( 6.907514182033759553, -0.4531076517439984186, 2.017496682098403937 ) ) ;
#31104=CARTESIAN_POINT ( 'NONE',  ( 2.242426168690789368, -1.824373289281261634, -0.3667376154973446267 ) ) ;
#31105=CARTESIAN_POINT ( 'NONE',  ( 3.263068207883256466, 1.795673413606920565, -0.4063787724192802209 ) ) ;
#31110=CARTESIAN_POINT ( 'NONE',  ( 3.211752199052122503, -0.4303563718574507369, 2.164345902561148005 ) ) ;
#31111=CARTESIAN_POINT ( 'NONE',  ( 6.116559975520791781, 1.526041019664432508, -1.670398689176689544 ) ) ;
#31113=CARTESIAN_POINT ( 'NONE',  ( 5.695527492674265169, 1.670499194714653468, -0.7014341174245084520 ) ) ;
#31114=CARTESIAN_POINT ( 'NONE',  ( 5.190618481123168593, 1.446159319891277661, -1.256491027437984354 ) ) ;
#31117=CARTESIAN_POINT ( 'NONE',  ( 6.069203928793593050, 0.1358119448514639727, -1.865795782587629681 ) ) ;
#31118=CARTESIAN_POINT ( 'NONE',  ( 5.652756593210860103, -0.4525561148686143009, -1.805067620203390177 ) ) ;
#31120=CARTESIAN_POINT ( 'NONE',  ( 6.684453129459355658, -1.736675761049325972, -0.3400495950729911510 ) ) ;
#31121=CARTESIAN_POINT ( 'NONE',  ( 1.393767942625488532, -2.000731169080074423, 0.2516357431460446992 ) ) ;
#31123=CARTESIAN_POINT ( 'NONE',  ( 2.877667905955140437, 1.999614821268459020, -0.6613089454029356107 ) ) ;
#31128=CARTESIAN_POINT ( 'NONE',  ( 3.410420005539113841, -2.017668111602511694, -0.09479391224248739922 ) ) ;
#31131=CARTESIAN_POINT ( 'NONE',  ( 3.110779230992101407, 1.568002374463087989, -1.488160049990403078 ) ) ;
#31132=CARTESIAN_POINT ( 'NONE',  ( 6.610000000000011866, 2.967812824040619191, 2.453181572820534395 ) ) ;
#31139=CARTESIAN_POINT ( 'NONE',  ( 1.751786407749492014, 2.185395279939935431, -0.1653414253460702699 ) ) ;
#31141=CARTESIAN_POINT ( 'NONE',  ( 2.325404209529509103, -2.741642530189327160E-05, 2.262689075223401236 ) ) ;
#31149=CARTESIAN_POINT ( 'NONE',  ( 3.338855477594515175, -1.562335520734370320, 0.8312421073871211208 ) ) ;
#31151=CARTESIAN_POINT ( 'NONE',  ( 6.352570083819033542, 0.6862697483850827007, 2.097430819677794656 ) ) ;
#31154=CARTESIAN_POINT ( 'NONE',  ( 4.921500000981174239, -1.427949280599305482, -1.423951169029838315 ) ) ;
#31155=ORIENTED_EDGE ( 'NONE', *, *, #194375, .F. ) ;
#31156=CARTESIAN_POINT ( 'NONE',  ( 3.414787578387419309, 1.690673485743508619, 0.8009127983473337542 ) ) ;
#31158=CARTESIAN_POINT ( 'NONE',  ( 3.414952709633051864, -1.570776679111930640, 1.348709175982481856 ) ) ;
#31164=CARTESIAN_POINT ( 'NONE',  ( 1.406358598101828283, -1.903450966454448334, -0.1843715739238485085 ) ) ;
#31165=CARTESIAN_POINT ( 'NONE',  ( 2.365611650783586040, -0.4327418640146083462, 1.913375882425945917 ) ) ;
#31166=CARTESIAN_POINT ( 'NONE',  ( 1.317732270343049183, -1.591076063098846527, 1.238129638497114549 ) ) ;
#31170=CARTESIAN_POINT ( 'NONE',  ( 6.714144427970111906, -0.9273952116407166990, -1.739565242892411545 ) ) ;
#31172=CARTESIAN_POINT ( 'NONE',  ( 2.179941694947628683, 1.973542599225884153, -0.3968540688959447116 ) ) ;
#31174=CARTESIAN_POINT ( 'NONE',  ( 2.513409721704229494, -1.974398269817168483, 0.7648893725459534609 ) ) ;
#31176=CARTESIAN_POINT ( 'NONE',  ( 3.314952806421948672, -1.569539724514938950, 1.350292352848787569 ) ) ;
#31178=CARTESIAN_POINT ( 'NONE',  ( 5.753879374300719718, 0.8463200818398952663, 1.911864941374420201 ) ) ;
#31180=CARTESIAN_POINT ( 'NONE',  ( 3.961776442328440506, 1.811803316853294765, -0.2231971713724384965 ) ) ;
#31185=CARTESIAN_POINT ( 'NONE',  ( 6.493228066955544442, 1.923254169853494178, -1.081975473724585912 ) ) ;
#31188=CARTESIAN_POINT ( 'NONE',  ( 4.811142580195256535, 1.587781804131962682, -1.065416552848017284 ) ) ;
#31194=CARTESIAN_POINT ( 'NONE',  ( 0.8195642880178370948, 1.096917009463085790, -1.478703137254427924 ) ) ;
#31199=CARTESIAN_POINT ( 'NONE',  ( 4.727732462671866642, -1.149354582003499159, -1.475719300151681512 ) ) ;
#31206=CARTESIAN_POINT ( 'NONE',  ( 1.199983893365302201, 0.8030756602186311932, -1.798478550607261583 ) ) ;
#31207=CARTESIAN_POINT ( 'NONE',  ( 2.601185598297011570, -0.1948207814224910128, 2.006963067508853005 ) ) ;
#31211=CARTESIAN_POINT ( 'NONE',  ( 2.168174125648382411, -1.346884454587377711, 1.728604079486287137 ) ) ;
#31220=CARTESIAN_POINT ( 'NONE',  ( 4.423293856316495187, -1.136390847421838490, -1.448631019334602144 ) ) ;
#31221=CARTESIAN_POINT ( 'NONE',  ( 1.998691314347844417, -1.974684511280549559, -0.3905480285893418446 ) ) ;
#31222=CARTESIAN_POINT ( 'NONE',  ( 2.864987100074483539, -0.7226686165877260759, 2.181857903572166801 ) ) ;
#31224=CARTESIAN_POINT ( 'NONE',  ( 1.744728380183872218, -0.2665191970635071295, -1.841615994452956873 ) ) ;
#31227=CARTESIAN_POINT ( 'NONE',  ( 5.168181644781757456, 1.909928461159452251, -0.09994665148223277895 ) ) ;
#31230=CARTESIAN_POINT ( 'NONE',  ( 4.704676425016507402, 1.819892833079386651, 1.028999879293402531 ) ) ;
#31231=CARTESIAN_POINT ( 'NONE',  ( 3.203821283898714345, -1.868584281295191607, 0.09040415888627445495 ) ) ;
#31234=CARTESIAN_POINT ( 'NONE',  ( 5.741722636381445533, 1.839460222191912964, 0.08393339073512617876 ) ) ;
#31237=CARTESIAN_POINT ( 'NONE',  ( 4.846200500028392533, 1.720618765505038006, 0.1221847348328516936 ) ) ;
#31241=SURFACE_SIDE_STYLE ('',( #95187 ) ) ;
#31242=CARTESIAN_POINT ( 'NONE',  ( 4.504835797669192843, 0.5730007755406724135, 2.094059341655955198 ) ) ;
#31243=CARTESIAN_POINT ( 'NONE',  ( 3.369579884941567016, 1.780956498284639533, -0.4009276245297774266 ) ) ;
#31244=CARTESIAN_POINT ( 'NONE',  ( 1.252704021237858401, -0.4712815170893420724, -1.904206577484176321 ) ) ;
#31245=CARTESIAN_POINT ( 'NONE',  ( 5.612555052430599822, 2.041346303960121400, 0.5620598648080311621 ) ) ;
#31248=CARTESIAN_POINT ( 'NONE',  ( 6.269073568569841548, 2.194993726949866719, -0.6609628413071825248 ) ) ;
#31253=CARTESIAN_POINT ( 'NONE',  ( 2.051582899450168362, -1.892833867889589960, 0.9560217657286762538 ) ) ;
#31257=CARTESIAN_POINT ( 'NONE',  ( 6.051681997923831879, 1.638823605779341053, 1.424080724270002873 ) ) ;
#31258=CARTESIAN_POINT ( 'NONE',  ( 6.883263157960358924, 4.692138088316172073, 2.616388454592593504 ) ) ;
#31260=CARTESIAN_POINT ( 'NONE',  ( 2.895431823567701457, -0.1657752626464791268, -2.215182847160178881 ) ) ;
#31262=CARTESIAN_POINT ( 'NONE',  ( 6.574846728087075931, -0.8593996854794653251, 1.822268861383633531 ) ) ;
#31264=CARTESIAN_POINT ( 'NONE',  ( 5.682507089483013196, 1.232960659210121879, -1.653321649057968967 ) ) ;
#31269=CARTESIAN_POINT ( 'NONE',  ( 0.1333542156527321720, 1.344858830485482937, -2.298444861300387387 ) ) ;
#31270=CARTESIAN_POINT ( 'NONE',  ( 5.583513413114173041, -0.8223277247318347971, 1.647484189299788682 ) ) ;
#31273=CARTESIAN_POINT ( 'NONE',  ( 1.518105509412637444, 1.162241833864360974, -1.274548180342775838 ) ) ;
#31274=CARTESIAN_POINT ( 'NONE',  ( 1.323454262349359922, -1.463929862531297976, -1.387097294446783868 ) ) ;
#31275=CARTESIAN_POINT ( 'NONE',  ( 1.530362799304554100, -1.938799508460651522, 1.234721073783265233 ) ) ;
#31277=CARTESIAN_POINT ( 'NONE',  ( 2.179354884421313088, -0.1095372306593382361, -2.259850278934079970 ) ) ;
#31278=CARTESIAN_POINT ( 'NONE',  ( 4.195997148085639061, -0.8063668458072065226, 1.945788449171739876 ) ) ;
#31280=CARTESIAN_POINT ( 'NONE',  ( 2.090717947541526289, 1.542569122296926221, -0.8672550169683733712 ) ) ;
#31285=CARTESIAN_POINT ( 'NONE',  ( 5.888988880356018640, -2.109219445749145994, -0.6973366327849057633 ) ) ;
#31286=CARTESIAN_POINT ( 'NONE',  ( 3.574349206294104242, -2.111947977397998777, -0.5846811180381800144 ) ) ;
#31290=CARTESIAN_POINT ( 'NONE',  ( 6.481110812017948142, -1.938455339442773706, -0.8599551062365147214 ) ) ;
#31294=CARTESIAN_POINT ( 'NONE',  ( 6.275647701495586261, 0.3610785225884837746, -2.089460823871174266 ) ) ;
#31296=ORIENTED_EDGE ( 'NONE', *, *, #69557, .F. ) ;
#31300=CARTESIAN_POINT ( 'NONE',  ( 6.462460624273299814, -1.686435539877573220, -0.7394478613861471539 ) ) ;
#31304=CARTESIAN_POINT ( 'NONE',  ( 2.137881509367345778, 0.3822841233627124469, 1.697745509426834332 ) ) ;
#31307=CARTESIAN_POINT ( 'NONE',  ( 6.438358464623771482, 2.137424745569570295, 0.3223339197731683869 ) ) ;
#31310=CARTESIAN_POINT ( 'NONE',  ( 5.998930166150279852, 1.769978137569449883, -1.240765152474863520 ) ) ;
#31314=CARTESIAN_POINT ( 'NONE',  ( 6.239525796224010712, -1.426203020326064275, -1.361167568813693718 ) ) ;
#31315=CARTESIAN_POINT ( 'NONE',  ( 5.343005094570719038, -0.9615459055183853687, 1.442522970604209531 ) ) ;
#31318=CARTESIAN_POINT ( 'NONE',  ( 2.191216702865448784, 1.696344223602393786, 1.387594652289561248 ) ) ;
#31319=CARTESIAN_POINT ( 'NONE',  ( 3.522812192065057690, 1.465757825172078865, -1.782263946013421974 ) ) ;
#31321=CARTESIAN_POINT ( 'NONE',  ( 6.028604891774052454, 1.984808026635048961, 0.5540661066990509864 ) ) ;
#31322=CARTESIAN_POINT ( 'NONE',  ( 1.464679669172624488, 0.1433081720705318696, -1.936712990118959032 ) ) ;
#31327=CARTESIAN_POINT ( 'NONE',  ( 4.183913158364858553, 2.056144659531285779, -0.5182805708664262045 ) ) ;
#31328=CARTESIAN_POINT ( 'NONE',  ( 1.899064777474347654, -0.9530127170578571727, -1.777010740487514173 ) ) ;
#31330=CARTESIAN_POINT ( 'NONE',  ( 5.051906976816819217, 0.6964463896041681590, -2.094057263239030853 ) ) ;
#31333=CARTESIAN_POINT ( 'NONE',  ( 0.02954982209854748257, -1.120125052174587577, -1.442194003765177257 ) ) ;
#31339=CARTESIAN_POINT ( 'NONE',  ( 4.293860741714614626, -0.7905101867788848491, 1.903454510683154188 ) ) ;
#31342=UNCERTAINTY_MEASURE_WITH_UNIT (LENGTH_MEASURE( 1.000000000000000082E-05 ), #63187, 'distance_accuracy_value', 'NONE');
#31346=CARTESIAN_POINT ( 'NONE',  ( 3.246744516521868018, 1.970913372098213712, 0.4403762775553735631 ) ) ;
#31350=CARTESIAN_POINT ( 'NONE',  ( 3.608323775901512764, -0.8336323056173270407, -1.884943839506166174 ) ) ;
#31351=CARTESIAN_POINT ( 'NONE',  ( 6.727182134110200273, 0.5640974741700152117, 2.241195997201197443 ) ) ;
#31353=CARTESIAN_POINT ( 'NONE',  ( -0.2408018239684096284, 1.329574536483958846, -2.350731018214331947 ) ) ;
#31354=CARTESIAN_POINT ( 'NONE',  ( 1.148114065366242498, -1.452583890646602205, 1.131155481815901753 ) ) ;
#31355=CARTESIAN_POINT ( 'NONE',  ( 0.3468381721418262731, 2.301974930567828537, 0.1634500305177730706 ) ) ;
#31357=CARTESIAN_POINT ( 'NONE',  ( 3.022914066069124051, 2.034213141994867247, 0.7313807043239917149 ) ) ;
#31359=CARTESIAN_POINT ( 'NONE',  ( 1.428923106112218067, -1.700960256238340573, 1.082842518468102089 ) ) ;
#31360=CARTESIAN_POINT ( 'NONE',  ( 2.495865491978021211, 2.229134443137513966, 0.5594839687708874632 ) ) ;
#31363=CARTESIAN_POINT ( 'NONE',  ( 4.399269495383588691, 1.582840427583383613, 1.175083439883710890 ) ) ;
#31364=CARTESIAN_POINT ( 'NONE',  ( 5.085172837459294826, 1.651341431264556014, 1.157102043685846793 ) ) ;
#31368=CARTESIAN_POINT ( 'NONE',  ( 6.533818191484063398, -1.374270492279753286, -1.595981979862278077 ) ) ;
#31369=CARTESIAN_POINT ( 'NONE',  ( 6.268043187460373922, -2.055199631210803624, 0.2494731385529954104 ) ) ;
#31373=CARTESIAN_POINT ( 'NONE',  ( 3.907068546088189986, 1.690197745946390162, 1.014639218175046764 ) ) ;
#31374=CARTESIAN_POINT ( 'NONE',  ( 6.082287225941254150, 1.041776932085249907, 1.730260143339139134 ) ) ;
#31376=CARTESIAN_POINT ( 'NONE',  ( 4.389522222404328211, 2.062498103173298514, -1.035318202965694434 ) ) ;
#31377=CARTESIAN_POINT ( 'NONE',  ( 2.184505357994303232, 1.191016756910455943, -1.683754781088636632 ) ) ;
#31384=CARTESIAN_POINT ( 'NONE',  ( 4.475155579853315579, 1.983319414854123552, 0.8838481202026007288 ) ) ;
#31387=CARTESIAN_POINT ( 'NONE',  ( 2.841158510722852970, 0.6603703904487292498, -1.718939526767604420 ) ) ;
#31389=CARTESIAN_POINT ( 'NONE',  ( 6.040607902356621928, -1.852314659301615096, 1.170993205287726990 ) ) ;
#31391=CARTESIAN_POINT ( 'NONE',  ( 6.245044592044297183, -1.915350782734099200, 1.204081839623271311 ) ) ;
#31397=CARTESIAN_POINT ( 'NONE',  ( 6.327411112729964593, -1.665570200489007169, 0.5986406977509810545 ) ) ;
#31399=CARTESIAN_POINT ( 'NONE',  ( 4.617841973404108735, -0.5345865524139911118, 1.940763608534997520 ) ) ;
#31402=CARTESIAN_POINT ( 'NONE',  ( 2.520660759794272732, 1.376564137786383091, -1.593852158419235332 ) ) ;
#31403=CARTESIAN_POINT ( 'NONE',  ( 2.653800294728881681, 1.026947457930127872, 1.616878242289141676 ) ) ;
#31405=CARTESIAN_POINT ( 'NONE',  ( 3.350016042381760872, -0.8005406348832925234, 1.799716665148870964 ) ) ;
#31406=CARTESIAN_POINT ( 'NONE',  ( 1.533845512228737551, 0.9248708299973290581, -1.625957014461040906 ) ) ;
#31407=CARTESIAN_POINT ( 'NONE',  ( 1.557006721180295150, 1.605793932651664813, -1.126831546849601740 ) ) ;
#31408=CARTESIAN_POINT ( 'NONE',  ( 4.406709194360526993, 1.330975820509268104, -1.097133727364963729 ) ) ;
#31409=CARTESIAN_POINT ( 'NONE',  ( -0.1581436608063293003, -1.178060542814472367, -1.506996232563104776 ) ) ;
#31411=CARTESIAN_POINT ( 'NONE',  ( 1.664966938652842954, -1.558911317520403239, 1.562347339584921002 ) ) ;
#31417=CARTESIAN_POINT ( 'NONE',  ( 6.420769920452011448, -1.468259139554881409, 1.459777494992514857 ) ) ;
#31418=CARTESIAN_POINT ( 'NONE',  ( 0.6607010325807397555, -0.6960017893198193750, -1.950014918625786020 ) ) ;
#31423=CARTESIAN_POINT ( 'NONE',  ( 5.549516566986255839, -1.916978305411633166, 0.9067721062034905799 ) ) ;
#31428=CARTESIAN_POINT ( 'NONE',  ( 6.619590441841329387, 0.3365870006281460047, -1.932621868259084330 ) ) ;
#31430=CARTESIAN_POINT ( 'NONE',  ( 4.235703761680151835, -1.880146911114020325, -0.7282675588539261335 ) ) ;
#31431=CARTESIAN_POINT ( 'NONE',  ( 3.573361294032686430, 1.391295603808204051, 1.317194196901736669 ) ) ;
#31433=CARTESIAN_POINT ( 'NONE',  ( 1.505704256594592838, -2.174480876681058827, 0.2726767719730335826 ) ) ;
#31434=CARTESIAN_POINT ( 'NONE',  ( 0.1333692844072802142, 0.2389375359408679178, -2.087895146362698906 ) ) ;
#31435=CARTESIAN_POINT ( 'NONE',  ( 2.846779338809723559, -1.557328454271855955, 1.035869100625155470 ) ) ;
#31439=CARTESIAN_POINT ( 'NONE',  ( 5.308266703545434062, 1.260341450243172678, -1.701113402177101053 ) ) ;
#31441=CARTESIAN_POINT ( 'NONE',  ( 2.630511997247253486, 0.2585083551314356631, 2.074647729848762889 ) ) ;
#31443=CARTESIAN_POINT ( 'NONE',  ( 1.342334339533798104, 0.3310447913058271463, 1.692513552724637771 ) ) ;
#31456=CARTESIAN_POINT ( 'NONE',  ( 1.488595082971344352, -1.720062743487455581, -0.5684112265044569678 ) ) ;
#31460=CARTESIAN_POINT ( 'NONE',  ( 6.639320575229255006, 7.629137130509086262, 2.396737603865983779 ) ) ;
#31467=CARTESIAN_POINT ( 'NONE',  ( 2.875287963320713569, -0.1852811808005799254, 1.851819283609082323 ) ) ;
#31469=CARTESIAN_POINT ( 'NONE',  ( -0.07089544441234334193, -1.481030113823898375, -1.214736957437832832 ) ) ;
#31470=CARTESIAN_POINT ( 'NONE',  ( 6.545928648987922038, 0.7364953880720639390, -1.780233924599901929 ) ) ;
#31476=CARTESIAN_POINT ( 'NONE',  ( 4.223468175789964363, 0.2452432568937177593, -1.954070501097299850 ) ) ;
#31477=CARTESIAN_POINT ( 'NONE',  ( 1.700013272279196963, 1.464590769506744161, 1.533662747278791816 ) ) ;
#31481=CARTESIAN_POINT ( 'NONE',  ( 5.507841377412062478, -0.9828142975771281264, -1.958786091674463714 ) ) ;
#31483=CARTESIAN_POINT ( 'NONE',  ( 4.629859910813647339, -1.184627732843917647, -1.519026826222178661 ) ) ;
#31485=CARTESIAN_POINT ( 'NONE',  ( 0.1647065507319189492, -1.628042339203483957, -0.8261295386280396169 ) ) ;
#31486=CARTESIAN_POINT ( 'NONE',  ( 0.6806489137391663613, -1.222764829241920426, 1.836970590647703849 ) ) ;
#31487=CARTESIAN_POINT ( 'NONE',  ( 6.925078400183550364, -0.007619068086212391067, 2.144148427808051594 ) ) ;
#31493=CARTESIAN_POINT ( 'NONE',  ( 6.297704708030454235, -1.423956832742166112, -1.360762174370538258 ) ) ;
#31494=CARTESIAN_POINT ( 'NONE',  ( 1.751409898207861415, 1.936723520591139058, -0.1449614948935191994 ) ) ;
#31495=CARTESIAN_POINT ( 'NONE',  ( 6.696599425470320277, -1.493074370650529392, -1.747488531831635550 ) ) ;
#31497=CARTESIAN_POINT ( 'NONE',  ( 5.700015841690603935, 0.7557596558054953118, -1.700775360669419145 ) ) ;
#31503=CARTESIAN_POINT ( 'NONE',  ( 1.540847765565691585, -1.849059859674206496, 1.176127931831471907 ) ) ;
#31507=CARTESIAN_POINT ( 'NONE',  ( 1.963248404482214049, 0.3131683437365209710, -1.798463397695612809 ) ) ;
#31512=CARTESIAN_POINT ( 'NONE',  ( 6.287720257080702702, 1.262826302610157381, 1.318732360701305062 ) ) ;
#31513=CARTESIAN_POINT ( 'NONE',  ( 4.311346321947408633, -1.628642355029306987, -1.093319670275281652 ) ) ;
#31516=CARTESIAN_POINT ( 'NONE',  ( 4.107102485094754840, -0.3736803571842538529, 2.159302612355806339 ) ) ;
#31519=CARTESIAN_POINT ( 'NONE',  ( 3.836834752522141567, -1.993853832596056197, -0.5568897355931883286 ) ) ;
#31522=ORIENTED_EDGE ( 'NONE', *, *, #190238, .T. ) ;
#31523=CARTESIAN_POINT ( 'NONE',  ( 3.657115705757322477, 1.277955821227232613, 1.910552683106376382 ) ) ;
#31529=CARTESIAN_POINT ( 'NONE',  ( 3.503789773231671845, -0.7878879028691202491, -1.775113385239434072 ) ) ;
#31533=CARTESIAN_POINT ( 'NONE',  ( 4.166199421025416960, 1.911861072351704882, -0.05224187775455800542 ) ) ;
#31535=CARTESIAN_POINT ( 'NONE',  ( 5.403229623239121260, 1.412049869051584361, 0.9901104176405839397 ) ) ;
#31536=CARTESIAN_POINT ( 'NONE',  ( 5.050017674172561755, 0.9981218692422781924, 1.752141108012375437 ) ) ;
#31537=CARTESIAN_POINT ( 'NONE',  ( 5.397245865906225681, -1.031513598091776673, -2.054350403923683732 ) ) ;
#31538=CARTESIAN_POINT ( 'NONE',  ( 1.225528936851564721, -0.05108506852482053856, 2.206457870188942572 ) ) ;
#31541=CARTESIAN_POINT ( 'NONE',  ( 6.098865926757823352, 1.445600302716108843, -1.020594415802724919 ) ) ;
#31543=CARTESIAN_POINT ( 'NONE',  ( 1.570720025219290328, -2.177795595024238473, -0.7155201368211090429 ) ) ;
#31544=CARTESIAN_POINT ( 'NONE',  ( 1.534671620441448558, -1.258764033546970529, -1.202027791382529909 ) ) ;
#31547=CARTESIAN_POINT ( 'NONE',  ( 0.6668559383766320403, -0.5766704339003425606, -1.635293367498649397 ) ) ;
#31550=CARTESIAN_POINT ( 'NONE',  ( 1.697964449562241018, -1.571978469985369831, -1.497844480664213052 ) ) ;
#31551=CARTESIAN_POINT ( 'NONE',  ( 2.659388954101277847, 1.913261587491304150, -0.6371546050257800298 ) ) ;
#31554=CARTESIAN_POINT ( 'NONE',  ( 6.006463946069247939, -0.6956954824784820079, -1.796673741800159707 ) ) ;
#31556=CARTESIAN_POINT ( 'NONE',  ( 2.795431959603801086, -0.1677860356435970368, -2.215157990583861203 ) ) ;
#31563=CARTESIAN_POINT ( 'NONE',  ( 5.354937190278808323, 0.3318421670873850648, -1.708331137930273913 ) ) ;
#31564=CARTESIAN_POINT ( 'NONE',  ( 3.332423539472821439, -1.170687260143790320, 1.574129132985650825 ) ) ;
#31568=CARTESIAN_POINT ( 'NONE',  ( 4.903763976872734354, -0.6097993234682648200, 2.178603239016148052 ) ) ;
#31569=CARTESIAN_POINT ( 'NONE',  ( 1.205618545266523567, -1.624909386276121692, -1.270427818644123796 ) ) ;
#31571=CARTESIAN_POINT ( 'NONE',  ( 2.430887666589570451, 2.194555640652501527, 0.5498776597147712053 ) ) ;
#31574=CARTESIAN_POINT ( 'NONE',  ( 2.020564968092851021, 1.743606242109306148, 0.6777753874912318954 ) ) ;
#31575=CARTESIAN_POINT ( 'NONE',  ( 1.687715598229572844, 1.441817134274174794, 0.9631580532376384784 ) ) ;
#31577=CARTESIAN_POINT ( 'NONE',  ( 5.038714576072483631, -1.879839391954684746, 1.126354835186346603 ) ) ;
#31578=CARTESIAN_POINT ( 'NONE',  ( 0.3412290553763823175, 0.3797058362894655814, 2.173699509851903855 ) ) ;
#31579=CARTESIAN_POINT ( 'NONE',  ( 4.434552454296070145, 2.119417814153037316, 0.4246342833542292028 ) ) ;
#31580=CARTESIAN_POINT ( 'NONE',  ( 5.103436805131417842, -1.932407887632971555, 0.1922973783335303055 ) ) ;
#31582=CARTESIAN_POINT ( 'NONE',  ( 6.784453417974287248, -1.834524189944960471, -0.3643881242741816018 ) ) ;
#31583=CARTESIAN_POINT ( 'NONE',  ( 2.062500000000001776, -1.451031289061204266, -1.451031289061035956 ) ) ;
#31588=CARTESIAN_POINT ( 'NONE',  ( 5.379529795981254914, -0.4926393568372189335, -1.955173248319847845 ) ) ;
#31592=CARTESIAN_POINT ( 'NONE',  ( 3.809063337113669068, 1.566667275063510445, 0.9371452329686791316 ) ) ;
#31598=CARTESIAN_POINT ( 'NONE',  ( 0.3342475891858322501, -1.084071894752016041, -1.704023929676929727 ) ) ;
#31599=CARTESIAN_POINT ( 'NONE',  ( 1.155114678095255254, 0.4172207117813032662, 2.078868179971034902 ) ) ;
#31603=CARTESIAN_POINT ( 'NONE',  ( 6.596562995212404523, -0.5471746534140635720, -1.986858483302299083 ) ) ;
#31604=CARTESIAN_POINT ( 'NONE',  ( 6.346327303948391396, 0.3419391630616851474, -1.987045965717588958 ) ) ;
#31605=EDGE_LOOP ( 'NONE', ( #101538, #82930, #73485, #181055 ) ) ;
#31607=CARTESIAN_POINT ( 'NONE',  ( 4.084924167595121780, -0.1881231333150361895, -1.917172266129524294 ) ) ;
#31612=CARTESIAN_POINT ( 'NONE',  ( 6.883263157960391787, -0.001104538646235289417, 1.946037152736757925 ) ) ;
#31615=CARTESIAN_POINT ( 'NONE',  ( 5.712267477471262289, -1.587595409608580255, -1.242535230690837489 ) ) ;
#31616=CARTESIAN_POINT ( 'NONE',  ( 4.874869531740305462, 1.716800804850382223, -0.6655867697097294089 ) ) ;
#31618=CARTESIAN_POINT ( 'NONE',  ( 0.07700591528354487625, 0.7269319812311864082, -1.993543990282041767 ) ) ;
#31619=CARTESIAN_POINT ( 'NONE',  ( 2.913035970020665388, 1.671030660360285802, -1.591803581779531074 ) ) ;
#31621=CARTESIAN_POINT ( 'NONE',  ( 5.870447946289019114, -1.376328297836002301, 1.666777564274177781 ) ) ;
#31623=CARTESIAN_POINT ( 'NONE',  ( 1.101004982060274751, -0.4702163980460572490, 1.884172457509038834 ) ) ;
#31628=CARTESIAN_POINT ( 'NONE',  ( 4.838664814796108438, 0.3202261158844340594, 1.842872994462002367 ) ) ;
#31629=CARTESIAN_POINT ( 'NONE',  ( 0.9492982845318720386, -1.727743609841876360, 0.8201845251225792222 ) ) ;
#31632=CARTESIAN_POINT ( 'NONE',  ( 3.369938178094655346, 2.153121441420174698, -0.4834393813165636100 ) ) ;
#31638=CARTESIAN_POINT ( 'NONE',  ( 2.126188665331921079, 1.138154612934966670, -1.609425365540081865 ) ) ;
#31639=CARTESIAN_POINT ( 'NONE',  ( 0.7984239956072606281, -0.8271026589724904676, 2.154427444091823851 ) ) ;
#31640=CARTESIAN_POINT ( 'NONE',  ( 1.890992312513404716, 0.1891058464698439912, 1.952711869325058691 ) ) ;
#31641=CARTESIAN_POINT ( 'NONE',  ( 5.313357764218651802, -1.739529159241906875, -1.108013508251452395 ) ) ;
#31648=CARTESIAN_POINT ( 'NONE',  ( 1.235490768065301337, -0.05108008202716606688, -2.170608684345101125 ) ) ;
#31650=CARTESIAN_POINT ( 'NONE',  ( 6.339398910184078417, 0.6979989802004606947, -1.704029730133400866 ) ) ;
#31654=CARTESIAN_POINT ( 'NONE',  ( 1.633845377418343237, 0.9265681688636999702, -1.624882239709434018 ) ) ;
#31655=CARTESIAN_POINT ( 'NONE',  ( 5.589210384452774960, 1.909260796540311000, -1.013481389624170115 ) ) ;
#31657=CARTESIAN_POINT ( 'NONE',  ( -0.02244404828160086532, 2.859736408857795009, -2.677210243787793598 ) ) ;
#31659=CARTESIAN_POINT ( 'NONE',  ( 1.893074787327468700, -0.09523556418119562272, -1.910042277862213034 ) ) ;
#31660=CARTESIAN_POINT ( 'NONE',  ( 2.852158073610413513, 0.5945245674133512459, 1.667141438756434058 ) ) ;
#31662=CARTESIAN_POINT ( 'NONE',  ( 0.9262460828363194842, -0.8603794558708977025, -1.707882697979688391 ) ) ;
#31664=CARTESIAN_POINT ( 'NONE',  ( 5.009359837557266992, -1.817519814519794830, 0.6052834035694378834 ) ) ;
#31665=CARTESIAN_POINT ( 'NONE',  ( 6.742638201966631328, -1.931250359857048515, -0.3855633916233728309 ) ) ;
#31667=CARTESIAN_POINT ( 'NONE',  ( 0.5629301599625028407, 0.6213668382478373386, 2.027498709647377773 ) ) ;
#31669=CARTESIAN_POINT ( 'NONE',  ( 4.539837415608827698, 0.7997722286730184482, -1.691214532891088362 ) ) ;
#31670=CARTESIAN_POINT ( 'NONE',  ( 1.031563979315492485, -1.156294252604734396, -1.412831148817683680 ) ) ;
#31672=CARTESIAN_POINT ( 'NONE',  ( 4.266400587755204477, 1.039063272370500668, 1.946970035688735390 ) ) ;
#31675=CARTESIAN_POINT ( 'NONE',  ( 1.504421023514388889, 2.060217768730878696, 0.1034037034779722308 ) ) ;
#31684=CARTESIAN_POINT ( 'NONE',  ( 4.562978833902987752, 1.602482145440896399, -1.310924660355553106 ) ) ;
#31686=CARTESIAN_POINT ( 'NONE',  ( 1.036653925908154639, 2.129443126370239803, 0.3705773954724435604 ) ) ;
#31688=CARTESIAN_POINT ( 'NONE',  ( 1.945969044768879552, -1.321035068824018222, -1.527795347589502972 ) ) ;
#31695=CARTESIAN_POINT ( 'NONE',  ( 0.7257964430846426396, 0.8128130212789463904, -1.845628942776005088 ) ) ;
#31696=CARTESIAN_POINT ( 'NONE',  ( 4.652002595327206613, 0.8389548150543740812, 2.024815518666116088 ) ) ;
#31698=CARTESIAN_POINT ( 'NONE',  ( 4.711142613322857109, 1.586760866459841379, -1.067142987418716604 ) ) ;
#31702=CARTESIAN_POINT ( 'NONE',  ( 2.214470461757975794, 1.956567829827577931, 0.4871813834786202224 ) ) ;
#31704=CARTESIAN_POINT ( 'NONE',  ( -0.005774900045998726007, -2.292045413227526751, -0.04753075064714216980 ) ) ;
#31706=CARTESIAN_POINT ( 'NONE',  ( 4.067213672036010585, 0.2104045600922407611, -1.711820660605578137 ) ) ;
#31715=CARTESIAN_POINT ( 'NONE',  ( 5.180233172056982305, 0.8977705535664436409, 1.573279850597033347 ) ) ;
#31719=CARTESIAN_POINT ( 'NONE',  ( 6.252603509501785339, 1.792834410666717337, 0.2582872775454737591 ) ) ;
#31722=CARTESIAN_POINT ( 'NONE',  ( 2.871223686158608679, 2.080653275041044026, -0.6881803712485771163 ) ) ;
#31726=CARTESIAN_POINT ( 'NONE',  ( 6.443805748662878585, 1.284351271648530357, 1.347085863211768819 ) ) ;
#31728=CARTESIAN_POINT ( 'NONE',  ( 3.638217106272136903, 0.6927189700525613336, 1.786146362908203944 ) ) ;
#31734=CARTESIAN_POINT ( 'NONE',  ( 0.2687375195599971400, -1.410744835756465365, 1.637978619736128127 ) ) ;
#31737=CARTESIAN_POINT ( 'NONE',  ( 2.010518257881420023, 1.354885872097401078, -1.223726681998098087 ) ) ;
#31739=CARTESIAN_POINT ( 'NONE',  ( 3.434410497111122673, 1.780829521046650932, 0.4009754434649847044 ) ) ;
#31742=ORIENTED_EDGE ( 'NONE', *, *, #66878, .T. ) ;
#31743=CARTESIAN_POINT ( 'NONE',  ( 2.787508051956408384, -1.838732291863707236, 0.7063352763673010903 ) ) ;
#31744=ORIENTED_EDGE ( 'NONE', *, *, #68712, .F. ) ;
#31745=CARTESIAN_POINT ( 'NONE',  ( 5.214377421777850685, 1.795891487756570815, 0.7396389662707256729 ) ) ;
#31749=CARTESIAN_POINT ( 'NONE',  ( 5.695592476053609410, 1.958610405324921588, -0.8133567297157192622 ) ) ;
#31752=CARTESIAN_POINT ( 'NONE',  ( 2.561071438676546741, -1.588783617390630898, 1.063917234122884858 ) ) ;
#31758=CARTESIAN_POINT ( 'NONE',  ( 4.389318492827157137, -0.002256833108382152835, -2.013265972533995640 ) ) ;
#31760=CARTESIAN_POINT ( 'NONE',  ( 5.531824841778981927, -1.161409778037244100, -1.408645805323349487 ) ) ;
#31761=CARTESIAN_POINT ( 'NONE',  ( 0.2915762745691782287, -1.893489616766583117, 0.8377075429084477332 ) ) ;
#31766=CARTESIAN_POINT ( 'NONE',  ( 5.295714669793899709, -0.6724083694377264164, 1.745798414713333413 ) ) ;
#31775=CARTESIAN_POINT ( 'NONE',  ( 0.7958623839904412911, -1.461433461687311253, -1.466603172318406090 ) ) ;
#31776=CARTESIAN_POINT ( 'NONE',  ( 1.845463042662376818, 0.3584012047737962781, -2.086523245552903472 ) ) ;
#31779=CARTESIAN_POINT ( 'NONE',  ( 0.8835773814684219074, -1.871821877138898582, 0.6126781507047509567 ) ) ;
#31784=CARTESIAN_POINT ( 'NONE',  ( 2.238584135424640298, 0.5043332063416061661, 2.235947581072089907 ) ) ;
#31786=CARTESIAN_POINT ( 'NONE',  ( 1.863391182279940494, -1.538030936729195552, -1.136358088520472931 ) ) ;
#31790=CARTESIAN_POINT ( 'NONE',  ( 0.9494776711209992337, -1.818202237497710483, 0.8646994008154506028 ) ) ;
#31791=CARTESIAN_POINT ( 'NONE',  ( 1.533958681542445301, 1.164210590399002321, 1.578835587694705334 ) ) ;
#31795=CARTESIAN_POINT ( 'NONE',  ( 4.154300538700359091, -1.549125135342351856, 1.404095012314343416 ) ) ;
#31796=CARTESIAN_POINT ( 'NONE',  ( 2.869705036365962858, 0.9450794480442193946, 1.496173807068044148 ) ) ;
#31799=CARTESIAN_POINT ( 'NONE',  ( 5.771479170232404421, 1.361120583587755783, 1.844262159060359174 ) ) ;
#31800=CARTESIAN_POINT ( 'NONE',  ( 4.786887925959832479, 1.292461281945065599, 1.165648420485969394 ) ) ;
#31803=CARTESIAN_POINT ( 'NONE',  ( 3.954193900006929052, 1.254965027507263464, 1.196595854207074261 ) ) ;
#31804=CARTESIAN_POINT ( 'NONE',  ( 4.668535151219040280, -0.9243884330643321601, -1.964686384670484953 ) ) ;
#31806=CARTESIAN_POINT ( 'NONE',  ( 5.331267653506235327, -1.592659417495114083, -1.236803018183525449 ) ) ;
#31807=CARTESIAN_POINT ( 'NONE',  ( 6.718719045489192965, -0.7860540964614262105, 1.895863743164223347 ) ) ;
#31809=CARTESIAN_POINT ( 'NONE',  ( 3.241151106802504511, -1.699520814979482264, 0.9069582849330155572 ) ) ;
#31811=CARTESIAN_POINT ( 'NONE',  ( 5.959279902674206042, -1.877032357297861109, 1.187784507339540108 ) ) ;
#31813=CARTESIAN_POINT ( 'NONE',  ( 6.983263157960380774, 2.077058603031848527, 2.154533585220330227 ) ) ;
#31816=CARTESIAN_POINT ( 'NONE',  ( 1.963841274844113194, -1.786346139091129270, -1.320113705855001207 ) ) ;
#31824=CARTESIAN_POINT ( 'NONE',  ( 4.949704379398387033, 1.526268909138599028, 1.387654848983727485 ) ) ;
#31828=CARTESIAN_POINT ( 'NONE',  ( 6.134044790494318278, 0.9221746925026914621, -1.627378824227587062 ) ) ;
#31829=CARTESIAN_POINT ( 'NONE',  ( 6.170542255345159433, 1.203217383492904746, 1.249094692781686611 ) ) ;
#31830=CARTESIAN_POINT ( 'NONE',  ( 4.423245670630183923, -1.075405338609165318, -1.368339626032973211 ) ) ;
#31833=CARTESIAN_POINT ( 'NONE',  ( 2.419810632640221115, -1.322813552229468614, -1.872022261021451639 ) ) ;
#31835=CARTESIAN_POINT ( 'NONE',  ( 0.9547317490294878750, 0.3612830171869831353, -1.805165878648997690 ) ) ;
#31837=CARTESIAN_POINT ( 'NONE',  ( 1.887459117809231701, 1.256508940344562397, 1.324596713471258402 ) ) ;
#31838=CARTESIAN_POINT ( 'NONE',  ( 2.514296259408643319, -1.880434619097739013, 0.7283795345095490648 ) ) ;
#31839=CARTESIAN_POINT ( 'NONE',  ( 1.429895766826321690, 1.077743243251317429, -1.908043295719801025 ) ) ;
#31841=CARTESIAN_POINT ( 'NONE',  ( 4.348724867337580235, 0.5594899878812797933, 2.030215228624824952 ) ) ;
#31843=CARTESIAN_POINT ( 'NONE',  ( 1.609917502266303480, 0.6029389078928657497, -1.980602105166151095 ) ) ;
#31846=CARTESIAN_POINT ( 'NONE',  ( 3.194099758881031814, 1.346771490053525033, 1.637864368873870990 ) ) ;
#31848=CARTESIAN_POINT ( 'NONE',  ( 6.358013415952256331, 1.820405254634300363, -0.1396899356524081148 ) ) ;
#31856=CARTESIAN_POINT ( 'NONE',  ( 3.551039915000217206, 0.3004019028194653829, 1.997212655505080203 ) ) ;
#31857=CARTESIAN_POINT ( 'NONE',  ( 1.448413646618036399, 2.103543699351087870, 0.1036336169341102176 ) ) ;
#31861=CARTESIAN_POINT ( 'NONE',  ( 5.014427361338555933, 0.7098351839037967403, 1.720451000603514524 ) ) ;
#31866=CARTESIAN_POINT ( 'NONE',  ( 6.192271402255323132, -2.050732637037344208, -0.2044092671329711397 ) ) ;
#31870=CARTESIAN_POINT ( 'NONE',  ( 2.881899232214884865, -0.1729783253755692307, 1.725191050717300945 ) ) ;
#31871=CARTESIAN_POINT ( 'NONE',  ( 1.446757823190962577, 0.5079132294574678630, -1.664563843253030750 ) ) ;
#31872=CARTESIAN_POINT ( 'NONE',  ( 6.691963835194851384, -0.9925954392468823162, 2.080958020993000979 ) ) ;
#31875=CARTESIAN_POINT ( 'NONE',  ( 2.917317126705867736, -0.2052410828034083035, 2.050554836033135597 ) ) ;
#31877=CARTESIAN_POINT ( 'NONE',  ( 1.581407437776818581, 1.356094323556347181, -1.492024998029889638 ) ) ;
#31878=CARTESIAN_POINT ( 'NONE',  ( 0.1331565106231598072, 7.629137130509052511, -2.545925718843544239 ) ) ;
#31881=CARTESIAN_POINT ( 'NONE',  ( 1.692193703850993103, -1.961769708113933808, -0.1953840112930530781 ) ) ;
#31882=CARTESIAN_POINT ( 'NONE',  ( 4.763870730211980487, 0.5944114921396548290, -1.817767169311027997 ) ) ;
#31884=CARTESIAN_POINT ( 'NONE',  ( 5.918643953348324160, 1.484978324971843566, -1.632713241052483832 ) ) ;
#31888=CARTESIAN_POINT ( 'NONE',  ( 0.04752895628580295490, -1.845665702319599921, 0.8205699430347112022 ) ) ;
#31890=CARTESIAN_POINT ( 'NONE',  ( 4.155530545730415248, -1.916392541607782496, -1.285185436265631642 ) ) ;
#31891=CARTESIAN_POINT ( 'NONE',  ( 4.773855682050706761, -1.924389145058275963, 0.3807478752155256663 ) ) ;
#31892=CARTESIAN_POINT ( 'NONE',  ( 2.342563710341159400, -1.922903400459201828, -0.3876519335672747313 ) ) ;
#31896=CARTESIAN_POINT ( 'NONE',  ( 0.09316046741510237983, 1.845552173327277501, 1.037660268145562004 ) ) ;
#31899=CARTESIAN_POINT ( 'NONE',  ( 1.148114065366242498, -1.452583890646602205, 1.131155481815901531 ) ) ;
#31901=CARTESIAN_POINT ( 'NONE',  ( 4.118177926953592305, 2.155335829443456142, -0.2601999948229383741 ) ) ;
#31903=CARTESIAN_POINT ( 'NONE',  ( 1.863691559860299884, -1.706161385809309650, -1.259181899442491037 ) ) ;
#31908=CARTESIAN_POINT ( 'NONE',  ( 3.057942249777849675, 2.051182028257723999, -0.1983934154812707074 ) ) ;
#31910=CARTESIAN_POINT ( 'NONE',  ( 0.6613494997313728030, 0.9071737413179328247, 1.602200521169500957 ) ) ;
#31912=CARTESIAN_POINT ( 'NONE',  ( -0.02244404828157658613, -0.004869073801674199918, -2.189079685368473527 ) ) ;
#31915=CARTESIAN_POINT ( 'NONE',  ( 2.073834635255236147, 2.165437736866062224, -0.6553434645707820749 ) ) ;
#31917=CARTESIAN_POINT ( 'NONE',  ( 0.8612205622890884982, -1.428740940428592898, -1.113706988620609240 ) ) ;
#31918=CARTESIAN_POINT ( 'NONE',  ( 2.272541799296357468, -0.3318032026102230581, -1.886604652318550901 ) ) ;
#31919=CARTESIAN_POINT ( 'NONE',  ( 2.647004975520852454, -0.3514972095969396970, -2.040143077068845123 ) ) ;
#31921=CARTESIAN_POINT ( 'NONE',  ( 2.184392200726268829, -1.933073530578834465, -0.3863716293817393566 ) ) ;
#31922=CARTESIAN_POINT ( 'NONE',  ( 5.408790948643045660, 1.457530049539386141, -1.259864545333173158 ) ) ;
#31923=CARTESIAN_POINT ( 'NONE',  ( 0.7335963760657808752, 0.1754145531542888048, 2.301085101356622697 ) ) ;
#31926=CARTESIAN_POINT ( 'NONE',  ( 4.949704379398387033, 1.526268909138599028, 1.387654848983727485 ) ) ;
#31929=CARTESIAN_POINT ( 'NONE',  ( 6.756868576547260474, -1.630415217921374671, 1.332730856581629375 ) ) ;
#31931=CARTESIAN_POINT ( 'NONE',  ( 4.903692054014650026, -0.5817465652163296141, 2.081756923971528117 ) ) ;
#31932=CARTESIAN_POINT ( 'NONE',  ( 4.934242777533356161, -1.082215927170935954, -1.705062858592779174 ) ) ;
#31933=CARTESIAN_POINT ( 'NONE',  ( -0.1399997263889612154, 1.357298622859517856, -2.254419820505838334 ) ) ;
#31939=CARTESIAN_POINT ( 'NONE',  ( 3.503138892209650024, -0.1435209762444041581, 2.011451614702438828 ) ) ;
#31944=CARTESIAN_POINT ( 'NONE',  ( 4.997027575558514734, 1.799266821141291661, -1.197868618907194316 ) ) ;
#31949=CARTESIAN_POINT ( 'NONE',  ( 5.044546077387519922, -1.458546410489666600, 1.392558106302365095 ) ) ;
#31951=CARTESIAN_POINT ( 'NONE',  ( 1.910387937834428174, 1.279409190829815746, -1.157040217339623034 ) ) ;
#31957=CARTESIAN_POINT ( 'NONE',  ( 6.643822754079466542, 0.7155741859487285694, -1.728458771772640512 ) ) ;
#31958=CARTESIAN_POINT ( 'NONE',  ( 0.3990879006048999589, -0.2487020831964822098, -1.997621932491387531 ) ) ;
#31960=CARTESIAN_POINT ( 'NONE',  ( 3.065657736429776126, 0.3252250816505456998, -2.182562984848686938 ) ) ;
#31962=ORIENTED_EDGE ( 'NONE', *, *, #50413, .T. ) ;
#31964=CARTESIAN_POINT ( 'NONE',  ( 2.526173596586390957, -2.097057114080549844, 0.3136139059176298871 ) ) ;
#31965=CARTESIAN_POINT ( 'NONE',  ( 1.353138909097661768, 0.1455122274086443901, -2.011206940682720212 ) ) ;
#31966=CARTESIAN_POINT ( 'NONE',  ( 2.531291980686082521, -0.1736719688998221156, 1.803202784768900502 ) ) ;
#31975=CARTESIAN_POINT ( 'NONE',  ( 0.4619447194890722308, -1.061692323622511536, 1.594387217869216888 ) ) ;
#31976=AXIS2_PLACEMENT_3D ( 'NONE', #209144, #12023, #60783 ) ;
#31983=CARTESIAN_POINT ( 'NONE',  ( 5.401312781148372544, 1.764888628567515827, 1.247983453017486477 ) ) ;
#31986=CARTESIAN_POINT ( 'NONE',  ( 1.705496241919310707, 1.842552997918958768, -1.049655202612943095 ) ) ;
#31987=CARTESIAN_POINT ( 'NONE',  ( 6.704125975539116489, -1.825092170400946845, 0.04854515157103055090 ) ) ;
#31988=CARTESIAN_POINT ( 'NONE',  ( 3.163306973099208275, 0.2928498925126362673, -1.949387327701812334 ) ) ;
#31989=ORIENTED_EDGE ( 'NONE', *, *, #113502, .F. ) ;
#31990=CARTESIAN_POINT ( 'NONE',  ( 6.689911425329987615, -1.285551722473629477, -1.492250998650017202 ) ) ;
#31991=CARTESIAN_POINT ( 'NONE',  ( 1.359210844938564033, 1.913264527786652902, -0.3316978906799557536 ) ) ;
#31996=CARTESIAN_POINT ( 'NONE',  ( 2.203177794981598492, -0.4570653145323905764, 2.039892330567660839 ) ) ;
#32000=CARTESIAN_POINT ( 'NONE',  ( -0.1051951494144076904, -0.1375245761873785666, -1.781266614511106683 ) ) ;
#32002=CARTESIAN_POINT ( 'NONE',  ( 4.881566871873391555, 2.059980941486462047, -0.7921658822237287456 ) ) ;
#32003=CARTESIAN_POINT ( 'NONE',  ( 2.204404769108789797, -2.206272049354717879, 0.05393164079612458583 ) ) ;
#32005=CARTESIAN_POINT ( 'NONE',  ( 0.3988866192712777758, -0.2342882197893907670, -1.897819253221716851 ) ) ;
#32008=CARTESIAN_POINT ( 'NONE',  ( 3.877443546529443452, -0.1552652338182025915, 2.064615508632794860 ) ) ;
#32010=CARTESIAN_POINT ( 'NONE',  ( 1.780366757100563913, -1.156431984057613827, 1.826190802295484472 ) ) ;
#32011=CARTESIAN_POINT ( 'NONE',  ( 3.280998142716429200, 1.980384277226649559, -0.9389412094223739125 ) ) ;
#32017=CARTESIAN_POINT ( 'NONE',  ( 0.4928148368598186946, -2.006445878461552645, 0.2004378712678403507 ) ) ;
#32019=CARTESIAN_POINT ( 'NONE',  ( 4.329010850845236291, -1.929826300244817272, -0.7499136367685385052 ) ) ;
#32020=CARTESIAN_POINT ( 'NONE',  ( 5.536746206892352085, -1.668647081869235826, 1.303048207008510317 ) ) ;
#32023=CARTESIAN_POINT ( 'NONE',  ( 3.977371423044063103, -0.1491618029233315879, 1.963883198941584585 ) ) ;
#32024=CARTESIAN_POINT ( 'NONE',  ( 6.052705554163346768, -1.962971892542137553, -1.183510860282228405 ) ) ;
#32025=CARTESIAN_POINT ( 'NONE',  ( 4.143042835627613663, -1.587387879459275286, 0.9017181768668989239 ) ) ;
#32031=CARTESIAN_POINT ( 'NONE',  ( 4.851819109577236055, -1.426696570994885116, -1.420647396805594820 ) ) ;
#32032=CARTESIAN_POINT ( 'NONE',  ( 6.328761054056312396, 0.8840516187795799397, -2.122072247225449626 ) ) ;
#32033=CARTESIAN_POINT ( 'NONE',  ( 4.065250617491710905, 1.680331827152386159, 1.012218702928203706 ) ) ;
#32038=CARTESIAN_POINT ( 'NONE',  ( 0.6969597590469852610, 1.711416582936477804, 1.200673393543179479 ) ) ;
#32039=CARTESIAN_POINT ( 'NONE',  ( 5.946140033727446372, 1.768047588762114986, 0.08285011829376774661 ) ) ;
#32041=CARTESIAN_POINT ( 'NONE',  ( 5.595633723370948331, -1.942124712531563491, 0.002075263307293323100 ) ) ;
#32042=CARTESIAN_POINT ( 'NONE',  ( 2.238457302780196390, 0.4817095239468481283, 2.137691825660259948 ) ) ;
#32043=CARTESIAN_POINT ( 'NONE',  ( 1.417106933825535986, -0.9663644154882103932, -1.447271084069596370 ) ) ;
#32045=CARTESIAN_POINT ( 'NONE',  ( 1.295042460130943152, 1.303850460046240833, 1.129354085073847491 ) ) ;
#32046=CARTESIAN_POINT ( 'NONE',  ( 1.400213348495438437, -0.7931047570679079506, -2.043190674350242819 ) ) ;
#32047=CARTESIAN_POINT ( 'NONE',  ( 4.178501018151202118, -1.271701901513167421, 1.803451139310302986 ) ) ;
#32048=CARTESIAN_POINT ( 'NONE',  ( 1.270657207514551246, -0.9741964446108697384, -1.940257991389877201 ) ) ;
#32050=CARTESIAN_POINT ( 'NONE',  ( 2.395853177668628931, -2.093565527891564582, 0.3158384217898829727 ) ) ;
#32054=CARTESIAN_POINT ( 'NONE',  ( 2.701037021348651646, 1.938191879511786730, 1.223809664465740354 ) ) ;
#32058=CARTESIAN_POINT ( 'NONE',  ( 4.776165916792348476, 2.197254790419100434, -0.3252806346676767046 ) ) ;
#32066=CARTESIAN_POINT ( 'NONE',  ( 3.164685561777963230, 1.281361203394768111, 1.556908733426412450 ) ) ;
#32068=CARTESIAN_POINT ( 'NONE',  ( 1.288015978462764277, -1.305315335096700613, -1.597021576285734268 ) ) ;
#32074=CARTESIAN_POINT ( 'NONE',  ( 5.296902861200166512, 1.790115547914197247, 1.263834295783084150 ) ) ;
#32075=CARTESIAN_POINT ( 'NONE',  ( 1.951796282902381163, -1.844710420878793444, -0.8146254186931353169 ) ) ;
#32076=CARTESIAN_POINT ( 'NONE',  ( 1.593040506729075823, -0.6195558395927207584, 1.734028948791266345 ) ) ;
#32078=CARTESIAN_POINT ( 'NONE',  ( 5.069292194207453583, 0.1776299070984053985, -1.816928125296768393 ) ) ;
#32079=CARTESIAN_POINT ( 'NONE',  ( 6.610000000000006537, 0.002781820520842553934, 2.000159646111852929 ) ) ;
#32081=CARTESIAN_POINT ( 'NONE',  ( 4.417028899805944597, 2.066919071766720517, 0.9206345982136554529 ) ) ;
#32083=CARTESIAN_POINT ( 'NONE',  ( 0.7859291816119529095, 1.415994179718871759, 1.559173624910270783 ) ) ;
#32085=CARTESIAN_POINT ( 'NONE',  ( 4.633297751427938316, 0.003287558298453730800, -2.070544812459538253 ) ) ;
#32095=CARTESIAN_POINT ( 'NONE',  ( 1.512141599020993432, -0.7094941370262074498, 1.998545949238240027 ) ) ;
#32096=CARTESIAN_POINT ( 'NONE',  ( 1.354101172232239580, -1.613524214714330940, -1.527088627841047375 ) ) ;
#32101=CARTESIAN_POINT ( 'NONE',  ( 3.596105239937871456, 0.8843387906064968940, -1.751336483779348585 ) ) ;
#32107=CARTESIAN_POINT ( 'NONE',  ( 2.478903650112133317, -1.459102030866548994, 1.539066919819010781 ) ) ;
#32109=CARTESIAN_POINT ( 'NONE',  ( 5.389097038490845648, 0.1425914310585977562, 1.956722230749983193 ) ) ;
#32110=CARTESIAN_POINT ( 'NONE',  ( 2.922914210685311431, 2.035003303901411265, 0.7295308445595325431 ) ) ;
#32111=CARTESIAN_POINT ( 'NONE',  ( 2.665370095338463585, 0.9869154847663293983, 1.554228294351194473 ) ) ;
#32114=CARTESIAN_POINT ( 'NONE',  ( 4.400191647014492169, 1.342938829013840207, -1.106906270395467295 ) ) ;
#32118=CARTESIAN_POINT ( 'NONE',  ( 1.762795743007524063, -1.528684080660724920, 1.528680807790387286 ) ) ;
#32120=CARTESIAN_POINT ( 'NONE',  ( 5.026720154644213068, 1.994564127574052215, -0.2930270067487000252 ) ) ;
#32122=CARTESIAN_POINT ( 'NONE',  ( 0.7257156204387126275, -2.052300050329861847, 0.6792298617422781737 ) ) ;
#32125=CARTESIAN_POINT ( 'NONE',  ( 2.372288100061814564, -1.215664946315485606, 1.551802774678180619 ) ) ;
#32126=CARTESIAN_POINT ( 'NONE',  ( 6.509000000000034092, 7.052765612591089806, 2.598154238703707541 ) ) ;
#32127=CARTESIAN_POINT ( 'NONE',  ( 3.737779845645439636, 1.932976868219363764, 0.1874624384631869700 ) ) ;
#32136=CARTESIAN_POINT ( 'NONE',  ( 1.290363523627102049, -0.9912053058820711193, 1.971723787660728977 ) ) ;
#32139=CARTESIAN_POINT ( 'NONE',  ( 5.366048076001885825, -1.952644961629325548, 0.1885061251027941032 ) ) ;
#32140=CARTESIAN_POINT ( 'NONE',  ( 3.221969581791602977, 0.9480887764680032692, -1.893252576601434756 ) ) ;
#32143=CARTESIAN_POINT ( 'NONE',  ( 4.558453444723221892, -1.645810703501834782, -0.8254300276653584456 ) ) ;
#32147=CARTESIAN_POINT ( 'NONE',  ( 5.678019686890188211, 2.088907387943875982, -0.3644037002746222664 ) ) ;
#32151=CARTESIAN_POINT ( 'NONE',  ( 6.257116178607133428, -1.765205416791076010, -1.063208849337776485 ) ) ;
#32153=CARTESIAN_POINT ( 'NONE',  ( 1.345918344774723163, -0.8409936141995101311, 1.660288665089631799 ) ) ;
#32154=CARTESIAN_POINT ( 'NONE',  ( 4.159580895514263688, 0.8717668643758098579, 1.621812032879976329 ) ) ;
#32157=( BOUNDED_SURFACE ( )  B_SPLINE_SURFACE ( 3, 3, ( 
 ( #66773, #198919, #50565, #116686, #35369, #101444, #118823, #136094, #169646, #7123, #39648, #38587, #205331, #71051, #104664, #137167, #21231, #69982, #173949, #25523, #24441, #206405, #56969, #106839, #91631, #170711, #4973, #124194, #105757, #123142, #189100, #22296, #202110, #54837, #73196, #171783, #40733, #139302, #88409, #23379, #157683, #53770, #154477, #103589, #119903, #190157, #90553, #172870, #156616, #185877, #6055, #8206, #72126, #203191, #138233, #188020, #204247, #37513, #87335, #153402, #55899, #74291, #120988, #155544, #140386, #186955, #122056, #89489, #58030, #41812, #107925, #108985, #129523, #10332, #111114, #175004, #42877, #95895, #128459, #26590, #112189, #179261, #61232, #63367, #60160, #46068, #211729, #28735, #30883, #94820, #93755, #77475, #195503, #160871, #96962, #47139, #113256, #59093, #125253, #45005, #127387, #9281, #177118, #12465, #75353, #62300, #178193, #145729, #191214, #209586, #29810, #126315, #76406, #92691, #161948, #158737, #142515, #141466, #207474, #144657, #143594, #208524, #192275, #43936, #110051, #176064, #27660, #159794, #11397, #193360, #13540, #78540, #210672, #194427, #79610, #98023, #64433, #114321, #163010, #182426, #117508, #118573, #52447, #147827, #200796, #167269, #134789, #83865, #213846, #183501, #198668, #18854, #184559, #149956, #80689, #197614, #35109, #49258, #1525, #65464, #151027, #115379, #166188, #51387, #67589, #131615, #181373, #180319, #32997, #146780, #15658, #81745, #31939, #82803, #164078, #99074, #165127, #36180, #16718, #14593, #148879, #212795, #199741, #130577, #68665, #452, #196567, #66520, #101180, #132663, #48209, #50315, #116433, #84938, #34053, #100126, #17777, #133734, #2596, #172610, #203992, #154215, #170452, #86011, #57779, #70794, #72944, #119643, #205073, #106582, #103329, #136907, #169392, #104403, #186698, #185626, #39394, #89232, #22037, #168330, #201862, #105489, #202934, #153144, #189908, #123940, #102256, #20977, #156359, #56715, #88148, #122884, #38327, #7944, #139047, #152085, #19925, #4719, #54577, #5787, #69733, #120725, #71864, #55640, #188842, #37259, #137973, #171522, #40478, #24186, #121796, #187764, #3655, #23115, #155284, #87074, #6865, #90290, #135837, #74034, #53508, #140125, #206151, #95649, #93505, #210417, #45821, #209333, #159546, #41553, #109805, #126062, #42623, #190958, #78288, #157432, #177944, #211480, #108733, #9025, #161700, #11143, #207221, #107666, #60981, #62059, #63116, #145484, #26334, #79366, #111942, #13293, #176869, #92448, #128214, #77220, #29558, #129281, #28481, #173694, #76160, #194176, #142265, #94572, #158487, #25270, #208276, #44756, #144415, #160616, #10086, #59908, #58844, #192025, #91372, #174761, #43688, #125001, #175814, #27407, #143339, #127135, #75100, #193106, #141210, #110863, #12217, #17529, #18611, #100930, #31695, #84691, #81499, #83617, #15408, #167018, #113004, #196321, #67338, #150778, #97770, #146533, #64191, #163830, #51131, #82550, #32744, #49010, #179015, #2340, #147577, #165944, #212550, #149699, #199485, #47965, #213596, #114081, #197368, #65220, #130332, #132421, #182174, #115129, #46891, #80433, #198422, #131372, #181124, #68417, #195255, #30631, #180072, #34855, #1280, #98826, #133483, #164875, #96717, #117253, #162766, #14344, #16470, #148637, #203, #66273, #50066 ),
 ( #116189, #33803, #99882, #183252, #137726, #6615, #52195, #70539, #155030, #152889, #69480, #103080, #38080, #136658, #156101, #134544, #85757, #202683, #171268, #168079, #5533, #203745, #184307, #7687, #35931, #54332, #170200, #102009, #19677, #40217, #135588, #21784, #151838, #3414, #72695, #39147, #201609, #22862, #90043, #186443, #188584, #185376, #88975, #122623, #153966, #200549, #71613, #4467, #120471, #106326, #55390, #118321, #172349, #23939, #53258, #119388, #87893, #104152, #36996, #121545, #187516, #169135, #105228, #138790, #56461, #20730, #204810, #86825, #190706, #140949, #25012, #110612, #41301, #189650, #139866, #193914, #209078, #142011, #161439, #42367, #206962, #124746, #108478, #174502, #57531, #26079, #91114, #176612, #123688, #143085, #109552, #92193, #8768, #107409, #10884, #43428, #158242, #60715, #74850, #9831, #58591, #157173, #73770, #177683, #29295, #28224, #210150, #126879, #94317, #95388, #75907, #208026, #127960, #175557, #192836, #44495, #59653, #205897, #125811, #76959, #27147, #160358, #11961, #173432, #191773, #111676, #93251, #159285, #78034, #144159, #45561, #61793, #116989, #113812, #115924, #47698, #133214, #145215, #14075, #99617, #199220, #63916, #178755, #96454, #130072, #83348, #114861, #64967, #81235, #211222, #182989, #196067, #198164, #30367, #181912, #17271, #80165, #179812, #146270, #15149, #97508, #162505, #164618, #214380, #147317, #79097, #112743, #16203, #31431, #163565, #100674, #34606, #13020, #212282, #67079, #33544, #213344, #165683, #131121, #50867, #49798, #62848, #129009, #197109, #48748, #180861, #194986, #32483, #98557, #82285, #149433, #148378, #66010, #132159, #1014, #46622, #120204, #70281, #166753, #20477, #36731, #167814, #101747, #206438, #68151, #91665, #125286, #19414, #134284, #9313, #4213, #118064, #18348, #186179, #124228, #191246, #59128, #151579, #207509, #173982, #141501, #87632, #3147, #190187, #202414, #25554, #42910, #153704, #84427, #201349, #41843, #52989, #5272, #69216, #157717, #119126, #169937, #58062, #71350, #135335, #185106, #184049, #102818, #150516, #85492, #168873, #35668, #86564, #152626, #136397, #54070, #2077, #200289, #37813, #140421, #103889, #107955, #75387, #21521, #51940, #176098, #111154, #193397, #126352, #46105, #95927, #28772, #175038, #208557, #112223, #209625, #159834, #196598, #64468, #130610, #27698, #163047, #63401, #177154, #211763, #45041, #14626, #79646, #92725, #109019, #11434, #61266, #12502, #76444, #127425, #94854, #210707, #195539, #43971, #160905, #178230, #129554, #113289, #62335, #78574, #26624, #144694, #128494, #110086, #93795, #145762, #10367, #30919, #158772, #77510, #142552, #80721, #194462, #60192, #192312, #29845, #47176, #143630, #212830, #161982, #146812, #179296, #13573, #96995, #33029, #2624, #83895, #52474, #19954, #183532, #180350, #82836, #68695, #148911, #35138, #99107, #36206, #485, #51416, #151061, #101212, #165158, #16751, #65498, #66552, #31975, #115411, #181404, #131646, #182458, #49295, #132694, #198701, #3685, #50345, #86038, #116466, #69762, #84969, #152114, #168359, #34086, #135868, #100158, #134818, #166221, #17811, #48241, #149985, #197648, #164108, #199771, #1558, #67619, #167298, #133763, #117537, #18884, #200823, #114354, #118600, #98054, #184588, #102282, #15692, #81778, #147860 ),
 ( #213876, #24216, #9057, #22066, #136939, #41582, #171551, #40509, #188869, #170481, #53537, #186732, #205102, #23146, #106613, #139078, #88178, #89262, #157462, #119669, #154249, #21006, #185656, #107697, #7973, #56743, #74062, #37287, #138004, #140155, #5821, #202966, #71896, #105517, #204021, #75132, #201887, #153173, #55669, #90318, #87103, #72973, #122911, #103360, #169423, #4748, #121825, #155312, #70823, #54606, #173723, #120754, #6895, #38355, #104433, #206179, #172640, #187795, #156388, #39423, #57808, #25301, #123969, #189937, #91402, #160645, #96746, #12245, #11175, #209366, #113038, #78320, #14373, #195288, #46920, #190989, #42653, #176900, #193139, #129311, #28513, #94603, #179044, #194207, #177975, #63148, #108763, #127169, #95676, #43719, #208308, #92477, #29589, #174789, #26363, #207250, #30662, #62085, #61011, #141241, #109835, #59938, #192055, #175845, #27436, #125032, #93534, #158517, #159578, #77252, #10115, #143368, #76190, #144444, #162796, #44787, #58876, #110893, #142298, #126093, #210447, #128243, #45852, #111973, #161730, #13322, #79395, #145513, #211512, #184345, #35968, #34891, #2375, #67374, #117289, #102046, #115162, #15440, #134582, #50101, #133516, #199522, #49042, #146563, #65253, #83648, #116222, #51167, #17562, #181156, #182213, #168115, #212582, #32779, #114110, #64222, #200582, #100963, #149734, #167052, #130363, #16503, #18644, #98857, #81529, #164908, #198456, #82584, #80463, #196352, #31728, #148670, #183286, #180102, #165978, #1312, #47995, #97801, #163861, #237, #33837, #147609, #213628, #52230, #131402, #99917, #197399, #66310, #84723, #150812, #132457, #68453, #118358, #71648, #73806, #70574, #56499, #7724, #39180, #189684, #105265, #104187, #87927, #205931, #171305, #107444, #139900, #57564, #69516, #135624, #55427, #137762, #123721, #121579, #187550, #41336, #72731, #122657, #156140, #201645, #5569, #188620, #136692, #86861, #185412, #40252, #53292, #119425, #85794, #19715, #155066, #154001, #151874, #202717, #152926, #54368, #3448, #4504, #120508, #37030, #203782, #20767, #186484, #38116, #103116, #170237, #169173, #21821, #22897, #106363, #89013, #6654, #138827, #204846, #172387, #23975, #90077, #145251, #143121, #174536, #45595, #211257, #9865, #124780, #42403, #75941, #29329, #60751, #10918, #27180, #157204, #129049, #142042, #144194, #190739, #61826, #177720, #26112, #208057, #92224, #175590, #43466, #108510, #110645, #160392, #93286, #25048, #58627, #176646, #59684, #125844, #46657, #195024, #173469, #158275, #13054, #127993, #159322, #193948, #109585, #79135, #210188, #8801, #91150, #191801, #76994, #209113, #140987, #126914, #192871, #44527, #111711, #28258, #94351, #11993, #95423, #161476, #78068, #62880, #74880, #206996, #197143, #113850, #47732, #149467, #14110, #34640, #68184, #179845, #80199, #166786, #164654, #63951, #112778, #132190, #67116, #134315, #2110, #97542, #150548, #117027, #84458, #33577, #163600, #133249, #148415, #183024, #200323, #99650, #30403, #147349, #199255, #213376, #165719, #15182, #100711, #64999, #115958, #1051, #17307, #81271, #131153, #130106, #48781, #18380, #50901, #114897, #178790, #180895, #96490, #83385, #162540, #146303, #32517, #98591, #16238, #212315, #82322, #159460, #66047, #196099, #31469, #198199, #49833, #181948, #56230, #5301 ),
 ( #19445, #106097, #103923, #3177, #51973, #71383, #6386, #7457, #155867, #36764, #89821, #122391, #23713, #187285, #102850, #72458, #87663, #188348, #73534, #38912, #184083, #86594, #138559, #152660, #104996, #168905, #39987, #4242, #55166, #154799, #171036, #20509, #70313, #69248, #136429, #35701, #119154, #185137, #135365, #186212, #53021, #202444, #54100, #139637, #120236, #118099, #37844, #101777, #88743, #167845, #172119, #169967, #85522, #21553, #151608, #201381, #153733, #137495, #203511, #204580, #121311, #22633, #189424, #41065, #24779, #91951, #58362, #140718, #8533, #57296, #75677, #90881, #108246, #107173, #174270, #158013, #173199, #156942, #74612, #206732, #124516, #190474, #42134, #25844, #9600, #205660, #141787, #123461, #36772, #55173, #186221, #187294, #173206, #69256, #3185, #22642, #172126, #24786, #107180, #202454, #41073, #7464, #189431, #138566, #54108, #23720, #38920, #73543, #90889, #204587, #135373, #37852, #89827, #103931, #56239, #120243, #205667, #169975, #6393, #106104, #122398, #21563, #87669, #20519, #153741, #201391, #70321, #136438, #86602, #137502, #4252, #5309, #71390, #53029, #203519, #119162, #121318, #185148, #39996, #102858, #123468, #105004, #168914, #171043, #152668, #88750, #154807, #72466, #188356, #155875, #139646, #57305, #108255, #25851, #207799, #12788, #44263, #208856, #10662, #140726, #112508, #125585, #127727, #174276, #45329, #161202, #158020, #191545, #9608, #159066, #26916, #91961, #94092, #143927, #76734, #8540, #110385, #60487, #142852, #160131, #30130, #178520, #156948, #75685, #210988, #111448, #126645, #177453, #93025, #62615, #193685, #206739, #74622, #59427, #109326, #192610, #124524, #175334, #176390, #27995, #29067, #141795, #43210, #11730, #95150, #78862, #77806, #209922, #58370, #61561, #144983, #128777, #194754, #46391, #190481, #42140, #51723, #163336, #63693, #150293, #148156, #47468, #117845, #50639, #18117, #83126, #132992, #183837, #130893, #31207, #1860, #65783, #149206, #781, #64751, #162270, #81009, #82064, #129847, #195830, #214157, #196887, #131933, #96219, #13857, #48525, #113583, #79934, #67921, #116765, #99399, #182763, #146039, #32263, #34380, #114645, #97281, #180638, #197943, #98330, #212053, #179585, #14915, #164396, #198993, #147097, #181688, #165452, #213121, #15979, #49571, #115696, #33318, #17047, #66848, #134065, #100453, #166526, #84204, #200074, #122136, #154555, #69000, #138311, #205414, #87420, #89571, #86345, #72203, #23459, #54916, #57053, #121067, #119984, #103676, #7205, #187035, #123217, #155620, #73278, #85272, #151359, #71132, #153486, #139382, #137250, #203270, #35446, #88494, #204326, #171865, #2928, #21313, #55984, #152416, #102602, #201133, #188102, #135117, #52771, #101525, #167595, #170793, #169724, #19194, #3995, #168656, #70064, #136176, #202195, #118907, #53851, #184891, #38667, #36515, #5057, #20261, #185961, #37593, #104746, #22385, #6134, #39733, #105838, #190234, #157764, #41893, #140475, #189181, #78623, #207554, #109071, #76490, #61320, #124276, #75436, #126401, #143684, #193451, #142600, #92778, #40818, #42962, #59174, #108004, #174031, #11489, #90638, #111204, #144747, #25602, #156698, #28822, #26675, #206487, #106926, #208610, #209676, #210759, #62379, #91715, #12548, #45095, #160958, #110138, #9364, #127480 ),
 ( #10418, #172950, #27750, #77561, #177208, #24529, #175087, #94907, #141548, #125333, #58117, #8289, #74373, #191296, #158822, #60242, #176150, #192361, #44019, #93846, #159884, #179348, #163098, #30970, #112270, #80775, #79695, #81827, #100204, #114402, #128543, #97045, #63452, #29893, #65548, #98105, #14678, #49341, #129605, #146862, #195591, #145808, #194509, #17862, #83945, #82883, #50395, #115460, #165209, #150036, #212884, #47225, #182505, #164156, #181450, #33081, #64515, #46157, #113343, #180400, #95979, #162031, #32020, #130660, #15742, #1606, #178284, #196650, #13622, #211815, #34135, #148960, #131693, #532, #48290, #147910, #66599, #213925, #197699, #99156, #16799, #132745, #198747, #116515, #166270, #167347, #187844, #68746, #169470, #18933, #101263, #154296, #186779, #85019, #170531, #23194, #119723, #121873, #118652, #104488, #55719, #87152, #89310, #153223, #152164, #135914, #39470, #4793, #155357, #105568, #171601, #117589, #183580, #103409, #185702, #67666, #21055, #70871, #133810, #120803, #22116, #204067, #35187, #53588, #88227, #184638, #134868, #151108, #5871, #2674, #200875, #199824, #51465, #203013, #201932, #52520, #36255, #102335, #168407, #20004, #86088, #3733, #69808, #37336, #136986, #54655, #38406, #71944, #138054, #156440, #122959, #158568, #191042, #189983, #142350, #8024, #41635, #74114, #172688, #6942, #110943, #176950, #175897, #143421, #208360, #43771, #28566, #107749, #140209, #61061, #42707, #59991, #126144, #173775, #73023, #206229, #207303, #188919, #40557, #58925, #25350, #108815, #94653, #139121, #91450, #106662, #205148, #127220, #27488, #10167, #93588, #56791, #157511, #159632, #9106, #57856, #75182, #125084, #141294, #24266, #90371, #124018, #174838, #109884, #26416, #92528, #76241, #11228, #192106, #209415, #77308, #193189, #44837, #285, #212626, #112020, #160697, #180150, #115209, #116268, #50145, #145560, #198500, #164956, #132502, #81574, #211558, #181199, #196399, #16548, #182258, #147658, #78371, #195335, #32827, #46966, #213674, #63193, #148715, #113083, #163911, #49089, #65299, #129357, #179089, #178021, #30711, #144491, #13369, #79443, #29639, #80511, #161777, #96794, #162843, #33883, #14421, #12291, #146608, #210499, #197448, #62134, #66356, #64267, #128294, #130411, #194256, #45902, #95725, #48044, #114157, #98903, #31776, #97848, #15487, #131447, #82630, #170279, #201693, #151916, #168159, #83696, #55471, #68497, #70622, #117337, #202761, #104233, #101011, #134625, #167102, #102089, #184390, #183334, #37079, #86907, #19757, #166025, #53336, #3489, #85839, #103158, #187595, #121626, #99961, #18688, #154046, #54412, #69559, #120552, #36009, #5612, #136736, #149784, #17610, #150857, #52277, #135669, #67420, #118403, #119471, #185458, #186531, #34938, #200629, #169219, #38160, #21867, #20811, #152975, #1358, #4550, #87973, #84771, #2420, #133562, #71695, #137807, #199569, #51213, #203826, #44304, #77845, #6700, #138875, #162310, #40302, #143968, #204893, #72776, #128813, #161242, #56546, #145025, #212092, #94133, #96257, #90123, #78903, #30169, #61601, #63728, #127771, #126689, #110426, #13895, #193727, #129887, #79976, #146080, #89059, #155117, #209962, #160172, #39222, #45371, #111487, #105312, #95191, #211029, #178559, #122706, #28038, #62654, #156190, #106410, #188670 ),
 ( #76774, #10705, #22944, #208897, #172433, #177495, #171351, #11772, #24022, #142897, #60528, #192651, #29108, #12828, #176429, #194794, #46431, #112549, #48565, #147135, #195871, #85315, #151399, #150333, #117884, #182806, #18159, #2971, #16019, #130935, #35489, #165495, #34423, #100496, #164433, #47510, #180678, #181728, #163379, #14953, #33359, #82105, #17089, #69039, #113622, #148198, #81051, #179625, #101567, #1900, #199033, #67960, #31245, #131975, #134104, #214198, #196928, #65827, #99440, #197985, #97322, #213161, #64791, #49613, #84247, #114685, #32303, #83167, #98370, #115738, #149250, #823, #66893, #133033, #50681, #116806, #166571, #200113, #167634, #51764, #183876, #19235, #52813, #71172, #155660, #153528, #70104, #103713, #38708, #137290, #156737, #135156, #86387, #203308, #171907, #168697, #6175, #138351, #184930, #8328, #36554, #54957, #170834, #102641, #20302, #40859, #136217, #22425, #152455, #4034, #7242, #39777, #202237, #23503, #90676, #187075, #189220, #185999, #89609, #123255, #154597, #201174, #72244, #5097, #121109, #106965, #204368, #118951, #172989, #24570, #53889, #120024, #88535, #104788, #37634, #56025, #122179, #169764, #188145, #73319, #57090, #21353, #105882, #139422, #87460, #205457, #25639, #111240, #41930, #190273, #140512, #194544, #209712, #142640, #162066, #42997, #141585, #125368, #109110, #191332, #58155, #26712, #91751, #27786, #46190, #60280, #74413, #175125, #9402, #108042, #11527, #44056, #92814, #61357, #75472, #158858, #207592, #157804, #206524, #178322, #29930, #28857, #210792, #127516, #177244, #96014, #10455, #59211, #128579, #110175, #193488, #45130, #76528, #208649, #174067, #112306, #126437, #192400, #124314, #93884, #94944, #176186, #159923, #77597, #143720, #78656, #160992, #12584, #144784, #62415, #49370, #17893, #199855, #148988, #145844, #48323, #182538, #114434, #563, #212916, #1638, #180433, #16832, #116546, #66629, #64550, #130694, #31004, #196684, #211850, #80806, #146896, #97078, #147944, #14714, #32050, #98139, #183614, #164188, #51496, #15774, #35221, #50427, #117623, #133844, #81860, #101297, #213957, #13656, #79728, #63487, #197730, #65578, #100236, #129642, #131725, #179383, #163131, #115488, #83979, #181481, #33111, #99188, #195628, #47263, #165239, #198778, #82915, #34165, #150067, #132775, #166304, #67697, #113377, #37364, #184668, #104517, #154327, #87185, #18966, #120833, #70904, #21082, #170561, #40589, #122991, #188949, #86121, #6971, #121905, #169500, #55749, #103439, #73052, #138083, #151137, #167377, #3762, #119752, #137015, #134897, #185731, #153250, #54683, #39501, #102366, #53619, #22144, #187874, #171631, #186809, #203042, #85050, #4825, #38437, #168436, #20035, #204097, #68778, #89340, #2704, #200903, #88258, #5901, #71974, #139151, #105599, #52552, #205180, #56822, #118683, #36288, #23228, #155388, #152195, #69837, #135947, #201963, #159660, #143451, #28599, #156471, #92558, #61093, #9138, #173803, #57886, #209448, #74146, #8059, #172719, #12322, #27519, #174869, #194289, #75212, #25381, #157541, #141323, #207336, #90401, #58958, #124049, #60022, #78403, #158598, #106694, #125113, #41667, #140239, #43802, #76272, #191071, #93618, #107778, #42737, #91481, #190015, #24297, #210533, #62167, #127252, #94687, #11261, #193223, #128326, #108843 ),
 ( #10197, #26449, #142380, #206261, #208389, #126174, #192137, #109915, #160729, #44870, #175926, #110975, #77338, #176981, #144523, #64296, #195366, #14452, #163943, #48074, #67451, #45934, #211588, #114185, #82662, #79474, #131476, #49123, #95755, #133596, #161807, #180183, #81603, #13398, #145592, #166057, #46997, #147688, #63224, #129387, #132534, #164989, #113114, #148746, #1390, #97882, #99991, #96823, #315, #33915, #65329, #112053, #149819, #178053, #66386, #182289, #32859, #198531, #29671, #80543, #179119, #17643, #15518, #98934, #16579, #146640, #30742, #162872, #31806, #212655, #130442, #213705, #196429, #197479, #115241, #181231, #50178, #116298, #83728, #39257, #5648, #202796, #71729, #117370, #135702, #137841, #3520, #134656, #168191, #103193, #201728, #6733, #199602, #150890, #53369, #21900, #18718, #70658, #54446, #34971, #72812, #101043, #119504, #20842, #167133, #84802, #105351, #200659, #86941, #2452, #68528, #203863, #104266, #52308, #88010, #155151, #37115, #171388, #36042, #154081, #187630, #4584, #51244, #136768, #69592, #185489, #22979, #120588, #183367, #89098, #118438, #184425, #102122, #153007, #169256, #19790, #186566, #38194, #85872, #170312, #55508, #121662, #151950, #124859, #93369, #41419, #206012, #90162, #175673, #106448, #40342, #204933, #44611, #59771, #207078, #12082, #107526, #57647, #189767, #173557, #25130, #122743, #91232, #156228, #92313, #110727, #190823, #138913, #157292, #73898, #172471, #76025, #108593, #8882, #125930, #139991, #74961, #123807, #7805, #176727, #141071, #160475, #27261, #28340, #94436, #58710, #56584, #42484, #188706, #24059, #174621, #26197, #158356, #11004, #9949, #142128, #208141, #191888, #43550, #209199, #109671, #159405, #77081, #143209, #60839, #127000, #192959, #95509, #180979, #82406, #79221, #46746, #145339, #80286, #162618, #161556, #15266, #65081, #212399, #144279, #31551, #196179, #146385, #81353, #165803, #33657, #99732, #211340, #132270, #32601, #64041, #98676, #14194, #198279, #48864, #61911, #78149, #129134, #30486, #47821, #45679, #96570, #130186, #179928, #164732, #13145, #178875, #147433, #16321, #148495, #97626, #113932, #210273, #163684, #213457, #62964, #195110, #114979, #194029, #63, #128073, #112859, #111796, #49920, #131235, #29418, #177801, #197224, #66127, #116041, #182029, #2194, #55253, #21637, #203600, #152745, #68270, #186298, #53109, #87745, #121400, #4326, #149551, #52053, #37934, #118180, #70396, #134403, #5392, #184167, #20592, #120322, #136514, #200405, #35788, #34718, #101864, #1136, #84543, #150633, #100789, #151697, #18465, #167932, #19532, #187372, #85608, #3265, #86678, #105087, #39002, #17388, #69333, #71469, #104008, #135444, #170052, #201465, #137582, #202533, #67199, #83471, #119242, #185225, #36849, #199340, #102932, #168993, #54182, #153821, #166872, #133336, #50986, #117108, #183109, #124603, #74700, #171125, #24865, #41154, #172209, #106185, #207882, #72548, #93103, #126731, #23799, #138647, #10746, #8618, #122478, #22719, #190563, #125662, #192691, #60572, #155956, #208937, #175413, #142936, #92042, #7542, #191624, #206815, #26996, #44345, #158099, #88833, #205748, #43287, #57380, #9687, #73626, #159144, #123544, #174356, #59505, #75765, #139725, #189508, #188439, #107263, #154888, #89904, #173283, #40073, #90968 ) ),
 .UNSPECIFIED., .T., .F., .T. ) 
 B_SPLINE_SURFACE_WITH_KNOTS ( ( 4, 3, 4 ),
 ( 4, 1, 1, 1, 1, 1, 1, 1, 1, 1, 1, 1, 1, 1, 1, 1, 1, 1, 1, 1, 1, 1, 1, 1, 1, 1, 1, 1, 1, 1, 1, 1, 1, 1, 1, 1, 1, 1, 1, 1, 1, 1, 1, 1, 1, 1, 1, 1, 1, 1, 1, 1, 1, 1, 1, 1, 1, 1, 1, 1, 1, 1, 1, 1, 1, 1, 1, 1, 1, 1, 1, 1, 1, 1, 1, 1, 1, 1, 1, 1, 1, 1, 1, 1, 1, 1, 1, 1, 1, 1, 1, 1, 1, 1, 1, 1, 1, 1, 1, 1, 1, 1, 1, 1, 1, 1, 1, 1, 1, 1, 1, 1, 1, 1, 1, 1, 1, 1, 1, 1, 1, 1, 1, 1, 1, 1, 1, 1, 1, 1, 1, 1, 1, 1, 1, 1, 1, 1, 1, 1, 1, 1, 1, 1, 1, 1, 1, 1, 1, 1, 1, 1, 1, 1, 1, 1, 1, 1, 1, 1, 1, 1, 1, 1, 1, 1, 1, 1, 1, 1, 1, 1, 1, 1, 1, 1, 1, 1, 1, 1, 1, 1, 1, 1, 1, 1, 1, 1, 1, 1, 1, 1, 1, 1, 1, 1, 1, 1, 1, 1, 1, 1, 1, 1, 1, 1, 1, 1, 1, 1, 1, 1, 1, 1, 1, 1, 1, 1, 1, 1, 1, 1, 1, 1, 1, 1, 1, 1, 1, 1, 1, 1, 1, 1, 1, 1, 1, 1, 1, 1, 1, 1, 1, 1, 1, 1, 1, 1, 1, 1, 1, 1, 1, 1, 1, 1, 1, 1, 1, 1, 1, 1, 1, 1, 1, 1, 1, 1, 1, 1, 1, 1, 1, 1, 1, 1, 1, 1, 1, 1, 1, 1, 1, 1, 1, 1, 1, 1, 1, 1, 1, 1, 1, 1, 1, 1, 1, 1, 1, 1, 1, 1, 1, 1, 1, 1, 1, 1, 1, 1, 1, 1, 1, 1, 1, 1, 1, 1, 1, 1, 1, 1, 1, 1, 1, 1, 1, 1, 1, 1, 1, 1, 1, 1, 1, 1, 1, 1, 1, 1, 1, 1, 1, 1, 1, 1, 1, 1, 1, 1, 1, 1, 1, 1, 1, 1, 1, 1, 1, 1, 1, 1, 1, 1, 1, 1, 1, 1, 1, 1, 1, 1, 1, 1, 1, 1, 1, 1, 1, 1, 1, 1, 1, 1, 4 ),
 ( 0.000000000000000000, 0.5000000000000000000, 1.000000000000000000 ),
 ( 0.000000000000000000, 0.002600034503794030130, 0.005208798665460326327, 0.007813183304800875098, 0.01041632952039499814, 0.01302078637366306003, 0.01562487905948694092, 0.01822913957756216313, 0.02083328395591756144, 0.02343739818322774712, 0.02604168118785421884, 0.02864568517727394958, 0.03125004130332968699, 0.03385401862675675722, 0.03645834363201481965, 0.03906241290072134942, 0.04166661303991354287, 0.04427083116291704451, 0.04687488238457573897, 0.04947921467585455341, 0.05208318889621989245, 0.05468754274347345512, 0.05729155431138267807, 0.05989582568988525285, 0.06249996760622017478, 0.06510408932096034551, 0.06770837349117478365, 0.07031237295078232585, 0.07291672927807971161, 0.07552070761765239393, 0.07812503204114096267, 0.08072910085791458468, 0.08333330089851145872, 0.08593751883178461781, 0.08854156980611090078, 0.09114590188302622298, 0.09374987588873062716, 0.09635422952249227124, 0.09895824087764454324, 0.1015625120427016276, 0.1041666537503683765, 0.1067707752516706410, 0.1093750592157429480, 0.1119790584643299974, 0.1145834145867499904, 0.1171873927198607973, 0.1197917169388799108, 0.1223957855539345302, 0.1249999853896588409, 0.1276042031245507580, 0.1302082538950744550, 0.1328125857752754935, 0.1354165595809520839, 0.1380209130188291833, 0.1406249241787864424, 0.1432291951479887082, 0.1458333366646657747, 0.1484374579699756502, 0.1510417417453218114, 0.1536457408005802994, 0.1562500967354857329, 0.1588540746797905134, 0.1614583987117299280, 0.1640624671426803571, 0.1666666667910262079, 0.1692708843450304312, 0.1718749349293641482, 0.1744792666302357464, 0.1770832402535473249, 0.1796875935129024493, 0.1822916044953091785, 0.1848958752860835608, 0.1875000166293293857, 0.1901041377562054102, 0.1927084213602507368, 0.1953124202398235920, 0.1979167760045740521, 0.2005207537777317084, 0.2031250776399721736, 0.2057291459044250093, 0.2083333453828807025, 0.2109375627734847158, 0.2135416131892344249, 0.2161459447281551538, 0.2187499181867580689, 0.2213542712849473904, 0.2239582821074418695, 0.2265625527372090720, 0.2291666939245756707, 0.2317708148905701926, 0.2343750983407339450, 0.2369790970622578097, 0.2395834526742069426, 0.2421874302938704648, 0.2447917540037867212, 0.2473958221193426621, 0.2500000214453905190, 0.2526042386900758108, 0.2552082889548416555, 0.2578126203491843960, 0.2604165936607292231, 0.2630209466151033904, 0.2656249572953180982, 0.2682292277814931625, 0.2708333688305272213, 0.2734374896531870935, 0.2760417729668830367, 0.2786457715479891406, 0.2812501270244852081, 0.2838541045083020076, 0.2864584280832634389, 0.2890624960675178268, 0.2916666952586349781, 0.2942709123748779576, 0.2968749625062547248, 0.2994792937733871119, 0.3020832669555192918, 0.3046876197834237909, 0.3072916303389863768, 0.3098959006989794318, 0.3125000416272227799, 0.3151041623240899980, 0.3177084455187270673, 0.3203124439770417831, 0.3229167993354283839, 0.3255207767010412923, 0.3281251001584127303, 0.3307291680289564662, 0.3333333671026155187, 0.3359375841078879321, 0.3385416341234662174, 0.3411459652807516951, 0.3437499383511121720, 0.3463542910698884647, 0.3489583015184220538, 0.3515625717696388985, 0.3541667125946290073, 0.3567708331832410984, 0.3593751162762241491, 0.3619791146293697692, 0.3645834698869864221, 0.3671874471520340522, 0.3697917705091763874, 0.3723958382835964032, 0.3750000372572658280, 0.3776042541690359799, 0.3802083040864021046, 0.3828126351512001757, 0.3854166081274262856, 0.3880209607544118922, 0.3906249711135359459, 0.3932292412733790488, 0.3958333820126498370, 0.3984375025105409418, 0.4010417855192715542, 0.4036457837848667074, 0.4062501389590495449, 0.4088541161411674008, 0.4114584394154381930, 0.4140625071113177014, 0.4166667060024629166, 0.4192709228381954478, 0.4218749726749327911, 0.4244793036646000717, 0.4270832765643259310, 0.4296876291168554296, 0.4322916394041865784, 0.4348959094900549660, 0.4375000501611374104, 0.4401041705858387276, 0.4427084535277153732, 0.4453124517233759683, 0.4479168068314584583, 0.4505207839482789911, 0.4531251071570330247, 0.4557291747919532399, 0.4583333736180368323, 0.4609375903951940523, 0.4635416401688834398, 0.4661459711007739370, 0.4687499439416310532, 0.4713542964370365795, 0.4739583066701890113, 0.4765625766994796009, 0.4791667173199026797, 0.4817708376889431876, 0.4843751205813623395, 0.4869791187247021202, 0.4895834737840155659, 0.4921874508531692838, 0.4947917740137594000, 0.4973958416052992049, 0.5000000403837819851, 0.5026042571198243714, 0.5052083068480445194, 0.5078126377395105751, 0.5104166105391289010, 0.5130209629947408700, 0.5156249731913270518, 0.5182292431814352618, 0.5208333837687260104, 0.5234375040996330775, 0.5260417869599895990, 0.5286457850686206994, 0.5312501400964950715, 0.5338541171356111503, 0.5364584402653888029, 0.5390625078311259699, 0.5416667065794673608, 0.5442709232918542250, 0.5468749729921829061, 0.5494793038605755298, 0.5520832766365837418, 0.5546876290697317913, 0.5572916392473630243, 0.5598959092156829964, 0.5625000497873680061, 0.5651041700976676685, 0.5677084529433557014, 0.5703124510348895893, 0.5729168060486536929, 0.5755207830753605869, 0.5781251061916765632, 0.5807291737491879768, 0.5833333724848467350, 0.5859375891910368894, 0.5885416388810509325, 0.5911459697437208005, 0.5937499425137473530, 0.5963542949417601768, 0.5989583051180477069, 0.6015625750819736384, 0.6041667156555785567, 0.6067708359627971282, 0.6093751188112106476, 0.6119791169032582356, 0.6145834719202413199, 0.6171874489521673723, 0.6197917720723722379, 0.6223958396392350600, 0.6250000383796699976, 0.6276042550971219214, 0.6302083047943985994, 0.6328126356686964993, 0.6354166084503697354, 0.6380209608905765828, 0.6406249710831318778, 0.6432292410600577437, 0.6458333816531092175, 0.6484375019747732338, 0.6510417848433065480, 0.6536457829534795261, 0.6562501379910111732, 0.6588541150457848383, 0.6614584381872300467, 0.6640625057810221055, 0.6666667045436925898, 0.6692709212898660942, 0.6718749710119833463, 0.6744793019152608426, 0.6770832747262099938, 0.6796876271959411131, 0.6822916374223763070, 0.6848959074296973037, 0.6875000480597228680, 0.6901041684133596421, 0.6927084513194080584, 0.6953124494653194487, 0.6979168045407300180, 0.7005207816359816375, 0.7031251048160196415, 0.7057291724543196532, 0.7083333712566866058, 0.7109375880490425015, 0.7135416378135795989, 0.7161459687631898108, 0.7187499416210458847, 0.7213542941376326345, 0.7239583044155618596, 0.7265625744706748490, 0.7291667151552034820, 0.7317708355583423252, 0.7343751185193033715, 0.7369791167185673064, 0.7395834718491895998, 0.7421874490025512916, 0.7447917722385364314, 0.7473958399389256657, 0.7500000387984516736, 0.7526042556544531026, 0.7552083054789914263, 0.7578126364922896929, 0.7604166094146853627, 0.7630209619954617661, 0.7656249723425013753, 0.7682292424628052174, 0.7708333832193684509, 0.7734375036895410060, 0.7760417867228139865, 0.7786457849930478181, 0.7812501401962168579, 0.7838541174253229604, 0.7864584407346123518, 0.7890625085146746320, 0.7916667074488250577, 0.7942709243859374935, 0.7968749742880611997, 0.7994793053824050810, 0.8020832783869765725, 0.8046876310492792062, 0.8072916414830481058, 0.8098959116859448804, 0.8125000525320774658, 0.8151041730868179291, 0.8177084562098055898, 0.8203124545686294455, 0.8229168098616829186, 0.8255207871841712119, 0.8281251105841250792, 0.8307291784614470043, 0.8333333774876906519, 0.8359375945233833427, 0.8385416445206798075, 0.8411459757134309712, 0.8437499488178175078, 0.8463543015789862789, 0.8489583121171074831, 0.8515625824200027116, 0.8541667233732427311, 0.8567708440300897399, 0.8593751272601987123, 0.8619791257252362726, 0.8645834811255164176, 0.8671874585590289009, 0.8697917820670107991, 0.8723958500591838527, 0.8750000491949933012, 0.8776042663467393812, 0.8802083164568000884, 0.8828126477653241988, 0.8854166209871692228, 0.8880209738645485906, 0.8906249845246493324, 0.8932292549449527552, 0.8958333960228427317, 0.8984375167993386979, 0.9010418001539796107, 0.9036457987428592187, 0.9062501542677121602, 0.9088541318298947180, 0.9114584554632734203, 0.9140625235878931942, 0.9166667228507454634, 0.9192709401360219523, 0.9218749903764450471, 0.9244793218181143191, 0.9270832951750564987, 0.9296876481859919217, 0.9322916589857459524, 0.9348959295408556525, 0.9375000707608250883, 0.9401041916746273319, 0.9427084751713679101, 0.9453124739016935951, 0.9479168295687272483, 0.9505208072738278169, 0.9531251310501845930, 0.9557291993520028450, 0.9583333987332913750, 0.9609376160454207172, 0.9635416666839513589, 0.9661459986354887786, 0.9687499708159389433, 0.9713543235632202677, 0.9739583390673558494, 0.9765626083347638264, 0.9791667417950460361, 0.9817708662416058107, 0.9843751381318576188, 0.9869792129215403387, 0.9895836736503123010, 0.9921868305638316121, 0.9947912020913856068, 0.9973999845648282569, 1.000000000000000000 ),
 .UNSPECIFIED. ) 
 GEOMETRIC_REPRESENTATION_ITEM ( )  RATIONAL_B_SPLINE_SURFACE ( (
 ( 1.000000000000000222, 1.000000000000000222, 1.000000000000000222, 1.000000000000000222, 0.9999999999999996669, 0.9999999999999997780, 1.000000000000000444, 1.000000000000000000, 1.000000000000000000, 1.000000000000000000, 0.9999999999999997780, 1.000000000000000000, 1.000000000000000000, 1.000000000000000000, 1.000000000000000000, 0.9999999999999997780, 1.000000000000000222, 0.9999999999999996669, 1.000000000000000000, 0.9999999999999997780, 1.000000000000000222, 1.000000000000000000, 1.000000000000000222, 0.9999999999999996669, 1.000000000000000000, 1.000000000000000222, 0.9999999999999996669, 1.000000000000000444, 1.000000000000000000, 0.9999999999999997780, 1.000000000000000222, 1.000000000000000222, 1.000000000000000222, 1.000000000000000000, 1.000000000000000000, 0.9999999999999997780, 1.000000000000000000, 1.000000000000000000, 1.000000000000000000, 1.000000000000000000, 1.000000000000000222, 1.000000000000000222, 1.000000000000000000, 1.000000000000000000, 1.000000000000000000, 0.9999999999999996669, 1.000000000000000222, 1.000000000000000000, 1.000000000000000000, 0.9999999999999997780, 0.9999999999999997780, 1.000000000000000000, 0.9999999999999996669, 1.000000000000000222, 0.9999999999999997780, 1.000000000000000222, 0.9999999999999997780, 0.9999999999999997780, 1.000000000000000222, 1.000000000000000222, 0.9999999999999997780, 1.000000000000000222, 1.000000000000000000, 1.000000000000000222, 1.000000000000000000, 0.9999999999999997780, 1.000000000000000000, 1.000000000000000000, 1.000000000000000222, 1.000000000000000222, 1.000000000000000000, 0.9999999999999997780, 1.000000000000000000, 1.000000000000000222, 0.9999999999999997780, 1.000000000000000444, 0.9999999999999996669, 1.000000000000000000, 1.000000000000000222, 0.9999999999999997780, 0.9999999999999997780, 0.9999999999999997780, 1.000000000000000000, 0.9999999999999997780, 1.000000000000000000, 0.9999999999999997780, 1.000000000000000222, 1.000000000000000000, 1.000000000000000222, 1.000000000000000000, 0.9999999999999997780, 1.000000000000000000, 1.000000000000000000, 0.9999999999999997780, 1.000000000000000222, 1.000000000000000000, 1.000000000000000000, 1.000000000000000000, 1.000000000000000222, 0.9999999999999996669, 1.000000000000000222, 1.000000000000000000, 1.000000000000000000, 0.9999999999999997780, 1.000000000000000000, 0.9999999999999997780, 1.000000000000000000, 1.000000000000000222, 1.000000000000000000, 0.9999999999999997780, 1.000000000000000222, 1.000000000000000222, 0.9999999999999996669, 1.000000000000000222, 1.000000000000000000, 1.000000000000000444, 0.9999999999999996669, 1.000000000000000000, 1.000000000000000222, 1.000000000000000222, 1.000000000000000222, 1.000000000000000222, 1.000000000000000000, 0.9999999999999997780, 1.000000000000000222, 1.000000000000000000, 1.000000000000000222, 0.9999999999999996669, 1.000000000000000000, 1.000000000000000000, 1.000000000000000222, 1.000000000000000222, 0.9999999999999997780, 1.000000000000000000, 0.9999999999999997780, 1.000000000000000222, 1.000000000000000000, 1.000000000000000222, 1.000000000000000000, 1.000000000000000444, 0.9999999999999996669, 1.000000000000000444, 0.9999999999999996669, 0.9999999999999997780, 0.9999999999999997780, 1.000000000000000222, 1.000000000000000000, 0.9999999999999997780, 1.000000000000000000, 0.9999999999999997780, 0.9999999999999996669, 1.000000000000000222, 1.000000000000000000, 0.9999999999999997780, 1.000000000000000000, 1.000000000000000000, 1.000000000000000222, 1.000000000000000000, 1.000000000000000000, 1.000000000000000444, 0.9999999999999997780, 1.000000000000000222, 1.000000000000000222, 0.9999999999999997780, 1.000000000000000444, 0.9999999999999996669, 1.000000000000000000, 0.9999999999999997780, 1.000000000000000222, 0.9999999999999997780, 1.000000000000000222, 1.000000000000000000, 1.000000000000000222, 0.9999999999999997780, 0.9999999999999997780, 1.000000000000000000, 1.000000000000000000, 0.9999999999999997780, 1.000000000000000222, 0.9999999999999997780, 1.000000000000000000, 1.000000000000000000, 1.000000000000000222, 1.000000000000000000, 0.9999999999999997780, 1.000000000000000222, 1.000000000000000444, 1.000000000000000000, 1.000000000000000000, 1.000000000000000000, 1.000000000000000000, 0.9999999999999997780, 1.000000000000000000, 1.000000000000000222, 1.000000000000000000, 1.000000000000000222, 0.9999999999999996669, 1.000000000000000000, 1.000000000000000000, 0.9999999999999994449, 1.000000000000000444, 1.000000000000000000, 1.000000000000000222, 0.9999999999999997780, 1.000000000000000000, 1.000000000000000222, 1.000000000000000000, 0.9999999999999996669, 1.000000000000000444, 0.9999999999999997780, 1.000000000000000444, 0.9999999999999996669, 1.000000000000000000, 0.9999999999999996669, 1.000000000000000444, 1.000000000000000000, 0.9999999999999997780, 1.000000000000000222, 1.000000000000000000, 0.9999999999999997780, 1.000000000000000444, 1.000000000000000222, 0.9999999999999997780, 1.000000000000000000, 1.000000000000000222, 0.9999999999999997780, 1.000000000000000222, 1.000000000000000222, 1.000000000000000000, 1.000000000000000000, 0.9999999999999996669, 1.000000000000000222, 0.9999999999999997780, 1.000000000000000000, 0.9999999999999997780, 1.000000000000000444, 1.000000000000000000, 1.000000000000000000, 0.9999999999999997780, 1.000000000000000444, 1.000000000000000000, 0.9999999999999997780, 1.000000000000000444, 0.9999999999999996669, 1.000000000000000444, 1.000000000000000000, 1.000000000000000444, 1.000000000000000222, 1.000000000000000222, 0.9999999999999997780, 1.000000000000000000, 0.9999999999999997780, 1.000000000000000444, 0.9999999999999996669, 1.000000000000000000, 1.000000000000000000, 1.000000000000000222, 1.000000000000000000, 1.000000000000000222, 1.000000000000000000, 1.000000000000000000, 0.9999999999999997780, 1.000000000000000000, 1.000000000000000000, 0.9999999999999997780, 1.000000000000000000, 1.000000000000000000, 0.9999999999999997780, 1.000000000000000000, 1.000000000000000222, 1.000000000000000000, 1.000000000000000000, 1.000000000000000000, 1.000000000000000000, 0.9999999999999996669, 1.000000000000000222, 1.000000000000000000, 0.9999999999999997780, 1.000000000000000000, 1.000000000000000222, 1.000000000000000000, 1.000000000000000222, 1.000000000000000222, 1.000000000000000000, 1.000000000000000222, 1.000000000000000000, 1.000000000000000000, 1.000000000000000000, 1.000000000000000222, 0.9999999999999996669, 1.000000000000000222, 0.9999999999999996669, 1.000000000000000222, 1.000000000000000222, 1.000000000000000222, 1.000000000000000222, 0.9999999999999996669, 1.000000000000000444, 1.000000000000000000, 1.000000000000000000, 1.000000000000000222, 1.000000000000000444, 0.9999999999999996669, 1.000000000000000444, 1.000000000000000222, 0.9999999999999996669, 1.000000000000000222, 0.9999999999999997780, 1.000000000000000000, 1.000000000000000000, 0.9999999999999997780, 1.000000000000000000, 0.9999999999999997780, 1.000000000000000000, 1.000000000000000000, 1.000000000000000444, 0.9999999999999997780, 1.000000000000000222, 0.9999999999999997780, 0.9999999999999997780, 1.000000000000000000, 1.000000000000000000, 0.9999999999999996669, 1.000000000000000000, 1.000000000000000222, 1.000000000000000222, 0.9999999999999997780, 1.000000000000000222, 0.9999999999999997780, 0.9999999999999997780, 1.000000000000000000, 1.000000000000000000, 1.000000000000000000, 1.000000000000000222, 1.000000000000000000, 1.000000000000000222, 1.000000000000000000, 0.9999999999999996669, 0.9999999999999997780, 1.000000000000000444, 0.9999999999999996669, 1.000000000000000444, 0.9999999999999997780, 0.9999999999999997780, 1.000000000000000222, 0.9999999999999997780, 1.000000000000000222, 1.000000000000000000, 1.000000000000000000, 0.9999999999999997780, 1.000000000000000222, 1.000000000000000222, 1.000000000000000000, 1.000000000000000222, 1.000000000000000000, 1.000000000000000000, 0.9999999999999997780, 1.000000000000000000, 1.000000000000000000, 0.9999999999999997780, 1.000000000000000000, 0.9999999999999996669, 1.000000000000000222, 0.9999999999999997780, 1.000000000000000222, 0.9999999999999997780, 1.000000000000000000, 0.9999999999999997780, 1.000000000000000222, 0.9999999999999997780, 1.000000000000000000, 1.000000000000000000, 1.000000000000000000, 1.000000000000000000, 0.9999999999999997780, 1.000000000000000222, 1.000000000000000000, 0.9999999999999997780, 1.000000000000000000, 1.000000000000000000, 1.000000000000000222, 1.000000000000000222, 1.000000000000000000, 1.000000000000000222, 1.000000000000000000, 1.000000000000000000, 1.000000000000000000),
 ( 0.3333333333333334259, 0.3333333333333334259, 0.3333333333333334259, 0.3333333333333333703, 0.3333333333333333148, 0.3333333333333333703, 0.3333333333333334259, 0.3333333333333333703, 0.3333333333333333703, 0.3333333333333334259, 0.3333333333333332593, 0.3333333333333334259, 0.3333333333333333703, 0.3333333333333333703, 0.3333333333333333703, 0.3333333333333333703, 0.3333333333333333703, 0.3333333333333333148, 0.3333333333333334259, 0.3333333333333333148, 0.3333333333333334259, 0.3333333333333333148, 0.3333333333333333703, 0.3333333333333333703, 0.3333333333333333148, 0.3333333333333334814, 0.3333333333333332593, 0.3333333333333334814, 0.3333333333333333148, 0.3333333333333333148, 0.3333333333333334259, 0.3333333333333333703, 0.3333333333333334814, 0.3333333333333332593, 0.3333333333333334259, 0.3333333333333333703, 0.3333333333333333703, 0.3333333333333333148, 0.3333333333333333703, 0.3333333333333333703, 0.3333333333333334814, 0.3333333333333333703, 0.3333333333333334259, 0.3333333333333333703, 0.3333333333333333148, 0.3333333333333333148, 0.3333333333333333703, 0.3333333333333334259, 0.3333333333333333703, 0.3333333333333333703, 0.3333333333333333148, 0.3333333333333333703, 0.3333333333333332593, 0.3333333333333334259, 0.3333333333333333148, 0.3333333333333333703, 0.3333333333333333703, 0.3333333333333333703, 0.3333333333333333703, 0.3333333333333335369, 0.3333333333333332593, 0.3333333333333334259, 0.3333333333333333703, 0.3333333333333334259, 0.3333333333333334259, 0.3333333333333333148, 0.3333333333333334259, 0.3333333333333334259, 0.3333333333333334259, 0.3333333333333334814, 0.3333333333333333703, 0.3333333333333333148, 0.3333333333333333148, 0.3333333333333333703, 0.3333333333333334259, 0.3333333333333333703, 0.3333333333333333703, 0.3333333333333333703, 0.3333333333333333703, 0.3333333333333333148, 0.3333333333333333703, 0.3333333333333332593, 0.3333333333333333703, 0.3333333333333333148, 0.3333333333333333148, 0.3333333333333333703, 0.3333333333333333703, 0.3333333333333333148, 0.3333333333333333703, 0.3333333333333333703, 0.3333333333333333703, 0.3333333333333333703, 0.3333333333333334259, 0.3333333333333332593, 0.3333333333333334259, 0.3333333333333333148, 0.3333333333333333703, 0.3333333333333333148, 0.3333333333333334814, 0.3333333333333332038, 0.3333333333333335369, 0.3333333333333332593, 0.3333333333333333703, 0.3333333333333333703, 0.3333333333333333148, 0.3333333333333333703, 0.3333333333333333148, 0.3333333333333334259, 0.3333333333333334259, 0.3333333333333332593, 0.3333333333333334814, 0.3333333333333333703, 0.3333333333333332593, 0.3333333333333334814, 0.3333333333333334259, 0.3333333333333334259, 0.3333333333333332593, 0.3333333333333333703, 0.3333333333333333703, 0.3333333333333334259, 0.3333333333333333703, 0.3333333333333334259, 0.3333333333333333703, 0.3333333333333333148, 0.3333333333333334814, 0.3333333333333333703, 0.3333333333333334259, 0.3333333333333333703, 0.3333333333333333703, 0.3333333333333333148, 0.3333333333333334259, 0.3333333333333334259, 0.3333333333333333703, 0.3333333333333333148, 0.3333333333333333148, 0.3333333333333334259, 0.3333333333333334814, 0.3333333333333333148, 0.3333333333333334259, 0.3333333333333334814, 0.3333333333333333148, 0.3333333333333334814, 0.3333333333333332038, 0.3333333333333333703, 0.3333333333333333148, 0.3333333333333333703, 0.3333333333333334259, 0.3333333333333332038, 0.3333333333333334259, 0.3333333333333333148, 0.3333333333333332038, 0.3333333333333334259, 0.3333333333333333148, 0.3333333333333334259, 0.3333333333333332593, 0.3333333333333334259, 0.3333333333333333703, 0.3333333333333334259, 0.3333333333333333703, 0.3333333333333334259, 0.3333333333333333703, 0.3333333333333333703, 0.3333333333333334814, 0.3333333333333333703, 0.3333333333333335369, 0.3333333333333332038, 0.3333333333333333703, 0.3333333333333333703, 0.3333333333333333703, 0.3333333333333333148, 0.3333333333333333703, 0.3333333333333333703, 0.3333333333333334259, 0.3333333333333333148, 0.3333333333333334259, 0.3333333333333333148, 0.3333333333333334814, 0.3333333333333332593, 0.3333333333333333703, 0.3333333333333334259, 0.3333333333333333148, 0.3333333333333333703, 0.3333333333333333148, 0.3333333333333334259, 0.3333333333333332593, 0.3333333333333333703, 0.3333333333333334814, 0.3333333333333333703, 0.3333333333333333703, 0.3333333333333333703, 0.3333333333333333703, 0.3333333333333333148, 0.3333333333333333703, 0.3333333333333333703, 0.3333333333333334259, 0.3333333333333333703, 0.3333333333333333703, 0.3333333333333333703, 0.3333333333333333703, 0.3333333333333332038, 0.3333333333333334814, 0.3333333333333333703, 0.3333333333333333703, 0.3333333333333333148, 0.3333333333333333148, 0.3333333333333334259, 0.3333333333333334259, 0.3333333333333332593, 0.3333333333333335369, 0.3333333333333332593, 0.3333333333333334814, 0.3333333333333332593, 0.3333333333333334259, 0.3333333333333332038, 0.3333333333333335369, 0.3333333333333333148, 0.3333333333333333703, 0.3333333333333334259, 0.3333333333333333148, 0.3333333333333333148, 0.3333333333333335369, 0.3333333333333334259, 0.3333333333333333703, 0.3333333333333333148, 0.3333333333333334259, 0.3333333333333333148, 0.3333333333333334259, 0.3333333333333334259, 0.3333333333333333703, 0.3333333333333333703, 0.3333333333333333148, 0.3333333333333333703, 0.3333333333333333703, 0.3333333333333334259, 0.3333333333333333703, 0.3333333333333335369, 0.3333333333333333148, 0.3333333333333333703, 0.3333333333333332593, 0.3333333333333335369, 0.3333333333333333148, 0.3333333333333333148, 0.3333333333333334814, 0.3333333333333332593, 0.3333333333333334814, 0.3333333333333333703, 0.3333333333333334259, 0.3333333333333334814, 0.3333333333333333703, 0.3333333333333333703, 0.3333333333333333148, 0.3333333333333332593, 0.3333333333333334814, 0.3333333333333333148, 0.3333333333333333703, 0.3333333333333333703, 0.3333333333333333703, 0.3333333333333333703, 0.3333333333333334259, 0.3333333333333333703, 0.3333333333333333703, 0.3333333333333333148, 0.3333333333333333703, 0.3333333333333334259, 0.3333333333333332593, 0.3333333333333334814, 0.3333333333333333703, 0.3333333333333333703, 0.3333333333333334259, 0.3333333333333333703, 0.3333333333333334259, 0.3333333333333333703, 0.3333333333333334259, 0.3333333333333332593, 0.3333333333333333703, 0.3333333333333334259, 0.3333333333333333148, 0.3333333333333333148, 0.3333333333333333703, 0.3333333333333334814, 0.3333333333333333148, 0.3333333333333333703, 0.3333333333333334259, 0.3333333333333333703, 0.3333333333333333703, 0.3333333333333333148, 0.3333333333333333703, 0.3333333333333333148, 0.3333333333333335369, 0.3333333333333332593, 0.3333333333333333703, 0.3333333333333333148, 0.3333333333333333703, 0.3333333333333334259, 0.3333333333333334259, 0.3333333333333333703, 0.3333333333333333148, 0.3333333333333334259, 0.3333333333333334259, 0.3333333333333333148, 0.3333333333333334259, 0.3333333333333335369, 0.3333333333333332593, 0.3333333333333333703, 0.3333333333333335369, 0.3333333333333332038, 0.3333333333333334259, 0.3333333333333333148, 0.3333333333333333703, 0.3333333333333333703, 0.3333333333333333703, 0.3333333333333333148, 0.3333333333333333703, 0.3333333333333333703, 0.3333333333333334259, 0.3333333333333334259, 0.3333333333333333148, 0.3333333333333334259, 0.3333333333333333148, 0.3333333333333333703, 0.3333333333333333148, 0.3333333333333334259, 0.3333333333333332038, 0.3333333333333333703, 0.3333333333333334259, 0.3333333333333335369, 0.3333333333333333148, 0.3333333333333333703, 0.3333333333333333703, 0.3333333333333333703, 0.3333333333333333703, 0.3333333333333333703, 0.3333333333333333703, 0.3333333333333334259, 0.3333333333333333703, 0.3333333333333333703, 0.3333333333333333703, 0.3333333333333332038, 0.3333333333333333703, 0.3333333333333335369, 0.3333333333333333148, 0.3333333333333334814, 0.3333333333333333703, 0.3333333333333332593, 0.3333333333333335369, 0.3333333333333333148, 0.3333333333333333703, 0.3333333333333333703, 0.3333333333333333148, 0.3333333333333333703, 0.3333333333333334259, 0.3333333333333334259, 0.3333333333333333703, 0.3333333333333334259, 0.3333333333333333148, 0.3333333333333333703, 0.3333333333333332593, 0.3333333333333333703, 0.3333333333333333703, 0.3333333333333333703, 0.3333333333333333703, 0.3333333333333333703, 0.3333333333333333703, 0.3333333333333333148, 0.3333333333333334259, 0.3333333333333333703, 0.3333333333333334259, 0.3333333333333333148, 0.3333333333333334259, 0.3333333333333333148, 0.3333333333333333703, 0.3333333333333334259, 0.3333333333333333703, 0.3333333333333333148, 0.3333333333333333148, 0.3333333333333334259, 0.3333333333333333703, 0.3333333333333333703, 0.3333333333333334259, 0.3333333333333333703, 0.3333333333333333148, 0.3333333333333334814, 0.3333333333333333703, 0.3333333333333334259, 0.3333333333333333703, 0.3333333333333333703, 0.3333333333333333703),
 ( 0.3333333333333334259, 0.3333333333333334259, 0.3333333333333334259, 0.3333333333333333703, 0.3333333333333333148, 0.3333333333333333703, 0.3333333333333334259, 0.3333333333333333703, 0.3333333333333333703, 0.3333333333333334259, 0.3333333333333332593, 0.3333333333333334259, 0.3333333333333333703, 0.3333333333333333703, 0.3333333333333333703, 0.3333333333333333703, 0.3333333333333333703, 0.3333333333333333148, 0.3333333333333334259, 0.3333333333333333148, 0.3333333333333334259, 0.3333333333333333148, 0.3333333333333333703, 0.3333333333333333703, 0.3333333333333333148, 0.3333333333333334814, 0.3333333333333332593, 0.3333333333333334814, 0.3333333333333333148, 0.3333333333333333148, 0.3333333333333334259, 0.3333333333333333703, 0.3333333333333334814, 0.3333333333333332593, 0.3333333333333334259, 0.3333333333333333703, 0.3333333333333333703, 0.3333333333333333148, 0.3333333333333333703, 0.3333333333333333703, 0.3333333333333334814, 0.3333333333333333703, 0.3333333333333334259, 0.3333333333333333703, 0.3333333333333333148, 0.3333333333333333148, 0.3333333333333333703, 0.3333333333333334259, 0.3333333333333333703, 0.3333333333333333703, 0.3333333333333333148, 0.3333333333333333703, 0.3333333333333332593, 0.3333333333333334259, 0.3333333333333333148, 0.3333333333333333703, 0.3333333333333333703, 0.3333333333333333703, 0.3333333333333333703, 0.3333333333333335369, 0.3333333333333332593, 0.3333333333333334259, 0.3333333333333333703, 0.3333333333333334259, 0.3333333333333334259, 0.3333333333333333148, 0.3333333333333334259, 0.3333333333333334259, 0.3333333333333334259, 0.3333333333333334814, 0.3333333333333333703, 0.3333333333333333148, 0.3333333333333333148, 0.3333333333333333703, 0.3333333333333334259, 0.3333333333333333703, 0.3333333333333333703, 0.3333333333333333703, 0.3333333333333333703, 0.3333333333333333148, 0.3333333333333333703, 0.3333333333333332593, 0.3333333333333333703, 0.3333333333333333148, 0.3333333333333333148, 0.3333333333333333703, 0.3333333333333333703, 0.3333333333333333148, 0.3333333333333333703, 0.3333333333333333703, 0.3333333333333333703, 0.3333333333333333703, 0.3333333333333334259, 0.3333333333333332593, 0.3333333333333334259, 0.3333333333333333148, 0.3333333333333333703, 0.3333333333333333148, 0.3333333333333334814, 0.3333333333333332038, 0.3333333333333335369, 0.3333333333333332593, 0.3333333333333333703, 0.3333333333333333703, 0.3333333333333333148, 0.3333333333333333703, 0.3333333333333333148, 0.3333333333333334259, 0.3333333333333334259, 0.3333333333333332593, 0.3333333333333334814, 0.3333333333333333703, 0.3333333333333332593, 0.3333333333333334814, 0.3333333333333334259, 0.3333333333333334259, 0.3333333333333332593, 0.3333333333333333703, 0.3333333333333333703, 0.3333333333333334259, 0.3333333333333333703, 0.3333333333333334259, 0.3333333333333333703, 0.3333333333333333148, 0.3333333333333334814, 0.3333333333333333703, 0.3333333333333334259, 0.3333333333333333703, 0.3333333333333333703, 0.3333333333333333148, 0.3333333333333334259, 0.3333333333333334259, 0.3333333333333333703, 0.3333333333333333148, 0.3333333333333333148, 0.3333333333333334259, 0.3333333333333334814, 0.3333333333333333148, 0.3333333333333334259, 0.3333333333333334814, 0.3333333333333333148, 0.3333333333333334814, 0.3333333333333332038, 0.3333333333333333703, 0.3333333333333333148, 0.3333333333333333703, 0.3333333333333334259, 0.3333333333333332038, 0.3333333333333334259, 0.3333333333333333148, 0.3333333333333332038, 0.3333333333333334259, 0.3333333333333333148, 0.3333333333333334259, 0.3333333333333332593, 0.3333333333333334259, 0.3333333333333333703, 0.3333333333333334259, 0.3333333333333333703, 0.3333333333333334259, 0.3333333333333333703, 0.3333333333333333703, 0.3333333333333334814, 0.3333333333333333703, 0.3333333333333335369, 0.3333333333333332038, 0.3333333333333333703, 0.3333333333333333703, 0.3333333333333333703, 0.3333333333333333148, 0.3333333333333333703, 0.3333333333333333703, 0.3333333333333334259, 0.3333333333333333148, 0.3333333333333334259, 0.3333333333333333148, 0.3333333333333334814, 0.3333333333333332593, 0.3333333333333333703, 0.3333333333333334259, 0.3333333333333333148, 0.3333333333333333703, 0.3333333333333333148, 0.3333333333333334259, 0.3333333333333332593, 0.3333333333333333703, 0.3333333333333334814, 0.3333333333333333703, 0.3333333333333333703, 0.3333333333333333703, 0.3333333333333333703, 0.3333333333333333148, 0.3333333333333333703, 0.3333333333333333703, 0.3333333333333334259, 0.3333333333333333703, 0.3333333333333333703, 0.3333333333333333703, 0.3333333333333333703, 0.3333333333333332038, 0.3333333333333334814, 0.3333333333333333703, 0.3333333333333333703, 0.3333333333333333148, 0.3333333333333333148, 0.3333333333333334259, 0.3333333333333334259, 0.3333333333333332593, 0.3333333333333335369, 0.3333333333333332593, 0.3333333333333334814, 0.3333333333333332593, 0.3333333333333334259, 0.3333333333333332038, 0.3333333333333335369, 0.3333333333333333148, 0.3333333333333333703, 0.3333333333333334259, 0.3333333333333333148, 0.3333333333333333148, 0.3333333333333335369, 0.3333333333333334259, 0.3333333333333333703, 0.3333333333333333148, 0.3333333333333334259, 0.3333333333333333148, 0.3333333333333334259, 0.3333333333333334259, 0.3333333333333333703, 0.3333333333333333703, 0.3333333333333333148, 0.3333333333333333703, 0.3333333333333333703, 0.3333333333333334259, 0.3333333333333333703, 0.3333333333333335369, 0.3333333333333333148, 0.3333333333333333703, 0.3333333333333332593, 0.3333333333333335369, 0.3333333333333333148, 0.3333333333333333148, 0.3333333333333334814, 0.3333333333333332593, 0.3333333333333334814, 0.3333333333333333703, 0.3333333333333334259, 0.3333333333333334814, 0.3333333333333333703, 0.3333333333333333703, 0.3333333333333333148, 0.3333333333333332593, 0.3333333333333334814, 0.3333333333333333148, 0.3333333333333333703, 0.3333333333333333703, 0.3333333333333333703, 0.3333333333333333703, 0.3333333333333334259, 0.3333333333333333703, 0.3333333333333333703, 0.3333333333333333148, 0.3333333333333333703, 0.3333333333333334259, 0.3333333333333332593, 0.3333333333333334814, 0.3333333333333333703, 0.3333333333333333703, 0.3333333333333334259, 0.3333333333333333703, 0.3333333333333334259, 0.3333333333333333703, 0.3333333333333334259, 0.3333333333333332593, 0.3333333333333333703, 0.3333333333333334259, 0.3333333333333333148, 0.3333333333333333148, 0.3333333333333333703, 0.3333333333333334814, 0.3333333333333333148, 0.3333333333333333703, 0.3333333333333334259, 0.3333333333333333703, 0.3333333333333333703, 0.3333333333333333148, 0.3333333333333333703, 0.3333333333333333148, 0.3333333333333335369, 0.3333333333333332593, 0.3333333333333333703, 0.3333333333333333148, 0.3333333333333333703, 0.3333333333333334259, 0.3333333333333334259, 0.3333333333333333703, 0.3333333333333333148, 0.3333333333333334259, 0.3333333333333334259, 0.3333333333333333148, 0.3333333333333334259, 0.3333333333333335369, 0.3333333333333332593, 0.3333333333333333703, 0.3333333333333335369, 0.3333333333333332038, 0.3333333333333334259, 0.3333333333333333148, 0.3333333333333333703, 0.3333333333333333703, 0.3333333333333333703, 0.3333333333333333148, 0.3333333333333333703, 0.3333333333333333703, 0.3333333333333334259, 0.3333333333333334259, 0.3333333333333333148, 0.3333333333333334259, 0.3333333333333333148, 0.3333333333333333703, 0.3333333333333333148, 0.3333333333333334259, 0.3333333333333332038, 0.3333333333333333703, 0.3333333333333334259, 0.3333333333333335369, 0.3333333333333333148, 0.3333333333333333703, 0.3333333333333333703, 0.3333333333333333703, 0.3333333333333333703, 0.3333333333333333703, 0.3333333333333333703, 0.3333333333333334259, 0.3333333333333333703, 0.3333333333333333703, 0.3333333333333333703, 0.3333333333333332038, 0.3333333333333333703, 0.3333333333333335369, 0.3333333333333333148, 0.3333333333333334814, 0.3333333333333333703, 0.3333333333333332593, 0.3333333333333335369, 0.3333333333333333148, 0.3333333333333333703, 0.3333333333333333703, 0.3333333333333333148, 0.3333333333333333703, 0.3333333333333334259, 0.3333333333333334259, 0.3333333333333333703, 0.3333333333333334259, 0.3333333333333333148, 0.3333333333333333703, 0.3333333333333332593, 0.3333333333333333703, 0.3333333333333333703, 0.3333333333333333703, 0.3333333333333333703, 0.3333333333333333703, 0.3333333333333333703, 0.3333333333333333148, 0.3333333333333334259, 0.3333333333333333703, 0.3333333333333334259, 0.3333333333333333148, 0.3333333333333334259, 0.3333333333333333148, 0.3333333333333333703, 0.3333333333333334259, 0.3333333333333333703, 0.3333333333333333148, 0.3333333333333333148, 0.3333333333333334259, 0.3333333333333333703, 0.3333333333333333703, 0.3333333333333334259, 0.3333333333333333703, 0.3333333333333333148, 0.3333333333333334814, 0.3333333333333333703, 0.3333333333333334259, 0.3333333333333333703, 0.3333333333333333703, 0.3333333333333333703),
 ( 1.000000000000000222, 1.000000000000000222, 1.000000000000000222, 1.000000000000000222, 0.9999999999999996669, 0.9999999999999997780, 1.000000000000000444, 1.000000000000000000, 1.000000000000000000, 1.000000000000000000, 0.9999999999999997780, 1.000000000000000000, 1.000000000000000000, 1.000000000000000000, 1.000000000000000000, 0.9999999999999997780, 1.000000000000000222, 0.9999999999999996669, 1.000000000000000000, 0.9999999999999997780, 1.000000000000000222, 1.000000000000000000, 1.000000000000000222, 0.9999999999999996669, 1.000000000000000000, 1.000000000000000222, 0.9999999999999996669, 1.000000000000000444, 1.000000000000000000, 0.9999999999999997780, 1.000000000000000222, 1.000000000000000222, 1.000000000000000222, 1.000000000000000000, 1.000000000000000000, 0.9999999999999997780, 1.000000000000000000, 1.000000000000000000, 1.000000000000000000, 1.000000000000000000, 1.000000000000000222, 1.000000000000000222, 1.000000000000000000, 1.000000000000000000, 1.000000000000000000, 0.9999999999999996669, 1.000000000000000222, 1.000000000000000000, 1.000000000000000000, 0.9999999999999997780, 0.9999999999999997780, 1.000000000000000000, 0.9999999999999996669, 1.000000000000000222, 0.9999999999999997780, 1.000000000000000222, 0.9999999999999997780, 0.9999999999999997780, 1.000000000000000222, 1.000000000000000222, 0.9999999999999997780, 1.000000000000000222, 1.000000000000000000, 1.000000000000000222, 1.000000000000000000, 0.9999999999999997780, 1.000000000000000000, 1.000000000000000000, 1.000000000000000222, 1.000000000000000222, 1.000000000000000000, 0.9999999999999997780, 1.000000000000000000, 1.000000000000000222, 0.9999999999999997780, 1.000000000000000444, 0.9999999999999996669, 1.000000000000000000, 1.000000000000000222, 0.9999999999999997780, 0.9999999999999997780, 0.9999999999999997780, 1.000000000000000000, 0.9999999999999997780, 1.000000000000000000, 0.9999999999999997780, 1.000000000000000222, 1.000000000000000000, 1.000000000000000222, 1.000000000000000000, 0.9999999999999997780, 1.000000000000000000, 1.000000000000000000, 0.9999999999999997780, 1.000000000000000222, 1.000000000000000000, 1.000000000000000000, 1.000000000000000000, 1.000000000000000222, 0.9999999999999996669, 1.000000000000000222, 1.000000000000000000, 1.000000000000000000, 0.9999999999999997780, 1.000000000000000000, 0.9999999999999997780, 1.000000000000000000, 1.000000000000000222, 1.000000000000000000, 0.9999999999999997780, 1.000000000000000222, 1.000000000000000222, 0.9999999999999996669, 1.000000000000000222, 1.000000000000000000, 1.000000000000000444, 0.9999999999999996669, 1.000000000000000000, 1.000000000000000222, 1.000000000000000222, 1.000000000000000222, 1.000000000000000222, 1.000000000000000000, 0.9999999999999997780, 1.000000000000000222, 1.000000000000000000, 1.000000000000000222, 0.9999999999999996669, 1.000000000000000000, 1.000000000000000000, 1.000000000000000222, 1.000000000000000222, 0.9999999999999997780, 1.000000000000000000, 0.9999999999999997780, 1.000000000000000222, 1.000000000000000000, 1.000000000000000222, 1.000000000000000000, 1.000000000000000444, 0.9999999999999996669, 1.000000000000000444, 0.9999999999999996669, 0.9999999999999997780, 0.9999999999999997780, 1.000000000000000222, 1.000000000000000000, 0.9999999999999997780, 1.000000000000000000, 0.9999999999999997780, 0.9999999999999996669, 1.000000000000000222, 1.000000000000000000, 0.9999999999999997780, 1.000000000000000000, 1.000000000000000000, 1.000000000000000222, 1.000000000000000000, 1.000000000000000000, 1.000000000000000444, 0.9999999999999997780, 1.000000000000000222, 1.000000000000000222, 0.9999999999999997780, 1.000000000000000444, 0.9999999999999996669, 1.000000000000000000, 0.9999999999999997780, 1.000000000000000222, 0.9999999999999997780, 1.000000000000000222, 1.000000000000000000, 1.000000000000000222, 0.9999999999999997780, 0.9999999999999997780, 1.000000000000000000, 1.000000000000000000, 0.9999999999999997780, 1.000000000000000222, 0.9999999999999997780, 1.000000000000000000, 1.000000000000000000, 1.000000000000000222, 1.000000000000000000, 0.9999999999999997780, 1.000000000000000222, 1.000000000000000444, 1.000000000000000000, 1.000000000000000000, 1.000000000000000000, 1.000000000000000000, 0.9999999999999997780, 1.000000000000000000, 1.000000000000000222, 1.000000000000000000, 1.000000000000000222, 0.9999999999999996669, 1.000000000000000000, 1.000000000000000000, 0.9999999999999994449, 1.000000000000000444, 1.000000000000000000, 1.000000000000000222, 0.9999999999999997780, 1.000000000000000000, 1.000000000000000222, 1.000000000000000000, 0.9999999999999996669, 1.000000000000000444, 0.9999999999999997780, 1.000000000000000444, 0.9999999999999996669, 1.000000000000000000, 0.9999999999999996669, 1.000000000000000444, 1.000000000000000000, 0.9999999999999997780, 1.000000000000000222, 1.000000000000000000, 0.9999999999999997780, 1.000000000000000444, 1.000000000000000222, 0.9999999999999997780, 1.000000000000000000, 1.000000000000000222, 0.9999999999999997780, 1.000000000000000222, 1.000000000000000222, 1.000000000000000000, 1.000000000000000000, 0.9999999999999996669, 1.000000000000000222, 0.9999999999999997780, 1.000000000000000000, 0.9999999999999997780, 1.000000000000000444, 1.000000000000000000, 1.000000000000000000, 0.9999999999999997780, 1.000000000000000444, 1.000000000000000000, 0.9999999999999997780, 1.000000000000000444, 0.9999999999999996669, 1.000000000000000444, 1.000000000000000000, 1.000000000000000444, 1.000000000000000222, 1.000000000000000222, 0.9999999999999997780, 1.000000000000000000, 0.9999999999999997780, 1.000000000000000444, 0.9999999999999996669, 1.000000000000000000, 1.000000000000000000, 1.000000000000000222, 1.000000000000000000, 1.000000000000000222, 1.000000000000000000, 1.000000000000000000, 0.9999999999999997780, 1.000000000000000000, 1.000000000000000000, 0.9999999999999997780, 1.000000000000000000, 1.000000000000000000, 0.9999999999999997780, 1.000000000000000000, 1.000000000000000222, 1.000000000000000000, 1.000000000000000000, 1.000000000000000000, 1.000000000000000000, 0.9999999999999996669, 1.000000000000000222, 1.000000000000000000, 0.9999999999999997780, 1.000000000000000000, 1.000000000000000222, 1.000000000000000000, 1.000000000000000222, 1.000000000000000222, 1.000000000000000000, 1.000000000000000222, 1.000000000000000000, 1.000000000000000000, 1.000000000000000000, 1.000000000000000222, 0.9999999999999996669, 1.000000000000000222, 0.9999999999999996669, 1.000000000000000222, 1.000000000000000222, 1.000000000000000222, 1.000000000000000222, 0.9999999999999996669, 1.000000000000000444, 1.000000000000000000, 1.000000000000000000, 1.000000000000000222, 1.000000000000000444, 0.9999999999999996669, 1.000000000000000444, 1.000000000000000222, 0.9999999999999996669, 1.000000000000000222, 0.9999999999999997780, 1.000000000000000000, 1.000000000000000000, 0.9999999999999997780, 1.000000000000000000, 0.9999999999999997780, 1.000000000000000000, 1.000000000000000000, 1.000000000000000444, 0.9999999999999997780, 1.000000000000000222, 0.9999999999999997780, 0.9999999999999997780, 1.000000000000000000, 1.000000000000000000, 0.9999999999999996669, 1.000000000000000000, 1.000000000000000222, 1.000000000000000222, 0.9999999999999997780, 1.000000000000000222, 0.9999999999999997780, 0.9999999999999997780, 1.000000000000000000, 1.000000000000000000, 1.000000000000000000, 1.000000000000000222, 1.000000000000000000, 1.000000000000000222, 1.000000000000000000, 0.9999999999999996669, 0.9999999999999997780, 1.000000000000000444, 0.9999999999999996669, 1.000000000000000444, 0.9999999999999997780, 0.9999999999999997780, 1.000000000000000222, 0.9999999999999997780, 1.000000000000000222, 1.000000000000000000, 1.000000000000000000, 0.9999999999999997780, 1.000000000000000222, 1.000000000000000222, 1.000000000000000000, 1.000000000000000222, 1.000000000000000000, 1.000000000000000000, 0.9999999999999997780, 1.000000000000000000, 1.000000000000000000, 0.9999999999999997780, 1.000000000000000000, 0.9999999999999996669, 1.000000000000000222, 0.9999999999999997780, 1.000000000000000222, 0.9999999999999997780, 1.000000000000000000, 0.9999999999999997780, 1.000000000000000222, 0.9999999999999997780, 1.000000000000000000, 1.000000000000000000, 1.000000000000000000, 1.000000000000000000, 0.9999999999999997780, 1.000000000000000222, 1.000000000000000000, 0.9999999999999997780, 1.000000000000000000, 1.000000000000000000, 1.000000000000000222, 1.000000000000000222, 1.000000000000000000, 1.000000000000000222, 1.000000000000000000, 1.000000000000000000, 1.000000000000000000),
 ( 0.3333333333333334259, 0.3333333333333334259, 0.3333333333333334259, 0.3333333333333333703, 0.3333333333333333148, 0.3333333333333333703, 0.3333333333333334259, 0.3333333333333333703, 0.3333333333333333703, 0.3333333333333334259, 0.3333333333333332593, 0.3333333333333334259, 0.3333333333333333703, 0.3333333333333333703, 0.3333333333333333703, 0.3333333333333333703, 0.3333333333333333703, 0.3333333333333333148, 0.3333333333333334259, 0.3333333333333333148, 0.3333333333333334259, 0.3333333333333333148, 0.3333333333333333703, 0.3333333333333333703, 0.3333333333333333148, 0.3333333333333334814, 0.3333333333333332593, 0.3333333333333334814, 0.3333333333333333148, 0.3333333333333333148, 0.3333333333333334259, 0.3333333333333333703, 0.3333333333333334814, 0.3333333333333332593, 0.3333333333333334259, 0.3333333333333333703, 0.3333333333333333703, 0.3333333333333333148, 0.3333333333333333703, 0.3333333333333333703, 0.3333333333333334814, 0.3333333333333333703, 0.3333333333333334259, 0.3333333333333333703, 0.3333333333333333148, 0.3333333333333333148, 0.3333333333333333703, 0.3333333333333334259, 0.3333333333333333703, 0.3333333333333333703, 0.3333333333333333148, 0.3333333333333333703, 0.3333333333333332593, 0.3333333333333334259, 0.3333333333333333148, 0.3333333333333333703, 0.3333333333333333703, 0.3333333333333333703, 0.3333333333333333703, 0.3333333333333335369, 0.3333333333333332593, 0.3333333333333334259, 0.3333333333333333703, 0.3333333333333334259, 0.3333333333333334259, 0.3333333333333333148, 0.3333333333333334259, 0.3333333333333334259, 0.3333333333333334259, 0.3333333333333334814, 0.3333333333333333703, 0.3333333333333333148, 0.3333333333333333148, 0.3333333333333333703, 0.3333333333333334259, 0.3333333333333333703, 0.3333333333333333703, 0.3333333333333333703, 0.3333333333333333703, 0.3333333333333333148, 0.3333333333333333703, 0.3333333333333332593, 0.3333333333333333703, 0.3333333333333333148, 0.3333333333333333148, 0.3333333333333333703, 0.3333333333333333703, 0.3333333333333333148, 0.3333333333333333703, 0.3333333333333333703, 0.3333333333333333703, 0.3333333333333333703, 0.3333333333333334259, 0.3333333333333332593, 0.3333333333333334259, 0.3333333333333333148, 0.3333333333333333703, 0.3333333333333333148, 0.3333333333333334814, 0.3333333333333332038, 0.3333333333333335369, 0.3333333333333332593, 0.3333333333333333703, 0.3333333333333333703, 0.3333333333333333148, 0.3333333333333333703, 0.3333333333333333148, 0.3333333333333334259, 0.3333333333333334259, 0.3333333333333332593, 0.3333333333333334814, 0.3333333333333333703, 0.3333333333333332593, 0.3333333333333334814, 0.3333333333333334259, 0.3333333333333334259, 0.3333333333333332593, 0.3333333333333333703, 0.3333333333333333703, 0.3333333333333334259, 0.3333333333333333703, 0.3333333333333334259, 0.3333333333333333703, 0.3333333333333333148, 0.3333333333333334814, 0.3333333333333333703, 0.3333333333333334259, 0.3333333333333333703, 0.3333333333333333703, 0.3333333333333333148, 0.3333333333333334259, 0.3333333333333334259, 0.3333333333333333703, 0.3333333333333333148, 0.3333333333333333148, 0.3333333333333334259, 0.3333333333333334814, 0.3333333333333333148, 0.3333333333333334259, 0.3333333333333334814, 0.3333333333333333148, 0.3333333333333334814, 0.3333333333333332038, 0.3333333333333333703, 0.3333333333333333148, 0.3333333333333333703, 0.3333333333333334259, 0.3333333333333332038, 0.3333333333333334259, 0.3333333333333333148, 0.3333333333333332038, 0.3333333333333334259, 0.3333333333333333148, 0.3333333333333334259, 0.3333333333333332593, 0.3333333333333334259, 0.3333333333333333703, 0.3333333333333334259, 0.3333333333333333703, 0.3333333333333334259, 0.3333333333333333703, 0.3333333333333333703, 0.3333333333333334814, 0.3333333333333333703, 0.3333333333333335369, 0.3333333333333332038, 0.3333333333333333703, 0.3333333333333333703, 0.3333333333333333703, 0.3333333333333333148, 0.3333333333333333703, 0.3333333333333333703, 0.3333333333333334259, 0.3333333333333333148, 0.3333333333333334259, 0.3333333333333333148, 0.3333333333333334814, 0.3333333333333332593, 0.3333333333333333703, 0.3333333333333334259, 0.3333333333333333148, 0.3333333333333333703, 0.3333333333333333148, 0.3333333333333334259, 0.3333333333333332593, 0.3333333333333333703, 0.3333333333333334814, 0.3333333333333333703, 0.3333333333333333703, 0.3333333333333333703, 0.3333333333333333703, 0.3333333333333333148, 0.3333333333333333703, 0.3333333333333333703, 0.3333333333333334259, 0.3333333333333333703, 0.3333333333333333703, 0.3333333333333333703, 0.3333333333333333703, 0.3333333333333332038, 0.3333333333333334814, 0.3333333333333333703, 0.3333333333333333703, 0.3333333333333333148, 0.3333333333333333148, 0.3333333333333334259, 0.3333333333333334259, 0.3333333333333332593, 0.3333333333333335369, 0.3333333333333332593, 0.3333333333333334814, 0.3333333333333332593, 0.3333333333333334259, 0.3333333333333332038, 0.3333333333333335369, 0.3333333333333333148, 0.3333333333333333703, 0.3333333333333334259, 0.3333333333333333148, 0.3333333333333333148, 0.3333333333333335369, 0.3333333333333334259, 0.3333333333333333703, 0.3333333333333333148, 0.3333333333333334259, 0.3333333333333333148, 0.3333333333333334259, 0.3333333333333334259, 0.3333333333333333703, 0.3333333333333333703, 0.3333333333333333148, 0.3333333333333333703, 0.3333333333333333703, 0.3333333333333334259, 0.3333333333333333703, 0.3333333333333335369, 0.3333333333333333148, 0.3333333333333333703, 0.3333333333333332593, 0.3333333333333335369, 0.3333333333333333148, 0.3333333333333333148, 0.3333333333333334814, 0.3333333333333332593, 0.3333333333333334814, 0.3333333333333333703, 0.3333333333333334259, 0.3333333333333334814, 0.3333333333333333703, 0.3333333333333333703, 0.3333333333333333148, 0.3333333333333332593, 0.3333333333333334814, 0.3333333333333333148, 0.3333333333333333703, 0.3333333333333333703, 0.3333333333333333703, 0.3333333333333333703, 0.3333333333333334259, 0.3333333333333333703, 0.3333333333333333703, 0.3333333333333333148, 0.3333333333333333703, 0.3333333333333334259, 0.3333333333333332593, 0.3333333333333334814, 0.3333333333333333703, 0.3333333333333333703, 0.3333333333333334259, 0.3333333333333333703, 0.3333333333333334259, 0.3333333333333333703, 0.3333333333333334259, 0.3333333333333332593, 0.3333333333333333703, 0.3333333333333334259, 0.3333333333333333148, 0.3333333333333333148, 0.3333333333333333703, 0.3333333333333334814, 0.3333333333333333148, 0.3333333333333333703, 0.3333333333333334259, 0.3333333333333333703, 0.3333333333333333703, 0.3333333333333333148, 0.3333333333333333703, 0.3333333333333333148, 0.3333333333333335369, 0.3333333333333332593, 0.3333333333333333703, 0.3333333333333333148, 0.3333333333333333703, 0.3333333333333334259, 0.3333333333333334259, 0.3333333333333333703, 0.3333333333333333148, 0.3333333333333334259, 0.3333333333333334259, 0.3333333333333333148, 0.3333333333333334259, 0.3333333333333335369, 0.3333333333333332593, 0.3333333333333333703, 0.3333333333333335369, 0.3333333333333332038, 0.3333333333333334259, 0.3333333333333333148, 0.3333333333333333703, 0.3333333333333333703, 0.3333333333333333703, 0.3333333333333333148, 0.3333333333333333703, 0.3333333333333333703, 0.3333333333333334259, 0.3333333333333334259, 0.3333333333333333148, 0.3333333333333334259, 0.3333333333333333148, 0.3333333333333333703, 0.3333333333333333148, 0.3333333333333334259, 0.3333333333333332038, 0.3333333333333333703, 0.3333333333333334259, 0.3333333333333335369, 0.3333333333333333148, 0.3333333333333333703, 0.3333333333333333703, 0.3333333333333333703, 0.3333333333333333703, 0.3333333333333333703, 0.3333333333333333703, 0.3333333333333334259, 0.3333333333333333703, 0.3333333333333333703, 0.3333333333333333703, 0.3333333333333332038, 0.3333333333333333703, 0.3333333333333335369, 0.3333333333333333148, 0.3333333333333334814, 0.3333333333333333703, 0.3333333333333332593, 0.3333333333333335369, 0.3333333333333333148, 0.3333333333333333703, 0.3333333333333333703, 0.3333333333333333148, 0.3333333333333333703, 0.3333333333333334259, 0.3333333333333334259, 0.3333333333333333703, 0.3333333333333334259, 0.3333333333333333148, 0.3333333333333333703, 0.3333333333333332593, 0.3333333333333333703, 0.3333333333333333703, 0.3333333333333333703, 0.3333333333333333703, 0.3333333333333333703, 0.3333333333333333703, 0.3333333333333333148, 0.3333333333333334259, 0.3333333333333333703, 0.3333333333333334259, 0.3333333333333333148, 0.3333333333333334259, 0.3333333333333333148, 0.3333333333333333703, 0.3333333333333334259, 0.3333333333333333703, 0.3333333333333333148, 0.3333333333333333148, 0.3333333333333334259, 0.3333333333333333703, 0.3333333333333333703, 0.3333333333333334259, 0.3333333333333333703, 0.3333333333333333148, 0.3333333333333334814, 0.3333333333333333703, 0.3333333333333334259, 0.3333333333333333703, 0.3333333333333333703, 0.3333333333333333703),
 ( 0.3333333333333334259, 0.3333333333333334259, 0.3333333333333334259, 0.3333333333333333703, 0.3333333333333333148, 0.3333333333333333703, 0.3333333333333334259, 0.3333333333333333703, 0.3333333333333333703, 0.3333333333333334259, 0.3333333333333332593, 0.3333333333333334259, 0.3333333333333333703, 0.3333333333333333703, 0.3333333333333333703, 0.3333333333333333703, 0.3333333333333333703, 0.3333333333333333148, 0.3333333333333334259, 0.3333333333333333148, 0.3333333333333334259, 0.3333333333333333148, 0.3333333333333333703, 0.3333333333333333703, 0.3333333333333333148, 0.3333333333333334814, 0.3333333333333332593, 0.3333333333333334814, 0.3333333333333333148, 0.3333333333333333148, 0.3333333333333334259, 0.3333333333333333703, 0.3333333333333334814, 0.3333333333333332593, 0.3333333333333334259, 0.3333333333333333703, 0.3333333333333333703, 0.3333333333333333148, 0.3333333333333333703, 0.3333333333333333703, 0.3333333333333334814, 0.3333333333333333703, 0.3333333333333334259, 0.3333333333333333703, 0.3333333333333333148, 0.3333333333333333148, 0.3333333333333333703, 0.3333333333333334259, 0.3333333333333333703, 0.3333333333333333703, 0.3333333333333333148, 0.3333333333333333703, 0.3333333333333332593, 0.3333333333333334259, 0.3333333333333333148, 0.3333333333333333703, 0.3333333333333333703, 0.3333333333333333703, 0.3333333333333333703, 0.3333333333333335369, 0.3333333333333332593, 0.3333333333333334259, 0.3333333333333333703, 0.3333333333333334259, 0.3333333333333334259, 0.3333333333333333148, 0.3333333333333334259, 0.3333333333333334259, 0.3333333333333334259, 0.3333333333333334814, 0.3333333333333333703, 0.3333333333333333148, 0.3333333333333333148, 0.3333333333333333703, 0.3333333333333334259, 0.3333333333333333703, 0.3333333333333333703, 0.3333333333333333703, 0.3333333333333333703, 0.3333333333333333148, 0.3333333333333333703, 0.3333333333333332593, 0.3333333333333333703, 0.3333333333333333148, 0.3333333333333333148, 0.3333333333333333703, 0.3333333333333333703, 0.3333333333333333148, 0.3333333333333333703, 0.3333333333333333703, 0.3333333333333333703, 0.3333333333333333703, 0.3333333333333334259, 0.3333333333333332593, 0.3333333333333334259, 0.3333333333333333148, 0.3333333333333333703, 0.3333333333333333148, 0.3333333333333334814, 0.3333333333333332038, 0.3333333333333335369, 0.3333333333333332593, 0.3333333333333333703, 0.3333333333333333703, 0.3333333333333333148, 0.3333333333333333703, 0.3333333333333333148, 0.3333333333333334259, 0.3333333333333334259, 0.3333333333333332593, 0.3333333333333334814, 0.3333333333333333703, 0.3333333333333332593, 0.3333333333333334814, 0.3333333333333334259, 0.3333333333333334259, 0.3333333333333332593, 0.3333333333333333703, 0.3333333333333333703, 0.3333333333333334259, 0.3333333333333333703, 0.3333333333333334259, 0.3333333333333333703, 0.3333333333333333148, 0.3333333333333334814, 0.3333333333333333703, 0.3333333333333334259, 0.3333333333333333703, 0.3333333333333333703, 0.3333333333333333148, 0.3333333333333334259, 0.3333333333333334259, 0.3333333333333333703, 0.3333333333333333148, 0.3333333333333333148, 0.3333333333333334259, 0.3333333333333334814, 0.3333333333333333148, 0.3333333333333334259, 0.3333333333333334814, 0.3333333333333333148, 0.3333333333333334814, 0.3333333333333332038, 0.3333333333333333703, 0.3333333333333333148, 0.3333333333333333703, 0.3333333333333334259, 0.3333333333333332038, 0.3333333333333334259, 0.3333333333333333148, 0.3333333333333332038, 0.3333333333333334259, 0.3333333333333333148, 0.3333333333333334259, 0.3333333333333332593, 0.3333333333333334259, 0.3333333333333333703, 0.3333333333333334259, 0.3333333333333333703, 0.3333333333333334259, 0.3333333333333333703, 0.3333333333333333703, 0.3333333333333334814, 0.3333333333333333703, 0.3333333333333335369, 0.3333333333333332038, 0.3333333333333333703, 0.3333333333333333703, 0.3333333333333333703, 0.3333333333333333148, 0.3333333333333333703, 0.3333333333333333703, 0.3333333333333334259, 0.3333333333333333148, 0.3333333333333334259, 0.3333333333333333148, 0.3333333333333334814, 0.3333333333333332593, 0.3333333333333333703, 0.3333333333333334259, 0.3333333333333333148, 0.3333333333333333703, 0.3333333333333333148, 0.3333333333333334259, 0.3333333333333332593, 0.3333333333333333703, 0.3333333333333334814, 0.3333333333333333703, 0.3333333333333333703, 0.3333333333333333703, 0.3333333333333333703, 0.3333333333333333148, 0.3333333333333333703, 0.3333333333333333703, 0.3333333333333334259, 0.3333333333333333703, 0.3333333333333333703, 0.3333333333333333703, 0.3333333333333333703, 0.3333333333333332038, 0.3333333333333334814, 0.3333333333333333703, 0.3333333333333333703, 0.3333333333333333148, 0.3333333333333333148, 0.3333333333333334259, 0.3333333333333334259, 0.3333333333333332593, 0.3333333333333335369, 0.3333333333333332593, 0.3333333333333334814, 0.3333333333333332593, 0.3333333333333334259, 0.3333333333333332038, 0.3333333333333335369, 0.3333333333333333148, 0.3333333333333333703, 0.3333333333333334259, 0.3333333333333333148, 0.3333333333333333148, 0.3333333333333335369, 0.3333333333333334259, 0.3333333333333333703, 0.3333333333333333148, 0.3333333333333334259, 0.3333333333333333148, 0.3333333333333334259, 0.3333333333333334259, 0.3333333333333333703, 0.3333333333333333703, 0.3333333333333333148, 0.3333333333333333703, 0.3333333333333333703, 0.3333333333333334259, 0.3333333333333333703, 0.3333333333333335369, 0.3333333333333333148, 0.3333333333333333703, 0.3333333333333332593, 0.3333333333333335369, 0.3333333333333333148, 0.3333333333333333148, 0.3333333333333334814, 0.3333333333333332593, 0.3333333333333334814, 0.3333333333333333703, 0.3333333333333334259, 0.3333333333333334814, 0.3333333333333333703, 0.3333333333333333703, 0.3333333333333333148, 0.3333333333333332593, 0.3333333333333334814, 0.3333333333333333148, 0.3333333333333333703, 0.3333333333333333703, 0.3333333333333333703, 0.3333333333333333703, 0.3333333333333334259, 0.3333333333333333703, 0.3333333333333333703, 0.3333333333333333148, 0.3333333333333333703, 0.3333333333333334259, 0.3333333333333332593, 0.3333333333333334814, 0.3333333333333333703, 0.3333333333333333703, 0.3333333333333334259, 0.3333333333333333703, 0.3333333333333334259, 0.3333333333333333703, 0.3333333333333334259, 0.3333333333333332593, 0.3333333333333333703, 0.3333333333333334259, 0.3333333333333333148, 0.3333333333333333148, 0.3333333333333333703, 0.3333333333333334814, 0.3333333333333333148, 0.3333333333333333703, 0.3333333333333334259, 0.3333333333333333703, 0.3333333333333333703, 0.3333333333333333148, 0.3333333333333333703, 0.3333333333333333148, 0.3333333333333335369, 0.3333333333333332593, 0.3333333333333333703, 0.3333333333333333148, 0.3333333333333333703, 0.3333333333333334259, 0.3333333333333334259, 0.3333333333333333703, 0.3333333333333333148, 0.3333333333333334259, 0.3333333333333334259, 0.3333333333333333148, 0.3333333333333334259, 0.3333333333333335369, 0.3333333333333332593, 0.3333333333333333703, 0.3333333333333335369, 0.3333333333333332038, 0.3333333333333334259, 0.3333333333333333148, 0.3333333333333333703, 0.3333333333333333703, 0.3333333333333333703, 0.3333333333333333148, 0.3333333333333333703, 0.3333333333333333703, 0.3333333333333334259, 0.3333333333333334259, 0.3333333333333333148, 0.3333333333333334259, 0.3333333333333333148, 0.3333333333333333703, 0.3333333333333333148, 0.3333333333333334259, 0.3333333333333332038, 0.3333333333333333703, 0.3333333333333334259, 0.3333333333333335369, 0.3333333333333333148, 0.3333333333333333703, 0.3333333333333333703, 0.3333333333333333703, 0.3333333333333333703, 0.3333333333333333703, 0.3333333333333333703, 0.3333333333333334259, 0.3333333333333333703, 0.3333333333333333703, 0.3333333333333333703, 0.3333333333333332038, 0.3333333333333333703, 0.3333333333333335369, 0.3333333333333333148, 0.3333333333333334814, 0.3333333333333333703, 0.3333333333333332593, 0.3333333333333335369, 0.3333333333333333148, 0.3333333333333333703, 0.3333333333333333703, 0.3333333333333333148, 0.3333333333333333703, 0.3333333333333334259, 0.3333333333333334259, 0.3333333333333333703, 0.3333333333333334259, 0.3333333333333333148, 0.3333333333333333703, 0.3333333333333332593, 0.3333333333333333703, 0.3333333333333333703, 0.3333333333333333703, 0.3333333333333333703, 0.3333333333333333703, 0.3333333333333333703, 0.3333333333333333148, 0.3333333333333334259, 0.3333333333333333703, 0.3333333333333334259, 0.3333333333333333148, 0.3333333333333334259, 0.3333333333333333148, 0.3333333333333333703, 0.3333333333333334259, 0.3333333333333333703, 0.3333333333333333148, 0.3333333333333333148, 0.3333333333333334259, 0.3333333333333333703, 0.3333333333333333703, 0.3333333333333334259, 0.3333333333333333703, 0.3333333333333333148, 0.3333333333333334814, 0.3333333333333333703, 0.3333333333333334259, 0.3333333333333333703, 0.3333333333333333703, 0.3333333333333333703),
 ( 1.000000000000000222, 1.000000000000000222, 1.000000000000000222, 1.000000000000000222, 0.9999999999999996669, 0.9999999999999997780, 1.000000000000000444, 1.000000000000000000, 1.000000000000000000, 1.000000000000000000, 0.9999999999999997780, 1.000000000000000000, 1.000000000000000000, 1.000000000000000000, 1.000000000000000000, 0.9999999999999997780, 1.000000000000000222, 0.9999999999999996669, 1.000000000000000000, 0.9999999999999997780, 1.000000000000000222, 1.000000000000000000, 1.000000000000000222, 0.9999999999999996669, 1.000000000000000000, 1.000000000000000222, 0.9999999999999996669, 1.000000000000000444, 1.000000000000000000, 0.9999999999999997780, 1.000000000000000222, 1.000000000000000222, 1.000000000000000222, 1.000000000000000000, 1.000000000000000000, 0.9999999999999997780, 1.000000000000000000, 1.000000000000000000, 1.000000000000000000, 1.000000000000000000, 1.000000000000000222, 1.000000000000000222, 1.000000000000000000, 1.000000000000000000, 1.000000000000000000, 0.9999999999999996669, 1.000000000000000222, 1.000000000000000000, 1.000000000000000000, 0.9999999999999997780, 0.9999999999999997780, 1.000000000000000000, 0.9999999999999996669, 1.000000000000000222, 0.9999999999999997780, 1.000000000000000222, 0.9999999999999997780, 0.9999999999999997780, 1.000000000000000222, 1.000000000000000222, 0.9999999999999997780, 1.000000000000000222, 1.000000000000000000, 1.000000000000000222, 1.000000000000000000, 0.9999999999999997780, 1.000000000000000000, 1.000000000000000000, 1.000000000000000222, 1.000000000000000222, 1.000000000000000000, 0.9999999999999997780, 1.000000000000000000, 1.000000000000000222, 0.9999999999999997780, 1.000000000000000444, 0.9999999999999996669, 1.000000000000000000, 1.000000000000000222, 0.9999999999999997780, 0.9999999999999997780, 0.9999999999999997780, 1.000000000000000000, 0.9999999999999997780, 1.000000000000000000, 0.9999999999999997780, 1.000000000000000222, 1.000000000000000000, 1.000000000000000222, 1.000000000000000000, 0.9999999999999997780, 1.000000000000000000, 1.000000000000000000, 0.9999999999999997780, 1.000000000000000222, 1.000000000000000000, 1.000000000000000000, 1.000000000000000000, 1.000000000000000222, 0.9999999999999996669, 1.000000000000000222, 1.000000000000000000, 1.000000000000000000, 0.9999999999999997780, 1.000000000000000000, 0.9999999999999997780, 1.000000000000000000, 1.000000000000000222, 1.000000000000000000, 0.9999999999999997780, 1.000000000000000222, 1.000000000000000222, 0.9999999999999996669, 1.000000000000000222, 1.000000000000000000, 1.000000000000000444, 0.9999999999999996669, 1.000000000000000000, 1.000000000000000222, 1.000000000000000222, 1.000000000000000222, 1.000000000000000222, 1.000000000000000000, 0.9999999999999997780, 1.000000000000000222, 1.000000000000000000, 1.000000000000000222, 0.9999999999999996669, 1.000000000000000000, 1.000000000000000000, 1.000000000000000222, 1.000000000000000222, 0.9999999999999997780, 1.000000000000000000, 0.9999999999999997780, 1.000000000000000222, 1.000000000000000000, 1.000000000000000222, 1.000000000000000000, 1.000000000000000444, 0.9999999999999996669, 1.000000000000000444, 0.9999999999999996669, 0.9999999999999997780, 0.9999999999999997780, 1.000000000000000222, 1.000000000000000000, 0.9999999999999997780, 1.000000000000000000, 0.9999999999999997780, 0.9999999999999996669, 1.000000000000000222, 1.000000000000000000, 0.9999999999999997780, 1.000000000000000000, 1.000000000000000000, 1.000000000000000222, 1.000000000000000000, 1.000000000000000000, 1.000000000000000444, 0.9999999999999997780, 1.000000000000000222, 1.000000000000000222, 0.9999999999999997780, 1.000000000000000444, 0.9999999999999996669, 1.000000000000000000, 0.9999999999999997780, 1.000000000000000222, 0.9999999999999997780, 1.000000000000000222, 1.000000000000000000, 1.000000000000000222, 0.9999999999999997780, 0.9999999999999997780, 1.000000000000000000, 1.000000000000000000, 0.9999999999999997780, 1.000000000000000222, 0.9999999999999997780, 1.000000000000000000, 1.000000000000000000, 1.000000000000000222, 1.000000000000000000, 0.9999999999999997780, 1.000000000000000222, 1.000000000000000444, 1.000000000000000000, 1.000000000000000000, 1.000000000000000000, 1.000000000000000000, 0.9999999999999997780, 1.000000000000000000, 1.000000000000000222, 1.000000000000000000, 1.000000000000000222, 0.9999999999999996669, 1.000000000000000000, 1.000000000000000000, 0.9999999999999994449, 1.000000000000000444, 1.000000000000000000, 1.000000000000000222, 0.9999999999999997780, 1.000000000000000000, 1.000000000000000222, 1.000000000000000000, 0.9999999999999996669, 1.000000000000000444, 0.9999999999999997780, 1.000000000000000444, 0.9999999999999996669, 1.000000000000000000, 0.9999999999999996669, 1.000000000000000444, 1.000000000000000000, 0.9999999999999997780, 1.000000000000000222, 1.000000000000000000, 0.9999999999999997780, 1.000000000000000444, 1.000000000000000222, 0.9999999999999997780, 1.000000000000000000, 1.000000000000000222, 0.9999999999999997780, 1.000000000000000222, 1.000000000000000222, 1.000000000000000000, 1.000000000000000000, 0.9999999999999996669, 1.000000000000000222, 0.9999999999999997780, 1.000000000000000000, 0.9999999999999997780, 1.000000000000000444, 1.000000000000000000, 1.000000000000000000, 0.9999999999999997780, 1.000000000000000444, 1.000000000000000000, 0.9999999999999997780, 1.000000000000000444, 0.9999999999999996669, 1.000000000000000444, 1.000000000000000000, 1.000000000000000444, 1.000000000000000222, 1.000000000000000222, 0.9999999999999997780, 1.000000000000000000, 0.9999999999999997780, 1.000000000000000444, 0.9999999999999996669, 1.000000000000000000, 1.000000000000000000, 1.000000000000000222, 1.000000000000000000, 1.000000000000000222, 1.000000000000000000, 1.000000000000000000, 0.9999999999999997780, 1.000000000000000000, 1.000000000000000000, 0.9999999999999997780, 1.000000000000000000, 1.000000000000000000, 0.9999999999999997780, 1.000000000000000000, 1.000000000000000222, 1.000000000000000000, 1.000000000000000000, 1.000000000000000000, 1.000000000000000000, 0.9999999999999996669, 1.000000000000000222, 1.000000000000000000, 0.9999999999999997780, 1.000000000000000000, 1.000000000000000222, 1.000000000000000000, 1.000000000000000222, 1.000000000000000222, 1.000000000000000000, 1.000000000000000222, 1.000000000000000000, 1.000000000000000000, 1.000000000000000000, 1.000000000000000222, 0.9999999999999996669, 1.000000000000000222, 0.9999999999999996669, 1.000000000000000222, 1.000000000000000222, 1.000000000000000222, 1.000000000000000222, 0.9999999999999996669, 1.000000000000000444, 1.000000000000000000, 1.000000000000000000, 1.000000000000000222, 1.000000000000000444, 0.9999999999999996669, 1.000000000000000444, 1.000000000000000222, 0.9999999999999996669, 1.000000000000000222, 0.9999999999999997780, 1.000000000000000000, 1.000000000000000000, 0.9999999999999997780, 1.000000000000000000, 0.9999999999999997780, 1.000000000000000000, 1.000000000000000000, 1.000000000000000444, 0.9999999999999997780, 1.000000000000000222, 0.9999999999999997780, 0.9999999999999997780, 1.000000000000000000, 1.000000000000000000, 0.9999999999999996669, 1.000000000000000000, 1.000000000000000222, 1.000000000000000222, 0.9999999999999997780, 1.000000000000000222, 0.9999999999999997780, 0.9999999999999997780, 1.000000000000000000, 1.000000000000000000, 1.000000000000000000, 1.000000000000000222, 1.000000000000000000, 1.000000000000000222, 1.000000000000000000, 0.9999999999999996669, 0.9999999999999997780, 1.000000000000000444, 0.9999999999999996669, 1.000000000000000444, 0.9999999999999997780, 0.9999999999999997780, 1.000000000000000222, 0.9999999999999997780, 1.000000000000000222, 1.000000000000000000, 1.000000000000000000, 0.9999999999999997780, 1.000000000000000222, 1.000000000000000222, 1.000000000000000000, 1.000000000000000222, 1.000000000000000000, 1.000000000000000000, 0.9999999999999997780, 1.000000000000000000, 1.000000000000000000, 0.9999999999999997780, 1.000000000000000000, 0.9999999999999996669, 1.000000000000000222, 0.9999999999999997780, 1.000000000000000222, 0.9999999999999997780, 1.000000000000000000, 0.9999999999999997780, 1.000000000000000222, 0.9999999999999997780, 1.000000000000000000, 1.000000000000000000, 1.000000000000000000, 1.000000000000000000, 0.9999999999999997780, 1.000000000000000222, 1.000000000000000000, 0.9999999999999997780, 1.000000000000000000, 1.000000000000000000, 1.000000000000000222, 1.000000000000000222, 1.000000000000000000, 1.000000000000000222, 1.000000000000000000, 1.000000000000000000, 1.000000000000000000) ) ) 
 REPRESENTATION_ITEM ( '' )  SURFACE ( )  );
#32160=CARTESIAN_POINT ( 'NONE',  ( 2.930518499080053907, 1.225513248159842083, -1.835134156090315605 ) ) ;
#32161=CARTESIAN_POINT ( 'NONE',  ( 4.745575995134789338, -1.744828745684245508, -1.440138369970354493 ) ) ;
#32163=CARTESIAN_POINT ( 'NONE',  ( 5.027533431531807651, -0.2580777524966316738, 1.792966082415799800 ) ) ;
#32164=CARTESIAN_POINT ( 'NONE',  ( 5.436718845459293625, -1.505851745483515858, 1.184076087961029700 ) ) ;
#32166=CARTESIAN_POINT ( 'NONE',  ( 6.455916552660014851, 1.865467424361374249, -0.1398750677365916961 ) ) ;
#32167=CARTESIAN_POINT ( 'NONE',  ( 5.459367789976862895, 1.521435002614815790, 1.071484558867175529 ) ) ;
#32169=CARTESIAN_POINT ( 'NONE',  ( 6.649276393164253562, -1.424495517243940856, -1.050074490644896441 ) ) ;
#32170=CARTESIAN_POINT ( 'NONE',  ( 1.042204282965590201, 0.8216761606248854655, 1.841732292558920570 ) ) ;
#32172=CARTESIAN_POINT ( 'NONE',  ( 3.387430394310109616, 1.903944824823229798, -0.9005924351132842398 ) ) ;
#32177=CARTESIAN_POINT ( 'NONE',  ( 2.232681213900446160, 1.316219961256912763, -1.532148775131780383 ) ) ;
#32180=CARTESIAN_POINT ( 'NONE',  ( 2.847126979364768218, -1.798887516807456954, 1.198237791991546564 ) ) ;
#32181=CARTESIAN_POINT ( 'NONE',  ( 6.889999999999973035, 7.629137130509070275, 2.319999999999996287 ) ) ;
#32189=CARTESIAN_POINT ( 'NONE',  ( 1.101424459656743071, -0.5276332240332289869, 2.126988402630063835 ) ) ;
#32191=CARTESIAN_POINT ( 'NONE',  ( 2.430887666589570451, 2.194555640652501527, 0.5498776597147712053 ) ) ;
#32198=CARTESIAN_POINT ( 'NONE',  ( 3.040057762974816224, 1.755912757559551007, 0.2203070401886226548 ) ) ;
#32199=CARTESIAN_POINT ( 'NONE',  ( 6.229534195615700654, -2.079954537573494466, 0.7377168454194837910 ) ) ;
#32202=ORIENTED_EDGE ( 'NONE', *, *, #87069, .T. ) ;
#32204=CARTESIAN_POINT ( 'NONE',  ( 5.624625116526842383, 0.3961212581503182339, 1.976953148079656719 ) ) ;
#32205=CARTESIAN_POINT ( 'NONE',  ( 4.851724922005476337, -1.286371495869711667, -1.275854292049487304 ) ) ;
#32208=CARTESIAN_POINT ( 'NONE',  ( 2.078771448894382701, -0.08914341469279042640, -1.868647664167771394 ) ) ;
#32209=CARTESIAN_POINT ( 'NONE',  ( 3.362232293424003426, -2.068089847843882279, 0.09686330349460009481 ) ) ;
#32211=CARTESIAN_POINT ( 'NONE',  ( 1.564566645345835116, 0.6029492335615972420, 1.814891859350221459 ) ) ;
#32217=CARTESIAN_POINT ( 'NONE',  ( 1.072351618572921605, 0.7776387867773438822, 1.747342548420704578 ) ) ;
#32219=CARTESIAN_POINT ( 'NONE',  ( 2.682025323810240280, -1.127217178123595565, -1.605522638798158264 ) ) ;
#32220=CARTESIAN_POINT ( 'NONE',  ( 0.3509351863830567075, -0.9528684895154272416, 1.776737725368633614 ) ) ;
#32224=CARTESIAN_POINT ( 'NONE',  ( 0.2275331484566482099, -1.145445245298154946, -1.479381579510357980 ) ) ;
#32226=CARTESIAN_POINT ( 'NONE',  ( 2.426041559740747200, -1.990683941386611311, 0.2996653706425453367 ) ) ;
#32228=CARTESIAN_POINT ( 'NONE',  ( 1.757563674541680721, 2.025006261547353414, -0.6180173261674735130 ) ) ;
#32230=CARTESIAN_POINT ( 'NONE',  ( 3.490741092712910998, 2.019281663078629219, 0.4563312328872348722 ) ) ;
#32232=CARTESIAN_POINT ( 'NONE',  ( 5.718719656712253574, -0.05221879637645754357, 2.090152071033167136 ) ) ;
#32234=CARTESIAN_POINT ( 'NONE',  ( 3.680510133705969800, -1.759192178946006990, -0.4875382671739314500 ) ) ;
#32239=CARTESIAN_POINT ( 'NONE',  ( 6.141676493652540536, -1.594220855400224401, -1.526124331276897950 ) ) ;
#32241=ORIENTED_EDGE ( 'NONE', *, *, #26940, .F. ) ;
#32242=CARTESIAN_POINT ( 'NONE',  ( 5.549440478958017842, -1.726947976793650197, 0.8215754744917986852 ) ) ;
#32250=CARTESIAN_POINT ( 'NONE',  ( 0.2570343420702363435, 1.821350608449383124, -0.2692129421619017804 ) ) ;
#32253=CARTESIAN_POINT ( 'NONE',  ( 4.956247902659736582, 0.7144662795386286236, 1.728917671469521800 ) ) ;
#32254=CARTESIAN_POINT ( 'NONE',  ( -0.02338929933909209349, 2.063686797106215387, -2.128951798380565918 ) ) ;
#32261=CARTESIAN_POINT ( 'NONE',  ( 1.182395473146230946, 1.177546377092754337, -1.578453288034264990 ) ) ;
#32263=CARTESIAN_POINT ( 'NONE',  ( 2.179314750421776026, 1.560514648525725967, 1.277027416600539755 ) ) ;
#32267=CARTESIAN_POINT ( 'NONE',  ( 2.009981539508858273, -1.034714594384738229, -1.931790675223004738 ) ) ;
#32274=AXIS2_PLACEMENT_3D ( 'NONE', #29191, #128899, #148283 ) ;
#32278=CARTESIAN_POINT ( 'NONE',  ( 5.073706409418358376, -1.018251046719556685, 1.533866337327425278 ) ) ;
#32279=CARTESIAN_POINT ( 'NONE',  ( 1.840491241682026047, 1.157229580565920513, -1.647056139248611384 ) ) ;
#32280=CARTESIAN_POINT ( 'NONE',  ( 3.480086682454126557, 2.076208366568982555, 0.9861560518420305899 ) ) ;
#32282=CARTESIAN_POINT ( 'NONE',  ( 0.6021283177516533192, 1.855420301818105910, 0.1446146731104556993 ) ) ;
#32285=CARTESIAN_POINT ( 'NONE',  ( 5.396708386617175890, -1.867154475869851504, -0.4128305108781898936 ) ) ;
#32288=CARTESIAN_POINT ( 'NONE',  ( 3.245728744149275702, 2.090933975402937683, -0.002398190518447183318 ) ) ;
#32289=CARTESIAN_POINT ( 'NONE',  ( 3.362029495745801899, 0.8400119854848131506, 1.671504782411597612 ) ) ;
#32291=CARTESIAN_POINT ( 'NONE',  ( 6.444863656277017405, -1.483217659742748218, -1.090817886357238198 ) ) ;
#32295=CARTESIAN_POINT ( 'NONE',  ( 5.496639145235802104, -0.4250261254647030307, -1.671567591930831043 ) ) ;
#32297=CARTESIAN_POINT ( 'NONE',  ( 0.5450593487147866734, -1.257523079656326148, 1.194353625382915673 ) ) ;
#32300=CARTESIAN_POINT ( 'NONE',  ( 4.873980352634836422, -2.130485078384927178, 0.4170503277054308788 ) ) ;
#32301=CARTESIAN_POINT ( 'NONE',  ( 3.562960707638890501, -1.610701098693729350, -0.8595150645765645692 ) ) ;
#32302=CARTESIAN_POINT ( 'NONE',  ( 0.7780835697005838991, -1.044612314895682292, -1.660310580060719188 ) ) ;
#32303=CARTESIAN_POINT ( 'NONE',  ( 5.366459209908462036, -2.066393128712967098, -0.4610789482254721294 ) ) ;
#32304=CARTESIAN_POINT ( 'NONE',  ( 6.110887424941569002, -0.2848874328069994633, 2.274520343394012212 ) ) ;
#32308=CARTESIAN_POINT ( 'NONE',  ( 1.910938629679886480, -0.5684797485801665884, -2.042784538176869003 ) ) ;
#32312=CARTESIAN_POINT ( 'NONE',  ( 6.315302488195832176, -1.857785929941946135, -1.123309179604212504 ) ) ;
#32313=CARTESIAN_POINT ( 'NONE',  ( 6.983263157960330147, 2.416677186285462575, 2.534499922921686021 ) ) ;
#32315=CARTESIAN_POINT ( 'NONE',  ( 1.963841274844113194, -1.786346139091129270, -1.320113705855001207 ) ) ;
#32317=CARTESIAN_POINT ( 'NONE',  ( -0.1042281025761494367, -0.9885194109933435058, -2.072332397174360352 ) ) ;
#32319=CARTESIAN_POINT ( 'NONE',  ( 5.963753124799120897, -0.5065058054696270906, 1.999279329544477513 ) ) ;
#32325=CARTESIAN_POINT ( 'NONE',  ( 4.563899478665734755, -1.199029595066217313, 1.397436126395680267 ) ) ;
#32327=CARTESIAN_POINT ( 'NONE',  ( -0.2104748580754201015, 7.629137130509078268, -2.703678718140526627 ) ) ;
#32328=CARTESIAN_POINT ( 'NONE',  ( 1.869703332329395895, 0.8828569656042523084, 1.481527559500251501 ) ) ;
#32330=( BOUNDED_SURFACE ( )  B_SPLINE_SURFACE ( 3, 3, ( 
 ( #186996, #59137, #58074, #157728, #204286, #171824, #23418, #205373, #122096, #154514 ),
 ( #72163, #89529, #42919, #9323, #40778, #6095, #139343, #57008, #137209, #22340 ),
 ( #87376, #123180, #189140, #106884, #172910, #24484, #41854, #207518, #153446, #90596 ),
 ( #54876, #104703, #88454, #156655, #173992, #8248, #203231, #74332, #140434, #124236 ),
 ( #121029, #107964, #25564, #125296, #191254, #38627, #43979, #60201, #161994, #94865 ),
 ( #158780, #209636, #14639, #193408, #192321, #211775, #196613, #27709, #113302, #109029 ),
 ( #126362, #142561, #160919, #110098, #210717, #128505, #159844, #130621, #26633, #111164 ) ),
 .UNSPECIFIED., .T., .F., .T. ) 
 B_SPLINE_SURFACE_WITH_KNOTS ( ( 4, 3, 4 ),
 ( 4, 1, 1, 1, 1, 1, 1, 4 ),
 ( 0.000000000000000000, 0.5000000000000000000, 1.000000000000000000 ),
 ( 0.000000000000000000, 0.09853459476447307130, 0.1926867929487333375, 0.2613852218134048999, 0.3629775382994345767, 0.5216635214973427415, 0.7338723600040717443, 1.000000000000000000 ),
 .UNSPECIFIED. ) 
 GEOMETRIC_REPRESENTATION_ITEM ( )  RATIONAL_B_SPLINE_SURFACE ( (
 ( 1.000000000000000000, 1.000000000000000000, 1.000000000000000222, 1.000000000000000000, 0.9999999999999997780, 1.000000000000000000, 0.9999999999999997780, 0.9999999999999997780, 1.000000000000000000, 1.000000000000000000),
 ( 0.3333333333333333703, 0.3333333333333333703, 0.3333333333333334259, 0.3333333333333333703, 0.3333333333333332593, 0.3333333333333334259, 0.3333333333333333148, 0.3333333333333333148, 0.3333333333333333703, 0.3333333333333333703),
 ( 0.3333333333333333703, 0.3333333333333333703, 0.3333333333333334259, 0.3333333333333333703, 0.3333333333333332593, 0.3333333333333334259, 0.3333333333333333148, 0.3333333333333333148, 0.3333333333333333703, 0.3333333333333333703),
 ( 1.000000000000000000, 1.000000000000000000, 1.000000000000000222, 1.000000000000000000, 0.9999999999999997780, 1.000000000000000000, 0.9999999999999997780, 0.9999999999999997780, 1.000000000000000000, 1.000000000000000000),
 ( 0.3333333333333333703, 0.3333333333333333703, 0.3333333333333334259, 0.3333333333333333703, 0.3333333333333332593, 0.3333333333333334259, 0.3333333333333333148, 0.3333333333333333148, 0.3333333333333333703, 0.3333333333333333703),
 ( 0.3333333333333333703, 0.3333333333333333703, 0.3333333333333334259, 0.3333333333333333703, 0.3333333333333332593, 0.3333333333333334259, 0.3333333333333333148, 0.3333333333333333148, 0.3333333333333333703, 0.3333333333333333703),
 ( 1.000000000000000000, 1.000000000000000000, 1.000000000000000222, 1.000000000000000000, 0.9999999999999997780, 1.000000000000000000, 0.9999999999999997780, 0.9999999999999997780, 1.000000000000000000, 1.000000000000000000) ) ) 
 REPRESENTATION_ITEM ( '' )  SURFACE ( )  );
#32332=CARTESIAN_POINT ( 'NONE',  ( 1.124742813458483814, 1.347236035482470839, -1.817372803150618221 ) ) ;
#32333=CARTESIAN_POINT ( 'NONE',  ( 3.897179185067170870, 1.779300596213341690, -1.126466309965125756 ) ) ;
#32335=CARTESIAN_POINT ( 'NONE',  ( 2.020411781336392210, 1.649200945362235826, 0.6424177339450982682 ) ) ;
#32343=CARTESIAN_POINT ( 'NONE',  ( 5.396815004230996138, -2.167347303010109805, -0.4865036897706440100 ) ) ;
#32344=CARTESIAN_POINT ( 'NONE',  ( 2.959115643078192193, 0.3208686883675835877, -2.167707805308824121 ) ) ;
#32350=CARTESIAN_POINT ( 'NONE',  ( 6.609999999999973674, 0.5530568637619069916, 2.330679033986877258 ) ) ;
#32352=CARTESIAN_POINT ( 'NONE',  ( 5.554972086574996304, 0.4156608669513594534, 2.079290889414136423 ) ) ;
#32359=CARTESIAN_POINT ( 'NONE',  ( 6.075717905342373548, -0.9791751913862613010, 1.559117742379905858 ) ) ;
#32363=CARTESIAN_POINT ( 'NONE',  ( 2.067524827727816650, -1.070173352442949311, 1.372458522238986234 ) ) ;
#32365=CARTESIAN_POINT ( 'NONE',  ( 0.5901948623465642640, 1.011764341257429978, -1.680720577067334354 ) ) ;
#32368=CARTESIAN_POINT ( 'NONE',  ( 6.174726448494309849, -2.051094451480539149, -0.6828207641706719455 ) ) ;
#32372=CARTESIAN_POINT ( 'NONE',  ( 5.418883921851007202, 1.995750516393671514, 0.8311057252617033431 ) ) ;
#32376=CARTESIAN_POINT ( 'NONE',  ( 6.362572844203587152, -1.395794784517788045, 1.392370165595870679 ) ) ;
#32377=CARTESIAN_POINT ( 'NONE',  ( 5.167242596723413683, -0.5858957144197572964, -1.632003580468445847 ) ) ;
#32379=CARTESIAN_POINT ( 'NONE',  ( 1.716621854089026344, 2.046377219401524616, 0.7848826361863747714 ) ) ;
#32380=CARTESIAN_POINT ( 'NONE',  ( 3.593080373992099119, -0.4475695053229776788, -2.263611109821815681 ) ) ;
#32381=CARTESIAN_POINT ( 'NONE',  ( 4.499328421682089463, 1.652694973434418291, 1.230784805264173221 ) ) ;
#32382=CARTESIAN_POINT ( 'NONE',  ( 0.6736475468689150370, -1.079418705485206020, 1.614127575861698416 ) ) ;
#32387=CARTESIAN_POINT ( 'NONE',  ( 3.867525618572264623, -1.764951123045129577, -1.175235903013646332 ) ) ;
#32388=CARTESIAN_POINT ( 'NONE',  ( 0.8619541869999207684, -0.05229984143813663777, -2.015912905633105101 ) ) ;
#32390=CARTESIAN_POINT ( 'NONE',  ( 4.313639225654395837, -0.3805011380913872476, 2.173570407251994574 ) ) ;
#32398=CARTESIAN_POINT ( 'NONE',  ( 4.135659164760732587, -1.419885373862592726, -1.493960738838293389 ) ) ;
#32401=CARTESIAN_POINT ( 'NONE',  ( 3.317061382196756281, 1.590690956008104395, -1.244364558649863728 ) ) ;
#32405=CARTESIAN_POINT ( 'NONE',  ( 3.590745217537123057, -0.4003831998886059340, -2.021439917362640504 ) ) ;
#32408=CARTESIAN_POINT ( 'NONE',  ( -0.2411972340276023752, 5.722880186377757639, -2.494559970919587588 ) ) ;
#32409=CARTESIAN_POINT ( 'NONE',  ( 0.7965151530783078915, 1.503791256141374211, 1.061989520254283059 ) ) ;
#32410=CARTESIAN_POINT ( 'NONE',  ( 6.551417122825020201, -1.769646310455678995, -1.318412661681533260 ) ) ;
#32412=CARTESIAN_POINT ( 'NONE',  ( 1.511231465835579879, 1.905624552496063995, 1.020381674553122231 ) ) ;
#32414=CARTESIAN_POINT ( 'NONE',  ( 2.466030083290056130, -1.032479112849067793, 1.731996155473938259 ) ) ;
#32416=CARTESIAN_POINT ( 'NONE',  ( 1.810362406828632365, -1.941531176516932522, 1.229804462443480295 ) ) ;
#32418=CARTESIAN_POINT ( 'NONE',  ( 0.3736316133628528879, 1.073300769168658908, 1.531925686032776124 ) ) ;
#32420=CARTESIAN_POINT ( 'NONE',  ( 5.084826545086224669, -0.2406546161831616404, -1.956650619579934469 ) ) ;
#32421=CARTESIAN_POINT ( 'NONE',  ( 5.208220363674559650, 1.197307938467083055, -1.622483861274232719 ) ) ;
#32425=CARTESIAN_POINT ( 'NONE',  ( 5.813134535821789406, 1.856751089961257373, 0.9939634876292826604 ) ) ;
#32427=CARTESIAN_POINT ( 'NONE',  ( 6.654741963219192868, -0.5482099483974657295, -1.996413779700876301 ) ) ;
#32430=CARTESIAN_POINT ( 'NONE',  ( 6.639320575229251453, 2.441375407831634536, 2.385816205380648203 ) ) ;
#32431=CARTESIAN_POINT ( 'NONE',  ( 5.203380996274193038, 1.779418458119955915, -0.9556711282029080046 ) ) ;
#32433=CARTESIAN_POINT ( 'NONE',  ( 3.844573663522454332, 2.296428955072826295, 0.2277027427845106922 ) ) ;
#32434=CARTESIAN_POINT ( 'NONE',  ( 1.551709131853472368, 1.559248165652558082, 1.350213067335771511 ) ) ;
#32441=CARTESIAN_POINT ( 'NONE',  ( 4.264261594705793357, -2.165624863444326920, 0.1558643175220644772 ) ) ;
#32444=CARTESIAN_POINT ( 'NONE',  ( 3.315785976855676775, 1.165629053876730659, -1.425327459889616177 ) ) ;
#32446=CARTESIAN_POINT ( 'NONE',  ( 4.265290774032561849, 2.125562838249666964, -0.5332280334861272397 ) ) ;
#32448=CARTESIAN_POINT ( 'NONE',  ( 6.016560025881092066, 1.524636124814653382, -1.671835012792993735 ) ) ;
#32453=CARTESIAN_POINT ( 'NONE',  ( 6.485617131683707903, 1.222450955268041373, 1.279935727357548458 ) ) ;
#32454=CARTESIAN_POINT ( 'NONE',  ( 3.668611300974702782, 0.7265845916090816203, 1.877559629772174166 ) ) ;
#32456=CARTESIAN_POINT ( 'NONE',  ( 2.889785439676189505, 1.488280975668257344, 1.490260817651526182 ) ) ;
#32457=CARTESIAN_POINT ( 'NONE',  ( 1.704550880262687640, 1.788078052428695219, 0.6877594758711459422 ) ) ;
#32459=CARTESIAN_POINT ( 'NONE',  ( 3.508217419976053630, 1.969739563948954331, 0.002549893942540777322 ) ) ;
#32461=CARTESIAN_POINT ( 'NONE',  ( 4.869401706892690029, -1.708532917064720991, -1.076912495999365449 ) ) ;
#32462=CARTESIAN_POINT ( 'NONE',  ( 0.7955152940811484052, -0.6771210053572243037, 1.743984199989514927 ) ) ;
#32463=CARTESIAN_POINT ( 'NONE',  ( 0.9769180011504545735, 1.811320799089161993, 0.7541596914439269161 ) ) ;
#32464=CARTESIAN_POINT ( 'NONE',  ( 0.3867804997886997720, -1.801505969789623629, -0.6421655129100201087 ) ) ;
#32467=CARTESIAN_POINT ( 'NONE',  ( 6.192256348250350761, -1.861847689568534081, -0.1814220289034565448 ) ) ;
#32469=CARTESIAN_POINT ( 'NONE',  ( 6.983263157960365675, -0.006178392973848687020, 2.053544886540019210 ) ) ;
#32470=CARTESIAN_POINT ( 'NONE',  ( 1.381394743813993964, -0.05274132383669553892, 2.069866178704109938 ) ) ;
#32475=CARTESIAN_POINT ( 'NONE',  ( 5.162787349232583090, 0.6159572760087471677, 2.029033592890214788 ) ) ;
#32479=EDGE_CURVE ( 'NONE', #102469, #141519, #35632, .T. ) ;
#32480=CARTESIAN_POINT ( 'NONE',  ( 6.180128940399614912, -1.088687182605744042, -1.631870318916525120 ) ) ;
#32482=CARTESIAN_POINT ( 'NONE',  ( 4.446638634790680555, 1.314796391739966985, 1.528506369862133285 ) ) ;
#32483=CARTESIAN_POINT ( 'NONE',  ( 3.239363768214057249, 0.4605203156026844158, -1.859431460922003509 ) ) ;
#32485=CARTESIAN_POINT ( 'NONE',  ( 1.575987392057216940, -1.168677030305173004, 1.853764812240476623 ) ) ;
#32487=CARTESIAN_POINT ( 'NONE',  ( 3.479631686803522417, 1.184185218286455621, 1.448006030947253331 ) ) ;
#32491=CARTESIAN_POINT ( 'NONE',  ( 5.659793223991267830, 1.261623160278273481, 1.700126385781860927 ) ) ;
#32494=CARTESIAN_POINT ( 'NONE',  ( 2.103177918021365223, -0.4551342947399418248, 2.040444103505714146 ) ) ;
#32496=CARTESIAN_POINT ( 'NONE',  ( 1.289626238417174831, -0.7804147442260088718, 1.538193839892360471 ) ) ;
#32506=CARTESIAN_POINT ( 'NONE',  ( 2.086290463123147365, -1.113812826415590651, 1.428500571052490953 ) ) ;
#32511=CARTESIAN_POINT ( 'NONE',  ( 6.639320575229251453, 2.090987163941595561, 2.106969785032047238 ) ) ;
#32516=CARTESIAN_POINT ( 'NONE',  ( 3.121387120179277996, 0.2756568158089545695, -1.840403582779404745 ) ) ;
#32517=CARTESIAN_POINT ( 'NONE',  ( 0.06975588353394339414, -0.9023057962903738849, 1.689756990376343859 ) ) ;
#32518=CARTESIAN_POINT ( 'NONE',  ( 6.229514091203088633, -1.813738808949336478, 0.6494875524521417365 ) ) ;
#32519=CARTESIAN_POINT ( 'NONE',  ( 5.951642636407408204, 1.565221049572671497, 1.355249363302114096 ) ) ;
#32525=CARTESIAN_POINT ( 'NONE',  ( 4.434397634191796556, -1.137439385922611290, 1.607554744723362017 ) ) ;
#32527=CARTESIAN_POINT ( 'NONE',  ( 1.787894333202539654, 2.028250040683087008, -0.6185522307536188702 ) ) ;
#32529=CARTESIAN_POINT ( 'NONE',  ( 6.777182134110200096, 7.629137130509069387, 2.789055895399249696 ) ) ;
#32531=CARTESIAN_POINT ( 'NONE',  ( 6.087848540548081999, -2.180536604488235941, -0.2183335821156970336 ) ) ;
#32533=CARTESIAN_POINT ( 'NONE',  ( 4.032187520235196665, 1.031363847994439142, -1.626874456138996949 ) ) ;
#32535=EDGE_CURVE ( 'NONE', #144405, #53136, #96838, .T. ) ;
#32536=CARTESIAN_POINT ( 'NONE',  ( 0.6569167496461197908, -1.539450689919025450, -0.9809549629347170674 ) ) ;
#32537=CARTESIAN_POINT ( 'NONE',  ( 0.5752038918783763943, -2.079344756725898691, -0.7397341299467048437 ) ) ;
#32540=CARTESIAN_POINT ( 'NONE',  ( 6.244967536942622743, -0.2852903188887367936, -1.948516424197583197 ) ) ;
#32541=CARTESIAN_POINT ( 'NONE',  ( 1.698673089578231599, 1.615691133820891467, 1.077277171393706379 ) ) ;
#32542=CARTESIAN_POINT ( 'NONE',  ( 6.309976275596433481, -1.946771231211348319, 1.221538734657970693 ) ) ;
#32544=CARTESIAN_POINT ( 'NONE',  ( 5.119887769377023723, 1.841019424034021412, -0.2705144023524996277 ) ) ;
#32549=CARTESIAN_POINT ( 'NONE',  ( 1.892365914234435120, -0.5883382831698009685, -2.111031122750434808 ) ) ;
#32551=ORIENTED_EDGE ( 'NONE', *, *, #21794, .T. ) ;
#32554=CARTESIAN_POINT ( 'NONE',  ( 1.312830284664792790, 1.609138963534262778, 0.8624270714618911260 ) ) ;
#32559=CARTESIAN_POINT ( 'NONE',  ( 6.199803715563785289, -0.6102442156579389598, 1.720816905678754782 ) ) ;
#32560=CARTESIAN_POINT ( 'NONE',  ( 4.944172655442597097, -0.9282843415348587257, 1.728263438747808856 ) ) ;
#32563=CARTESIAN_POINT ( 'NONE',  ( 5.039744756118590630, -2.013340025477545758, 0.6656774797743277849 ) ) ;
#32564=CARTESIAN_POINT ( 'NONE',  ( 4.441096743985088580, -1.694418930461354611, -1.389946530008886905 ) ) ;
#32568=CARTESIAN_POINT ( 'NONE',  ( 2.430607852509637290, -1.277051959022021066, 1.629327859714514659 ) ) ;
#32573=CARTESIAN_POINT ( 'NONE',  ( 3.147439182535469726, 1.035885224147353512, 2.052142740569740109 ) ) ;
#32577=CARTESIAN_POINT ( 'NONE',  ( 6.620655732516645742, 3.706282450693794139, 2.340867613974298767 ) ) ;
#32579=CARTESIAN_POINT ( 'NONE',  ( 4.031144971506396502, -1.339966268285474715, -1.405800288483616045 ) ) ;
#32582=CARTESIAN_POINT ( 'NONE',  ( 3.550944491985886575, 0.2853618425060593378, 1.890879049853078087 ) ) ;
#32584=CARTESIAN_POINT ( 'NONE',  ( 4.998908393266289885, 1.432429904705156520, -0.9603719661937599739 ) ) ;
#32585=CARTESIAN_POINT ( 'NONE',  ( 3.344935638061694139, -1.780668040901035143, -0.9463001528628791625 ) ) ;
#32586=CARTESIAN_POINT ( 'NONE',  ( 5.608098314261791728, -0.05969564267381716194, 2.298051806275173359 ) ) ;
#32588=CARTESIAN_POINT ( 'NONE',  ( 0.3818278861203865393, 2.057605126571937060, -0.7983354260262252033 ) ) ;
#32590=CARTESIAN_POINT ( 'NONE',  ( 6.010986587707961348, 1.561705629380090832, 0.8325338966498199156 ) ) ;
#32592=CARTESIAN_POINT ( 'NONE',  ( 1.922231132759700589, 1.317440867170904362, -1.875679006090027690 ) ) ;
#32594=CARTESIAN_POINT ( 'NONE',  ( 0.7259949354544228406, 0.1236639744153274628, 1.736007293746767655 ) ) ;
#32600=CARTESIAN_POINT ( 'NONE',  ( 1.012457490462664644, 2.168662962709181574, -0.1065306264821704596 ) ) ;
#32601=CARTESIAN_POINT ( 'NONE',  ( 2.501185699981960830, -0.1928336239410358699, 2.007256303757164240 ) ) ;
#32603=CARTESIAN_POINT ( 'NONE',  ( 5.250583079984638246, 0.5609921762826737268, 1.843012466491249723 ) ) ;
#32605=CARTESIAN_POINT ( 'NONE',  ( 2.303257990033405367, -0.3847559998488152000, -2.187706203110438175 ) ) ;
#32610=CARTESIAN_POINT ( 'NONE',  ( 5.073663595168481422, -0.9608294848038684277, 1.450969404730037660 ) ) ;
#32611=CARTESIAN_POINT ( 'NONE',  ( 3.068751266904270025, 1.422870340827029345, -1.350941015047700366 ) ) ;
#32615=CARTESIAN_POINT ( 'NONE',  ( 4.657670937300908420, 0.5017462980881717272, -2.205921056424357651 ) ) ;
#32616=CARTESIAN_POINT ( 'NONE',  ( 0.7134213396373456639, -1.741552128810987421, -1.105017490550715742 ) ) ;
#32620=CARTESIAN_POINT ( 'NONE',  ( 1.903560677580185656, 1.881515123832262715, 1.256258119677531315 ) ) ;
#32623=CARTESIAN_POINT ( 'NONE',  ( 2.231529376059933956, -1.218349341866202362, -1.419469154777988296 ) ) ;
#32624=CARTESIAN_POINT ( 'NONE',  ( 1.705275228087951955, 1.618143048327233435, 0.6241232001420042863 ) ) ;
#32625=CARTESIAN_POINT ( 'NONE',  ( 5.671465802443460547, 1.304529079428708549, 1.760837017921567771 ) ) ;
#32626=CARTESIAN_POINT ( 'NONE',  ( 6.704155097142892927, -2.307279366673311127, 0.04705588035085367382 ) ) ;
#32627=CARTESIAN_POINT ( 'NONE',  ( 1.288041055883992536, -0.9272951443832450069, 1.840570288256936804 ) ) ;
#32628=CARTESIAN_POINT ( 'NONE',  ( 4.259667731375265554, 0.9167342216760937523, 1.711951518900257430 ) ) ;
#32631=CARTESIAN_POINT ( 'NONE',  ( 6.573518820989788125, 1.789947451694914982, -0.5432430119688207437 ) ) ;
#32632=CARTESIAN_POINT ( 'NONE',  ( 1.500000000000001110, -8.632537233970167800E-14, -2.052068128417951165 ) ) ;
#32635=CARTESIAN_POINT ( 'NONE',  ( 6.520861224751243412, 2.010896128390584625, -0.1455136175190149816 ) ) ;
#32637=CARTESIAN_POINT ( 'NONE',  ( 6.100232455412330168, -0.2440331339308223768, 2.001510902166554473 ) ) ;
#32641=CARTESIAN_POINT ( 'NONE',  ( 2.560947663861262491, -1.588335953301520220, -0.9000364273514869229 ) ) ;
#32643=CARTESIAN_POINT ( 'NONE',  ( -0.1296875068448125334, 4.095146142119266308, -2.381513845672214913 ) ) ;
#32648=CARTESIAN_POINT ( 'NONE',  ( 0.3518269803744868418, -1.431374087835567632, -1.425298768015555551 ) ) ;
#32649=CARTESIAN_POINT ( 'NONE',  ( 6.568989397875739655, -1.719265429537725431, 1.406094356362475706 ) ) ;
#32653=CARTESIAN_POINT ( 'NONE',  ( 6.789916310432966284, -0.8843476597930698402, 1.859958747594625317 ) ) ;
#32654=CARTESIAN_POINT ( 'NONE',  ( 4.992814645674491736, -2.006446365708704160, 0.2004330516618065550 ) ) ;
#32655=EDGE_LOOP ( 'NONE', ( #115956, #113285, #195009, #23475 ) ) ;
#32662=CARTESIAN_POINT ( 'NONE',  ( 4.956407584168041502, 1.492027487219639514, 1.356091576722208369 ) ) ;
#32663=CARTESIAN_POINT ( 'NONE',  ( 4.857273802806507668, 1.820629801081237620, -0.2732171615176108848 ) ) ;
#32665=CARTESIAN_POINT ( 'NONE',  ( 3.668876216774307863, -1.550535085938867352, 1.709345553852769095 ) ) ;
#32667=CARTESIAN_POINT ( 'NONE',  ( 5.518883860308030798, 1.994880785013030788, 0.8329173350848093627 ) ) ;
#32669=CARTESIAN_POINT ( 'NONE',  ( 0.6966983018150345597, 1.588492033560371830, 1.117026046969020303 ) ) ;
#32677=CARTESIAN_POINT ( 'NONE',  ( 3.010468980803046257, 1.356049738124785353, -1.288842618233053683 ) ) ;
#32678=CARTESIAN_POINT ( 'NONE',  ( 1.722773492080275748, 1.414811824084385661, -1.286832238068566392 ) ) ;
#32681=CARTESIAN_POINT ( 'NONE',  ( 2.596532132193625664, -2.201043451360765957, -0.1612727490639675743 ) ) ;
#32687=CARTESIAN_POINT ( 'NONE',  ( 0.5265599218138971027, 1.885207356905926668, 0.5763402985480212681 ) ) ;
#32688=CARTESIAN_POINT ( 'NONE',  ( 1.677271382912606246, -2.191714306423699021, -0.7221938283701042627 ) ) ;
#32689=CARTESIAN_POINT ( 'NONE',  ( 1.767943819387544968, -1.947426213878332035, 0.2369139692007388165 ) ) ;
#32690=CARTESIAN_POINT ( 'NONE',  ( 5.330950330247254065, -1.940297947978512960, -0.6998911787638012472 ) ) ;
#32697=CARTESIAN_POINT ( 'NONE',  ( 1.323347942641838415, -1.961697495959934479, -0.9305402519725998189 ) ) ;
#32699=CARTESIAN_POINT ( 'NONE',  ( 6.550350952284553330, -1.418464805562440922, 1.173678288350611609 ) ) ;
#32702=CARTESIAN_POINT ( 'NONE',  ( 1.405301488743180061, -0.4598193086536165319, 1.813012767170335993 ) ) ;
#32703=CARTESIAN_POINT ( 'NONE',  ( 5.606754022945427351, 1.640879930231559758, -1.407263238018638507 ) ) ;
#32708=CARTESIAN_POINT ( 'NONE',  ( 1.260255548581414642, 1.910129771108992625, 0.09294656408432439010 ) ) ;
#32709=CARTESIAN_POINT ( 'NONE',  ( 3.467426238747231881, 1.726840169280913662, -0.3869839817904097701 ) ) ;
#32710=CARTESIAN_POINT ( 'NONE',  ( 0.7328884408557728714, 1.767063509844998492, 0.7314339715377634610 ) ) ;
#32712=CARTESIAN_POINT ( 'NONE',  ( 5.185127790529111991, 1.568658432645179124, 1.099198482053822534 ) ) ;
#32713=CARTESIAN_POINT ( 'NONE',  ( 6.109808257530946918, 0.5734047718448382902, -1.884209069281018500 ) ) ;
#32715=CARTESIAN_POINT ( 'NONE',  ( 1.441811196653530747, -1.994930912159533332, 0.7194735443712959588 ) ) ;
#32717=CARTESIAN_POINT ( 'NONE',  ( 4.487079325084206260, 1.670935625628103605, -0.8411387520786617333 ) ) ;
#32718=CARTESIAN_POINT ( 'NONE',  ( 0.8030139110496161692, 1.490934425176414502, 1.053415343471690857 ) ) ;
#32720=CARTESIAN_POINT ( 'NONE',  ( 4.213639274598267370, -0.3785452818781535611, 2.174016619501429215 ) ) ;
#32723=CARTESIAN_POINT ( 'NONE',  ( 1.574752048370867907, 1.386759265612296455, -1.527078818449955966 ) ) ;
#32732=CARTESIAN_POINT ( 'NONE',  ( 4.668459276380106715, -0.8822503692092443783, -1.873099891353036561 ) ) ;
#32735=CARTESIAN_POINT ( 'NONE',  ( 1.001511639980020130, 1.766541945284912263, 1.245431700958275600 ) ) ;
#32737=CARTESIAN_POINT ( 'NONE',  ( 2.508468462390922138, -2.014426205243079693, -0.1462163075645859234 ) ) ;
#32744=CARTESIAN_POINT ( 'NONE',  ( 0.4445464637146989695, -1.457232572767804379, 1.394089106691732693 ) ) ;
#32745=CARTESIAN_POINT ( 'NONE',  ( 5.442994344319362021, -1.727133847215430729, -1.348975639928217118 ) ) ;
#32748=CARTESIAN_POINT ( 'NONE',  ( 3.691585721427274702, 1.799035686688513325, -0.6489376663148455071 ) ) ;
#32752=CARTESIAN_POINT ( 'NONE',  ( 1.810172953844836341, 1.158670025852935437, -1.650096248209935945 ) ) ;
#32754=CARTESIAN_POINT ( 'NONE',  ( 0.2930494462585155335, 1.901387222806522503, -1.280258756811911702 ) ) ;
#32756=CARTESIAN_POINT ( 'NONE',  ( 3.838627834895870450, 0.2530714650476103555, 1.705954220825799617 ) ) ;
#32757=CARTESIAN_POINT ( 'NONE',  ( -0.1399997263889820043, 5.722209607272843002, -2.594334538518060729 ) ) ;
#32760=( BOUNDED_CURVE ( )  B_SPLINE_CURVE ( 3, ( #138442, #56114, #91838, #208739 ),
 .UNSPECIFIED., .F., .T. ) 
 B_SPLINE_CURVE_WITH_KNOTS ( ( 4, 4 ),
 ( 0.000000000000000000, 0.5000000000000027756 ),
 .UNSPECIFIED. ) 
 CURVE ( )  GEOMETRIC_REPRESENTATION_ITEM ( )  RATIONAL_B_SPLINE_CURVE ( ( 1.000000000000000000, 0.3333333333333296511, 0.3333333333333333703, 1.000000000000003775 ) ) 
 REPRESENTATION_ITEM ( '' )  );
#32762=CARTESIAN_POINT ( 'NONE',  ( 0.3911966820569385828, 1.383097094795827209, 1.259704262696823118 ) ) ;
#32764=CARTESIAN_POINT ( 'NONE',  ( 0.07516593201273641389, 2.869485459350088696, -2.532657826882792840 ) ) ;
#32766=CARTESIAN_POINT ( 'NONE',  ( 0.3212534483023680165, -1.847719145540312358, -0.9339786784923130858 ) ) ;
#32768=CARTESIAN_POINT ( 'NONE',  ( 5.514259914679787045, -1.811656974672648746, 0.006318095929410197376 ) ) ;
#32772=CARTESIAN_POINT ( 'NONE',  ( 5.918593472536316291, -0.6585524616501952089, -1.687715565691887187 ) ) ;
#32775=CARTESIAN_POINT ( 'NONE',  ( 2.484552680892829546, -0.3758780662847274190, -2.158817762932266682 ) ) ;
#32777=CARTESIAN_POINT ( 'NONE',  ( 6.654761307663171976, -0.4979203083825957110, -1.793151784937331961 ) ) ;
#32779=CARTESIAN_POINT ( 'NONE',  ( 3.937047882288559286, -1.594636078160330150, -1.061121380078999143 ) ) ;
#32787=CARTESIAN_POINT ( 'NONE',  ( 5.471900407082693540, -0.9496530807377671080, 1.892462605218522720 ) ) ;
#32788=CARTESIAN_POINT ( 'NONE',  ( 0.8312129145573650124, 0.1600495679085281175, 2.155820468135719814 ) ) ;
#32792=CARTESIAN_POINT ( 'NONE',  ( 1.096400207583309028, -0.4391605778215034173, -1.771851442210800709 ) ) ;
#32795=CARTESIAN_POINT ( 'NONE',  ( 3.012524388372894713, 1.323457619556423381, -1.257707024427484388 ) ) ;
#32798=CARTESIAN_POINT ( 'NONE',  ( 2.594150448275188481, 0.9308562254837976502, -1.735710503097695145 ) ) ;
#32800=CARTESIAN_POINT ( 'NONE',  ( 5.302268720778519295, 1.468090865803386880, -1.271420572733022780 ) ) ;
#32803=CARTESIAN_POINT ( 'NONE',  ( 5.238584497427841491, 1.261362679698872169, -1.704546977916908457 ) ) ;
#32805=CARTESIAN_POINT ( 'NONE',  ( 3.018110381800835018, -1.909997030407738938, 0.09613604992317337228 ) ) ;
#32810=CARTESIAN_POINT ( 'NONE',  ( 3.861980204584365861, 0.6760143841026149403, -1.896330825423567568 ) ) ;
#32812=CARTESIAN_POINT ( 'NONE',  ( 4.723181480036696023, -0.08661695748878039947, 1.823760500460340550 ) ) ;
#32813=CARTESIAN_POINT ( 'NONE',  ( 0.7134375191242479097, -1.748147108003229810, -1.108949491591210146 ) ) ;
#32818=CARTESIAN_POINT ( 'NONE',  ( 5.436355746168001879, 1.843147576875401983, 0.3187000444574567548 ) ) ;
#32826=CARTESIAN_POINT ( 'NONE',  ( 6.666846200133992539, 1.614693783697606522, -1.451540455714307010 ) ) ;
#32827=CARTESIAN_POINT ( 'NONE',  ( 2.513409721704229494, -1.974398269817168483, 0.7648893725459534609 ) ) ;
#32830=CARTESIAN_POINT ( 'NONE',  ( 6.596543124887806364, 2.046857425119428697, 0.3097440254393943881 ) ) ;
#32835=CARTESIAN_POINT ( 'NONE',  ( 2.871321604122719418, 2.176383266876817046, -0.7197843628353149947 ) ) ;
#32838=CARTESIAN_POINT ( 'NONE',  ( 2.531394148431935776, -0.1834752923718513118, 1.903540536635806912 ) ) ;
#32841=CARTESIAN_POINT ( 'NONE',  ( 0.8264323289940983530, -0.9090603351678091526, -1.796376205119714298 ) ) ;
#32842=CARTESIAN_POINT ( 'NONE',  ( 1.059338230090471011, 1.600537254139059673, 1.134074526779847769 ) ) ;
#32847=CARTESIAN_POINT ( 'NONE',  ( 3.574242788201603016, -2.014869992041759872, -0.5574694344734670848 ) ) ;
#32848=CARTESIAN_POINT ( 'NONE',  ( 2.201683042903946230, -1.769559083619182349, 0.04015057502057895605 ) ) ;
#32852=CARTESIAN_POINT ( 'NONE',  ( 5.279328977631358555, 1.536242920967767711, 1.701453964730540447 ) ) ;
#32853=CARTESIAN_POINT ( 'NONE',  ( 4.013389373331836651, -0.8969206028703354816, -1.491242602974415243 ) ) ;
#32856=CARTESIAN_POINT ( 'NONE',  ( 4.446485213073447795, 1.132808404574834782, 1.312715084458302872 ) ) ;
#32857=CARTESIAN_POINT ( 'NONE',  ( 4.633362100890871638, 0.004430012494727622249, -2.171350061612055349 ) ) ;
#32859=CARTESIAN_POINT ( 'NONE',  ( 5.542203953035277131, 0.8216685229280199509, 1.841735684200429990 ) ) ;
#32860=CARTESIAN_POINT ( 'NONE',  ( 0.9375000000000007772, 1.451031289061083251, -1.451031289061159413 ) ) ;
#32862=CARTESIAN_POINT ( 'NONE',  ( 2.309485145960771035, -0.4240201670873133266, 1.878992650109307716 ) ) ;
#32864=CARTESIAN_POINT ( 'NONE',  ( 6.117462548578989967, 1.846355941783444976, 1.234888080409371369 ) ) ;
#32866=CARTESIAN_POINT ( 'NONE',  ( 6.883263157960335832, 7.629137130509037412, 2.646189081643287810 ) ) ;
#32869=CARTESIAN_POINT ( 'NONE',  ( 1.752877424878969803, 2.197725149470313166, 0.3219655503990859757 ) ) ;
#32870=CARTESIAN_POINT ( 'NONE',  ( 6.812952578306354035, -1.517200236233799071, 1.243500037895749921 ) ) ;
#32877=CARTESIAN_POINT ( 'NONE',  ( 4.404768648179163471, 0.5469982912414109721, 1.988780625590305329 ) ) ;
#32881=CARTESIAN_POINT ( 'NONE',  ( 5.905500869136258046, -0.4549164269060863020, 1.814235589242949587 ) ) ;
#32882=CARTESIAN_POINT ( 'NONE',  ( 4.781731028689206298, 1.437863813525115830, -0.9690746147167289548 ) ) ;
#32883=CARTESIAN_POINT ( 'NONE',  ( 4.001278354253400948, -1.735443821832120870, 0.1328310682092836426 ) ) ;
#32885=CARTESIAN_POINT ( 'NONE',  ( 2.454944477651953783, -1.996203790030710801, -1.126857184891062236 ) ) ;
#32887=CARTESIAN_POINT ( 'NONE',  ( 5.214434122969894503, 1.932256357821033887, 0.7989942847940935122 ) ) ;
#32888=CARTESIAN_POINT ( 'NONE',  ( 0.6910384644343779970, -0.6650364481293036256, 1.717017257891314097 ) ) ;
#32890=CARTESIAN_POINT ( 'NONE',  ( 3.024064729735044921, -1.777011313454954999, 0.9530116517338580451 ) ) ;
#32891=CARTESIAN_POINT ( 'NONE',  ( 0.8850414913617115076, 1.931072968267994794, -1.036053359626129655 ) ) ;
#32894=CARTESIAN_POINT ( 'NONE',  ( 1.486871883557450369, 1.994755712061954123, 0.5540851298423480342 ) ) ;
#32897=CARTESIAN_POINT ( 'NONE',  ( 3.809332071562030908, 1.790574611000576244, -1.135637872363919110 ) ) ;
#32899=CARTESIAN_POINT ( 'NONE',  ( 6.498675964634617941, -0.4922777150685350156, -1.758009983081544991 ) ) ;
#32906=CARTESIAN_POINT ( 'NONE',  ( 3.761977063697896639, 0.6766415394236917624, -1.903234751996728757 ) ) ;
#32907=CARTESIAN_POINT ( 'NONE',  ( 6.545939543708723107, 0.8506627741289953804, -2.036432556493542823 ) ) ;
#32911=CARTESIAN_POINT ( 'NONE',  ( 5.067181549875774849, 1.617961714123143047, 0.9193176493522186021 ) ) ;
#32916=CARTESIAN_POINT ( 'NONE',  ( 6.561407802241105536, 0.3549014609278942078, -2.029936712941163623 ) ) ;
#32921=CARTESIAN_POINT ( 'NONE',  ( 2.231429653443087080, -1.583367121652721421, -0.7069697159475217818 ) ) ;
#32922=CARTESIAN_POINT ( 'NONE',  ( 1.183123967286016986, -0.7853004192260810701, 1.553138493749019133 ) ) ;
#32923=CARTESIAN_POINT ( 'NONE',  ( 0.4116873800214932988, 2.009943462479982124, 1.133530718095694168 ) ) ;
#32926=CARTESIAN_POINT ( 'NONE',  ( 2.126313425470290674, 1.189129703756890644, -1.682874868902742405 ) ) ;
#32928=EDGE_CURVE ( 'NONE', #8531, #144405, #132626, .T. ) ;
#32929=CARTESIAN_POINT ( 'NONE',  ( 1.001327120302420548, 1.985796081718914419, 0.3474166314290441648 ) ) ;
#32932=CARTESIAN_POINT ( 'NONE',  ( 6.578970801323708706, -0.09418725797194843485, -1.868394071727994543 ) ) ;
#32934=CARTESIAN_POINT ( 'NONE',  ( 4.131050151015442928, 1.750605847248308145, 0.7702136748066327199 ) ) ;
#32936=CARTESIAN_POINT ( 'NONE',  ( 5.637410271038987730, -1.996576301129053377, 0.9405272304151901519 ) ) ;
#32941=CARTESIAN_POINT ( 'NONE',  ( 0.3990893844944528590, -0.2493554465154389221, -2.004162882155545056 ) ) ;
#32944=CARTESIAN_POINT ( 'NONE',  ( 5.087122877145462851, -0.2765918260761930925, -2.290891016797763413 ) ) ;
#32945=CARTESIAN_POINT ( 'NONE',  ( 4.492601031306558745, 1.923586649950057792, 0.3847822903023030428 ) ) ;
#32946=CARTESIAN_POINT ( 'NONE',  ( 1.815213341579174688, -1.679845371888911698, -1.013028538569618719 ) ) ;
#32950=CARTESIAN_POINT ( 'NONE',  ( 6.491432910188612126, -0.4373703761123280964, 1.975813455233149218 ) ) ;
#32953=CARTESIAN_POINT ( 'NONE',  ( 0.7613493127172387132, 0.9053670157611827252, 1.603083849714491027 ) ) ;
#32955=CARTESIAN_POINT ( 'NONE',  ( 4.592743594998466072, 2.127975290613278503, 0.4296678846467619772 ) ) ;
#32957=CARTESIAN_POINT ( 'NONE',  ( 2.320699612028754188, -0.8158636990020677882, -1.957571985684476212 ) ) ;
#32961=CARTESIAN_POINT ( 'NONE',  ( 1.546242023939500276, 2.058303352229321703, 0.1039559743286587457 ) ) ;
#32965=CARTESIAN_POINT ( 'NONE',  ( -0.02244404828160087226, 0.2256878572204877031, -2.222431841814066278 ) ) ;
#32967=CARTESIAN_POINT ( 'NONE',  ( 5.848291733227988232, 0.9385554955868085081, -1.666026892748099009 ) ) ;
#32969=CARTESIAN_POINT ( 'NONE',  ( 1.687200700035433876, -0.3313812920804170559, -2.237873883018532073 ) ) ;
#32971=CARTESIAN_POINT ( 'NONE',  ( 1.880848235559588799, -1.657448921354220506, -0.7316143304627804600 ) ) ;
#32972=CARTESIAN_POINT ( 'NONE',  ( 2.307709453281155731, -1.106667911223922829, -1.563510803672981231 ) ) ;
#32973=CARTESIAN_POINT ( 'NONE',  ( 2.910663983731573090, 0.6951178490613962868, 1.950330170896700022 ) ) ;
#32975=CARTESIAN_POINT ( 'NONE',  ( 1.164844247922683707, -1.781316891034259164, -0.8450378345598685836 ) ) ;
#32976=CARTESIAN_POINT ( 'NONE',  ( 5.900991307970250510, 1.573582866467116759, -1.111162877451849162 ) ) ;
#32977=CARTESIAN_POINT ( 'NONE',  ( 0.9444605492630732124, 0.9306326543588975264, -2.111904739147156818 ) ) ;
#32980=CARTESIAN_POINT ( 'NONE',  ( 5.529752758335351182, 1.988887524167002985, -0.5466100825702590038 ) ) ;
#32984=CARTESIAN_POINT ( 'NONE',  ( -0.005051300619423290325, -0.4623140147347043483, -2.061856797492032545 ) ) ;
#32987=CARTESIAN_POINT ( 'NONE',  ( 5.395850447034295172, -0.7835752172833524432, 2.014745138864987073 ) ) ;
#32988=CARTESIAN_POINT ( 'NONE',  ( 5.233071810066631357, 1.866936204443689462, 0.7709723521613828234 ) ) ;
#32997=CARTESIAN_POINT ( 'NONE',  ( 3.573454097414618946, 1.463926983822515293, 1.387100322000796027 ) ) ;
#33002=CARTESIAN_POINT ( 'NONE',  ( 5.155217493315787713, -1.824165352752779246, -1.159627250419709155 ) ) ;
#33006=CARTESIAN_POINT ( 'NONE',  ( 5.958611281643053204, -1.915606116362132072, -0.6298603123368745615 ) ) ;
#33008=CARTESIAN_POINT ( 'NONE',  ( 0.9962403866136140262, -0.4152203131645367806, -1.674012925115143213 ) ) ;
#33013=CARTESIAN_POINT ( 'NONE',  ( 6.854772330626868637, -1.445518619047950981, 1.186913843143226233 ) ) ;
#33014=CARTESIAN_POINT ( 'NONE',  ( 0.5924399621960573237, -1.116526876179738226, 1.674895298907061569 ) ) ;
#33015=CARTESIAN_POINT ( 'NONE',  ( 6.539320575229279342, 6.038407674219216759, 2.491644695858772796 ) ) ;
#33017=CARTESIAN_POINT ( 'NONE',  ( 2.907470687441279455, 1.863611109782586484, 1.181582751932461095 ) ) ;
#33021=CARTESIAN_POINT ( 'NONE',  ( 2.367978261241600713, 0.5630001329197281690, -2.044326955284565539 ) ) ;
#33022=CARTESIAN_POINT ( 'NONE',  ( 1.300407892936685794, 1.352140309104767013, -1.496066053310755262 ) ) ;
#33023=CARTESIAN_POINT ( 'NONE',  ( 2.267558116911760902, 0.4800365151868010716, -1.746770699433045415 ) ) ;
#33025=CARTESIAN_POINT ( 'NONE',  ( 6.297764839082774735, -0.7330946318361495351, 2.033732118066629457 ) ) ;
#33029=CARTESIAN_POINT ( 'NONE',  ( 0.8310839537030527691, -1.512174478060366534, -1.176066492228915017 ) ) ;
#33037=CARTESIAN_POINT ( 'NONE',  ( 4.293933718354110418, -0.8299404887524585162, 1.996233173270183903 ) ) ;
#33040=CARTESIAN_POINT ( 'NONE',  ( 2.074623746436579985, 0.9110886696130392481, 1.915067268644244702 ) ) ;
#33041=CARTESIAN_POINT ( 'NONE',  ( 6.598675984083053336, -0.4903212918116289232, -1.758449130657411041 ) ) ;
#33042=CARTESIAN_POINT ( 'NONE',  ( 3.602765292730988556, 1.556248219076960870, -1.210034843411099681 ) ) ;
#33043=CARTESIAN_POINT ( 'NONE',  ( 5.976807594091997800, -1.347613670528555740, 1.357171208065083512 ) ) ;
#33046=ADVANCED_FACE ( 'NONE', ( #44716 ), #22007, .F. ) ;
#33047=CARTESIAN_POINT ( 'NONE',  ( 6.478958751509338754, 1.837172605331442332, 0.7103315708588151534 ) ) ;
#33048=CARTESIAN_POINT ( 'NONE',  ( 1.306472565299764410, 1.712382563992039586, 0.9159111323687963990 ) ) ;
#33053=CARTESIAN_POINT ( 'NONE',  ( 2.343796043118621775, 2.090200655756014658, 0.05028463699395351039 ) ) ;
#33057=CARTESIAN_POINT ( 'NONE',  ( -0.1110810684432986112, 0.002541288824218449188, -1.796853612742685513 ) ) ;
#33059=CARTESIAN_POINT ( 'NONE',  ( 4.951907052881864502, 0.6945806438464277033, -2.094803410698709900 ) ) ;
#33060=CARTESIAN_POINT ( 'NONE',  ( 2.063769564651290356, 0.3772465526380370804, -2.174136642525636098 ) ) ;
#33062=CARTESIAN_POINT ( 'NONE',  ( 0.8559432719405724033, 0.7744784914341161786, -1.748599447100062321 ) ) ;
#33063=DIRECTION ( 'NONE',  ( -0.9999980456341537316, 0.000000000000000000, -0.001977050295949950038 ) ) ;
#33065=CARTESIAN_POINT ( 'NONE',  ( 3.771986465066007099, -2.040223509676724944, 0.3510349978646867264 ) ) ;
#33068=CARTESIAN_POINT ( 'NONE',  ( 2.026462046419864826, 1.244889377058140845, -1.767065586814352773 ) ) ;
#33069=CARTESIAN_POINT ( 'NONE',  ( 4.177398808104064720, 1.432170664236757540, 1.658919600136643524 ) ) ;
#33076=CARTESIAN_POINT ( 'NONE',  ( 5.942016496743827147, -1.492280758002052510, -0.8831153342708076837 ) ) ;
#33080=CARTESIAN_POINT ( 'NONE',  ( 5.172746982222708567, 1.431596967658786745, -1.495705434250683918 ) ) ;
#33081=CARTESIAN_POINT ( 'NONE',  ( 5.659793223991267830, 1.261623160278273481, 1.700126385781860927 ) ) ;
#33084=CARTESIAN_POINT ( 'NONE',  ( 3.801571140118775727, -1.488283618643148287, -1.289908803443328145 ) ) ;
#33085=CARTESIAN_POINT ( 'NONE',  ( 5.560555354427807906, -2.070165260436385601, -0.9845844755148360772 ) ) ;
#33086=CARTESIAN_POINT ( 'NONE',  ( 2.648829494986388422, -1.517897411861212076, 1.014145048410304284 ) ) ;
#33093=CARTESIAN_POINT ( 'NONE',  ( 3.832292871861494810, -1.038684978035837592, -1.724458057284683710 ) ) ;
#33094=CARTESIAN_POINT ( 'NONE',  ( 4.487127722112081329, 0.09209952633786910869, 1.959694304038139379 ) ) ;
#33098=CARTESIAN_POINT ( 'NONE',  ( 0.2223640086436579066, 2.001884549173582606, 0.6031067468692548061 ) ) ;
#33099=CARTESIAN_POINT ( 'NONE',  ( 5.436323762753620947, 1.744125921451036065, 0.2996227856876289564 ) ) ;
#33102=CARTESIAN_POINT ( 'NONE',  ( 1.711130781365449716, -0.2659051965858104660, 2.175189728913041964 ) ) ;
#33103=CARTESIAN_POINT ( 'NONE',  ( 0.9249085282522085949, -1.102964995092512890, -1.346285399390812598 ) ) ;
#33105=CARTESIAN_POINT ( 'NONE',  ( 0.1335669894368864130, 4.084991946249068029, -2.708374394877795410 ) ) ;
#33106=CARTESIAN_POINT ( 'NONE',  ( 1.488428555967473921, -0.2500744359604460954, -1.706524604440103898 ) ) ;
#33107=CARTESIAN_POINT ( 'NONE',  ( 0.6619992422990974568, 1.085049530943157148, 1.904046507712559455 ) ) ;
#33108=CARTESIAN_POINT ( 'NONE',  ( 2.631697372267821855, -2.058793095894187353, 0.7952504953367269813 ) ) ;
#33109=CARTESIAN_POINT ( 'NONE',  ( 1.393694035345336424, -1.963709693186867833, 0.9261614696171887040 ) ) ;
#33111=CARTESIAN_POINT ( 'NONE',  ( 1.938805156862877022, -1.633297379596149845, 1.347353381010838458 ) ) ;
#33113=CARTESIAN_POINT ( 'NONE',  ( 6.000991310419570901, 1.574649422783209740, -1.109465276731670613 ) ) ;
#33115=CARTESIAN_POINT ( 'NONE',  ( 2.402247335887615964, -0.8806970201959153366, -2.116636687559919849 ) ) ;
#33119=CARTESIAN_POINT ( 'NONE',  ( 5.408899451717416262, -0.5379699361975317506, -2.155043070319954790 ) ) ;
#33126=CARTESIAN_POINT ( 'NONE',  ( 2.971327447312217984, -1.987046587055636637, -0.3419355124290662240 ) ) ;
#33128=CARTESIAN_POINT ( 'NONE',  ( 1.094667215044333952, 2.031392189445472063, 0.3564975109212295545 ) ) ;
#33133=CARTESIAN_POINT ( 'NONE',  ( 4.259861650310483583, 1.032037387010206198, 1.933225914978464299 ) ) ;
#33134=CARTESIAN_POINT ( 'NONE',  ( 1.459611520199757706, -1.915600648959712382, -0.6298732728240025169 ) ) ;
#33135=CARTESIAN_POINT ( 'NONE',  ( 1.294213439101927321, 1.504999338701202394, -1.060447551955064016 ) ) ;
#33136=CARTESIAN_POINT ( 'NONE',  ( 4.593604542485023146, -1.840816577468977533, -0.04244875611379012037 ) ) ;
#33138=CARTESIAN_POINT ( 'NONE',  ( 2.343750000000001332, 1.895863743164134307, 0.7852924748298687474 ) ) ;
#33139=CARTESIAN_POINT ( 'NONE',  ( 4.981388616008130654, 1.702979688329594676, -0.6582044668519275721 ) ) ;
#33140=CARTESIAN_POINT ( 'NONE',  ( 5.590470263882489910, -0.4872053753022275169, 1.956560708789633285 ) ) ;
#33142=CARTESIAN_POINT ( 'NONE',  ( 4.856464543430921488, 0.8614301073998543723, 2.092300974686135184 ) ) ;
#33144=CARTESIAN_POINT ( 'NONE',  ( 0.5925747745999773164, -2.090437052192719136, -0.2555399532009738350 ) ) ;
#33146=CARTESIAN_POINT ( 'NONE',  ( 4.369627354678314646, -0.3570511267821044332, 2.039192500141631115 ) ) ;
#33155=CARTESIAN_POINT ( 'NONE',  ( 0.3520121086563637314, -1.504009422257305495, -1.495223887398588358 ) ) ;
#33156=CARTESIAN_POINT ( 'NONE',  ( 2.145073868429191677, 2.156049884074415779, 0.5345358195362903686 ) ) ;
#33160=CARTESIAN_POINT ( 'NONE',  ( 2.928120951529111338, 1.047165451586975049, 1.658829547137883775 ) ) ;
#33166=CARTESIAN_POINT ( 'NONE',  ( 2.109781586379317897, 1.642293606977158538, 1.341614810521203349 ) ) ;
#33168=CARTESIAN_POINT ( 'NONE',  ( 4.439869198996494681, 1.279870211898268550, 1.486999339763886097 ) ) ;
#33169=CARTESIAN_POINT ( 'NONE',  ( 3.643588467267334874, -1.635511012911139650, -1.413612897787956513 ) ) ;
#33170=CARTESIAN_POINT ( 'NONE',  ( 2.806014743833366687, 1.331929863061011243, -1.271513748034671432 ) ) ;
#33174=CARTESIAN_POINT ( 'NONE',  ( 4.716618446111438878, -0.08105245650613655817, 1.738572149171065062 ) ) ;
#33179=CARTESIAN_POINT ( 'NONE',  ( 1.815512348505427642, -0.2646426633909418347, 2.145385951886819242 ) ) ;
#33180=CARTESIAN_POINT ( 'NONE',  ( 4.235703761680151835, -1.880146911114020325, -0.7282675588539261335 ) ) ;
#33182=CARTESIAN_POINT ( 'NONE',  ( 1.358524781292804517, 0.8764843271744371389, 1.976213614152767750 ) ) ;
#33183=CARTESIAN_POINT ( 'NONE',  ( 2.407442502341358814, -0.4355224260998523111, 1.922489325443673236 ) ) ;
#33185=CARTESIAN_POINT ( 'NONE',  ( 3.649888709942475273, 0.7017510601828327310, 1.811005675494174350 ) ) ;
#33193=CARTESIAN_POINT ( 'NONE',  ( 1.255210933454937283, -1.738917431694649407, 1.358592805172780693 ) ) ;
#33196=CARTESIAN_POINT ( 'NONE',  ( 5.102378460580520247, 1.956245014681293970, 0.1482201060269832671 ) ) ;
#33198=CARTESIAN_POINT ( 'NONE',  ( 3.309862381128574338, -1.264700674563856264, -1.697971918580774675 ) ) ;
#33201=CARTESIAN_POINT ( 'NONE',  ( 4.066218318298571610, -1.718653781379267276, -0.6607852518168353395 ) ) ;
#33206=CARTESIAN_POINT ( 'NONE',  ( 5.537388447972660721, -0.05000006065614125139, 2.120159173171487055 ) ) ;
#33208=CARTESIAN_POINT ( 'NONE',  ( 5.536423053809180317, 2.029556968340691547, 0.3564751269278207957 ) ) ;
#33210=CARTESIAN_POINT ( 'NONE',  ( 0.7833917827068856976, -1.768883884249613736, 0.5786898513908571573 ) ) ;
#33211=CARTESIAN_POINT ( 'NONE',  ( 2.436835438956724165, -1.365703447793526371, -1.235134912642745775 ) ) ;
#33217=CARTESIAN_POINT ( 'NONE',  ( 2.895379187063460424, 1.892502543702856865, -1.135010264495312837 ) ) ;
#33218=CARTESIAN_POINT ( 'NONE',  ( 5.272873185648853323, -2.127775705341850898, -0.7691360568998426572 ) ) ;
#33220=CARTESIAN_POINT ( 'NONE',  ( 5.062699594374425516, 0.5334270428436416189, 1.731249764757249343 ) ) ;
#33221=CARTESIAN_POINT ( 'NONE',  ( 5.102711585370895975, 1.772601733252886280, 0.7270577078305997532 ) ) ;
#33223=CARTESIAN_POINT ( 'NONE',  ( 4.944154083221365070, 1.865701114312174225, 0.1370711555178441010 ) ) ;
#33224=CARTESIAN_POINT ( 'NONE',  ( 4.949569884170424316, 1.378596123743974555, 1.250361270004763714 ) ) ;
#33227=CARTESIAN_POINT ( 'NONE',  ( 6.666889860676148416, -1.620333765578816587, -0.7124167289687727278 ) ) ;
#33228=CARTESIAN_POINT ( 'NONE',  ( 0.2687680251878405424, -0.2516378192510167477, -2.000730910237565663 ) ) ;
#33230=CARTESIAN_POINT ( 'NONE',  ( 3.018300108557407935, -1.038308444602775271, -1.832253800920932596 ) ) ;
#33233=CARTESIAN_POINT ( 'NONE',  ( 0.07479286986305370977, 0.004866263145587856019, -1.855573292446038414 ) ) ;
#33235=CARTESIAN_POINT ( 'NONE',  ( 1.564719475598770337, 0.6377593443319184985, 1.916497437154760508 ) ) ;
#33239=CARTESIAN_POINT ( 'NONE',  ( 3.040462492942562545, 2.144887288335277198, 0.2678724578094940356 ) ) ;
#33240=CARTESIAN_POINT ( 'NONE',  ( 6.610000000000028741, 4.695285100415147461, 2.562642482393460597 ) ) ;
#33247=CARTESIAN_POINT ( 'NONE',  ( 0.6619992422990974568, 1.085049530943157148, 1.904046507712559455 ) ) ;
#33249=CARTESIAN_POINT ( 'NONE',  ( 1.165308694782108301, -2.046298710749935079, -0.9655196508330918803 ) ) ;
#33256=CARTESIAN_POINT ( 'NONE',  ( 3.514700139928600198, 1.598748483301600354, 0.7592613872578843903 ) ) ;
#33258=CARTESIAN_POINT ( 'NONE',  ( 6.018643902988223715, 1.486383190695803158, -1.631276885294789203 ) ) ;
#33262=CARTESIAN_POINT ( 'NONE',  ( 5.571888728144736902, -0.9040954357531080232, 1.802425742427179012 ) ) ;
#33264=CARTESIAN_POINT ( 'NONE',  ( 2.658895327995167701, -1.626580691111864985, -0.9237732865615968514 ) ) ;
#33265=CARTESIAN_POINT ( 'NONE',  ( 3.555589372526322567, 1.629040189086952140, 1.277421477176057252 ) ) ;
#33267=CARTESIAN_POINT ( 'NONE',  ( 2.390748813209525814, -1.831196095803063528, -0.5514187292172747501 ) ) ;
#33272=CARTESIAN_POINT ( 'NONE',  ( 1.125099709691119276, 1.687896996356451629, 0.8989547360247207575 ) ) ;
#33274=CARTESIAN_POINT ( 'NONE',  ( 2.576550507925364109, 1.283677811227203147, -1.483670167215108693 ) ) ;
#33277=CARTESIAN_POINT ( 'NONE',  ( 5.449516625918088053, -1.916229881892789866, 0.9086369058012438993 ) ) ;
#33279=CARTESIAN_POINT ( 'NONE',  ( 6.450460791689297757, 0.6159929566152704261, 1.872736359496610659 ) ) ;
#33281=CARTESIAN_POINT ( 'NONE',  ( 2.127199591969671122, 1.800101769773830185, 0.9015413830680671925 ) ) ;
#33283=CARTESIAN_POINT ( 'NONE',  ( 1.511481539699152776, -1.992283995360244253, 0.7168839309619617906 ) ) ;
#33286=CARTESIAN_POINT ( 'NONE',  ( 3.174344110969638866, -1.018096006688212096, -1.802650257252853772 ) ) ;
#33288=CARTESIAN_POINT ( 'NONE',  ( 6.210894578592706772, -0.2570060295814159401, 2.074700711848826096 ) ) ;
#33290=CARTESIAN_POINT ( 'NONE',  ( 4.172732250082421324, -1.703408510751417193, -0.6570589383413026896 ) ) ;
#33295=CARTESIAN_POINT ( 'NONE',  ( 4.946401613871812764, 2.200551846729232430, 0.1665617540023768828 ) ) ;
#33298=CARTESIAN_POINT ( 'NONE',  ( 3.879479457080482696, 0.2311173251203814394, -1.898182577502210977 ) ) ;
#33303=CARTESIAN_POINT ( 'NONE',  ( 6.567925981381852907, -1.350348970527824211, 1.726830949945204363 ) ) ;
#33305=CARTESIAN_POINT ( 'NONE',  ( 0.8020088176248600931, 1.394402496181508466, -1.202495849378336423 ) ) ;
#33308=CARTESIAN_POINT ( 'NONE',  ( 5.290257391050456448, -1.856285702826396156, -0.2301478561287788605 ) ) ;
#33317=CARTESIAN_POINT ( 'NONE',  ( 1.112081256596690437, 1.967444819121874744, -0.09107992038001262725 ) ) ;
#33318=CARTESIAN_POINT ( 'NONE',  ( 1.845327587665198443, 0.3419125196015109225, -1.987051676161588620 ) ) ;
#33321=CARTESIAN_POINT ( 'NONE',  ( 6.727182134110200273, 0.5640974741700152117, 2.241195997201197443 ) ) ;
#33322=CARTESIAN_POINT ( 'NONE',  ( 2.818527994553555516, 2.063739945100159900, 0.7375456357434084786 ) ) ;
#33323=CARTESIAN_POINT ( 'NONE',  ( 5.936143289257818978, 0.8957264799932495025, -1.590785280889392528 ) ) ;
#33331=CARTESIAN_POINT ( 'NONE',  ( 4.774869596704574448, 1.716175909155163382, -0.6674964387535023969 ) ) ;
#33332=CARTESIAN_POINT ( 'NONE',  ( 0.9439945835589347300, -1.278642754803262171, -1.554848376591860815 ) ) ;
#33333=CARTESIAN_POINT ( 'NONE',  ( 2.952824900933643804, 1.623659768481898302, 1.626969957801235989 ) ) ;
#33335=CARTESIAN_POINT ( 'NONE',  ( 1.059155247252058896, 1.517088508067988117, 1.077460967357747990 ) ) ;
#33339=CARTESIAN_POINT ( 'NONE',  ( 4.605663860560767375, 1.420894170025093439, 1.280184534114735095 ) ) ;
#33342=CARTESIAN_POINT ( 'NONE',  ( 3.228152448572230160, 2.040302950407224536, 0.4557642060307572907 ) ) ;
#33343=CARTESIAN_POINT ( 'NONE',  ( 2.307302758404996545, -0.4121581357655336175, 1.824517092411604979 ) ) ;
#33346=CARTESIAN_POINT ( 'NONE',  ( 6.128435733830499998, 0.1874100934057248424, 1.831705376836203936 ) ) ;
#33350=CARTESIAN_POINT ( 'NONE',  ( 4.705503516419368815, -0.4560151319670002756, 1.663429522189649790 ) ) ;
#33352=CARTESIAN_POINT ( 'NONE',  ( 0.5626190647941519130, -0.9651924803987484980, 1.440457774218842690 ) ) ;
#33356=CARTESIAN_POINT ( 'NONE',  ( 4.557605255626766549, 1.740051450181074877, 1.298158460866901454 ) ) ;
#33357=CARTESIAN_POINT ( 'NONE',  ( 3.791466046568803705, 1.323482414808102137, 1.257835202898072380 ) ) ;
#33358=CARTESIAN_POINT ( 'NONE',  ( 1.498799732657706718, 0.3773721054241683248, 1.924948185394937283 ) ) ;
#33359=CARTESIAN_POINT ( 'NONE',  ( 5.823477710672365859, -1.535350753823118586, -1.458276433397849514 ) ) ;
#33360=CARTESIAN_POINT ( 'NONE',  ( 6.146038201015474378, 0.7148980135479511278, 2.178090959246486324 ) ) ;
#33364=CARTESIAN_POINT ( 'NONE',  ( 1.717596852896427606, 1.764750374324057347, 1.175337852406685757 ) ) ;
#33368=CARTESIAN_POINT ( 'NONE',  ( 6.280164127638760085, -1.199209930833704085, -1.809645864181265384 ) ) ;
#33369=CARTESIAN_POINT ( 'NONE',  ( 6.883263157960362477, -0.004191378316371896506, 2.053658919477070910 ) ) ;
#33371=CARTESIAN_POINT ( 'NONE',  ( 1.840792944257110042, 1.275724102719773434, -1.818268329069183897 ) ) ;
#33373=CARTESIAN_POINT ( 'NONE',  ( 6.258435431136967431, 1.928752767684217106, -0.5880170417187426946 ) ) ;
#33375=CARTESIAN_POINT ( 'NONE',  ( 4.293840196874755044, -1.418639180022958080, -1.497458912744116022 ) ) ;
#33377=CARTESIAN_POINT ( 'NONE',  ( -0.2409995289980003397, 4.087843961663322645, -2.555282842491034323 ) ) ;
#33381=CARTESIAN_POINT ( 'NONE',  ( 0.2168896333464042925, -0.1002974801882359490, 2.088354908755992945 ) ) ;
#33382=CARTESIAN_POINT ( 'NONE',  ( 4.599059095968327071, -0.4863373063577690059, 1.775805238918099382 ) ) ;
#33387=CARTESIAN_POINT ( 'NONE',  ( 1.852176121455822777, 0.5370312411601232405, 1.639109186831126053 ) ) ;
#33389=CARTESIAN_POINT ( 'NONE',  ( 1.618275512070939115, 0.2312369868452644750, 2.287056861988717493 ) ) ;
#33391=CARTESIAN_POINT ( 'NONE',  ( 1.458695031449417590, 0.9167444482420561425, 2.068505399879524642 ) ) ;
#33392=CARTESIAN_POINT ( 'NONE',  ( 4.617860632714274161, -2.065554989951523535, 0.4101935312739966588 ) ) ;
#33394=CARTESIAN_POINT ( 'NONE',  ( 2.776313302798124383, -1.692206278411222176, -0.5179841425143881795 ) ) ;
#33401=CARTESIAN_POINT ( 'NONE',  ( 4.904621534589208132, -2.204716393758818782, -0.2710871420372409912 ) ) ;
#33402=CARTESIAN_POINT ( 'NONE',  ( 3.750093249908572623, 0.7883579158753216687, 2.044908353623323016 ) ) ;
#33405=CARTESIAN_POINT ( 'NONE',  ( 5.619825546450978315, -0.5151785252428126016, 2.056841324599982368 ) ) ;
#33408=CARTESIAN_POINT ( 'NONE',  ( 6.609999999999999432, 2.404169510734831761, 2.660384318335922149 ) ) ;
#33410=CARTESIAN_POINT ( 'NONE',  ( 5.308877466510794285, -0.5174029350529658622, -2.056363676157816123 ) ) ;
#33414=CARTESIAN_POINT ( 'NONE',  ( 6.579002408576895000, -0.1006694238701970334, -2.159482418181729813 ) ) ;
#33416=CARTESIAN_POINT ( 'NONE',  ( 6.058133912487986272, -1.297239342979487509, 1.306937132449899508 ) ) ;
#33420=CARTESIAN_POINT ( 'NONE',  ( 1.434671803396998291, -1.260233744827907953, -1.200652698350104686 ) ) ;
#33426=CARTESIAN_POINT ( 'NONE',  ( 5.102478102407745908, -0.7247817745383768884, -2.036717088958202471 ) ) ;
#33429=CARTESIAN_POINT ( 'NONE',  ( 4.540002997438313592, 0.9271085556134452954, -1.952944755896801610 ) ) ;
#33433=CARTESIAN_POINT ( 'NONE',  ( 5.483651708025924165, 1.321867191758316462, 1.462689542499737039 ) ) ;
#33434=CARTESIAN_POINT ( 'NONE',  ( 5.413366682498521598, 0.5056653987138818307, 1.658472451074376242 ) ) ;
#33436=CARTESIAN_POINT ( 'NONE',  ( 1.663894474538109236, 1.130263417742288112, 1.877492182091732076 ) ) ;
#33437=CARTESIAN_POINT ( 'NONE',  ( 1.993646994336109257, 2.007229749184535450, -1.138263614794749801 ) ) ;
#33438=CARTESIAN_POINT ( 'NONE',  ( 4.516905262009872857, 1.882569317753344240, 0.8387543118332175807 ) ) ;
#33439=CARTESIAN_POINT ( 'NONE',  ( 6.614805133705309537, -0.1285734799129842065, 1.912263277720785970 ) ) ;
#33443=CARTESIAN_POINT ( 'NONE',  ( 4.394861267144759331, -2.057662932662501110, -0.5123870273424437904 ) ) ;
#33444=CARTESIAN_POINT ( 'NONE',  ( 1.108046318188542489, -0.04667474159409169127, 2.016033875899234662 ) ) ;
#33446=CARTESIAN_POINT ( 'NONE',  ( 4.717920652503574175, -2.164970738276258189, 0.4266498443898231185 ) ) ;
#33455=CARTESIAN_POINT ( 'NONE',  ( 3.432544477427549534, 2.010279954523132240, 0.4531449079418439774 ) ) ;
#33459=CARTESIAN_POINT ( 'NONE',  ( 3.018227828326583762, -2.017275923677069205, 0.1012127129823153504 ) ) ;
#33462=CARTESIAN_POINT ( 'NONE',  ( 1.797801859905317823, -0.6954313725856995365, 1.940136720205553278 ) ) ;
#33465=CARTESIAN_POINT ( 'NONE',  ( -0.2408018239684642792, 0.2331886253038339407, -2.134526469895109635 ) ) ;
#33467=CARTESIAN_POINT ( 'NONE',  ( 1.798526679444776954, 1.530131497970032450, 1.023642133485637595 ) ) ;
#33469=CARTESIAN_POINT ( 'NONE',  ( 0.2062968637084483525, -0.6088960595307371104, 2.225859948526871079 ) ) ;
#33471=CARTESIAN_POINT ( 'NONE',  ( 1.968271169257681752, 1.109365460190291586, 1.855047589327807778 ) ) ;
#33473=CARTESIAN_POINT ( 'NONE',  ( 2.360564879530482330, -1.931125380751706810, -0.5807522007576990664 ) ) ;
#33474=CARTESIAN_POINT ( 'NONE',  ( 2.196985159075715011, -1.500492831465898513, -1.741107174271120384 ) ) ;
#33477=CARTESIAN_POINT ( 'NONE',  ( 0.1099206271272800961, -0.7955684105149689600, -1.691499381818922343 ) ) ;
#33479=CARTESIAN_POINT ( 'NONE',  ( 4.276219423538512032, -1.135946514926335915, 1.611120745738093385 ) ) ;
#33480=CARTESIAN_POINT ( 'NONE',  ( 3.098842478760281516, 1.825076540557273974, 0.8578426345753201732 ) ) ;
#33485=CARTESIAN_POINT ( 'NONE',  ( 6.305314546112477103, 1.749969596565099650, 1.171488565500600654 ) ) ;
#33486=CARTESIAN_POINT ( 'NONE',  ( 4.809070886388271404, -1.664838503569150419, 1.230558894880565246 ) ) ;
#33490=CARTESIAN_POINT ( 'NONE',  ( 4.939715878566554252, -1.916525930768823383, 0.6376727893300809802 ) ) ;
#33492=CARTESIAN_POINT ( 'NONE',  ( 3.580997583313150212, -2.223846063185720645, -0.6162045312432282707 ) ) ;
#33493=CARTESIAN_POINT ( 'NONE',  ( 1.094667215044333952, 2.031392189445472063, 0.3564975109212295545 ) ) ;
#33500=CARTESIAN_POINT ( 'NONE',  ( 3.578747896202236323, 1.379726198893852729, -1.676393335895840497 ) ) ;
#33504=CARTESIAN_POINT ( 'NONE',  ( 2.770863647982471534, 1.747605724785822767, -0.5798694457997202178 ) ) ;
#33506=CARTESIAN_POINT ( 'NONE',  ( 4.546525781634036534, -1.759932548463913671, 1.305750774140898685 ) ) ;
#33508=CARTESIAN_POINT ( 'NONE',  ( 5.049841537476964959, 0.7145653451936549994, -2.146778123354900814 ) ) ;
#33513=CARTESIAN_POINT ( 'NONE',  ( 6.257089712715798058, -1.519072588978742200, -0.9077291607378096261 ) ) ;
#33515=CARTESIAN_POINT ( 'NONE',  ( 4.477201648280199286, -1.799136850145161892, -0.9032412251695760563 ) ) ;
#33517=CARTESIAN_POINT ( 'NONE',  ( 2.784315802839703036, -1.083654668052931536, 1.805616322045165312 ) ) ;
#33518=CARTESIAN_POINT ( 'NONE',  ( 0.5267775621587212909, -1.642505510697172655, 0.9855279480080190169 ) ) ;
#33520=CARTESIAN_POINT ( 'NONE',  ( 2.207411625193840266, -1.579985490969371575, -1.175680343436244391 ) ) ;
#33521=CARTESIAN_POINT ( 'NONE',  ( 0.7076149179639171782, -1.862046558926268913, 0.1791945732521060819 ) ) ;
#33522=CARTESIAN_POINT ( 'NONE',  ( 1.012071980069819910, 1.959787197952606252, -0.09269708818125664551 ) ) ;
#33523=CARTESIAN_POINT ( 'NONE',  ( 0.05278957052760185897, 0.3289079202175131389, 1.883742972368242174 ) ) ;
#33528=CARTESIAN_POINT ( 'NONE',  ( 6.403191318657627029, 1.556466930477506505, 1.037356966126230517 ) ) ;
#33530=CARTESIAN_POINT ( 'NONE',  ( 6.930528400284448054, -1.278709912597691511, 1.628784411136071197 ) ) ;
#33532=CARTESIAN_POINT ( 'NONE',  ( 1.328672132201724532, -1.314895749051579132, 1.599177317581280455 ) ) ;
#33537=CARTESIAN_POINT ( 'NONE',  ( 5.918629486560170960, -0.7630358368452618834, -1.978611909900826582 ) ) ;
#33541=CARTESIAN_POINT ( 'NONE',  ( 6.408651779211167465, 0.6141799454031526828, 1.863335524608072502 ) ) ;
#33543=CARTESIAN_POINT ( 'NONE',  ( 2.829453700430568652, -1.392333688140505510, 1.458332250898628057 ) ) ;
#33544=CARTESIAN_POINT ( 'NONE',  ( 3.450306162294475065, -1.282734793626014280, 1.423081227541162841 ) ) ;
#33546=CARTESIAN_POINT ( 'NONE',  ( 1.189316404147572337, 1.662717542896676504, 1.427817766309902314 ) ) ;
#33547=CARTESIAN_POINT ( 'NONE',  ( 0.2335667940003048615, 5.721530573166598188, -2.747389403444942868 ) ) ;
#33548=CARTESIAN_POINT ( 'NONE',  ( 3.092876253348992410, 1.606159189733218140, -0.9584765265276545820 ) ) ;
#33552=CARTESIAN_POINT ( 'NONE',  ( 5.325823331840044084, 0.8572517883133590200, -1.936080889991494747 ) ) ;
#33555=CARTESIAN_POINT ( 'NONE',  ( 6.777786256569462431, -2.009253640576996514, 0.4989836931604470505 ) ) ;
#33556=CARTESIAN_POINT ( 'NONE',  ( 2.612926333352751929, -0.2020284733853395243, 2.080942194061443651 ) ) ;
#33558=CARTESIAN_POINT ( 'NONE',  ( 1.131409910074301806, -1.089654060068695252, -1.336973495911207843 ) ) ;
#33567=CARTESIAN_POINT ( 'NONE',  ( 0.9260600326868747567, -0.8135480099433598511, -1.618595788997332363 ) ) ;
#33572=CARTESIAN_POINT ( 'NONE',  ( 6.539320575229274901, 7.053161517996441532, 2.494893549996656912 ) ) ;
#33576=CARTESIAN_POINT ( 'NONE',  ( 2.629178708315405455, 0.09452080204645990635, -1.858793618116144186 ) ) ;
#33577=CARTESIAN_POINT ( 'NONE',  ( 0.6146668332816725977, 0.1418531279011990553, 1.910429497406636479 ) ) ;
#33578=CARTESIAN_POINT ( 'NONE',  ( 6.352563997503644977, 0.6048113787208497794, 1.829064924511276002 ) ) ;
#33584=CARTESIAN_POINT ( 'NONE',  ( 5.137539950512164388, 1.839066438578255136, -0.7051811603524612559 ) ) ;
#33586=CARTESIAN_POINT ( 'NONE',  ( 1.225412164737609055, 1.871785320780447792, 0.9964087003688710809 ) ) ;
#33590=CARTESIAN_POINT ( 'NONE',  ( 5.947271710577298087, 0.6394180277670692414, -2.096098967930816848 ) ) ;
#33592=CARTESIAN_POINT ( 'NONE',  ( 4.014609399936463596, 1.362939121162042078, -1.361637018764590534 ) ) ;
#33595=CARTESIAN_POINT ( 'NONE',  ( 1.102499568101540817, -2.207063161980229005, 0.003256074490760872773 ) ) ;
#33601=CARTESIAN_POINT ( 'NONE',  ( 5.893399327195629311, -1.782088370946652622, 0.8386133760364660183 ) ) ;
#33602=CARTESIAN_POINT ( 'NONE',  ( 1.768985407559420020, 1.857901784229658793, -0.5654475766003872472 ) ) ;
#33604=CARTESIAN_POINT ( 'NONE',  ( 0.2278875137335881207, -1.799627942332830965, -0.9090566646320766830 ) ) ;
#33606=CARTESIAN_POINT ( 'NONE',  ( 4.891365455385704664, -1.702569429429393599, 0.7516348641289184451 ) ) ;
#33612=CARTESIAN_POINT ( 'NONE',  ( 0.5389544483674936215, -1.876709678404146153, 1.131566444868239874 ) ) ;
#33617=CARTESIAN_POINT ( 'NONE',  ( 1.365546509989667534, 1.798985258052044900, -0.3101867277976525505 ) ) ;
#33619=CARTESIAN_POINT ( 'NONE',  ( 3.269848819717678712, 1.566352396371019973, -0.7445194440909275180 ) ) ;
#33621=CARTESIAN_POINT ( 'NONE',  ( 6.609000000000036401, 1.265604115953523845, 2.115306440354140172 ) ) ;
#33623=CARTESIAN_POINT ( 'NONE',  ( 6.568987803155795113, -1.671525225137669102, -0.7347104647430282576 ) ) ;
#33624=CARTESIAN_POINT ( 'NONE',  ( 4.328923052438288899, -1.828919189252835142, -0.7100325158947775606 ) ) ;
#33627=CARTESIAN_POINT ( 'NONE',  ( 4.617906949270495609, -0.5647423089508787353, 2.043846993246847710 ) ) ;
#33629=CARTESIAN_POINT ( 'NONE',  ( 6.609000000000020414, 4.695354556932705314, 2.562644781943985706 ) ) ;
#33630=CARTESIAN_POINT ( 'NONE',  ( 2.571216573722459486, 1.847313327574741315, 0.9347662400437593000 ) ) ;
#33632=ORIENTED_EDGE ( 'NONE', *, *, #25909, .F. ) ;
#33633=CARTESIAN_POINT ( 'NONE',  ( 2.444286548701213757, -2.001697433659669567, -1.129998469374261072 ) ) ;
#33640=CARTESIAN_POINT ( 'NONE',  ( 4.113462262696740979, 1.539102623358613586, 1.134910093507961237 ) ) ;
#33642=CARTESIAN_POINT ( 'NONE',  ( 5.596639136713698726, -0.4230586844520961010, -1.671955901692462998 ) ) ;
#33643=CARTESIAN_POINT ( 'NONE',  ( 3.749232653202066778, 0.2420323627391370025, -2.001857840249580800 ) ) ;
#33644=CARTESIAN_POINT ( 'NONE',  ( 5.291695567192507887, 1.742433043099327561, -1.499359156687163575 ) ) ;
#33646=CARTESIAN_POINT ( 'NONE',  ( 0.9794701899953797142, -0.05759512415488829418, -2.206297691287119722 ) ) ;
#33648=CARTESIAN_POINT ( 'NONE',  ( 5.465970981792784400, 0.8728298736929670509, 1.539401198699318352 ) ) ;
#33650=CARTESIAN_POINT ( 'NONE',  ( 2.010137459244505820, -1.083026110817113086, -2.020279618534262855 ) ) ;
#33651=CARTESIAN_POINT ( 'NONE',  ( 6.580030785786400216, -1.806642183828395920, -0.3538341520857649081 ) ) ;
#33656=CARTESIAN_POINT ( 'NONE',  ( 0.6081839208269465002, 0.6806018353129331677, -2.061787349250172596 ) ) ;
#33657=CARTESIAN_POINT ( 'NONE',  ( 2.571500236035813902, 1.429449181443824823, 1.422607194786096541 ) ) ;
#33660=CARTESIAN_POINT ( 'NONE',  ( 5.180268977979770817, -1.068588414017849653, 1.602784418908353548 ) ) ;
#33662=CARTESIAN_POINT ( 'NONE',  ( 2.812952309885875746, -0.6487812942810657901, -2.124531788647378239 ) ) ;
#33669=CARTESIAN_POINT ( 'NONE',  ( 4.054071295385909934, -1.286197829845928675, 1.172710138673456415 ) ) ;
#33671=CARTESIAN_POINT ( 'NONE',  ( 3.350005920730843911, -0.7974703105717847462, 1.792663495558038056 ) ) ;
#33677=CARTESIAN_POINT ( 'NONE',  ( 1.029816311724339961, 1.988459969548944439, -0.5481627708354539497 ) ) ;
#33680=CARTESIAN_POINT ( 'NONE',  ( 0.6732104281652334654, -2.131434628316424273, -0.7592435237872022791 ) ) ;
#33681=ORIENTED_EDGE ( 'NONE', *, *, #38690, .F. ) ;
#33683=CARTESIAN_POINT ( 'NONE',  ( 2.512791842090915218, 1.668957736969980621, 0.8448945032545759348 ) ) ;
#33684=CARTESIAN_POINT ( 'NONE',  ( 1.037308000539336694, -1.367553460919969543, 1.066146521862390673 ) ) ;
#33685=CARTESIAN_POINT ( 'NONE',  ( 5.161759341795384870, 1.079763445194487970, 1.907048802792680631 ) ) ;
#33686=CARTESIAN_POINT ( 'NONE',  ( 6.317414003067519879, -0.2912348092876380079, 2.289091032272353221 ) ) ;
#33687=CARTESIAN_POINT ( 'NONE',  ( 1.217730312517154800, -2.010830008989676898, 0.4507304159913956831 ) ) ;
#33688=CARTESIAN_POINT ( 'NONE',  ( 2.906119529042447969, 1.406244311732379293, -1.339499261486200465 ) ) ;
#33692=CARTESIAN_POINT ( 'NONE',  ( 6.063714619507535097, 1.842885348237649490, -0.3194776537047139264 ) ) ;
#33693=CARTESIAN_POINT ( 'NONE',  ( 1.218750000000000888, -0.7852924748299231483, 1.895863743164115656 ) ) ;
#33695=CARTESIAN_POINT ( 'NONE',  ( 6.468125021464292246, 1.674632898861495134, 1.122323893169609565 ) ) ;
#33697=CARTESIAN_POINT ( 'NONE',  ( 4.588517629802620235, -0.5350896943857390564, 1.944070981013111155 ) ) ;
#33701=CARTESIAN_POINT ( 'NONE',  ( 2.648829494986388422, -1.517897411861212076, 1.014145048410304284 ) ) ;
#33709=CARTESIAN_POINT ( 'NONE',  ( -0.2106725631050176961, -0.004273297132588448587, -2.003483006309704439 ) ) ;
#33710=CARTESIAN_POINT ( 'NONE',  ( 0.5574859923395922845, -1.816599148028580579, 1.093606109393664427 ) ) ;
#33714=CARTESIAN_POINT ( 'NONE',  ( 6.420785563114608685, 1.921975812937461781, 0.7442927364858693551 ) ) ;
#33715=CARTESIAN_POINT ( 'NONE',  ( 5.309220276109914316, 1.198862193007979471, -1.621181151826488254 ) ) ;
#33724=CARTESIAN_POINT ( 'NONE',  ( 5.466172646012215530, 1.646588110366095314, 1.163089216160061001 ) ) ;
#33725=CARTESIAN_POINT ( 'NONE',  ( 5.208873985248447802, -0.2666229848188906848, 1.821608446441948193 ) ) ;
#33726=CARTESIAN_POINT ( 'NONE',  ( 0.07661050522435489119, 2.064768137775649048, -2.128874817076317871 ) ) ;
#33727=CARTESIAN_POINT ( 'NONE',  ( 3.651255599878608926, -1.887205614810626209, 1.327874790813722949 ) ) ;
#33729=CARTESIAN_POINT ( 'NONE',  ( 4.903692054014650026, -0.5817465652163296141, 2.081756923971528117 ) ) ;
#33730=CARTESIAN_POINT ( 'NONE',  ( 3.362517798112668821, -1.944730434982215650, -0.5331690889110105580 ) ) ;
#33732=CARTESIAN_POINT ( 'NONE',  ( 0.7845916355662507780, 1.712027273464492350, -0.9168598982515554496 ) ) ;
#33736=CARTESIAN_POINT ( 'NONE',  ( 3.696050037196423332, -1.868490534004090931, -0.09263902202472777681 ) ) ;
#33737=CARTESIAN_POINT ( 'NONE',  ( 0.8965662283535699162, -1.866366896104875162, -0.4163465257057268332 ) ) ;
#33741=CARTESIAN_POINT ( 'NONE',  ( 3.282038605231399231, 1.400092287458438722, 1.705885466304429166 ) ) ;
#33747=CARTESIAN_POINT ( 'NONE',  ( 0.6320224300673723539, 1.017306711037075262, -1.688479424803266404 ) ) ;
#33749=CARTESIAN_POINT ( 'NONE',  ( 0.1656154469977044186, -2.063490973871735967, -1.033197247175041467 ) ) ;
#33750=CARTESIAN_POINT ( 'NONE',  ( 1.627322669196319849, 0.1476378700930695564, -1.956383933670035713 ) ) ;
#33751=CARTESIAN_POINT ( 'NONE',  ( 4.592669665391247769, 2.021776019120101520, 0.4074096221951555297 ) ) ;
#33759=CARTESIAN_POINT ( 'NONE',  ( 1.200314488179974326, 0.8819602860624680130, -1.984045050410755406 ) ) ;
#33761=CARTESIAN_POINT ( 'NONE',  ( 6.146043377905669125, 0.5841948715668408010, 1.746183665442810007 ) ) ;
#33764=CARTESIAN_POINT ( 'NONE',  ( 1.879943753831798015, -1.004885234286160722, 1.577526331995420472 ) ) ;
#33765=CARTESIAN_POINT ( 'NONE',  ( 5.378265110509337532, -1.205767192478784500, 1.793856531414832256 ) ) ;
#33767=CARTESIAN_POINT ( 'NONE',  ( -0.02264175331115856477, 0.2280268304470518537, -2.122276614016995744 ) ) ;
#33770=CARTESIAN_POINT ( 'NONE',  ( 0.9965660710522584731, -1.865815080690262917, -0.4182784585613218420 ) ) ;
#33771=CARTESIAN_POINT ( 'NONE',  ( 2.518099203671141595, 1.158133694123581359, -1.338384833553945663 ) ) ;
#33773=CARTESIAN_POINT ( 'NONE',  ( 0.6274217273865910771, -0.2802014979648696502, 1.891502685196179812 ) ) ;
#33775=CARTESIAN_POINT ( 'NONE',  ( 5.941025102908992217, -1.645668167864361431, -0.9802026474072849105 ) ) ;
#33776=CARTESIAN_POINT ( 'NONE',  ( 6.795365950078042339, -1.759944107108902367, 0.8842400836535941888 ) ) ;
#33777=CARTESIAN_POINT ( 'NONE',  ( 0.8441712343106638761, -1.349783269286155774, -1.635521010841307410 ) ) ;
#33779=CARTESIAN_POINT ( 'NONE',  ( 3.854256360616271415, 0.6726810918341770140, 1.745705178215435582 ) ) ;
#33780=CARTESIAN_POINT ( 'NONE',  ( 0.6623940301842005107, -1.324425631624454036, 1.256838194884236204 ) ) ;
#33782=CARTESIAN_POINT ( 'NONE',  ( 3.475398437264758833, 0.05438942809191970457, -2.206374867412825402 ) ) ;
#33785=CARTESIAN_POINT ( 'NONE',  ( 1.486864572717770283, 1.987365476997263292, 0.5519934122387574194 ) ) ;
#33790=CARTESIAN_POINT ( 'NONE',  ( 6.433860211133586304, -1.853236450885078712, 0.4715264990977630077 ) ) ;
#33793=CARTESIAN_POINT ( 'NONE',  ( 4.404779037558821386, 0.5491149005726041477, 1.996164414091922135 ) ) ;
#33795=CARTESIAN_POINT ( 'NONE',  ( 1.370646902836635261, -1.372427557409527488, 1.669970663979184256 ) ) ;
#33797=CARTESIAN_POINT ( 'NONE',  ( 1.594405160661801490, -1.078473704070359140, 1.707419690039575499 ) ) ;
#33802=CARTESIAN_POINT ( 'NONE',  ( 6.714220164357198151, -1.617572894677368422, -1.203167480739217421 ) ) ;
#33803=CARTESIAN_POINT ( 'NONE',  ( 6.503150280507321135, -0.1381757461387123076, 1.884094533524976578 ) ) ;
#33805=CARTESIAN_POINT ( 'NONE',  ( 4.810206850810132551, 1.511280187219691928, -1.587364365194674276 ) ) ;
#33807=CARTESIAN_POINT ( 'NONE',  ( 3.340010735810138520, -1.142844047782382466, -1.533173144288489276 ) ) ;
#33811=CARTESIAN_POINT ( 'NONE',  ( 1.651970485933237143, 1.039013645561959853, 1.727991324714774013 ) ) ;
#33814=CARTESIAN_POINT ( 'NONE',  ( 0.6094042559229868594, -0.3290114652876909296, 2.268531362689259812 ) ) ;
#33816=CARTESIAN_POINT ( 'NONE',  ( 4.242953580973901850, -1.500179917044243139, 0.8508681493539415053 ) ) ;
#33820=CARTESIAN_POINT ( 'NONE',  ( 1.205434515183744226, -1.544416933936803904, -1.209700862059132964 ) ) ;
#33822=CARTESIAN_POINT ( 'NONE',  ( 0.07536363704233395300, 5.720741966631408104, -2.738263776839637398 ) ) ;
#33823=VERTEX_POINT ( 'NONE', #193874 ) ;
#33827=CARTESIAN_POINT ( 'NONE',  ( 4.811091142047322577, 1.503129720864199381, -1.010622461758519552 ) ) ;
#33830=CARTESIAN_POINT ( 'NONE',  ( 6.234996492879100849, 1.692908850720629799, 0.6451080659017217611 ) ) ;
#33835=CARTESIAN_POINT ( 'NONE',  ( 5.828513650932020340, -1.180329482691832244, 1.438830759754748723 ) ) ;
#33837=CARTESIAN_POINT ( 'NONE',  ( 3.462411278976515128, -1.846996576941996482, -0.5078680121572733963 ) ) ;
#33842=CARTESIAN_POINT ( 'NONE',  ( 6.034383107294147841, 0.6662506799693500570, 2.009816206752083723 ) ) ;
#33843=CARTESIAN_POINT ( 'NONE',  ( 1.165152350680317195, -1.954565670758709128, -0.9236901323337529668 ) ) ;
#33846=CARTESIAN_POINT ( 'NONE',  ( 0.5338675855391886715, 0.9430634504648884864, -1.562995807167219642 ) ) ;
#33848=CARTESIAN_POINT ( 'NONE',  ( 3.662960631648714216, -1.609669772967847079, -0.8612380056681954166 ) ) ;
#33850=CARTESIAN_POINT ( 'NONE',  ( 2.689602200614676697, 1.814610489020528350, -0.6038049036062518304 ) ) ;
#33852=CARTESIAN_POINT ( 'NONE',  ( 2.383201438719654064, -0.002954665228930426248, 1.969739564733210324 ) ) ;
#33853=CARTESIAN_POINT ( 'NONE',  ( 4.370608360784649093, -0.003437861098648780072, -1.942234966449083000 ) ) ;
#33856=CARTESIAN_POINT ( 'NONE',  ( 5.097945154717048233, 1.425953928781589886, 1.569717048080176314 ) ) ;
#33858=CARTESIAN_POINT ( 'NONE',  ( 2.455592584850064153, -1.418247937500687561, -1.282927761235647335 ) ) ;
#33861=ORIENTED_EDGE ( 'NONE', *, *, #25909, .T. ) ;
#33866=CARTESIAN_POINT ( 'NONE',  ( 4.758326833623739205, 0.7015320795021735556, 1.685726030614169924 ) ) ;
#33867=CARTESIAN_POINT ( 'NONE',  ( 6.192592252150040721, 1.490973663936447258, -1.357864438797616868 ) ) ;
#33872=CARTESIAN_POINT ( 'NONE',  ( 5.119927267529915227, -1.001353885182048931, -1.579878405157906673 ) ) ;
#33878=( NAMED_UNIT ( * ) PLANE_ANGLE_UNIT ( ) SI_UNIT ( $, .RADIAN. ) );
#33882=CARTESIAN_POINT ( 'NONE',  ( 6.807499178464245126, -1.738453852359397978, -1.300317965242798968 ) ) ;
#33883=CARTESIAN_POINT ( 'NONE',  ( 2.144302737913783119, 0.9084621246772636161, 1.912570996397492618 ) ) ;
#33886=CARTESIAN_POINT ( 'NONE',  ( 5.805552407531882508, -1.628464769346991581, -1.278160613847306504 ) ) ;
#33891=CARTESIAN_POINT ( 'NONE',  ( 2.080407636089614432, -2.248563537884174846, -0.4446712507181517782 ) ) ;
#33894=CARTESIAN_POINT ( 'NONE',  ( 2.074333847954575205, 0.8209984392052707136, 1.727357542596375861 ) ) ;
#33897=CARTESIAN_POINT ( 'NONE',  ( 1.107682593029035711, 1.527310012579755183, 1.311747809748030846 ) ) ;
#33898=CARTESIAN_POINT ( 'NONE',  ( 0.6726124357511429341, 1.356994209013298036, -1.416925378234991095 ) ) ;
#33902=CARTESIAN_POINT ( 'NONE',  ( 3.609396000958647210, -2.059664220577660743, 0.3575658041875314219 ) ) ;
#33903=CARTESIAN_POINT ( 'NONE',  ( 1.990718100289643244, 1.541686266772484437, -0.8690610084590517648 ) ) ;
#33906=CARTESIAN_POINT ( 'NONE',  ( 5.666080500323320557, -1.458056995643598475, 1.768786637700834108 ) ) ;
#33907=CARTESIAN_POINT ( 'NONE',  ( 3.450842174108187610, 0.4214097805228322891, -1.688396943527884053 ) ) ;
#33912=CARTESIAN_POINT ( 'NONE',  ( 3.848775019297555389, -0.8554209813324518130, 1.508043379464953260 ) ) ;
#33913=CARTESIAN_POINT ( 'NONE',  ( 3.525983582677540085, 2.118976886349494659, -0.4726038967238275212 ) ) ;
#33915=CARTESIAN_POINT ( 'NONE',  ( 5.665250009225348826, 1.861346387706263261, -0.7762253298396750711 ) ) ;
#33916=CARTESIAN_POINT ( 'NONE',  ( 0.8437500000000005551, 1.895863743164106774, 0.7852924748299443536 ) ) ;
#33919=CARTESIAN_POINT ( 'NONE',  ( 2.502848596126582059, 1.548454276800725449, -1.145803370841493418 ) ) ;
#33921=CARTESIAN_POINT ( 'NONE',  ( 5.730790430626864662, 1.492114905813126446, -1.645873056973495618 ) ) ;
#33923=CARTESIAN_POINT ( 'NONE',  ( 6.983263157960361234, 3.701227967198342128, 2.360532479264612071 ) ) ;
#33928=CARTESIAN_POINT ( 'NONE',  ( 1.998975601324129769, -2.179183720934555701, -0.4297205562568666148 ) ) ;
#33929=CARTESIAN_POINT ( 'NONE',  ( 6.742638286788313451, -1.923764577213080029, -0.3838556375530403630 ) ) ;
#33936=CARTESIAN_POINT ( 'NONE',  ( 4.070800801938780467, 1.460776800910084994, -1.456535598646004237 ) ) ;
#33940=CARTESIAN_POINT ( 'NONE',  ( 6.063714619507535097, 1.842885348237649490, -0.3194776537047139264 ) ) ;
#33941=CARTESIAN_POINT ( 'NONE',  ( 4.746542152430166972, 1.714266118827989516, -0.2609391866443058206 ) ) ;
#33942=CARTESIAN_POINT ( 'NONE',  ( 4.985792865680892305, -1.728136641771714777, -0.2059490554011476626 ) ) ;
#33944=CARTESIAN_POINT ( 'NONE',  ( 1.927642574099263983, -1.500803908722462499, -1.732858182149794812 ) ) ;
#33946=CARTESIAN_POINT ( 'NONE',  ( 5.565992953457829628, -1.325659382304938960, 1.616758296502271097 ) ) ;
#33947=CARTESIAN_POINT ( 'NONE',  ( 0.8668490835730925381, 1.774987751554598869, -0.4888055736953432207 ) ) ;
#33950=CARTESIAN_POINT ( 'NONE',  ( 1.125625214514534900, 0.3961039030971893471, 1.976955501819408711 ) ) ;
#33956=CARTESIAN_POINT ( 'NONE',  ( 3.703867829435038672, 1.536975034498413661, 1.461131120854219700 ) ) ;
#33958=CARTESIAN_POINT ( 'NONE',  ( 5.338443970399977978, 1.799313579390570128, 0.3082849261525285600 ) ) ;
#33964=CARTESIAN_POINT ( 'NONE',  ( 2.970967976831692781, -1.526577591334898454, 1.322595846222093030 ) ) ;
#33965=CARTESIAN_POINT ( 'NONE',  ( 0.4640741377587159211, 2.083006155408675397, -0.3091503547662070583 ) ) ;
#33967=CARTESIAN_POINT ( 'NONE',  ( 3.783913598179854176, -1.105313619694109795, -1.496993097346049462 ) ) ;
#33974=CARTESIAN_POINT ( 'NONE',  ( 6.772340629568521564, -1.270048932776141726, 1.623522132280514896 ) ) ;
#33978=CARTESIAN_POINT ( 'NONE',  ( 2.248989396041571887, -1.699371294898213369, -0.3429280648484279714 ) ) ;
#33979=CARTESIAN_POINT ( 'NONE',  ( 1.710509606392306647, -0.2150479285965025134, 1.726905287013901225 ) ) ;
#33980=CARTESIAN_POINT ( 'NONE',  ( 0.4293363604773897113, 2.209526777583595170, 0.6654907822973181730 ) ) ;
#33982=CARTESIAN_POINT ( 'NONE',  ( 1.036483977676525114, 2.029821650745375905, 0.3549538351500410305 ) ) ;
#33985=CARTESIAN_POINT ( 'NONE',  ( 0.2454708137151571101, -1.954895187565863779, -0.4925657318226167591 ) ) ;
#33988=CARTESIAN_POINT ( 'NONE',  ( 6.350466393003619814, 0.5888352225367661230, 1.775644890098279749 ) ) ;
#33989=CARTESIAN_POINT ( 'NONE',  ( 4.588094604188536429, 1.105678411722615051, 1.560157546714964871 ) ) ;
#33992=CARTESIAN_POINT ( 'NONE',  ( 6.551417122825020201, -1.769646310455678995, -1.318412661681533260 ) ) ;
#33996=CARTESIAN_POINT ( 'NONE',  ( 0.06511101446048017660, -1.620675302784078786, 1.204964419619258376 ) ) ;
#33998=CARTESIAN_POINT ( 'NONE',  ( 2.977863636430440941, 2.191611430486348766, -0.7225824955255434334 ) ) ;
#33999=CARTESIAN_POINT ( 'NONE',  ( 4.668382477721988444, -0.8370036265390871089, -1.774476930476886594 ) ) ;
#34000=CARTESIAN_POINT ( 'NONE',  ( 1.340592890135338555, -1.912720961655197893, -0.4351338972534216087 ) ) ;
#34004=CARTESIAN_POINT ( 'NONE',  ( 0.3920140705387532010, -2.106502388992930630, 0.2143382252216985973 ) ) ;
#34007=CARTESIAN_POINT ( 'NONE',  ( 1.359045109759978498, 1.814150759811587355, -0.3131490413979670651 ) ) ;
#34008=CARTESIAN_POINT ( 'NONE',  ( 4.487298306821032590, 0.1004956810540975631, 2.168842786202809680 ) ) ;
#34010=CARTESIAN_POINT ( 'NONE',  ( 1.793382672576701919, -0.1090974814243403090, -2.117938670719583527 ) ) ;
#34016=CARTESIAN_POINT ( 'NONE',  ( 2.091158219120598183, 1.794587730539594972, -1.012862355382545765 ) ) ;
#34024=CARTESIAN_POINT ( 'NONE',  ( 4.863870654145381778, 0.5962773724161560818, -1.817021391602849034 ) ) ;
#34026=CARTESIAN_POINT ( 'NONE',  ( 1.212636322461498217, -1.017548795778918214, -2.020700439389290892 ) ) ;
#34028=CARTESIAN_POINT ( 'NONE',  ( 1.318313199092124188, -0.6538357601561273214, -1.689641652304620045 ) ) ;
#34029=CARTESIAN_POINT ( 'NONE',  ( 1.428765994036251818, -1.616370030362016985, 1.027966131488191381 ) ) ;
#34031=CARTESIAN_POINT ( 'NONE',  ( 2.980987059868035693, 1.948563265827065960, 0.6999735360200682877 ) ) ;
#34033=CARTESIAN_POINT ( 'NONE',  ( 0.6374961883623613268, -1.392493025731633027, -1.395827840033945000 ) ) ;
#34034=CARTESIAN_POINT ( 'NONE',  ( 5.197847267195914611, -0.6914886683457229788, 1.798296804713859220 ) ) ;
#34035=CARTESIAN_POINT ( 'NONE',  ( 1.436587813502993249, 1.134030013130071346, -2.009770128656597876 ) ) ;
#34038=CARTESIAN_POINT ( 'NONE',  ( 5.283662074727401681, -1.959763400824132251, 0.6436608119341418188 ) ) ;
#34042=CARTESIAN_POINT ( 'NONE',  ( 5.368238606676455582, 1.035150450411811640, 1.833903993397972387 ) ) ;
#34044=CARTESIAN_POINT ( 'NONE',  ( 0.6433370543819162402, -0.2662039958584628829, -2.154713702345659510 ) ) ;
#34046=CARTESIAN_POINT ( 'NONE',  ( 4.622454487542247747, 1.333869025858843482, -1.700861402727947169 ) ) ;
#34047=CARTESIAN_POINT ( 'NONE',  ( 5.760417579480547445, 2.017467016246987210, 0.09685271086026786547 ) ) ;
#34048=CARTESIAN_POINT ( 'NONE',  ( -0.1399997263889836974, 2.022132088033218533, -2.415689637818136948 ) ) ;
#34053=CARTESIAN_POINT ( 'NONE',  ( 3.116422982138194353, 1.968445132739887748, 0.4370783100892047801 ) ) ;
#34058=CARTESIAN_POINT ( 'NONE',  ( 5.436455051933180016, 2.129025116502227810, 0.3735886874452337691 ) ) ;
#34063=CARTESIAN_POINT ( 'NONE',  ( 5.255482535091188012, 1.942537579172060047, -0.5405093616211650298 ) ) ;
#34065=CARTESIAN_POINT ( 'NONE',  ( 1.136830759877343722, -1.561040526032995590, 0.7340551814495520633 ) ) ;
#34070=CARTESIAN_POINT ( 'NONE',  ( 6.204356031920277736, -0.6731288877953770511, -1.745422550748019441 ) ) ;
#34071=CARTESIAN_POINT ( 'NONE',  ( 6.363545146358847937, -1.619577101098391925, -1.195656717203520403 ) ) ;
#34078=CARTESIAN_POINT ( 'NONE',  ( 2.473420802178166067, -1.846219560914775570, -1.042883725575906029 ) ) ;
#34079=CARTESIAN_POINT ( 'NONE',  ( 2.144157856786413241, 0.8647422840215597262, 1.821734841475818101 ) ) ;
#34080=CARTESIAN_POINT ( 'NONE',  ( 2.337905319157699502, -1.045887089798164915, -1.478944033197209462 ) ) ;
#34082=CARTESIAN_POINT ( 'NONE',  ( 6.579002408576895000, -0.1006694238701970334, -2.159482418181729813 ) ) ;
#34086=CARTESIAN_POINT ( 'NONE',  ( 0.1806861152609346710, 1.591142543434557632, -1.066548322639774504 ) ) ;
#34094=CARTESIAN_POINT ( 'NONE',  ( 4.206063578812153203, -2.156103337031569200, 0.1562769059922017589 ) ) ;
#34097=CARTESIAN_POINT ( 'NONE',  ( 2.355864820516640812, -1.574449018071517825, -1.420800595792824028 ) ) ;
#34099=CARTESIAN_POINT ( 'NONE',  ( 3.497303454036035930, 1.552041748764835249, 1.215357900914854516 ) ) ;
#34100=CARTESIAN_POINT ( 'NONE',  ( 5.467032840998240495, -1.503656711810175350, 1.181500457595338505 ) ) ;
#34103=CARTESIAN_POINT ( 'NONE',  ( 5.723099352235532677, -1.779878778038428200, -0.8436364978330126441 ) ) ;
#34104=CARTESIAN_POINT ( 'NONE',  ( 1.992034801999421623, -0.5177828490160235608, -1.871580480717034645 ) ) ;
#34111=CARTESIAN_POINT ( 'NONE',  ( 5.690081826675051246, 1.142623417513729089, 1.533212917768103534 ) ) ;
#34113=CARTESIAN_POINT ( 'NONE',  ( 2.789901687333019797, 1.561178712900921584, 1.560079944692857046 ) ) ;
#34114=CARTESIAN_POINT ( 'NONE',  ( 2.239569982544288518, -1.971322999760493300, 0.9919465654871155724 ) ) ;
#34117=CARTESIAN_POINT ( 'NONE',  ( 1.066890508724306130, -1.507026839618429426, 1.177014404800474479 ) ) ;
#34120=CARTESIAN_POINT ( 'NONE',  ( 4.633297751427937428, 0.003287558298453730800, -2.070544812459538253 ) ) ;
#34123=CARTESIAN_POINT ( 'NONE',  ( 1.903414394802248166, 1.797162532295241366, 1.201017911493490020 ) ) ;
#34124=CARTESIAN_POINT ( 'NONE',  ( 3.456733517523991051, -1.933646301634945885, -1.031433503814835007 ) ) ;
#34132=CARTESIAN_POINT ( 'NONE',  ( 5.537694164425770005, -1.361542515911953855, 1.073868356900798959 ) ) ;
#34134=CARTESIAN_POINT ( 'NONE',  ( 3.045825399726838079, 1.460771095745692527, 1.467265538693182991 ) ) ;
#34135=CARTESIAN_POINT ( 'NONE',  ( 5.396159345875370938, -0.9528639288615829983, -1.890782970011774422 ) ) ;
#34138=CARTESIAN_POINT ( 'NONE',  ( 2.992966325197043531, 0.2361965902525232364, 1.955129705961492270 ) ) ;
#34139=CARTESIAN_POINT ( 'NONE',  ( 0.6328886395040033142, 1.767934563615305432, 0.7296191750566642931 ) ) ;
#34140=CARTESIAN_POINT ( 'NONE',  ( 5.736350775408121550, 0.4420370857395071740, 2.249087507758650517 ) ) ;
#34141=CARTESIAN_POINT ( 'NONE',  ( 2.402731849113007190, 1.466575434288765800, -1.087121784572639527 ) ) ;
#34147=CARTESIAN_POINT ( 'NONE',  ( 4.078389064453043389, 0.9529185939490876223, 1.773430079992607045 ) ) ;
#34148=CARTESIAN_POINT ( 'NONE',  ( 4.258614474744500278, -0.6113484564182982695, -1.864166799412938502 ) ) ;
#34152=CARTESIAN_POINT ( 'NONE',  ( -0.07645973585807680495, -1.289725328510348934, -1.646077999003342729 ) ) ;
#34153=CARTESIAN_POINT ( 'NONE',  ( 6.227411129102443432, -1.664988906758845921, 0.6005623136680103835 ) ) ;
#34155=CARTESIAN_POINT ( 'NONE',  ( 1.992365796559266267, -0.5863786240636535974, -2.111471653062434672 ) ) ;
#34156=CARTESIAN_POINT ( 'NONE',  ( -0.09478571475088257148, -0.7418789811804274992, -1.573373712294885207 ) ) ;
#34159=CARTESIAN_POINT ( 'NONE',  ( 0.5742808809356505506, -1.622453496466894407, -0.5859570326207633739 ) ) ;
#34160=CARTESIAN_POINT ( 'NONE',  ( 0.2577194443907256383, 2.166829308800602316, -0.3276212646995610989 ) ) ;
#34161=CARTESIAN_POINT ( 'NONE',  ( 6.186827581914116081, -0.9662774195124073096, -1.439361474112188954 ) ) ;
#34162=CARTESIAN_POINT ( 'NONE',  ( 2.930518499080053907, 1.225513248159842083, -1.835134156090315605 ) ) ;
#34163=CARTESIAN_POINT ( 'NONE',  ( 6.848074921520021618, -0.9335981340678388696, 1.958013476854936652 ) ) ;
#34165=CARTESIAN_POINT ( 'NONE',  ( 1.815762809344774187, -1.387149605378830586, -1.599721994570136197 ) ) ;
#34166=CARTESIAN_POINT ( 'NONE',  ( 6.827182134110196365, 7.629137130509086262, 2.889055895399252005 ) ) ;
#34167=CARTESIAN_POINT ( 'NONE',  ( 5.508790920392054424, 1.458765576344657866, -1.258282468310659707 ) ) ;
#34168=CARTESIAN_POINT ( 'NONE',  ( 3.087719631786550956, -0.9270648334414759439, 2.096714421332421807 ) ) ;
#34172=CARTESIAN_POINT ( 'NONE',  ( 5.039773670486915158, -2.109617592216144644, 0.6956167390435584741 ) ) ;
#34179=CARTESIAN_POINT ( 'NONE',  ( 2.584611472894111195, -0.6298744119781033435, 1.915600275669691488 ) ) ;
#34181=CARTESIAN_POINT ( 'NONE',  ( 0.6024794235527919373, 2.056786662827071233, 0.1555941968269194953 ) ) ;
#34185=CARTESIAN_POINT ( 'NONE',  ( 3.644632398932126094, -1.791719913761843364, 1.261548167004488130 ) ) ;
#34186=CARTESIAN_POINT ( 'NONE',  ( 1.617814789376757156, 0.2004366740697149929, 2.006445999502483257 ) ) ;
#34187=CARTESIAN_POINT ( 'NONE',  ( 1.382094229771430705, -0.2707140722739818650, -1.821126350552772610 ) ) ;
#34188=CARTESIAN_POINT ( 'NONE',  ( 5.355124402800013783, 0.4497703203518633175, -2.247661708361737620 ) ) ;
#34189=CARTESIAN_POINT ( 'NONE',  ( 4.031074566243696644, -1.271087849624694233, -1.332192834049110486 ) ) ;
#34192=CARTESIAN_POINT ( 'NONE',  ( 4.524309061075334704, 1.122661849025725189, -1.439470297551891154 ) ) ;
#34193=CARTESIAN_POINT ( 'NONE',  ( 4.465470312728934132, -1.956561007648183192, -0.4872041746135646889 ) ) ;
#34195=CARTESIAN_POINT ( 'NONE',  ( 5.084992976345711568, -0.2718087151927280343, -2.246069130642995404 ) ) ;
#34197=CARTESIAN_POINT ( 'NONE',  ( 6.247117736759643769, -1.781108002423707592, 1.123397916191863244 ) ) ;
#34199=CARTESIAN_POINT ( 'NONE',  ( 4.773920332862017446, -2.031068740936771366, 0.4005940302675218834 ) ) ;
#34204=CARTESIAN_POINT ( 'NONE',  ( 2.561056213344356181, -1.676160556340213992, -0.9495491084439124929 ) ) ;
#34207=CARTESIAN_POINT ( 'NONE',  ( 6.578958714233388072, 1.836342173298356917, 0.7121609383471518839 ) ) ;
#34211=CARTESIAN_POINT ( 'NONE',  ( 1.019968326173793960, -0.5097545255977399270, 2.058319881341897695 ) ) ;
#34212=CARTESIAN_POINT ( 'NONE',  ( 1.758359454726521998, 0.8447074013377148249, -2.054735579953733904 ) ) ;
#34213=CARTESIAN_POINT ( 'NONE',  ( 3.522586592847714471, 1.337535325648725459, -1.626654721158872885 ) ) ;
#34216=CARTESIAN_POINT ( 'NONE',  ( 2.699599903323801620, -1.451799986561516764, -1.319707477925702310 ) ) ;
#34223=CARTESIAN_POINT ( 'NONE',  ( 1.459403507577087700, -1.788631592985808538, 1.138920039206146928 ) ) ;
#34226=CARTESIAN_POINT ( 'NONE',  ( 4.879329150013382410, -0.09822140645733207220, 1.959542894978071992 ) ) ;
#34227=CARTESIAN_POINT ( 'NONE',  ( 3.450221060135277629, 2.161883445724331665, 0.001893877739161941697 ) ) ;
#34228=CARTESIAN_POINT ( 'NONE',  ( 2.436835438956724165, -1.365703447793526149, -1.235134912642745553 ) ) ;
#34231=CARTESIAN_POINT ( 'NONE',  ( 4.523245630038312370, -1.073764689188366317, -1.369494959904279829 ) ) ;
#34235=CARTESIAN_POINT ( 'NONE',  ( 1.956163130892615731, 2.155914767609674598, -0.1587918856347721730 ) ) ;
#34236=CARTESIAN_POINT ( 'NONE',  ( 5.061874962716293780, 1.677747168027879709, -1.117663061872615771 ) ) ;
#34239=CARTESIAN_POINT ( 'NONE',  ( 1.622176833581047806, -1.201014165160016356, -1.797165035535647659 ) ) ;
#34240=CARTESIAN_POINT ( 'NONE',  ( 3.573081558413326864, 0.04979752193529430465, -1.971001165494235652 ) ) ;
#34243=CARTESIAN_POINT ( 'NONE',  ( 3.052217916795424202, -1.468930141372110088, 1.270444820450331358 ) ) ;
#34247=ORIENTED_EDGE ( 'NONE', *, *, #24409, .F. ) ;
#34252=CARTESIAN_POINT ( 'NONE',  ( 0.3587983166186413109, 0.8468606107991830667, 2.038007455039527294 ) ) ;
#34254=CARTESIAN_POINT ( 'NONE',  ( 5.629730433169950921, 1.891637868780412068, -0.5196590155819302836 ) ) ;
#34255=CARTESIAN_POINT ( 'NONE',  ( 1.424454163599726320, -1.462446849824734274, -1.388484543128357229 ) ) ;
#34257=CARTESIAN_POINT ( 'NONE',  ( 3.643865571896960809, 2.100859469783818323, -0.2634356371126170826 ) ) ;
#34261=CARTESIAN_POINT ( 'NONE',  ( 4.259580805731934205, 0.8699401392010926992, 1.622648742527862620 ) ) ;
#34264=CARTESIAN_POINT ( 'NONE',  ( 4.746395313581045272, 1.087821826000658909, -1.820160695957805608 ) ) ;
#34268=CARTESIAN_POINT ( 'NONE',  ( 5.835248319207797074, -1.864956875241881251, 0.8770506743334179900 ) ) ;
#34271=CARTESIAN_POINT ( 'NONE',  ( 1.170091191536073660, -0.8321358839059491697, -1.664716676500255010 ) ) ;
#34272=CARTESIAN_POINT ( 'NONE',  ( 2.682954136603598272, 1.303717545168959990, 1.300458928786947688 ) ) ;
#34276=CARTESIAN_POINT ( 'NONE',  ( 2.631697372267821855, -2.058793095894187353, 0.7952504953367269813 ) ) ;
#34277=CARTESIAN_POINT ( 'NONE',  ( 5.343176995970949861, -1.944282970029135083, 1.156607043288411019 ) ) ;
#34279=CARTESIAN_POINT ( 'NONE',  ( 4.535318187750695174, -0.08185482751379420663, 1.809849901470663491 ) ) ;
#34280=CARTESIAN_POINT ( 'NONE',  ( 5.841025094292755071, -1.646784362596087625, -0.9785371348113005574 ) ) ;
#34282=CARTESIAN_POINT ( 'NONE',  ( 5.084763247618332649, -0.2297073032716222263, -1.856415652357709778 ) ) ;
#34284=CARTESIAN_POINT ( 'NONE',  ( 4.703460533163725366, -1.437978410778781857, -1.181371033526560144 ) ) ;
#34287=CARTESIAN_POINT ( 'NONE',  ( 6.825078400183545391, 0.005516643811322509937, 1.755566376062764222 ) ) ;
#34288=CARTESIAN_POINT ( 'NONE',  ( 0.1632964843477149597, 1.879801964727344732, -0.7303121171872913875 ) ) ;
#34290=CARTESIAN_POINT ( 'NONE',  ( 1.365998295032941900, 2.074639164447332540, -0.3615360007043573187 ) ) ;
#34295=CARTESIAN_POINT ( 'NONE',  ( 1.828384590600404591, -0.9557513975326953348, -1.779375440769872752 ) ) ;
#34297=CARTESIAN_POINT ( 'NONE',  ( 6.620655732516643965, 2.083750514537034970, 2.135603474206409835 ) ) ;
#34300=CARTESIAN_POINT ( 'NONE',  ( 2.688937055384226671, -0.3666181952855402382, -2.130111032054008646 ) ) ;
#34301=CARTESIAN_POINT ( 'NONE',  ( 6.610000000000006537, 2.052567036419289614, 2.306714106643445561 ) ) ;
#34306=CARTESIAN_POINT ( 'NONE',  ( 0.5213437761196970666, -2.079166062760181788, 0.6930039600180630810 ) ) ;
#34308=CARTESIAN_POINT ( 'NONE',  ( 1.938691616020698172, 2.238021082172815479, 0.3313278802117639033 ) ) ;
#34316=CARTESIAN_POINT ( 'NONE',  ( 2.635733503900684838, 0.8381847041133619891, -1.558674532600109686 ) ) ;
#34318=CARTESIAN_POINT ( 'NONE',  ( 6.827182134110222123, -0.006956174471953178659, 2.188967759425272330 ) ) ;
#34323=CARTESIAN_POINT ( 'NONE',  ( 5.659779856126235131, 1.203369751103126717, 1.617807692209996207 ) ) ;
#34324=CARTESIAN_POINT ( 'NONE',  ( 4.781432078664868079, 0.1701398743050798745, -1.803555781593807250 ) ) ;
#34326=CARTESIAN_POINT ( 'NONE',  ( 2.254581950620972997, -1.447608085528677480, 1.184820545849271767 ) ) ;
#34327=CARTESIAN_POINT ( 'NONE',  ( 2.289971195246335078, -1.349064171463711936, -1.570471239911851669 ) ) ;
#34329=CARTESIAN_POINT ( 'NONE',  ( 2.021601768330282045, -0.4154675118966509317, 1.866563793090275203 ) ) ;
#34334=CARTESIAN_POINT ( 'NONE',  ( 0.2285749388857594433, 1.317234250586714284, -1.386657971642536014 ) ) ;
#34336=CARTESIAN_POINT ( 'NONE',  ( 1.486689167417578394, 1.889818972856545987, 0.5264814339432166701 ) ) ;
#34339=CARTESIAN_POINT ( 'NONE',  ( 5.027636390373715791, -0.3086946445357249824, 2.097867224209007730 ) ) ;
#34343=CARTESIAN_POINT ( 'NONE',  ( 0.4209003391736841349, -0.09842406703440903515, 1.868101828653282226 ) ) ;
#34345=CARTESIAN_POINT ( 'NONE',  ( 1.916272853804147136, -2.012662139290276819, 0.05368196500972129831 ) ) ;
#34347=CARTESIAN_POINT ( 'NONE',  ( 0.7380959315415897004, 2.114583753240849795, -0.1084930780173159887 ) ) ;
#34349=CARTESIAN_POINT ( 'NONE',  ( 2.418496320782090869, 0.8830982243829659240, 1.872697815963566992 ) ) ;
#34353=CARTESIAN_POINT ( 'NONE',  ( 5.841762345275034463, 2.088193589346263312, 0.1035180442379990684 ) ) ;
#34355=CARTESIAN_POINT ( 'NONE',  ( 4.647361241834577328, -1.411646026218037253, -1.157555111390089264 ) ) ;
#34356=CARTESIAN_POINT ( 'NONE',  ( 2.894932696777189118, -0.1353093493836102779, -1.806485987321084341 ) ) ;
#34361=CARTESIAN_POINT ( 'NONE',  ( 5.702238492974306183, -2.206952906645575307, -0.005361432510411765114 ) ) ;
#34364=CARTESIAN_POINT ( 'NONE',  ( 3.861887077619485797, 0.6414691495152945455, -1.801623935260010079 ) ) ;
#34371=CARTESIAN_POINT ( 'NONE',  ( 0.09881949811249221560, -0.4921898920670075839, 1.774194203830472993 ) ) ;
#34374=CARTESIAN_POINT ( 'NONE',  ( 3.796049943699483453, -1.868292110373217740, -0.09463876624429126694 ) ) ;
#34379=CARTESIAN_POINT ( 'NONE',  ( 6.491088764554701740, 0.1969099459505334604, 2.060843999385448821 ) ) ;
#34380=CARTESIAN_POINT ( 'NONE',  ( 2.161732667986946410, 1.242745142284812365, 1.587824664567152766 ) ) ;
#34384=CARTESIAN_POINT ( 'NONE',  ( 2.361504994916805877, 2.148894721571582789, -0.4289216190115978100 ) ) ;
#34385=CARTESIAN_POINT ( 'NONE',  ( 6.481070005604858686, -0.09514881109910081070, -1.823337098959529001 ) ) ;
#34394=CARTESIAN_POINT ( 'NONE',  ( 4.001369526190221571, -1.836035423186295201, 0.1395379388276704880 ) ) ;
#34395=CARTESIAN_POINT ( 'NONE',  ( 0.6627443117090633384, 0.5862905632768620201, 1.925809981296212170 ) ) ;
#34396=CARTESIAN_POINT ( 'NONE',  ( 2.671599042396528123, -0.8780164823973014565, -2.124237947079451683 ) ) ;
#34398=CARTESIAN_POINT ( 'NONE',  ( 1.006444858994318681, 0.5332790290331288485, 1.782932314864177137 ) ) ;
#34402=CARTESIAN_POINT ( 'NONE',  ( 4.728717205193702533, 1.314622909153417174, -1.389140896021365368 ) ) ;
#34406=CARTESIAN_POINT ( 'NONE',  ( 3.931257944464498166, -1.443263031577642463, -1.512909484191153897 ) ) ;
#34407=CARTESIAN_POINT ( 'NONE',  ( 2.043623373375623942, 0.7184291972081280342, -1.727395513401897453 ) ) ;
#34410=CARTESIAN_POINT ( 'NONE',  ( 6.198766299729112639, 1.534709720371667308, 1.016988835930050739 ) ) ;
#34415=CARTESIAN_POINT ( 'NONE',  ( 3.738627921261325149, 0.2550716744767547728, 1.705777993037333129 ) ) ;
#34417=CARTESIAN_POINT ( 'NONE',  ( 6.604147088760183415, -2.206502607372296421, 0.04933187264975073122 ) ) ;
#34420=CARTESIAN_POINT ( 'NONE',  ( 5.225502712144541206, 0.2199120275673121516, -2.159938666613583802 ) ) ;
#34421=CARTESIAN_POINT ( 'NONE',  ( 3.176193443437186126, -1.086901434622984830, 1.466744820640853098 ) ) ;
#34422=CARTESIAN_POINT ( 'NONE',  ( 1.340592890135338555, -1.912720961655197893, -0.4351338972534216087 ) ) ;
#34423=CARTESIAN_POINT ( 'NONE',  ( 5.964083501069187498, -1.130735325014235793, 1.789944102876602328 ) ) ;
#34425=CARTESIAN_POINT ( 'NONE',  ( 5.478174288590652807, -2.235914823156583964, -0.5050262530511948622 ) ) ;
#34428=CARTESIAN_POINT ( 'NONE',  ( 1.418772191123615078, -0.7664089246972278779, -1.977313068770427229 ) ) ;
#34433=CARTESIAN_POINT ( 'NONE',  ( 6.297752264732417338, -1.566808387090750765, -1.503110733841714675 ) ) ;
#34434=CARTESIAN_POINT ( 'NONE',  ( 6.883263157960357148, 2.018753856957363535, 2.456789959645651500 ) ) ;
#34436=CARTESIAN_POINT ( 'NONE',  ( 1.331071098547026654, 1.488246241617418697, -1.649206797639357180 ) ) ;
#34438=CARTESIAN_POINT ( 'NONE',  ( 5.994767569012836361, -2.000857541758268354, 0.2496038112331094849 ) ) ;
#34440=CARTESIAN_POINT ( 'NONE',  ( 4.364169495198770399, -2.057374995403418172, 0.1468088122822813202 ) ) ;
#34445=CARTESIAN_POINT ( 'NONE',  ( -0.01160896700787457207, -0.4585933848370716270, -2.046879979534850236 ) ) ;
#34446=CARTESIAN_POINT ( 'NONE',  ( 5.133435478496918947, 0.5880181904946503169, 1.928752423557971829 ) ) ;
#34447=CARTESIAN_POINT ( 'NONE',  ( 4.106863108761789505, -0.3106082297497716471, 1.814695527881895476 ) ) ;
#34452=CARTESIAN_POINT ( 'NONE',  ( 2.291662735322400835, -0.7404417586454847822, 1.557896076775511451 ) ) ;
#34454=CARTESIAN_POINT ( 'NONE',  ( 2.409158461118418693, -1.326566255432750197, -1.877132621748223373 ) ) ;
#34456=CARTESIAN_POINT ( 'NONE',  ( 0.9489188801723142941, 0.6573868573102136237, 2.164820675142268058 ) ) ;
#34457=CARTESIAN_POINT ( 'NONE',  ( 2.526118869349633034, -1.213293402057673775, -1.721263080769465992 ) ) ;
#34462=CARTESIAN_POINT ( 'NONE',  ( 6.750000000000005329, 3.748112931134527976E-13, 1.999999999999984901 ) ) ;
#34467=CARTESIAN_POINT ( 'NONE',  ( 4.553117645631366450, 0.3812515705259692522, 2.188315991368384505 ) ) ;
#34468=CARTESIAN_POINT ( 'NONE',  ( 3.802820697025221630, 1.879323313303274734, 1.126966401794778250 ) ) ;
#34472=CARTESIAN_POINT ( 'NONE',  ( 6.610000000000009202, 1.996100381701769289, 2.581056663040970811 ) ) ;
#34474=CARTESIAN_POINT ( 'NONE',  ( 5.185831674374465905, 2.043064739972153543, -0.5678235988075125418 ) ) ;
#34480=CARTESIAN_POINT ( 'NONE',  ( 5.794452930745782382, 1.501506822132542718, -1.065412412061928160 ) ) ;
#34482=CARTESIAN_POINT ( 'NONE',  ( 0.6436349260668382533, 0.5032331446216579129, 1.666064694988089512 ) ) ;
#34487=CARTESIAN_POINT ( 'NONE',  ( 4.944278945467968533, 2.155654431248493985, 0.1625706239713892443 ) ) ;
#34490=CARTESIAN_POINT ( 'NONE',  ( 5.137646372127643524, -1.526005641499485810, -1.531359247741073570 ) ) ;
#34493=CARTESIAN_POINT ( 'NONE',  ( 6.028588005634209601, 1.899229357904350879, 0.5280594692760686160 ) ) ;
#34494=CARTESIAN_POINT ( 'NONE',  ( 5.009033543107539899, 1.729337909971711662, 0.1259922892337256017 ) ) ;
#34496=CARTESIAN_POINT ( 'NONE',  ( 2.156058135970494227, 0.9403143569667195001, 1.979733194660021622 ) ) ;
#34497=CARTESIAN_POINT ( 'NONE',  ( 2.380262917520099553, 1.419673959206497527, 1.819133949716137844 ) ) ;
#34498=CARTESIAN_POINT ( 'NONE',  ( 5.167286647625595641, 0.2060095241231186813, -2.050478191761321956 ) ) ;
#34499=CARTESIAN_POINT ( 'NONE',  ( 0.1990292396216531146, -0.5187523925454742280, 1.871322268447791703 ) ) ;
#34504=CARTESIAN_POINT ( 'NONE',  ( 3.392942708002244068, -2.044739723715986113, -0.5619712599038150236 ) ) ;
#34506=CARTESIAN_POINT ( 'NONE',  ( 1.371720446232262081, -0.2986288616722633793, -1.994071132515719658 ) ) ;
#34508=CARTESIAN_POINT ( 'NONE',  ( 4.260898339918250066, -1.637375743694971408, 1.479669880875638999 ) ) ;
#34510=CARTESIAN_POINT ( 'NONE',  ( 1.586513592238134374, 1.791619466816740003, 0.5028711289422735931 ) ) ;
#34511=CARTESIAN_POINT ( 'NONE',  ( -0.1290005225502918740, 6.946858002156244716, -2.769053915224591211 ) ) ;
#34515=CARTESIAN_POINT ( 'NONE',  ( 6.825078400183551608, 4.689370880799383912, 2.706890346843467299 ) ) ;
#34517=CARTESIAN_POINT ( 'NONE',  ( 3.098563410164618226, -0.5969507786072983935, -1.972546241584592241 ) ) ;
#34521=CARTESIAN_POINT ( 'NONE',  ( 2.315108654539797861, 1.620709295712051246, -1.204917113890991320 ) ) ;
#34524=CARTESIAN_POINT ( 'NONE',  ( 1.973578683463860672, 1.972434364383905292, -0.5973212362519930707 ) ) ;
#34529=CARTESIAN_POINT ( 'NONE',  ( -0.1409997244346088419, 5.722143553014046979, -2.594341442600463843 ) ) ;
#34530=CARTESIAN_POINT ( 'NONE',  ( 1.025062291269123405, -1.166378923895025510, -1.424538887614942739 ) ) ;
#34531=CARTESIAN_POINT ( 'NONE',  ( 5.901041445831936016, 1.806360628843254768, -1.267562117129708232 ) ) ;
#34533=CARTESIAN_POINT ( 'NONE',  ( 1.405796033167512116, -0.5266655099175953092, 2.096309153942426562 ) ) ;
#34535=CARTESIAN_POINT ( 'NONE',  ( 2.096888995370162156, 1.803417055948232761, 0.9023429676050932491 ) ) ;
#34540=CARTESIAN_POINT ( 'NONE',  ( 4.416843060293515144, 1.802029179758830812, 0.8000101564944164245 ) ) ;
#34541=CARTESIAN_POINT ( 'NONE',  ( 3.608611488583326032, 1.916353073142588403, 0.6279913346786819561 ) ) ;
#34545=CARTESIAN_POINT ( 'NONE',  ( -0.01666059994226073634, -0.1612322585618740090, -2.171656592459796808 ) ) ;
#34546=CARTESIAN_POINT ( 'NONE',  ( 5.758279222819879806, -2.070544812512797428, -0.003756845764937844813 ) ) ;
#34549=CARTESIAN_POINT ( 'NONE',  ( 6.539320575229258914, 2.958022083381315337, 2.556018433155104574 ) ) ;
#34550=CARTESIAN_POINT ( 'NONE',  ( 5.396742217995451618, -1.971451684502657287, -0.4385051361721309937 ) ) ;
#34552=CARTESIAN_POINT ( 'NONE',  ( 1.217717225187223473, 0.4062273103370617755, -2.022011198395957887 ) ) ;
#34560=CARTESIAN_POINT ( 'NONE',  ( 2.893231026729268685, 0.2635377995367886861, 2.155045766152231757 ) ) ;
#34563=CARTESIAN_POINT ( 'NONE',  ( 2.946635061770470632, -1.506786691049965432, -1.057933238436038925 ) ) ;
#34565=CARTESIAN_POINT ( 'NONE',  ( 4.775033345069852331, 2.044829088842615494, -0.7888500489584143738 ) ) ;
#34567=CARTESIAN_POINT ( 'NONE',  ( 4.874029165478985348, 1.298689969358796770, 1.852503425883561095 ) ) ;
#34573=CARTESIAN_POINT ( 'NONE',  ( 0.1096998152198442600, -0.7512755041745984297, -1.601369504124000587 ) ) ;
#34574=CARTESIAN_POINT ( 'NONE',  ( 3.756497301808682465, 2.003587623774540472, 0.1952383342433745284 ) ) ;
#34576=CARTESIAN_POINT ( 'NONE',  ( 3.047987177024631844, 0.7594498649067694673, -1.964434322149722245 ) ) ;
#34577=CARTESIAN_POINT ( 'NONE',  ( 1.405720392582618938, -1.065544983005232371, -1.591680324291492310 ) ) ;
#34580=CARTESIAN_POINT ( 'NONE',  ( 1.838274926946784182, -1.056231965017372598, 1.662188548998255078 ) ) ;
#34581=CARTESIAN_POINT ( 'NONE',  ( 0.2329894512427649333, -1.712236961970284632, 0.7538099095961707796 ) ) ;
#34582=CARTESIAN_POINT ( 'NONE',  ( 1.469116868872882620, 1.728625619535430369, 0.9278086228877155950 ) ) ;
#34583=CARTESIAN_POINT ( 'NONE',  ( 6.486573133654839118, -1.106559166176981579, 1.434805384617921842 ) ) ;
#34588=CARTESIAN_POINT ( 'NONE',  ( 5.576977133510579776, -0.04717937999037385977, -1.870219006134994588 ) ) ;
#34592=CARTESIAN_POINT ( 'NONE',  ( 5.014543041041934046, 0.7873211189074662553, 1.914903133430221116 ) ) ;
#34596=CARTESIAN_POINT ( 'NONE',  ( 0.1861046438572169504, -1.272802160389638892, -1.633586439835111648 ) ) ;
#34603=CARTESIAN_POINT ( 'NONE',  ( 5.705508943770692731, -1.545575431542939970, -1.208212526538715137 ) ) ;
#34605=CARTESIAN_POINT ( 'NONE',  ( 3.673203737196802710, -0.8145011343782401214, -1.844427810980188820 ) ) ;
#34606=CARTESIAN_POINT ( 'NONE',  ( 3.520622370129117940, 0.2863239327370070697, 1.894091974173327531 ) ) ;
#34608=CARTESIAN_POINT ( 'NONE',  ( 0.9959476074029066650, -2.191739723303193887, 0.005169097091584087637 ) ) ;
#34609=CARTESIAN_POINT ( 'NONE',  ( 0.2331713839410758660, 6.947498546895825022, -2.548426565200106353 ) ) ;
#34610=CARTESIAN_POINT ( 'NONE',  ( 3.338976900156843453, -1.651226333174139693, 0.8788041501476551165 ) ) ;
#34614=CARTESIAN_POINT ( 'NONE',  ( 4.886377882447483501, -0.7144107685513987338, -1.993165935382594789 ) ) ;
#34616=CARTESIAN_POINT ( 'NONE',  ( 5.969205681473694902, 1.824102622056431811, 0.9793482939001868504 ) ) ;
#34617=CARTESIAN_POINT ( 'NONE',  ( 2.507466893629331395, -2.067604658949507179, 0.3094350269009105703 ) ) ;
#34619=CARTESIAN_POINT ( 'NONE',  ( 0.9907087679515521605, 1.524132375323374200, -0.8073730212512005844 ) ) ;
#34621=B_SPLINE_CURVE_WITH_KNOTS ( 'NONE', 3,
 ( #91126, #27162, #109567, #158258, #74863, #93267, #75922, #76974, #209094, #156118, #159300, #124761, #143101, #138804, #123702, #188600, #26093, #140966, #42383, #108493, #73783, #126892, #110626, #7700, #192850, #44509, #176627, #88991, #155044, #6630, #72709, #122637, #40231, #174517, #106342, #189663, #139879, #205910, #57545, #41315, #112757, #66807, #178769, #198954, #1819, #99362, #116721, #145229, #28238, #211234, #165413, #132949, #11975, #85226, #83085, #151315, #79111, #67877, #200030, #167552, #46634, #13034, #161454, #33277, #118863, #94331, #134023, #52729, #29308, #51682, #100414, #183795, #19153, #2883, #117803, #68954, #135075, #201088, #741, #182721, #129024, #166484, #149164, #160373, #144173, #17009, #50596, #34339, #18076, #35404, #84163, #150251, #62859, #78049, #195000, #101482, #210165, #61806, #127975, #193927, #45574, #111690, #177697, #95402, #3951, #22339, #169682, #139342, #6094, #189138, #55942, #155581, #58072, #74331, #40777, #136134, #38626, #20215, #8247, #154513, #186995, #73235, #72162, #140433, #171823, #121028, #138271, #57007, #204285, #172909, #203230, #88453, #188059, #205372, #54875, #122095, #105799, #184849, #39688, #5017, #156654, #119940, #23417, #123179, #70018, #206445, #104702, #36477, #89528, #7165, #37550, #90595, #106883, #24483, #87375, #152373, #170753, #53811, #202150, #102550, #168613, #185916, #103630, #86303, #21270, #153445, #71091, #137208, #94864, #107963, #45051, #127437, #13583, #126361, #110097, #192320, #9322, #190195, #157727, #10375, #128504, #210716, #173991, #158779, #75396, #61275, #76452, #124235, #41853, #77520, #25563, #62344, #160918, #194472, #92734, #208566, #46114, #177163, #193407, #43978, #28781, #141508, #91674, #207517, #142560, #112232, #27708, #209635, #143641, #176108, #11445, #12512, #42918, #93803, #211774, #59136, #78583, #145773, #125295, #144705, #111163, #178241, #191253, #79656, #109028, #60200, #159843, #29857, #95937, #161993, #175047, #26632, #181413, #151071, #179308, #65510, #99118, #213888, #16762, #34097, #131656, #129563, #132705, #149996, #100168, #98064, #115421, #197659, #17823, #18895, #167308, #48251, #30929, #80732, #97005, #33040, #114366, #83906, #165167, #67629, #148922, #166233, #133774, #82846, #14638, #84979, #130620, #66563, #182468, #164120, #163058, #1567, #199782, #146822, #64479, #51428, #31986, #35149, #195550, #180360, #49305, #495, #198711, #117548, #147872, #50356, #116478, #63412, #183542, #15703, #101225, #196612, #212842, #47188, #113301, #81789, #154262, #139086, #205113, #155322, #56756, #122921, #55679, #120765, #119681, #184600, #136951, #86049, #36217, #187806, #121835, #2633, #134828, #170493, #118612, #89273, #39434, #6906, #185668, #87114, #72983, #106623, #4758, #202976, #70834, #102296, #68706, #168370, #103370, #188879, #186743, #88189, #22077, #54617, #104444, #105527, #135878, #38365, #90329, #200832, #171561, #19965, #5836, #40520, #152125, #71907, #52483, #172652, #3695, #21016, #153184, #138016, #204031, #24227, #23159, #69772, #201898, #53550, #37297, #169432, #192065, #75142, #208319, #141251, #127182, #7984, #11187, #28526, #193150, #190999, #59949, #76199, #110905, #111985, #45864, #207260, #57817, #173733, #189947, #126105, #58889, #10124, #128256, #93544, #144456, #44800, #12257 ),
 .UNSPECIFIED., .F., .F.,
 ( 4, 1, 1, 1, 1, 1, 1, 1, 1, 1, 1, 1, 1, 1, 1, 1, 1, 1, 1, 1, 1, 1, 1, 1, 1, 1, 1, 1, 1, 1, 1, 1, 1, 1, 1, 1, 1, 1, 1, 1, 1, 1, 1, 1, 1, 1, 1, 1, 1, 1, 1, 1, 1, 1, 1, 1, 1, 1, 1, 1, 1, 1, 1, 1, 1, 1, 1, 1, 1, 1, 1, 1, 1, 1, 1, 1, 1, 1, 1, 1, 1, 1, 1, 1, 1, 1, 1, 1, 1, 1, 1, 1, 1, 1, 1, 1, 1, 1, 1, 1, 1, 1, 1, 1, 1, 1, 1, 1, 1, 1, 1, 1, 1, 1, 1, 1, 1, 1, 1, 1, 1, 1, 1, 1, 1, 1, 1, 1, 1, 1, 1, 1, 1, 1, 1, 1, 1, 1, 1, 1, 1, 1, 1, 1, 1, 1, 1, 1, 1, 1, 1, 1, 1, 1, 1, 1, 1, 1, 1, 1, 1, 1, 1, 1, 1, 1, 1, 1, 1, 1, 1, 1, 1, 1, 1, 1, 1, 1, 1, 1, 1, 1, 1, 1, 1, 1, 1, 1, 1, 1, 1, 1, 1, 1, 1, 1, 1, 1, 1, 1, 1, 1, 1, 1, 1, 1, 1, 1, 1, 1, 1, 1, 1, 1, 1, 1, 1, 1, 1, 1, 1, 1, 1, 1, 1, 1, 1, 1, 1, 1, 1, 1, 1, 1, 1, 1, 1, 1, 1, 1, 1, 1, 1, 1, 1, 1, 1, 1, 1, 1, 1, 1, 1, 1, 1, 1, 1, 1, 1, 1, 1, 1, 1, 1, 1, 1, 1, 1, 1, 1, 1, 1, 1, 1, 1, 1, 1, 1, 1, 1, 1, 1, 1, 1, 1, 1, 1, 1, 1, 1, 1, 1, 1, 1, 1, 1, 1, 1, 1, 1, 1, 1, 1, 1, 1, 1, 1, 1, 1, 1, 1, 1, 1, 1, 1, 1, 1, 1, 1, 1, 1, 1, 1, 1, 1, 1, 1, 1, 1, 1, 1, 1, 1, 1, 1, 1, 1, 1, 1, 1, 1, 1, 1, 1, 1, 1, 1, 1, 1, 1, 1, 1, 1, 1, 1, 1, 1, 1, 1, 1, 1, 1, 1, 1, 1, 1, 1, 1, 1, 1, 1, 1, 1, 1, 1, 1, 1, 1, 1, 1, 1, 1, 1, 1, 4 ),
 ( 0.000000000000000000, 0.002599942752653872004, 0.005208763852970823248, 0.007813103504395044890, 0.01041666580238601383, 0.01302040446826325734, 0.01562503794709516405, 0.01822898659850798186, 0.02083325479626091381, 0.02343751936515397344, 0.02604147156932860516, 0.02864593660736421826, 0.03124971754428982826, 0.03385421962853985695, 0.03645805019290717514, 0.03906245553539786086, 0.04166655880408994678, 0.04427067902208449424, 0.04687506736766395427, 0.04947890482860387018, 0.05208340383233839299, 0.05468718329397467132, 0.05729165635893663372, 0.05989559287350183087, 0.06249988401580178210, 0.06510415622071820396, 0.06770810475871495704, 0.07031256650665723695, 0.07291634835701975292, 0.07552085129243907291, 0.07812468146351797538, 0.08072908640827750060, 0.08333318980393969455, 0.08593730989448074287, 0.08854169822802662737, 0.09114553558425014801, 0.09375003453682481669, 0.09635381396055957282, 0.09895828689139142542, 0.1015622234206122604, 0.1041665143989399522, 0.1067707866525781646, 0.1093747350801187734, 0.1119791968332524285, 0.1145829786367304204, 0.1171874814968899975, 0.1197913116783300008, 0.1223957164865987768, 0.1249998199429257079, 0.1276039399106482508, 0.1302083283009266290, 0.1328121656006459317, 0.1354166645410730119, 0.1380204439687620910, 0.1406249168095159707, 0.1432288533966223909, 0.1458331442541831724, 0.1484374165996726891, 0.1510413649597071029, 0.1536458267615184170, 0.1562496085608837959, 0.1588541113892728840, 0.1614579416238982879, 0.1640623463390579739, 0.1666664498991252963, 0.1692705697871219883, 0.1718749582774928841, 0.1744787955635339893, 0.1770832945353020271, 0.1796870740097127606, 0.1822915468038420750, 0.1848954834917516388, 0.1874997742717963711, 0.1901040467523684718, 0.1927079950878241021, 0.1953124569817516476, 0.1979162388197689970, 0.2005207416598733527, 0.2031245719904950509, 0.2057289766559125821, 0.2083330803627857220, 0.2109372002141371993, 0.2135415888479497148, 0.2161454261631269858, 0.2187499252097131475, 0.2213537047736018060, 0.2239581775645482220, 0.2265621143961681627, 0.2291664051419355919, 0.2317706778008114532, 0.2343746261546043874, 0.2369790881840763974, 0.2395828701034999064, 0.2421873729987945312, 0.2447912034682135918, 0.2473956081272447038, 0.2499997120239797754, 0.2526038318817556694, 0.2552082207023498306, 0.2578120580894675551, 0.2604165572543392093, 0.2630203369504529598, 0.2656248097816475973, 0.2682287467998764607, 0.2708330375545950908, 0.2734373104349877015, 0.2760412588500244513, 0.2786457210584605826, 0.2812495031020356140, 0.2838540060959860445, 0.2864578367469951536, 0.2890622414429859233, 0.2916663455726313803, 0.2942704654798921071, 0.2968748545306000852, 0.2994786920324540302, 0.3020831913590704687, 0.3046869712301484290, 0.3072914441450140810, 0.3098953813927431966, 0.3124996721996327054, 0.3151039453447485039, 0.3177078938639273376, 0.3203123562947402525, 0.3229161385052047861, 0.3255206416412691484, 0.3281244725166545528, 0.3307288772929431464, 0.3333329816985414751, 0.3359371016983396796, 0.3385414910224879836, 0.3411453286818670882, 0.3437498282136811634, 0.3463536083024566503, 0.3489580813444087548, 0.3515620188645239841, 0.3541663097667969717, 0.3567705832198370119, 0.3593745318860498972, 0.3619789945826469846, 0.3645827770027332826, 0.3671872803243637073, 0.3697911114669067967, 0.3723955163668249413, 0.3749996210914142147, 0.3776037412267966853, 0.3802081308677072724, 0.3828119687273952576, 0.3854164685078552144, 0.3880202488570567709, 0.3906247220695055478, 0.3932286599048890885, 0.3958329509457525486, 0.3984372247499146091, 0.4010411736060487398, 0.4036456366118335581, 0.4062494192842699414, 0.4088539228349143406, 0.4114577542873927851, 0.4140621593542673784, 0.4166662644408827831, 0.4192703847548917562, 0.4218747747558840855, 0.4244786128586610641, 0.4270831129312115948, 0.4296868935835649328, 0.4322913670099168826, 0.4348953052034483235, 0.4374995964261053638, 0.4401038706245853915, 0.4427078197135246862, 0.4453122830718987402, 0.4479160660394111426, 0.4505205698625146526, 0.4531244016677045128, 0.4557288069448597878, 0.4583329124365353446, 0.4609370329722101700, 0.4635414233766025904, 0.4661452617652466213, 0.4687497621733308639, 0.4713535431715604185, 0.4739580168552197104, 0.4765619554497781962, 0.4791662468974299260, 0.4817705215334236457, 0.4843744708980504132, 0.4869789346524148743, 0.4895827179577280641, 0.4921872220967347111, 0.4947910542974118808, 0.4973954598281701278, 0.4999995657679404681, 0.5026036865683194410, 0.5052080774194306345, 0.5078119161367193879, 0.5104164169237808135, 0.5130201983106112973, 0.5156246722949818784, 0.5182286113334474420, 0.5208329030492938605, 0.5234371781659985512, 0.5260411278491948783, 0.5286455920429519173, 0.5312493757287917173, 0.5338538802271461936, 0.5364577128660878991, 0.5390621186937718523, 0.5416662251246735504, 0.5442703462327953545, 0.5468747375739465566, 0.5494785766626585355, 0.5520830778721422805, 0.5546868596903002935, 0.5572913340187868325, 0.5598952735440421158, 0.5624995655712847764, 0.5651038412119004928, 0.5677077912565504647, 0.5703122559331050834, 0.5729160400421993149, 0.5755205449433484777, 0.5781243780633351648, 0.5807287842312690573, 0.5833328911963423513, 0.5859370126552478908, 0.5885414045297637786, 0.5911452440326808722, 0.5937497457080352925, 0.5963535280002507655, 0.5989580027162609843, 0.6015619427711926814, 0.6041662351530351360, 0.6067705113607667622, 0.6093744618097575172, 0.6119789270125192138, 0.6145827115875999169, 0.6171872169349945647, 0.6197910505788110092, 0.6223954571303226269, 0.6249995646726131948, 0.6276036865253464825, 0.6302080789765573954, 0.6328119189364656005, 0.6354164211211439373, 0.6380202039301521300, 0.6406246790770983024, 0.6432286197045988807, 0.6458329124842493441, 0.6484371893023079814, 0.6510411401985315427, 0.6536456059709156996, 0.6562493910547204656, 0.6588538968918166150, 0.6614577311022542538, 0.6640621380806766005, 0.6666662462432366709, 0.6692703685328477148, 0.6718747616040910975, 0.6744786020637821844, 0.6770831048012443398, 0.6796868881697873954, 0.6822913637910873463, 0.6848953050340567117, 0.6874995982547292828, 0.6901038757263339152, 0.6927078271126885234, 0.6953122934981186276, 0.6979160791333920422, 0.7005205855036529261, 0.7031244203235108570, 0.7057288277721832648, 0.7083329365980738368, 0.7109370593676189731, 0.7135414531022405971, 0.7161452941045143294, 0.7187497974382286436, 0.7213535814090563658, 0.7239580575481356917, 0.7265619994494829648, 0.7291662931543987369, 0.7317705713227778963, 0.7343745232421703406, 0.7369789902840787610, 0.7395827765135741805, 0.7421872834604720248, 0.7447911189325585601, 0.7473955268948287989, 0.7499996364271210858, 0.7526037597196653106, 0.7552081541610216053, 0.7578119957486867397, 0.7604164997221309896, 0.7630202843380037292, 0.7656247610382975743, 0.7682287036409420899, 0.7708329978733315935, 0.7734372767817252470, 0.7760412292770711984, 0.7786456970189011839, 0.7812494838853828449, 0.7838539914523996455, 0.7864578276195345330, 0.7890622361387605865, 0.7916663464205372369, 0.7942704702791556493, 0.7968748654706151457, 0.7994787076864910969, 0.8020832123431549388, 0.8046869976468442598, 0.8072914749517984268, 0.8098954182986718431, 0.8124997131017763774, 0.8151039927934364826, 0.8177079459076636025, 0.8203124143928716139, 0.8229162019391148553, 0.8255207101697450423, 0.8281245470747605752, 0.8307289561943111966, 0.8333330672686687368, 0.8359371917364484261, 0.8385415877213925340, 0.8411454306083117061, 0.8437499359916976749, 0.8463537220259882421, 0.8489581999790609679, 0.8515621441131088210, 0.8541664395301816759, 0.8567707200483754004, 0.8593746738244238959, 0.8619791430964799384, 0.8645829313652741988, 0.8671874403030259693, 0.8697912779887684298, 0.8723956877520262498, 0.8749997996620757501, 0.8776039247821166844, 0.8802083216039426894, 0.8828121652047509205, 0.8854166713583762061, 0.8880204581660676721, 0.8906249368107317377, 0.8932288817749149956, 0.8958331778492237829, 0.8984374592372342816, 0.9010414137180589034, 0.9036458838204490807, 0.9062496728545991198, 0.9088541825429954368, 0.9114580210523274273, 0.9140624315026897317, 0.9166665442915585826, 0.9192706701069754960, 0.9218750678090992245, 0.9244789121666602272, 0.9270834191340497910, 0.9296872067579531329, 0.9322916861377325004, 0.9348956319750387767, 0.9374999287497546296, 0.9401042110508202043, 0.9427081662796877870, 0.9453126372565492375, 0.9479164270979697493, 0.9505209375757615042, 0.9531247769568838013, 0.9557291881641908349, 0.9583333018366511080, 0.9609374282806871781, 0.9635418271385329803, 0.9661456726567504427, 0.9687501794391485399, 0.9713539669241311181, 0.9739584505366999378, 0.9765624007674321705, 0.9791666904763859369, 0.9817709514985233366, 0.9843749191276834898, 0.9869795472165283634, 0.9895832986789295793, 0.9921868791097946394, 0.9947912178632822844, 0.9974000636350187632, 1.000000000000000000 ),
 .UNSPECIFIED. ) ;
#34629=CARTESIAN_POINT ( 'NONE',  ( 0.3283783949157508819, 1.250606878306897984, -1.310747381600821049 ) ) ;
#34638=EDGE_CURVE ( 'NONE', #46524, #110107, #134577, .T. ) ;
#34639=CARTESIAN_POINT ( 'NONE',  ( 3.437814515362676016, 1.178941034414218603, 1.440021488233768521 ) ) ;
#34640=CARTESIAN_POINT ( 'NONE',  ( 0.8959254483255777446, -0.8623397379431455567, -1.710623486014851480 ) ) ;
#34641=CARTESIAN_POINT ( 'NONE',  ( 0.7508259783030580836, 2.089789393294994468, 0.3585813216958123606 ) ) ;
#34647=CARTESIAN_POINT ( 'NONE',  ( 4.539879430399799354, 1.283355579558099091, 1.494016145327778045 ) ) ;
#34648=CARTESIAN_POINT ( 'NONE',  ( 1.032067064438058068, -2.067986175307830798, 0.4682213744369929098 ) ) ;
#34652=CARTESIAN_POINT ( 'NONE',  ( 6.386699327874667986, 1.908680410311427655, -1.076638258889956345 ) ) ;
#34654=CARTESIAN_POINT ( 'NONE',  ( 4.102502470231626397, -0.6033306519132185519, -1.829551733875626862 ) ) ;
#34656=CARTESIAN_POINT ( 'NONE',  ( 0.2174332111963481196, -1.791455004416471430, 0.3504355335035569396 ) ) ;
#34657=CARTESIAN_POINT ( 'NONE',  ( 0.8388348947251201837, 2.174866457552121268, 0.3736606161612308630 ) ) ;
#34661=CARTESIAN_POINT ( 'NONE',  ( 6.262555971378708897, -0.7055598467285629782, -1.838920630280465041 ) ) ;
#34662=CARTESIAN_POINT ( 'NONE',  ( 0.7318534483069280006, 1.913536139905326339, 0.3307262847246707493 ) ) ;
#34663=CARTESIAN_POINT ( 'NONE',  ( 0.1399997263886003374, 0.002789056014650820314, -1.999853399661279063 ) ) ;
#34665=CARTESIAN_POINT ( 'NONE',  ( 4.539814342829402882, 1.213294893355709503, 1.411164879910733472 ) ) ;
#34670=CARTESIAN_POINT ( 'NONE',  ( 0.4159077360078728969, -1.177411712353953588, -1.848246096435968600 ) ) ;
#34674=CARTESIAN_POINT ( 'NONE',  ( 1.787459277025660542, 1.258035843444211155, 1.323286951131589895 ) ) ;
#34677=CARTESIAN_POINT ( 'NONE',  ( 3.463219708433932009, -1.672243815576504700, -0.4589255088537134153 ) ) ;
#34679=CARTESIAN_POINT ( 'NONE',  ( 6.509000000000039421, 4.695815278351551214, 2.562658139094181386 ) ) ;
#34681=CARTESIAN_POINT ( 'NONE',  ( 0.06489154195065281738, -1.720053269671377949, -0.8678208687467499072 ) ) ;
#34682=CARTESIAN_POINT ( 'NONE',  ( 4.891432378139471737, -1.795214109662087942, 0.7913882323652280393 ) ) ;
#34685=CARTESIAN_POINT ( 'NONE',  ( 4.846395287928321416, 1.089488137594313510, -1.819044145143506208 ) ) ;
#34689=CARTESIAN_POINT ( 'NONE',  ( 3.327070777303439364, -1.911029926764183040, -0.7966718667702379353 ) ) ;
#34692=ORIENTED_EDGE ( 'NONE', *, *, #126637, .F. ) ;
#34693=CARTESIAN_POINT ( 'NONE',  ( 2.672825289193903942, 1.627854652907471777, 1.623211659370107363 ) ) ;
#34701=CARTESIAN_POINT ( 'NONE',  ( 4.552931727387078631, 0.3324577288378940954, 1.883125075537089854 ) ) ;
#34703=CARTESIAN_POINT ( 'NONE',  ( 4.700069144524660736, -1.724479993061514449, -0.04023236952926077803 ) ) ;
#34704=CARTESIAN_POINT ( 'NONE',  ( 3.467982673848205355, -0.9896861206786079501, 1.756853968756578066 ) ) ;
#34705=CARTESIAN_POINT ( 'NONE',  ( 4.711759750379289180, 2.199509664246365848, 0.6680300025654511975 ) ) ;
#34707=CARTESIAN_POINT ( 'NONE',  ( 1.084930333755677045, -2.153824616689365978, -0.4803136671489223741 ) ) ;
#34709=CARTESIAN_POINT ( 'NONE',  ( 6.186734212497608354, -0.2616995340462315300, -1.750118319643848119 ) ) ;
#34711=CARTESIAN_POINT ( 'NONE',  ( 1.500361222516993331, -0.8285058210528316591, -2.137470567302256708 ) ) ;
#34712=CARTESIAN_POINT ( 'NONE',  ( 0.3216633777232960067, 1.663872621647478622, 0.5102041932069888430 ) ) ;
#34717=CARTESIAN_POINT ( 'NONE',  ( 0.5202908490967810273, 2.147468835798187037, -0.3191156193892603632 ) ) ;
#34718=CARTESIAN_POINT ( 'NONE',  ( 1.341030165941111241, -1.731997234073547220, -1.032477317303444053 ) ) ;
#34720=CARTESIAN_POINT ( 'NONE',  ( 5.848256421918945236, 1.924412893870678820, 0.09223618542448899782 ) ) ;
#34722=CARTESIAN_POINT ( 'NONE',  ( 2.777807369331359411, 0.3217554308703252652, -2.197856884423950774 ) ) ;
#34723=ORIENTED_EDGE ( 'NONE', *, *, #178034, .T. ) ;
#34729=CARTESIAN_POINT ( 'NONE',  ( 4.159493969870859509, 0.8249727819007621754, 1.532509256507504025 ) ) ;
#34730=CARTESIAN_POINT ( 'NONE',  ( 2.207404936347991065, -1.573848641742966459, -1.171066219227391070 ) ) ;
#34735=CARTESIAN_POINT ( 'NONE',  ( 0.5200786239168513347, 2.040466299037096309, -0.3010312105025755303 ) ) ;
#34738=CARTESIAN_POINT ( 'NONE',  ( 0.9368240258568013568, 2.229511284875786536, 0.3842425355367936057 ) ) ;
#34741=CARTESIAN_POINT ( 'NONE',  ( 2.881944908259078453, -0.9649329312324153030, 1.602325162460143559 ) ) ;
#34742=CARTESIAN_POINT ( 'NONE',  ( 1.089978434334002433, -0.4226591196558672214, 1.681707840898168937 ) ) ;
#34743=CARTESIAN_POINT ( 'NONE',  ( 5.847271748948593029, 0.6375361197438635941, -2.096799129279611762 ) ) ;
#34744=CARTESIAN_POINT ( 'NONE',  ( 5.807753868445137080, -0.5680028841938968842, 2.236484270104825089 ) ) ;
#34745=CARTESIAN_POINT ( 'NONE',  ( 1.147419824990800752, -1.624031055642958243, -1.268641727334917313 ) ) ;
#34746=CARTESIAN_POINT ( 'NONE',  ( 3.204954726155031963, -0.3781314774268499379, 1.904617838069742275 ) ) ;
#34748=CARTESIAN_POINT ( 'NONE',  ( 5.641831084104285132, 0.7588036158820666843, -1.709917670604633066 ) ) ;
#34749=CARTESIAN_POINT ( 'NONE',  ( 0.9375000000000007772, 1.451031289061083251, -1.451031289061159413 ) ) ;
#34751=CARTESIAN_POINT ( 'NONE',  ( 0.4909827745146425060, 1.656533638411663345, 0.5119339833263967243 ) ) ;
#34753=CARTESIAN_POINT ( 'NONE',  ( 4.535779832184696936, -1.617819081767550182, 1.203352566194588746 ) ) ;
#34757=CARTESIAN_POINT ( 'NONE',  ( 1.910518402784128433, 1.353611321597010253, -1.225282022559864625 ) ) ;
#34764=ADVANCED_FACE ( 'NONE', ( #56966 ), #154891, .F. ) ;
#34767=CARTESIAN_POINT ( 'NONE',  ( 0.1408863878445747453, 1.934039905153326799, 0.5823465565887532280 ) ) ;
#34768=CARTESIAN_POINT ( 'NONE',  ( 0.06529689308308950224, -1.700389599856198863, 1.266735544122286283 ) ) ;
#34773=CARTESIAN_POINT ( 'NONE',  ( 5.401267763076613271, 1.683455835520174526, 1.188505893847252581 ) ) ;
#34774=CARTESIAN_POINT ( 'NONE',  ( 5.572888750952301073, -0.9041123360693378297, 1.802415994888312722 ) ) ;
#34781=CARTESIAN_POINT ( 'NONE',  ( 4.921249881687197458, 0.7690040753521177885, 1.863882819927860535 ) ) ;
#34782=CARTESIAN_POINT ( 'NONE',  ( 4.716662652015527257, -0.08744826293657045890, 1.839185557975311358 ) ) ;
#34783=CARTESIAN_POINT ( 'NONE',  ( -0.02319159430947542386, 5.725354828811364705, -2.405035539666657840 ) ) ;
#34784=CARTESIAN_POINT ( 'NONE',  ( 3.000898454221593958, -0.6702494718498009929, -2.208213912191819617 ) ) ;
#34786=CARTESIAN_POINT ( 'NONE',  ( 4.973979902034267653, 1.240098594129716458, 1.770319513135506062 ) ) ;
#34788=CARTESIAN_POINT ( 'NONE',  ( 6.480030769895370746, -1.807141314969593848, -0.3518929191878711338 ) ) ;
#34793=CARTESIAN_POINT ( 'NONE',  ( 3.274138816734498025, -1.115311402298941656, 1.501645261301733481 ) ) ;
#34795=CARTESIAN_POINT ( 'NONE',  ( 1.705181254219298115, 1.662258477346746588, -0.9455041445245655485 ) ) ;
#34798=CARTESIAN_POINT ( 'NONE',  ( 2.807470779205251343, 1.864772411128329477, 1.179945617918669143 ) ) ;
#34803=CARTESIAN_POINT ( 'NONE',  ( 0.1925371440497048448, -0.4299567264692584212, -1.931277891087788579 ) ) ;
#34804=CARTESIAN_POINT ( 'NONE',  ( 0.4820102390354238375, 2.151571070674349606, -0.8345519191893053801 ) ) ;
#34805=CARTESIAN_POINT ( 'NONE',  ( 1.223018651738450480, -1.772137153356953432, -0.8420139538000551704 ) ) ;
#34806=CARTESIAN_POINT ( 'NONE',  ( 4.170800697546906299, 1.462118435030785646, -1.455038044888419702 ) ) ;
#34814=CARTESIAN_POINT ( 'NONE',  ( 6.215302479579098538, -1.858902078722439732, -1.121643639950772764 ) ) ;
#34816=CARTESIAN_POINT ( 'NONE',  ( 6.532758020889952277, -1.641319963461195464, 0.8346263169811756200 ) ) ;
#34818=CARTESIAN_POINT ( 'NONE',  ( 1.528351178377739927, 1.801267752838480840, 0.5040548479407629401 ) ) ;
#34823=CARTESIAN_POINT ( 'NONE',  ( 1.066890508724306130, -1.507026839618429648, 1.177014404800474479 ) ) ;
#34825=CARTESIAN_POINT ( 'NONE',  ( 3.520126680498508520, 1.123421168108656776, -1.367553765667248955 ) ) ;
#34826=CARTESIAN_POINT ( 'NONE',  ( 0.5043727151736315806, -1.897847990334254886, -0.2338014693106793551 ) ) ;
#34828=CARTESIAN_POINT ( 'NONE',  ( 3.814002402653454027, 1.021707883093534885, -1.620180217528136568 ) ) ;
#34830=CARTESIAN_POINT ( 'NONE',  ( 5.898876253247024692, 0.3825491175142159417, 1.931855958600266154 ) ) ;
#34831=CARTESIAN_POINT ( 'NONE',  ( 0.9144942500491148873, -2.120778211678171488, 0.005759991200282587286 ) ) ;
#34833=CARTESIAN_POINT ( 'NONE',  ( 3.678450976403758066, -1.802590750232490491, -0.4997190347926713794 ) ) ;
#34834=CARTESIAN_POINT ( 'NONE',  ( 1.084280211047653264, -1.780658692889337091, -0.4022698149812459212 ) ) ;
#34836=CARTESIAN_POINT ( 'NONE',  ( 3.194164748978207680, -0.8942147705085048415, 2.017778291555922809 ) ) ;
#34839=CARTESIAN_POINT ( 'NONE',  ( 0.5728089798012192535, 1.423622861147020302, -1.492835154123072883 ) ) ;
#34844=CARTESIAN_POINT ( 'NONE',  ( 6.539320575229249144, 0.007148032025052972194, 1.896977914940492393 ) ) ;
#34846=CARTESIAN_POINT ( 'NONE',  ( 3.859880467719906783, -0.6038372105774907350, 1.980330894321411517 ) ) ;
#34848=CARTESIAN_POINT ( 'NONE',  ( 1.194844697948213463, -0.5240009448631496314, -2.097013730318515456 ) ) ;
#34850=CARTESIAN_POINT ( 'NONE',  ( 1.471359524643547134, -1.733428207583002756, -1.036219422855472194 ) ) ;
#34854=CARTESIAN_POINT ( 'NONE',  ( 6.731795954091533751, -1.842168972580451536, -0.8196458303668037182 ) ) ;
#34855=CARTESIAN_POINT ( 'NONE',  ( -0.03006412033006514162, -0.9462945741195265548, 1.780671068589256834 ) ) ;
#34856=CARTESIAN_POINT ( 'NONE',  ( 6.539320575229278454, 3.689604457162498630, 2.617406275049142916 ) ) ;
#34857=CARTESIAN_POINT ( 'NONE',  ( 5.302338810847700756, 1.659911028786088760, -1.431018553749351829 ) ) ;
#34860=CARTESIAN_POINT ( 'NONE',  ( 3.111475685156277038, 1.510342251817019532, 1.173009309769344588 ) ) ;
#34864=CARTESIAN_POINT ( 'NONE',  ( 1.107046246104196552, -0.04665650516593074226, 2.016035445577879504 ) ) ;
#34866=CARTESIAN_POINT ( 'NONE',  ( 0.3984806668858055789, -0.7796899918033869392, -2.155833124811225687 ) ) ;
#34868=CARTESIAN_POINT ( 'NONE',  ( 3.680403716343355836, -1.662106674541915075, -0.4603510507015916020 ) ) ;
#34869=CARTESIAN_POINT ( 'NONE',  ( -0.1405533004718703405, 5.725074605807632722, -2.314389626777931586 ) ) ;
#34872=CARTESIAN_POINT ( 'NONE',  ( 0.9241798626423223251, 0.9638202082158978667, 1.708698881219716137 ) ) ;
#34875=CARTESIAN_POINT ( 'NONE',  ( 0.07536363704235479744, 6.947016338497881804, -2.739277465201896078 ) ) ;
#34879=CARTESIAN_POINT ( 'NONE',  ( 3.510248027248025426, -1.809562450863181127, -0.08562717191654131699 ) ) ;
#34883=CARTESIAN_POINT ( 'NONE',  ( 5.461500695664097904, -1.431772717462083566, -1.109608708211702099 ) ) ;
#34885=SURFACE_STYLE_FILL_AREA ( #1308 ) ;
#34888=ADVANCED_FACE ( 'NONE', ( #30628 ), #88478, .F. ) ;
#34889=CARTESIAN_POINT ( 'NONE',  ( 5.934019871859393724, 1.109147300373466871, 1.494279092885692606 ) ) ;
#34891=CARTESIAN_POINT ( 'NONE',  ( 4.323789496349770722, 0.8154102246901802076, -1.733521564635835732 ) ) ;
#34898=CARTESIAN_POINT ( 'NONE',  ( 0.6202742476981680797, -1.157488721396517040, -1.825510493854154426 ) ) ;
#34902=CARTESIAN_POINT ( 'NONE',  ( 0.3229203692996869823, -0.09522068211164493035, 1.823229820405058099 ) ) ;
#34904=CARTESIAN_POINT ( 'NONE',  ( 2.994927033977520914, 1.566606242385214731, -0.9370212210159311050 ) ) ;
#34906=CARTESIAN_POINT ( 'NONE',  ( 1.670022949053862948, 1.907054940702714863, -0.1439945843566131367 ) ) ;
#34908=CARTESIAN_POINT ( 'NONE',  ( 2.541402807867772840, 1.801932494976875576, -0.7955018757880153446 ) ) ;
#34909=CARTESIAN_POINT ( 'NONE',  ( 5.267111086673036624, 1.870628123453799363, -0.5216035295831971119 ) ) ;
#34912=CARTESIAN_POINT ( 'NONE',  ( 3.639029512587122372, 2.014767915268770082, 0.6618469929612482705 ) ) ;
#34922=CARTESIAN_POINT ( 'NONE',  ( 5.426323838365306074, 1.084245000580752238, -1.468710674947353967 ) ) ;
#34927=CARTESIAN_POINT ( 'NONE',  ( 6.051601594667258333, 0.5412791183288803154, -1.790613848972313571 ) ) ;
#34929=CARTESIAN_POINT ( 'NONE',  ( 3.650929903551769939, -1.574478333125122864, 1.109889904662264115 ) ) ;
#34938=CARTESIAN_POINT ( 'NONE',  ( 0.9489988177146626569, -1.915858558953801749, -0.9014485902382618487 ) ) ;
#34942=CARTESIAN_POINT ( 'NONE',  ( 6.666853767972947153, 1.538155548931797956, -1.385880503156889487 ) ) ;
#34943=CARTESIAN_POINT ( 'NONE',  ( 1.927068723821170559, -1.203646435588998420, -1.393412863611859454 ) ) ;
#34947=CARTESIAN_POINT ( 'NONE',  ( 0.9027369068667027152, 1.732534852245724233, -1.501034128341944607 ) ) ;
#34951=ORIENTED_EDGE ( 'NONE', *, *, #71220, .F. ) ;
#34953=CARTESIAN_POINT ( 'NONE',  ( 1.019790247428183472, -0.4849793317353002786, 1.953821064534920326 ) ) ;
#34954=CARTESIAN_POINT ( 'NONE',  ( 0.6023038706522118035, 1.956103482322549825, 0.1501044349687257751 ) ) ;
#34959=CARTESIAN_POINT ( 'NONE',  ( 3.908215892115148637, 1.478387765550030153, -1.478483494758761951 ) ) ;
#34960=CARTESIAN_POINT ( 'NONE',  ( 2.817004693338585941, -0.1753839976894235320, 1.761133515796961868 ) ) ;
#34964=CARTESIAN_POINT ( 'NONE',  ( 4.998102599042142380, -0.7687487195138610341, -2.159632177038037337 ) ) ;
#34965=CARTESIAN_POINT ( 'NONE',  ( 3.714586447349605081, -0.1257948980903991487, 1.735838019273880928 ) ) ;
#34968=CARTESIAN_POINT ( 'NONE',  ( 2.776348759439921654, -1.715481723685903903, 0.2504971047874882117 ) ) ;
#34969=CARTESIAN_POINT ( 'NONE',  ( 3.666621648402784484, -0.8769701800699877259, -1.986351817242467677 ) ) ;
#34971=CARTESIAN_POINT ( 'NONE',  ( 4.786342355033275986, -0.6839347017603314427, -1.897111394664739326 ) ) ;
#34972=CARTESIAN_POINT ( 'NONE',  ( 1.125000000000000888, -2.052068128417952497, 6.471134675641443159E-14 ) ) ;
#34975=CARTESIAN_POINT ( 'NONE',  ( 1.957912498325198536, 1.921386756000037055, -0.1395382256239047214 ) ) ;
#34977=CARTESIAN_POINT ( 'NONE',  ( 5.133148801814766848, 2.052693810517117079, 0.8496366593433544168 ) ) ;
#34979=CARTESIAN_POINT ( 'NONE',  ( -0.1110810684433142237, 6.948330828014858795, -2.391984312838004278 ) ) ;
#34985=CARTESIAN_POINT ( 'NONE',  ( 1.840792944257110042, 1.275724102719773434, -1.818268329069183897 ) ) ;
#34986=CARTESIAN_POINT ( 'NONE',  ( 6.303176765056641706, -1.658072099422291057, 1.048360225930293321 ) ) ;
#34989=CARTESIAN_POINT ( 'NONE',  ( 6.872354139354274416, -1.400524804419982727, 1.777693731722047588 ) ) ;
#34992=CARTESIAN_POINT ( 'NONE',  ( 4.316881300680885047, -1.530586319191833633, 1.382930202259499364 ) ) ;
#34996=CARTESIAN_POINT ( 'NONE',  ( 6.397708313642382905, -0.6301307688901837123, 1.761319926792910495 ) ) ;
#34997=CARTESIAN_POINT ( 'NONE',  ( 4.412597608232919022, -1.071937594435016683, -1.363045487976799475 ) ) ;
#34998=CARTESIAN_POINT ( 'NONE',  ( 4.598987173745545221, -0.4583060902535853187, 1.678952109248931901 ) ) ;
#35000=CARTESIAN_POINT ( 'NONE',  ( 2.437429393347473994, -1.701094670537067755, -1.536833775788006173 ) ) ;
#35002=CARTESIAN_POINT ( 'NONE',  ( 5.899963319545262763, -0.7533809947482277281, -1.950465142816688813 ) ) ;
#35003=CARTESIAN_POINT ( 'NONE',  ( 6.580031058444741454, -1.904989947508778814, -0.3762313139713204801 ) ) ;
#35005=CARTESIAN_POINT ( 'NONE',  ( 1.354138928560550292, 0.1455316553338575902, -2.011204400906742240 ) ) ;
#35010=CARTESIAN_POINT ( 'NONE',  ( 3.053504691927158898, -1.869126254513186591, 1.001442229663196182 ) ) ;
#35012=CARTESIAN_POINT ( 'NONE',  ( 5.250558533952181861, 0.5335417292645014964, 1.745990657226546894 ) ) ;
#35019=CARTESIAN_POINT ( 'NONE',  ( 3.129170305635332383, 1.827809467758968243, 0.8596994449004448091 ) ) ;
#35020=CARTESIAN_POINT ( 'NONE',  ( 6.335036379411270957, 0.2100110484798515254, 2.196758413611602290 ) ) ;
#35022=CARTESIAN_POINT ( 'NONE',  ( 3.959670595502752022, -0.5440038360976228171, 1.779617975935204655 ) ) ;
#35030=CARTESIAN_POINT ( 'NONE',  ( 1.862203476926355794, -0.5897614712949137417, 1.630587920151181924 ) ) ;
#35031=CARTESIAN_POINT ( 'NONE',  ( 1.692878195147719422, -0.5885122380313506651, 1.637943671576999272 ) ) ;
#35032=CARTESIAN_POINT ( 'NONE',  ( 0.4644773334415828736, 2.281836724062924038, -0.3429670027690605583 ) ) ;
#35035=CARTESIAN_POINT ( 'NONE',  ( 1.651711298185059684, 0.6011997390959940013, -1.971106496394055885 ) ) ;
#35038=CARTESIAN_POINT ( 'NONE',  ( 0.3685172633814579601, -0.5404119286356176000, 1.942243004588292354 ) ) ;
#35042=CARTESIAN_POINT ( 'NONE',  ( 0.5144491564793505223, 1.361202580669124584, -1.426332009298651116 ) ) ;
#35043=CARTESIAN_POINT ( 'NONE',  ( 4.429883728109570207, -1.874397765517330061, 0.3784635845696313061 ) ) ;
#35045=CARTESIAN_POINT ( 'NONE',  ( 6.428370569364434850, 1.274405893209800356, -1.801548588985131039 ) ) ;
#35050=CARTESIAN_POINT ( 'NONE',  ( 0.3112020186443940628, 1.677875239561373855, -1.123872588032665210 ) ) ;
#35052=CARTESIAN_POINT ( 'NONE',  ( 2.907580275951544113, 1.948851909871853749, 1.235431545971882095 ) ) ;
#35053=CARTESIAN_POINT ( 'NONE',  ( 4.545333077707183200, 1.753367681936630840, -0.8802267832125689750 ) ) ;
#35054=CARTESIAN_POINT ( 'NONE',  ( 0.4616703453074429975, -0.5288386019042885522, 1.889040479230045255 ) ) ;
#35058=CARTESIAN_POINT ( 'NONE',  ( 0.4447203898077173312, -1.529029696559053741, 1.464872618488068490 ) ) ;
#35061=CARTESIAN_POINT ( 'NONE',  ( 0.1636598862229492191, -1.205073137261414962, 1.392071761982638378 ) ) ;
#35062=CARTESIAN_POINT ( 'NONE',  ( 3.538082186586584577, 1.373364251514897383, 1.681533162179976060 ) ) ;
#35064=CARTESIAN_POINT ( 'NONE',  ( 1.266058358664986949, 0.6103625328083387425, -2.030891291126469600 ) ) ;
#35069=CARTESIAN_POINT ( 'NONE',  ( 2.337248977212981860, -1.842284197780035493, 0.9235709308827669828 ) ) ;
#35074=CARTESIAN_POINT ( 'NONE',  ( 0.07755575628183573877, 1.996246338214379801, -2.602582295553407032 ) ) ;
#35077=CARTESIAN_POINT ( 'NONE',  ( 4.354103434560454566, 0.8146061972254794448, -1.730223316255767196 ) ) ;
#35079=CARTESIAN_POINT ( 'NONE',  ( 1.493865258296807275, 1.713033017868152763, 1.477889207592040455 ) ) ;
#35081=CARTESIAN_POINT ( 'NONE',  ( 1.546807606353679754, 0.1796435140209233228, 1.802673299184972322 ) ) ;
#35082=CARTESIAN_POINT ( 'NONE',  ( 0.8838324889288513564, -1.915903395820263366, 0.003361870754229472590 ) ) ;
#35083=CARTESIAN_POINT ( 'NONE',  ( 2.242711981562468093, -2.029969483702593003, -0.4061203719310027549 ) ) ;
#35086=CARTESIAN_POINT ( 'NONE',  ( 0.07499057489264608634, 0.002531239327739977750, -1.955573237620360949 ) ) ;
#35087=CARTESIAN_POINT ( 'NONE',  ( 5.285741052758629266, 1.295255816434317753, 1.426247342039884014 ) ) ;
#35089=CARTESIAN_POINT ( 'NONE',  ( 0.3468381721418262731, 2.301974930567828537, 0.1634500305177730706 ) ) ;
#35092=CARTESIAN_POINT ( 'NONE',  ( 4.703617135414410733, -1.592502274362836978, -1.310920101374695168 ) ) ;
#35097=CARTESIAN_POINT ( 'NONE',  ( 5.790091041381728587, -0.9498100376258570288, 1.879691625423451029 ) ) ;
#35099=CARTESIAN_POINT ( 'NONE',  ( 0.5730174903513629570, 1.496870926018354364, -1.572904236412080436 ) ) ;
#35101=CARTESIAN_POINT ( 'NONE',  ( 5.272814564875167420, -2.033366364591123521, -0.7337546567489710014 ) ) ;
#35102=CARTESIAN_POINT ( 'NONE',  ( 5.303380940763749329, 1.780254367526274972, -0.9538449857209270188 ) ) ;
#35109=CARTESIAN_POINT ( 'NONE',  ( 3.784388871581423786, -0.6371526190629381858, -1.913262240507591416 ) ) ;
#35113=CARTESIAN_POINT ( 'NONE',  ( 5.172814640947125397, -2.034155943344346795, -0.7319064324283753864 ) ) ;
#35118=CARTESIAN_POINT ( 'NONE',  ( 6.028922772295511656, -1.701938481575874684, 1.081082441910637071 ) ) ;
#35120=CARTESIAN_POINT ( 'NONE',  ( 0.9258787065367773961, 1.030881334376580805, -1.382772916119678897 ) ) ;
#35125=CARTESIAN_POINT ( 'NONE',  ( 5.290257391050456448, -1.856285702826396156, -0.2301478561287788605 ) ) ;
#35126=CARTESIAN_POINT ( 'NONE',  ( 6.275645410888611941, 0.3399709936107355168, -1.984134265935801000 ) ) ;
#35127=CARTESIAN_POINT ( 'NONE',  ( 6.539320575229256249, 2.979067782826944288, 2.350490835693247682 ) ) ;
#35132=CARTESIAN_POINT ( 'NONE',  ( 2.157031413788193852, 0.4673396547767159070, 2.068183735011968061 ) ) ;
#35133=CARTESIAN_POINT ( 'NONE',  ( 2.319935610374638468, 0.9480221781073931986, -1.779637559903464394 ) ) ;
#35135=CARTESIAN_POINT ( 'NONE',  ( 6.086834708314957432, -0.3123483334277510348, -2.138898144987111838 ) ) ;
#35138=CARTESIAN_POINT ( 'NONE',  ( 0.6553225869628921396, 1.845336034500634437, -0.5141059209906836402 ) ) ;
#35145=CARTESIAN_POINT ( 'NONE',  ( 4.065412822539622439, 0.2671453805177248508, -2.145074402785766665 ) ) ;
#35149=CARTESIAN_POINT ( 'NONE',  ( 1.687894460584405731, 2.027760172737497424, -0.6205009303206151516 ) ) ;
#35150=CARTESIAN_POINT ( 'NONE',  ( 6.827182134110198142, 0.003888933837258023996, 1.810856214465889069 ) ) ;
#35151=CARTESIAN_POINT ( 'NONE',  ( 2.688696339244216915, -0.3334303690454739066, -1.942799078106532074 ) ) ;
#35152=CARTESIAN_POINT ( 'NONE',  ( 4.552931727387078631, 0.3324577288378940954, 1.883125075537089854 ) ) ;
#35155=CARTESIAN_POINT ( 'NONE',  ( 6.039503384146654774, 1.820429283694004141, -0.7522724601281975954 ) ) ;
#35156=CARTESIAN_POINT ( 'NONE',  ( 1.341630539043844106, 1.939701883965805562, 0.09577479888067677583 ) ) ;
#35164=CARTESIAN_POINT ( 'NONE',  ( 5.883449979803576646, 0.1360998956825946737, -1.907488392096804874 ) ) ;
#35166=CARTESIAN_POINT ( 'NONE',  ( 3.492985898914053866, -0.4302566696539159574, -2.164365734511737305 ) ) ;
#35167=CARTESIAN_POINT ( 'NONE',  ( 1.641937377912294771, -1.598774535768614280, -1.521335986861327427 ) ) ;
#35169=CARTESIAN_POINT ( 'NONE',  ( 0.2406774923011632261, 1.829974501424940891, 0.5550298453492612527 ) ) ;
#35172=CARTESIAN_POINT ( 'NONE',  ( 3.262232429473245432, -2.068111870375147987, 0.09887451149894616043 ) ) ;
#35176=CARTESIAN_POINT ( 'NONE',  ( 1.411231610350563992, 1.906656261001705488, 1.018656936289302539 ) ) ;
#35177=CARTESIAN_POINT ( 'NONE',  ( 3.861010967126535576, 0.2669419790740577558, -2.175157288012785184 ) ) ;
#35184=CARTESIAN_POINT ( 'NONE',  ( 6.363864384548370445, -0.09514871459133207587, -1.731698918886691363 ) ) ;
#35186=CARTESIAN_POINT ( 'NONE',  ( 3.959880360806608213, -0.6057208360459276353, 1.979630382156400303 ) ) ;
#35187=CARTESIAN_POINT ( 'NONE',  ( 4.482099252480286289, -2.116778089722763045, -0.05043497882678028149 ) ) ;
#35191=CARTESIAN_POINT ( 'NONE',  ( 2.975404341296074229, -0.1976578167360588389, 1.959527558586687146 ) ) ;
#35192=CARTESIAN_POINT ( 'NONE',  ( 0.3692113334803036606, -1.616751421056546789, -1.021125667832627260 ) ) ;
#35193=CARTESIAN_POINT ( 'NONE',  ( 4.277453538519633724, 1.495592673709666531, 1.737217383791799463 ) ) ;
#35194=CARTESIAN_POINT ( 'NONE',  ( 2.842213963582499670, 1.811911227886909614, 0.2232855069103783507 ) ) ;
#35200=CARTESIAN_POINT ( 'NONE',  ( 3.480730050573742851, -1.348849006198136635, 1.494714382889005488 ) ) ;
#35201=CARTESIAN_POINT ( 'NONE',  ( 4.012515129279304205, 0.7020173944642660313, 1.832041770129029468 ) ) ;
#35204=CARTESIAN_POINT ( 'NONE',  ( 0.1755611466353446948, 4.081716065625639267, -2.798746370182193743 ) ) ;
#35205=CARTESIAN_POINT ( 'NONE',  ( 0.3629773032866591143, 0.2007434131479734207, -2.081070348792604108 ) ) ;
#35206=CARTESIAN_POINT ( 'NONE',  ( 5.910986595158141732, 1.562736066445655769, 0.8308124446602130897 ) ) ;
#35208=B_SPLINE_CURVE_WITH_KNOTS ( 'NONE', 3,
 ( #35150, #86050, #1568, #135879, #116479, #100169, #50357, #152127, #31987, #17824, #83907, #49306, #149997, #98065, #33041, #213889, #167309, #67630, #133775, #65511, #148923, #199783, #99119, #165168, #496, #84980, #151072, #2634, #23160, #122922, #25311, #39435, #189948, #204032, #138017, #21018, #205114, #202977, #206190, #54618, #56758, #41597, #188880, #72984, #136952, #169433, #9069, #55680, #6907, #121836, #105528, #88190, #22078, #40521, #104446, #107708, #139087, #87115, #170494, #103371, #70835, #89274, #53551, #155323, #156399, #187808, #171562, #106624, #119682, #154263, #7985, #153185, #5837, #157473, #201899, #71908, #24228, #91413, #172653, #90330, #4759, #75143, #120766, #185669, #74074, #37298, #140168, #57818, #123980, #173734, #186744, #38366, #128258, #127183, #195301, #158528, #46931, #161742, #210460, #194220, #129324, #143380, #160662, #77267, #44802, #27447, #175859, #62098, #43729, #113049, #12258, #108775, #109844, #42666, #10125, #45865, #110906, #174800, #13333, #162807, #93545, #209379, #207261, #159589, #79407, #26376, #11188, #96757, #141253, #61023, #177989, #30674, #193151, #176912, #92490, #14384, #58890, #76200, #125045, #28527, #179055, #208320, #59950, #145524, #142310, #191000, #29602, #126106, #95688, #192066, #144457, #63159, #94618, #78335, #111986, #211524, #98869, #168126, #134594, #165991, #65267, #114123, #102061, #18657, #80477, #50114, #17576, #149750, #48005, #196365, #167065, #163876, #130375, #49054, #116235, #180115, #132467, #146575, #184358, #68467, #251, #33848, #212594, #148683, #66323, #164921, #84737, #64232, #198469, #16514, #81540, #182225, #200595, #15452, #31739, #133528, #99929, #83660, #97812, #181169, #52242, #100976, #150825, #147622, #1327, #2388, #118370, #67388, #199536, #35980, #51178, #213641, #82597, #117301, #131413, #183298, #197413, #115174, #32795, #34904, #106377, #202729, #203793, #201658, #71661, #107460, #123737, #7736, #154015, #137775, #55439, #70590, #90091, #54381, #120519, #6667, #19727, #135637, #21833, #121591, #204857, #169186, #185426, #72743, #5581, #187564, #69530, #186497, #139917, #104202, #103128, #122673, #85806, #152941, #23989, #151887, #37044, #20779, #53307, #39190, #86874, #170248, #119439, #22911, #4517, #156155, #136705, #89027, #38128, #205947, #40266, #155080, #138841, #73822, #87941, #105279, #57579, #56513, #189698, #171316, #188636, #172401, #41351, #3460, #141004, #75957, #74895, #42419, #78085, #143137, #207011, #45610, #195038, #59700, #129066, #193962, #9882, #160408, #8820, #128009, #93302, #173486, #142060, #210205, #62896, #191819, #208074, #58642, #46672, #25063, #124795, #91165, #125862, #211273, #159338, #43484, #10934, #175608, #190756, #95441, #12011, #111725, #13070, #176661, #161491, #109602, #158291, #92242, #27196, #77010, #157221, #79149, #44545, #209132, #60770, #126930, #108524, #174553, #192887, #26129, #110660, #28274, #94366, #177733, #144209, #61841, #29346, #145265, #163619, #114914, #66063, #180912, #32536, #199275, #100726, #178804, #148431, #149485, #212332, #47751, #113866, #98610, #16254, #7289, #15199, #183040, #81290, #147367, #99666, #200338, #14125, #164671, #132206, #83403, #115977, #196114, #179861, #34656, #150565, #198214, #31485, #82339, #133266, #166805, #63970, #49849, #117044 ),
 .UNSPECIFIED., .F., .F.,
 ( 4, 1, 1, 1, 1, 1, 1, 1, 1, 1, 1, 1, 1, 1, 1, 1, 1, 1, 1, 1, 1, 1, 1, 1, 1, 1, 1, 1, 1, 1, 1, 1, 1, 1, 1, 1, 1, 1, 1, 1, 1, 1, 1, 1, 1, 1, 1, 1, 1, 1, 1, 1, 1, 1, 1, 1, 1, 1, 1, 1, 1, 1, 1, 1, 1, 1, 1, 1, 1, 1, 1, 1, 1, 1, 1, 1, 1, 1, 1, 1, 1, 1, 1, 1, 1, 1, 1, 1, 1, 1, 1, 1, 1, 1, 1, 1, 1, 1, 1, 1, 1, 1, 1, 1, 1, 1, 1, 1, 1, 1, 1, 1, 1, 1, 1, 1, 1, 1, 1, 1, 1, 1, 1, 1, 1, 1, 1, 1, 1, 1, 1, 1, 1, 1, 1, 1, 1, 1, 1, 1, 1, 1, 1, 1, 1, 1, 1, 1, 1, 1, 1, 1, 1, 1, 1, 1, 1, 1, 1, 1, 1, 1, 1, 1, 1, 1, 1, 1, 1, 1, 1, 1, 1, 1, 1, 1, 1, 1, 1, 1, 1, 1, 1, 1, 1, 1, 1, 1, 1, 1, 1, 1, 1, 1, 1, 1, 1, 1, 1, 1, 1, 1, 1, 1, 1, 1, 1, 1, 1, 1, 1, 1, 1, 1, 1, 1, 1, 1, 1, 1, 1, 1, 1, 1, 1, 1, 1, 1, 1, 1, 1, 1, 1, 1, 1, 1, 1, 1, 1, 1, 1, 1, 1, 1, 1, 1, 1, 1, 1, 1, 1, 1, 1, 1, 1, 1, 1, 1, 1, 1, 1, 1, 1, 1, 1, 1, 1, 1, 1, 1, 1, 1, 1, 1, 1, 1, 1, 1, 1, 1, 1, 1, 1, 1, 1, 1, 1, 1, 1, 1, 1, 1, 1, 1, 1, 1, 1, 1, 1, 1, 1, 1, 1, 1, 1, 1, 1, 1, 1, 1, 1, 1, 1, 1, 1, 1, 1, 1, 1, 1, 1, 1, 1, 1, 1, 1, 1, 1, 1, 1, 1, 1, 1, 1, 1, 1, 1, 1, 1, 1, 1, 1, 1, 1, 1, 1, 1, 1, 1, 1, 1, 1, 1, 1, 1, 1, 1, 1, 1, 1, 1, 1, 1, 1, 1, 1, 1, 1, 1, 1, 1, 1, 1, 1, 1, 1, 1, 1, 1, 1, 1, 1, 1, 1, 4 ),
 ( 0.000000000000000000, 0.002600214693118923798, 0.005208871813129847643, 0.007813341859462101871, 0.01041561011214237054, 0.01302159838915000617, 0.01562452542669844589, 0.01822945805747129902, 0.02083332260852943998, 0.02343713088342555886, 0.02604210653276634729, 0.02864513693292065552, 0.03125071383394792401, 0.03385356881896259273, 0.03645895053148855841, 0.03906228851054763251, 0.04166670673482164577, 0.04427111720854654681, 0.04687446234244373178, 0.04947983976256019323, 0.05208269766733494843, 0.05468827385445936690, 0.05729129101459448647, 0.05989628262864687969, 0.06250008845252298662, 0.06510390268380349121, 0.06770888856031336001, 0.07031191025079500112, 0.07291748459129859805, 0.07552033970978830335, 0.07812571920045624507, 0.08072905536012038585, 0.08333347174482363950, 0.08593788071299547637, 0.08854122383090638759, 0.09114659965375219997, 0.09374945576594469199, 0.09635503022752239799, 0.09895804583665256116, 0.1015630356028039000, 0.1041668400134527495, 0.1067706523020897913, 0.1093756367037285043, 0.1119786565701353653, 0.1145842293264338063, 0.1171870828570002881, 0.1197924606432616973, 0.1223957954228293843, 0.1250002099740243899, 0.1276046175975352470, 0.1302079588893767237, 0.1328133332639841735, 0.1354161877457908392, 0.1380217606440506395, 0.1406247748629219918, 0.1432297629411592166, 0.1458335661004374617, 0.1484373766077259071, 0.1510423596945167368, 0.1536453778991425101, 0.1562509492307036785, 0.1588538013357113088, 0.1614591775772540871, 0.1640625111385781432, 0.1666669240170048083, 0.1692713304565471311, 0.1718746700842041231, 0.1744800431702197008, 0.1770828961840006377, 0.1796884676783837009, 0.1822914806691622869, 0.1848964672195632097, 0.1875002692887918765, 0.1901040781760970355, 0.1927090601080766463, 0.1953120768130981733, 0.1979176468793322763, 0.2005204977210985895, 0.2031258725775486607, 0.2057292050824250096, 0.2083336164487647746, 0.2109380218649763994, 0.2135413599902747928, 0.2161467319472901716, 0.2187495836553486062, 0.2213551539052408534, 0.2239581658300387468, 0.2265631510126252801, 0.2291669521530730058, 0.2317707595817034838, 0.2343757405188569010, 0.2369787558863956922, 0.2395843248466610342, 0.2421871745874512594, 0.2447925482183819501, 0.2473958798285567084, 0.2500002898434375842, 0.2526046943969075254, 0.2552080311816201097, 0.2578134021691782518, 0.2604162527337665622, 0.2630218218985046486, 0.2656248329193858781, 0.2682298168941298910, 0.2708336172670197106, 0.2734374233982336255, 0.2760424035005001331, 0.2786454176926287940, 0.2812509857062375773, 0.2838538345082703418, 0.2864592070732082663, 0.2890625379503836689, 0.2916669467743862043, 0.2942713506256608436, 0.2968746862315132518, 0.2994800564091141259, 0.3020829059924399762, 0.3046884742313171190, 0.3072914845103039694, 0.3098964674371332273, 0.3125002672036480411, 0.3151040721986592130, 0.3177090516259382103, 0.3203120648046862140, 0.3229176320309106729, 0.3255204800563645251, 0.3281258517147956355, 0.3307291820206363919, 0.3333335898142997245, 0.3359379931238887229, 0.3385413277125659537, 0.3411466972396727249, 0.3437495460039050044, 0.3463551134761772565, 0.3489581231752558743, 0.3515631052140602009, 0.3541669045353489920, 0.3567707085553323276, 0.3593756874674896018, 0.3619786997948497009, 0.3645842663929277916, 0.3671871138039469185, 0.3697924847153226668, 0.3723958146114617063, 0.3750002215352895019, 0.3776046244636719340, 0.3802079581968237365, 0.3828133272328684833, 0.3854161753401436075, 0.3880217422050354359, 0.3906247514861621029, 0.3932297327967993472, 0.3958335318339832876, 0.3984373350400814418, 0.4010423135969549691, 0.4036453252348887744, 0.4062508913640303643, 0.4088537383227308641, 0.4114591086464738368, 0.4140624382945181647, 0.4166668445089845574, 0.4192712472166146842, 0.4218745802558619973, 0.4244799489602520959, 0.4270827965726798348, 0.4296883629893904488, 0.4322913720144979099, 0.4348963527567997200, 0.4375001516709778882, 0.4401039542243071478, 0.4427089325857130886, 0.4453119436961573974, 0.4479175095155500941, 0.4505203561840259718, 0.4531257260795358843, 0.4557290556410732441, 0.4583334613066292196, 0.4609378639539425948, 0.4635411964608836533, 0.4661465649930071620, 0.4687494122726767465, 0.4713549784003855381, 0.4739579873313886638, 0.4765629676651664814, 0.4791667666174222462, 0.4817705686790782482, 0.4843755470048167200, 0.4869785577496898998, 0.4895841234185048796, 0.4921869699588339309, 0.4947923395854939010, 0.4973956692220981579, 0.5000000744991768276, 0.5026044772465965149, 0.5052078093828125116, 0.5078131779020444991, 0.5104160250110306718, 0.5130215910089035436, 0.5156246000077054914, 0.5182295800927568807, 0.5208333792441637300, 0.5234371809752277338, 0.5260421594250891397, 0.5286451699662961801, 0.5312507356436946271, 0.5338535822179446555, 0.5364589517351265879, 0.5390622816083643354, 0.5416666866573878192, 0.5442710896653298880, 0.5468744215923915242, 0.5494797902580997873, 0.5520826373584690749, 0.5546882033856646022, 0.5572912126141627009, 0.5598961926102767883, 0.5624999921219043797, 0.5651037936834493181, 0.5677087724172201755, 0.5703117829166597375, 0.5729173487617980065, 0.5755201955320329299, 0.5781255650991041772, 0.5807288953705399548, 0.5833333003519244331, 0.5859377037808047861, 0.5885410356602774895, 0.5911464046318289922, 0.5937492518856454238, 0.5963548181013198501, 0.5989578277214122615, 0.6015628077883760083, 0.6041666078212959423, 0.6067704093743923055, 0.6093753885518610192, 0.6119783991714310423, 0.6145839653434672645, 0.6171868124717531101, 0.6197921822480817466, 0.6223955130792849788, 0.6249999181534476866, 0.6276043221636865566, 0.6302076541571374202, 0.6328130235939036785, 0.6354158711632348355, 0.6380214377265494008, 0.6406244479001403924, 0.6432294281977445349, 0.6458332289130368498, 0.6484370306187589028, 0.6510420103997216490, 0.6536450213013255128, 0.6562505879594253688, 0.6588534356078361576, 0.6614588057527972520, 0.6640621373053481324, 0.6666665426327121891, 0.6692709473847417989, 0.6718742796537453543, 0.6744796497151083203, 0.6770824977620315543, 0.6796880648321572682, 0.6822910757211636534, 0.6848960564092084757, 0.6874998579679674204, 0.6901036599873985322, 0.6927086405316660311, 0.6953116518772185506, 0.6979172191805607106, 0.7005200675111846742, 0.7031254381841663958, 0.7057287706196612165, 0.7083331763606625087, 0.7109375820149322900, 0.7135409147210758363, 0.7161462855664346705, 0.7187491342530435423, 0.7213547019891674017, 0.7239577137555243125, 0.7265626949938263079, 0.7291664975571658935, 0.7317703000514055311, 0.7343752815188082650, 0.7369782934702413524, 0.7395838615780243597, 0.7421867107529701579, 0.7447920821133793279, 0.7473954155934371402, 0.7499998219085300954, 0.7526042286255122393, 0.7552075619304030596, 0.7578129337191791270, 0.7604157832075884027, 0.7630213517689198310, 0.7656243645745874904, 0.7682293465229839136, 0.7708331502520449074, 0.7734369533822141873, 0.7760419359326080624, 0.7786449486518774998, 0.7812505177233250997, 0.7838533679047272607, 0.7864587401119955690, 0.7890620747982641792, 0.7916664818479275390, 0.7942708897881238794, 0.7968742238533942368, 0.7994795967450375462, 0.8020824471973901915, 0.8046880167431663677, 0.8072910307501349747, 0.8098960135684915018, 0.8124998186244467568, 0.8151036225516941069, 0.8177086063449673370, 0.8203116199940584385, 0.8229171901884252405, 0.8255200415384508217, 0.8281254147520410447, 0.8307287508062024539, 0.8333331587509454907, 0.8359375680748931670, 0.8385409030622068549, 0.8411462772162020540, 0.8437491287946751184, 0.8463546994841673055, 0.8489577148544642515, 0.8515626987026798655, 0.8541665052467400931, 0.8567703101322480252, 0.8593752953283267937, 0.8619783100692604005, 0.8645838815458386506, 0.8671867342266933454, 0.8697921086061042306, 0.8723954461898817403, 0.8749998551902504751, 0.8776042660585271493, 0.8802076021295854868, 0.8828129777054576355, 0.8854158305722678035, 0.8880214025647872322, 0.8906244194604823194, 0.8932294044984951942, 0.8958332126919159588, 0.8984370186969063976, 0.9010420054557602976, 0.9036450214505988843, 0.9062505943687239052, 0.9088534485426573717, 0.9114588242474312985, 0.9140621635225948394, 0.9166665737391771485, 0.9192709863124074454, 0.9218743236289563825, 0.9244797007862803895, 0.9270825551036790957, 0.9296881285585824051, 0.9322911471418501295, 0.9348961335295734587, 0.9374999435335269471, 0.9401037508197458425, 0.9427087393012421046, 0.9453117567106092967, 0.9479173312323898593, 0.9505201870615167525, 0.9531255642405720430, 0.9557289053967781278, 0.9583333169903581750, 0.9609377312744702415, 0.9635410702737328137, 0.9661464495301401723, 0.9687493035862174695, 0.9713548794777306927, 0.9739579066090123804, 0.9765628826531806972, 0.9791666865793459129, 0.9817705523293528413, 0.9843754818126480011, 0.9869784094881522973, 0.9895843956701340094, 0.9921866610829068733, 0.9947911313000845634, 0.9973997837621362272, 1.000000000000000000 ),
 .UNSPECIFIED. ) ;
#35209=CARTESIAN_POINT ( 'NONE',  ( 1.869323357045350686, 2.096458975851514861, -0.6381942758529115522 ) ) ;
#35210=CARTESIAN_POINT ( 'NONE',  ( 0.3095773630682343569, 1.202386210327820004, -1.258585571321766627 ) ) ;
#35213=CARTESIAN_POINT ( 'NONE',  ( 0.2331713839410941569, 0.7381306520543399197, -2.038767774274966360 ) ) ;
#35214=CARTESIAN_POINT ( 'NONE',  ( 0.2227383504175127205, -0.09031333296150539924, 1.722639462886750517 ) ) ;
#35215=CARTESIAN_POINT ( 'NONE',  ( 1.195116192591906046, -1.458952948520657156, -1.775991855458454838 ) ) ;
#35216=CARTESIAN_POINT ( 'NONE',  ( 0.4159077360078728969, -1.177411712353953588, -1.848246096435968600 ) ) ;
#35217=CARTESIAN_POINT ( 'NONE',  ( 2.825073394047578734, 2.078234123670623212, 0.7428476018367863309 ) ) ;
#35218=ADVANCED_FACE ( 'NONE', ( #144156 ), #51153, .T. ) ;
#35219=CARTESIAN_POINT ( 'NONE',  ( 6.637192348400761333, -0.09982221633967082453, -2.168999452382541993 ) ) ;
#35221=CARTESIAN_POINT ( 'NONE',  ( 2.290374991995058895, -0.8151648431981967091, -1.954327666539334762 ) ) ;
#35222=CARTESIAN_POINT ( 'NONE',  ( 6.727182134110201162, 1.237345558575110083, 2.302850971298702198 ) ) ;
#35223=CARTESIAN_POINT ( 'NONE',  ( 5.192375284248013756, -1.911820684568351192, -0.2360692857661383648 ) ) ;
#35225=CARTESIAN_POINT ( 'NONE',  ( 2.788958495631514545, 1.964664059585927491, -1.180940832111162520 ) ) ;
#35230=CARTESIAN_POINT ( 'NONE',  ( 4.301594116137519741, 1.984124119141786657, -0.9988866673766303439 ) ) ;
#35237=CARTESIAN_POINT ( 'NONE',  ( 3.041638857185970046, -1.525043868314728934, 1.319228477497782714 ) ) ;
#35239=CARTESIAN_POINT ( 'NONE',  ( 0.7606827552629210620, -0.6912373536034731591, -1.943445369992405025 ) ) ;
#35244=CARTESIAN_POINT ( 'NONE',  ( 4.101666331917613206, -2.185647184384610586, 0.1603006067264350909 ) ) ;
#35245=CARTESIAN_POINT ( 'NONE',  ( 0.9322677863709986079, -1.591319861332978425, -1.238319039483272599 ) ) ;
#35246=CARTESIAN_POINT ( 'NONE',  ( 1.171164436615620863, 1.096940724416964885, 1.478650282607060662 ) ) ;
#35247=CARTESIAN_POINT ( 'NONE',  ( 4.739906352223059116, 2.286097037578460611, 0.1700548269078107355 ) ) ;
#35248=CARTESIAN_POINT ( 'NONE',  ( 2.993917163610838816, -0.5349900852187582379, -1.761688665035024304 ) ) ;
#35250=CARTESIAN_POINT ( 'NONE',  ( 3.891465932158610030, 1.322013910284997262, 1.259209046625270556 ) ) ;
#35251=CARTESIAN_POINT ( 'NONE',  ( 5.361953999179126740, -0.05229508359532940298, -2.015913028294749942 ) ) ;
#35253=CARTESIAN_POINT ( 'NONE',  ( 4.891644337148946420, 1.673267685831375307, 1.523052275532793320 ) ) ;
#35255=CARTESIAN_POINT ( 'NONE',  ( 6.211965580189116487, -2.090513352778848422, 0.2539706045930691380 ) ) ;
#35257=CARTESIAN_POINT ( 'NONE',  ( 4.000488093070094564, 2.060113009926473726, 0.2059288336104248551 ) ) ;
#35262=CARTESIAN_POINT ( 'NONE',  ( 1.822755070894378271, 1.797457900398396813, 0.6936678961073846628 ) ) ;
#35264=CARTESIAN_POINT ( 'NONE',  ( 6.666861335811934630, 1.461617314166022474, -1.320220550599479070 ) ) ;
#35268=CARTESIAN_POINT ( 'NONE',  ( 0.5629301599625028407, 0.6213668382478373386, 2.027498709647377773 ) ) ;
#35269=CARTESIAN_POINT ( 'NONE',  ( 1.529832089473160517, -0.2657924667638748017, 2.205375646708715998 ) ) ;
#35270=CARTESIAN_POINT ( 'NONE',  ( 2.977667800601135895, 2.000151994021987623, -0.6593727523046940542 ) ) ;
#35273=CARTESIAN_POINT ( 'NONE',  ( 0.3614606035443160836, -0.5022670859271642918, 1.791915111541013461 ) ) ;
#35276=( BOUNDED_CURVE ( )  B_SPLINE_CURVE ( 3, ( #185094, #118054, #103878, #166742 ),
 .UNSPECIFIED., .F., .T. ) 
 B_SPLINE_CURVE_WITH_KNOTS ( ( 4, 4 ),
 ( 0.5000000000000005551, 1.000000000000000000 ),
 .UNSPECIFIED. ) 
 CURVE ( )  GEOMETRIC_REPRESENTATION_ITEM ( )  RATIONAL_B_SPLINE_CURVE ( ( 0.9999999999999994449, 0.3333333333333334259, 0.3333333333333341475, 1.000000000000000222 ) ) 
 REPRESENTATION_ITEM ( '' )  );
#35281=CARTESIAN_POINT ( 'NONE',  ( 1.529697670087664108, -0.2543295609688834835, 2.105205558366497698 ) ) ;
#35284=CARTESIAN_POINT ( 'NONE',  ( 4.773855682050706761, -1.924389145058275963, 0.3807478752155256663 ) ) ;
#35285=CARTESIAN_POINT ( 'NONE',  ( 2.975616057669258741, 2.053088362031017855, -0.6768339029224537118 ) ) ;
#35286=CARTESIAN_POINT ( 'NONE',  ( 1.294213439101927321, 1.504999338701202394, -1.060447551955064016 ) ) ;
#35290=CARTESIAN_POINT ( 'NONE',  ( 4.101278252482940978, -1.735469017763660027, 0.1308211784099410635 ) ) ;
#35294=CARTESIAN_POINT ( 'NONE',  ( 2.079201547314021070, -0.1057080177612122196, -2.159229931372666389 ) ) ;
#35295=CARTESIAN_POINT ( 'NONE',  ( 3.005232341680406094, 2.000550758621592706, 0.2495690156183311137 ) ) ;
#35297=CARTESIAN_POINT ( 'NONE',  ( 1.780366757100563913, -1.156431984057613827, 1.826190802295484472 ) ) ;
#35299=CARTESIAN_POINT ( 'NONE',  ( 3.801606108737245471, -0.5733388152893458267, 1.886244881718708521 ) ) ;
#35300=CARTESIAN_POINT ( 'NONE',  ( 6.509000000000010999, 0.004788705324892603143, 2.000274819378269786 ) ) ;
#35301=CARTESIAN_POINT ( 'NONE',  ( 3.702622889756892022, 1.667158369460784106, 0.9958445826224509023 ) ) ;
#35306=CARTESIAN_POINT ( 'NONE',  ( -0.1106856583841086261, 0.2435294909829844312, -2.031701206977332586 ) ) ;
#35311=CARTESIAN_POINT ( 'NONE',  ( 6.791963826450252206, -0.9943653912195188349, 2.080009744879149913 ) ) ;
#35313=CARTESIAN_POINT ( 'NONE',  ( 4.276187414114787089, -1.004825795036960567, -1.684713053385626269 ) ) ;
#35314=CARTESIAN_POINT ( 'NONE',  ( 1.301407962653992501, 1.352153127569672098, -1.496052916918483744 ) ) ;
#35315=ORIENTED_EDGE ( 'NONE', *, *, #132876, .T. ) ;
#35316=CARTESIAN_POINT ( 'NONE',  ( 3.907494643824228397, -2.025022917198250560, 0.6182885518764801303 ) ) ;
#35319=CARTESIAN_POINT ( 'NONE',  ( 2.677489186553199563, -0.9463553590365642032, 1.579155189138586213 ) ) ;
#35324=CARTESIAN_POINT ( 'NONE',  ( 5.713165544288242970, 1.732532623411761286, -1.222520872474173848 ) ) ;
#35325=CARTESIAN_POINT ( 'NONE',  ( -0.1399997263889597998, 7.629137130509076492, -2.600276787041354787 ) ) ;
#35327=CARTESIAN_POINT ( 'NONE',  ( 5.852824474907069252, -1.627199953678662991, 1.264450640605979892 ) ) ;
#35330=CARTESIAN_POINT ( 'NONE',  ( 0.5196754285911856508, 1.841638447829671899, -0.2671899778997516850 ) ) ;
#35331=CARTESIAN_POINT ( 'NONE',  ( 2.630204301513817455, 0.2276190002089127917, 1.827071974840013269 ) ) ;
#35336=CARTESIAN_POINT ( 'NONE',  ( 2.737190076726934151, 0.2709513247245790013, 2.190122135706531914 ) ) ;
#35337=CARTESIAN_POINT ( 'NONE',  ( 5.395900114300756556, -0.8213888976819706533, 2.108206106441696370 ) ) ;
#35339=CARTESIAN_POINT ( 'NONE',  ( 5.080233222017616512, 0.8995743074830947483, 1.572398339973365422 ) ) ;
#35340=CARTESIAN_POINT ( 'NONE',  ( 4.803869215722607500, -1.030175745946705801, -1.614969243545740785 ) ) ;
#35343=CARTESIAN_POINT ( 'NONE',  ( 3.537922462266992252, 0.8877721971902104992, -1.760348037230663021 ) ) ;
#35344=CARTESIAN_POINT ( 'NONE',  ( 4.785944050937030347, -0.8815013282119155136, 1.649949660215948688 ) ) ;
#35346=CARTESIAN_POINT ( 'NONE',  ( 4.984723811273123140, 1.780707155018296239, 0.5408319247705763999 ) ) ;
#35350=CARTESIAN_POINT ( 'NONE',  ( 0.2160302486270138655, 1.032475520995678853, -1.731998313101141163 ) ) ;
#35352=CARTESIAN_POINT ( 'NONE',  ( 1.260533433194007236, 0.8550034467163977192, 1.924895685913818655 ) ) ;
#35356=CARTESIAN_POINT ( 'NONE',  ( 3.463236921083117981, -1.731491641549892435, 1.224000437801611163 ) ) ;
#35358=CARTESIAN_POINT ( 'NONE',  ( 1.599874016572962798, 1.395964939349272349, 1.459955266877453806 ) ) ;
#35363=CARTESIAN_POINT ( 'NONE',  ( 1.704591423195594535, -0.7763021076895926242, -2.017573427605146907 ) ) ;
#35364=CARTESIAN_POINT ( 'NONE',  ( 6.890000000000007674, 6.036127733823692054, 2.594896729422516923 ) ) ;
#35369=CARTESIAN_POINT ( 'NONE',  ( 6.456263137377813877, -1.236968576560824040, 1.593241027169020052 ) ) ;
#35371=CARTESIAN_POINT ( 'NONE',  ( 1.154151856878969928, 0.8927059368322427524, 2.001694687108931170 ) ) ;
#35374=CARTESIAN_POINT ( 'NONE',  ( 1.130147970125170431, -1.436987675322987101, -1.747601730595295333 ) ) ;
#35382=CARTESIAN_POINT ( 'NONE',  ( 3.967213729759576868, 0.2084270747255561884, -1.712163910207653128 ) ) ;
#35384=CARTESIAN_POINT ( 'NONE',  ( 1.651228947852514173, 0.5200303365089484764, -1.691588852159523704 ) ) ;
#35385=CARTESIAN_POINT ( 'NONE',  ( 3.035794076406534536, -1.939542403429166395, 0.5389024948808174287 ) ) ;
#35386=CARTESIAN_POINT ( 'NONE',  ( 5.842855468016632692, 0.4250294216477692455, 2.165293060021292515 ) ) ;
#35389=CARTESIAN_POINT ( 'NONE',  ( 4.991814629660241920, -2.006445540622634915, 0.2004526995145126111 ) ) ;
#35391=CARTESIAN_POINT ( 'NONE',  ( 2.746779440450992649, -1.556306552617524597, 1.037596984913228937 ) ) ;
#35392=CARTESIAN_POINT ( 'NONE',  ( 6.721331454403435934, -0.1262074967819451221, 1.796610827203233063 ) ) ;
#35393=CARTESIAN_POINT ( 'NONE',  ( 1.722773492080275748, 1.414811824084385661, -1.286832238068566392 ) ) ;
#35398=CARTESIAN_POINT ( 'NONE',  ( -0.1054227091227821350, -1.855472971956134920, -0.4628026090111520552 ) ) ;
#35400=CARTESIAN_POINT ( 'NONE',  ( 1.732786548908150870, -1.861864252656076912, -0.6185235971247133868 ) ) ;
#35404=CARTESIAN_POINT ( 'NONE',  ( 4.992489932941453823, -1.175987964647656536, 1.764448611491518548 ) ) ;
#35407=CARTESIAN_POINT ( 'NONE',  ( 0.2450992160058732550, -1.441561472518913867, -1.191725768352129622 ) ) ;
#35409=CARTESIAN_POINT ( 'NONE',  ( 2.232683648988046610, 1.311727534961094177, -1.527327462066043084 ) ) ;
#35412=CARTESIAN_POINT ( 'NONE',  ( 0.5798918133415768006, -0.7576680531077238934, 1.977200763303339714 ) ) ;
#35414=CARTESIAN_POINT ( 'NONE',  ( 2.945825538390862697, 1.462269270728074222, 1.465923284304726737 ) ) ;
#35418=CARTESIAN_POINT ( 'NONE',  ( 4.681631697639319079, -0.9857103537862299536, 1.843662662672640007 ) ) ;
#35420=CARTESIAN_POINT ( 'NONE',  ( 3.487140482124751362, 1.650829432287181264, -0.7796944959364560113 ) ) ;
#35421=CARTESIAN_POINT ( 'NONE',  ( 3.000440247697288676, -1.785030861869114638, -0.3072999389705335926 ) ) ;
#35423=CARTESIAN_POINT ( 'NONE',  ( 6.270183524512255246, 1.130759168108757873, 1.895055401287759178 ) ) ;
#35426=CARTESIAN_POINT ( 'NONE',  ( 5.122202071631626552, -1.176711583861598243, -1.866687997650509301 ) ) ;
#35430=CARTESIAN_POINT ( 'NONE',  ( 4.178302048780179412, 0.9043031410675538284, 1.684961085834511874 ) ) ;
#35439=CARTESIAN_POINT ( 'NONE',  ( 4.059713336928523653, 1.856696190431494475, -0.2264497139414511362 ) ) ;
#35441=CARTESIAN_POINT ( 'NONE',  ( -0.2409995289980246813, 5.721856934700204178, -2.594540323675114113 ) ) ;
#35443=CARTESIAN_POINT ( 'NONE',  ( 0.2988868148526523938, -0.2362956723594503705, -1.897694653714178781 ) ) ;
#35445=CARTESIAN_POINT ( 'NONE',  ( 0.4968415868889561882, 0.3310222599195339899, 1.941247527895247904 ) ) ;
#35446=CARTESIAN_POINT ( 'NONE',  ( 1.230092461119953517, 2.014234866427236259, 0.09611455020034495589 ) ) ;
#35451=CARTESIAN_POINT ( 'NONE',  ( 1.640847625397081622, -1.850035366842089024, 1.174371965539475093 ) ) ;
#35461=CARTESIAN_POINT ( 'NONE',  ( 3.403688466941825475, -0.7492148395099357261, -1.682118234477212537 ) ) ;
#35462=CARTESIAN_POINT ( 'NONE',  ( 0.3814940398445298420, 0.1953205766255173559, -2.003579427208526553 ) ) ;
#35463=CARTESIAN_POINT ( 'NONE',  ( 3.269240723250285363, -2.295843464198448203, 0.1100516299901241751 ) ) ;
#35465=CARTESIAN_POINT ( 'NONE',  ( 0.5142147075538996415, 0.7048593813003102282, 1.722512033545370080 ) ) ;
#35469=CARTESIAN_POINT ( 'NONE',  ( 4.447458312869024155, -1.746245811230532130, 0.7801085911468002010 ) ) ;
#35473=CARTESIAN_POINT ( 'NONE',  ( 3.878531184313998015, -0.2068018975109634505, -2.080507369234054771 ) ) ;
#35474=CARTESIAN_POINT ( 'NONE',  ( 2.623731232481395725, -1.075365945362505293, -1.530472918023266571 ) ) ;
#35477=CARTESIAN_POINT ( 'NONE',  ( 3.280519990774858119, 1.572054556770419387, -0.7471684773981291938 ) ) ;
#35482=CARTESIAN_POINT ( 'NONE',  ( 4.160587402808674007, -1.276020550970466516, 1.160787852381778062 ) ) ;
#35484=CARTESIAN_POINT ( 'NONE',  ( 6.094375512030342001, -2.195847865938059140, -0.2203403561373064590 ) ) ;
#35486=CARTESIAN_POINT ( 'NONE',  ( 3.924824802941798030, -1.462044496099848212, 1.605114832664520153 ) ) ;
#35487=CARTESIAN_POINT ( 'NONE',  ( 2.051128252772801641, -1.465761996925791122, -1.088229512710245261 ) ) ;
#35488=CARTESIAN_POINT ( 'NONE',  ( 0.4616703453074429975, -0.5288386019042885522, 1.889040479230045255 ) ) ;
#35489=CARTESIAN_POINT ( 'NONE',  ( 5.999228916948370127, -0.2569761400621084491, 2.101594505611179109 ) ) ;
#35491=CARTESIAN_POINT ( 'NONE',  ( 6.163675082799745297, 1.174783243402954591, 1.968361872208840069 ) ) ;
#35494=CARTESIAN_POINT ( 'NONE',  ( 1.805496089173063812, 1.843435535509674317, -1.047849062051921853 ) ) ;
#35501=CARTESIAN_POINT ( 'NONE',  ( 1.084998894000373637, -1.405142754555653628, 1.720412613360406295 ) ) ;
#35503=CARTESIAN_POINT ( 'NONE',  ( 6.416638760586134360, -1.319225726833603840, -1.525046029381103452 ) ) ;
#35505=CARTESIAN_POINT ( 'NONE',  ( 3.942276525692486544, -1.021014944866809326, 1.792092113122957242 ) ) ;
#35510=CARTESIAN_POINT ( 'NONE',  ( 0.4102503234837206469, 1.440240287209685111, -1.515647972008065780 ) ) ;
#35511=CARTESIAN_POINT ( 'NONE',  ( 5.151017605526480025, 0.9962996879465220168, 1.753031629501592192 ) ) ;
#35512=CARTESIAN_POINT ( 'NONE',  ( 4.142028884782995135, 0.4951553702221401232, 1.773339192993342639 ) ) ;
#35514=CARTESIAN_POINT ( 'NONE',  ( 0.6215558277854142943, -0.9165932506310509043, -1.460862699585960822 ) ) ;
#35517=CARTESIAN_POINT ( 'NONE',  ( 0.4405775615070831042, -1.946229768708742647, -1.222969628347547966 ) ) ;
#35519=CARTESIAN_POINT ( 'NONE',  ( 1.775094195334154135, -2.148033089049032895, -0.7103491116851842202 ) ) ;
#35520=CARTESIAN_POINT ( 'NONE',  ( 3.545630178961965751, -1.594748897588176950, -1.375714639268589279 ) ) ;
#35525=CARTESIAN_POINT ( 'NONE',  ( 6.531249988543854634, -0.7852927567036558365, -1.895863743163934245 ) ) ;
#35531=CARTESIAN_POINT ( 'NONE',  ( 5.484718290073375080, -1.409174384840453653, 1.717275654355006509 ) ) ;
#35532=CARTESIAN_POINT ( 'NONE',  ( 3.451304434523004172, 0.5324976444292061073, -2.125649318046138880 ) ) ;
#35535=CARTESIAN_POINT ( 'NONE',  ( 5.424254290899477304, 0.9654600744411747648, 1.707767180430696641 ) ) ;
#35537=CARTESIAN_POINT ( 'NONE',  ( 6.610000000000026965, 7.052677709320480659, 2.598153670447616470 ) ) ;
#35539=CARTESIAN_POINT ( 'NONE',  ( 4.904590598983499916, -2.104870323260544129, -0.2570220051709286579 ) ) ;
#35543=CARTESIAN_POINT ( 'NONE',  ( 6.209879897626497502, -2.145988306206991325, 0.2596296833028768347 ) ) ;
#35545=CARTESIAN_POINT ( 'NONE',  ( 4.933073973922719624, -1.305863698873997780, -1.298312775753200699 ) ) ;
#35547=CARTESIAN_POINT ( 'NONE',  ( 1.487455728203713745, -1.732000560005091616, -0.1708635279896036641 ) ) ;
#35551=CARTESIAN_POINT ( 'NONE',  ( 5.260679775997886054, -1.568431141927080219, 1.487858469166832176 ) ) ;
#35554=CARTESIAN_POINT ( 'NONE',  ( 4.645497774645744649, -1.668943667408796294, -1.373881373981879594 ) ) ;
#35556=CARTESIAN_POINT ( 'NONE',  ( 4.850830000233872674, -1.585153962374891812, 1.171817952366477344 ) ) ;
#35557=CARTESIAN_POINT ( 'NONE',  ( 4.516742233720687949, 1.733484511791906879, -0.04249706786149141935 ) ) ;
#35558=CARTESIAN_POINT ( 'NONE',  ( 0.9432342461353732110, -1.730868645791438842, -1.344178957308760802 ) ) ;
#35559=CARTESIAN_POINT ( 'NONE',  ( 2.292384291596425427, -0.9864983578860975211, 2.086231237977907327 ) ) ;
#35560=CARTESIAN_POINT ( 'NONE',  ( 5.079397637315079983, 1.924335792300538861, -0.7379084467255945246 ) ) ;
#35561=CARTESIAN_POINT ( 'NONE',  ( 0.3044966626061855752, 1.689057509992748729, 0.9581197715371556622 ) ) ;
#35564=CARTESIAN_POINT ( 'NONE',  ( -0.2110808730067274541, 0.0005491059566040365795, -1.796958327270286704 ) ) ;
#35566=CARTESIAN_POINT ( 'NONE',  ( 1.617814789376757156, 0.2004366740697149929, 2.006445999502483257 ) ) ;
#35569=CARTESIAN_POINT ( 'NONE',  ( 3.909358855915114006, 1.891329263188616938, 1.136761501516952766 ) ) ;
#35571=CARTESIAN_POINT ( 'NONE',  ( 1.340418531419234505, -1.814007083311576451, -0.4145509422008378242 ) ) ;
#35572=CARTESIAN_POINT ( 'NONE',  ( -0.02880301295725678015, 0.2243704974793322426, -2.307247863525173859 ) ) ;
#35576=CARTESIAN_POINT ( 'NONE',  ( 6.925078400183534377, -0.01048729610059369148, 2.244148362790527429 ) ) ;
#35579=CARTESIAN_POINT ( 'NONE',  ( 3.045831416509756195, 0.7432089164593397301, -1.922393172558758634 ) ) ;
#35581=UNCERTAINTY_MEASURE_WITH_UNIT (LENGTH_MEASURE( 1.000000000000000082E-05 ), #45925, 'distance_accuracy_value', 'NONE');
#35583=CARTESIAN_POINT ( 'NONE',  ( 2.649087060217536926, 0.2492969965636695762, 2.004170148778378735 ) ) ;
#35586=CARTESIAN_POINT ( 'NONE',  ( 2.219669609025213930, -1.999274383190910775, 0.4996674803129513842 ) ) ;
#35590=CARTESIAN_POINT ( 'NONE',  ( -0.2411972340276386517, 4.090764154511560058, -2.455280512047691044 ) ) ;
#35592=CARTESIAN_POINT ( 'NONE',  ( 6.024089167411393220, -1.222679950896175205, -1.837027303407394507 ) ) ;
#35594=CARTESIAN_POINT ( 'NONE',  ( 1.177287030172860183, -0.05180490295666682898, -2.161124318685260004 ) ) ;
#35596=CARTESIAN_POINT ( 'NONE',  ( 2.167204200501818612, 1.841733140229084853, -0.8216742516050157263 ) ) ;
#35598=CARTESIAN_POINT ( 'NONE',  ( 2.372814144171823791, -0.5044604469449982531, 2.242205522996820743 ) ) ;
#35602=CARTESIAN_POINT ( 'NONE',  ( 2.184254540302111636, -1.834043650784190405, -0.3674020703766100460 ) ) ;
#35603=CARTESIAN_POINT ( 'NONE',  ( 3.555875268649951959, 1.124244472066991518, 1.673854899288424347 ) ) ;
#35607=CARTESIAN_POINT ( 'NONE',  ( 5.514326386059018148, -0.9456761151771397866, -1.881892731060728519 ) ) ;
#35610=CARTESIAN_POINT ( 'NONE',  ( 6.539320575229256249, 7.052319431262985105, 2.701414634427783845 ) ) ;
#35611=CARTESIAN_POINT ( 'NONE',  ( 5.045178214694073127, 0.1526089617210572014, 2.014106518579480642 ) ) ;
#35613=CARTESIAN_POINT ( 'NONE',  ( 0.5321751443473606846, 1.184493745614173310, 1.688377367428809173 ) ) ;
#35621=CARTESIAN_POINT ( 'NONE',  ( 3.350208609569472529, -0.8826205156595956502, 1.983864470818137660 ) ) ;
#35624=CARTESIAN_POINT ( 'NONE',  ( 2.173174093899932657, 1.133995793187540180, 1.450494936146892622 ) ) ;
#35626=CARTESIAN_POINT ( 'NONE',  ( 3.931328349035985603, -1.512150646884598215, -1.586510368271301541 ) ) ;
#35627=CARTESIAN_POINT ( 'NONE',  ( 6.883263157960357148, 2.018753856957363535, 2.456789959645651500 ) ) ;
#35628=CARTESIAN_POINT ( 'NONE',  ( 4.399490234458226290, 1.814852776126129497, 1.350843829522253792 ) ) ;
#35632=CIRCLE ( 'NONE', #115343, 0.05000000000000056483 ) ;
#35635=CARTESIAN_POINT ( 'NONE',  ( 0.1273423419134401269, -1.083036363347224418, -1.400124042496312615 ) ) ;
#35636=CARTESIAN_POINT ( 'NONE',  ( 3.317044347720001785, 1.585670248135360838, -1.240117154037506886 ) ) ;
#35638=CARTESIAN_POINT ( 'NONE',  ( 1.958176110230916755, 2.100372442369624171, -0.1540336313638566157 ) ) ;
#35639=CARTESIAN_POINT ( 'NONE',  ( 1.159628707424670280, 1.142309718407741093, 1.537566464135895261 ) ) ;
#35642=CARTESIAN_POINT ( 'NONE',  ( 1.820693447614455618, -1.395048584331352703, 1.390583823087336857 ) ) ;
#35643=CARTESIAN_POINT ( 'NONE',  ( 0.6548940681232479077, -1.578012236938080015, -1.004313744925364071 ) ) ;
#35644=CARTESIAN_POINT ( 'NONE',  ( 0.6780837441340243910, -1.046368970337024473, -1.659334490400856454 ) ) ;
#35645=CARTESIAN_POINT ( 'NONE',  ( 0.01762790050853849447, -0.5081247445114078776, 1.843608005305336528 ) ) ;
#35649=CARTESIAN_POINT ( 'NONE',  ( 6.121928861531041655, -1.040746078065577063, -1.554202398018275755 ) ) ;
#35652=CARTESIAN_POINT ( 'NONE',  ( 5.752806990244247132, -0.4974732019265227234, -2.009498513695342936 ) ) ;
#35664=CARTESIAN_POINT ( 'NONE',  ( 5.353941776413853937, -0.7077614321437855072, 1.829919609802006741 ) ) ;
#35666=CARTESIAN_POINT ( 'NONE',  ( 2.636092105226188309, 0.1017362925337349233, -2.013677536115268563 ) ) ;
#35668=CARTESIAN_POINT ( 'NONE',  ( 2.202218669689899322, 1.248139960717888908, -1.453441320886917243 ) ) ;
#35671=CARTESIAN_POINT ( 'NONE',  ( 0.8377433530848135135, 0.8832496248250313320, -2.005872107257236969 ) ) ;
#35672=CARTESIAN_POINT ( 'NONE',  ( 0.1333692844072559558, 0.7140749627707367875, -2.136770008611441618 ) ) ;
#35673=CARTESIAN_POINT ( 'NONE',  ( 3.567518508692040236, 1.825626599287116791, -0.4067673385957787380 ) ) ;
#35677=CARTESIAN_POINT ( 'NONE',  ( 4.710634317702605323, 2.026528413205666013, 0.6131292256000410168 ) ) ;
#35679=CARTESIAN_POINT ( 'NONE',  ( 5.670397268163976712, -0.9275489576153757021, -1.851018422006404096 ) ) ;
#35680=CARTESIAN_POINT ( 'NONE',  ( 0.9782033901477287241, -2.040585271250746846, -0.4545043172074214599 ) ) ;
#35682=CARTESIAN_POINT ( 'NONE',  ( 0.4809449578498920519, 1.612012756419522352, -0.6139154093185476002 ) ) ;
#35692=CARTESIAN_POINT ( 'NONE',  ( 0.4163052458206939477, -0.6087807487058238820, -1.706225765549937545 ) ) ;
#35701=CARTESIAN_POINT ( 'NONE',  ( 6.011342256177334420, -1.897693555989588887, 0.6820111564242032909 ) ) ;
#35702=CARTESIAN_POINT ( 'NONE',  ( 0.8387270772249322270, 1.259995426201226953, -1.705408266269872630 ) ) ;
#35709=CARTESIAN_POINT ( 'NONE',  ( 3.713681502677267154, 0.4829771288026918907, -1.909149233777557075 ) ) ;
#35710=CARTESIAN_POINT ( 'NONE',  ( 1.418772191123615078, -0.7664089246972278779, -1.977313068770427451 ) ) ;
#35713=CARTESIAN_POINT ( 'NONE',  ( 6.727182134110202938, 2.016807574165893513, 2.492494991173601182 ) ) ;
#35715=CARTESIAN_POINT ( 'NONE',  ( 6.052700813158569559, -1.877759139263988297, -1.129571069393126459 ) ) ;
#35717=CARTESIAN_POINT ( 'NONE',  ( 3.979452554116496898, 1.814262220864255815, -0.6480193189529972475 ) ) ;
#35719=CARTESIAN_POINT ( 'NONE',  ( -0.1298852118744100725, 7.629137130509058728, -2.326516543997098729 ) ) ;
#35720=CARTESIAN_POINT ( 'NONE',  ( 1.348561525465460820, 2.204488851003219896, 0.1053889787279923829 ) ) ;
#35724=CARTESIAN_POINT ( 'NONE',  ( 6.561384255921438147, 1.635440365473137536, 1.096959908523033711 ) ) ;
#35725=CARTESIAN_POINT ( 'NONE',  ( 0.5560688330792910028, -1.405822068596472407, 1.340092691751965770 ) ) ;
#35726=CARTESIAN_POINT ( 'NONE',  ( 6.081499288503829703, 1.550124037452194958, -1.697122508851423905 ) ) ;
#35728=CARTESIAN_POINT ( 'NONE',  ( 4.153051346612735450, 1.574026050290713963, -0.9924080308383613769 ) ) ;
#35734=CARTESIAN_POINT ( 'NONE',  ( 6.720655732516647163, 3.705577233864749243, 2.340827588962008043 ) ) ;
#35735=CARTESIAN_POINT ( 'NONE',  ( 6.567919234911265391, -1.285863816539883908, 1.649083965234589000 ) ) ;
#35740=CARTESIAN_POINT ( 'NONE',  ( 0.5393321728033516615, -1.288848960320065462, -1.293324666950084190 ) ) ;
#35743=CARTESIAN_POINT ( 'NONE',  ( 2.496349097179047405, -1.714988558773246741, 0.2561001183170578677 ) ) ;
#35748=CARTESIAN_POINT ( 'NONE',  ( 6.533835636172961259, -1.196796279342365210, -1.378804128639096849 ) ) ;
#35749=CARTESIAN_POINT ( 'NONE',  ( 2.834756127989654484, -1.875839772035441388, -0.5741054328185363209 ) ) ;
#35753=CARTESIAN_POINT ( 'NONE',  ( 4.688201205076114597, 1.221562550966972527, 1.733079268972044895 ) ) ;
#35757=CARTESIAN_POINT ( 'NONE',  ( 2.465759480183654428, -0.4578044685884518072, 2.018832516862689275 ) ) ;
#35758=CARTESIAN_POINT ( 'NONE',  ( 6.827182134110246103, 3.705739211453744630, 2.325493694733235195 ) ) ;
#35760=CARTESIAN_POINT ( 'NONE',  ( 4.846434531455360073, 1.142681229152305633, -1.904705486840562179 ) ) ;
#35762=CARTESIAN_POINT ( 'NONE',  ( 2.514614159817552430, -2.143548176638510938, 0.8305585572774812908 ) ) ;
#35770=CARTESIAN_POINT ( 'NONE',  ( 3.691585721427274258, 1.799035686688513325, -0.6489376663148455071 ) ) ;
#35772=CARTESIAN_POINT ( 'NONE',  ( 3.856244308521704411, 0.6209911617112495730, 1.609288963722750765 ) ) ;
#35773=CARTESIAN_POINT ( 'NONE',  ( 3.432827581131673522, -1.645759781613131967, 1.164986487700324425 ) ) ;
#35774=CARTESIAN_POINT ( 'NONE',  ( 4.061395409788411293, -1.323216277904919691, 1.879509618897465817 ) ) ;
#35776=CARTESIAN_POINT ( 'NONE',  ( 6.393207918867057415, 1.833407501889987357, -1.036277073347695588 ) ) ;
#35778=CARTESIAN_POINT ( 'NONE',  ( 4.921055611120458195, -0.08698325021493956422, 1.767741905644197642 ) ) ;
#35780=CARTESIAN_POINT ( 'NONE',  ( 0.4281777144111223454, 1.173252442481845126, -1.969132371278771831 ) ) ;
#35781=CARTESIAN_POINT ( 'NONE',  ( -0.02988540731103071432, 0.005807295984020746475, -1.726291166677936362 ) ) ;
#35783=CARTESIAN_POINT ( 'NONE',  ( 6.714806894218784628, -0.1628439675423892508, 2.155775914164249407 ) ) ;
#35787=CARTESIAN_POINT ( 'NONE',  ( 6.848098043024292814, -0.8888149443028300345, 1.868052569137634400 ) ) ;
#35788=CARTESIAN_POINT ( 'NONE',  ( 1.358611653602972646, -1.916354379050893009, -0.6279873632355145174 ) ) ;
#35790=CARTESIAN_POINT ( 'NONE',  ( 5.057218277682078877, -1.628452160524866521, -1.029070375190293873 ) ) ;
#35792=CARTESIAN_POINT ( 'NONE',  ( 1.318920400837508167, -0.8056321388932115024, -2.070341401348996691 ) ) ;
#35800=CARTESIAN_POINT ( 'NONE',  ( 4.598987173745545221, -0.4583060902535853187, 1.678952109248931901 ) ) ;
#35801=CARTESIAN_POINT ( 'NONE',  ( 2.980854556682940082, 1.846358069237159949, 0.6635599008937702603 ) ) ;
#35807=CARTESIAN_POINT ( 'NONE',  ( 0.2388349330707796314, -2.000390574439359526, -0.5026286349697464129 ) ) ;
#35810=CARTESIAN_POINT ( 'NONE',  ( 5.471888747823221877, -0.9023485654677811940, 1.803414228490702209 ) ) ;
#35811=CARTESIAN_POINT ( 'NONE',  ( 1.253188901120566134, -1.782426524439745030, 1.393456103103172250 ) ) ;
#35814=CARTESIAN_POINT ( 'NONE',  ( 3.110468855859845672, 1.357358932127524120, -1.287316363804760888 ) ) ;
#35815=CARTESIAN_POINT ( 'NONE',  ( 1.511953044659793077, -1.632839461445406481, 0.5843666143663208690 ) ) ;
#35817=CARTESIAN_POINT ( 'NONE',  ( 5.108995794240286159, -0.3219066699026683631, 2.167653318578148358 ) ) ;
#35818=CARTESIAN_POINT ( 'NONE',  ( 5.157380949817064852, -1.946147191792221953, -1.239698497533547661 ) ) ;
#35819=CARTESIAN_POINT ( 'NONE',  ( 0.9364841293936125854, 2.030268333626069843, 0.3529954148920669277 ) ) ;
#35820=CARTESIAN_POINT ( 'NONE',  ( 3.925673184153520179, 1.037972095618071133, -1.641099617876127015 ) ) ;
#35822=CARTESIAN_POINT ( 'NONE',  ( 6.010993879215096314, 1.649516084216671397, 0.8821100558755522458 ) ) ;
#35824=CARTESIAN_POINT ( 'NONE',  ( 6.731795954091533751, -1.842168972580451314, -0.8196458303668037182 ) ) ;
#35826=CARTESIAN_POINT ( 'NONE',  ( 4.043592392309851569, -1.492256208629010761, 1.356298961253152413 ) ) ;
#35830=CARTESIAN_POINT ( 'NONE',  ( 1.840199252755945425, 1.805614550920462635, 0.2691313018618191055 ) ) ;
#35839=CARTESIAN_POINT ( 'NONE',  ( 5.461584154626091703, -1.593396655685812124, -1.240940796477793873 ) ) ;
#35840=CARTESIAN_POINT ( 'NONE',  ( 6.633471381225481522, -0.1569934505771773126, 2.186332552071496682 ) ) ;
#35843=CARTESIAN_POINT ( 'NONE',  ( 5.629779042149522184, -1.305697561153400965, -1.594503516446880154 ) ) ;
#35844=CARTESIAN_POINT ( 'NONE',  ( 4.957657809308734898, -1.899617967926207740, -0.6767155953601931007 ) ) ;
#35846=VERTEX_POINT ( 'NONE', #100693 ) ;
#35853=CARTESIAN_POINT ( 'NONE',  ( 5.343124974464078747, -1.122324884721880078, 1.674632237393176792 ) ) ;
#35854=CARTESIAN_POINT ( 'NONE',  ( 3.644333108393753573, -1.504320797718930791, 1.061230752167609204 ) ) ;
#35856=CARTESIAN_POINT ( 'NONE',  ( 2.051827946393524726, -1.855052535695273841, -1.372493790568436012 ) ) ;
#35858=CARTESIAN_POINT ( 'NONE',  ( 4.640002929648442631, 0.9288797265196678810, -1.951996720969489951 ) ) ;
#35860=CARTESIAN_POINT ( 'NONE',  ( 0.4857531807862237594, -1.927505705540471403, -0.2366729787525098105 ) ) ;
#35865=CARTESIAN_POINT ( 'NONE',  ( 3.814061661026487915, -1.881531058455442329, 1.319806432912509209 ) ) ;
#35868=CARTESIAN_POINT ( 'NONE',  ( 3.414787578387419309, 1.690673485743508619, 0.8009127983473337542 ) ) ;
#35870=CARTESIAN_POINT ( 'NONE',  ( 6.807508289679640612, -0.4357806327412223624, 1.929964574933268340 ) ) ;
#35873=CARTESIAN_POINT ( 'NONE',  ( 1.559489335033688251, -1.894147805384650995, -1.132260830144316888 ) ) ;
#35878=CARTESIAN_POINT ( 'NONE',  ( 6.807508289679640612, -0.4357806327412223624, 1.929964574933268340 ) ) ;
#35879=CARTESIAN_POINT ( 'NONE',  ( 6.709642313893407817, -0.5169605766506181199, 2.257632290342121539 ) ) ;
#35880=CARTESIAN_POINT ( 'NONE',  ( 1.820681965693775162, -1.389665069980907441, 1.385087887197037571 ) ) ;
#35881=CARTESIAN_POINT ( 'NONE',  ( 4.662968416576672048, 1.597784760895196721, -1.304382716673627707 ) ) ;
#35889=CARTESIAN_POINT ( 'NONE',  ( 6.232918786939658062, -2.059688491082920070, -0.6869823432723211054 ) ) ;
#35893=CARTESIAN_POINT ( 'NONE',  ( 1.756895065592100291, -1.601674646019658255, -0.9660157589584242865 ) ) ;
#35898=CARTESIAN_POINT ( 'NONE',  ( 1.137202173061176547, -0.04613941135153501460, 1.911881008470908361 ) ) ;
#35900=CARTESIAN_POINT ( 'NONE',  ( 2.711481306777110412, -1.750889404861367460, 0.2573583090697410536 ) ) ;
#35901=CARTESIAN_POINT ( 'NONE',  ( 1.137202173061176547, -0.04613941135153502154, 1.911881008470908139 ) ) ;
#35904=CARTESIAN_POINT ( 'NONE',  ( 4.851152330137978197, 0.1832884931825354280, -1.906798003172151867 ) ) ;
#35906=CARTESIAN_POINT ( 'NONE',  ( 5.793399386127640049, -1.781339898235247077, 0.8404781526112365952 ) ) ;
#35907=CARTESIAN_POINT ( 'NONE',  ( 1.090261293813089560, 1.267680250814690934, 1.699812782343253170 ) ) ;
#35909=CARTESIAN_POINT ( 'NONE',  ( 3.485083742438867649, 1.691615344724434200, -0.7988839237506044633 ) ) ;
#35910=CARTESIAN_POINT ( 'NONE',  ( 6.709587848829112744, -0.3662258548819911086, 1.691549535187387932 ) ) ;
#35912=CARTESIAN_POINT ( 'NONE',  ( 3.387540773601561916, 1.995160029947869340, -0.9435142334218297178 ) ) ;
#35915=CARTESIAN_POINT ( 'NONE',  ( 1.311062339077714078, -1.627386490012251663, 1.267307609633941956 ) ) ;
#35922=CARTESIAN_POINT ( 'NONE',  ( 3.068866956829822801, 1.501395149897828851, -1.425812640530661479 ) ) ;
#35924=CARTESIAN_POINT ( 'NONE',  ( 1.300320450452172594, -2.161773191439372965, -0.001381507821696103871 ) ) ;
#35926=CARTESIAN_POINT ( 'NONE',  ( 1.436200859769844129, -1.123848162932556072, -1.677891559433869473 ) ) ;
#35928=CARTESIAN_POINT ( 'NONE',  ( 0.1749903794560592751, 2.884130749173496877, -2.444045186936738112 ) ) ;
#35931=CARTESIAN_POINT ( 'NONE',  ( 6.104688764726555306, 1.790162971792093272, 0.6826718079199489697 ) ) ;
#35932=CARTESIAN_POINT ( 'NONE',  ( 6.639320575229294086, 2.948176855103799454, 2.655556053213734558 ) ) ;
#35933=CARTESIAN_POINT ( 'NONE',  ( 3.931328349035985603, -1.512150646884598215, -1.586510368271301541 ) ) ;
#35935=CARTESIAN_POINT ( 'NONE',  ( 2.988426722125224533, -1.135634098421594240, 1.538566774472991394 ) ) ;
#35939=CARTESIAN_POINT ( 'NONE',  ( 0.9664229901367871189, -1.967894173845800898, -0.4390061282484733485 ) ) ;
#35942=CARTESIAN_POINT ( 'NONE',  ( 0.7852321044731135347, 2.018311417075705272, -1.086964541883679303 ) ) ;
#35944=CARTESIAN_POINT ( 'NONE',  ( 4.576996085227628797, -0.001753933126501586170, -1.724958192235986232 ) ) ;
#35946=CARTESIAN_POINT ( 'NONE',  ( -0.1405533004718494683, 4.096626656942652822, -2.275097870671268563 ) ) ;
#35950=CARTESIAN_POINT ( 'NONE',  ( 1.047228354049560828, 1.731870006261830630, -0.9216698261682305660 ) ) ;
#35953=CARTESIAN_POINT ( 'NONE',  ( 0.07536363704233049743, 2.002983476668462881, -2.558365315478607904 ) ) ;
#35955=CARTESIAN_POINT ( 'NONE',  ( 0.3739936534635743270, -2.030981289472892026, 0.4004457479018645460 ) ) ;
#35958=CARTESIAN_POINT ( 'NONE',  ( 3.879414023784663712, 0.2179053609261162039, -1.798230022952992613 ) ) ;
#35962=CARTESIAN_POINT ( 'NONE',  ( 5.426340414154960712, -0.8198882401838718526, -1.615393417293700784 ) ) ;
#35966=CARTESIAN_POINT ( 'NONE',  ( 6.742638014206057129, -1.825417518414352180, -0.3614582840437295941 ) ) ;
#35968=CARTESIAN_POINT ( 'NONE',  ( 4.341351955572036125, 0.4158663518127497793, -1.869753321735210916 ) ) ;
#35975=CARTESIAN_POINT ( 'NONE',  ( 1.059701713109785670, 0.4209238396889225520, -2.120155868012041811 ) ) ;
#35978=CARTESIAN_POINT ( 'NONE',  ( 0.9733497034139363402, 1.760643049788807257, -0.4823509818385819936 ) ) ;
#35980=CARTESIAN_POINT ( 'NONE',  ( 3.170728842436408179, -1.686227525993441834, -0.7000332573987508855 ) ) ;
#35982=CARTESIAN_POINT ( 'NONE',  ( 1.564566645345835116, 0.6029492335615972420, 1.814891859350221459 ) ) ;
#35983=CARTESIAN_POINT ( 'NONE',  ( 2.471101528187972463, 1.758070753236480988, 0.8880565435460830992 ) ) ;
#35984=CARTESIAN_POINT ( 'NONE',  ( 3.702622889756892022, 1.667158369460784106, 0.9958445826224509023 ) ) ;
#35987=CARTESIAN_POINT ( 'NONE',  ( 4.113620189327307664, 1.705085180707970771, 1.260635662952174663 ) ) ;
#35994=CARTESIAN_POINT ( 'NONE',  ( 3.791466046568803705, 1.323482414808102137, 1.257835202898072380 ) ) ;
#35999=CARTESIAN_POINT ( 'NONE',  ( 4.996879044411707937, 1.554903924810165705, -1.039696167511289238 ) ) ;
#36001=CARTESIAN_POINT ( 'NONE',  ( 3.299358975845566810, 1.519210379524044585, 1.184558777233129412 ) ) ;
#36002=CARTESIAN_POINT ( 'NONE',  ( 6.192239757033616065, 0.9699301198475211994, -1.705161095427814466 ) ) ;
#36009=CARTESIAN_POINT ( 'NONE',  ( 1.177538910780148385, 1.606043500598727247, 1.379722209976147251 ) ) ;
#36013=CARTESIAN_POINT ( 'NONE',  ( 6.403194803628889709, -1.752124481401344358, 1.102429006916323395 ) ) ;
#36014=CARTESIAN_POINT ( 'NONE',  ( 0.8723036553972834950, -0.04505207493780280514, -1.840872848514919502 ) ) ;
#36016=CARTESIAN_POINT ( 'NONE',  ( 6.451773728000877561, -2.099535003536470157, -0.9362560538537908483 ) ) ;
#36020=CARTESIAN_POINT ( 'NONE',  ( 1.025772235718758196, -1.457823864038493733, -1.768965695191491827 ) ) ;
#36023=CARTESIAN_POINT ( 'NONE',  ( 5.753840666697315420, 0.7890659797671593090, 1.774590222461839506 ) ) ;
#36026=CARTESIAN_POINT ( 'NONE',  ( 0.4572897223803442102, -1.724499148370229218, 1.038616540587710357 ) ) ;
#36027=CARTESIAN_POINT ( 'NONE',  ( 6.438686429976131720, -1.555646628146038157, 1.282773817382940162 ) ) ;
#36031=CARTESIAN_POINT ( 'NONE',  ( 2.888710413438722924, 1.792813287458893790, -1.075199139784080771 ) ) ;
#36032=CARTESIAN_POINT ( 'NONE',  ( 2.799370285489965138, -0.5572909556486020932, 1.679871745949900408 ) ) ;
#36035=CARTESIAN_POINT ( 'NONE',  ( 5.033284615878021562, -1.618354306187347769, -1.623638663579999752 ) ) ;
#36036=CARTESIAN_POINT ( 'NONE',  ( 3.573892692743201760, -1.677664982382242931, -0.4625120326062928111 ) ) ;
#36039=CARTESIAN_POINT ( 'NONE',  ( 3.813592814792550190, -1.418126570600848124, 0.9972168832048341480 ) ) ;
#36040=CARTESIAN_POINT ( 'NONE',  ( 3.561125603554469610, 1.713606050895712718, -1.333181090037469652 ) ) ;
#36042=CARTESIAN_POINT ( 'NONE',  ( 4.452361426671761713, -1.313546101436880109, 1.530156479064001207 ) ) ;
#36043=CARTESIAN_POINT ( 'NONE',  ( 1.375000000000000888, 2.052068128417951609, -7.865587939079325464E-14 ) ) ;
#36045=CARTESIAN_POINT ( 'NONE',  ( 2.045805558669851365, 0.7393754583576680472, -1.779040955004469904 ) ) ;
#36047=CARTESIAN_POINT ( 'NONE',  ( 5.379204547434111028, -2.008251482569714419, -0.9497353344293004707 ) ) ;
#36049=CARTESIAN_POINT ( 'NONE',  ( -0.1108833634137010304, 6.948331553507800962, -2.491992042620773340 ) ) ;
#36054=CARTESIAN_POINT ( 'NONE',  ( 0.1006276693296826175, -1.041319732255343355, 1.962097497535258084 ) ) ;
#36055=CARTESIAN_POINT ( 'NONE',  ( 6.092239754786219486, 0.9682357284593717806, -1.706234036142616928 ) ) ;
#36058=CARTESIAN_POINT ( 'NONE',  ( 0.1753634416057497925, 0.0001173177735149660839, -2.144164757042037017 ) ) ;
#36059=CLOSED_SHELL ( 'NONE', ( #159368, #23887, #44999, #191268, #113541, #202502, #41438, #160091 ) ) ;
#36062=CARTESIAN_POINT ( 'NONE',  ( 4.492669715648281326, 2.022274968565600517, 0.4054665169595774721 ) ) ;
#36066=CARTESIAN_POINT ( 'NONE',  ( 5.659403934932580427, 0.3656299861228041181, -1.834283699791404043 ) ) ;
#36067=CARTESIAN_POINT ( 'NONE',  ( 4.271880269886525916, 1.546599990029189575, -0.7845881139060503218 ) ) ;
#36068=CARTESIAN_POINT ( 'NONE',  ( 3.192619200838729743, 1.373927285412982036, 1.068286041690246657 ) ) ;
#36070=CARTESIAN_POINT ( 'NONE',  ( 2.367065275503206667, 0.1088462660112088087, -2.289894902259086429 ) ) ;
#36072=CARTESIAN_POINT ( 'NONE',  ( 5.689037021386003090, 1.583751769416761324, 1.365026519206056665 ) ) ;
#36073=CARTESIAN_POINT ( 'NONE',  ( 0.04061758243546764735, -1.421021341975825969, -1.170429047309962112 ) ) ;
#36075=CARTESIAN_POINT ( 'NONE',  ( 1.529922885524274134, -1.701946718671920600, 1.081067414773040802 ) ) ;
#36076=CARTESIAN_POINT ( 'NONE',  ( 0.05887529153619439071, -1.959562692596405364, -0.9812908054248059564 ) ) ;
#36080=CARTESIAN_POINT ( 'NONE',  ( 2.561320117580662803, -1.761587792986643475, 1.180070990429403555 ) ) ;
#36082=CARTESIAN_POINT ( 'NONE',  ( 5.971303284387838417, 0.1295235881030691594, -1.821162830480331563 ) ) ;
#36087=CARTESIAN_POINT ( 'NONE',  ( 2.267837486342203057, 0.5347344578308220742, -1.947668537691170876 ) ) ;
#36088=CARTESIAN_POINT ( 'NONE',  ( 0.09494852110062798611, -0.4603312545960658864, -2.062269868324863253 ) ) ;
#36090=CARTESIAN_POINT ( 'NONE',  ( 4.082723863713003887, 1.765846151219726101, 0.5873946967244033646 ) ) ;
#36099=CARTESIAN_POINT ( 'NONE',  ( 1.528208422804043121, 1.709223377337875549, -0.2899604983128030722 ) ) ;
#36100=CARTESIAN_POINT ( 'NONE',  ( 1.288542162703592231, 1.315766340102142662, 1.139191825253932366 ) ) ;
#36101=CARTESIAN_POINT ( 'NONE',  ( 5.127664261384059508, -2.192653808335935928, 0.7197182627937804833 ) ) ;
#36104=CARTESIAN_POINT ( 'NONE',  ( 1.458354148090333258, 0.8324554894755629153, 1.885337613027091352 ) ) ;
#36107=CARTESIAN_POINT ( 'NONE',  ( 6.784486029815019137, -2.232095771774603055, 0.5478248251382932255 ) ) ;
#36111=CARTESIAN_POINT ( 'NONE',  ( 0.4617158845385913590, 1.950347379310466422, -0.2869839225536646166 ) ) ;
#36113=CARTESIAN_POINT ( 'NONE',  ( 4.007995338699682719, -0.7271224857151190601, 1.768968726348684406 ) ) ;
#36115=CARTESIAN_POINT ( 'NONE',  ( 6.006501602161061548, -0.7906231143557163055, -2.060575041408031272 ) ) ;
#36120=CARTESIAN_POINT ( 'NONE',  ( -0.07552420640595960966, -0.8660980012666683603, -1.823048286210580793 ) ) ;
#36122=CARTESIAN_POINT ( 'NONE',  ( 3.259088711995949517, -1.748676463734340603, 1.505793948229345869 ) ) ;
#36123=CARTESIAN_POINT ( 'NONE',  ( 4.721123852359588646, -1.751549048416237486, -0.8839179009662299080 ) ) ;
#36124=CARTESIAN_POINT ( 'NONE',  ( 0.3913574919355842785, -1.795980968407092426, 0.7896611536716554580 ) ) ;
#36127=CARTESIAN_POINT ( 'NONE',  ( 0.3041147963815365451, -1.138459102943665036, -1.785081232699109233 ) ) ;
#36132=CARTESIAN_POINT ( 'NONE',  ( 3.450208493196211812, -0.8844140035146315082, 1.982955601465713258 ) ) ;
#36134=CARTESIAN_POINT ( 'NONE',  ( 0.6156802735862785259, 1.737094954450137285, 1.216079458918501333 ) ) ;
#36139=CARTESIAN_POINT ( 'NONE',  ( 2.020846523693183627, 1.921700534952670791, 0.7446803044362272361 ) ) ;
#36146=CARTESIAN_POINT ( 'NONE',  ( 4.652931681422667332, 0.3304644650514582116, 1.883354098946861344 ) ) ;
#36148=CARTESIAN_POINT ( 'NONE',  ( 0.4216216942964992609, -0.1093418885590720091, 2.259903825829346680 ) ) ;
#36151=CARTESIAN_POINT ( 'NONE',  ( 1.458926887072587553, -1.529292093677349307, 0.9708203095366783053 ) ) ;
#36153=CARTESIAN_POINT ( 'NONE',  ( 0.7607752342545861524, -0.05021853532924521607, -1.915246365852550037 ) ) ;
#36154=CARTESIAN_POINT ( 'NONE',  ( 1.434126425884488354, 1.231690216755284562, 1.664001042209894088 ) ) ;
#36156=CARTESIAN_POINT ( 'NONE',  ( 6.754772315933175619, -1.444328698515121800, 1.188528157999017454 ) ) ;
#36157=CARTESIAN_POINT ( 'NONE',  ( 5.496683133134654398, -0.4700625557551000866, -1.868158488084943780 ) ) ;
#36158=CARTESIAN_POINT ( 'NONE',  ( 0.03047818801908425135, -1.425887938121385590, -1.815451699675968644 ) ) ;
#36161=CARTESIAN_POINT ( 'NONE',  ( 3.807127647779250168, -1.688003362470591684, 1.185206751978077788 ) ) ;
#36166=CARTESIAN_POINT ( 'NONE',  ( 5.034254431704021648, 1.084988065057530982, -1.804815602348212256 ) ) ;
#36170=CARTESIAN_POINT ( 'NONE',  ( 6.021949436824264978, 2.040384406434097464, -0.3501103912618847014 ) ) ;
#36172=CARTESIAN_POINT ( 'NONE',  ( 4.727887898869392203, -1.325758432718616042, -1.707240035374466114 ) ) ;
#36173=CARTESIAN_POINT ( 'NONE',  ( 4.688151973431080144, 1.164670015804763370, 1.649827500200540253 ) ) ;
#36180=CARTESIAN_POINT ( 'NONE',  ( 3.415250174187448362, -1.861344788686780438, 0.7762291900053899241 ) ) ;
#36185=CARTESIAN_POINT ( 'NONE',  ( 6.720655732516647163, 2.019696082639847567, 2.477441386028636394 ) ) ;
#36187=CARTESIAN_POINT ( 'NONE',  ( 4.763296089436113157, 1.880429982106451181, -0.7283946704290320540 ) ) ;
#36189=CARTESIAN_POINT ( 'NONE',  ( 0.1699431646460221601, -1.131269863993559222, 1.302202208916112269 ) ) ;
#36194=CARTESIAN_POINT ( 'NONE',  ( 5.993391575003322203, 1.416176893967495687, 1.222094818194748189 ) ) ;
#36195=CARTESIAN_POINT ( 'NONE',  ( 6.416276891523604142, -2.012660772237227391, 0.05378525197091872656 ) ) ;
#36200=CARTESIAN_POINT ( 'NONE',  ( 0.1402502066264778580, 0.7743353953559418690, 1.862009890338502505 ) ) ;
#36201=CARTESIAN_POINT ( 'NONE',  ( 1.177659378823514791, 1.784474613499857032, -0.3112490768260189333 ) ) ;
#36203=CARTESIAN_POINT ( 'NONE',  ( 5.840740251263128791, 0.4172088472891195554, 2.120894824392767664 ) ) ;
#36206=CARTESIAN_POINT ( 'NONE',  ( 0.6201578395632812990, 1.887877179178775400, 0.3243255173654129297 ) ) ;
#36208=DIRECTION ( 'NONE',  ( 1.014813233446432150E-15, 1.000000000000000000, -4.583713267641621330E-32 ) ) ;
#36214=CARTESIAN_POINT ( 'NONE',  ( 3.678741886385179072, -2.082744454470350615, -0.5786317199799120292 ) ) ;
#36217=CARTESIAN_POINT ( 'NONE',  ( 1.143014088299774578, 2.045220145331683614, 0.5602274146137007360 ) ) ;
#36219=CARTESIAN_POINT ( 'NONE',  ( 2.266812238764161158, -1.800804572728794239, -0.8025143323158872022 ) ) ;
#36220=CARTESIAN_POINT ( 'NONE',  ( 4.271672842113056312, 0.4137096367802223784, -1.866957553337177611 ) ) ;
#36223=CARTESIAN_POINT ( 'NONE',  ( 6.197704753879455630, -1.425424270160932094, -1.359389694413483562 ) ) ;
#36224=CARTESIAN_POINT ( 'NONE',  ( 0.9197484630441244979, 1.157134895311136669, -1.559417598425276719 ) ) ;
#36231=CARTESIAN_POINT ( 'NONE',  ( 4.899028947338643469, -0.2378672112019977747, -1.897373119303269018 ) ) ;
#36233=CARTESIAN_POINT ( 'NONE',  ( 3.334799921508072806, 2.153101868192684343, 0.4835390122766567433 ) ) ;
#36234=CARTESIAN_POINT ( 'NONE',  ( 2.397764582540245382, 1.705505620506567510, 1.400368488499253994 ) ) ;
#36236=CARTESIAN_POINT ( 'NONE',  ( 0.4164788467995067522, -0.6444665046171775824, -1.800526059235994403 ) ) ;
#36237=CARTESIAN_POINT ( 'NONE',  ( -0.02319159430947542386, 5.725354828811364705, -2.405035539666657840 ) ) ;
#36240=CARTESIAN_POINT ( 'NONE',  ( 3.121598655985452275, 0.3063859900464052100, -2.047459029603612368 ) ) ;
#36244=CARTESIAN_POINT ( 'NONE',  ( 0.7960496800812133511, -0.7770375076890515542, 2.017388685454111652 ) ) ;
#36245=CARTESIAN_POINT ( 'NONE',  ( 2.859115728684503477, 0.3189004193784421015, -2.168101852914063876 ) ) ;
#36252=CARTESIAN_POINT ( 'NONE',  ( 6.100242454504600786, -0.2022020391262440986, 1.722246827497366795 ) ) ;
#36254=CARTESIAN_POINT ( 'NONE',  ( 3.678634981485491728, 1.317094234756083893, -1.597214816249421743 ) ) ;
#36255=CARTESIAN_POINT ( 'NONE',  ( 4.236029508982094072, 2.116713919566749702, -0.05380437090627546853 ) ) ;
#36259=CARTESIAN_POINT ( 'NONE',  ( 2.922656654487673311, -1.361644196593906342, 1.423118114318456584 ) ) ;
#36261=CARTESIAN_POINT ( 'NONE',  ( 0.9317291061951762376, -1.865162313430932750, 0.4216105838140621342 ) ) ;
#36262=CARTESIAN_POINT ( 'NONE',  ( 4.804755513996577854, 1.992766236949112812, 1.132715491657744877 ) ) ;
#36263=CARTESIAN_POINT ( 'NONE',  ( 2.719161800852238464, -0.1789327596440904167, 1.816892639718168168 ) ) ;
#36268=CARTESIAN_POINT ( 'NONE',  ( 4.500248159151196248, -0.9453760218497176959, 1.777399672076788617 ) ) ;
#36270=CARTESIAN_POINT ( 'NONE',  ( 4.557442073745519018, 1.573120015848201492, 1.171846803954358363 ) ) ;
#36273=CARTESIAN_POINT ( 'NONE',  ( 0.1753634416057741896, 2.865130778691078905, -2.632309609290182095 ) ) ;
#36274=CARTESIAN_POINT ( 'NONE',  ( 0.09931936810910445279, -0.5537021472524807919, 2.016037456109684989 ) ) ;
#36275=CARTESIAN_POINT ( 'NONE',  ( 5.313276456144085280, -0.2569279779609782155, 1.750970204404985964 ) ) ;
#36277=CARTESIAN_POINT ( 'NONE',  ( 1.394752248596371702, 1.789971953256053627, -1.264032476404143512 ) ) ;
#36278=CARTESIAN_POINT ( 'NONE',  ( 6.193256023596829252, -0.5794974496134881470, 1.641157367357688246 ) ) ;
#36280=CARTESIAN_POINT ( 'NONE',  ( 0.1333692844072559558, 0.7140749627707367875, -2.136770008611441618 ) ) ;
#36281=CARTESIAN_POINT ( 'NONE',  ( 0.8028309281867166414, 1.407482529003287075, 0.9968052580264019635 ) ) ;
#36282=CARTESIAN_POINT ( 'NONE',  ( 0.1874131419884322858, 1.628132678060219884, 1.467219630700428157 ) ) ;
#36283=CARTESIAN_POINT ( 'NONE',  ( 6.573613466494099278, 1.281508381366827765, -1.168108599551227478 ) ) ;
#36284=CARTESIAN_POINT ( 'NONE',  ( 3.352369063006555905, 2.207063162671081713, 4.936380160885933677E-05 ) ) ;
#36285=CARTESIAN_POINT ( 'NONE',  ( 6.509000000000012776, 0.004788705324892602276, 2.000274819378269342 ) ) ;
#36286=CARTESIAN_POINT ( 'NONE',  ( 6.877413710614480813, -0.1567828624706164298, 2.136824976188213654 ) ) ;
#36288=CARTESIAN_POINT ( 'NONE',  ( 0.7084050413898737020, 1.255986415914780885, -1.704487872487458144 ) ) ;
#36291=CARTESIAN_POINT ( 'NONE',  ( 6.053727987682750999, 0.5585614288021992779, -1.843621721047507878 ) ) ;
#36294=CARTESIAN_POINT ( 'NONE',  ( 1.628911237561550873, 0.2300632485819526785, 2.280818132175948421 ) ) ;
#36298=CARTESIAN_POINT ( 'NONE',  ( 3.879691667246706110, 0.2712996660018602846, -2.204593333604548455 ) ) ;
#36304=CARTESIAN_POINT ( 'NONE',  ( 1.688125190044654556, 1.678006053171029688, 1.117831401076685660 ) ) ;
#36306=CARTESIAN_POINT ( 'NONE',  ( 1.077094301713815039, 1.904230998939509867, 0.7929820198450258095 ) ) ;
#36311=CARTESIAN_POINT ( 'NONE',  ( 3.802820697025221630, 1.879323313303274734, 1.126966401794778250 ) ) ;
#36312=CARTESIAN_POINT ( 'NONE',  ( 0.9146856577476671912, -1.281363086869342194, -1.556907195799726917 ) ) ;
#36313=CARTESIAN_POINT ( 'NONE',  ( 0.6789530235665336422, 1.236279375446739603, 1.364625092910062953 ) ) ;
#36314=CARTESIAN_POINT ( 'NONE',  ( 5.249693134425458041, 2.289860626911474739, -0.1101728261837572470 ) ) ;
#36315=CARTESIAN_POINT ( 'NONE',  ( 3.468544592087896561, 0.04396668885017079864, -1.840778273432375212 ) ) ;
#36318=CARTESIAN_POINT ( 'NONE',  ( 3.680510133705969800, -1.759192178946006990, -0.4875382671739314500 ) ) ;
#36319=CARTESIAN_POINT ( 'NONE',  ( 5.115861365725078436, 0.1511377038382749338, 2.010826595755777824 ) ) ;
#36321=CARTESIAN_POINT ( 'NONE',  ( 4.786124093267453361, -1.070777880904892232, 1.993102913963458400 ) ) ;
#36323=CARTESIAN_POINT ( 'NONE',  ( 6.475619172616331909, 2.016361193322095957, -0.6077647485315963438 ) ) ;
#36325=CARTESIAN_POINT ( 'NONE',  ( 3.314952806421948672, -1.569539724514938950, 1.350292352848787569 ) ) ;
#36330=CARTESIAN_POINT ( 'NONE',  ( 1.541497387563552479, -1.395045264726347600, -1.328863961831990181 ) ) ;
#36333=CARTESIAN_POINT ( 'NONE',  ( 0.4144234639597261238, 0.7504023841088992564, 1.821203888109582447 ) ) ;
#36338=CARTESIAN_POINT ( 'NONE',  ( 1.635333617853749200, 2.074933741853498770, 0.7937918740310870858 ) ) ;
#36339=CARTESIAN_POINT ( 'NONE',  ( 3.645630060059632083, -1.593344849414342290, -1.377153647973597073 ) ) ;
#36342=CARTESIAN_POINT ( 'NONE',  ( 0.9767415019392856612, 1.717539547389279830, 0.7171521658363362306 ) ) ;
#36347=CARTESIAN_POINT ( 'NONE',  ( 1.775790443353560732, 0.3575140072833470906, -2.090081039791711337 ) ) ;
#36350=CARTESIAN_POINT ( 'NONE',  ( 4.510177812457000002, 1.961482754637720927, -0.04604004567236585910 ) ) ;
#36351=CARTESIAN_POINT ( 'NONE',  ( 3.010779355932476253, 1.566693023359872372, -1.489686202715050145 ) ) ;
#36352=CARTESIAN_POINT ( 'NONE',  ( 1.522747961674526085, -1.733470594775164075, 0.6210259959333885860 ) ) ;
#36356=CARTESIAN_POINT ( 'NONE',  ( 4.435344831996881787, 0.7407458870649418214, -1.574957418989342939 ) ) ;
#36361=CARTESIAN_POINT ( 'NONE',  ( 1.516726440323381331, 1.451591637995581996, -1.601975981646540426 ) ) ;
#36364=CARTESIAN_POINT ( 'NONE',  ( 3.427111092251767133, 0.9039706872599994059, 1.802141633730186543 ) ) ;
#36366=CARTESIAN_POINT ( 'NONE',  ( 0.7784641540938314064, -1.199969256800371697, 1.797863220954009966 ) ) ;
#36367=CARTESIAN_POINT ( 'NONE',  ( 3.151204110225252819, -1.610897424746060791, -1.136263970179009819 ) ) ;
#36368=CARTESIAN_POINT ( 'NONE',  ( 6.609000000000015973, 2.967897204652646614, 2.453190122791535366 ) ) ;
#36369=CARTESIAN_POINT ( 'NONE',  ( 3.790518096397344383, 1.638939831120878932, -1.041601972383674468 ) ) ;
#36374=CARTESIAN_POINT ( 'NONE',  ( -0.1106856583841242386, 6.948332279000682732, -2.591999772403537516 ) ) ;
#36380=CARTESIAN_POINT ( 'NONE',  ( 0.1478802723770406002, -1.707511933842900564, -1.397569297917726550 ) ) ;
#36382=CARTESIAN_POINT ( 'NONE',  ( 3.977359813172594905, -0.1486911861427446802, 1.956209631609528099 ) ) ;
#36384=CARTESIAN_POINT ( 'NONE',  ( 1.758435621656749603, 1.928751379572872571, -0.5880216644931559600 ) ) ;
#36386=CARTESIAN_POINT ( 'NONE',  ( 3.098929814713128561, 1.916056983672033587, 0.9012583305440853287 ) ) ;
#36388=CARTESIAN_POINT ( 'NONE',  ( 0.1747926744264677590, 2.047238405490480861, -2.272669950590770149 ) ) ;
#36390=CARTESIAN_POINT ( 'NONE',  ( 2.993917163610838816, -0.5349900852187582379, -1.761688665035024304 ) ) ;
#36394=CARTESIAN_POINT ( 'NONE',  ( 4.219064148821600746, 1.637239594409030330, -1.347683705884415106 ) ) ;
#36398=CARTESIAN_POINT ( 'NONE',  ( 5.694623797941932963, -0.4965738858758206309, -1.999944147208564171 ) ) ;
#36399=CARTESIAN_POINT ( 'NONE',  ( 0.8712809235682484887, -0.2783187086575014679, 1.840006102165496982 ) ) ;
#36400=CARTESIAN_POINT ( 'NONE',  ( 2.173174093899932657, 1.133995793187540180, 1.450494936146892622 ) ) ;
#36406=CARTESIAN_POINT ( 'NONE',  ( 2.508667999599442755, -0.8457060194008919618, -2.038605049697986615 ) ) ;
#36407=CARTESIAN_POINT ( 'NONE',  ( 4.903763976872734354, -0.6097993234682648200, 2.178603239016148052 ) ) ;
#36409=CARTESIAN_POINT ( 'NONE',  ( 4.974790932252576958, -1.306838681284767212, 1.254843474919357105 ) ) ;
#36410=CARTESIAN_POINT ( 'NONE',  ( 4.329236433732988942, -1.484621416154695117, -1.210779873830228670 ) ) ;
#36412=CARTESIAN_POINT ( 'NONE',  ( 3.432457938460992342, 1.923125764579440844, 0.4332125842720236375 ) ) ;
#36413=CARTESIAN_POINT ( 'NONE',  ( 5.524238439434661530, 1.113281918156138639, -1.503147240406087271 ) ) ;
#36414=CARTESIAN_POINT ( 'NONE',  ( 5.195690723081275664, -1.315925274417349522, -1.316268238436297144 ) ) ;
#36417=CARTESIAN_POINT ( 'NONE',  ( 0.04025042243083893495, 0.7762349914572730381, 1.861342399428978389 ) ) ;
#36419=CARTESIAN_POINT ( 'NONE',  ( 2.262461133243711675, 0.9012960022399997273, 1.903611236745775814 ) ) ;
#36424=CARTESIAN_POINT ( 'NONE',  ( 0.07479286986305544449, 2.888457405263197941, -2.344396930208477947 ) ) ;
#36425=CARTESIAN_POINT ( 'NONE',  ( 3.480829117359967917, -1.421471314662653196, 1.573842340227212366 ) ) ;
#36427=CARTESIAN_POINT ( 'NONE',  ( 1.617450697425420802, 1.681603173096592796, 1.118491831857356456 ) ) ;
#36433=CARTESIAN_POINT ( 'NONE',  ( 2.565889408427945995, 2.120439650033152379, -0.4189318973958494619 ) ) ;
#36434=CARTESIAN_POINT ( 'NONE',  ( 6.890000000000025437, 1.315307137738566556, 1.839292676857922304 ) ) ;
#36442=CARTESIAN_POINT ( 'NONE',  ( 1.400213348495438437, -0.7931047570679079506, -2.043190674350242819 ) ) ;
#36444=CARTESIAN_POINT ( 'NONE',  ( 1.762946358529001056, -1.599227303849257043, 1.600698272852623338 ) ) ;
#36451=CARTESIAN_POINT ( 'NONE',  ( 3.685938805993322909, -0.8483273805379875077, 1.501759545097125059 ) ) ;
#36453=CARTESIAN_POINT ( 'NONE',  ( 2.442341840454059554, 0.3829199517304190947, 1.727643488062768240 ) ) ;
#36454=CARTESIAN_POINT ( 'NONE',  ( 2.860023507607223792, 0.7224298503675909977, -1.879176508647899535 ) ) ;
#36455=CARTESIAN_POINT ( 'NONE',  ( 5.860442804830619856, 0.8892231252738895808, 2.019869304780027353 ) ) ;
#36457=CARTESIAN_POINT ( 'NONE',  ( 4.043226763451240657, 0.1031935428237283348, 2.017299519520795670 ) ) ;
#36459=CARTESIAN_POINT ( 'NONE',  ( 3.480092364642515701, -2.014234743589532695, -0.09611699103692641910 ) ) ;
#36460=CARTESIAN_POINT ( 'NONE',  ( 4.394648900434598104, -1.758782010937329110, -0.4337233627825891613 ) ) ;
#36463=CARTESIAN_POINT ( 'NONE',  ( 2.992876365407059147, 1.605230647100181596, -0.9602576221170722182 ) ) ;
#36465=CARTESIAN_POINT ( 'NONE',  ( 1.898553772666348394, -1.876154101037771582, -0.3696338911259658411 ) ) ;
#36471=CARTESIAN_POINT ( 'NONE',  ( 0.3692113334803036606, -1.616751421056546789, -1.021125667832627260 ) ) ;
#36474=CARTESIAN_POINT ( 'NONE',  ( 1.767943819387544968, -1.947426213878332035, 0.2369139692007388165 ) ) ;
#36475=CARTESIAN_POINT ( 'NONE',  ( 0.3685172633814579046, -0.5404119286356176000, 1.942243004588292132 ) ) ;
#36477=CARTESIAN_POINT ( 'NONE',  ( 3.972980863544761654, -1.569110274459505350, 1.426624754300914510 ) ) ;
#36480=CARTESIAN_POINT ( 'NONE',  ( 5.518811311470022574, 1.820418058502238035, 0.7569790930031635723 ) ) ;
#36483=CARTESIAN_POINT ( 'NONE',  ( 1.599367111750239934, -0.2554771505851380908, 2.101684664062503316 ) ) ;
#36485=CARTESIAN_POINT ( 'NONE',  ( 3.051297593704501043, 1.777051743073382761, -1.062048545217339823 ) ) ;
#36489=CARTESIAN_POINT ( 'NONE',  ( 4.400388060213418662, 1.616114658936588011, -1.326231919226998901 ) ) ;
#36491=CARTESIAN_POINT ( 'NONE',  ( 3.311362000969253039, -0.3573404788377897989, 1.790086433339547201 ) ) ;
#36492=CARTESIAN_POINT ( 'NONE',  ( 1.119438638434491429, -0.4408070000805932032, 1.756890142956100576 ) ) ;
#36496=CARTESIAN_POINT ( 'NONE',  ( 5.807716119225245777, -0.5415507062403871474, 2.139171552897000339 ) ) ;
#36499=CARTESIAN_POINT ( 'NONE',  ( 4.160738352132353768, 0.5130957772990808463, 1.842076966104645663 ) ) ;
#36502=CARTESIAN_POINT ( 'NONE',  ( 6.672334155782003506, -0.9722939650993901450, -1.827837255792996718 ) ) ;
#36505=CARTESIAN_POINT ( 'NONE',  ( 6.603104432341277530, -0.4828188497946246382, 2.145653685147373313 ) ) ;
#36508=CARTESIAN_POINT ( 'NONE',  ( 3.268673085221412311, -1.727008210369033847, -0.7190761260571985058 ) ) ;
#36514=CARTESIAN_POINT ( 'NONE',  ( 0.2859135117265668158, -1.207096249910791563, -1.556650298907244823 ) ) ;
#36515=CARTESIAN_POINT ( 'NONE',  ( 0.7554827284574801016, 1.942536278707338360, -0.5405140857882018146 ) ) ;
#36519=CARTESIAN_POINT ( 'NONE',  ( 0.9553299046189435151, 0.4242123182428610972, -2.149831459026855907 ) ) ;
#36520=CARTESIAN_POINT ( 'NONE',  ( 6.006453938882227561, -0.6616566355047011072, -1.701761020394356283 ) ) ;
#36527=CARTESIAN_POINT ( 'NONE',  ( 3.931074656914943954, -1.272613488525012659, -1.330884258478791438 ) ) ;
#36528=CARTESIAN_POINT ( 'NONE',  ( 0.7857919059152475016, 1.939557017834290020, -0.5388494671653855095 ) ) ;
#36529=CARTESIAN_POINT ( 'NONE',  ( 1.827921470121370850, -1.625240468190300103, 1.625389258475460563 ) ) ;
#36531=CARTESIAN_POINT ( 'NONE',  ( 0.4087542164426588021, -1.499397391050528050, 1.102066480322369202 ) ) ;
#36535=CARTESIAN_POINT ( 'NONE',  ( 4.166199421025416960, 1.911861072351704882, -0.05224187775455800542 ) ) ;
#36539=CARTESIAN_POINT ( 'NONE',  ( 3.790639713653580767, 1.765158817303988048, -1.120165474576743536 ) ) ;
#36540=CARTESIAN_POINT ( 'NONE',  ( 2.447944060942487621, 1.870205405844455049, 0.04815357881200743595 ) ) ;
#36543=CARTESIAN_POINT ( 'NONE',  ( 3.122313433385078607, 0.04571620936353942150, 1.740018996352102443 ) ) ;
#36546=CARTESIAN_POINT ( 'NONE',  ( 3.633171361085251849, -1.593041208078986193, 0.6618793944016196917 ) ) ;
#36548=CARTESIAN_POINT ( 'NONE',  ( 3.702820756938397295, 1.880440254450808757, 1.125299312022425280 ) ) ;
#36549=CARTESIAN_POINT ( 'NONE',  ( 6.006501602161061548, -0.7906231143557163055, -2.060575041408031272 ) ) ;
#36551=CARTESIAN_POINT ( 'NONE',  ( 4.153319900303814372, 1.837149938469440302, -1.156618460589062813 ) ) ;
#36552=CARTESIAN_POINT ( 'NONE',  ( 2.332394550857110893, 1.770734860448031300, 0.4440693575865002907 ) ) ;
#36554=CARTESIAN_POINT ( 'NONE',  ( 4.768830992622041798, -0.2625661012465319022, -2.100967800990781509 ) ) ;
#36556=CARTESIAN_POINT ( 'NONE',  ( 4.493851497812589635, -2.291808737193799406, -0.05710960328321466883 ) ) ;
#36558=CARTESIAN_POINT ( 'NONE',  ( 6.720655732516650716, 1.268691918110446570, 2.040305333170799429 ) ) ;
#36560=CARTESIAN_POINT ( 'NONE',  ( 0.9266185682500321930, -0.9568284065921551784, -1.892426592148554132 ) ) ;
#36566=CARTESIAN_POINT ( 'NONE',  ( 6.883263157960366030, 0.5727201817382967519, 2.105997115537924902 ) ) ;
#36569=CARTESIAN_POINT ( 'NONE',  ( 5.731092321990707283, 2.014232586630093191, 0.09613807139101374077 ) ) ;
#36571=CARTESIAN_POINT ( 'NONE',  ( 4.821169966264648998, -1.840000718094082943, -0.9321929973984711681 ) ) ;
#36577=CARTESIAN_POINT ( 'NONE',  ( 1.078203232848734094, -2.040033308301641757, -0.4564361842656887713 ) ) ;
#36578=CARTESIAN_POINT ( 'NONE',  ( 4.518204034511161815, -1.842447959940773705, 0.8197716922626956393 ) ) ;
#36579=CARTESIAN_POINT ( 'NONE',  ( 4.476008884455379366, -1.787108923542475525, -0.4427587100873929815 ) ) ;
#36581=CARTESIAN_POINT ( 'NONE',  ( 0.9204217893557011809, 1.591181625417271039, 0.6660807200309772913 ) ) ;
#36583=CARTESIAN_POINT ( 'NONE',  ( 1.319383182065179128, 1.127869332580781148, -2.002907031218110312 ) ) ;
#36585=CARTESIAN_POINT ( 'NONE',  ( 1.792605694782311243, -2.251445656634944559, -0.2226877779667023882 ) ) ;
#36586=CARTESIAN_POINT ( 'NONE',  ( 2.947987317136715468, 0.7576180897185936791, -1.965265766029665295 ) ) ;
#36590=CARTESIAN_POINT ( 'NONE',  ( 6.187500000000010658, -1.451031289060719320, 1.451031289061361473 ) ) ;
#36595=CARTESIAN_POINT ( 'NONE',  ( 4.676165968894677505, 2.197079021736783044, -0.3272799971512970196 ) ) ;
#36596=CARTESIAN_POINT ( 'NONE',  ( 2.045129345224237394, -1.761195505111545989, -1.303888621850733509 ) ) ;
#36599=CARTESIAN_POINT ( 'NONE',  ( 4.949637131784443866, 1.452432516441283905, 1.319008059494260143 ) ) ;
#36601=CARTESIAN_POINT ( 'NONE',  ( 6.890000000000044977, 2.990039200936049468, 2.173945303097582382 ) ) ;
#36605=CARTESIAN_POINT ( 'NONE',  ( 4.201511661969238531, 1.892856375164463367, -0.9562558712687405649 ) ) ;
#36611=CARTESIAN_POINT ( 'NONE',  ( 4.757273854911123756, 1.820453720981948242, -0.2752165127944474210 ) ) ;
#36614=CARTESIAN_POINT ( 'NONE',  ( 0.6084659026615606425, -0.2575236531317924293, 1.721126145854386946 ) ) ;
#36618=CARTESIAN_POINT ( 'NONE',  ( 5.436455051933180016, 2.129025116502227810, 0.3735886874452337691 ) ) ;
#36623=CARTESIAN_POINT ( 'NONE',  ( 5.120075222393803749, -1.153228217640640985, -1.828211184805514922 ) ) ;
#36625=CARTESIAN_POINT ( 'NONE',  ( 5.167239647397361857, 0.1962102620695851674, -1.961592271633934903 ) ) ;
#36626=CARTESIAN_POINT ( 'NONE',  ( 3.866272716362227690, -0.5049011280162157833, 1.658656615756588959 ) ) ;
#36627=CARTESIAN_POINT ( 'NONE',  ( 0.9607770615731696662, -1.983481723135366304, -0.9323335341336475013 ) ) ;
#36628=CARTESIAN_POINT ( 'NONE',  ( 2.503307172793560298, 1.853534942699623045, -1.374368423928104876 ) ) ;
#36629=CARTESIAN_POINT ( 'NONE',  ( 5.184866321732980232, -0.2479502356789231865, -2.045719655484798949 ) ) ;
#36630=CARTESIAN_POINT ( 'NONE',  ( 6.269086997039995168, 1.857158234874217939, -0.5679118324898363435 ) ) ;
#36638=CARTESIAN_POINT ( 'NONE',  ( 3.346891443098894303, 0.5343612633194516626, 2.140983517310310891 ) ) ;
#36640=CARTESIAN_POINT ( 'NONE',  ( 0.4087542164426588021, -1.499397391050528050, 1.102066480322369202 ) ) ;
#36645=CARTESIAN_POINT ( 'NONE',  ( 6.925078400183521943, 1.220207665023531174, 2.355644635573426182 ) ) ;
#36648=CARTESIAN_POINT ( 'NONE',  ( 2.834896919975951057, 0.2507222237850720847, 2.045500233692464587 ) ) ;
#36651=CARTESIAN_POINT ( 'NONE',  ( 2.613930769413209898, -0.6315753767559011411, 1.918467498408537919 ) ) ;
#36654=CARTESIAN_POINT ( 'NONE',  ( 1.727488365587977359, -1.940856233752264348, 0.6934696639643816996 ) ) ;
#36660=CARTESIAN_POINT ( 'NONE',  ( 5.303435803989668074, 1.802500012205746183, 1.273053691228965389 ) ) ;
#36661=CARTESIAN_POINT ( 'NONE',  ( 1.054251131370760319, 2.159144779032458050, -0.1049546803274861440 ) ) ;
#36663=CARTESIAN_POINT ( 'NONE',  ( 0.3742329010679063539, -2.001858617179689492, -0.2420261300371470137 ) ) ;
#36667=CARTESIAN_POINT ( 'NONE',  ( 1.744777856283234785, -1.581906188472384400, 0.9981555316627908070 ) ) ;
#36668=CARTESIAN_POINT ( 'NONE',  ( 3.678922940808615483, 1.700962499606586853, -1.082838980105811366 ) ) ;
#36672=CARTESIAN_POINT ( 'NONE',  ( 4.705754021700633949, -0.5625300431781330435, 2.029483779808038957 ) ) ;
#36678=CARTESIAN_POINT ( 'NONE',  ( 4.799084794409138155, -0.2512425647771680537, -2.004053532012660455 ) ) ;
#36681=CARTESIAN_POINT ( 'NONE',  ( 0.9892170606862679128, 0.1480104381128030111, 2.057284718974061288 ) ) ;
#36688=CARTESIAN_POINT ( 'NONE',  ( 2.963510081828163223, 1.832883945819727689, 1.163594247970006990 ) ) ;
#36691=CARTESIAN_POINT ( 'NONE',  ( 2.190726087351921425, 1.424366561657765207, 1.166803476217087576 ) ) ;
#36694=CARTESIAN_POINT ( 'NONE',  ( 4.722331747100577459, 2.097238624054961864, 0.6360808509995665716 ) ) ;
#36695=CARTESIAN_POINT ( 'NONE',  ( 6.883263157960404222, 4.689511904294953126, 2.716359706997414136 ) ) ;
#36696=CARTESIAN_POINT ( 'NONE',  ( 5.243177039506740300, -1.943355607328334678, 1.158386780943015504 ) ) ;
#36703=CARTESIAN_POINT ( 'NONE',  ( 5.360532716240259177, -1.281408969121943464, 1.220901466008792235 ) ) ;
#36705=CARTESIAN_POINT ( 'NONE',  ( 2.169099057653073093, -1.925109178590768799, -0.8542606987168609445 ) ) ;
#36708=CARTESIAN_POINT ( 'NONE',  ( 2.558991062574625275, 1.583523548174452733, -1.170949712736363502 ) ) ;
#36709=CARTESIAN_POINT ( 'NONE',  ( 1.094370286708164386, -0.4508366001288487412, -1.815394955969009239 ) ) ;
#36710=CARTESIAN_POINT ( 'NONE',  ( 0.1683002474503410839, -0.8351952195557797998, -1.773497582445908938 ) ) ;
#36711=CARTESIAN_POINT ( 'NONE',  ( 5.924035771748266122, -1.796794102754266431, 0.2306889152782486963 ) ) ;
#36716=CARTESIAN_POINT ( 'NONE',  ( 5.524238439434661530, 1.113281918156138639, -1.503147240406087271 ) ) ;
#36718=CARTESIAN_POINT ( 'NONE',  ( 5.858279169847476098, -2.070434559870216074, -0.005763162253501210100 ) ) ;
#36728=CARTESIAN_POINT ( 'NONE',  ( 4.861744986159981075, -0.5251177144562025889, 1.890194517805739771 ) ) ;
#36730=CARTESIAN_POINT ( 'NONE',  ( 3.479842141819572188, 1.821463063354014533, 0.8645922719773958542 ) ) ;
#36731=CARTESIAN_POINT ( 'NONE',  ( 3.010844082872287331, 0.05196181304293297915, 1.915202476457795511 ) ) ;
#36733=CARTESIAN_POINT ( 'NONE',  ( 0.2225716830646235489, 2.098996182288978218, 0.6302611576235670476 ) ) ;
#36735=CARTESIAN_POINT ( 'NONE',  ( 0.2331713839410941569, 0.7381306520543399197, -2.038767774274966360 ) ) ;
#36736=CARTESIAN_POINT ( 'NONE',  ( 2.583089905966722277, 1.711919019956799737, -0.7542334906679578621 ) ) ;
#36738=CARTESIAN_POINT ( 'NONE',  ( 3.832292871861494810, -1.038684978035837592, -1.724458057284683710 ) ) ;
#36741=CARTESIAN_POINT ( 'NONE',  ( 4.411780756640943046, -1.303739072956756617, -1.668109288273095014 ) ) ;
#36743=CARTESIAN_POINT ( 'NONE',  ( 5.635237798060349412, -0.04710594754482424346, -2.069988403558701062 ) ) ;
#36744=CARTESIAN_POINT ( 'NONE',  ( 1.663735998746267652, 1.077533827470295913, 1.791552697131219229 ) ) ;
#36745=CARTESIAN_POINT ( 'NONE',  ( 6.720655732516641834, 2.402268298795938950, 2.653651172607660591 ) ) ;
#36746=CARTESIAN_POINT ( 'NONE',  ( 6.334959139596201716, 0.1821375521317940283, 1.816452708017932238 ) ) ;
#36755=CARTESIAN_POINT ( 'NONE',  ( 0.6272531361488179469, -0.2670696439982013781, 1.791522762418327419 ) ) ;
#36764=CARTESIAN_POINT ( 'NONE',  ( 6.468375372808552903, -1.978050569928070379, -0.3905794195708453542 ) ) ;
#36765=CARTESIAN_POINT ( 'NONE',  ( 0.4520119014386895229, -1.502510013782244025, -1.496567369470555020 ) ) ;
#36767=CARTESIAN_POINT ( 'NONE',  ( 0.1405533004714253908, 5.720147882271004569, -2.873730252010114228 ) ) ;
#36771=CARTESIAN_POINT ( 'NONE',  ( 4.047672669870348905, 1.423397643995693684, 1.361350234347382226 ) ) ;
#36772=CARTESIAN_POINT ( 'NONE',  ( 5.079703922733037835, -0.7231256174668048153, 1.882480835741196845 ) ) ;
#36777=CARTESIAN_POINT ( 'NONE',  ( 4.980524279605372584, -0.2661484459187679064, -2.175167798947100994 ) ) ;
#36778=CARTESIAN_POINT ( 'NONE',  ( 3.592722855893375478, -0.3746021097269113809, -1.889456300395859989 ) ) ;
#36780=CARTESIAN_POINT ( 'NONE',  ( -0.02968770228140015649, 0.7448490463385792903, -1.910291535987144629 ) ) ;
#36786=CARTESIAN_POINT ( 'NONE',  ( 5.664895447484411761, 1.493751497301420761, -1.283663174101207005 ) ) ;
#36787=CARTESIAN_POINT ( 'NONE',  ( 0.1869208759678643028, 1.439853572182720587, 1.303434232916983015 ) ) ;
#36788=CARTESIAN_POINT ( 'NONE',  ( 4.371743676962040581, 0.4387793907001916738, -1.964547544987900851 ) ) ;
#36789=CARTESIAN_POINT ( 'NONE',  ( 5.026898302747025760, 2.274369689431681163, -0.3307130315356506256 ) ) ;
#36791=CARTESIAN_POINT ( 'NONE',  ( 4.240933880512650411, -0.1787712432332102808, -1.852300418306342955 ) ) ;
#36797=CARTESIAN_POINT ( 'NONE',  ( 0.8025787753177977546, 1.655945718051672566, -1.435626523826734280 ) ) ;
#36803=CARTESIAN_POINT ( 'NONE',  ( 0.3459771380207553593, 1.820543102168985961, 0.1377627428671979182 ) ) ;
#36805=CARTESIAN_POINT ( 'NONE',  ( 2.637049607583162203, 0.5866705090989009497, 1.632017879250416525 ) ) ;
#36808=CARTESIAN_POINT ( 'NONE',  ( 5.619710272201024814, -1.780234218580947436, 0.4041525643716862848 ) ) ;
#36809=CARTESIAN_POINT ( 'NONE',  ( 3.467582345443523728, -0.3871886708083654427, 1.922995549214156608 ) ) ;
#36814=CARTESIAN_POINT ( 'NONE',  ( 4.424552244980545446, -0.9075887007226298708, -1.916591080935086788 ) ) ;
#36818=CARTESIAN_POINT ( 'NONE',  ( 2.940353189855488658, -1.068159618217549234, 1.773299548953041871 ) ) ;
#36821=CARTESIAN_POINT ( 'NONE',  ( 4.231244787023562992, 2.030907777374240997, 0.9001406952713184584 ) ) ;
#36822=VERTEX_POINT ( 'NONE', #31487 ) ;
#36823=CARTESIAN_POINT ( 'NONE',  ( 3.129784643070336436, 0.5604733119842463251, 2.229205935122404725 ) ) ;
#36830=CARTESIAN_POINT ( 'NONE',  ( 2.830216799141628492, -0.9462872844297947061, -1.661813493071498726 ) ) ;
#36832=CARTESIAN_POINT ( 'NONE',  ( 4.559404828610894356, 0.3762245950137115269, -1.683048502377647804 ) ) ;
#36833=CARTESIAN_POINT ( 'NONE',  ( 3.819546216251490822, -1.394084564108012403, -1.457236891723237449 ) ) ;
#36834=CARTESIAN_POINT ( 'NONE',  ( 3.868082235913085309, -0.2263641512248204812, -2.287543476887623051 ) ) ;
#36836=CARTESIAN_POINT ( 'NONE',  ( 0.1533209562146371774, -1.769702838771534559, 1.318327933512997152 ) ) ;
#36839=CARTESIAN_POINT ( 'NONE',  ( 4.481574309046215454, 1.155277477370730832, 1.340746495013745543 ) ) ;
#36841=CARTESIAN_POINT ( 'NONE',  ( 0.6566820891428931661, -1.656472902050255991, 1.584714856167362074 ) ) ;
#36842=CARTESIAN_POINT ( 'NONE',  ( 0.3393031230796061948, 1.735299727462248587, 0.1329522994921657764 ) ) ;
#36844=CARTESIAN_POINT ( 'NONE',  ( 5.736325210887869730, 0.4244523575273988492, 2.149783713274712404 ) ) ;
#36848=CARTESIAN_POINT ( 'NONE',  ( 0.2214384409217939054, -1.939739064610836339, -0.9756505802681545436 ) ) ;
#36849=CARTESIAN_POINT ( 'NONE',  ( 0.8312679839070147292, -1.592664559859976237, -1.236796411087807801 ) ) ;
#36851=CARTESIAN_POINT ( 'NONE',  ( 4.811117629317255506, 1.676929503210132122, 0.9481960042460689797 ) ) ;
#36853=CARTESIAN_POINT ( 'NONE',  ( 0.7212869692094016072, 1.677245448433011710, -1.456619292340176841 ) ) ;
#36862=CARTESIAN_POINT ( 'NONE',  ( 4.423245670630183923, -1.075405338609165318, -1.368339626032973211 ) ) ;
#36863=CARTESIAN_POINT ( 'NONE',  ( 2.734756269166933151, -1.876540383875524576, -0.5722209215143353456 ) ) ;
#36869=CARTESIAN_POINT ( 'NONE',  ( 6.877413162628407406, -0.1429737755889188000, 1.930079329684093237 ) ) ;
#36872=CARTESIAN_POINT ( 'NONE',  ( 4.979703994296570180, -0.7212954316567052881, 1.883311551353183511 ) ) ;
#36874=CARTESIAN_POINT ( 'NONE',  ( 1.095004809772756493, -0.5519004177921453813, -2.194067758203117169 ) ) ;
#36878=CARTESIAN_POINT ( 'NONE',  ( 1.370139650511486007, -1.190941340819328564, 1.442406204513801971 ) ) ;
#36879=CARTESIAN_POINT ( 'NONE',  ( 0.4043864329151745651, -0.9253471945274373001, -1.466404024333650247 ) ) ;
#36880=CARTESIAN_POINT ( 'NONE',  ( 4.019203527901527018, -2.096847714747759106, 0.6372333828079318474 ) ) ;
#36881=CARTESIAN_POINT ( 'NONE',  ( 6.124106107054944736, -1.275020473110911157, -1.923184551904693507 ) ) ;
#36882=CARTESIAN_POINT ( 'NONE',  ( 0.8134386948647929216, -0.3029782207385351422, 2.038374528180360912 ) ) ;
#36883=CARTESIAN_POINT ( 'NONE',  ( 3.872937777176552299, 1.828215432968218535, -0.6551730591081408317 ) ) ;
#36885=CARTESIAN_POINT ( 'NONE',  ( 5.466025653875023593, 0.9211120992074215419, 1.627924866423650530 ) ) ;
#36890=CARTESIAN_POINT ( 'NONE',  ( 4.289685514112329123, 1.556909497225898109, -1.281360267751927129 ) ) ;
#36894=CARTESIAN_POINT ( 'NONE',  ( 2.525780997283606499, -1.050937884436175418, -1.492673824175783093 ) ) ;
#36903=CARTESIAN_POINT ( 'NONE',  ( 5.619787797283516184, -0.4887302510508689801, 1.959527308111078669 ) ) ;
#36904=CARTESIAN_POINT ( 'NONE',  ( 0.3641364058636682999, 0.6611385597973111761, -2.014868753213174823 ) ) ;
#36908=CARTESIAN_POINT ( 'NONE',  ( 5.875869988399868404, 1.225711027941748466, 1.656622483273604729 ) ) ;
#36909=CARTESIAN_POINT ( 'NONE',  ( 5.203750078570229753, 1.864167652161516031, 0.7691231355932278690 ) ) ;
#36918=CARTESIAN_POINT ( 'NONE',  ( 4.815779736370030761, -1.620933320526974031, 1.198678058543983571 ) ) ;
#36919=CARTESIAN_POINT ( 'NONE',  ( 4.101369424419714527, -1.836060619117799497, 0.1375280490283348478 ) ) ;
#36920=CARTESIAN_POINT ( 'NONE',  ( -0.02338929933905826986, 0.006294950389555685130, -1.710968156697996401 ) ) ;
#36921=CARTESIAN_POINT ( 'NONE',  ( 2.456097291302907770, 0.6137686719557032822, -2.224517260854632639 ) ) ;
#36923=CARTESIAN_POINT ( 'NONE',  ( 4.587301040747738590, 1.933109172225886185, -0.9673573668882375909 ) ) ;
#36925=CARTESIAN_POINT ( 'NONE',  ( -0.02402099761080173090, -1.884047281740467872, -0.4708274727777494451 ) ) ;
#36930=CARTESIAN_POINT ( 'NONE',  ( 3.555401268124198655, 0.4554524271490404952, -1.814226883376020671 ) ) ;
#36931=CARTESIAN_POINT ( 'NONE',  ( 6.244996228834688523, -1.665663155820007013, 1.054347381401467887 ) ) ;
#36935=CARTESIAN_POINT ( 'NONE',  ( 2.192262590105994668, -0.9421081357594159877, 1.995820444975453745 ) ) ;
#36943=CARTESIAN_POINT ( 'NONE',  ( 1.001173315506132422, 1.609201512179364135, 1.138472824994830379 ) ) ;
#36944=CARTESIAN_POINT ( 'NONE',  ( 6.551428954101934821, -1.849038126066489207, -1.380618780084260644 ) ) ;
#36945=CARTESIAN_POINT ( 'NONE',  ( 0.8362905744919849615, -1.092891352686057527, 1.629061181365853539 ) ) ;
#36947=CARTESIAN_POINT ( 'NONE',  ( 4.416881224320576393, -1.531859844946925397, 1.381376250335116795 ) ) ;
#36955=CARTESIAN_POINT ( 'NONE',  ( 6.830535128024421532, -1.341686296255087063, 1.707861204732928018 ) ) ;
#36957=CARTESIAN_POINT ( 'NONE',  ( 5.319803798718575116, 1.092037692397327620, -1.482314076171886708 ) ) ;
#36965=CARTESIAN_POINT ( 'NONE',  ( 1.172351427048579531, 0.7757545017167379875, 1.748050575570128107 ) ) ;
#36966=CARTESIAN_POINT ( 'NONE',  ( 1.674285954873380167, -1.679204462075728488, -0.5593204692268695100 ) ) ;
#36967=CARTESIAN_POINT ( 'NONE',  ( 5.848296790250511634, 0.9903421736442417078, -1.752559156024376508 ) ) ;
#36969=CARTESIAN_POINT ( 'NONE',  ( 4.622610566699385082, 0.3315282304991398754, 1.886534565956134335 ) ) ;
#36971=CARTESIAN_POINT ( 'NONE',  ( 5.670349227943210835, -0.8838483254627060859, -1.760150121488897490 ) ) ;
#36972=CARTESIAN_POINT ( 'NONE',  ( 6.187761630889374587, 1.931537729788906477, -0.5904018810464291001 ) ) ;
#36974=CARTESIAN_POINT ( 'NONE',  ( 4.065207594588423845, 0.2294239933214488880, -1.856472568989680161 ) ) ;
#36975=CARTESIAN_POINT ( 'NONE',  ( 6.129511981615775262, -1.621618681806114459, 0.5882815792577487102 ) ) ;
#36977=CARTESIAN_POINT ( 'NONE',  ( 3.809358915828209735, 1.892446193107431451, 1.135094405146239049 ) ) ;
#36980=CARTESIAN_POINT ( 'NONE',  ( 0.3267250850040852583, -1.348467290049197853, 1.560915443186759122 ) ) ;
#36985=ADVANCED_FACE ( 'NONE', ( #198216 ), #18399, .T. ) ;
#36988=CARTESIAN_POINT ( 'NONE',  ( 2.857943571468853250, -0.6518772230660694333, 1.965110387975615991 ) ) ;
#36992=CARTESIAN_POINT ( 'NONE',  ( 0.8385427299653764877, 1.201306043029852777, -1.623412603403198373 ) ) ;
#36993=CARTESIAN_POINT ( 'NONE',  ( 0.1747926744264659826, 0.006858446013176252437, -1.855468577918440332 ) ) ;
#36995=CARTESIAN_POINT ( 'NONE',  ( 6.468125021464291358, 1.674632898861495134, 1.122323893169609565 ) ) ;
#36996=CARTESIAN_POINT ( 'NONE',  ( 5.507027455500737467, -0.04000985115821522470, 1.915467925163343965 ) ) ;
#36997=CARTESIAN_POINT ( 'NONE',  ( 6.639320575229281651, 0.5623622132289189945, 2.255000583061476771 ) ) ;
#36998=CARTESIAN_POINT ( 'NONE',  ( 3.298540952264991777, 1.726358142885858316, -1.349911518210664241 ) ) ;
#37001=CARTESIAN_POINT ( 'NONE',  ( 2.250135261179100343, 0.8981609309555338427, -1.688322754368525747 ) ) ;
#37005=CARTESIAN_POINT ( 'NONE',  ( 0.5445462702219765472, -1.458543044971000402, 1.392561646250379814 ) ) ;
#37007=CARTESIAN_POINT ( 'NONE',  ( 5.987848539424092564, -2.180829346447300310, -0.2163489798085171945 ) ) ;
#37009=CARTESIAN_POINT ( 'NONE',  ( 2.537784596217841138, 0.8154259780687975745, -1.519840121599738803 ) ) ;
#37014=CARTESIAN_POINT ( 'NONE',  ( 1.293326634533353170, -1.775083115552608559, 0.8357255594537355003 ) ) ;
#37016=CARTESIAN_POINT ( 'NONE',  ( 0.07556134207196538166, 0.2286499876833356648, -2.278112926217394030 ) ) ;
#37020=CARTESIAN_POINT ( 'NONE',  ( 3.949720763895887110, -1.252031560403286337, -1.309370340798710730 ) ) ;
#37024=CARTESIAN_POINT ( 'NONE',  ( 5.391193890671133637, -0.05051413884850668168, -1.810949582550380521 ) ) ;
#37028=CARTESIAN_POINT ( 'NONE',  ( 5.107777090148794663, 0.5842497386982176133, -1.767012650282340003 ) ) ;
#37030=CARTESIAN_POINT ( 'NONE',  ( 2.425271589312021359, -1.421058436811825754, -1.284788359014801706 ) ) ;
#37040=CARTESIAN_POINT ( 'NONE',  ( 0.8145359132093257237, 1.932373828749304856, 0.7984225692715187783 ) ) ;
#37042=CARTESIAN_POINT ( 'NONE',  ( 1.360069071312763223, 0.7361036424862777983, 1.670779996689908398 ) ) ;
#37044=CARTESIAN_POINT ( 'NONE',  ( 2.344514592193002400, 0.3973361102717864468, 1.781653928021959432 ) ) ;
#37047=CARTESIAN_POINT ( 'NONE',  ( 1.933716311909071006, -1.854087253938462521, 0.4680378644332866545 ) ) ;
#37048=CARTESIAN_POINT ( 'NONE',  ( 1.099984078287146394, 0.8012805854674235340, -1.799388124431312797 ) ) ;
#37050=CARTESIAN_POINT ( 'NONE',  ( 4.036618323093550842, -1.688041843851136425, 0.9601762628524412868 ) ) ;
#37054=CARTESIAN_POINT ( 'NONE',  ( 4.535463010148616192, -0.1012041512906610846, 2.118281909017679432 ) ) ;
#37058=CARTESIAN_POINT ( 'NONE',  ( 0.2331563151865738703, 7.629137130509052511, -2.545728013813946866 ) ) ;
#37062=CARTESIAN_POINT ( 'NONE',  ( 4.301258635363705451, 1.467727663998198429, 1.085573330547324744 ) ) ;
#37068=CARTESIAN_POINT ( 'NONE',  ( 5.084763247618332649, -0.2297073032716222263, -1.856415652357709778 ) ) ;
#37070=CARTESIAN_POINT ( 'NONE',  ( 1.857912668630396169, 1.921361403365331677, -0.1415498456752254663 ) ) ;
#37071=CARTESIAN_POINT ( 'NONE',  ( 6.209812062937981381, 0.5727486527220859713, -1.876249287704085722 ) ) ;
#37079=CARTESIAN_POINT ( 'NONE',  ( 1.458780272697857594, -2.011719176664223951, -0.6602987507247930488 ) ) ;
#37082=CARTESIAN_POINT ( 'NONE',  ( 6.051642586050198780, 1.563818258945088191, 1.356687170345116211 ) ) ;
#37083=CARTESIAN_POINT ( 'NONE',  ( 0.5207438388301621757, -1.748553680932497745, 0.5769860859521497298 ) ) ;
#37085=CARTESIAN_POINT ( 'NONE',  ( 6.135373049470649320, 0.7166818055565070678, 2.184152129457237912 ) ) ;
#37089=CARTESIAN_POINT ( 'NONE',  ( 1.201600019185744994, -0.5526092242729553350, 2.224544611104557035 ) ) ;
#37093=CARTESIAN_POINT ( 'NONE',  ( 6.509718631618705231, -0.9178700960432868428, -1.711342201762585002 ) ) ;
#37098=CARTESIAN_POINT ( 'NONE',  ( -0.01731850797281712928, -1.311767784893268285, 1.527291784361783922 ) ) ;
#37099=CARTESIAN_POINT ( 'NONE',  ( 6.298064597363540074, -0.9548514761729166578, -1.776169100128288658 ) ) ;
#37103=CARTESIAN_POINT ( 'NONE',  ( 2.835970919032384963, 2.074939634868844252, 0.2550863383830522801 ) ) ;
#37104=CARTESIAN_POINT ( 'NONE',  ( 1.674285954873380167, -1.679204462075728488, -0.5593204692268695100 ) ) ;
#37108=CARTESIAN_POINT ( 'NONE',  ( 4.277453538519633724, 1.495592673709666531, 1.737217383791799463 ) ) ;
#37109=CARTESIAN_POINT ( 'NONE',  ( 3.064111502348449978, -1.608305157344312564, -0.6653965878143754953 ) ) ;
#37112=CARTESIAN_POINT ( 'NONE',  ( 3.233448856393176474, -1.601016440221241455, -0.6660543662743572124 ) ) ;
#37113=CARTESIAN_POINT ( 'NONE',  ( 3.684171759641508448, -1.290596846074614223, -1.745836057026050714 ) ) ;
#37115=CARTESIAN_POINT ( 'NONE',  ( 4.487517715496184501, -0.5331711073110931842, 1.944729879240604253 ) ) ;
#37116=CARTESIAN_POINT ( 'NONE',  ( 2.562500000000001332, -1.451031289061222251, -1.451031289061014196 ) ) ;
#37118=CARTESIAN_POINT ( 'NONE',  ( 1.659075543930859764, -1.650851203806924294, -0.9926060514057006845 ) ) ;
#37120=CARTESIAN_POINT ( 'NONE',  ( 4.201594209339031494, 1.983332154306137518, -1.000733898520693499 ) ) ;
#37122=CARTESIAN_POINT ( 'NONE',  ( -0.1106856583841086261, 0.2435294909829844312, -2.031701206977332586 ) ) ;
#37127=CARTESIAN_POINT ( 'NONE',  ( 0.2764465059262249391, 2.196205179236205396, -0.3323138113263158222 ) ) ;
#37128=CARTESIAN_POINT ( 'NONE',  ( 5.986763597034561180, 1.890319730748804439, 0.5246630281777533433 ) ) ;
#37130=CARTESIAN_POINT ( 'NONE',  ( 0.6148119136215323133, 1.491057340773978668, -1.565211586912764741 ) ) ;
#37133=CARTESIAN_POINT ( 'NONE',  ( 3.121586329596927722, 0.3053734461533639255, -2.039847365138738766 ) ) ;
#37138=CARTESIAN_POINT ( 'NONE',  ( 5.114452126850835612, 1.290914414355217366, -1.353902443742838191 ) ) ;
#37139=CARTESIAN_POINT ( 'NONE',  ( 3.867547151669390448, -0.1745043776680033631, -1.725349009328189576 ) ) ;
#37140=CARTESIAN_POINT ( 'NONE',  ( 3.473892794100913672, -1.678317346756386108, -0.4606119698754263525 ) ) ;
#37141=CARTESIAN_POINT ( 'NONE',  ( 0.2930494462585155335, 1.901387222806522503, -1.280258756811911702 ) ) ;
#37143=CARTESIAN_POINT ( 'NONE',  ( 6.075741423153157683, -1.117747424998961403, 1.766673535877111290 ) ) ;
#37144=CARTESIAN_POINT ( 'NONE',  ( 6.369087006730828726, 1.857646680926292815, -0.5659663566517159072 ) ) ;
#37147=CARTESIAN_POINT ( 'NONE',  ( 2.057267738415057057, -1.238319999287675888, 1.591319116112683618 ) ) ;
#37149=CARTESIAN_POINT ( 'NONE',  ( 0.4456111923471540170, 0.6836232613432815519, -2.082162021007263331 ) ) ;
#37154=CARTESIAN_POINT ( 'NONE',  ( 2.438272501909013901, -1.223040458498025673, -1.732039452853536776 ) ) ;
#37158=CARTESIAN_POINT ( 'NONE',  ( 5.777927443424748510, 1.091106472389313131, 1.463626628978510702 ) ) ;
#37165=CARTESIAN_POINT ( 'NONE',  ( 2.707290811070970804, 1.730213373471348737, -1.041854834777849126 ) ) ;
#37166=CARTESIAN_POINT ( 'NONE',  ( 0.3234443461216755522, -0.1028566021752069376, 2.103582624919388078 ) ) ;
#37168=CARTESIAN_POINT ( 'NONE',  ( 4.399146427517338864, -1.620787001191201560, 0.9142094169404291204 ) ) ;
#37176=CARTESIAN_POINT ( 'NONE',  ( 5.004447790439923160, -0.6182884515001166870, -1.717943145347331502 ) ) ;
#37180=CARTESIAN_POINT ( 'NONE',  ( 1.510678448032206189, 1.731588368038105896, 0.09119125932234918575 ) ) ;
#37181=CARTESIAN_POINT ( 'NONE',  ( 0.2865101139537007402, 1.286042648715233216, 1.172746904078510122 ) ) ;
#37182=CARTESIAN_POINT ( 'NONE',  ( 5.075001523147505189, -2.171532227461204556, -0.7813444033149226087 ) ) ;
#37185=CARTESIAN_POINT ( 'NONE',  ( 1.475930922893650798, 1.225283507603215805, 1.656815433548680438 ) ) ;
#37186=CARTESIAN_POINT ( 'NONE',  ( 6.433027599926354867, 1.173280253959343211, 1.976260322036479167 ) ) ;
#37189=CARTESIAN_POINT ( 'NONE',  ( 0.1101414390347132816, -0.8398613168552993002, -1.781629259513841657 ) ) ;
#37191=CARTESIAN_POINT ( 'NONE',  ( 3.638835171272115421, 1.817485770107383436, 0.5952672491930725007 ) ) ;
#37193=CARTESIAN_POINT ( 'NONE',  ( 5.391335350415090488, 1.947751002805158560, -1.037606470750504828 ) ) ;
#37199=CARTESIAN_POINT ( 'NONE',  ( 5.602226918196428151, -0.9533447246646039597, 1.894147766696724799 ) ) ;
#37201=CARTESIAN_POINT ( 'NONE',  ( 3.821538862543779391, -0.1730032229720068482, 2.301163704417693356 ) ) ;
#37202=CARTESIAN_POINT ( 'NONE',  ( 4.070719198475009293, 1.388998261151509039, -1.385754695631277844 ) ) ;
#37204=CARTESIAN_POINT ( 'NONE',  ( 1.252704021237858401, -0.4712815170893420724, -1.904206577484176321 ) ) ;
#37208=CARTESIAN_POINT ( 'NONE',  ( 6.087125082597877324, 1.679220375458953862, 1.116214469231976869 ) ) ;
#37211=CARTESIAN_POINT ( 'NONE',  ( 3.678747780723041760, 1.381198535464265520, -1.675025177318607783 ) ) ;
#37213=CARTESIAN_POINT ( 'NONE',  ( 0.7738737444688469358, 0.4079195088417563730, -2.080830740624163955 ) ) ;
#37219=CARTESIAN_POINT ( 'NONE',  ( 1.282574848904423082, -2.009897191344016232, -0.4543217371432185514 ) ) ;
#37225=CARTESIAN_POINT ( 'NONE',  ( 4.266199323752727146, 1.911794059647478949, -0.05023246155653331158 ) ) ;
#37231=CARTESIAN_POINT ( 'NONE',  ( 0.3338568476279568653, -0.9693210200989417213, -1.530242633214883963 ) ) ;
#37233=CARTESIAN_POINT ( 'NONE',  ( 0.6553225869628921396, 1.845336034500634437, -0.5141059209906836402 ) ) ;
#37234=CARTESIAN_POINT ( 'NONE',  ( 1.803268859043684058, -1.750145871244257467, 1.105767233283899920 ) ) ;
#37237=CARTESIAN_POINT ( 'NONE',  ( 1.059376886711576260, 0.3867523390363221125, -1.932997803022660666 ) ) ;
#37238=CARTESIAN_POINT ( 'NONE',  ( 2.508196354075361789, -0.6984789837382252564, -1.686990664346368796 ) ) ;
#37239=CARTESIAN_POINT ( 'NONE',  ( 0.4698728525199142303, 0.2201595520019784535, -2.297181220480988717 ) ) ;
#37242=CARTESIAN_POINT ( 'NONE',  ( 3.771981659335025938, -2.032644659601599457, 0.3498187521492699403 ) ) ;
#37248=CARTESIAN_POINT ( 'NONE',  ( 4.999102919943527290, 1.752478773177888582, -1.167534824283325667 ) ) ;
#37250=CARTESIAN_POINT ( 'NONE',  ( 6.197728532230423859, -1.496850047335227085, -1.430563974149069661 ) ) ;
#37252=CARTESIAN_POINT ( 'NONE',  ( 3.321700061091820366, -2.084211496276411779, 0.5730272365244912791 ) ) ;
#37253=CARTESIAN_POINT ( 'NONE',  ( 3.861976953351463848, 0.6784905939434657807, -1.902444917487989606 ) ) ;
#37254=CARTESIAN_POINT ( 'NONE',  ( 6.620655732516628866, 4.686767102414819419, 2.836268676114994669 ) ) ;
#37259=CARTESIAN_POINT ( 'NONE',  ( 2.219935720625454412, 0.9462983093676997637, -1.780669029686342331 ) ) ;
#37264=( NAMED_UNIT ( * ) SI_UNIT ( $, .STERADIAN. ) SOLID_ANGLE_UNIT ( ) );
#37267=CARTESIAN_POINT ( 'NONE',  ( 4.622672832840883039, 0.3474877929729481840, 1.986098205159859909 ) ) ;
#37269=CARTESIAN_POINT ( 'NONE',  ( 6.088827306860007837, -0.2580713809433569650, -1.705207211698676062 ) ) ;
#37274=CARTESIAN_POINT ( 'NONE',  ( 5.624238404463478780, 1.114819804898508515, -1.501858222471161408 ) ) ;
#37275=CARTESIAN_POINT ( 'NONE',  ( 0.2057266557286231146, 1.493221433009199517, 1.350316897416648843 ) ) ;
#37280=CARTESIAN_POINT ( 'NONE',  ( 1.107046246104196552, -0.04665650516593074226, 2.016035445577879504 ) ) ;
#37281=CARTESIAN_POINT ( 'NONE',  ( 1.037045679623523897, -0.04297598538225732429, 1.811226269459820903 ) ) ;
#37287=CARTESIAN_POINT ( 'NONE',  ( 6.151949797202925119, 0.9892698599738621867, 1.640257924793379063 ) ) ;
#37292=ORIENTED_EDGE ( 'NONE', *, *, #137027, .F. ) ;
#37294=CARTESIAN_POINT ( 'NONE',  ( 3.696290335837215224, -2.159122111672501454, -0.1082323872379290508 ) ) ;
#37297=CARTESIAN_POINT ( 'NONE',  ( 0.2641366190093488164, 0.6592694798918593557, -2.015615888626711705 ) ) ;
#37298=CARTESIAN_POINT ( 'NONE',  ( 5.350558509363329662, 0.5315954154057299652, 1.746479326997903092 ) ) ;
#37299=CARTESIAN_POINT ( 'NONE',  ( 2.196496099369545263, -0.5219070890916230887, -1.900975273168264534 ) ) ;
#37300=CARTESIAN_POINT ( 'NONE',  ( 4.746305163667582150, 0.9781546018433548983, -1.643150005489722787 ) ) ;
#37303=CARTESIAN_POINT ( 'NONE',  ( 6.074653383054481104, 1.324031319358546677, -1.458257743282452834 ) ) ;
#37304=CARTESIAN_POINT ( 'NONE',  ( 0.7439598490389126573, 0.5628818913385369438, 1.858577368155549525 ) ) ;
#37310=CARTESIAN_POINT ( 'NONE',  ( 4.547458224165379370, -1.746952781796942133, 0.7782266863690868730 ) ) ;
#37312=CARTESIAN_POINT ( 'NONE',  ( 0.3412290553763823175, 0.3797058362894656369, 2.173699509851903855 ) ) ;
#37314=CARTESIAN_POINT ( 'NONE',  ( 6.217445370822936468, 1.674971474680493788, 1.116412877057591624 ) ) ;
#37315=CARTESIAN_POINT ( 'NONE',  ( -0.02319159430949797526, 7.629137130509074716, -2.410989586153565067 ) ) ;
#37318=CARTESIAN_POINT ( 'NONE',  ( 2.611853368047814872, 0.5545374748289233491, -1.994631108499920646 ) ) ;
#37323=CARTESIAN_POINT ( 'NONE',  ( 0.6730137850648570952, -2.035850703004048246, -0.7271551459356735414 ) ) ;
#37329=CARTESIAN_POINT ( 'NONE',  ( 6.825078400183582694, 7.052760558784821221, 2.553807217019073761 ) ) ;
#37331=CARTESIAN_POINT ( 'NONE',  ( 5.643113243286411063, 0.7107029072939261560, 1.582047324045066095 ) ) ;
#37335=CARTESIAN_POINT ( 'NONE',  ( 3.661042849074844785, 1.635018244968543977, -1.269851595989857085 ) ) ;
#37336=CARTESIAN_POINT ( 'NONE',  ( 4.112992273575425628, 0.1058706520744826102, 2.114715381611050660 ) ) ;
#37339=CARTESIAN_POINT ( 'NONE',  ( 2.711712322018722698, 0.5300763513187057852, -1.896665901777684127 ) ) ;
#37340=CARTESIAN_POINT ( 'NONE',  ( 0.8965662283535699162, -1.866366896104875162, -0.4163465257057268332 ) ) ;
#37341=CARTESIAN_POINT ( 'NONE',  ( 4.875077803184670877, 2.140050280577758812, -0.8218066810307764758 ) ) ;
#37342=CARTESIAN_POINT ( 'NONE',  ( 3.281694405262673087, 1.158851912627656189, 1.410738560442346801 ) ) ;
#37346=CARTESIAN_POINT ( 'NONE',  ( 3.920185232657522167, -2.007512044478755531, 0.1524921764288286741 ) ) ;
#37347=CARTESIAN_POINT ( 'NONE',  ( 2.922649740298603138, -1.356309479035762378, 1.417576456850026867 ) ) ;
#37351=CARTESIAN_POINT ( 'NONE',  ( 6.615180898807764720, -2.028213694748048024, 0.5066274125750843682 ) ) ;
#37352=CARTESIAN_POINT ( 'NONE',  ( 4.539784583036060361, 0.7555593814247036910, -1.600612801534553542 ) ) ;
#37354=CARTESIAN_POINT ( 'NONE',  ( 0.7795418844130063141, 1.474435645617519164, 1.621430000501473900 ) ) ;
#37355=CARTESIAN_POINT ( 'NONE',  ( 0.1337851541256071808, 0.2942392587969425155, 1.715217768732644643 ) ) ;
#37358=CARTESIAN_POINT ( 'NONE',  ( 0.8787516259003292918, -0.3353366030727308877, 2.273710652787809039 ) ) ;
#37359=CARTESIAN_POINT ( 'NONE',  ( 0.3104468679729632807, 1.506874830639578056, -1.591553791636945991 ) ) ;
#37360=CARTESIAN_POINT ( 'NONE',  ( 6.714187037452940210, -1.395258515317991943, -1.029009966057025549 ) ) ;
#37361=CARTESIAN_POINT ( 'NONE',  ( 3.492985898914053866, -0.4302566696539159574, -2.164365734511737305 ) ) ;
#37363=CARTESIAN_POINT ( 'NONE',  ( 6.461400869420954152, 1.801464151850284301, 1.211653227174382952 ) ) ;
#37364=CARTESIAN_POINT ( 'NONE',  ( 1.710321574826153324, 1.214426542090217609, -1.734289745093554380 ) ) ;
#37365=CARTESIAN_POINT ( 'NONE',  ( 4.062500000000002665, -1.451031289061280205, -1.451031289060952467 ) ) ;
#37366=CARTESIAN_POINT ( 'NONE',  ( 6.620655732516642189, 2.417337544263608251, 2.554705107920357321 ) ) ;
#37367=CARTESIAN_POINT ( 'NONE',  ( 4.963854806921006002, 1.905440169433350484, -0.2825122895667788181 ) ) ;
#37369=CARTESIAN_POINT ( 'NONE',  ( 1.048812564444784989, -1.803156034432966681, 1.415383320267731726 ) ) ;
#37374=CARTESIAN_POINT ( 'NONE',  ( 4.073042245396302441, -1.645747789204109468, 1.492029542161198430 ) ) ;
#37380=CARTESIAN_POINT ( 'NONE',  ( 2.162732623366144136, 1.242727809108796322, 1.587836805404294171 ) ) ;
#37382=CARTESIAN_POINT ( 'NONE',  ( 6.373490837812130216, -0.2564121905142978664, 2.046633738985944806 ) ) ;
#37385=CARTESIAN_POINT ( 'NONE',  ( 6.251467208264422482, 1.735085017428819931, -0.1376019381845137446 ) ) ;
#37388=CARTESIAN_POINT ( 'NONE',  ( 2.547821756505376012, 1.769265940657601011, 0.04812675368598590825 ) ) ;
#37389=CARTESIAN_POINT ( 'NONE',  ( 1.213517774399593740, 1.944071949784083264, 0.5350861613380719639 ) ) ;
#37390=CARTESIAN_POINT ( 'NONE',  ( -0.1237769027084348328, -0.1346504581853508187, -1.811164470923332104 ) ) ;
#37391=CARTESIAN_POINT ( 'NONE',  ( 4.933284685991359275, -1.619851263076008019, -1.622297632854825755 ) ) ;
#37392=CARTESIAN_POINT ( 'NONE',  ( 3.363068133243895197, 1.796009578954290253, -0.4044003374430102382 ) ) ;
#37394=CARTESIAN_POINT ( 'NONE',  ( 3.715676801689533626, -1.798647723735953496, 0.3114480851732701061 ) ) ;
#37395=CARTESIAN_POINT ( 'NONE',  ( 5.098279808040273586, -0.2930726886911338425, 1.994869512123042199 ) ) ;
#37397=CARTESIAN_POINT ( 'NONE',  ( 3.538171838403024516, 1.019457259465136101, -2.019903332531754803 ) ) ;
#37399=CARTESIAN_POINT ( 'NONE',  ( 6.440466061264603859, 2.082495663875443714, 0.3126870252899079938 ) ) ;
#37402=CARTESIAN_POINT ( 'NONE',  ( 3.191909353267761151, -1.388477207968623839, -1.535938721777901472 ) ) ;
#37405=CARTESIAN_POINT ( 'NONE',  ( 6.340501840829311675, 1.221348521443364143, -1.733245716811770087 ) ) ;
#37408=CARTESIAN_POINT ( 'NONE',  ( 1.805176890173798565, 1.601487618425012638, 1.070529213009919101 ) ) ;
#37410=CARTESIAN_POINT ( 'NONE',  ( 6.403175662787183420, -1.665661181276241853, 1.050507712364300072 ) ) ;
#37415=CARTESIAN_POINT ( 'NONE',  ( 0.8970957097632881183, -2.168902827774013442, -0.4795612232612302961 ) ) ;
#37416=CARTESIAN_POINT ( 'NONE',  ( 3.680784645728672810, -2.029037780879865416, -0.5636793167548505012 ) ) ;
#37419=CARTESIAN_POINT ( 'NONE',  ( 0.7833917827068856976, -1.768883884249613736, 0.5786898513908571573 ) ) ;
#37424=CARTESIAN_POINT ( 'NONE',  ( 0.9320672075895162223, -2.067649466203642206, 0.4702014512557165515 ) ) ;
#37427=CARTESIAN_POINT ( 'NONE',  ( 4.000408739481801312, 1.952204270133122810, 0.1946113827649766925 ) ) ;
#37428=CARTESIAN_POINT ( 'NONE',  ( 1.604591590977550108, -0.7782141685120853580, -2.016947388195994062 ) ) ;
#37429=CARTESIAN_POINT ( 'NONE',  ( 2.261056740009634414, 1.805359621025553363, -0.3608742708730780513 ) ) ;
#37432=CARTESIAN_POINT ( 'NONE',  ( 3.433312839113885850, 0.7810296162102482453, -1.555295924109141303 ) ) ;
#37437=CARTESIAN_POINT ( 'NONE',  ( 0.5851287433712646369, -0.2658872486876809327, -2.145209338178376335 ) ) ;
#37438=CARTESIAN_POINT ( 'NONE',  ( 3.743517394402117837, -1.942243990624907823, -0.5404084370827856310 ) ) ;
#37441=CARTESIAN_POINT ( 'NONE',  ( 3.256668630020958410, -1.493913901992610205, 1.286540209188108630 ) ) ;
#37442=CARTESIAN_POINT ( 'NONE',  ( 6.509000000000021657, 1.267728212239338959, 2.115804336118334295 ) ) ;
#37443=CARTESIAN_POINT ( 'NONE',  ( 2.524863302051027159, -1.811236869417539141, 0.7011504990855742525 ) ) ;
#37444=CARTESIAN_POINT ( 'NONE',  ( 6.451426615364327155, -1.705040744490589066, 0.8662930942644477827 ) ) ;
#37452=CARTESIAN_POINT ( 'NONE',  ( 0.3939699847536023980, 1.636818068892214040, 1.480257586202008646 ) ) ;
#37454=CARTESIAN_POINT ( 'NONE',  ( 4.012515129279304205, 0.7020173944642660313, 1.832041770129029468 ) ) ;
#37456=CARTESIAN_POINT ( 'NONE',  ( 1.670546294658280084, 1.392546765991018454, 1.458555661489918442 ) ) ;
#37458=CARTESIAN_POINT ( 'NONE',  ( 2.325544253341553347, -1.572509993196508971, -1.418087145738779808 ) ) ;
#37462=CARTESIAN_POINT ( 'NONE',  ( 3.626748959588219634, -1.700609458330613055, 0.7059681596332522124 ) ) ;
#37466=CARTESIAN_POINT ( 'NONE',  ( 4.623349522974431025, 1.846400237221163865, 1.042759738753673338 ) ) ;
#37470=CARTESIAN_POINT ( 'NONE',  ( 4.956353021003493176, 0.7848952607251434843, 1.905660951107574608 ) ) ;
#37472=CARTESIAN_POINT ( 'NONE',  ( 2.911469271472226339, -0.9098125248445630975, -1.600700954789348263 ) ) ;
#37479=CARTESIAN_POINT ( 'NONE',  ( 1.858336453454629611, 2.200810804183956026, -0.1644699235988852648 ) ) ;
#37480=CARTESIAN_POINT ( 'NONE',  ( 3.831548730252303248, -2.092150397999822165, 0.8615055239265239084 ) ) ;
#37482=CARTESIAN_POINT ( 'NONE',  ( 3.621195883455626596, 1.556580008595293219, 0.9264731596013916493 ) ) ;
#37483=CARTESIAN_POINT ( 'NONE',  ( 4.047977829471119726, 0.9080738158676031624, 1.686857792009839097 ) ) ;
#37485=CARTESIAN_POINT ( 'NONE',  ( 4.118015666179648093, -1.012585719757435498, -1.691412322542594326 ) ) ;
#37486=CARTESIAN_POINT ( 'NONE',  ( 1.448133341116746964, 1.924057924963176180, 0.09734726817032554602 ) ) ;
#37487=CARTESIAN_POINT ( 'NONE',  ( 4.539837415608827698, 0.7997722286730184482, -1.691214532891088362 ) ) ;
#37488=CARTESIAN_POINT ( 'NONE',  ( 3.264621958926614109, 1.037573782609865436, 2.061359394274730583 ) ) ;
#37489=CARTESIAN_POINT ( 'NONE',  ( 4.510102262511601623, 1.860682779278443277, -0.04454786357706643635 ) ) ;
#37493=CARTESIAN_POINT ( 'NONE',  ( 0.3039231887648624619, -1.082844287645868375, -1.700959134490941160 ) ) ;
#37494=EDGE_CURVE ( 'NONE', #65102, #70481, #168799, .T. ) ;
#37496=CARTESIAN_POINT ( 'NONE',  ( 1.629656122859889811, -1.982562362509328047, 0.7109879831135539341 ) ) ;
#37500=CARTESIAN_POINT ( 'NONE',  ( 2.742561299210785286, 1.174483946500170184, -1.765453564165630596 ) ) ;
#37502=CARTESIAN_POINT ( 'NONE',  ( 0.7737015921927943296, 0.3898077916253924746, -1.981631471940727973 ) ) ;
#37507=CARTESIAN_POINT ( 'NONE',  ( 2.442841770826277958, 0.4709965094221583159, 2.109507199432036018 ) ) ;
#37510=CARTESIAN_POINT ( 'NONE',  ( 6.925078400183531713, 2.446544591822760850, 2.338552149501707422 ) ) ;
#37513=CARTESIAN_POINT ( 'NONE',  ( 5.524625123954316486, 0.3981063221985549072, 1.976670730632006601 ) ) ;
#37515=CARTESIAN_POINT ( 'NONE',  ( 0.2752733618501881363, 2.042644424557562122, -0.7945232813236638991 ) ) ;
#37517=CARTESIAN_POINT ( 'NONE',  ( 0.6907310396802420760, -2.245820052064306349, -0.2739839911451089627 ) ) ;
#37524=CARTESIAN_POINT ( 'NONE',  ( 4.160587402808674007, -1.276020550970466516, 1.160787852381778062 ) ) ;
#37526=CARTESIAN_POINT ( 'NONE',  ( 1.580939025779507956, 1.637719487297364163, -0.6712238910871449749 ) ) ;
#37527=CARTESIAN_POINT ( 'NONE',  ( 2.824860481609407614, 1.456601328488495106, -1.389772560336500318 ) ) ;
#37528=CARTESIAN_POINT ( 'NONE',  ( 4.788207028248289809, -1.043783763870303360, 1.944324211313207318 ) ) ;
#37530=CARTESIAN_POINT ( 'NONE',  ( 4.236585392707596043, 1.239412559483305198, -1.594744479876673005 ) ) ;
#37532=CARTESIAN_POINT ( 'NONE',  ( 4.512424090126602394, -2.120028616272570332, -0.05109941365945279423 ) ) ;
#37533=CARTESIAN_POINT ( 'NONE',  ( 4.569935513796226978, -0.9480243344661150040, 1.779636403143824985 ) ) ;
#37538=CARTESIAN_POINT ( 'NONE',  ( 1.955717210371358483, 1.865846021326333926, -0.1348392221205765851 ) ) ;
#37540=CARTESIAN_POINT ( 'NONE',  ( 6.199861008060345569, 1.254605797456327831, 1.306922710324806225 ) ) ;
#37545=CARTESIAN_POINT ( 'NONE',  ( -0.2108831679770960255, -0.001785917861228669690, -1.896958272444612792 ) ) ;
#37547=CARTESIAN_POINT ( 'NONE',  ( 1.873419974815058842, -0.2433403713097622156, 1.946663811685337420 ) ) ;
#37550=CARTESIAN_POINT ( 'NONE',  ( 3.920270587443939636, -2.114697630030224929, 0.1593259359235904837 ) ) ;
#37553=CARTESIAN_POINT ( 'NONE',  ( 5.026621361268301946, 1.885657091993764745, 0.5748499752153258813 ) ) ;
#37555=CARTESIAN_POINT ( 'NONE',  ( 0.8088407350804104334, -0.4930801656862683346, -1.951752914270672212 ) ) ;
#37557=CARTESIAN_POINT ( 'NONE',  ( 0.8786900280967164800, -0.5185874880111912555, -2.052613615991748297 ) ) ;
#37559=CARTESIAN_POINT ( 'NONE',  ( 3.086448098943677998, 1.152334561581969785, -1.719836228861029603 ) ) ;
#37564=CARTESIAN_POINT ( 'NONE',  ( 4.998031443873323099, -0.7039345487453112504, -1.968691415026160962 ) ) ;
#37566=CARTESIAN_POINT ( 'NONE',  ( 3.627796970749700201, -1.086779551322129445, -1.466705181690882709 ) ) ;
#37567=CARTESIAN_POINT ( 'NONE',  ( 1.576514528963068429, -1.280961997807128938, 1.281107859597712118 ) ) ;
#37571=CARTESIAN_POINT ( 'NONE',  ( 4.208205882762393379, -2.201082536721191474, 0.1591639695062776749 ) ) ;
#37575=CARTESIAN_POINT ( 'NONE',  ( 3.826736342760712173, 1.350229473097919630, -1.354399478966497261 ) ) ;
#37578=CARTESIAN_POINT ( 'NONE',  ( 6.232888004217203459, -1.964670499678453197, -0.6532144590316590893 ) ) ;
#37579=CARTESIAN_POINT ( 'NONE',  ( 5.478137895480934105, -2.137967713159651506, -0.4810252310911074525 ) ) ;
#37587=CARTESIAN_POINT ( 'NONE',  ( 3.198369223161025676, -0.5396142385952484855, -1.791042426047453784 ) ) ;
#37592=CARTESIAN_POINT ( 'NONE',  ( 6.473496638176248652, -0.2593738453590052617, 2.053908440964563376 ) ) ;
#37593=CARTESIAN_POINT ( 'NONE',  ( 0.6851730022342136239, 1.650096953764205399, 1.158669022729153175 ) ) ;
#37597=CARTESIAN_POINT ( 'NONE',  ( 1.623246906879351581, -2.062630869249089116, 0.7406334225198917265 ) ) ;
#37598=CARTESIAN_POINT ( 'NONE',  ( 5.971303284387838417, 0.1295235881030691594, -1.821162830480331563 ) ) ;
#37606=CARTESIAN_POINT ( 'NONE',  ( 4.194743914777058436, 1.481411246205705412, 1.093257649623424754 ) ) ;
#37607=CARTESIAN_POINT ( 'NONE',  ( 0.8912715949961318440, -0.05164314158133917476, -2.012595864970234238 ) ) ;
#37608=CARTESIAN_POINT ( 'NONE',  ( 1.986132587416184370, 2.144477605524505393, 0.8272852225373708013 ) ) ;
#37610=CARTESIAN_POINT ( 'NONE',  ( 6.121922100595678096, 1.933298025717408608, -0.3319332437697538607 ) ) ;
#37614=CARTESIAN_POINT ( 'NONE',  ( 4.992401499097729456, -1.057410677138232780, 1.593263788312593743 ) ) ;
#37618=CARTESIAN_POINT ( 'NONE',  ( 2.911755628046075906, -1.032623549580795608, -1.817877418097467501 ) ) ;
#37619=CARTESIAN_POINT ( 'NONE',  ( 2.254581950620972997, -1.447608085528677480, 1.184820545849271767 ) ) ;
#37622=CARTESIAN_POINT ( 'NONE',  ( 3.350842269037973331, 0.4194941847268919832, -1.688999647770361490 ) ) ;
#37626=CARTESIAN_POINT ( 'NONE',  ( 4.195721234439112379, -0.6572638427989171417, 1.594953032058670894 ) ) ;
#37627=CARTESIAN_POINT ( 'NONE',  ( 3.984055765753656164, -2.167877601896048390, -0.3204034371554059235 ) ) ;
#37628=CARTESIAN_POINT ( 'NONE',  ( 5.988949835885216011, -0.3198878037087344306, -2.183464699167809275 ) ) ;
#37631=CARTESIAN_POINT ( 'NONE',  ( 3.696278757040452057, 0.9809249153905131857, -1.936940462344426628 ) ) ;
#37632=CARTESIAN_POINT ( 'NONE',  ( 2.244514701088017539, 0.3993153960501935051, 1.781317584591130432 ) ) ;
#37634=CARTESIAN_POINT ( 'NONE',  ( 4.171193994350897327, 1.889596262492127199, -0.9554925290978563135 ) ) ;
#37637=CARTESIAN_POINT ( 'NONE',  ( 5.196947908113320302, 1.872795242347685463, 1.321741379092307600 ) ) ;
#37639=CARTESIAN_POINT ( 'NONE',  ( 6.620655732516644854, 4.701125524277991907, 2.388986273831222640 ) ) ;
#37641=CARTESIAN_POINT ( 'NONE',  ( 0.3816889160728508812, 0.2035859187828891470, -2.110680546376259681 ) ) ;
#37649=CARTESIAN_POINT ( 'NONE',  ( 5.151017605526480025, 0.9962996879465220168, 1.753031629501592192 ) ) ;
#37651=CARTESIAN_POINT ( 'NONE',  ( 4.557522945366278222, 1.653560713460072051, 1.232637662666216549 ) ) ;
#37653=FACE_OUTER_BOUND ( 'NONE', #174303, .T. ) ;
#37658=CARTESIAN_POINT ( 'NONE',  ( 0.1817335109410072314, -0.9834369453871127931, 1.844881371607492326 ) ) ;
#37659=CARTESIAN_POINT ( 'NONE',  ( 4.430314669760617718, -1.560499787156752971, -1.277043788614096176 ) ) ;
#37660=CARTESIAN_POINT ( 'NONE',  ( 3.315785976855676775, 1.165629053876730659, -1.425327459889616177 ) ) ;
#37664=CARTESIAN_POINT ( 'NONE',  ( 0.4106395295978342297, 1.496939291644447279, 0.8566152473860905170 ) ) ;
#37666=CARTESIAN_POINT ( 'NONE',  ( 0.6338907866723633155, 0.6742984703760960263, 2.197570948669794966 ) ) ;
#37668=CARTESIAN_POINT ( 'NONE',  ( 0.4216216942964992609, -0.1093418885590720091, 2.259903825829346680 ) ) ;
#37669=CARTESIAN_POINT ( 'NONE',  ( 3.229229631591294503, 0.05193219833012594627, 2.105601595880735033 ) ) ;
#37673=CARTESIAN_POINT ( 'NONE',  ( 6.281249999999699796, 0.7852924748228357066, 1.895863743163936022 ) ) ;
#37678=CARTESIAN_POINT ( 'NONE',  ( 2.443736651115399283, -1.977012053918187906, 0.7674769708189137507 ) ) ;
#37679=CARTESIAN_POINT ( 'NONE',  ( 3.533611464748823927, -0.1604399991079318022, 2.215644447872004985 ) ) ;
#37680=CARTESIAN_POINT ( 'NONE',  ( 1.834175572193702530, 2.167931929539984814, 0.3193665180123914094 ) ) ;
#37683=CARTESIAN_POINT ( 'NONE',  ( 6.039501783790233169, 1.813256598412491982, -0.7494862575098264479 ) ) ;
#37687=ORIENTED_EDGE ( 'NONE', *, *, #102848, .T. ) ;
#37688=CARTESIAN_POINT ( 'NONE',  ( 4.605793411009856619, 1.573235607984494688, 1.422142093439874522 ) ) ;
#37692=CARTESIAN_POINT ( 'NONE',  ( 6.350466702034289312, 0.6732396885240909956, 2.054270918568662729 ) ) ;
#37694=CARTESIAN_POINT ( 'NONE',  ( 5.091278345985558396, -0.6575378499774006125, 1.720029930423284448 ) ) ;
#37698=CARTESIAN_POINT ( 'NONE',  ( 0.5908509756735094154, -0.6286620326499070543, 1.623129586062905805 ) ) ;
#37702=CARTESIAN_POINT ( 'NONE',  ( 5.207972885698374022, -2.151664816535401314, 0.2080130470862306957 ) ) ;
#37706=CARTESIAN_POINT ( 'NONE',  ( 4.944278945467968533, 2.155654431248493985, 0.1625706239713892443 ) ) ;
#37707=CARTESIAN_POINT ( 'NONE',  ( 5.378184286887115029, -1.097432272127541131, 1.637457850930480241 ) ) ;
#37708=CARTESIAN_POINT ( 'NONE',  ( 3.919074646851735455, 0.6231337533108800564, 1.618193163429545223 ) ) ;
#37709=CARTESIAN_POINT ( 'NONE',  ( 1.101424459656743071, -0.5276332240332289869, 2.126988402630063835 ) ) ;
#37710=CARTESIAN_POINT ( 'NONE',  ( 1.747554699363640607, -1.948627443588932806, 1.235768562340158194 ) ) ;
#37711=CARTESIAN_POINT ( 'NONE',  ( 3.444654265643578128, 0.4973230594479564060, 1.999757164544394561 ) ) ;
#37712=CARTESIAN_POINT ( 'NONE',  ( 0.3572357504952353158, 1.920940290975415854, -0.2841381762913769427 ) ) ;
#37717=CARTESIAN_POINT ( 'NONE',  ( 3.083271082906696048, -0.1608111237268796401, -2.200959079826501075 ) ) ;
#37720=CARTESIAN_POINT ( 'NONE',  ( 0.2505320230819003680, -0.3960800208489853036, -1.824604621477694311 ) ) ;
#37721=CARTESIAN_POINT ( 'NONE',  ( -0.1288028175206881731, 1.984098898469729200, -2.687169534535143178 ) ) ;
#37724=CARTESIAN_POINT ( 'NONE',  ( 6.825078400183572036, 7.629137130509069387, 2.744348168701661095 ) ) ;
#37727=CARTESIAN_POINT ( 'NONE',  ( 3.327077596220921141, 0.04893577929474152155, 2.060475874978876298 ) ) ;
#37730=CARTESIAN_POINT ( 'NONE',  ( -0.1290005225502922348, 7.629137130509076492, -2.773995091683972625 ) ) ;
#37732=EDGE_CURVE ( 'NONE', #90486, #100328, #131377, .T. ) ;
#37735=CARTESIAN_POINT ( 'NONE',  ( 1.463821189631772990, 2.030551501382936497, -0.3513165408277911794 ) ) ;
#37741=CARTESIAN_POINT ( 'NONE',  ( 5.672569038193632451, -1.402732290180560337, 1.703733612381942653 ) ) ;
#37742=CARTESIAN_POINT ( 'NONE',  ( 0.2280961430754513408, -1.329988288769240024, -1.704746276402234528 ) ) ;
#37745=CARTESIAN_POINT ( 'NONE',  ( 0.3215004009857677092, -1.429452135790244549, -1.422604240635255479 ) ) ;
#37746=CARTESIAN_POINT ( 'NONE',  ( 1.529136539685072238, 2.264261833246409505, -0.3938019620175516322 ) ) ;
#37748=CARTESIAN_POINT ( 'NONE',  ( 6.375647946566725288, 0.3219878414668366218, -1.884816399834337686 ) ) ;
#37750=CARTESIAN_POINT ( 'NONE',  ( 1.516246529245099284, 1.258767711876613848, -1.383943980506313398 ) ) ;
#37751=CARTESIAN_POINT ( 'NONE',  ( 3.362517798112668821, -1.944730434982215650, -0.5331690889110105580 ) ) ;
#37753=CARTESIAN_POINT ( 'NONE',  ( 6.639320575229257670, 2.033582276073117701, 2.408309898857839304 ) ) ;
#37756=CARTESIAN_POINT ( 'NONE',  ( 5.549480973255512595, -1.659368771798474196, -1.296820645603852018 ) ) ;
#37761=CARTESIAN_POINT ( 'NONE',  ( 3.761977063697896639, 0.6766415394236917624, -1.903234751996728757 ) ) ;
#37764=CARTESIAN_POINT ( 'NONE',  ( 0.2860855845884663351, -1.266418373674676134, -1.628825195542679793 ) ) ;
#37766=CARTESIAN_POINT ( 'NONE',  ( 5.518883860308030798, 1.994880785013030788, 0.8329173350848093627 ) ) ;
#37771=CARTESIAN_POINT ( 'NONE',  ( 2.629531826656985150, 0.1086732114553476541, -2.168588674111065817 ) ) ;
#37774=CARTESIAN_POINT ( 'NONE',  ( 2.014959344526063845, -1.785600367564584179, 0.4486904387498573676 ) ) ;
#37776=CARTESIAN_POINT ( 'NONE',  ( 2.964592600559623037, -2.025863808726846127, -0.8364240203130177687 ) ) ;
#37777=FACE_OUTER_BOUND ( 'NONE', #175724, .T. ) ;
#37778=CARTESIAN_POINT ( 'NONE',  ( 4.926805006903203221, 2.163674774341369123, 0.6614253976126910350 ) ) ;
#37785=CARTESIAN_POINT ( 'NONE',  ( 5.975818619601467319, 1.055637459841787473, 1.420274316496936917 ) ) ;
#37788=CARTESIAN_POINT ( 'NONE',  ( 2.327300794530688055, -0.001011052439145453856, 2.106147100168444197 ) ) ;
#37791=CARTESIAN_POINT ( 'NONE',  ( 1.978894816976022097, 1.836590731562221412, 0.7118427970769640734 ) ) ;
#37794=CARTESIAN_POINT ( 'NONE',  ( 6.064714483498689468, 0.5772776769059180246, 1.717211531030158556 ) ) ;
#37799=CARTESIAN_POINT ( 'NONE',  ( 5.102362337376947998, -0.6309395149336484154, -1.761181640970374884 ) ) ;
#37800=CARTESIAN_POINT ( 'NONE',  ( 6.069205674026176389, 1.823072449729469247, 0.9810699074010442722 ) ) ;
#37810=CARTESIAN_POINT ( 'NONE',  ( 5.195737816846159873, -1.386088135442983260, -1.388664821390848347 ) ) ;
#37812=CARTESIAN_POINT ( 'NONE',  ( 3.198592129611950607, -1.351947076146834403, -1.495823048609262296 ) ) ;
#37813=CARTESIAN_POINT ( 'NONE',  ( 2.079167605185348044, 1.483516914179264790, 1.212129443301296128 ) ) ;
#37815=CARTESIAN_POINT ( 'NONE',  ( -0.04112450405316381286, -1.960553898366865555, -0.9795403211517728082 ) ) ;
#37816=CARTESIAN_POINT ( 'NONE',  ( 2.336979506217982117, -1.672866993182718698, 0.8370366242000035761 ) ) ;
#37818=CARTESIAN_POINT ( 'NONE',  ( 4.183843882646627321, 1.951733592454238497, -0.4931575689418183917 ) ) ;
#37821=CARTESIAN_POINT ( 'NONE',  ( 4.394233635046361108, -0.9068805580662200327, -1.913321081533605028 ) ) ;
#37823=CARTESIAN_POINT ( 'NONE',  ( 6.496543107701719499, 2.047251205643263017, 0.3077783505985449142 ) ) ;
#37824=CARTESIAN_POINT ( 'NONE',  ( 1.487951815845720338, -2.081006265264739419, -0.2013860056617396421 ) ) ;
#37825=CARTESIAN_POINT ( 'NONE',  ( 6.194357462883206544, -1.817092693925310032, -0.1759843941628037589 ) ) ;
#37837=CARTESIAN_POINT ( 'NONE',  ( 0.3108108888784698598, 1.507076236086818399, -1.004716094995859121 ) ) ;
#37844=CARTESIAN_POINT ( 'NONE',  ( 5.817982510940042040, 0.9913841921252890543, -1.755779027446252138 ) ) ;
#37845=CARTESIAN_POINT ( 'NONE',  ( -0.09290056220616692284, -0.4702265987995763452, -2.075310686570643437 ) ) ;
#37846=CARTESIAN_POINT ( 'NONE',  ( 6.983263157960373668, 7.629137130509066722, 2.546189081643289942 ) ) ;
#37851=CARTESIAN_POINT ( 'NONE',  ( 3.010559277710533888, 0.6591459557328577246, 1.856027811050243947 ) ) ;
#37852=CARTESIAN_POINT ( 'NONE',  ( 4.675407748274028386, 1.496063595514389943, 1.352143027241403450 ) ) ;
#37854=FILL_AREA_STYLE ('',( #140465 ) ) ;
#37856=CARTESIAN_POINT ( 'NONE',  ( 5.138714532536901913, -1.880766731008373993, 1.124575086929799239 ) ) ;
#37858=CARTESIAN_POINT ( 'NONE',  ( 3.012629298554883484, 1.396463203792638996, -1.327218363718547511 ) ) ;
#37860=CARTESIAN_POINT ( 'NONE',  ( -0.1296875068448125334, 4.095146142119266308, -2.381513845672214913 ) ) ;
#37861=CARTESIAN_POINT ( 'NONE',  ( 0.1884680354247054990, -1.036234488384666586, 1.948478269905975946 ) ) ;
#37867=CARTESIAN_POINT ( 'NONE',  ( 4.575031941739591268, 1.798972412501558260, 0.8019633677735745758 ) ) ;
#37869=CARTESIAN_POINT ( 'NONE',  ( 0.3802858058059845336, -0.2390265653847540028, -1.927249604900363122 ) ) ;
#37870=CARTESIAN_POINT ( 'NONE',  ( 3.510405448560415032, -2.010878083398774052, -0.09666398930169986525 ) ) ;
#37871=CARTESIAN_POINT ( 'NONE',  ( 5.009243775243890973, 2.291699508649183592, 0.1762380284849179579 ) ) ;
#37873=CARTESIAN_POINT ( 'NONE',  ( 4.328838875689292820, -1.735142615721802395, -0.6730405439913983434 ) ) ;
#37879=CARTESIAN_POINT ( 'NONE',  ( 0.8553300576445364012, 0.4222666777726029608, -2.150330908352434012 ) ) ;
#37883=CARTESIAN_POINT ( 'NONE',  ( 0.04711308451243316486, -1.408776630263553375, -1.161003007932148501 ) ) ;
#37885=CARTESIAN_POINT ( 'NONE',  ( 2.742450610247765486, 1.725592070310760118, -0.1720703960508932762 ) ) ;
#37887=CARTESIAN_POINT ( 'NONE',  ( 6.509000000000048303, 0.5949247728001515467, 1.954148248227548290 ) ) ;
#37890=CARTESIAN_POINT ( 'NONE',  ( 0.7255434793691470929, 0.2065170452952343472, -2.059959488672699290 ) ) ;
#37891=CARTESIAN_POINT ( 'NONE',  ( 5.760330229460346452, 0.7440287100829169331, 1.667389206893993725 ) ) ;
#37892=CARTESIAN_POINT ( 'NONE',  ( 3.186327686730246800, 1.093712407854827706, -1.628379936052851917 ) ) ;
#37897=CARTESIAN_POINT ( 'NONE',  ( 3.422626747576805961, -0.8610355553571764631, -1.937992358232228041 ) ) ;
#37900=CARTESIAN_POINT ( 'NONE',  ( 1.358353136502856939, -2.070434559563800736, -0.003889755252693693176 ) ) ;
#37904=CARTESIAN_POINT ( 'NONE',  ( 4.670683837814712192, 0.8496151569591952057, 2.052583376702998397 ) ) ;
#37906=CARTESIAN_POINT ( 'NONE',  ( 1.600609022366938916, -0.2761435782051116505, 2.281986030651184993 ) ) ;
#37915=CARTESIAN_POINT ( 'NONE',  ( 2.724755696555291262, 1.382288352666941389, -1.321784923088549446 ) ) ;
#37917=CARTESIAN_POINT ( 'NONE',  ( 4.453923018928796829, 1.724380149092176850, -0.04373908735122617603 ) ) ;
#37918=CARTESIAN_POINT ( 'NONE',  ( 2.448454179885678705, -1.387098808145654560, 1.463928423225707931 ) ) ;
#37919=CARTESIAN_POINT ( 'NONE',  ( 3.832918613053246659, 0.7734572015929435107, -2.164792806810557746 ) ) ;
#37921=CARTESIAN_POINT ( 'NONE',  ( 5.971333374016301043, 0.1563851966441217600, -2.100315135224324337 ) ) ;
#37924=CARTESIAN_POINT ( 'NONE',  ( 4.604631121011967920, 1.368492104089440442, -1.122162792211104820 ) ) ;
#37926=CARTESIAN_POINT ( 'NONE',  ( 0.3051332635122120385, 1.997493689478089252, 1.124391992203729540 ) ) ;
#37927=CARTESIAN_POINT ( 'NONE',  ( 5.103375755629981469, -1.831930319445294719, 0.1838923505294575433 ) ) ;
#37929=CARTESIAN_POINT ( 'NONE',  ( 6.105464321129510097, -2.175355461714892691, 0.2646407054325700670 ) ) ;
#37933=CARTESIAN_POINT ( 'NONE',  ( 5.793440749948310042, -1.873300974885267589, 0.8818263447485861217 ) ) ;
#37934=CARTESIAN_POINT ( 'NONE',  ( 1.534389036647098692, 0.6371565916030231813, 1.913260934284975345 ) ) ;
#37936=CARTESIAN_POINT ( 'NONE',  ( 4.125552361149776637, -1.843237290211484192, 0.5602470265201089372 ) ) ;
#37938=CARTESIAN_POINT ( 'NONE',  ( 1.617743263029525869, 1.850308847857740968, 1.228972131997711381 ) ) ;
#37947=CARTESIAN_POINT ( 'NONE',  ( 4.704519267438088015, 1.517481324781422503, 0.8521212890505409643 ) ) ;
#37948=CARTESIAN_POINT ( 'NONE',  ( 2.594135478747404022, 0.9273930874063830432, -1.728848471177657942 ) ) ;
#37953=CARTESIAN_POINT ( 'NONE',  ( 6.408651779211167465, 0.6141799454031526828, 1.863335524608072502 ) ) ;
#37956=CARTESIAN_POINT ( 'NONE',  ( 5.085172837459294826, 1.651341431264556014, 1.157102043685846793 ) ) ;
#37957=CARTESIAN_POINT ( 'NONE',  ( 1.270828881381684150, -1.433710284283566949, 1.750253757905173124 ) ) ;
#37961=CARTESIAN_POINT ( 'NONE',  ( 1.862360739135361376, -1.326353699019737098, 1.319252464149045734 ) ) ;
#37962=CARTESIAN_POINT ( 'NONE',  ( 0.5626190647941519130, -0.9651924803987484980, 1.440457774218842690 ) ) ;
#37964=CARTESIAN_POINT ( 'NONE',  ( 4.722331747100577459, 2.097238624054961864, 0.6360808509995665716 ) ) ;
#37965=CARTESIAN_POINT ( 'NONE',  ( 5.491387719013633983, 2.038315193044057505, -1.081779828593228521 ) ) ;
#37966=CARTESIAN_POINT ( 'NONE',  ( 6.485628570817172367, 1.417799985879987901, 1.495801911481582813 ) ) ;
#37967=CARTESIAN_POINT ( 'NONE',  ( 3.099484260031000193, -1.939694849350329431, 0.09605879933238459234 ) ) ;
#37972=CARTESIAN_POINT ( 'NONE',  ( 4.711564657724523819, 1.930417226389494090, 0.5826574956761670920 ) ) ;
#37976=CARTESIAN_POINT ( 'NONE',  ( 0.8557438351849018243, 1.823752217391808372, -0.08689656109241167270 ) ) ;
#37982=CARTESIAN_POINT ( 'NONE',  ( 6.209851105358469958, -2.045643633555578766, 0.2495701479476707119 ) ) ;
#37986=CARTESIAN_POINT ( 'NONE',  ( 5.426427855750480589, -0.9099042507111715361, -1.803185865349592021 ) ) ;
#37987=CARTESIAN_POINT ( 'NONE',  ( 5.988988838570013407, -2.108473666775429134, -0.6992015888120094447 ) ) ;
#37991=STYLED_ITEM ( 'NONE', ( #177906 ), #24912 ) ;
#37992=CARTESIAN_POINT ( 'NONE',  ( 5.752824481226431530, -1.626044790292068498, 1.266090340377580947 ) ) ;
#37993=CARTESIAN_POINT ( 'NONE',  ( 4.342422763466713853, 0.4390309838058319425, -1.967887491402267486 ) ) ;
#38000=CARTESIAN_POINT ( 'NONE',  ( 3.813827237909522605, -1.649828814528127907, 1.158511658058670957 ) ) ;
#38001=CARTESIAN_POINT ( 'NONE',  ( 3.486116527793288178, -0.3603757036649730128, -1.805346353211812804 ) ) ;
#38003=CARTESIAN_POINT ( 'NONE',  ( 2.403307275528394626, 1.852421531443759539, -1.376039175078101806 ) ) ;
#38005=CARTESIAN_POINT ( 'NONE',  ( 4.552137767457805850, 2.161219302129935738, -0.04802546048104232301 ) ) ;
#38007=CARTESIAN_POINT ( 'NONE',  ( 6.603072989126265391, -0.3962418105841297722, 1.804722624154910360 ) ) ;
#38010=CARTESIAN_POINT ( 'NONE',  ( 4.112918304081806475, 0.7786346584819616723, -2.162581562504022337 ) ) ;
#38013=CARTESIAN_POINT ( 'NONE',  ( 2.254581950620972997, -1.447608085528677480, 1.184820545849271767 ) ) ;
#38014=CARTESIAN_POINT ( 'NONE',  ( 6.614144449397460157, -0.9292204182751627739, -1.738729380627493049 ) ) ;
#38017=CARTESIAN_POINT ( 'NONE',  ( 2.121956728516772639, -2.140194184088719531, 0.5379336890513550795 ) ) ;
#38024=CARTESIAN_POINT ( 'NONE',  ( 6.684453674706574589, -1.933370886519528264, -0.3848441959667763257 ) ) ;
#38025=CARTESIAN_POINT ( 'NONE',  ( 6.024106105913028308, -1.276746162841462695, -1.922164112325924989 ) ) ;
#38026=CARTESIAN_POINT ( 'NONE',  ( 0.5374593765826127800, 1.831924746014142791, -0.7026076897959919743 ) ) ;
#38027=CARTESIAN_POINT ( 'NONE',  ( 4.135635188098309101, 1.943850041002512352, -0.6901024340064102480 ) ) ;
#38035=CARTESIAN_POINT ( 'NONE',  ( 6.777770921962916972, -2.107754466287181661, 0.5206637005944132479 ) ) ;
#38038=CARTESIAN_POINT ( 'NONE',  ( 4.950658015114751009, -1.558304906039936988, -0.9804572199803849308 ) ) ;
#38041=CARTESIAN_POINT ( 'NONE',  ( 0.4560483712790652233, 0.7097975879313439540, 1.730851494400275747 ) ) ;
#38047=CARTESIAN_POINT ( 'NONE',  ( 2.131405713275540847, -1.153620894759581184, -1.342296593837268848 ) ) ;
#38048=CARTESIAN_POINT ( 'NONE',  ( 6.235026786510912800, 1.879206351595325231, 0.7223523585505615685 ) ) ;
#38050=CARTESIAN_POINT ( 'NONE',  ( 4.517137023955775099, -1.749796063449124084, 0.7800368752974867759 ) ) ;
#38051=CARTESIAN_POINT ( 'NONE',  ( -0.1409997244346088141, 1.357410162930408504, -2.254437325861287533 ) ) ;
#38052=CARTESIAN_POINT ( 'NONE',  ( 4.967230218399325103, 1.712698785223613740, 0.9724057732015491951 ) ) ;
#38053=CARTESIAN_POINT ( 'NONE',  ( 6.310808155552376952, -0.5427901682961560059, -1.945386456709609524 ) ) ;
#38056=CARTESIAN_POINT ( 'NONE',  ( 2.518242125168220102, 1.223528130051700025, -1.415109699333151561 ) ) ;
#38057=CARTESIAN_POINT ( 'NONE',  ( 6.076716319674939193, -1.640139352550730401, -0.5342243915677049593 ) ) ;
#38059=CARTESIAN_POINT ( 'NONE',  ( 3.352369063006555905, 2.207063162671081713, 4.936380160885933677E-05 ) ) ;
#38063=CARTESIAN_POINT ( 'NONE',  ( 0.8540550061131615411, -0.7440666694851668650, 1.923960566027690833 ) ) ;
#38070=CARTESIAN_POINT ( 'NONE',  ( 3.648938843998358106, -0.4010542052625790110, -2.030977206718207473 ) ) ;
#38074=CARTESIAN_POINT ( 'NONE',  ( 0.8033855960881201019, 1.780198652630104794, -0.9539489498650125521 ) ) ;
#38077=CARTESIAN_POINT ( 'NONE',  ( 0.1745949693968875116, 2.894395776691494060, -2.244452406707102110 ) ) ;
#38079=CARTESIAN_POINT ( 'NONE',  ( 6.872432811717262169, -0.4447407475622888740, 1.973694069355651282 ) ) ;
#38080=CARTESIAN_POINT ( 'NONE',  ( 6.315652784560811916, -1.257152391787072387, -1.445590397462018117 ) ) ;
#38081=CARTESIAN_POINT ( 'NONE',  ( 6.639320575229288757, 4.694344378759712555, 2.565881548192010975 ) ) ;
#38082=CARTESIAN_POINT ( 'NONE',  ( 3.280998142716429200, 1.980384277226649559, -0.9389412094223739125 ) ) ;
#38084=CARTESIAN_POINT ( 'NONE',  ( 2.302860652515531292, -0.3306829512400177862, -1.883434002855538081 ) ) ;
#38089=CARTESIAN_POINT ( 'NONE',  ( 1.511342449054883241, -1.897691915346022329, 0.6820157586827847451 ) ) ;
#38091=CARTESIAN_POINT ( 'NONE',  ( 5.759372899636661991, 2.159370146098410714, -0.3733810082120898044 ) ) ;
#38093=CARTESIAN_POINT ( 'NONE',  ( 2.678358392608829686, -1.649718294651691730, -0.5031959223205755283 ) ) ;
#38095=CARTESIAN_POINT ( 'NONE',  ( -0.1399997263889611598, 6.947783040739049731, -2.595329734540325006 ) ) ;
#38099=CARTESIAN_POINT ( 'NONE',  ( 1.029656018189710309, 1.891699080040713410, -0.5197978237033785698 ) ) ;
#38106=CARTESIAN_POINT ( 'NONE',  ( 3.633306742369224462, -0.1297899475344466980, 1.806866856981071967 ) ) ;
#38110=CARTESIAN_POINT ( 'NONE',  ( 4.582537834466095639, -1.179681096148448738, 1.374793604838970396 ) ) ;
#38114=CARTESIAN_POINT ( 'NONE',  ( 5.371493315669001234, -0.2729949515532895110, 1.840801060123838706 ) ) ;
#38116=CARTESIAN_POINT ( 'NONE',  ( 2.354979200267411255, 0.09147625538302081583, -1.913532508166473800 ) ) ;
#38124=CARTESIAN_POINT ( 'NONE',  ( 1.236401392562349155, 0.4093969531599008227, 2.049976805931138735 ) ) ;
#38126=CARTESIAN_POINT ( 'NONE',  ( 0.09436191691250192526, -0.3928898508825870439, -1.789253991261535726 ) ) ;
#38128=CARTESIAN_POINT ( 'NONE',  ( 2.133574855335911291, -1.190200692204022470, -1.384352166806518625 ) ) ;
#38131=CARTESIAN_POINT ( 'NONE',  ( 2.056764645581514728, 0.4224895836346024280, 1.864965418913032913 ) ) ;
#38132=CARTESIAN_POINT ( 'NONE',  ( 1.943746065852373972, 1.356001085411572049, 1.428673526509681047 ) ) ;
#38133=CARTESIAN_POINT ( 'NONE',  ( 3.333474266508968054, 0.8707927262202612706, -1.735945723835415677 ) ) ;
#38138=CARTESIAN_POINT ( 'NONE',  ( 3.814780496183818315, -0.6684712460508880350, -2.012520831323429515 ) ) ;
#38142=PLANE ( 'NONE',  #97876 ) ;
#38145=CARTESIAN_POINT ( 'NONE',  ( 3.668406916800326822, -1.225078373119499187, 1.353803248016255178 ) ) ;
#38146=CARTESIAN_POINT ( 'NONE',  ( 6.122279814772176643, 1.995267444086584296, 0.2910868170948808786 ) ) ;
#38151=CARTESIAN_POINT ( 'NONE',  ( 6.925078400183575233, 7.629137130509070275, 2.455651831298297338 ) ) ;
#38152=CARTESIAN_POINT ( 'NONE',  ( 4.328871119428026049, 0.09166491666120352155, 1.868520897946590598 ) ) ;
#38154=CARTESIAN_POINT ( 'NONE',  ( 1.734862838405337060, 0.1885825406544305305, 1.917253122483292715 ) ) ;
#38160=CARTESIAN_POINT ( 'NONE',  ( 0.8962975493561256002, -0.9559892387472949116, -1.889204697816506240 ) ) ;
#38163=CARTESIAN_POINT ( 'NONE',  ( 4.803616497939601437, -1.596918191575155133, -1.317456641179854726 ) ) ;
#38164=CARTESIAN_POINT ( 'NONE',  ( 0.2570343420702363435, 1.821350608449383124, -0.2692129421619017804 ) ) ;
#38166=CARTESIAN_POINT ( 'NONE',  ( 5.256544959696739738, 2.216068975266134000, -0.6104820095701003480 ) ) ;
#38170=CARTESIAN_POINT ( 'NONE',  ( 1.711265200625663008, -0.2773638578843647950, 2.275360193931966535 ) ) ;
#38174=CARTESIAN_POINT ( 'NONE',  ( 5.999939506776140519, -0.7010436009657755596, -1.811167765765375526 ) ) ;
#38178=CARTESIAN_POINT ( 'NONE',  ( -0.07006079923273231258, -1.973546630392996493, 0.3967976802892440036 ) ) ;
#38179=CARTESIAN_POINT ( 'NONE',  ( 5.841029835422532734, -1.731992920607817288, -1.032484497598872064 ) ) ;
#38183=CARTESIAN_POINT ( 'NONE',  ( 2.994169869935947137, -0.6075897704641713970, -2.000389221998987832 ) ) ;
#38184=CARTESIAN_POINT ( 'NONE',  ( 0.9886869571070689977, 1.563518247070281086, -0.8293041508813036033 ) ) ;
#38185=CARTESIAN_POINT ( 'NONE',  ( 6.451795992440088057, -1.844709169062180409, -0.8146298745319994206 ) ) ;
#38187=CARTESIAN_POINT ( 'NONE',  ( 3.767766022312348362, 1.272560033980062455, 1.906398719306565681 ) ) ;
#38188=CARTESIAN_POINT ( 'NONE',  ( 3.609068157710407565, -1.714216318138677808, 0.2993142247325294991 ) ) ;
#38191=CARTESIAN_POINT ( 'NONE',  ( 1.915017753259074862, 0.5389909111754992432, 1.648018863455216643 ) ) ;
#38192=CARTESIAN_POINT ( 'NONE',  ( 3.912682095371947444, 0.7780703539225676257, 2.027152283489948026 ) ) ;
#38194=CARTESIAN_POINT ( 'NONE',  ( 4.118375227313908482, 1.978554835517082555, 0.3886342876525810119 ) ) ;
#38195=CARTESIAN_POINT ( 'NONE',  ( 2.593750000000001776, -1.895863743164140525, -0.7852924748298559798 ) ) ;
#38197=CARTESIAN_POINT ( 'NONE',  ( 0.9559316444634465837, 1.924326902252432081, -0.09161688492189544453 ) ) ;
#38199=CARTESIAN_POINT ( 'NONE',  ( 4.605860659110106781, 1.647066397540638993, 1.490795591097130002 ) ) ;
#38201=CARTESIAN_POINT ( 'NONE',  ( -0.1106856583840877539, 4.089587022985669229, -2.551888050631024640 ) ) ;
#38206=CARTESIAN_POINT ( 'NONE',  ( 1.049838644336478000, -2.005893928647552116, 0.9545428114200222858 ) ) ;
#38208=CARTESIAN_POINT ( 'NONE',  ( 5.353941776413853937, -0.7077614321437855072, 1.829919609802006741 ) ) ;
#38211=CARTESIAN_POINT ( 'NONE',  ( 0.2105424042340813540, -0.9235240298187572527, -1.952328634516012684 ) ) ;
#38213=CARTESIAN_POINT ( 'NONE',  ( 3.736832797123919025, -1.987151705994869344, -0.5527697292582544053 ) ) ;
#38217=CARTESIAN_POINT ( 'NONE',  ( 4.534354090784907143, 1.834037221929617711, 0.3668691113338993226 ) ) ;
#38218=CARTESIAN_POINT ( 'NONE',  ( 3.621445620172254021, 0.2585195360361118300, 1.714627356041095840 ) ) ;
#38219=CARTESIAN_POINT ( 'NONE',  ( 3.069568678616676927, -1.034394858748697743, 1.399543075413912430 ) ) ;
#38220=CARTESIAN_POINT ( 'NONE',  ( 0.9434182766495626815, -1.811351811004081158, -1.404917595322150659 ) ) ;
#38222=CARTESIAN_POINT ( 'NONE',  ( 4.441018442196864591, -1.617167385086373033, -1.325159661343593420 ) ) ;
#38223=CARTESIAN_POINT ( 'NONE',  ( 0.4800843290509413386, -0.2225996465644273503, -1.827572303103291551 ) ) ;
#38225=CARTESIAN_POINT ( 'NONE',  ( 1.863907939170056149, -0.1017519224979606118, -2.013985838549677609 ) ) ;
#38226=CARTESIAN_POINT ( 'NONE',  ( 0.3225714733509216781, 2.098294765757203528, 0.6321472216322538973 ) ) ;
#38230=CARTESIAN_POINT ( 'NONE',  ( 2.543736517606724146, -1.977637755382474438, 0.7655657148115800892 ) ) ;
#38232=CARTESIAN_POINT ( 'NONE',  ( 4.389149243953620605, 1.629682310347341456, -0.8231139397327084106 ) ) ;
#38239=CARTESIAN_POINT ( 'NONE',  ( 1.933859055862125809, -1.958050917679872160, 0.4949566823095867263 ) ) ;
#38240=CARTESIAN_POINT ( 'NONE',  ( 6.141676493652540536, -1.594220855400224401, -1.526124331276897950 ) ) ;
#38242=CARTESIAN_POINT ( 'NONE',  ( 4.469486699700035537, -0.3212591861478170663, 1.832842066241076040 ) ) ;
#38248=CARTESIAN_POINT ( 'NONE',  ( 4.951681858558426796, 0.5695450498939165218, -1.734646904759745700 ) ) ;
#38253=CARTESIAN_POINT ( 'NONE',  ( 0.5086469178660666390, 1.728604602589098205, 0.1357594709466679594 ) ) ;
#38254=CARTESIAN_POINT ( 'NONE',  ( 0.4095771458324704573, 1.203761932438538462, -1.257115261623420022 ) ) ;
#38255=CARTESIAN_POINT ( 'NONE',  ( 5.514422467339478828, -1.033062203415137992, -2.063637023464809594 ) ) ;
#38257=CARTESIAN_POINT ( 'NONE',  ( 1.212264220565926198, -0.9239156619155285410, -1.842110158844072698 ) ) ;
#38259=CARTESIAN_POINT ( 'NONE',  ( 6.661448219487969169, -0.6026422599177021500, -2.217949877449727047 ) ) ;
#38262=CARTESIAN_POINT ( 'NONE',  ( 5.172658500931742509, -1.761684834526537680, -0.6294727512598657926 ) ) ;
#38263=CARTESIAN_POINT ( 'NONE',  ( 3.849791259674230748, -1.322437695595569673, -1.381667681676468140 ) ) ;
#38265=CARTESIAN_POINT ( 'NONE',  ( 4.899154391205060577, 1.836108854712194649, -1.224054507610386366 ) ) ;
#38270=CARTESIAN_POINT ( 'NONE',  ( 5.778019675193696969, 2.089136139637823852, -0.3624112956793351659 ) ) ;
#38272=CARTESIAN_POINT ( 'NONE',  ( 3.294260915971382264, -0.9370450057796105847, 2.108945393182542372 ) ) ;
#38273=CARTESIAN_POINT ( 'NONE',  ( 3.402741375674179114, 0.4741672551989496998, 1.903589013717405853 ) ) ;
#38275=CARTESIAN_POINT ( 'NONE',  ( 0.5671465430379521999, 1.703994235754960451, 0.9719838849941149217 ) ) ;
#38279=CARTESIAN_POINT ( 'NONE',  ( 5.788296071918774821, -0.7303023681345042206, -1.879805717804765353 ) ) ;
#38282=CARTESIAN_POINT ( 'NONE',  ( 3.520551232162504540, 0.9717998864677798165, 1.941468132180910189 ) ) ;
#38284=CARTESIAN_POINT ( 'NONE',  ( 1.125412309253082332, 1.872817075645373697, 0.9946839901537674056 ) ) ;
#38289=CARTESIAN_POINT ( 'NONE',  ( 0.5091468516268854438, 1.791808316595304040, 1.017857635437851904 ) ) ;
#38291=CARTESIAN_POINT ( 'NONE',  ( 6.827182134110200806, 4.698030009824885056, 2.473619993765368008 ) ) ;
#38295=CARTESIAN_POINT ( 'NONE',  ( 4.934190575774549892, -1.026228162776990249, -1.613408319405706504 ) ) ;
#38296=CARTESIAN_POINT ( 'NONE',  ( 5.278098682986631651, -0.9809853834585824384, 1.472868624863521880 ) ) ;
#38299=CARTESIAN_POINT ( 'NONE',  ( 0.6854714705560975840, 1.745592605935637920, -0.4840870370880663853 ) ) ;
#38301=CARTESIAN_POINT ( 'NONE',  ( 0.9717394072371825509, -0.8581575513351351603, 1.712793540333819919 ) ) ;
#38302=CARTESIAN_POINT ( 'NONE',  ( 2.260293373024503616, -2.069953001785612479, 0.04851313490940312168 ) ) ;
#38305=CARTESIAN_POINT ( 'NONE',  ( 0.1277242839827036902, -1.211146277544056460, -1.556326691921037675 ) ) ;
#38306=CARTESIAN_POINT ( 'NONE',  ( 2.560947663861262491, -1.588335953301520220, -0.9000364273514869229 ) ) ;
#38307=CARTESIAN_POINT ( 'NONE',  ( -0.004676085075996058368, -0.5178430341337829645, -2.257629771169813448 ) ) ;
#38310=CARTESIAN_POINT ( 'NONE',  ( 3.965324414628346172, 1.767556376804786611, 1.063002922270523953 ) ) ;
#38317=CARTESIAN_POINT ( 'NONE',  ( 6.760220206081136496, -2.069995208266177666, 0.04663682477341199450 ) ) ;
#38319=CARTESIAN_POINT ( 'NONE',  ( 3.251412196806032995, -1.765091617811213931, -1.247493029685270649 ) ) ;
#38320=CARTESIAN_POINT ( 'NONE',  ( 4.178382104804970076, 0.9538709814062135139, 1.780240436319034503 ) ) ;
#38321=CARTESIAN_POINT ( 'NONE',  ( 6.720655732516655156, 7.629137130509086262, 2.873739711112702544 ) ) ;
#38327=CARTESIAN_POINT ( 'NONE',  ( 2.448454179885679149, -1.387098808145654560, 1.463928423225707931 ) ) ;
#38331=CARTESIAN_POINT ( 'NONE',  ( 5.941656858135132779, -1.798430535887390658, 0.6506349336675710804 ) ) ;
#38334=CARTESIAN_POINT ( 'NONE',  ( 4.429314653828757109, -1.560513098751922900, -1.277029310785951388 ) ) ;
#38338=CARTESIAN_POINT ( 'NONE',  ( 6.493153095729292446, 1.497681883954028237, -0.8552637798607003461 ) ) ;
#38341=STYLED_ITEM ( 'NONE', ( #79887 ), #169543 ) ;
#38343=CARTESIAN_POINT ( 'NONE',  ( 5.342975940791072631, -1.604858128155508101, 0.9606422304059699657 ) ) ;
#38344=CARTESIAN_POINT ( 'NONE',  ( 6.170187344554162401, 2.007508049254663529, -0.1525455265532823512 ) ) ;
#38345=CARTESIAN_POINT ( 'NONE',  ( 2.641538584800803502, 1.894577224340647792, -0.8349662684224224973 ) ) ;
#38349=CARTESIAN_POINT ( 'NONE',  ( 0.5093889453341126083, -1.913797760093600919, 0.6352206787166372326 ) ) ;
#38355=CARTESIAN_POINT ( 'NONE',  ( 5.694928174475800908, 1.691819642972839599, 0.8984594094828317612 ) ) ;
#38362=CARTESIAN_POINT ( 'NONE',  ( 2.465889518630470789, 2.120156730345585938, -0.4209195040108040797 ) ) ;
#38365=CARTESIAN_POINT ( 'NONE',  ( 0.6332531790259123827, 1.961634380476449335, 0.8060562103610890983 ) ) ;
#38366=CARTESIAN_POINT ( 'NONE',  ( 5.245057492501287832, -1.564903486862476489, 0.9398553879134128319 ) ) ;
#38368=CARTESIAN_POINT ( 'NONE',  ( 2.126188665331921079, 1.138154612934966670, -1.609425365540081865 ) ) ;
#38369=CARTESIAN_POINT ( 'NONE',  ( 4.377155534175989793, -1.710687068321177007, -0.8549628122409487219 ) ) ;
#38370=ORIENTED_EDGE ( 'NONE', *, *, #152161, .F. ) ;
#38372=CARTESIAN_POINT ( 'NONE',  ( 4.580490420436008847, 1.213483934061266201, -1.551205257841874241 ) ) ;
#38373=CARTESIAN_POINT ( 'NONE',  ( -0.01194524340117873729, -0.4266214822964596309, -1.901745140312367521 ) ) ;
#38374=EDGE_LOOP ( 'NONE', ( #62520, #191794, #113837, #98613 ) ) ;
#38380=CARTESIAN_POINT ( 'NONE',  ( 4.881465217424630687, 0.1836680969147831965, -1.903426456924644183 ) ) ;
#38382=CARTESIAN_POINT ( 'NONE',  ( 0.4994150495197279827, 1.833458848295946186, -1.227822027206024957 ) ) ;
#38384=CARTESIAN_POINT ( 'NONE',  ( 6.604166866988625095, -0.8575501651001187220, 1.819208590218702071 ) ) ;
#38385=CARTESIAN_POINT ( 'NONE',  ( 0.07661050522431847587, 7.629137130509112907, -2.310792076560589603 ) ) ;
#38386=CARTESIAN_POINT ( 'NONE',  ( 5.349643074071059878, 2.189064600896481139, -0.1049423877047955811 ) ) ;
#38389=CARTESIAN_POINT ( 'NONE',  ( 3.332542965736586371, -1.235447621225284287, 1.661183390374972646 ) ) ;
#38394=CARTESIAN_POINT ( 'NONE',  ( 1.129994055010040022, -1.371941552271437770, -1.670562328977095445 ) ) ;
#38400=CARTESIAN_POINT ( 'NONE',  ( 6.925078400183546812, 2.074047572655359328, 2.163550030515603684 ) ) ;
#38402=CARTESIAN_POINT ( 'NONE',  ( 2.641814858895009444, 2.006371511526034546, -0.2024640970367599380 ) ) ;
#38403=CARTESIAN_POINT ( 'NONE',  ( 4.324694450628805420, 0.7358571774197277815, -1.570421820497726051 ) ) ;
#38405=CARTESIAN_POINT ( 'NONE',  ( 4.047765473330780850, 1.496028175931501947, 1.431257568052332729 ) ) ;
#38406=CARTESIAN_POINT ( 'NONE',  ( 4.060252369235962888, -1.217431538915053180, 1.732033588162092297 ) ) ;
#38409=CARTESIAN_POINT ( 'NONE',  ( 1.973436150528505406, -0.2460485697947655814, 1.953970194506114755 ) ) ;
#38410=CARTESIAN_POINT ( 'NONE',  ( 0.7910927259777954523, -0.04954035392716604758, -1.911929172785244102 ) ) ;
#38411=CARTESIAN_POINT ( 'NONE',  ( 5.279328977631358555, 1.536242920967767711, 1.701453964730540447 ) ) ;
#38412=CARTESIAN_POINT ( 'NONE',  ( 2.349991895876184511, 1.825291697999480434, 0.04531359951509549705 ) ) ;
#38417=CARTESIAN_POINT ( 'NONE',  ( 2.355728993131640525, -1.494696414742059387, -1.348868867694212881 ) ) ;
#38419=CARTESIAN_POINT ( 'NONE',  ( 3.590630163336411051, 1.912927474663427496, 0.4342120235502828773 ) ) ;
#38422=CARTESIAN_POINT ( 'NONE',  ( 0.07556134207196538166, 0.2286499876833356648, -2.278112926217394030 ) ) ;
#38424=CARTESIAN_POINT ( 'NONE',  ( 6.017543284830850325, -1.160447301756668104, -1.738784508216392855 ) ) ;
#38425=CARTESIAN_POINT ( 'NONE',  ( 4.733122822409558950, -1.617543599503493468, 0.7186682867280795861 ) ) ;
#38427=CARTESIAN_POINT ( 'NONE',  ( 0.5334774086375413393, -1.552487152004313087, -1.546944964277228607 ) ) ;
#38428=CARTESIAN_POINT ( 'NONE',  ( 6.386628771994263154, 1.510377909004370522, -0.8644441249686038997 ) ) ;
#38431=CARTESIAN_POINT ( 'NONE',  ( 0.2635768167446932986, -2.297931531924101822, -0.05306211189425556751 ) ) ;
#38434=CARTESIAN_POINT ( 'NONE',  ( 1.647397727484143592, -1.863059487452220386, 1.182652941231487453 ) ) ;
#38435=CARTESIAN_POINT ( 'NONE',  ( 0.7433368588017514877, -0.2641965325859591540, -2.154838077344235714 ) ) ;
#38437=CARTESIAN_POINT ( 'NONE',  ( 1.007203092032255665, -0.04580389244966718426, 2.116997601370627091 ) ) ;
#38438=CARTESIAN_POINT ( 'NONE',  ( 3.187500000000002665, -1.451031289060985330, 1.451031289061251117 ) ) ;
#38439=CARTESIAN_POINT ( 'NONE',  ( 6.727182134110200273, 0.5640974741700152117, 2.241195997201197443 ) ) ;
#38440=CARTESIAN_POINT ( 'NONE',  ( 4.243131921826915232, -1.676359970754065731, 0.9489593035170663660 ) ) ;
#38442=CARTESIAN_POINT ( 'NONE',  ( 1.699181366971340701, 1.908771516627869147, 1.269207382326368316 ) ) ;
#38446=CARTESIAN_POINT ( 'NONE',  ( 4.143395664610330265, 0.1093779850947790705, 2.218736840405158173 ) ) ;
#38455=CARTESIAN_POINT ( 'NONE',  ( 1.354138928560550292, 0.1455316553338575902, -2.011204400906742240 ) ) ;
#38457=CARTESIAN_POINT ( 'NONE',  ( 6.760222218534770455, -2.062298699534569124, 0.04672293413533928907 ) ) ;
#38460=CARTESIAN_POINT ( 'NONE',  ( -0.04178991631376138827, -1.644041690304678616, -0.8291446804715857377 ) ) ;
#38464=CARTESIAN_POINT ( 'NONE',  ( 1.827073579719180163, -1.668441312418825095, 0.5905873696427661468 ) ) ;
#38465=CARTESIAN_POINT ( 'NONE',  ( 0.5103889644224939293, -1.913802852362625151, 0.6352017490645140985 ) ) ;
#38466=CARTESIAN_POINT ( 'NONE',  ( 0.4328342922346357646, -1.301571265828086688, -1.302605208699902928 ) ) ;
#38467=CARTESIAN_POINT ( 'NONE',  ( 4.564210359040954401, -1.498010274845029244, 1.735314277699088858 ) ) ;
#38468=CARTESIAN_POINT ( 'NONE',  ( 3.679498877186979211, -0.9061679144062879665, 1.602619060095414216 ) ) ;
#38471=CARTESIAN_POINT ( 'NONE',  ( 3.750846114953470867, -1.492790808496821775, 1.050590184284278861 ) ) ;
#38472=CARTESIAN_POINT ( 'NONE',  ( 4.553361389630797618, -1.314998166741452090, 1.528740011303417745 ) ) ;
#38474=CARTESIAN_POINT ( 'NONE',  ( 3.116390431409152395, -1.113901014592171723, -1.969235179105185640 ) ) ;
#38476=CARTESIAN_POINT ( 'NONE',  ( 6.229533133763371922, -1.984190613765562494, 0.7061325270490863559 ) ) ;
#38478=CARTESIAN_POINT ( 'NONE',  ( 3.930184216435282707, 1.147649575447948100, 1.722966636330313550 ) ) ;
#38481=CARTESIAN_POINT ( 'NONE',  ( 5.936213163351175659, -1.177816969253571155, -1.763093882214488817 ) ) ;
#38484=CARTESIAN_POINT ( 'NONE',  ( 1.963383859451812041, 0.3296633872902128282, -1.897934821152784446 ) ) ;
#38486=CARTESIAN_POINT ( 'NONE',  ( 6.596547011414190642, 1.947522214285227760, 0.2922974700911728507 ) ) ;
#38490=CARTESIAN_POINT ( 'NONE',  ( 1.090412635922506368, 1.328748260410139492, 1.780047631856091606 ) ) ;
#38491=CARTESIAN_POINT ( 'NONE',  ( 2.907361098931018795, 1.778370309693329210, 1.127733957892971484 ) ) ;
#38494=CARTESIAN_POINT ( 'NONE',  ( 1.099803389655891195, 0.7588869020343449456, -1.699499299819209108 ) ) ;
#38499=( BOUNDED_CURVE ( )  B_SPLINE_CURVE ( 3, ( #88407, #71049, #202108, #86262 ),
 .UNSPECIFIED., .F., .T. ) 
 B_SPLINE_CURVE_WITH_KNOTS ( ( 4, 4 ),
 ( 0.000000000000000000, 0.5000000000000022204 ),
 .UNSPECIFIED. ) 
 CURVE ( )  GEOMETRIC_REPRESENTATION_ITEM ( )  RATIONAL_B_SPLINE_CURVE ( ( 1.000000000000000222, 0.3333333333333304838, 0.3333333333333334259, 1.000000000000003109 ) ) 
 REPRESENTATION_ITEM ( '' )  );
#38500=CARTESIAN_POINT ( 'NONE',  ( 1.494549364340029163, -1.129948290531690658, 1.794289463044356436 ) ) ;
#38503=CARTESIAN_POINT ( 'NONE',  ( 3.086327779807009009, 1.092107249913790712, -1.629585102321646328 ) ) ;
#38504=CARTESIAN_POINT ( 'NONE',  ( 1.850665834824256173, 0.6780317805383448970, 2.052694239800388676 ) ) ;
#38505=CARTESIAN_POINT ( 'NONE',  ( 1.469984750362408610, -1.748608032326857353, -0.5769476384821782267 ) ) ;
#38508=CARTESIAN_POINT ( 'NONE',  ( 3.907932343763017347, 1.228949333998660798, -1.232512660115521408 ) ) ;
#38512=CARTESIAN_POINT ( 'NONE',  ( 0.6026772488060898603, -0.7295331166810551382, -2.035022307366324945 ) ) ;
#38513=CARTESIAN_POINT ( 'NONE',  ( 3.145861080134567000, -0.1455099638626895786, -2.010896398064919488 ) ) ;
#38515=CARTESIAN_POINT ( 'NONE',  ( 0.4620835240300471547, 2.137967531602209981, -0.3185850937674692407 ) ) ;
#38516=CARTESIAN_POINT ( 'NONE',  ( 2.412907133309648788, 1.760172955399338823, 0.8881188249313717309 ) ) ;
#38517=CARTESIAN_POINT ( 'NONE',  ( 6.609000000000047947, 2.032467779867861868, 2.404707446487294842 ) ) ;
#38518=CARTESIAN_POINT ( 'NONE',  ( 2.823698466604074309, 1.076742338344888639, -1.616048498441272407 ) ) ;
#38519=CARTESIAN_POINT ( 'NONE',  ( 6.363533315466952445, -1.540175188624912650, -1.133462061071670579 ) ) ;
#38523=CARTESIAN_POINT ( 'NONE',  ( -0.1106856583841086261, 2.025759259886884323, -2.413105898545636840 ) ) ;
#38528=CARTESIAN_POINT ( 'NONE',  ( 0.4466624375424713689, 2.201045718399210038, 0.1599725512250807224 ) ) ;
#38530=CARTESIAN_POINT ( 'NONE',  ( 4.170719094083116474, 1.390339895272204362, -1.384257141873693087 ) ) ;
#38532=CARTESIAN_POINT ( 'NONE',  ( 1.617814789376757156, 0.2004366740697149929, 2.006445999502483257 ) ) ;
#38534=CARTESIAN_POINT ( 'NONE',  ( 2.307945874296753797, -1.223308491024234224, -1.728006348806595316 ) ) ;
#38538=CARTESIAN_POINT ( 'NONE',  ( 2.976309490518674217, -0.1360139883382974202, -1.836174483004118674 ) ) ;
#38542=CARTESIAN_POINT ( 'NONE',  ( 3.744478000529617656, 1.131475959888720295, -1.793321066073015224 ) ) ;
#38543=CARTESIAN_POINT ( 'NONE',  ( 0.3570341529223716726, 1.821527202347131169, -0.2672101559373847857 ) ) ;
#38546=CARTESIAN_POINT ( 'NONE',  ( 4.341127749375134570, -1.794969056106166860, 1.012190969697931209 ) ) ;
#38548=CARTESIAN_POINT ( 'NONE',  ( 1.575478407343299692, -0.9843019613302635973, 1.555867251595323353 ) ) ;
#38554=CARTESIAN_POINT ( 'NONE',  ( 2.385638622766753425, 2.017150886971270651, -0.8956362484653990208 ) ) ;
#38555=CARTESIAN_POINT ( 'NONE',  ( 3.849113346294403382, -1.852342442990447813, 1.298737409825992062 ) ) ;
#38558=CARTESIAN_POINT ( 'NONE',  ( 4.078215212670958323, 0.8593412415473808963, 1.594818892651229891 ) ) ;
#38559=CARTESIAN_POINT ( 'NONE',  ( 3.977677156295666538, -0.7278633372749753194, 1.772268029184346227 ) ) ;
#38560=CARTESIAN_POINT ( 'NONE',  ( 5.230950013807261101, -1.948248037745937022, -0.7008574099531189594 ) ) ;
#38563=CARTESIAN_POINT ( 'NONE',  ( 4.153168997088651615, -1.638446398916657776, -1.096151307749502868 ) ) ;
#38564=CARTESIAN_POINT ( 'NONE',  ( 1.483290174073574441, 1.780938433730950621, -0.7347945396837353149 ) ) ;
#38565=CARTESIAN_POINT ( 'NONE',  ( 3.660894226558962128, -1.649352935060313552, -0.8826137995501317501 ) ) ;
#38566=CARTESIAN_POINT ( 'NONE',  ( 3.106426088690077858, -2.305020500623474522, 0.1135576804369240328 ) ) ;
#38567=CARTESIAN_POINT ( 'NONE',  ( 3.982723974049819482, 1.766592268715084790, 0.5855280163863920695 ) ) ;
#38570=CARTESIAN_POINT ( 'NONE',  ( 1.506614580823143701, -0.7594792294695625889, -1.964545455775383642 ) ) ;
#38575=CARTESIAN_POINT ( 'NONE',  ( 2.707414796094851361, 1.816601298730673220, -1.093838055662835096 ) ) ;
#38577=CARTESIAN_POINT ( 'NONE',  ( 0.2112021888033519534, 1.676852382702203714, -1.125601893279993160 ) ) ;
#38581=CARTESIAN_POINT ( 'NONE',  ( 2.477987356985793088, 1.327747062846416526, 1.705691702009938915 ) ) ;
#38584=CARTESIAN_POINT ( 'NONE',  ( 6.825078400183544503, 2.075476428726834577, 2.163873318353096931 ) ) ;
#38587=CARTESIAN_POINT ( 'NONE',  ( 6.333220217719927270, -1.622483202430196725, -1.197309987464048486 ) ) ;
#38589=CARTESIAN_POINT ( 'NONE',  ( 6.339408610606328764, 0.7995911543839243629, -1.932009116241965252 ) ) ;
#38591=CARTESIAN_POINT ( 'NONE',  ( 0.7258825447220511595, -2.147484179761431022, 0.7124928158122600941 ) ) ;
#38598=CARTESIAN_POINT ( 'NONE',  ( 2.543205433794017978, -1.277680944696883092, -1.158960206811429750 ) ) ;
#38600=CARTESIAN_POINT ( 'NONE',  ( 2.495042215028328236, 1.364832443287033570, 1.126547774882515673 ) ) ;
#38601=CARTESIAN_POINT ( 'NONE',  ( 2.578773234406753101, -1.386572882437474341, 1.459666011457598556 ) ) ;
#38602=CARTESIAN_POINT ( 'NONE',  ( 5.368293279414073638, 1.083412401764087374, 1.922438065789177308 ) ) ;
#38604=CARTESIAN_POINT ( 'NONE',  ( 4.412371012857700947, -2.019438640443659505, -0.04532404540058888875 ) ) ;
#38606=CARTESIAN_POINT ( 'NONE',  ( 4.406960118137589255, -0.4655763551070742912, -2.068578822641816473 ) ) ;
#38607=CARTESIAN_POINT ( 'NONE',  ( 4.007435537932837910, -1.928747227692016564, 0.5880391185724976877 ) ) ;
#38608=CARTESIAN_POINT ( 'NONE',  ( 4.060681591697304249, 0.4892206165460743494, 1.744179128828279302 ) ) ;
#38612=CARTESIAN_POINT ( 'NONE',  ( 1.604156678829884886, -0.6703249191640224813, -1.746612230856612769 ) ) ;
#38614=CARTESIAN_POINT ( 'NONE',  ( 6.709597972018079837, -0.3944863986210072060, 1.789098616620278470 ) ) ;
#38615=CARTESIAN_POINT ( 'NONE',  ( 5.742768220754598474, 1.747532268389985433, 0.4768009125176131957 ) ) ;
#38620=CARTESIAN_POINT ( 'NONE',  ( 0.6153073421325053749, 1.564839666810373231, 1.099065937236625157 ) ) ;
#38623=CARTESIAN_POINT ( 'NONE',  ( 1.275752070009423367, -1.914805681740685106, 0.4264308320794732432 ) ) ;
#38626=CARTESIAN_POINT ( 'NONE',  ( 4.517907016363444939, -0.5628432189327194912, 2.044499502628312371 ) ) ;
#38627=CARTESIAN_POINT ( 'NONE',  ( -0.02988540731096045455, 2.895077309840556445, -2.215427197800499570 ) ) ;
#38629=CARTESIAN_POINT ( 'NONE',  ( 5.993430986175369846, 1.491191765471042041, 1.289477300995988118 ) ) ;
#38631=CARTESIAN_POINT ( 'NONE',  ( 0.6506401683969212923, 1.984111478139438667, 0.3401018483101604928 ) ) ;
#38633=CARTESIAN_POINT ( 'NONE',  ( 6.421125127611838401, -1.890376142121247494, 0.9539971363903186896 ) ) ;
#38635=CARTESIAN_POINT ( 'NONE',  ( 1.996617168637443429, 2.047528291220417351, 0.3059219562495316125 ) ) ;
#38639=CARTESIAN_POINT ( 'NONE',  ( 4.892568727727841349, 1.738426232616798295, -1.160983500135639890 ) ) ;
#38641=CARTESIAN_POINT ( 'NONE',  ( 3.522295995157864290, 1.158834602800838498, -1.410599190884161969 ) ) ;
#38642=CARTESIAN_POINT ( 'NONE',  ( 1.980848084912645524, -1.656539610615878955, -0.7334085510423118404 ) ) ;
#38644=CARTESIAN_POINT ( 'NONE',  ( 6.217417563691929772, -0.2743312036321900460, 2.189694890431858276 ) ) ;
#38647=CARTESIAN_POINT ( 'NONE',  ( 4.577303723630254062, 0.003709267837189236805, -2.206952907291927168 ) ) ;
#38650=CARTESIAN_POINT ( 'NONE',  ( 2.455592584850064153, -1.418247937500687561, -1.282927761235647335 ) ) ;
#38652=CARTESIAN_POINT ( 'NONE',  ( 6.004363041306050697, 2.067815565686380364, 0.1054426792976848049 ) ) ;
#38654=CARTESIAN_POINT ( 'NONE',  ( 6.251546423958431298, 2.185849743821382862, -0.1592787069685035195 ) ) ;
#38661=CARTESIAN_POINT ( 'NONE',  ( 3.233525009082056201, -1.253693836546897700, -1.388425355430204622 ) ) ;
#38666=CARTESIAN_POINT ( 'NONE',  ( 6.754741982670550371, -0.5462536098296210119, -1.996853278248729824 ) ) ;
#38667=CARTESIAN_POINT ( 'NONE',  ( 0.7730648107450198703, 1.777001872080404166, -0.9530316558409923644 ) ) ;
#38671=CARTESIAN_POINT ( 'NONE',  ( 1.342011898504836820, 2.189069585219292957, 0.1046993245200772138 ) ) ;
#38672=CARTESIAN_POINT ( 'NONE',  ( 4.723181480036696023, -0.08661695748878039947, 1.823760500460340550 ) ) ;
#38680=CARTESIAN_POINT ( 'NONE',  ( 3.350949008998193257, 0.4442310927498266948, -1.786741727165648497 ) ) ;
#38681=CARTESIAN_POINT ( 'NONE',  ( -0.1047997906430510606, -0.1421793342430139606, -1.981047221590222840 ) ) ;
#38682=CARTESIAN_POINT ( 'NONE',  ( 1.792731522490832230, -2.164186313916468762, 0.7742391241713635353 ) ) ;
#38684=CARTESIAN_POINT ( 'NONE',  ( 6.473494419632052299, -0.2434444386649399217, 1.946554233954982172 ) ) ;
#38687=CARTESIAN_POINT ( 'NONE',  ( 3.392734571251673881, -1.844325299564765652, -0.5055192353106837677 ) ) ;
#38690=EDGE_CURVE ( 'NONE', #97371, #180616, #51193, .T. ) ;
#38692=CARTESIAN_POINT ( 'NONE',  ( 2.841443172333203204, 0.7501175549536406306, -1.951742197369815912 ) ) ;
#38693=CARTESIAN_POINT ( 'NONE',  ( 1.287742131874554552, -0.8442722623961744777, 1.669378388412197767 ) ) ;
#38694=CARTESIAN_POINT ( 'NONE',  ( 2.179064334209149578, -0.9478932651061505732, -1.779355105811925020 ) ) ;
#38697=CARTESIAN_POINT ( 'NONE',  ( 2.823474877308090214, 0.9648067800103199421, -1.448311861076934104 ) ) ;
#38701=CARTESIAN_POINT ( 'NONE',  ( 3.844159338287247429, 1.716807015663003311, 0.1666082703000223986 ) ) ;
#38702=CARTESIAN_POINT ( 'NONE',  ( 3.825867475279482566, 1.171244075711602051, -1.852137614134836907 ) ) ;
#38705=CARTESIAN_POINT ( 'NONE',  ( 3.485384773837760353, 0.04839624821431457585, 2.170676210889192603 ) ) ;
#38706=CARTESIAN_POINT ( 'NONE',  ( 2.385134503015675200, 1.669401249834654433, -0.7394980648879890817 ) ) ;
#38708=CARTESIAN_POINT ( 'NONE',  ( 4.979753661315234226, -0.7591050579739184734, 1.976773538454196677 ) ) ;
#38709=CARTESIAN_POINT ( 'NONE',  ( 6.539320575229232269, 1.262224698349242669, 2.111181586620724637 ) ) ;
#38711=CARTESIAN_POINT ( 'NONE',  ( 5.267208303392540536, 2.209927380382335826, -0.6089511437187348220 ) ) ;
#38713=CARTESIAN_POINT ( 'NONE',  ( 6.620655732516652847, 2.468432086671234149, 2.210906647470804565 ) ) ;
#38715=CARTESIAN_POINT ( 'NONE',  ( 0.4168467196605326053, -0.7183999135813922132, -1.995210048009891102 ) ) ;
#38719=ADVANCED_FACE ( 'NONE', ( #124687 ), #199139, .F. ) ;
#38722=CARTESIAN_POINT ( 'NONE',  ( 5.555314621531947772, -1.277044735018734833, 1.560499014526220307 ) ) ;
#38724=CARTESIAN_POINT ( 'NONE',  ( 2.870046724737782995, -2.040761436538469198, 0.2982335875671269787 ) ) ;
#38726=CARTESIAN_POINT ( 'NONE',  ( -0.2408018239684278916, 6.947782644136219155, -2.695524888730389090 ) ) ;
#38730=CARTESIAN_POINT ( 'NONE',  ( 6.193348084369689310, -0.7418380161853586063, 2.062208804312585020 ) ) ;
#38731=CARTESIAN_POINT ( 'NONE',  ( 3.762342404062005041, 1.897698010425369786, -0.6819954029829021769 ) ) ;
#38732=CARTESIAN_POINT ( 'NONE',  ( 3.140019216317342376, 0.4501627324021878485, 1.785233193441162491 ) ) ;
#38734=CARTESIAN_POINT ( 'NONE',  ( 0.4458014021226979207, 1.719615392401403708, 0.1342584403209358679 ) ) ;
#38736=CARTESIAN_POINT ( 'NONE',  ( 1.090962482291182312, -0.5517420707249369727, 2.231415953587682299 ) ) ;
#38738=CARTESIAN_POINT ( 'NONE',  ( 6.455986150183742112, 2.257016316038124693, -0.1587017259171065731 ) ) ;
#38739=CARTESIAN_POINT ( 'NONE',  ( 3.457739842999438817, 0.5116738510754537117, -2.042838612040797752 ) ) ;
#38748=CARTESIAN_POINT ( 'NONE',  ( 4.430067838210618447, -2.178247905445731103, 0.4349904863075284567 ) ) ;
#38749=CARTESIAN_POINT ( 'NONE',  ( 2.642740014504705304, -1.821389600533461994, 1.218302608185666491 ) ) ;
#38753=CARTESIAN_POINT ( 'NONE',  ( 5.318788500806308051, -1.422220495204097546, 1.351624447685224162 ) ) ;
#38755=CARTESIAN_POINT ( 'NONE',  ( 6.610000000000042952, 4.702635990354799844, 2.282722937023287102 ) ) ;
#38757=CARTESIAN_POINT ( 'NONE',  ( 4.342108446431157454, -1.306982937058022820, -1.669832246961988176 ) ) ;
#38760=CARTESIAN_POINT ( 'NONE',  ( 5.700121470611750674, -2.161883445634639411, -0.004416275431240455560 ) ) ;
#38762=CARTESIAN_POINT ( 'NONE',  ( 4.985823801847525161, -1.827980399782932697, -0.2200341325891697619 ) ) ;
#38765=CARTESIAN_POINT ( 'NONE',  ( 0.2393033055489251493, 1.735545043620636996, 0.1309560527960016429 ) ) ;
#38766=CARTESIAN_POINT ( 'NONE',  ( 6.727182134110222478, 3.706444386917655986, 2.325533714637216143 ) ) ;
#38769=CARTESIAN_POINT ( 'NONE',  ( 3.872077330825273389, 1.198917189070296541, 1.798566189592496034 ) ) ;
#38773=CARTESIAN_POINT ( 'NONE',  ( 3.327187652246216931, 0.05129554954072869377, 2.161254785723889515 ) ) ;
#38774=CARTESIAN_POINT ( 'NONE',  ( 4.534422775129973715, 1.932726017421485976, 0.3875534085790635630 ) ) ;
#38775=CARTESIAN_POINT ( 'NONE',  ( 3.602662725270942445, 0.7809228151291653930, -1.548105009325143833 ) ) ;
#38776=CARTESIAN_POINT ( 'NONE',  ( 1.136565065649897344, 0.4323997850379875385, 2.148315308122191514 ) ) ;
#38777=CARTESIAN_POINT ( 'NONE',  ( 1.360874125193665130, 0.9374058560891560532, 2.108772699047257948 ) ) ;
#38778=CARTESIAN_POINT ( 'NONE',  ( 3.479809507395460244, 1.304684485917747994, 1.595210877418812956 ) ) ;
#38779=CARTESIAN_POINT ( 'NONE',  ( 5.390160969041248862, -0.4756269310413098750, -1.882793909387857179 ) ) ;
#38786=CARTESIAN_POINT ( 'NONE',  ( 3.874219531129017291, 1.223701582695544854, 1.836212042189053761 ) ) ;
#38789=CARTESIAN_POINT ( 'NONE',  ( 1.234942694251008000, -0.03850059531256519452, -1.860717468297488297 ) ) ;
#38790=CARTESIAN_POINT ( 'NONE',  ( -0.1291982275798807533, 5.720674304969967316, -2.668085245563474484 ) ) ;
#38794=CARTESIAN_POINT ( 'NONE',  ( 6.925078400183590333, 2.001873123210990535, 2.545813127278444998 ) ) ;
#38797=CARTESIAN_POINT ( 'NONE',  ( 2.747006664573675039, -1.714185755289293622, 1.143718651939158670 ) ) ;
#38803=CARTESIAN_POINT ( 'NONE',  ( 1.041951191326966342, 0.8359002368949167705, -1.883948988615320896 ) ) ;
#38807=CARTESIAN_POINT ( 'NONE',  ( 5.830760709146560750, 2.125890151018691832, 0.5921790101122563765 ) ) ;
#38808=CARTESIAN_POINT ( 'NONE',  ( 6.591137597455673180, 1.973280021476801149, -1.106527213950120547 ) ) ;
#38810=CARTESIAN_POINT ( 'NONE',  ( 6.504213119055646253, -0.7662104867102972339, 1.640237621407932167 ) ) ;
#38811=CARTESIAN_POINT ( 'NONE',  ( 0.9015777671340443611, -1.966303774932298021, 0.4465067697373495403 ) ) ;
#38813=CARTESIAN_POINT ( 'NONE',  ( 1.370962024642598864, -0.5571102548348834116, 2.229726662508556778 ) ) ;
#38819=CARTESIAN_POINT ( 'NONE',  ( 1.463515404423965105, 1.843522461416190250, -0.3164952454337774390 ) ) ;
#38820=CARTESIAN_POINT ( 'NONE',  ( 2.202361591730035428, 1.313542931311746598, -1.530159205979222170 ) ) ;
#38824=CARTESIAN_POINT ( 'NONE',  ( 5.022148466640797615, -1.125808720090130111, -1.779717422886097244 ) ) ;
#38829=CARTESIAN_POINT ( 'NONE',  ( 4.465106368662499214, -1.619631974074808412, 1.206539259511850259 ) ) ;
#38832=CARTESIAN_POINT ( 'NONE',  ( 6.355934510867760956, -0.6984221382469282258, 1.940952099462374569 ) ) ;
#38834=CARTESIAN_POINT ( 'NONE',  ( 5.061884429210019576, 2.138887713127162638, -0.3115965683029159883 ) ) ;
#38840=CARTESIAN_POINT ( 'NONE',  ( 1.961612892103332229, 1.804449789391232795, 1.207184914618843807 ) ) ;
#38843=CARTESIAN_POINT ( 'NONE',  ( 1.575478407343299692, -0.9843019613302635973, 1.555867251595323353 ) ) ;
#38845=CARTESIAN_POINT ( 'NONE',  ( 2.999763140970078901, -2.188934734890151113, 0.1099877568606702771 ) ) ;
#38846=CARTESIAN_POINT ( 'NONE',  ( 6.983263157960365675, 7.052158404629149224, 2.651961988451009944 ) ) ;
#38847=CARTESIAN_POINT ( 'NONE',  ( 4.223666230214691453, -2.166182250408314580, 0.6532043330096364286 ) ) ;
#38853=CARTESIAN_POINT ( 'NONE',  ( 5.729715491186369469, -1.123817246201250786, -1.367138390065870457 ) ) ;
#38856=CARTESIAN_POINT ( 'NONE',  ( 1.536301591958776802, 1.038269187514633485, -1.832158284056581543 ) ) ;
#38860=CARTESIAN_POINT ( 'NONE',  ( 0.8890313061419883311, 0.1412731933134198092, 1.964529561086136189 ) ) ;
#38862=CARTESIAN_POINT ( 'NONE',  ( 0.2034672893990868703, -1.513989045467616146, -1.247398002513319781 ) ) ;
#38863=CARTESIAN_POINT ( 'NONE',  ( 6.170143040141627289, 1.806061762467878751, -0.1426304505553182556 ) ) ;
#38867=CARTESIAN_POINT ( 'NONE',  ( 5.155093292349416600, -1.580716073637401076, -1.000049079914612449 ) ) ;
#38868=CARTESIAN_POINT ( 'NONE',  ( 6.104363016364067640, 2.067617457866403718, 0.1074407263862015016 ) ) ;
#38879=CARTESIAN_POINT ( 'NONE',  ( 5.600043156098196917, 0.7966083592686534764, -1.793046234938546757 ) ) ;
#38881=CARTESIAN_POINT ( 'NONE',  ( 2.231795861093866851, -1.842164517099669441, -0.8196493499348647127 ) ) ;
#38883=CARTESIAN_POINT ( 'NONE',  ( 0.7147126110796617748, 2.027027023440019171, 0.8336157706642086662 ) ) ;
#38885=CARTESIAN_POINT ( 'NONE',  ( 2.126040175964475143, 1.080828230516362121, -1.526477596812993553 ) ) ;
#38887=CARTESIAN_POINT ( 'NONE',  ( 3.849861664782163739, -1.391318219759619002, -1.455273641467175860 ) ) ;
#38890=CARTESIAN_POINT ( 'NONE',  ( 3.972345043000875098, -2.094467101900459483, -0.3087697250930310222 ) ) ;
#38892=CARTESIAN_POINT ( 'NONE',  ( 6.074686117427479992, 1.393331124738606652, -1.531503843499823381 ) ) ;
#38893=CARTESIAN_POINT ( 'NONE',  ( 0.8903107040577078468, -0.5117213476562210150, -2.027015703535272717 ) ) ;
#38894=CARTESIAN_POINT ( 'NONE',  ( 6.720655732516648051, 2.039834428248034293, 2.379457109286802208 ) ) ;
#38895=CARTESIAN_POINT ( 'NONE',  ( 6.809597967592865508, -0.3964169337347979161, 1.788522171948719874 ) ) ;
#38904=CARTESIAN_POINT ( 'NONE',  ( 6.270165159132718991, 1.906809857242173445, -0.1455798257045255728 ) ) ;
#38912=CARTESIAN_POINT ( 'NONE',  ( 6.292592244351721043, 1.492246071875057423, -1.356311808412967723 ) ) ;
#38913=CARTESIAN_POINT ( 'NONE',  ( 0.5047332052380922862, -2.104974169346077506, -0.2554120829242333968 ) ) ;
#38919=CARTESIAN_POINT ( 'NONE',  ( 3.836728334651629879, -1.896773656598240709, -0.5296851528490874594 ) ) ;
#38920=CARTESIAN_POINT ( 'NONE',  ( 4.763296089436113157, 1.880429982106451181, -0.7283946704290320540 ) ) ;
#38923=CARTESIAN_POINT ( 'NONE',  ( 4.910206770677443266, 1.512653250323254817, -1.585896273577400706 ) ) ;
#38925=CARTESIAN_POINT ( 'NONE',  ( 3.627879330711426320, -1.146429500678107116, -1.547990911671823566 ) ) ;
#38927=CARTESIAN_POINT ( 'NONE',  ( -0.02948999725181991258, 7.629137130509059617, -2.526318448094333480 ) ) ;
#38928=CARTESIAN_POINT ( 'NONE',  ( 0.1181803206181560040, -2.163391993613572151, 0.4351206515559591370 ) ) ;
#38935=CARTESIAN_POINT ( 'NONE',  ( 4.873860229706322933, -1.932217566332248282, 0.3801659098390720581 ) ) ;
#38937=CARTESIAN_POINT ( 'NONE',  ( 0.8900594323104525918, -0.4731300603538539096, -1.883416623991182481 ) ) ;
#38938=CARTESIAN_POINT ( 'NONE',  ( 4.195951375888273382, 1.316525029674735947, 1.522990447314742424 ) ) ;
#38939=CARTESIAN_POINT ( 'NONE',  ( 5.677245700908649439, -1.026343684741271023, -2.056567161392281129 ) ) ;
#38941=CARTESIAN_POINT ( 'NONE',  ( 3.608110912359719258, 1.861131631771815842, 0.004268880383616681894 ) ) ;
#38947=CARTESIAN_POINT ( 'NONE',  ( 6.233939691744167177, 2.068093053085200417, 0.3059697267470474769 ) ) ;
#38953=CARTESIAN_POINT ( 'NONE',  ( -0.01727558406095473439, -0.1313277740116538805, -1.795991579427682616 ) ) ;
#38955=CARTESIAN_POINT ( 'NONE',  ( 3.023724745236521017, -1.528101708971361106, 0.8198667277116710173 ) ) ;
#38957=CARTESIAN_POINT ( 'NONE',  ( 6.509000000000016328, 7.053097208480951785, 2.498154145070859311 ) ) ;
#38960=CARTESIAN_POINT ( 'NONE',  ( 6.965710887581792576, -0.4882203796070741508, 2.123536573467856403 ) ) ;
#38961=CARTESIAN_POINT ( 'NONE',  ( 5.549374350267230582, -1.441814640532925074, -1.119852386600270533 ) ) ;
#38962=CARTESIAN_POINT ( 'NONE',  ( 3.344534541303633368, -1.931932779036081183, -0.3399374921491463142 ) ) ;
#38966=CARTESIAN_POINT ( 'NONE',  ( 4.125719030757846184, -0.3612518283466863434, 2.089324717668067599 ) ) ;
#38969=CARTESIAN_POINT ( 'NONE',  ( 1.832961912758425349, -1.964510197511709189, -0.6532998099852762586 ) ) ;
#38972=CARTESIAN_POINT ( 'NONE',  ( 4.530067796519579026, -2.178530490643998174, 0.4330045798939685109 ) ) ;
#38974=CARTESIAN_POINT ( 'NONE',  ( 2.215865853697509102, 2.230823145726851475, 0.5541181435367804609 ) ) ;
#38976=CARTESIAN_POINT ( 'NONE',  ( 6.666849506214659549, 1.532398756413049457, -1.380780335402414849 ) ) ;
#38979=CARTESIAN_POINT ( 'NONE',  ( 6.515202330376022921, -1.784155196879381622, 0.4545711315065634195 ) ) ;
#38983=CARTESIAN_POINT ( 'NONE',  ( 3.410326831400651404, -1.910418641682644969, -0.08914582809275289899 ) ) ;
#38985=CARTESIAN_POINT ( 'NONE',  ( 3.592533753846867128, -0.3360022577178176650, -1.691527450499834995 ) ) ;
#38986=CARTESIAN_POINT ( 'NONE',  ( 2.061732777098632230, 1.244387006429502396, 1.586668050434843158 ) ) ;
#38987=CARTESIAN_POINT ( 'NONE',  ( 3.973462176510922816, -2.273730406356341049, -0.3370867821424743949 ) ) ;
#38988=CARTESIAN_POINT ( 'NONE',  ( 4.024925711125073136, 2.146699088035211922, 0.7144036547655304714 ) ) ;
#38989=CARTESIAN_POINT ( 'NONE',  ( 0.1005910224048736229, -2.206496634663042133, -0.04943112074598519229 ) ) ;
#38992=CARTESIAN_POINT ( 'NONE',  ( 5.237463280334829996, -1.251769750873907849, -1.251277626909578222 ) ) ;
#38994=CARTESIAN_POINT ( 'NONE',  ( 0.9730957290566042417, -0.06121152481648738097, -2.291606990885884265 ) ) ;
#38995=CARTESIAN_POINT ( 'NONE',  ( 5.226429366918344144, 0.1390423275269437320, 1.835946739075666745 ) ) ;
#38997=CARTESIAN_POINT ( 'NONE',  ( 5.349643074071059878, 2.189064600896481139, -0.1049423877047955811 ) ) ;
#39001=CARTESIAN_POINT ( 'NONE',  ( 6.180147188013234150, -1.146869210499700920, -1.723488058659912392 ) ) ;
#39002=CARTESIAN_POINT ( 'NONE',  ( 1.077361674225948418, 1.530160568918725872, 1.313541346884481209 ) ) ;
#39005=CARTESIAN_POINT ( 'NONE',  ( 4.477124871421138685, -0.001476069148669684195, -1.926676517386548992 ) ) ;
#39007=CARTESIAN_POINT ( 'NONE',  ( 1.195894564581518660, 2.049875489592466238, -0.8564406981130603391 ) ) ;
#39011=DIRECTION ( 'NONE',  ( -1.000000000000000000, 0.000000000000000000, 0.000000000000000000 ) ) ;
#39016=CARTESIAN_POINT ( 'NONE',  ( 2.576550507925364109, 1.283677811227203147, -1.483670167215108693 ) ) ;
#39021=CARTESIAN_POINT ( 'NONE',  ( 6.672321430365630412, -0.9237476215336395402, -1.730755693189582667 ) ) ;
#39024=CARTESIAN_POINT ( 'NONE',  ( 6.807524309086420367, -0.4794501827766698421, 2.115671360755105646 ) ) ;
#39028=CARTESIAN_POINT ( 'NONE',  ( 1.106479506788549116, 1.420293003395491693, -1.217391549091076275 ) ) ;
#39029=CARTESIAN_POINT ( 'NONE',  ( -0.1054646484276201696, -0.7404878594409001202, -1.567598555697255369 ) ) ;
#39031=CARTESIAN_POINT ( 'NONE',  ( 3.667680160636753506, 1.218766932906123479, 1.821211977396507198 ) ) ;
#39032=CARTESIAN_POINT ( 'NONE',  ( 6.106511577925135548, -0.8227651472764373475, -2.156109995086146647 ) ) ;
#39033=CARTESIAN_POINT ( 'NONE',  ( 6.503207061003255518, 1.710746398682884140, 1.148667516769467767 ) ) ;
#39034=CARTESIAN_POINT ( 'NONE',  ( 2.378764330827160212, 1.775374922424903801, -0.7872989649762071052 ) ) ;
#39039=CARTESIAN_POINT ( 'NONE',  ( 2.918592439375994552, -1.356299846568160827, -1.492255409411530120 ) ) ;
#39043=CARTESIAN_POINT ( 'NONE',  ( 0.6975366375942676500, -0.6598540886826111951, 1.702458561391326342 ) ) ;
#39049=CARTESIAN_POINT ( 'NONE',  ( 6.385628592921421820, 1.419324251362139133, 1.494494355598655622 ) ) ;
#39054=CARTESIAN_POINT ( 'NONE',  ( 5.760417579480547445, 2.017467016246987210, 0.09685271086026786547 ) ) ;
#39055=CARTESIAN_POINT ( 'NONE',  ( 5.215582523826345351, 1.815199501411597582, 1.280085896050622507 ) ) ;
#39058=CARTESIAN_POINT ( 'NONE',  ( 5.260643881022500246, -1.494227509126961451, 1.419604852646045634 ) ) ;
#39059=CARTESIAN_POINT ( 'NONE',  ( 3.779922787921150995, 1.701948043757589124, -1.081065327119046016 ) ) ;
#39066=CARTESIAN_POINT ( 'NONE',  ( 3.972029700707707445, 1.727737986437705819, 1.038833660170018769 ) ) ;
#39067=CARTESIAN_POINT ( 'NONE',  ( 3.029072736150268952, -1.236975958831527445, -1.363863411116640334 ) ) ;
#39069=CARTESIAN_POINT ( 'NONE',  ( 2.420946758181366842, 1.505949115154591400, -1.748677306438247703 ) ) ;
#39072=CARTESIAN_POINT ( 'NONE',  ( 3.444745247808535638, 0.5215555581963465803, 2.097624034931542703 ) ) ;
#39075=CARTESIAN_POINT ( 'NONE',  ( 2.970384050378202634, 1.940355284992447027, 1.231690374697077095 ) ) ;
#39078=CARTESIAN_POINT ( 'NONE',  ( 2.184254540302111636, -1.834043650784190405, -0.3674020703766100460 ) ) ;
#39079=CARTESIAN_POINT ( 'NONE',  ( 0.3683541893860732275, -1.290952873633111953, 1.489922359098810878 ) ) ;
#39083=CARTESIAN_POINT ( 'NONE',  ( 1.858336453454629611, 2.200810804183956026, -0.1644699235988852648 ) ) ;
#39089=CARTESIAN_POINT ( 'NONE',  ( 5.858272006539261056, 0.7985356142178706707, 1.802671990260945156 ) ) ;
#39090=CARTESIAN_POINT ( 'NONE',  ( 5.936188932989287181, 1.142819166849334378, -2.004778302753240649 ) ) ;
#39091=CARTESIAN_POINT ( 'NONE',  ( 6.531710587413017244, 1.780498168465095787, -0.5416703039235416517 ) ) ;
#39093=CARTESIAN_POINT ( 'NONE',  ( 2.571201674526869763, 1.840362857814400455, 0.9314759700368970829 ) ) ;
#39101=CARTESIAN_POINT ( 'NONE',  ( 6.092256315220226703, 1.075607590566488803, -1.885974292122821527 ) ) ;
#39103=CARTESIAN_POINT ( 'NONE',  ( 5.108874002337426390, -0.2646564886703614006, 1.822002613180016883 ) ) ;
#39105=CARTESIAN_POINT ( 'NONE',  ( 6.620655732516651071, -0.002413161512292844035, 2.173887093218453082 ) ) ;
#39106=CARTESIAN_POINT ( 'NONE',  ( 0.2450992160058732550, -1.441561472518913867, -1.191725768352129622 ) ) ;
#39111=CARTESIAN_POINT ( 'NONE',  ( 0.06490398442321809735, -1.535895564731554863, 1.139000086266952705 ) ) ;
#39113=CARTESIAN_POINT ( 'NONE',  ( 2.271989177565427287, -1.091335633969382490, 1.393213513506918133 ) ) ;
#39114=CARTESIAN_POINT ( 'NONE',  ( -0.005422908085399994089, -1.854866876809873943, -0.4647201794698225252 ) ) ;
#39116=CARTESIAN_POINT ( 'NONE',  ( 3.884325381594720739, -0.6044542036256529416, -1.817792542802825428 ) ) ;
#39118=CARTESIAN_POINT ( 'NONE',  ( 5.178159682156908694, -1.051918566972683600, -1.664904379343169705 ) ) ;
#39119=CARTESIAN_POINT ( 'NONE',  ( 0.0004480315400831600455, -0.9938866557669153723, 1.873244595478529728 ) ) ;
#39121=CARTESIAN_POINT ( 'NONE',  ( 3.274138816734498025, -1.115311402298941656, 1.501645261301733481 ) ) ;
#39122=CARTESIAN_POINT ( 'NONE',  ( 6.692093555742618882, -0.7303567666399125580, 1.561414089659449944 ) ) ;
#39124=CARTESIAN_POINT ( 'NONE',  ( 1.805583701156989518, 1.836052299496168771, 1.224139149458243425 ) ) ;
#39127=CARTESIAN_POINT ( 'NONE',  ( 0.5200786239168513347, 2.040466299037096309, -0.3010312105025755303 ) ) ;
#39134=CARTESIAN_POINT ( 'NONE',  ( 3.437997351728830697, 1.311287738946330439, 1.602184970737066116 ) ) ;
#39138=CARTESIAN_POINT ( 'NONE',  ( 0.7682301616282152246, 2.017272972751768645, -0.1012717401170943471 ) ) ;
#39144=CARTESIAN_POINT ( 'NONE',  ( 0.1749903794560228876, 5.724274800596795387, -2.549334106949477263 ) ) ;
#39146=CARTESIAN_POINT ( 'NONE',  ( 5.677111188754776272, -0.9039728708103295096, -1.802140534545144890 ) ) ;
#39147=CARTESIAN_POINT ( 'NONE',  ( 5.911341210168471250, -1.801345639624308381, 0.6523577827844198040 ) ) ;
#39149=CARTESIAN_POINT ( 'NONE',  ( 3.316156725143477146, 1.388770557483296697, -1.695381604771596606 ) ) ;
#39151=CARTESIAN_POINT ( 'NONE',  ( 2.232540727315056373, 1.246330492051262784, -1.450604739030990187 ) ) ;
#39154=CARTESIAN_POINT ( 'NONE',  ( 1.159780049612362030, 1.203373692603469935, 1.617804775344060308 ) ) ;
#39156=CARTESIAN_POINT ( 'NONE',  ( 5.970311429539967740, -2.080533979117826782, -0.6889730390344513955 ) ) ;
#39158=CARTESIAN_POINT ( 'NONE',  ( 2.871755265489631448, 0.9208624611983186048, 1.458155879698035395 ) ) ;
#39159=ORIENTED_EDGE ( 'NONE', *, *, #155782, .F. ) ;
#39170=CARTESIAN_POINT ( 'NONE',  ( 3.598146505595464006, -0.8898571075792599538, 1.577739831003275084 ) ) ;
#39175=CARTESIAN_POINT ( 'NONE',  ( 4.230988290566616072, 1.657980831523006460, 0.7301630082575115699 ) ) ;
#39178=CARTESIAN_POINT ( 'NONE',  ( 5.424199618621329044, 0.9171840495176122321, 1.619240327305818683 ) ) ;
#39180=CARTESIAN_POINT ( 'NONE',  ( 3.145994354733801845, 0.8638979756431870438, 1.709836580976647813 ) ) ;
#39186=CARTESIAN_POINT ( 'NONE',  ( 1.710996362105126511, -0.2544465352872951613, 2.075019263894110733 ) ) ;
#39188=CARTESIAN_POINT ( 'NONE',  ( 6.317406038308035043, -0.2352959436980571473, 1.911917130847824886 ) ) ;
#39190=CARTESIAN_POINT ( 'NONE',  ( 2.291784574284541964, -0.7830779901500490858, 1.649245556672715773 ) ) ;
#39192=CARTESIAN_POINT ( 'NONE',  ( 1.627339542692422869, 0.1479755015179542166, -1.964067387968527312 ) ) ;
#39193=CARTESIAN_POINT ( 'NONE',  ( 3.931145062177692218, -1.341491907185809795, -1.404491712913302104 ) ) ;
#39196=CARTESIAN_POINT ( 'NONE',  ( 6.930517489306616596, -1.145039166549733922, 1.467359839328785664 ) ) ;
#39198=CARTESIAN_POINT ( 'NONE',  ( 3.709332143218791789, 1.789599998243587731, -1.137392358348317201 ) ) ;
#39204=AXIS2_PLACEMENT_3D ( 'NONE', #78254, #124962, #209295 ) ;
#39207=CARTESIAN_POINT ( 'NONE',  ( 3.896943178251357054, 1.541351720387572843, -0.9781566455248569270 ) ) ;
#39212=CARTESIAN_POINT ( 'NONE',  ( 4.258574955689950592, -1.386304660245713860, 1.256184814050688603 ) ) ;
#39214=CARTESIAN_POINT ( 'NONE',  ( 2.104012753913253153, -1.926084867047285654, 0.04718631861246740111 ) ) ;
#39222=CARTESIAN_POINT ( 'NONE',  ( 0.05257324754554763141, -1.379058229334565455, 1.606613856852637356 ) ) ;
#39225=CARTESIAN_POINT ( 'NONE',  ( 4.750872686184268723, -0.4484009487188305165, -2.020967519627144604 ) ) ;
#39226=CARTESIAN_POINT ( 'NONE',  ( 0.9074547957551477584, -0.8278116715597811925, -1.644758345054016191 ) ) ;
#39228=CARTESIAN_POINT ( 'NONE',  ( 4.957821946367388932, -2.163970343481158132, -0.7757635736431248707 ) ) ;
#39232=CARTESIAN_POINT ( 'NONE',  ( 0.4809653258567511691, -0.2865729554843428062, -2.274222260372929405 ) ) ;
#39235=CARTESIAN_POINT ( 'NONE',  ( 4.593657693847520207, -1.941558278569108120, -0.04622955632663238584 ) ) ;
#39240=CARTESIAN_POINT ( 'NONE',  ( -0.2047996464942871964, -0.1441562275304847374, -1.980932652848297115 ) ) ;
#39241=CARTESIAN_POINT ( 'NONE',  ( 5.999232488047271161, -0.2420365156972601739, 2.001857322483958423 ) ) ;
#39245=CARTESIAN_POINT ( 'NONE',  ( 2.748082359423655419, 0.7051493092682534769, 1.968258087557398284 ) ) ;
#39246=CARTESIAN_POINT ( 'NONE',  ( 0.8129392405988710157, -0.2653805273100506290, 1.749707594005883937 ) ) ;
#39249=CARTESIAN_POINT ( 'NONE',  ( 4.699361189290715224, -0.6141998521675575695, 2.208390280175839049 ) ) ;
#39250=CARTESIAN_POINT ( 'NONE',  ( 2.026944798790380364, -1.135751832872053058, -1.318713242574782507 ) ) ;
#39253=CARTESIAN_POINT ( 'NONE',  ( 2.196291916443537939, -1.129096229514385819, -1.315908775350557169 ) ) ;
#39255=CARTESIAN_POINT ( 'NONE',  ( 1.979201191301533047, 2.025398335218126622, 0.7825711269493199618 ) ) ;
#39257=CARTESIAN_POINT ( 'NONE',  ( 5.137907791644652278, 2.014008302827663854, -0.1037760698975112861 ) ) ;
#39258=CARTESIAN_POINT ( 'NONE',  ( 2.250000000000001776, 1.285947368876626068E-13, 2.052068128417949389 ) ) ;
#39260=CARTESIAN_POINT ( 'NONE',  ( 1.078981819582014445, -0.04439612541052954248, -1.926037623753373618 ) ) ;
#39262=CARTESIAN_POINT ( 'NONE',  ( 4.676165968894677505, 2.197079021736783044, -0.3272799971512970196 ) ) ;
#39269=CARTESIAN_POINT ( 'NONE',  ( 0.1709645942036420174, 0.8561845417300646410, 2.049862257243968422 ) ) ;
#39270=CARTESIAN_POINT ( 'NONE',  ( 5.301206097546149465, -1.683542251207278628, 1.007010407901312465 ) ) ;
#39273=CARTESIAN_POINT ( 'NONE',  ( 0.6323695665565836066, 1.111747700424435159, -1.853661729306683936 ) ) ;
#39275=CARTESIAN_POINT ( 'NONE',  ( 3.420431513525914902, 0.9250737872015384333, 1.843656989716379035 ) ) ;
#39279=CARTESIAN_POINT ( 'NONE',  ( 4.674985431947434655, 0.001863223488791227334, -1.870726058175266715 ) ) ;
#39280=CARTESIAN_POINT ( 'NONE',  ( 3.709331991548686425, 1.648016779243220320, 0.5399856063554776542 ) ) ;
#39281=CARTESIAN_POINT ( 'NONE',  ( 3.438731153704393417, -1.320290108414169605, -1.134124902983554062 ) ) ;
#39282=CARTESIAN_POINT ( 'NONE',  ( 0.9785521075769167965, -2.238008663356937156, -0.4956820494700850399 ) ) ;
#39285=CARTESIAN_POINT ( 'NONE',  ( 4.247661304151585604, 2.090252499381782147, -0.05307422152340918187 ) ) ;
#39286=CARTESIAN_POINT ( 'NONE',  ( 6.333930032320489900, 1.921166581771537318, 0.2825802787540276917 ) ) ;
#39289=CARTESIAN_POINT ( 'NONE',  ( 0.7389079861009685279, 2.013985778099684154, -0.1017531103126300962 ) ) ;
#39290=CARTESIAN_POINT ( 'NONE',  ( 0.6508261300204335464, 2.090236094481153550, 0.3566229023672163878 ) ) ;
#39296=CARTESIAN_POINT ( 'NONE',  ( 2.420699464796825850, -0.8139657014685426351, -1.958238820914718792 ) ) ;
#39298=CARTESIAN_POINT ( 'NONE',  ( 4.178209475066913647, -1.049361115903378883, 1.493786327181771068 ) ) ;
#39304=CARTESIAN_POINT ( 'NONE',  ( 1.810812951734928511, -0.5429070200502202903, -1.945354291398709412 ) ) ;
#39305=CARTESIAN_POINT ( 'NONE',  ( 5.491335294905154818, 1.948586811899848614, -1.035780281143129811 ) ) ;
#39307=CARTESIAN_POINT ( 'NONE',  ( 3.256551146222384396, -0.5358571751262303229, -1.782154170384263603 ) ) ;
#39314=CARTESIAN_POINT ( 'NONE',  ( 4.828627627824715773, 1.747987318788373656, 0.5269492854979712648 ) ) ;
#39318=CARTESIAN_POINT ( 'NONE',  ( 1.088703816646944267, 1.038853075768126910, -1.387971508864824788 ) ) ;
#39319=CARTESIAN_POINT ( 'NONE',  ( 6.421814705521882161, 1.055779539018763646, -1.508159643570324393 ) ) ;
#39320=CARTESIAN_POINT ( 'NONE',  ( 5.444061505814771884, 0.9398705156117830306, -2.107803560374045038 ) ) ;
#39322=CARTESIAN_POINT ( 'NONE',  ( 6.925078400183550364, -0.007619068086212391067, 2.144148427808051594 ) ) ;
#39324=CARTESIAN_POINT ( 'NONE',  ( 5.923294579110739200, 0.9235710928677911546, 2.104827929701275302 ) ) ;
#39328=CARTESIAN_POINT ( 'NONE',  ( 5.946149726614579301, 1.868617323842229894, 0.09011704611043556967 ) ) ;
#39329=CARTESIAN_POINT ( 'NONE',  ( 3.023589307540079041, -0.3687504995396119201, 1.876329818327879817 ) ) ;
#39331=CARTESIAN_POINT ( 'NONE',  ( 5.039771180630152614, -1.558841386063321455, -1.562417271110942307 ) ) ;
#39332=CARTESIAN_POINT ( 'NONE',  ( 4.223895228407223534, 0.9020499113536835090, -1.915681561053275139 ) ) ;
#39334=CARTESIAN_POINT ( 'NONE',  ( 6.883263157960399781, 2.038134514454426505, 2.350812138539408735 ) ) ;
#39337=CARTESIAN_POINT ( 'NONE',  ( 6.164709077089638001, 0.6648188651474650213, 2.013622499735030491 ) ) ;
#39338=CARTESIAN_POINT ( 'NONE',  ( 1.852963337694241819, 0.7249817717532834882, 2.190821962643316301 ) ) ;
#39339=CARTESIAN_POINT ( 'NONE',  ( 3.894932841003693191, 0.2855096342280309396, 1.940843471192068570 ) ) ;
#39342=CARTESIAN_POINT ( 'NONE',  ( 0.2331563151865486683, 0.005903526429595904942, -1.945944850731482934 ) ) ;
#39345=ORIENTED_EDGE ( 'NONE', *, *, #135974, .T. ) ;
#39346=CARTESIAN_POINT ( 'NONE',  ( 5.577361344084559747, 1.530155114678043660, 1.313547687611632764 ) ) ;
#39347=CARTESIAN_POINT ( 'NONE',  ( 0.05820987927622478519, -1.643049995186950829, -0.8308948761173093889 ) ) ;
#39349=CARTESIAN_POINT ( 'NONE',  ( 3.116274269780743733, 2.161009848182334991, -0.2084346501036362376 ) ) ;
#39351=CARTESIAN_POINT ( 'NONE',  ( 0.9144942500491148873, -2.120778211678171488, 0.005759991200282587286 ) ) ;
#39356=CARTESIAN_POINT ( 'NONE',  ( 0.7552377862659557239, -1.739527406477459515, -1.104632168941059867 ) ) ;
#39363=CARTESIAN_POINT ( 'NONE',  ( 2.912652942483742180, -0.5572119909246497915, -1.829279355302193544 ) ) ;
#39364=CARTESIAN_POINT ( 'NONE',  ( 5.629715507205930614, -1.125428185119830005, -1.365942169508828741 ) ) ;
#39367=CARTESIAN_POINT ( 'NONE',  ( 0.4745106373920011666, -1.311730567922615665, 1.249698552857400946 ) ) ;
#39369=CARTESIAN_POINT ( 'NONE',  ( 0.4619447194890722308, -1.061692323622511536, 1.594387217869216888 ) ) ;
#39370=CARTESIAN_POINT ( 'NONE',  ( 2.330607996690749140, -1.275545549462468120, 1.630658604070814199 ) ) ;
#39372=CARTESIAN_POINT ( 'NONE',  ( 6.315307248462690204, -0.2269180964024133385, 1.856785020699961875 ) ) ;
#39373=CARTESIAN_POINT ( 'NONE',  ( 2.349991895876184511, 1.825291697999480434, 0.04531359951509549705 ) ) ;
#39374=CARTESIAN_POINT ( 'NONE',  ( 6.568967528192747096, -2.015767819289843388, -0.8987472251835016968 ) ) ;
#39377=CARTESIAN_POINT ( 'NONE',  ( 4.070800801938780467, 1.460776800910084994, -1.456535598646004237 ) ) ;
#39381=DIRECTION ( 'NONE',  ( -1.000000000000000000, 0.000000000000000000, 0.000000000000000000 ) ) ;
#39382=CARTESIAN_POINT ( 'NONE',  ( 0.8081717762262634608, -2.151237856378166224, 0.2110218573620133986 ) ) ;
#39383=CARTESIAN_POINT ( 'NONE',  ( 6.672334155782003506, -0.9722939650993901450, -1.827837255792996718 ) ) ;
#39385=CARTESIAN_POINT ( 'NONE',  ( 3.919328646192806520, -0.1633067429045453600, 2.155504054270485970 ) ) ;
#39386=CARTESIAN_POINT ( 'NONE',  ( 3.774085898144818874, 2.004173781823472833, -0.2492677732841129534 ) ) ;
#39394=CARTESIAN_POINT ( 'NONE',  ( 2.729704159269104924, 0.7212915320151757070, -1.883313052590728454 ) ) ;
#39399=CARTESIAN_POINT ( 'NONE',  ( 5.256085721135645095, 0.7693902824621422498, -1.750971482026221437 ) ) ;
#39404=CARTESIAN_POINT ( 'NONE',  ( 4.851185501729457172, 0.1948232160459452411, -2.006962824030594561 ) ) ;
#39407=CARTESIAN_POINT ( 'NONE',  ( 6.141572722362285575, -1.252861708448499201, -1.185644778512841002 ) ) ;
#39410=CARTESIAN_POINT ( 'NONE',  ( 4.973830807571049561, 1.075732564348480746, 1.530087412091485799 ) ) ;
#39412=CARTESIAN_POINT ( 'NONE',  ( 2.342711862795249012, -2.029470198211943632, -0.4080651701656515251 ) ) ;
#39416=CARTESIAN_POINT ( 'NONE',  ( 0.6675924852559200762, 1.356316336250670496, 1.492241973137248934 ) ) ;
#39417=CARTESIAN_POINT ( 'NONE',  ( 1.248006495514828895, 0.8912474588982389756, -1.577060073313638622 ) ) ;
#39423=CARTESIAN_POINT ( 'NONE',  ( 5.589432567506730010, -0.4607417488133085381, 1.859251224981002482 ) ) ;
#39431=CARTESIAN_POINT ( 'NONE',  ( 3.098656953246520906, -0.6260995091542167490, -2.069055637940686143 ) ) ;
#39434=CARTESIAN_POINT ( 'NONE',  ( 1.002369745560643510, -0.9483682245385971488, 1.896766750748935415 ) ) ;
#39435=CARTESIAN_POINT ( 'NONE',  ( 6.299803673773761936, -0.6120917497752301761, 1.720027978493202436 ) ) ;
#39436=CARTESIAN_POINT ( 'NONE',  ( 2.354701247847644119, -1.526412939949482128, 1.247560610424301109 ) ) ;
#39439=CARTESIAN_POINT ( 'NONE',  ( 4.422284282497963126, 0.9263432559908044706, 1.738082477136545956 ) ) ;
#39440=CARTESIAN_POINT ( 'NONE',  ( 0.5154417807694658960, -1.038215432012145056, -1.640949389817857984 ) ) ;
#39447=CARTESIAN_POINT ( 'NONE',  ( 5.285773936917006921, 1.841837585529454202, -0.5139651673399318055 ) ) ;
#39449=CARTESIAN_POINT ( 'NONE',  ( 1.184930176456780337, -2.153272645635353033, -0.4822455307981614592 ) ) ;
#39451=CARTESIAN_POINT ( 'NONE',  ( -0.05814382529654647802, -1.176414490726215734, -1.508152472379259867 ) ) ;
#39452=CARTESIAN_POINT ( 'NONE',  ( 0.07661050522433666965, 0.7707917844542893082, -1.796988219766264550 ) ) ;
#39455=CARTESIAN_POINT ( 'NONE',  ( 2.805202726412972414, -1.722705984639979482, 1.148039668612794051 ) ) ;
#39460=CARTESIAN_POINT ( 'NONE',  ( 1.059701713109785670, 0.4209238396889224965, -2.120155868012041811 ) ) ;
#39465=CARTESIAN_POINT ( 'NONE',  ( 6.825078400183572036, 4.699117039843025090, 2.418333817060664526 ) ) ;
#39467=CARTESIAN_POINT ( 'NONE',  ( 4.992643705478089444, -1.725105917503889641, 0.1769386724924902066 ) ) ;
#39469=CARTESIAN_POINT ( 'NONE',  ( 2.905202624773518316, -1.723727875341171778, 1.146311801414557241 ) ) ;
#39470=CARTESIAN_POINT ( 'NONE',  ( 4.763340612834221943, 1.975027209670917161, -0.7632558447715469541 ) ) ;
#39473=CARTESIAN_POINT ( 'NONE',  ( 1.463649477047322733, -0.4837646206634453883, 1.908952741056660685 ) ) ;
#39475=CARTESIAN_POINT ( 'NONE',  ( 0.1758378621803426134, 1.891278220088285833, -0.2826890867150752551 ) ) ;
#39476=CARTESIAN_POINT ( 'NONE',  ( 4.541174964560028116, -1.770302748489580358, -1.456204954804733998 ) ) ;
#39477=CARTESIAN_POINT ( 'NONE',  ( 2.226930044512597906, -0.0006860120723567450030, 1.825872481329051444 ) ) ;
#39482=CARTESIAN_POINT ( 'NONE',  ( 3.357684704777043283, -1.527344908821237635, -1.311707263431096671 ) ) ;
#39483=CARTESIAN_POINT ( 'NONE',  ( 2.905073028004667712, -1.633678134795817360, 1.085783093053994453 ) ) ;
#39487=CARTESIAN_POINT ( 'NONE',  ( 5.665992906516797767, -1.327130266483244059, 1.615391119202228332 ) ) ;
#39488=CARTESIAN_POINT ( 'NONE',  ( 4.944116541256327935, 1.765280609655010879, 0.1280878748119110566 ) ) ;
#39490=CARTESIAN_POINT ( 'NONE',  ( 0.2170718473699268514, -0.1031819972749977166, 2.189145592210713698 ) ) ;
#39491=CARTESIAN_POINT ( 'NONE',  ( 5.947135546971048292, 0.4987507408355364991, -1.667328318302605528 ) ) ;
#39495=CARTESIAN_POINT ( 'NONE',  ( 6.363951117287210302, -0.1083456013219602776, -2.296273276487709847 ) ) ;
#39497=CARTESIAN_POINT ( 'NONE',  ( 5.606719662199564524, 0.7002562906495370942, -1.586348028144116462 ) ) ;
#39498=CARTESIAN_POINT ( 'NONE',  ( 2.104404934925046877, -2.206339196854599116, 0.05594281105186085790 ) ) ;
#39499=CARTESIAN_POINT ( 'NONE',  ( 6.285609470618021888, -2.046568710056245965, 0.7253697862827021003 ) ) ;
#39501=CARTESIAN_POINT ( 'NONE',  ( 1.182980447155062453, 1.727502145113229970, -1.224025170244628757 ) ) ;
#39502=CARTESIAN_POINT ( 'NONE',  ( 3.843750000000002220, 1.895863743164162063, 0.7852924748297951396 ) ) ;
#39503=CARTESIAN_POINT ( 'NONE',  ( 6.727182134110202938, 2.016807574165893513, 2.492494991173601182 ) ) ;
#39504=CARTESIAN_POINT ( 'NONE',  ( 4.629859910813647339, -1.184627732843917647, -1.519026826222178661 ) ) ;
#39505=CARTESIAN_POINT ( 'NONE',  ( 1.664984172775041182, 0.7006824767318786673, 2.107951039278654015 ) ) ;
#39507=CARTESIAN_POINT ( 'NONE',  ( 1.787097420474514031, 1.992035690054320574, -1.134270899834391999 ) ) ;
#39512=CARTESIAN_POINT ( 'NONE',  ( 3.967602866622577107, -1.847128000506767176, -1.233534119358855152 ) ) ;
#39518=CARTESIAN_POINT ( 'NONE',  ( 2.145157927413956944, 0.8647252629472859109, 1.821741647932619390 ) ) ;
#39520=CARTESIAN_POINT ( 'NONE',  ( 6.197729521560835231, -1.491448369540880670, -1.425081351520232964 ) ) ;
#39524=CARTESIAN_POINT ( 'NONE',  ( 0.09881949811249221560, -0.4921898920670075839, 1.774194203830472993 ) ) ;
#39527=CARTESIAN_POINT ( 'NONE',  ( 1.053533388295304629, 1.768092659605845052, -0.07913920300933743879 ) ) ;
#39528=CARTESIAN_POINT ( 'NONE',  ( 0.2291389764034670318, 2.011204493129043591, 0.1455304468792120720 ) ) ;
#39529=CARTESIAN_POINT ( 'NONE',  ( 0.3273695209934923689, 0.9472894719858866441, -1.578709817245539604 ) ) ;
#39530=CARTESIAN_POINT ( 'NONE',  ( 4.072042370276293788, -1.319783315292190284, 1.874172932857321339 ) ) ;
#39531=CARTESIAN_POINT ( 'NONE',  ( 3.134520880496123318, -1.623366475481220261, 0.8686021547102340534 ) ) ;
#39533=CARTESIAN_POINT ( 'NONE',  ( 2.836711209001481659, 0.2215568149019596367, 1.812007907362273018 ) ) ;
#39534=CARTESIAN_POINT ( 'NONE',  ( 4.272111401563948085, 1.799923229630392640, -0.9091438646662284295 ) ) ;
#39536=CARTESIAN_POINT ( 'NONE',  ( 3.379979430277161079, 1.433683275776801214, 1.750306659111708463 ) ) ;
#39538=CARTESIAN_POINT ( 'NONE',  ( 5.561587576256037835, 0.4139992630615954572, -2.064685544603379608 ) ) ;
#39540=CARTESIAN_POINT ( 'NONE',  ( 3.350112325975619587, -0.8415805752714689003, 1.891790567983504312 ) ) ;
#39543=CARTESIAN_POINT ( 'NONE',  ( 6.182307711929101224, 1.089732742074623006, 1.818925385317768928 ) ) ;
#39546=CARTESIAN_POINT ( 'NONE',  ( 0.9965603196819513565, -0.4670424642401714288, -1.868911657674779958 ) ) ;
#39553=CARTESIAN_POINT ( 'NONE',  ( 0.8794853950937852050, -2.011299634806243741, -0.9433073274909502537 ) ) ;
#39554=CARTESIAN_POINT ( 'NONE',  ( 2.538226622342924177, 0.9936286567288643568, -1.856823529840909481 ) ) ;
#39557=CARTESIAN_POINT ( 'NONE',  ( 6.948144928891270666, -0.7966579434352799582, 1.680504273975716334 ) ) ;
#39562=CARTESIAN_POINT ( 'NONE',  ( 0.1762450972803019933, 2.096614079038420897, -0.3174041833761130360 ) ) ;
#39565=CARTESIAN_POINT ( 'NONE',  ( 3.473055881322492322, 1.772541284497713976, 0.8411618914155660764 ) ) ;
#39566=CARTESIAN_POINT ( 'NONE',  ( 2.571340117545738657, 0.1069729528509130723, -2.159185227005658181 ) ) ;
#39567=CARTESIAN_POINT ( 'NONE',  ( 1.663359199420410883, 0.9473472845980964729, 1.578708189602283873 ) ) ;
#39570=CARTESIAN_POINT ( 'NONE',  ( 3.169568575122613918, -1.035934168062458971, 1.398253053441183891 ) ) ;
#39573=CARTESIAN_POINT ( 'NONE',  ( 0.7081719773709761467, -2.151164098719647200, 0.2130325561137471624 ) ) ;
#39574=CARTESIAN_POINT ( 'NONE',  ( 3.655624903986275154, -0.3905385215352343287, -1.977747697055858955 ) ) ;
#39575=DIRECTION ( 'NONE',  ( -3.451266460341926649E-31, -5.200010849845536803E-32, 1.000000000000000000 ) ) ;
#39576=CARTESIAN_POINT ( 'NONE',  ( 0.1456854043008250221, -1.672057201651616642, -1.369741535119282982 ) ) ;
#39577=CARTESIAN_POINT ( 'NONE',  ( 2.606273030088624765, -0.7529636864501542126, -1.822200628222752972 ) ) ;
#39579=CARTESIAN_POINT ( 'NONE',  ( 6.609000000000047947, 7.052356515605485932, 2.698153947863399793 ) ) ;
#39580=CARTESIAN_POINT ( 'NONE',  ( 2.489705217443307195, -1.937006489018164190, -0.1406711297040150188 ) ) ;
#39589=CARTESIAN_POINT ( 'NONE',  ( 5.473738792520003393, 2.225791634824420218, -0.6087584347118053518 ) ) ;
#39592=CARTESIAN_POINT ( 'NONE',  ( 3.660947809037872425, 1.549288415169544963, -1.203348422379519667 ) ) ;
#39594=CARTESIAN_POINT ( 'NONE',  ( 0.7916389524552719381, 1.525042296397002062, -1.319230309296010706 ) ) ;
#39596=CARTESIAN_POINT ( 'NONE',  ( 2.729822841111886333, 0.7574698553451510996, -1.977403127767562552 ) ) ;
#39599=CARTESIAN_POINT ( 'NONE',  ( 3.240019139272034110, 0.4481936114588759845, 1.785621944311803100 ) ) ;
#39602=CARTESIAN_POINT ( 'NONE',  ( 4.465154236216789307, -1.701427117168831549, 1.265499569954648962 ) ) ;
#39603=CARTESIAN_POINT ( 'NONE',  ( 0.5679803739370090643, -1.732728882149033645, -0.6228371021387222317 ) ) ;
#39608=CARTESIAN_POINT ( 'NONE',  ( 4.516905262009872857, 1.882569317753344240, 0.8387543118332175807 ) ) ;
#39610=CARTESIAN_POINT ( 'NONE',  ( 1.118424870118275738, -0.04499623084481922664, 1.840855209834332928 ) ) ;
#39614=CARTESIAN_POINT ( 'NONE',  ( 1.506762622594171930, -0.7967928049063888185, -2.058199171410409978 ) ) ;
#39615=CARTESIAN_POINT ( 'NONE',  ( 4.165478197628463164, 0.2823181557158191968, -2.244685958880874743 ) ) ;
#39617=CARTESIAN_POINT ( 'NONE',  ( 3.515680188161012687, -0.5209108127710823100, 1.735096886039680930 ) ) ;
#39618=CARTESIAN_POINT ( 'NONE',  ( 4.751152363292252545, 0.1813030634821456710, -1.907091066879146757 ) ) ;
#39619=CARTESIAN_POINT ( 'NONE',  ( 4.967269779104159788, 1.799668380515653920, 1.023422521214325309 ) ) ;
#39621=CARTESIAN_POINT ( 'NONE',  ( 2.729320057108883368, -1.840128979258702557, 0.7079907272262278006 ) ) ;
#39622=CARTESIAN_POINT ( 'NONE',  ( 0.9383530073892000223, 1.897354475554638320, 0.3323884044314562858 ) ) ;
#39623=CARTESIAN_POINT ( 'NONE',  ( 4.434354141042872399, 1.834536173243521917, 0.3649259964926266364 ) ) ;
#39624=CARTESIAN_POINT ( 'NONE',  ( 3.950101280099535650, 0.7789643570827823327, -2.172381230931414109 ) ) ;
#39625=CARTESIAN_POINT ( 'NONE',  ( 3.525696930263744200, 1.816150354290571034, -0.4055864600542318232 ) ) ;
#39627=CLOSED_SHELL ( 'NONE', ( #108625, #13250, #118798, #106672, #171398, #57973, #56911, #114876 ) ) ;
#39629=CARTESIAN_POINT ( 'NONE',  ( 1.067171494879548987, -1.904794536548588546, -0.8987870243707897222 ) ) ;
#39633=CARTESIAN_POINT ( 'NONE',  ( 6.749309733681256418, -1.731629633356733589, -1.293610171197785652 ) ) ;
#39634=CARTESIAN_POINT ( 'NONE',  ( 1.951583061186522583, -1.892041120407188304, 0.9578705467366486204 ) ) ;
#39636=CARTESIAN_POINT ( 'NONE',  ( 1.195576078702242473, 1.864576247583774160, -0.7769579012074608881 ) ) ;
#39642=CARTESIAN_POINT ( 'NONE',  ( 1.300320450452172594, -2.161773191439372965, -0.001381507821696103871 ) ) ;
#39645=CARTESIAN_POINT ( 'NONE',  ( 6.925078400183562799, 2.053856789352814793, 2.261525409452989965 ) ) ;
#39648=CARTESIAN_POINT ( 'NONE',  ( 6.350795928397162449, -1.845624747684541989, -0.8128223418941012968 ) ) ;
#39650=EDGE_CURVE ( 'NONE', #57181, #139360, #141372, .T. ) ;
#39651=CARTESIAN_POINT ( 'NONE',  ( 0.3807642395799659130, -0.2741851280289032688, -2.174293136291181483 ) ) ;
#39653=CARTESIAN_POINT ( 'NONE',  ( 0.5501786683353731000, 0.7064523498505774768, -2.149447411369388217 ) ) ;
#39658=CARTESIAN_POINT ( 'NONE',  ( 1.142033650006045731, 0.7776438622074226537, 1.750858609485239192 ) ) ;
#39662=CARTESIAN_POINT ( 'NONE',  ( 2.683889919492283394, -0.8868522494023568514, 1.479262710868123110 ) ) ;
#39664=CARTESIAN_POINT ( 'NONE',  ( 1.686396851806533315, -0.2532433360125495025, -1.751381468886082038 ) ) ;
#39665=CARTESIAN_POINT ( 'NONE',  ( 5.016741729952475914, 1.524926965779101140, -1.595359541877178877 ) ) ;
#39667=CARTESIAN_POINT ( 'NONE',  ( 4.078382194585396192, 0.9556978891391977315, 1.779404116599448082 ) ) ;
#39669=CARTESIAN_POINT ( 'NONE',  ( 4.846395287928321416, 1.089488137594313510, -1.819044145143506208 ) ) ;
#39670=CARTESIAN_POINT ( 'NONE',  ( 3.954703970953522774, -1.882481274494081980, -0.7231244775810635739 ) ) ;
#39671=CARTESIAN_POINT ( 'NONE',  ( 4.341949102618557710, -1.119799544600053265, -1.423922225892548354 ) ) ;
#39675=CARTESIAN_POINT ( 'NONE',  ( 1.322894217037653863, -0.04941562205608431707, 1.870173573632450736 ) ) ;
#39679=CARTESIAN_POINT ( 'NONE',  ( 6.340474544234134591, 1.036764729950395258, -1.485249760763515114 ) ) ;
#39684=VERTEX_POINT ( 'NONE', #30048 ) ;
#39688=CARTESIAN_POINT ( 'NONE',  ( 4.131183091185314460, 1.940096312829143299, 0.8565103500411813675 ) ) ;
#39691=CARTESIAN_POINT ( 'NONE',  ( 5.712177144062582812, -0.8841330711255364072, -1.762019952394773936 ) ) ;
#39694=CARTESIAN_POINT ( 'NONE',  ( 0.5803383592409648850, 0.9960403410373251942, 1.749501224816521816 ) ) ;
#39696=CARTESIAN_POINT ( 'NONE',  ( 6.456269881894531437, -1.301449686459619226, 1.670992065744638433 ) ) ;
#39698=CARTESIAN_POINT ( 'NONE',  ( 1.223191768902037957, -1.870915810643185795, -0.8869332102946840823 ) ) ;
#39702=CARTESIAN_POINT ( 'NONE',  ( 4.646477879911859787, -1.679251869332079483, 1.245118527403435094 ) ) ;
#39705=CARTESIAN_POINT ( 'NONE',  ( 2.819161699164650869, -0.1809198688003388622, 1.816599095187728219 ) ) ;
#39706=CARTESIAN_POINT ( 'NONE',  ( 1.822642882514250218, 1.341887823972046201, -1.217030898042359643 ) ) ;
#39708=CARTESIAN_POINT ( 'NONE',  ( 6.674453038267287752, -1.361800985140369402, 1.737325302230605661 ) ) ;
#39710=CARTESIAN_POINT ( 'NONE',  ( 4.014836333542094238, 1.562590183666903165, -1.558512549626612342 ) ) ;
#39714=CARTESIAN_POINT ( 'NONE',  ( 3.035702773332124238, -1.842316306609870891, 0.5122265333450183311 ) ) ;
#39716=CARTESIAN_POINT ( 'NONE',  ( 6.408651866624735405, 0.6456447432892989946, 1.967203394946090755 ) ) ;
#39719=CARTESIAN_POINT ( 'NONE',  ( 6.110890996357365879, -0.2699588104537915534, 2.174781792473476472 ) ) ;
#39727=CARTESIAN_POINT ( 'NONE',  ( -0.2409995289980246258, 1.355929887833319469, -2.254219809973062816 ) ) ;
#39731=CARTESIAN_POINT ( 'NONE',  ( 5.998901810315326877, 0.3981486965325408134, 2.031442706791640074 ) ) ;
#39732=CARTESIAN_POINT ( 'NONE',  ( 4.565017902933249161, -1.721472425840556930, -0.8649740032428044900 ) ) ;
#39733=CARTESIAN_POINT ( 'NONE',  ( 0.6148615108944045504, 0.1511614643284354409, 2.010825953887733775 ) ) ;
#39737=CARTESIAN_POINT ( 'NONE',  ( 1.675987266036529366, -1.170314894790158933, 1.852603040092117848 ) ) ;
#39738=CARTESIAN_POINT ( 'NONE',  ( 5.602125774977974260, -1.825872481414937853, 0.004271240736861136277 ) ) ;
#39747=CARTESIAN_POINT ( 'NONE',  ( 2.858754248528099229, 0.2676582106064147593, -1.821554178878769470 ) ) ;
#39748=CARTESIAN_POINT ( 'NONE',  ( 5.836195099138038245, -1.121959161234881819, -1.671398195203987136 ) ) ;
#39749=CARTESIAN_POINT ( 'NONE',  ( 2.179500908114082591, -1.083194949601238521, -2.027108130913716444 ) ) ;
#39751=CARTESIAN_POINT ( 'NONE',  ( 6.420756404446519738, -1.389671697431221542, 1.384925340169262054 ) ) ;
#39754=CARTESIAN_POINT ( 'NONE',  ( 3.111475685156277038, 1.510342251817019532, 1.173009309769344588 ) ) ;
#39756=CARTESIAN_POINT ( 'NONE',  ( 0.8716356842100521085, -0.3054578492302991721, 2.047597563663336118 ) ) ;
#39758=CARTESIAN_POINT ( 'NONE',  ( 2.138330579027637679, 0.4610650599585190967, 2.039099516977191495 ) ) ;
#39759=CARTESIAN_POINT ( 'NONE',  ( 1.305301652190330675, -0.4579020413679709689, 1.813615928118620380 ) ) ;
#39760=CARTESIAN_POINT ( 'NONE',  ( 2.091172504846372959, 1.163092143266548639, -1.646586049616038494 ) ) ;
#39764=CARTESIAN_POINT ( 'NONE',  ( 3.702475415089864441, 1.494950309154385426, 0.8909294612347866682 ) ) ;
#39768=CARTESIAN_POINT ( 'NONE',  ( 2.859633459980165160, 1.716568739768107532, -0.1690650336269062803 ) ) ;
#39769=CARTESIAN_POINT ( 'NONE',  ( 2.700927432832851860, 1.852951201923001223, 1.169960570980829839 ) ) ;
#39770=CARTESIAN_POINT ( 'NONE',  ( 0.05276861106134726059, -1.135576942788417254, 1.310739833803043819 ) ) ;
#39771=CARTESIAN_POINT ( 'NONE',  ( 5.057340365224886725, -1.863002784048470639, -1.182737378625432489 ) ) ;
#39773=( BOUNDED_SURFACE ( )  B_SPLINE_SURFACE ( 3, 3, ( 
 ( #106127, #173227, #91983, #190505, #44286, #60509, #42162, #75705, #207822, #59451, #125607, #22662, #191567, #43231, #109348, #175358, #93046, #88773, #154831, #138588, #204611, #172150, #81031, #113602, #147118, #130915, #30152, #214179, #65807, #96240, #212073, #61583, #63712, #161224, #177476, #196908, #178542, #48548, #162291, #163360, #131954, #160156, #47493, #82085, #78884, #213144, #114666, #94115, #79957, #176411, #29091, #14935, #13878, #148178, #97301, #95175, #197964, #111471, #146059, #64774, #180660, #129869, #145007, #110407, #62635, #12811, #32285, #211013, #98350, #46413, #164416, #128794, #45352, #16000, #112529, #195853, #179606, #28017, #127751, #31227, #11754, #77828, #194776, #143949, #209944, #193708, #51742, #151379, #117865, #37614, #84226, #116787, #102622, #53871, #100474, #120004, #182784, #133016, #83149, #166549, #66871, #199015, #167616, #87439, #34402, #118931, #103694, #18137, #67940, #50661, #49595, #33339, #183856, #150314, #1880, #99421, #71152, #134084, #200093, #69020, #35469, #169744, #202217, #101546, #181709, #19214, #85293, #2948, #21333, #135137, #201153, #152436, #52792, #803, #185980, #184911, #36535, #165475, #17071, #168677, #153507, #5077, #115719, #20281, #86365, #4015, #70084, #136199, #149228, #137269, #122155, #171885, #88515, #210510, #127231, #11239, #79454, #203289, #109895, #154577, #27498, #7222, #77318, #175907, #170815, #188123, #13379, #61072, #143431, #45913, #209427, #29651, #54936, #193201, #112031, #44848, #176961, #121088, #187055, #139400, #38687, #159642, #110954, #93598, #23482, #62146, #161788, #104766, #28577, #78382, #94665, #22406, #144503, #138330, #56004, #95736, #39754, #6153, #105859, #155638, #160708, #12302, #128305, #194267, #72223, #178033, #204346, #89589, #73297, #192117, #205433, #60001, #43781, #126154, #181211, #98915, #115220, #166037, #80521, #82642, #16559, #130422, #15497, #146619, #148726, #81585, #48054, #147668, #296, #32838, #66366, #132513, #213685, #17622, #83707, #65308, #131457, #30721, #197458, #212636, #64277, #198511, #97859, #50157, #163921, #164967, #149796, #49100, #1370, #116279, #195345, #145571, #211569, #14432, #182269, #33894, #114167, #99972, #63203, #129367, #96804, #46977, #162853, #196409, #180160, #113093, #179099, #31786, #111652, #175533, #210128, #78011, #192813, #9807, #93228, #60691, #177664, #27122, #144135, #30344, #110587, #94295, #92166, #109526, #125786, #160335, #46599, #193890, #59629, #42342, #43403, #208003, #127938, #158218, #10861, #96429, #190683, #162480, #29272, #159260, #14052, #191748, #176589, #79074, #211198, #44471, #76934, #80141, #143060, #209055, #145192, #126855, #161414, #28201, #62824, #11939, #61770, #95364, #45538, #12998, #128984, #124723, #75882, #194963, #112717, #178729, #146244, #212260, #108457, #174477, #26053, #141989, #65986, #51920, #98533, #131098, #116971, #68127, #114839, #134262, #197087, #147293, #97483, #180837, #81213, #213324, #181887, #101724, #48725, #133194, #118043, #32464, #82264, #64946, #63894, #47676, #132136, #164594, #16180, #113787, #85469, #148357, #214356, #83325, #198143, #184029, #2054, #49775, #196042, #115902, #33523, #99595, #35645, #165661, #17248, #166733, #149412, #15125, #200268, #994, #67058, #179789, #31409, #199196, #167795, #19390, #130049 ),
 ( #50844, #182968, #151557, #163540, #34583, #100655, #18324, #84407, #150495, #187234, #185087, #136376, #24728, #72407, #22585, #52967, #154751, #189372, #186161, #39938, #89773, #201329, #38863, #69194, #70262, #122341, #55115, #205611, #37794, #202395, #56180, #7403, #54047, #73484, #120184, #86541, #36711, #103869, #20458, #152606, #121261, #41015, #169918, #138507, #57248, #21504, #87613, #4192, #3125, #119105, #71329, #153684, #5252, #102797, #90831, #137444, #203461, #88691, #104946, #123408, #155819, #170986, #135315, #6335, #204530, #188298, #107124, #106046, #172069, #23663, #139584, #168855, #173147, #59374, #159015, #140667, #75633, #191490, #156893, #8481, #74568, #143875, #10609, #142801, #60435, #126595, #110333, #29013, #176336, #11679, #196835, #84147, #83069, #181634, #212001, #129797, #214104, #32205, #165395, #116705, #182705, #34324, #2869, #168598, #101466, #104686, #54858, #85212, #186976, #7148, #3933, #72147, #122080, #19135, #4996, #151298, #20198, #154498, #153427, #139326, #22321, #86287, #201073, #36460, #137190, #204269, #39671, #103611, #70003, #118848, #202132, #152358, #55922, #136117, #105782, #185899, #171807, #119924, #184830, #88434, #21252, #203212, #38608, #121009, #170735, #23399, #89512, #155566, #190181, #207498, #10359, #76436, #191239, #142544, #42902, #208550, #109011, #157708, #192303, #175030, #12494, #90580, #160898, #24467, #156640, #25547, #27688, #26617, #62328, #176090, #91655, #60184, #126343, #92718, #74315, #9305, #125277, #93787, #75378, #43962, #94847, #158764, #110078, #8232, #173973, #41836, #159823, #111146, #11426, #124219, #106865, #107947, #58054, #77502, #140412, #141492, #78567, #40759, #28763, #143621, #144687, #189124, #209616, #210698, #61258, #127416, #172892, #206430, #193388, #59120, #45032, #177146, #164102, #163040, #198695, #83889, #194453, #15685, #479, #197643, #128487, #66545, #63395, #195531, #166213, #113284, #149980, #179290, #80716, #31966, #115406, #131640, #213870, #145757, #132688, #129549, #14620, #65493, #114348, #1551, #34080, #180345, #181399, #49288, #33023, #99100, #17806, #47170, #165153, #16744, #96989, #98049, #30914, #82829, #81772, #146806, #147852, #148905, #50339, #116459, #182452, #48235, #46098, #112214, #100149, #178223, #79638, #29838, #212824, #64460, #95922, #196593, #161976, #13566, #211757, #130604, #53531, #155306, #136932, #117531, #105511, #23137, #151052, #55662, #5814, #201881, #199766, #135860, #52468, #84963, #187788, #184583, #69756, #170474, #134812, #18879, #71889, #118593, #19946, #51411, #183525, #102276, #39417, #137998, #67612, #186723, #36201, #152107, #2619, #68690, #167292, #104427, #200817, #3677, #37281, #204016, #202959, #87097, #133757, #103352, #169416, #21000, #4741, #70816, #22060, #154241, #89255, #140148, #28505, #76182, #26355, #56737, #158509, #193131, #189929, #43710, #93528, #205096, #190982, #72966, #74056, #126086, #58867, #44780, #208301, #206172, #110886, #7965, #125025, #175838, #159570, #75124, #41575, #176892, #173717, #57802, #27430, #123961, #109828, #157455, #11167, #25293, #156383, #59931, #9049, #42646, #10109, #6888, #172634, #141233, #77244, #207242, #107689, #91394, #108756, #174780, #92471, #142289, #192047, #209358, #143361, #61003, #127160, #94594, #139071, #122905, #188863 ),
 ( #40501, #106605, #24209, #144436, #14366, #13314, #79387, #210438, #182204, #30654, #177967, #180095, #161722, #96740, #95669, #29581, #45845, #131396, #145506, #129303, #111964, #164902, #81523, #31719, #33830, #160638, #64214, #211504, #196346, #179036, #97794, #130354, #128236, #63141, #12238, #15434, #163854, #62079, #147601, #132451, #195280, #197393, #32772, #194199, #47988, #78312, #46912, #65246, #212575, #198449, #213619, #113030, #50095, #162788, #114104, #115155, #98851, #80457, #146555, #116216, #49035, #181150, #16495, #82576, #148664, #230, #66302, #118351, #34883, #152920, #35962, #151867, #37024, #99909, #51159, #168109, #136686, #19708, #100956, #184339, #135618, #201638, #102040, #53286, #85787, #87920, #134575, #167046, #4499, #104182, #150805, #170231, #18638, #183279, #133510, #2369, #117281, #84717, #3442, #137756, #68446, #169166, #153994, #200576, #69509, #52223, #165970, #83641, #119419, #185406, #103108, #149728, #121573, #20761, #86855, #70567, #202711, #5563, #38110, #54362, #17555, #120503, #186474, #21816, #71643, #203775, #55419, #187544, #1306, #67366, #199514, #23969, #205925, #22890, #89007, #73800, #159316, #109580, #39175, #26107, #7716, #9859, #59679, #173461, #143116, #209107, #25041, #140980, #204840, #206989, #90071, #106357, #125839, #107437, #191797, #91142, #92219, #60745, #157198, #126907, #108506, #155059, #76989, #105258, #122651, #58618, #8795, #139894, #42396, #74874, #171299, #6646, #10913, #72725, #138819, #156134, #158270, #124774, #56493, #75935, #57558, #190733, #174529, #142036, #188614, #123716, #189677, #208052, #41327, #43459, #40246, #175584, #27174, #172380, #93278, #193942, #14103, #117821, #50613, #127988, #110639, #111705, #61821, #198969, #11988, #145244, #167569, #44522, #35421, #116738, #19169, #68972, #182737, #101499, #34356, #166500, #192866, #176641, #129041, #28253, #757, #100429, #80193, #13049, #51699, #151331, #94346, #66823, #67895, #18091, #160388, #134040, #45589, #177714, #85243, #29323, #2899, #95417, #211249, #96484, #84179, #150268, #132966, #210181, #200048, #161469, #62874, #1836, #178784, #78064, #144189, #30398, #183811, #195018, #46650, #112773, #162531, #202168, #105815, #171841, #103647, #121044, #53826, #23434, #187011, #87393, #38642, #89545, #138288, #155596, #7181, #118879, #104721, #201105, #119956, #39706, #170769, #172926, #122112, #185931, #106900, #136151, #22358, #73252, #139359, #203246, #169699, #24503, #153460, #37567, #205390, #21287, #57028, #71108, #123195, #5033, #70035, #188077, #137226, #88470, #72179, #135091, #86317, #54890, #189156, #154530, #6109, #204303, #55959, #40795, #90613, #156672, #8264, #52745, #184865, #36492, #102569, #168629, #20232, #152389, #3967, #157742, #107979, #125310, #91689, #9339, #192336, #112247, #59152, #143657, #128519, #191269, #92751, #75412, #74348, #58090, #142576, #141525, #207533, #124251, #95955, #158795, #42935, #93818, #109044, #62358, #12528, #208583, #206463, #60218, #175063, #26650, #194487, #10392, #76467, #177181, #126377, #25578, #78600, #43995, #110113, #190209, #41869, #176124, #46130, #144720, #140452, #61292, #27724, #159859, #11462, #77535, #174007, #45068, #209651, #127453, #193424, #210732, #111179, #28797, #162009, #94881, #160933, #178258, #29871, #32000, #33057 ),
 ( #197675, #195567, #212856, #14655, #49319, #150012, #82862, #163074, #145787, #146837, #97020, #16778, #47203, #114381, #199798, #79672, #67643, #148938, #51443, #101240, #511, #133790, #66578, #198725, #13598, #211790, #164136, #63428, #181427, #132720, #115436, #48268, #83922, #183557, #129580, #99135, #100183, #50371, #113318, #166248, #80749, #64493, #117562, #130635, #35164, #196627, #180376, #131673, #116494, #182483, #165184, #30945, #17838, #98081, #15720, #34111, #213904, #179325, #81805, #65527, #1582, #147888, #88202, #104461, #205125, #19979, #138030, #204044, #135893, #153199, #86063, #55694, #4770, #119698, #70849, #121849, #170508, #187820, #39447, #87129, #56769, #122935, #136963, #54630, #118627, #120777, #3708, #152140, #105542, #21031, #171575, #202991, #5850, #188892, #186757, #40533, #22090, #2648, #167323, #18909, #36231, #38380, #154275, #201911, #71921, #23172, #84993, #68721, #139098, #134843, #200846, #53564, #155336, #6919, #151084, #72996, #185681, #184613, #102309, #168383, #37310, #103384, #169446, #93559, #157489, #59966, #77282, #75157, #92503, #25326, #143395, #158542, #58906, #10139, #209392, #109859, #61036, #127197, #26391, #210473, #62111, #76214, #208334, #57832, #126120, #9083, #173749, #193164, #174815, #44814, #142324, #159603, #128270, #192080, #194232, #175873, #156412, #144469, #106637, #189961, #43746, #27461, #141267, #11201, #110918, #172665, #7999, #78346, #74091, #140183, #207275, #176924, #28539, #24242, #94631, #125059, #160674, #12270, #90343, #206204, #191015, #42682, #123993, #108789, #41611, #107723, #91427, #15464, #13345, #30686, #46943, #81550, #182234, #115185, #195312, #95700, #179067, #129336, #49065, #79420, #64243, #17586, #111998, #166001, #181180, #83670, #133539, #32805, #149760, #98880, #16524, #45876, #161754, #48018, #145537, #213651, #164933, #147633, #80488, #116245, #1337, #211535, #65277, #132477, #82607, #63170, #50124, #113061, #96769, #67398, #162821, #114134, #180126, #31752, #163889, #148692, #262, #131423, #97824, #33858, #197423, #66331, #210383, #44722, #14305, #178983, #110831, #111909, #62024, #194141, #128180, #96684, #126029, #29524, #58816, #145450, #208246, #191992, #162733, #43657, #80400, #109774, #11113, #176836, #45790, #177910, #144383, #76131, #211447, #59879, #159514, #95616, #28450, #146496, #30597, #94542, #161666, #13260, #79332, #63081, #124969, #175783, #129249, #195221, #27375, #160581, #93476, #46858, #12188, #77188, #78259, #112971, #190931, #42595, #108700, #193071, #174729, #26301, #92415, #158455, #10054, #142234, #143310, #209302, #60949, #127106, #150747, #132389, #51097, #168046, #198390, #85721, #67308, #47933, #35901, #19648, #81468, #17499, #50031, #181093, #1248, #116156, #101977, #114046, #184276, #180040, #31662, #48978, #117223, #182142, #212514, #199455, #115097, #83586, #165914, #66240, #97739, #32710, #148604, #183220, #98792, #149668, #118290, #33773, #99852, #163797, #197337, #213566, #133450, #134514, #34826, #147545, #130298, #131342, #65188, #100900, #15374, #164846, #64156, #196286, #52163, #166989, #16438, #82517, #18580, #173, #84658, #2308, #68385, #200518, #87862, #201580, #105197, #138760, #187484, #186411, #7655, #107375, #3381, #39114, #23908, #6583, #4438, #56431, #203712, #189620, #204777 ),
 ( #172318, #70508, #188552, #153934, #90012, #170166, #86793, #122590, #5503, #55360, #88944, #151808, #103050, #71583, #40184, #137692, #152860, #21754, #171234, #22830, #121512, #154998, #72662, #139836, #38048, #136623, #106297, #156068, #202650, #73739, #54299, #20700, #185345, #120437, #169103, #104119, #205864, #41267, #57498, #123657, #173398, #24979, #69450, #135556, #53226, #119357, #36967, #158209, #9798, #140916, #112708, #175523, #108447, #110578, #92156, #79064, #29263, #10852, #8735, #159251, #75873, #174467, #145182, #207994, #93220, #193880, #141980, #42333, #95355, #59621, #43394, #74816, #206930, #125777, #211188, #161405, #91082, #78002, #191738, #27113, #26043, #109516, #190672, #61760, #76925, #143051, #209046, #12989, #11931, #176580, #178719, #157142, #60682, #126846, #192803, #44462, #28190, #94286, #58559, #160326, #124712, #144126, #210119, #127928, #45528, #62813, #111643, #177655, #128974, #194953, #46589, #96419, #16171, #214347, #212251, #15115, #31399, #65977, #166723, #99587, #179780, #162469, #163530, #113778, #33515, #63885, #131090, #2045, #14043, #84398, #165653, #68116, #118033, #17240, #150486, #83315, #984, #30334, #80130, #180829, #146234, #198136, #149402, #132127, #64939, #100646, #200259, #130040, #49767, #116961, #67049, #196033, #182959, #97474, #81204, #134252, #147283, #51910, #213315, #197079, #148347, #133186, #199186, #115893, #47667, #34574, #48716, #114830, #181878, #82255, #32454, #98523, #50834, #18314, #164585, #154743, #204522, #73475, #102790, #56171, #122333, #54039, #21498, #103860, #188290, #5246, #137436, #203452, #39930, #139576, #35636, #101715, #55107, #167786, #19382, #3116, #69186, #185079, #50577, #114586, #180578, #46336, #136109, #138249, #202125, #121002, #35385, #53784, #151292, #71065, #2863, #105773, #135054, #201066, #153419, #119917, #36454, #4989, #37527, #52708, #118840, #102529, #168591, #20192, #86279, #186970, #103603, #152350, #203205, #3927, #137182, #169660, #38601, #104679, #22313, #204263, #55914, #122073, #109003, #61250, #76425, #92708, #193379, #8223, #126334, #192293, #124212, #141484, #74307, #43953, #207490, #107941, #59110, #110069, #158755, #176081, #27679, #75370, #45023, #111134, #125269, #42894, #106856, #175020, #206422, #140403, #93775, #9297, #159814, #191231, #208542, #28754, #26607, #155559, #10349, #205348, #7140, #73211, #24459, #142534, #60177, #190174, #11418, #77493, #139318, #56984, #127406, #189115, #40749, #58046, #143612, #209605, #172884, #90572, #41828, #156633, #173966, #25540, #91648, #157700, #30905, #81763, #145747, #48228, #471, #80708, #64451, #62318, #79628, #95913, #130596, #16736, #164095, #29829, #12484, #13557, #178213, #98042, #128478, #195522, #66540, #160889, #148898, #15677, #132681, #182444, #147844, #198687, #213863, #65484, #94838, #78558, #96980, #144676, #114340, #131633, #196585, #129541, #165145, #50332, #210690, #180336, #181391, #197632, #194445, #33014, #161966, #211748, #116450, #63386, #46088, #47159, #113275, #212814, #49277, #115398, #31958, #112206, #99093, #179280, #163029, #82822, #146798, #14611, #154234, #19941, #87091, #37275, #1543, #167286, #58596, #103345, #53524, #83883, #185643, #5805, #2613, #70811, #120742, #17795, #3672, #100142, #101198, #153161, #86027, #71882, #20995 ),
 ( #54595, #18871, #136924, #184576, #186716, #52462, #183518, #4736, #36195, #152101, #169410, #34071, #199760, #102271, #202951, #168346, #35126, #118588, #69748, #135854, #201876, #119658, #38344, #22054, #68682, #84955, #104420, #170468, #151044, #88164, #134806, #117524, #67605, #200812, #51404, #137991, #204009, #124751, #166206, #149973, #133751, #175561, #209083, #191777, #190711, #174507, #44500, #43433, #109557, #26083, #212287, #60720, #208030, #210155, #27152, #178760, #129014, #110617, #108483, #176617, #93256, #59658, #30372, #159290, #192841, #79102, #10889, #142015, #194991, #76964, #143091, #92198, #158248, #126883, #96459, #46625, #42372, #177688, #28229, #94322, #125815, #160363, #75912, #161444, #11966, #78039, #144163, #112748, #111681, #61797, #63921, #9836, #127966, #193918, #45564, #29299, #95393, #13025, #145220, #211226, #62852, #162509, #14080, #80170, #146276, #148385, #131126, #214386, #181918, #100681, #88718, #70288, #57272, #7428, #203486, #201355, #137472, #54075, #152632, #123434, #186185, #71356, #23687, #136404, #20483, #73509, #120210, #21528, #52996, #119132, #103895, #189396, #139612, #69222, #122367, #37818, #153710, #4219, #202420, #168879, #39963, #169943, #87639, #5279, #205634, #204555, #154777, #156919, #135341, #187260, #55139, #104972, #121284, #6361, #38887, #36738, #171013, #90855, #138532, #72430, #185112, #188323, #41038, #22610, #106071, #107148, #102824, #89797, #24753, #75653, #127692, #60456, #46357, #209888, #141760, #194718, #9576, #126613, #177418, #95119, #76702, #43177, #112477, #175300, #207768, #29036, #59395, #45294, #159034, #161168, #26886, #157988, #61526, #10627, #192576, #160097, #8508, #174246, #142819, #111414, #208826, #125551, #92989, #44231, #110352, #176355, #27963, #94056, #210955, #109290, #191512, #193652, #12754, #11700, #78828, #77774, #91928, #42108, #143894, #25818, #144949, #62582, #178486, #128744, #30096, #96186, #74589, #206708, #58335, #140692, #124491, #190450, #108221, #149169, #48492, #32226, #97245, #179551, #47433, #132955, #80973, #114610, #113548, #166489, #83090, #181655, #35409, #162237, #65752, #31172, #197906, #180601, #33281, #131898, #129814, #147064, #183799, #17014, #99366, #212016, #165418, #134028, #98298, #198958, #34345, #146006, #49535, #13823, #14880, #66812, #214123, #200035, #746, #213084, #51687, #163299, #115661, #116726, #100418, #15945, #164361, #117809, #82029, #64715, #182726, #148122, #50601, #18080, #84168, #150256, #1824, #67882, #79897, #63660, #195795, #101487, #52734, #169687, #138276, #21275, #102557, #119944, #137213, #203235, #103635, #54879, #87381, #89533, #136139, #168618, #154518, #105804, #152377, #171828, #20220, #184854, #135080, #3956, #118868, #70023, #5022, #139347, #202156, #170757, #155585, #53815, #185920, #37555, #167558, #85231, #153449, #71096, #121033, #151320, #123184, #187000, #38631, #104708, #22346, #7170, #39694, #88458, #19158, #6099, #72168, #204290, #73240, #55947, #122100, #188064, #23422, #205377, #57015, #189144, #2888, #68960, #201093, #25567, #58077, #94868, #157731, #42922, #143645, #107967, #206449, #193412, #91679, #207521, #24489, #90600, #75400, #160922, #111167, #40782, #27712, #9327, #125299, #190199, #124239, #140438, #11450, #173995, #141513, #41858, #45055, #176112, #60204 ),
 ( #172914, #12516, #43982, #78587, #156660, #93807, #144709, #159847, #77524, #8252, #74336, #191257, #59140, #208571, #209639, #76456, #109032, #177168, #210721, #175051, #142564, #127441, #110101, #26637, #62348, #92738, #158783, #10380, #126365, #192324, #61279, #146825, #98068, #33043, #197662, #65513, #63416, #66566, #129568, #80736, #131659, #180364, #150000, #100171, #15706, #99121, #165171, #16765, #82849, #17826, #47192, #148925, #498, #163063, #81792, #113305, #132708, #147875, #64482, #213891, #116481, #182471, #34100, #166236, #83909, #1570, #194476, #46119, #112236, #195555, #178246, #30933, #179312, #95941, #48254, #161997, #79660, #97009, #14643, #130623, #196615, #202979, #183545, #171564, #19969, #105530, #204034, #133778, #120768, #102299, #3698, #68709, #2637, #18898, #104449, #52486, #86053, #84982, #138019, #54620, #153188, #6909, #199785, #37300, #134832, #169436, #152129, #4761, #103374, #101229, #118616, #155325, #186747, #70837, #35152, #136954, #23162, #69774, #170497, #5839, #117551, #21020, #51431, #200835, #38369, #185671, #89277, #22080, #184603, #167311, #36220, #87117, #88192, #71910, #201901, #135882, #53553, #119685, #154265, #55683, #121839, #187811, #9072, #93548, #91416, #7990, #126109, #75146, #125048, #10128, #72986, #24231, #141256, #109848, #207264, #74079, #157477, #108778, #174804, #58894, #26380, #191003, #61026, #107711, #140171, #192069, #77271, #123983, #143383, #206193, #156402, #106627, #41600, #90333, #57821, #42670, #110908, #173737, #142313, #127187, #25315, #158531, #76203, #139090, #56760, #208323, #59954, #43734, #122924, #94621, #175862, #27450, #159592, #11191, #193154, #209382, #44804, #205117, #176914, #160664, #188882, #40523, #172656, #14387, #164923, #79410, #161744, #16516, #129326, #179057, #210463, #62101, #144459, #48007, #82599, #147624, #128260, #253, #145527, #46933, #33850, #113051, #99931, #30676, #96759, #130377, #49056, #15454, #97815, #162810, #132469, #146578, #196367, #163879, #194222, #165993, #71663, #3462, #4519, #169189, #86876, #103131, #203795, #18659, #136707, #202731, #134596, #69532, #84739, #54383, #135639, #118372, #201660, #120521, #20781, #186500, #38131, #85809, #55441, #17578, #53309, #119441, #117303, #37047, #68469, #52244, #21835, #19730, #87943, #152943, #70592, #149752, #154017, #1329, #5583, #133531, #199538, #51180, #34906, #137777, #183299, #184360, #100978, #167067, #35982, #102063, #168128, #155082, #72747, #156159, #158294, #25065, #192891, #92245, #7739, #190759, #58645, #173489, #204861, #73826, #41354, #9885, #139920, #124798, #10937, #91168, #74898, #138844, #90094, #106380, #141007, #27199, #174556, #40269, #22913, #205950, #188639, #108527, #56516, #57582, #77013, #171318, #159340, #26133, #143140, #105281, #75960, #209135, #142063, #208077, #89029, #6670, #107463, #122676, #42422, #59703, #207014, #123740, #175611, #60774, #125865, #157225, #8822, #191823, #172403, #189701, #43487, #93305, #126933, #45613, #62899, #80221, #146320, #46675, #212335, #112795, #35443, #79152, #111728, #97564, #48799, #95444, #117842, #177735, #128011, #78088, #161494, #61845, #193964, #162557, #85269, #29349, #113869, #101522, #13073, #129069, #145269, #44548, #28276, #178807, #211276, #195040, #94369, #68997, #30422, #96507, #63973 ) ),
 .UNSPECIFIED., .T., .F., .T. ) 
 B_SPLINE_SURFACE_WITH_KNOTS ( ( 4, 3, 4 ),
 ( 4, 1, 1, 1, 1, 1, 1, 1, 1, 1, 1, 1, 1, 1, 1, 1, 1, 1, 1, 1, 1, 1, 1, 1, 1, 1, 1, 1, 1, 1, 1, 1, 1, 1, 1, 1, 1, 1, 1, 1, 1, 1, 1, 1, 1, 1, 1, 1, 1, 1, 1, 1, 1, 1, 1, 1, 1, 1, 1, 1, 1, 1, 1, 1, 1, 1, 1, 1, 1, 1, 1, 1, 1, 1, 1, 1, 1, 1, 1, 1, 1, 1, 1, 1, 1, 1, 1, 1, 1, 1, 1, 1, 1, 1, 1, 1, 1, 1, 1, 1, 1, 1, 1, 1, 1, 1, 1, 1, 1, 1, 1, 1, 1, 1, 1, 1, 1, 1, 1, 1, 1, 1, 1, 1, 1, 1, 1, 1, 1, 1, 1, 1, 1, 1, 1, 1, 1, 1, 1, 1, 1, 1, 1, 1, 1, 1, 1, 1, 1, 1, 1, 1, 1, 1, 1, 1, 1, 1, 1, 1, 1, 1, 1, 1, 1, 1, 1, 1, 1, 1, 1, 1, 1, 1, 1, 1, 1, 1, 1, 1, 1, 1, 1, 1, 1, 1, 1, 1, 1, 1, 1, 1, 1, 1, 1, 1, 1, 1, 1, 1, 1, 1, 1, 1, 1, 1, 1, 1, 1, 1, 1, 1, 1, 1, 1, 1, 1, 1, 1, 1, 1, 1, 1, 1, 1, 1, 1, 1, 1, 1, 1, 1, 1, 1, 1, 1, 1, 1, 1, 1, 1, 1, 1, 1, 1, 1, 1, 1, 1, 1, 1, 1, 1, 1, 1, 1, 1, 1, 1, 1, 1, 1, 1, 1, 1, 1, 1, 1, 1, 1, 1, 1, 1, 1, 1, 1, 1, 1, 1, 1, 1, 1, 1, 1, 1, 1, 1, 1, 1, 1, 1, 1, 1, 1, 1, 1, 1, 1, 1, 1, 1, 1, 1, 1, 1, 1, 1, 1, 1, 1, 1, 1, 1, 1, 1, 1, 1, 1, 1, 1, 1, 1, 1, 1, 1, 1, 1, 1, 1, 1, 1, 1, 1, 1, 1, 1, 1, 1, 1, 1, 1, 1, 1, 1, 1, 1, 1, 1, 1, 1, 1, 1, 1, 1, 1, 1, 1, 1, 1, 1, 1, 1, 1, 1, 1, 1, 1, 1, 1, 1, 1, 1, 1, 1, 1, 1, 1, 1, 1, 1, 1, 1, 1, 1, 4 ),
 ( 0.000000000000000000, 0.5000000000000000000, 1.000000000000000000 ),
 ( 0.000000000000000000, 0.002600137934918278840, 0.005208846947063642402, 0.007813284371963545236, 0.01041597565644012714, 0.01302123463190214131, 0.01562472912267370319, 0.01822934229245065652, 0.02083335053635077330, 0.02343730581734793095, 0.02604195799539401474, 0.02864545692284610826, 0.03125045498156164142, 0.03385385361191795006, 0.03645873261014952182, 0.03906243010681619693, 0.04166674480109257978, 0.04427107247243720900, 0.04687475664952634596, 0.04947964045798968619, 0.05208303702386667122, 0.05468803228817373241, 0.05729153353077973132, 0.05989618223844375006, 0.06250015876865079589, 0.06510412050499821135, 0.06770877833268285073, 0.07031227041168378045, 0.07291726700687002627, 0.07552066596874357218, 0.07812554330212571896, 0.08072923942118487295, 0.08333355289058355653, 0.08593787945419822938, 0.08854156225015286097, 0.09114644488045960113, 0.09374984019314609729, 0.09635483420994474246, 0.09895833431534489799, 0.1015629817166532611, 0.1041669571688737805, 0.1067709175595765864, 0.1093755742645453749, 0.1119790650618166516, 0.1145840604711090005, 0.1171874582687142119, 0.1197923343547293018, 0.1223960294069747767, 0.1250003415701952669, 0.1276046670722256471, 0.1302083485727723866, 0.1328132300777099817, 0.1354166241949035232, 0.1380216170238739992, 0.1406251160503516617, 0.1432297622036773077, 0.1458337366370238142, 0.1484376957407889386, 0.1510423513813509144, 0.1536458409560605698, 0.1562508352375901466, 0.1588542319300798034, 0.1614591068269417562, 0.1640628008713490293, 0.1666671117869774343, 0.1692714362859856492, 0.1718751165501164191, 0.1744799969878772505, 0.1770833899687347668, 0.1796883816679979429, 0.1822918796746371972, 0.1848965246383280081, 0.1875004981115827030, 0.1901044559872153150, 0.1927091106216977379, 0.1953125990329364348, 0.1979175922448092595, 0.2005209878913200294, 0.2031258616572126918, 0.2057295547527302204, 0.2083338644793258920, 0.2109381880338489224, 0.2135418671205281671, 0.2161467465492790951, 0.2187501384529311477, 0.2213551290805818306, 0.2239586261264417955, 0.2265632699588193688, 0.2291672425307399730, 0.2317711992370185270, 0.2343758529237242316, 0.2369793402305566954, 0.2395843324308542799, 0.2421877270904984059, 0.2447925997835804779, 0.2473962919891333490, 0.2500006005852301039, 0.2526049232537817546, 0.2552086012219486610, 0.2578134796998332035, 0.2604168705853860954, 0.2630218601994954719, 0.2656253563436123954, 0.2682299991029740149, 0.2708339708322964334, 0.2734379264279751531, 0.2760425792251849364, 0.2786460654866522724, 0.2812510567334335909, 0.2838544504653006673, 0.2864593221437078951, 0.2890630135181997962, 0.2916673210423081364, 0.2942716428833813125, 0.2968753197919519748, 0.2994801973770923054, 0.3020835873036303854, 0.3046885759622478540, 0.3072920712636373342, 0.3098967130082584398, 0.3125006839536987324, 0.3151046384975096371, 0.3177092904634842285, 0.3203127757386058927, 0.3229177660899096303, 0.3255211589530693228, 0.3281260296749167193, 0.3307297202772326306, 0.3333340267878420748, 0.3359383478599109463, 0.3385420237677806976, 0.3411469005182800607, 0.3437502895448679152, 0.3463552773060237788, 0.3489587718236830116, 0.3515634126118191150, 0.3541673828320756612, 0.3567713363827305639, 0.3593759875757128741, 0.3619794719234893932, 0.3645844614373360826, 0.3671878534908398217, 0.3697927233142242476, 0.3723964132032320795, 0.3750007187588132451, 0.3776050391203355505, 0.3802087140863810166, 0.3828135900603256703, 0.3854169782460106219, 0.3880219651677176973, 0.3906254589606275029, 0.3932300988505167960, 0.3958340684042725433, 0.3984380210204655492, 0.4010426714986830565, 0.4036461549780977487, 0.4062511437124918245, 0.4088545350153757196, 0.4114594039983773821, 0.4140630932329303349, 0.4166673978919369636, 0.4192717176013560643, 0.4218753916844373286, 0.4244802669398990425, 0.4270836543437129262, 0.4296886404839689866, 0.4322921336110964741, 0.4348967726609613837, 0.4375007416068860122, 0.4401046933472957945, 0.4427093431689624881, 0.4453128258389836835, 0.4479178138519160357, 0.4505212044632024293, 0.4531260726638874359, 0.4557297613028266636, 0.4583340651236982866, 0.4609383842394453867, 0.4635420574984087105, 0.4661469320934465421, 0.4687503187744080368, 0.4713553041911981989, 0.4739587967114984313, 0.4765634349795482838, 0.4791674033763006491, 0.4817713542995921694, 0.4843760035229108252, 0.4869794854424946973, 0.4895844727919445583, 0.4921878627706443576, 0.4947927302470669919, 0.4973964183492232127, 0.5000007213903868708, 0.5026050399708832384, 0.5052087124645624483, 0.5078135864572254077, 0.5104169724743423675, 0.5130219572256408123, 0.5156254491980594157, 0.5182300867424926016, 0.5208340546487225664, 0.5234380048135498509, 0.5260426534967141965, 0.5286461347248060383, 0.5312511214687432037, 0.5338545108738584899, 0.5364593776840630435, 0.5390630653082590928, 0.5416673676281316130, 0.5442716857317909662, 0.5468753575190105076, 0.5494802309673390006, 0.5520836163796108975, 0.5546886005233833128, 0.5572920920068584749, 0.5598967288858642810, 0.5625006963602153798, 0.5651046458252231286, 0.5677092940264200083, 0.5703127746219572858, 0.5729177608183441128, 0.5755211497088699169, 0.5781260159108934094, 0.5807297031159460721, 0.5833340047729366207, 0.5859383224581667937, 0.5885419935977430628, 0.5911468665597719996, 0.5937502514261915332, 0.5963552350203973340, 0.5989587260738620245, 0.6015633623456233536, 0.6041673294467342359, 0.6067712782705607655, 0.6093759260479724160, 0.6119794060698863225, 0.6145843917766802278, 0.6171877802116071399, 0.6197926458634805957, 0.6223963327082033814, 0.6250006337607152407, 0.6276049510859208480, 0.6302086216366651339, 0.6328134941704254279, 0.6354168785499811900, 0.6380218616525755726, 0.6406253523349600965, 0.6432299880576550777, 0.6458339548441623945, 0.6484379030854412473, 0.6510425504972472410, 0.6536460300044655281, 0.6562510152796211527, 0.6588544033179367654, 0.6614592684776883225, 0.6640629550208935195, 0.6666672555273263079, 0.6692715725509107427, 0.6718752425716313370, 0.6744801147351520143, 0.6770834986868305982, 0.6796884813557668714, 0.6822919717260003125, 0.6848966069578048543, 0.6875005734883452568, 0.6901045212057073108, 0.6927091683100871089, 0.6953126473615357517, 0.6979176322630067375, 0.7005210199636988655, 0.7031258846893556624, 0.7057295709898557812, 0.7083338710086078960, 0.7109381877889758838, 0.7135418573384794128, 0.7161467291897904985, 0.7187501127725786088, 0.7213550950658099703, 0.7239585851828231888, 0.7265632199819130888, 0.7291671863151253374, 0.7317711335672014705, 0.7343757804223364216, 0.7369792590769420615, 0.7395842436626837157, 0.7421876310847422831, 0.7447924954343322357, 0.7473961815509432283, 0.7500004811404139549, 0.7526047977359727748, 0.7552084668730677519, 0.7578133384702019359, 0.7604167217430886083, 0.7630217037185706985, 0.7656251936412983294, 0.7682298280658512724, 0.7708337942603785686, 0.7734377411058018792, 0.7760423877698768846, 0.7786458660865690495, 0.7812508504145402322, 0.7838542376169586046, 0.7864591016485131814, 0.7890627876400562180, 0.7916670868586475063, 0.7942714033278103214, 0.7968750721113085911, 0.7994799435123028930, 0.8020833265342820484, 0.8046883082499752815, 0.8072917980373575109, 0.8098964321455554005, 0.8125003982600473851, 0.8151043447574546352, 0.8177089912886614798, 0.8203124693263749156, 0.8229174534545398156, 0.8255208404963184643, 0.8281257042678743518, 0.8307293901931780411, 0.8333336890992975032, 0.8359380055004849153, 0.8385416739892034288, 0.8411465452521027508, 0.8437499280821748604, 0.8463549095960458679, 0.8489583993070312085, 0.8515630331570626099, 0.8541669992501779163, 0.8567709454582125295, 0.8593755919147509914, 0.8619790697324273276, 0.8645840537187589048, 0.8671874406589066275, 0.8697923042285079509, 0.8723959901464106714, 0.8750002887984731359, 0.8776046051901155165, 0.8802082734428797739, 0.8828131446257380111, 0.8854165273229123168, 0.8880215086929368340, 0.8906249983864840125, 0.8932296320365455955, 0.8958335981669537373, 0.8984375441442679078, 0.9010421905843485346, 0.9036456682409392815, 0.9062506521434200435, 0.9088540390409564074, 0.9114589024666573946, 0.9140625884360091824, 0.9166668868924389146, 0.9192712033329777377, 0.9218748714086243412, 0.9244797425695093773, 0.9270831251927963423, 0.9296881064769593195, 0.9322915962120889022, 0.9348962297203436966, 0.9375001959466012780, 0.9401041417521586174, 0.9427087882339971747, 0.9453122657876905643, 0.9479172496658602176, 0.9505206365780075606, 0.9531254999124115779, 0.9557291860198475764, 0.9583334843266348990, 0.9609378007344983041, 0.9635414689593263526, 0.9661463405142474148, 0.9687497214891268582, 0.9713547029754164841, 0.9739581985331400293, 0.9765628250748574768, 0.9791667834374845336, 0.9817707607320566021, 0.9843753697534296521, 0.9869788348889786400, 0.9895840831931937975, 0.9921867700316038263, 0.9947911815772807476, 0.9973998924267860611, 1.000000000000000000 ),
 .UNSPECIFIED. ) 
 GEOMETRIC_REPRESENTATION_ITEM ( )  RATIONAL_B_SPLINE_SURFACE ( (
 ( 1.000000000000000000, 1.000000000000000000, 1.000000000000000000, 1.000000000000000222, 0.9999999999999996669, 1.000000000000000222, 0.9999999999999997780, 1.000000000000000000, 0.9999999999999997780, 1.000000000000000444, 1.000000000000000000, 0.9999999999999997780, 1.000000000000000222, 1.000000000000000000, 0.9999999999999997780, 1.000000000000000222, 0.9999999999999996669, 1.000000000000000000, 1.000000000000000222, 1.000000000000000000, 1.000000000000000000, 1.000000000000000444, 0.9999999999999994449, 1.000000000000000444, 0.9999999999999996669, 1.000000000000000222, 1.000000000000000000, 1.000000000000000444, 1.000000000000000000, 0.9999999999999997780, 1.000000000000000000, 1.000000000000000222, 0.9999999999999997780, 0.9999999999999997780, 1.000000000000000444, 0.9999999999999997780, 1.000000000000000444, 1.000000000000000222, 0.9999999999999996669, 1.000000000000000222, 1.000000000000000000, 1.000000000000000444, 0.9999999999999997780, 1.000000000000000222, 1.000000000000000222, 1.000000000000000222, 0.9999999999999997780, 1.000000000000000000, 1.000000000000000000, 1.000000000000000000, 0.9999999999999994449, 1.000000000000000444, 0.9999999999999997780, 1.000000000000000444, 0.9999999999999997780, 1.000000000000000000, 1.000000000000000000, 0.9999999999999997780, 1.000000000000000444, 0.9999999999999996669, 1.000000000000000444, 0.9999999999999996669, 1.000000000000000222, 0.9999999999999994449, 1.000000000000000222, 1.000000000000000000, 1.000000000000000000, 1.000000000000000000, 1.000000000000000000, 1.000000000000000222, 1.000000000000000000, 1.000000000000000222, 0.9999999999999996669, 1.000000000000000222, 1.000000000000000000, 1.000000000000000444, 1.000000000000000000, 1.000000000000000000, 0.9999999999999997780, 1.000000000000000222, 0.9999999999999997780, 0.9999999999999997780, 1.000000000000000444, 1.000000000000000000, 1.000000000000000222, 0.9999999999999996669, 1.000000000000000444, 0.9999999999999997780, 1.000000000000000222, 0.9999999999999997780, 1.000000000000000222, 1.000000000000000000, 1.000000000000000000, 1.000000000000000000, 1.000000000000000000, 1.000000000000000222, 1.000000000000000222, 0.9999999999999997780, 1.000000000000000222, 1.000000000000000000, 1.000000000000000222, 0.9999999999999997780, 1.000000000000000222, 1.000000000000000000, 1.000000000000000000, 0.9999999999999997780, 1.000000000000000000, 1.000000000000000000, 0.9999999999999997780, 1.000000000000000222, 0.9999999999999997780, 1.000000000000000222, 0.9999999999999997780, 1.000000000000000444, 1.000000000000000000, 0.9999999999999996669, 1.000000000000000444, 1.000000000000000000, 0.9999999999999997780, 1.000000000000000000, 0.9999999999999996669, 1.000000000000000000, 1.000000000000000222, 0.9999999999999996669, 1.000000000000000222, 0.9999999999999997780, 1.000000000000000000, 1.000000000000000222, 0.9999999999999997780, 1.000000000000000222, 0.9999999999999997780, 1.000000000000000222, 1.000000000000000000, 1.000000000000000000, 1.000000000000000000, 0.9999999999999997780, 1.000000000000000222, 0.9999999999999997780, 1.000000000000000222, 1.000000000000000000, 1.000000000000000000, 1.000000000000000000, 1.000000000000000000, 1.000000000000000444, 0.9999999999999997780, 1.000000000000000444, 0.9999999999999997780, 1.000000000000000222, 1.000000000000000000, 1.000000000000000000, 1.000000000000000000, 1.000000000000000000, 0.9999999999999997780, 1.000000000000000000, 1.000000000000000222, 0.9999999999999997780, 1.000000000000000222, 1.000000000000000000, 1.000000000000000000, 1.000000000000000222, 0.9999999999999997780, 1.000000000000000222, 0.9999999999999996669, 1.000000000000000444, 0.9999999999999994449, 1.000000000000000444, 0.9999999999999997780, 0.9999999999999997780, 1.000000000000000000, 1.000000000000000000, 1.000000000000000222, 1.000000000000000000, 1.000000000000000000, 1.000000000000000000, 1.000000000000000000, 1.000000000000000222, 1.000000000000000444, 0.9999999999999997780, 1.000000000000000222, 1.000000000000000000, 0.9999999999999996669, 1.000000000000000222, 1.000000000000000222, 1.000000000000000222, 1.000000000000000222, 1.000000000000000000, 1.000000000000000000, 1.000000000000000222, 1.000000000000000000, 1.000000000000000222, 1.000000000000000000, 1.000000000000000000, 1.000000000000000000, 1.000000000000000222, 0.9999999999999997780, 1.000000000000000000, 1.000000000000000222, 1.000000000000000000, 1.000000000000000222, 1.000000000000000000, 0.9999999999999997780, 1.000000000000000444, 1.000000000000000000, 0.9999999999999996669, 1.000000000000000222, 0.9999999999999997780, 1.000000000000000222, 1.000000000000000000, 1.000000000000000000, 1.000000000000000444, 0.9999999999999996669, 1.000000000000000000, 0.9999999999999997780, 1.000000000000000000, 0.9999999999999997780, 0.9999999999999997780, 1.000000000000000000, 1.000000000000000000, 1.000000000000000000, 0.9999999999999997780, 1.000000000000000000, 1.000000000000000222, 1.000000000000000222, 1.000000000000000000, 0.9999999999999997780, 1.000000000000000222, 1.000000000000000000, 1.000000000000000000, 1.000000000000000222, 1.000000000000000222, 1.000000000000000222, 1.000000000000000000, 0.9999999999999997780, 1.000000000000000444, 0.9999999999999997780, 1.000000000000000444, 0.9999999999999997780, 1.000000000000000000, 1.000000000000000222, 0.9999999999999997780, 1.000000000000000222, 0.9999999999999997780, 1.000000000000000222, 0.9999999999999997780, 1.000000000000000222, 0.9999999999999996669, 1.000000000000000222, 0.9999999999999997780, 1.000000000000000444, 1.000000000000000000, 1.000000000000000000, 0.9999999999999997780, 1.000000000000000222, 1.000000000000000000, 0.9999999999999996669, 1.000000000000000222, 0.9999999999999997780, 1.000000000000000000, 1.000000000000000222, 1.000000000000000000, 1.000000000000000222, 0.9999999999999996669, 1.000000000000000444, 0.9999999999999996669, 1.000000000000000000, 1.000000000000000000, 1.000000000000000000, 0.9999999999999997780, 1.000000000000000444, 1.000000000000000000, 1.000000000000000000, 1.000000000000000000, 1.000000000000000000, 0.9999999999999997780, 1.000000000000000222, 1.000000000000000222, 1.000000000000000222, 1.000000000000000000, 1.000000000000000222, 1.000000000000000000, 0.9999999999999997780, 1.000000000000000444, 1.000000000000000000, 0.9999999999999997780, 1.000000000000000222, 0.9999999999999996669, 1.000000000000000222, 1.000000000000000000, 1.000000000000000444, 1.000000000000000222, 0.9999999999999996669, 1.000000000000000222, 0.9999999999999997780, 1.000000000000000222, 1.000000000000000222, 0.9999999999999997780, 1.000000000000000222, 1.000000000000000000, 1.000000000000000222, 1.000000000000000222, 0.9999999999999997780, 1.000000000000000444, 0.9999999999999996669, 1.000000000000000222, 1.000000000000000222, 1.000000000000000000, 1.000000000000000000, 1.000000000000000000, 1.000000000000000222, 1.000000000000000000, 1.000000000000000000, 1.000000000000000222, 0.9999999999999996669, 1.000000000000000444, 1.000000000000000222, 0.9999999999999997780, 1.000000000000000222, 0.9999999999999997780, 1.000000000000000444, 0.9999999999999996669, 1.000000000000000666, 0.9999999999999994449, 1.000000000000000222, 0.9999999999999997780, 1.000000000000000444, 1.000000000000000000, 1.000000000000000222, 1.000000000000000222, 1.000000000000000000, 0.9999999999999997780, 0.9999999999999997780, 1.000000000000000444, 1.000000000000000000, 1.000000000000000000, 1.000000000000000000, 0.9999999999999997780, 1.000000000000000222, 1.000000000000000222, 0.9999999999999997780, 1.000000000000000222, 1.000000000000000000, 1.000000000000000444, 0.9999999999999996669, 1.000000000000000444, 0.9999999999999997780, 1.000000000000000000, 0.9999999999999997780, 1.000000000000000444, 0.9999999999999996669, 1.000000000000000444, 1.000000000000000000, 1.000000000000000000, 1.000000000000000000, 0.9999999999999997780, 1.000000000000000444, 1.000000000000000222, 0.9999999999999997780, 1.000000000000000444, 1.000000000000000000, 0.9999999999999996669, 1.000000000000000444, 1.000000000000000000, 1.000000000000000000, 1.000000000000000000, 0.9999999999999997780, 1.000000000000000222, 0.9999999999999997780, 1.000000000000000000, 1.000000000000000222, 0.9999999999999997780, 1.000000000000000000, 1.000000000000000000, 0.9999999999999997780, 1.000000000000000444, 0.9999999999999997780, 1.000000000000000444, 0.9999999999999994449, 1.000000000000000444, 0.9999999999999997780, 1.000000000000000444, 0.9999999999999997780, 1.000000000000000000, 0.9999999999999997780, 1.000000000000000222, 1.000000000000000222, 1.000000000000000000, 1.000000000000000000),
 ( 0.3333333333333333703, 0.3333333333333333703, 0.3333333333333333703, 0.3333333333333335369, 0.3333333333333333148, 0.3333333333333333703, 0.3333333333333333703, 0.3333333333333333148, 0.3333333333333333148, 0.3333333333333334259, 0.3333333333333333703, 0.3333333333333333148, 0.3333333333333334259, 0.3333333333333333148, 0.3333333333333334259, 0.3333333333333333148, 0.3333333333333333703, 0.3333333333333333148, 0.3333333333333334814, 0.3333333333333333148, 0.3333333333333334814, 0.3333333333333334814, 0.3333333333333333148, 0.3333333333333334259, 0.3333333333333333148, 0.3333333333333333703, 0.3333333333333333148, 0.3333333333333334814, 0.3333333333333333703, 0.3333333333333333703, 0.3333333333333333703, 0.3333333333333334259, 0.3333333333333333148, 0.3333333333333333148, 0.3333333333333334259, 0.3333333333333333703, 0.3333333333333334259, 0.3333333333333334259, 0.3333333333333332038, 0.3333333333333334814, 0.3333333333333333703, 0.3333333333333334814, 0.3333333333333332593, 0.3333333333333334259, 0.3333333333333333703, 0.3333333333333334259, 0.3333333333333333148, 0.3333333333333333703, 0.3333333333333334259, 0.3333333333333333148, 0.3333333333333332038, 0.3333333333333335369, 0.3333333333333332593, 0.3333333333333334814, 0.3333333333333333148, 0.3333333333333333703, 0.3333333333333334259, 0.3333333333333333703, 0.3333333333333334814, 0.3333333333333333703, 0.3333333333333334259, 0.3333333333333333148, 0.3333333333333334814, 0.3333333333333332038, 0.3333333333333334259, 0.3333333333333333148, 0.3333333333333333703, 0.3333333333333333703, 0.3333333333333334259, 0.3333333333333333148, 0.3333333333333333703, 0.3333333333333334259, 0.3333333333333333148, 0.3333333333333333703, 0.3333333333333333703, 0.3333333333333335369, 0.3333333333333333148, 0.3333333333333333703, 0.3333333333333333703, 0.3333333333333333703, 0.3333333333333333148, 0.3333333333333333703, 0.3333333333333334814, 0.3333333333333333148, 0.3333333333333334814, 0.3333333333333333703, 0.3333333333333334259, 0.3333333333333333148, 0.3333333333333334259, 0.3333333333333333148, 0.3333333333333334259, 0.3333333333333333148, 0.3333333333333333703, 0.3333333333333333703, 0.3333333333333333703, 0.3333333333333334259, 0.3333333333333334259, 0.3333333333333332593, 0.3333333333333334259, 0.3333333333333333703, 0.3333333333333334259, 0.3333333333333333148, 0.3333333333333334259, 0.3333333333333333703, 0.3333333333333333703, 0.3333333333333333148, 0.3333333333333334259, 0.3333333333333333703, 0.3333333333333333148, 0.3333333333333334259, 0.3333333333333332038, 0.3333333333333334814, 0.3333333333333333148, 0.3333333333333335369, 0.3333333333333334259, 0.3333333333333332038, 0.3333333333333334814, 0.3333333333333333703, 0.3333333333333332593, 0.3333333333333333703, 0.3333333333333332593, 0.3333333333333333703, 0.3333333333333334814, 0.3333333333333333148, 0.3333333333333334814, 0.3333333333333333148, 0.3333333333333334259, 0.3333333333333334259, 0.3333333333333333148, 0.3333333333333334259, 0.3333333333333333148, 0.3333333333333334259, 0.3333333333333333703, 0.3333333333333333703, 0.3333333333333334259, 0.3333333333333332593, 0.3333333333333334814, 0.3333333333333333148, 0.3333333333333333703, 0.3333333333333333703, 0.3333333333333333703, 0.3333333333333334259, 0.3333333333333334259, 0.3333333333333334814, 0.3333333333333333703, 0.3333333333333334259, 0.3333333333333333703, 0.3333333333333333703, 0.3333333333333333148, 0.3333333333333333703, 0.3333333333333334259, 0.3333333333333333148, 0.3333333333333333148, 0.3333333333333333148, 0.3333333333333334259, 0.3333333333333333148, 0.3333333333333334814, 0.3333333333333333148, 0.3333333333333334259, 0.3333333333333334259, 0.3333333333333333148, 0.3333333333333334814, 0.3333333333333333148, 0.3333333333333334814, 0.3333333333333332593, 0.3333333333333335369, 0.3333333333333333148, 0.3333333333333333703, 0.3333333333333333703, 0.3333333333333334259, 0.3333333333333333703, 0.3333333333333333703, 0.3333333333333333148, 0.3333333333333333703, 0.3333333333333332593, 0.3333333333333335369, 0.3333333333333334259, 0.3333333333333333703, 0.3333333333333334259, 0.3333333333333334259, 0.3333333333333332038, 0.3333333333333334814, 0.3333333333333333703, 0.3333333333333334259, 0.3333333333333333703, 0.3333333333333333703, 0.3333333333333333148, 0.3333333333333334814, 0.3333333333333333148, 0.3333333333333334814, 0.3333333333333334259, 0.3333333333333333148, 0.3333333333333333703, 0.3333333333333333703, 0.3333333333333333703, 0.3333333333333333703, 0.3333333333333334259, 0.3333333333333333148, 0.3333333333333334814, 0.3333333333333333148, 0.3333333333333333703, 0.3333333333333334814, 0.3333333333333332593, 0.3333333333333333148, 0.3333333333333334259, 0.3333333333333332593, 0.3333333333333335369, 0.3333333333333333703, 0.3333333333333334259, 0.3333333333333335369, 0.3333333333333333148, 0.3333333333333333703, 0.3333333333333333148, 0.3333333333333333703, 0.3333333333333333148, 0.3333333333333333148, 0.3333333333333333703, 0.3333333333333333703, 0.3333333333333333703, 0.3333333333333333148, 0.3333333333333333703, 0.3333333333333333703, 0.3333333333333334259, 0.3333333333333333703, 0.3333333333333333148, 0.3333333333333333703, 0.3333333333333333703, 0.3333333333333333703, 0.3333333333333334259, 0.3333333333333334259, 0.3333333333333334814, 0.3333333333333332593, 0.3333333333333334259, 0.3333333333333334259, 0.3333333333333333148, 0.3333333333333334259, 0.3333333333333333703, 0.3333333333333333148, 0.3333333333333334814, 0.3333333333333333703, 0.3333333333333334259, 0.3333333333333332593, 0.3333333333333334259, 0.3333333333333332593, 0.3333333333333334814, 0.3333333333333332593, 0.3333333333333334259, 0.3333333333333333148, 0.3333333333333334259, 0.3333333333333333703, 0.3333333333333334259, 0.3333333333333333703, 0.3333333333333333703, 0.3333333333333333703, 0.3333333333333333148, 0.3333333333333334259, 0.3333333333333333703, 0.3333333333333333148, 0.3333333333333334259, 0.3333333333333333148, 0.3333333333333333703, 0.3333333333333333148, 0.3333333333333334814, 0.3333333333333332593, 0.3333333333333333703, 0.3333333333333333703, 0.3333333333333334259, 0.3333333333333332593, 0.3333333333333335369, 0.3333333333333333703, 0.3333333333333333703, 0.3333333333333333703, 0.3333333333333333148, 0.3333333333333333148, 0.3333333333333334259, 0.3333333333333334814, 0.3333333333333334259, 0.3333333333333333703, 0.3333333333333334259, 0.3333333333333334259, 0.3333333333333333703, 0.3333333333333334814, 0.3333333333333333148, 0.3333333333333333148, 0.3333333333333334259, 0.3333333333333332038, 0.3333333333333334814, 0.3333333333333333148, 0.3333333333333335369, 0.3333333333333334259, 0.3333333333333333148, 0.3333333333333334814, 0.3333333333333333703, 0.3333333333333333703, 0.3333333333333334259, 0.3333333333333333703, 0.3333333333333334259, 0.3333333333333333703, 0.3333333333333334259, 0.3333333333333333148, 0.3333333333333333703, 0.3333333333333335369, 0.3333333333333332038, 0.3333333333333334814, 0.3333333333333333703, 0.3333333333333333148, 0.3333333333333334259, 0.3333333333333333703, 0.3333333333333333148, 0.3333333333333334259, 0.3333333333333333703, 0.3333333333333334259, 0.3333333333333332593, 0.3333333333333335369, 0.3333333333333334814, 0.3333333333333333148, 0.3333333333333334259, 0.3333333333333333148, 0.3333333333333335369, 0.3333333333333332593, 0.3333333333333335924, 0.3333333333333332593, 0.3333333333333333703, 0.3333333333333333703, 0.3333333333333334814, 0.3333333333333333703, 0.3333333333333334814, 0.3333333333333333703, 0.3333333333333334259, 0.3333333333333332593, 0.3333333333333334259, 0.3333333333333335369, 0.3333333333333333148, 0.3333333333333334814, 0.3333333333333333148, 0.3333333333333333703, 0.3333333333333334259, 0.3333333333333334259, 0.3333333333333332593, 0.3333333333333334259, 0.3333333333333333148, 0.3333333333333335369, 0.3333333333333332593, 0.3333333333333335369, 0.3333333333333333148, 0.3333333333333333148, 0.3333333333333333703, 0.3333333333333334814, 0.3333333333333333148, 0.3333333333333334259, 0.3333333333333333148, 0.3333333333333334259, 0.3333333333333333703, 0.3333333333333333148, 0.3333333333333334259, 0.3333333333333334814, 0.3333333333333333148, 0.3333333333333334814, 0.3333333333333333703, 0.3333333333333332593, 0.3333333333333334259, 0.3333333333333333703, 0.3333333333333334259, 0.3333333333333333703, 0.3333333333333333148, 0.3333333333333334259, 0.3333333333333333703, 0.3333333333333333148, 0.3333333333333334259, 0.3333333333333333148, 0.3333333333333333148, 0.3333333333333333703, 0.3333333333333333703, 0.3333333333333334259, 0.3333333333333333148, 0.3333333333333334259, 0.3333333333333332593, 0.3333333333333334259, 0.3333333333333333703, 0.3333333333333334259, 0.3333333333333333703, 0.3333333333333333703, 0.3333333333333333148, 0.3333333333333334814, 0.3333333333333334259, 0.3333333333333333703, 0.3333333333333333703),
 ( 0.3333333333333333703, 0.3333333333333333703, 0.3333333333333333703, 0.3333333333333335369, 0.3333333333333333148, 0.3333333333333333703, 0.3333333333333333703, 0.3333333333333333148, 0.3333333333333333148, 0.3333333333333334259, 0.3333333333333333703, 0.3333333333333333148, 0.3333333333333334259, 0.3333333333333333148, 0.3333333333333334259, 0.3333333333333333148, 0.3333333333333333703, 0.3333333333333333148, 0.3333333333333334814, 0.3333333333333333148, 0.3333333333333334814, 0.3333333333333334814, 0.3333333333333333148, 0.3333333333333334259, 0.3333333333333333148, 0.3333333333333333703, 0.3333333333333333148, 0.3333333333333334814, 0.3333333333333333703, 0.3333333333333333703, 0.3333333333333333703, 0.3333333333333334259, 0.3333333333333333148, 0.3333333333333333148, 0.3333333333333334259, 0.3333333333333333703, 0.3333333333333334259, 0.3333333333333334259, 0.3333333333333332038, 0.3333333333333334814, 0.3333333333333333703, 0.3333333333333334814, 0.3333333333333332593, 0.3333333333333334259, 0.3333333333333333703, 0.3333333333333334259, 0.3333333333333333148, 0.3333333333333333703, 0.3333333333333334259, 0.3333333333333333148, 0.3333333333333332038, 0.3333333333333335369, 0.3333333333333332593, 0.3333333333333334814, 0.3333333333333333148, 0.3333333333333333703, 0.3333333333333334259, 0.3333333333333333703, 0.3333333333333334814, 0.3333333333333333703, 0.3333333333333334259, 0.3333333333333333148, 0.3333333333333334814, 0.3333333333333332038, 0.3333333333333334259, 0.3333333333333333148, 0.3333333333333333703, 0.3333333333333333703, 0.3333333333333334259, 0.3333333333333333148, 0.3333333333333333703, 0.3333333333333334259, 0.3333333333333333148, 0.3333333333333333703, 0.3333333333333333703, 0.3333333333333335369, 0.3333333333333333148, 0.3333333333333333703, 0.3333333333333333703, 0.3333333333333333703, 0.3333333333333333148, 0.3333333333333333703, 0.3333333333333334814, 0.3333333333333333148, 0.3333333333333334814, 0.3333333333333333703, 0.3333333333333334259, 0.3333333333333333148, 0.3333333333333334259, 0.3333333333333333148, 0.3333333333333334259, 0.3333333333333333148, 0.3333333333333333703, 0.3333333333333333703, 0.3333333333333333703, 0.3333333333333334259, 0.3333333333333334259, 0.3333333333333332593, 0.3333333333333334259, 0.3333333333333333703, 0.3333333333333334259, 0.3333333333333333148, 0.3333333333333334259, 0.3333333333333333703, 0.3333333333333333703, 0.3333333333333333148, 0.3333333333333334259, 0.3333333333333333703, 0.3333333333333333148, 0.3333333333333334259, 0.3333333333333332038, 0.3333333333333334814, 0.3333333333333333148, 0.3333333333333335369, 0.3333333333333334259, 0.3333333333333332038, 0.3333333333333334814, 0.3333333333333333703, 0.3333333333333332593, 0.3333333333333333703, 0.3333333333333332593, 0.3333333333333333703, 0.3333333333333334814, 0.3333333333333333148, 0.3333333333333334814, 0.3333333333333333148, 0.3333333333333334259, 0.3333333333333334259, 0.3333333333333333148, 0.3333333333333334259, 0.3333333333333333148, 0.3333333333333334259, 0.3333333333333333703, 0.3333333333333333703, 0.3333333333333334259, 0.3333333333333332593, 0.3333333333333334814, 0.3333333333333333148, 0.3333333333333333703, 0.3333333333333333703, 0.3333333333333333703, 0.3333333333333334259, 0.3333333333333334259, 0.3333333333333334814, 0.3333333333333333703, 0.3333333333333334259, 0.3333333333333333703, 0.3333333333333333703, 0.3333333333333333148, 0.3333333333333333703, 0.3333333333333334259, 0.3333333333333333148, 0.3333333333333333148, 0.3333333333333333148, 0.3333333333333334259, 0.3333333333333333148, 0.3333333333333334814, 0.3333333333333333148, 0.3333333333333334259, 0.3333333333333334259, 0.3333333333333333148, 0.3333333333333334814, 0.3333333333333333148, 0.3333333333333334814, 0.3333333333333332593, 0.3333333333333335369, 0.3333333333333333148, 0.3333333333333333703, 0.3333333333333333703, 0.3333333333333334259, 0.3333333333333333703, 0.3333333333333333703, 0.3333333333333333148, 0.3333333333333333703, 0.3333333333333332593, 0.3333333333333335369, 0.3333333333333334259, 0.3333333333333333703, 0.3333333333333334259, 0.3333333333333334259, 0.3333333333333332038, 0.3333333333333334814, 0.3333333333333333703, 0.3333333333333334259, 0.3333333333333333703, 0.3333333333333333703, 0.3333333333333333148, 0.3333333333333334814, 0.3333333333333333148, 0.3333333333333334814, 0.3333333333333334259, 0.3333333333333333148, 0.3333333333333333703, 0.3333333333333333703, 0.3333333333333333703, 0.3333333333333333703, 0.3333333333333334259, 0.3333333333333333148, 0.3333333333333334814, 0.3333333333333333148, 0.3333333333333333703, 0.3333333333333334814, 0.3333333333333332593, 0.3333333333333333148, 0.3333333333333334259, 0.3333333333333332593, 0.3333333333333335369, 0.3333333333333333703, 0.3333333333333334259, 0.3333333333333335369, 0.3333333333333333148, 0.3333333333333333703, 0.3333333333333333148, 0.3333333333333333703, 0.3333333333333333148, 0.3333333333333333148, 0.3333333333333333703, 0.3333333333333333703, 0.3333333333333333703, 0.3333333333333333148, 0.3333333333333333703, 0.3333333333333333703, 0.3333333333333334259, 0.3333333333333333703, 0.3333333333333333148, 0.3333333333333333703, 0.3333333333333333703, 0.3333333333333333703, 0.3333333333333334259, 0.3333333333333334259, 0.3333333333333334814, 0.3333333333333332593, 0.3333333333333334259, 0.3333333333333334259, 0.3333333333333333148, 0.3333333333333334259, 0.3333333333333333703, 0.3333333333333333148, 0.3333333333333334814, 0.3333333333333333703, 0.3333333333333334259, 0.3333333333333332593, 0.3333333333333334259, 0.3333333333333332593, 0.3333333333333334814, 0.3333333333333332593, 0.3333333333333334259, 0.3333333333333333148, 0.3333333333333334259, 0.3333333333333333703, 0.3333333333333334259, 0.3333333333333333703, 0.3333333333333333703, 0.3333333333333333703, 0.3333333333333333148, 0.3333333333333334259, 0.3333333333333333703, 0.3333333333333333148, 0.3333333333333334259, 0.3333333333333333148, 0.3333333333333333703, 0.3333333333333333148, 0.3333333333333334814, 0.3333333333333332593, 0.3333333333333333703, 0.3333333333333333703, 0.3333333333333334259, 0.3333333333333332593, 0.3333333333333335369, 0.3333333333333333703, 0.3333333333333333703, 0.3333333333333333703, 0.3333333333333333148, 0.3333333333333333148, 0.3333333333333334259, 0.3333333333333334814, 0.3333333333333334259, 0.3333333333333333703, 0.3333333333333334259, 0.3333333333333334259, 0.3333333333333333703, 0.3333333333333334814, 0.3333333333333333148, 0.3333333333333333148, 0.3333333333333334259, 0.3333333333333332038, 0.3333333333333334814, 0.3333333333333333148, 0.3333333333333335369, 0.3333333333333334259, 0.3333333333333333148, 0.3333333333333334814, 0.3333333333333333703, 0.3333333333333333703, 0.3333333333333334259, 0.3333333333333333703, 0.3333333333333334259, 0.3333333333333333703, 0.3333333333333334259, 0.3333333333333333148, 0.3333333333333333703, 0.3333333333333335369, 0.3333333333333332038, 0.3333333333333334814, 0.3333333333333333703, 0.3333333333333333148, 0.3333333333333334259, 0.3333333333333333703, 0.3333333333333333148, 0.3333333333333334259, 0.3333333333333333703, 0.3333333333333334259, 0.3333333333333332593, 0.3333333333333335369, 0.3333333333333334814, 0.3333333333333333148, 0.3333333333333334259, 0.3333333333333333148, 0.3333333333333335369, 0.3333333333333332593, 0.3333333333333335924, 0.3333333333333332593, 0.3333333333333333703, 0.3333333333333333703, 0.3333333333333334814, 0.3333333333333333703, 0.3333333333333334814, 0.3333333333333333703, 0.3333333333333334259, 0.3333333333333332593, 0.3333333333333334259, 0.3333333333333335369, 0.3333333333333333148, 0.3333333333333334814, 0.3333333333333333148, 0.3333333333333333703, 0.3333333333333334259, 0.3333333333333334259, 0.3333333333333332593, 0.3333333333333334259, 0.3333333333333333148, 0.3333333333333335369, 0.3333333333333332593, 0.3333333333333335369, 0.3333333333333333148, 0.3333333333333333148, 0.3333333333333333703, 0.3333333333333334814, 0.3333333333333333148, 0.3333333333333334259, 0.3333333333333333148, 0.3333333333333334259, 0.3333333333333333703, 0.3333333333333333148, 0.3333333333333334259, 0.3333333333333334814, 0.3333333333333333148, 0.3333333333333334814, 0.3333333333333333703, 0.3333333333333332593, 0.3333333333333334259, 0.3333333333333333703, 0.3333333333333334259, 0.3333333333333333703, 0.3333333333333333148, 0.3333333333333334259, 0.3333333333333333703, 0.3333333333333333148, 0.3333333333333334259, 0.3333333333333333148, 0.3333333333333333148, 0.3333333333333333703, 0.3333333333333333703, 0.3333333333333334259, 0.3333333333333333148, 0.3333333333333334259, 0.3333333333333332593, 0.3333333333333334259, 0.3333333333333333703, 0.3333333333333334259, 0.3333333333333333703, 0.3333333333333333703, 0.3333333333333333148, 0.3333333333333334814, 0.3333333333333334259, 0.3333333333333333703, 0.3333333333333333703),
 ( 1.000000000000000000, 1.000000000000000000, 1.000000000000000000, 1.000000000000000222, 0.9999999999999996669, 1.000000000000000222, 0.9999999999999997780, 1.000000000000000000, 0.9999999999999997780, 1.000000000000000444, 1.000000000000000000, 0.9999999999999997780, 1.000000000000000222, 1.000000000000000000, 0.9999999999999997780, 1.000000000000000222, 0.9999999999999996669, 1.000000000000000000, 1.000000000000000222, 1.000000000000000000, 1.000000000000000000, 1.000000000000000444, 0.9999999999999994449, 1.000000000000000444, 0.9999999999999996669, 1.000000000000000222, 1.000000000000000000, 1.000000000000000444, 1.000000000000000000, 0.9999999999999997780, 1.000000000000000000, 1.000000000000000222, 0.9999999999999997780, 0.9999999999999997780, 1.000000000000000444, 0.9999999999999997780, 1.000000000000000444, 1.000000000000000222, 0.9999999999999996669, 1.000000000000000222, 1.000000000000000000, 1.000000000000000444, 0.9999999999999997780, 1.000000000000000222, 1.000000000000000222, 1.000000000000000222, 0.9999999999999997780, 1.000000000000000000, 1.000000000000000000, 1.000000000000000000, 0.9999999999999994449, 1.000000000000000444, 0.9999999999999997780, 1.000000000000000444, 0.9999999999999997780, 1.000000000000000000, 1.000000000000000000, 0.9999999999999997780, 1.000000000000000444, 0.9999999999999996669, 1.000000000000000444, 0.9999999999999996669, 1.000000000000000222, 0.9999999999999994449, 1.000000000000000222, 1.000000000000000000, 1.000000000000000000, 1.000000000000000000, 1.000000000000000000, 1.000000000000000222, 1.000000000000000000, 1.000000000000000222, 0.9999999999999996669, 1.000000000000000222, 1.000000000000000000, 1.000000000000000444, 1.000000000000000000, 1.000000000000000000, 0.9999999999999997780, 1.000000000000000222, 0.9999999999999997780, 0.9999999999999997780, 1.000000000000000444, 1.000000000000000000, 1.000000000000000222, 0.9999999999999996669, 1.000000000000000444, 0.9999999999999997780, 1.000000000000000222, 0.9999999999999997780, 1.000000000000000222, 1.000000000000000000, 1.000000000000000000, 1.000000000000000000, 1.000000000000000000, 1.000000000000000222, 1.000000000000000222, 0.9999999999999997780, 1.000000000000000222, 1.000000000000000000, 1.000000000000000222, 0.9999999999999997780, 1.000000000000000222, 1.000000000000000000, 1.000000000000000000, 0.9999999999999997780, 1.000000000000000000, 1.000000000000000000, 0.9999999999999997780, 1.000000000000000222, 0.9999999999999997780, 1.000000000000000222, 0.9999999999999997780, 1.000000000000000444, 1.000000000000000000, 0.9999999999999996669, 1.000000000000000444, 1.000000000000000000, 0.9999999999999997780, 1.000000000000000000, 0.9999999999999996669, 1.000000000000000000, 1.000000000000000222, 0.9999999999999996669, 1.000000000000000222, 0.9999999999999997780, 1.000000000000000000, 1.000000000000000222, 0.9999999999999997780, 1.000000000000000222, 0.9999999999999997780, 1.000000000000000222, 1.000000000000000000, 1.000000000000000000, 1.000000000000000000, 0.9999999999999997780, 1.000000000000000222, 0.9999999999999997780, 1.000000000000000222, 1.000000000000000000, 1.000000000000000000, 1.000000000000000000, 1.000000000000000000, 1.000000000000000444, 0.9999999999999997780, 1.000000000000000444, 0.9999999999999997780, 1.000000000000000222, 1.000000000000000000, 1.000000000000000000, 1.000000000000000000, 1.000000000000000000, 0.9999999999999997780, 1.000000000000000000, 1.000000000000000222, 0.9999999999999997780, 1.000000000000000222, 1.000000000000000000, 1.000000000000000000, 1.000000000000000222, 0.9999999999999997780, 1.000000000000000222, 0.9999999999999996669, 1.000000000000000444, 0.9999999999999994449, 1.000000000000000444, 0.9999999999999997780, 0.9999999999999997780, 1.000000000000000000, 1.000000000000000000, 1.000000000000000222, 1.000000000000000000, 1.000000000000000000, 1.000000000000000000, 1.000000000000000000, 1.000000000000000222, 1.000000000000000444, 0.9999999999999997780, 1.000000000000000222, 1.000000000000000000, 0.9999999999999996669, 1.000000000000000222, 1.000000000000000222, 1.000000000000000222, 1.000000000000000222, 1.000000000000000000, 1.000000000000000000, 1.000000000000000222, 1.000000000000000000, 1.000000000000000222, 1.000000000000000000, 1.000000000000000000, 1.000000000000000000, 1.000000000000000222, 0.9999999999999997780, 1.000000000000000000, 1.000000000000000222, 1.000000000000000000, 1.000000000000000222, 1.000000000000000000, 0.9999999999999997780, 1.000000000000000444, 1.000000000000000000, 0.9999999999999996669, 1.000000000000000222, 0.9999999999999997780, 1.000000000000000222, 1.000000000000000000, 1.000000000000000000, 1.000000000000000444, 0.9999999999999996669, 1.000000000000000000, 0.9999999999999997780, 1.000000000000000000, 0.9999999999999997780, 0.9999999999999997780, 1.000000000000000000, 1.000000000000000000, 1.000000000000000000, 0.9999999999999997780, 1.000000000000000000, 1.000000000000000222, 1.000000000000000222, 1.000000000000000000, 0.9999999999999997780, 1.000000000000000222, 1.000000000000000000, 1.000000000000000000, 1.000000000000000222, 1.000000000000000222, 1.000000000000000222, 1.000000000000000000, 0.9999999999999997780, 1.000000000000000444, 0.9999999999999997780, 1.000000000000000444, 0.9999999999999997780, 1.000000000000000000, 1.000000000000000222, 0.9999999999999997780, 1.000000000000000222, 0.9999999999999997780, 1.000000000000000222, 0.9999999999999997780, 1.000000000000000222, 0.9999999999999996669, 1.000000000000000222, 0.9999999999999997780, 1.000000000000000444, 1.000000000000000000, 1.000000000000000000, 0.9999999999999997780, 1.000000000000000222, 1.000000000000000000, 0.9999999999999996669, 1.000000000000000222, 0.9999999999999997780, 1.000000000000000000, 1.000000000000000222, 1.000000000000000000, 1.000000000000000222, 0.9999999999999996669, 1.000000000000000444, 0.9999999999999996669, 1.000000000000000000, 1.000000000000000000, 1.000000000000000000, 0.9999999999999997780, 1.000000000000000444, 1.000000000000000000, 1.000000000000000000, 1.000000000000000000, 1.000000000000000000, 0.9999999999999997780, 1.000000000000000222, 1.000000000000000222, 1.000000000000000222, 1.000000000000000000, 1.000000000000000222, 1.000000000000000000, 0.9999999999999997780, 1.000000000000000444, 1.000000000000000000, 0.9999999999999997780, 1.000000000000000222, 0.9999999999999996669, 1.000000000000000222, 1.000000000000000000, 1.000000000000000444, 1.000000000000000222, 0.9999999999999996669, 1.000000000000000222, 0.9999999999999997780, 1.000000000000000222, 1.000000000000000222, 0.9999999999999997780, 1.000000000000000222, 1.000000000000000000, 1.000000000000000222, 1.000000000000000222, 0.9999999999999997780, 1.000000000000000444, 0.9999999999999996669, 1.000000000000000222, 1.000000000000000222, 1.000000000000000000, 1.000000000000000000, 1.000000000000000000, 1.000000000000000222, 1.000000000000000000, 1.000000000000000000, 1.000000000000000222, 0.9999999999999996669, 1.000000000000000444, 1.000000000000000222, 0.9999999999999997780, 1.000000000000000222, 0.9999999999999997780, 1.000000000000000444, 0.9999999999999996669, 1.000000000000000666, 0.9999999999999994449, 1.000000000000000222, 0.9999999999999997780, 1.000000000000000444, 1.000000000000000000, 1.000000000000000222, 1.000000000000000222, 1.000000000000000000, 0.9999999999999997780, 0.9999999999999997780, 1.000000000000000444, 1.000000000000000000, 1.000000000000000000, 1.000000000000000000, 0.9999999999999997780, 1.000000000000000222, 1.000000000000000222, 0.9999999999999997780, 1.000000000000000222, 1.000000000000000000, 1.000000000000000444, 0.9999999999999996669, 1.000000000000000444, 0.9999999999999997780, 1.000000000000000000, 0.9999999999999997780, 1.000000000000000444, 0.9999999999999996669, 1.000000000000000444, 1.000000000000000000, 1.000000000000000000, 1.000000000000000000, 0.9999999999999997780, 1.000000000000000444, 1.000000000000000222, 0.9999999999999997780, 1.000000000000000444, 1.000000000000000000, 0.9999999999999996669, 1.000000000000000444, 1.000000000000000000, 1.000000000000000000, 1.000000000000000000, 0.9999999999999997780, 1.000000000000000222, 0.9999999999999997780, 1.000000000000000000, 1.000000000000000222, 0.9999999999999997780, 1.000000000000000000, 1.000000000000000000, 0.9999999999999997780, 1.000000000000000444, 0.9999999999999997780, 1.000000000000000444, 0.9999999999999994449, 1.000000000000000444, 0.9999999999999997780, 1.000000000000000444, 0.9999999999999997780, 1.000000000000000000, 0.9999999999999997780, 1.000000000000000222, 1.000000000000000222, 1.000000000000000000, 1.000000000000000000),
 ( 0.3333333333333333703, 0.3333333333333333703, 0.3333333333333333703, 0.3333333333333335369, 0.3333333333333333148, 0.3333333333333333703, 0.3333333333333333703, 0.3333333333333333148, 0.3333333333333333148, 0.3333333333333334259, 0.3333333333333333703, 0.3333333333333333148, 0.3333333333333334259, 0.3333333333333333148, 0.3333333333333334259, 0.3333333333333333148, 0.3333333333333333703, 0.3333333333333333148, 0.3333333333333334814, 0.3333333333333333148, 0.3333333333333334814, 0.3333333333333334814, 0.3333333333333333148, 0.3333333333333334259, 0.3333333333333333148, 0.3333333333333333703, 0.3333333333333333148, 0.3333333333333334814, 0.3333333333333333703, 0.3333333333333333703, 0.3333333333333333703, 0.3333333333333334259, 0.3333333333333333148, 0.3333333333333333148, 0.3333333333333334259, 0.3333333333333333703, 0.3333333333333334259, 0.3333333333333334259, 0.3333333333333332038, 0.3333333333333334814, 0.3333333333333333703, 0.3333333333333334814, 0.3333333333333332593, 0.3333333333333334259, 0.3333333333333333703, 0.3333333333333334259, 0.3333333333333333148, 0.3333333333333333703, 0.3333333333333334259, 0.3333333333333333148, 0.3333333333333332038, 0.3333333333333335369, 0.3333333333333332593, 0.3333333333333334814, 0.3333333333333333148, 0.3333333333333333703, 0.3333333333333334259, 0.3333333333333333703, 0.3333333333333334814, 0.3333333333333333703, 0.3333333333333334259, 0.3333333333333333148, 0.3333333333333334814, 0.3333333333333332038, 0.3333333333333334259, 0.3333333333333333148, 0.3333333333333333703, 0.3333333333333333703, 0.3333333333333334259, 0.3333333333333333148, 0.3333333333333333703, 0.3333333333333334259, 0.3333333333333333148, 0.3333333333333333703, 0.3333333333333333703, 0.3333333333333335369, 0.3333333333333333148, 0.3333333333333333703, 0.3333333333333333703, 0.3333333333333333703, 0.3333333333333333148, 0.3333333333333333703, 0.3333333333333334814, 0.3333333333333333148, 0.3333333333333334814, 0.3333333333333333703, 0.3333333333333334259, 0.3333333333333333148, 0.3333333333333334259, 0.3333333333333333148, 0.3333333333333334259, 0.3333333333333333148, 0.3333333333333333703, 0.3333333333333333703, 0.3333333333333333703, 0.3333333333333334259, 0.3333333333333334259, 0.3333333333333332593, 0.3333333333333334259, 0.3333333333333333703, 0.3333333333333334259, 0.3333333333333333148, 0.3333333333333334259, 0.3333333333333333703, 0.3333333333333333703, 0.3333333333333333148, 0.3333333333333334259, 0.3333333333333333703, 0.3333333333333333148, 0.3333333333333334259, 0.3333333333333332038, 0.3333333333333334814, 0.3333333333333333148, 0.3333333333333335369, 0.3333333333333334259, 0.3333333333333332038, 0.3333333333333334814, 0.3333333333333333703, 0.3333333333333332593, 0.3333333333333333703, 0.3333333333333332593, 0.3333333333333333703, 0.3333333333333334814, 0.3333333333333333148, 0.3333333333333334814, 0.3333333333333333148, 0.3333333333333334259, 0.3333333333333334259, 0.3333333333333333148, 0.3333333333333334259, 0.3333333333333333148, 0.3333333333333334259, 0.3333333333333333703, 0.3333333333333333703, 0.3333333333333334259, 0.3333333333333332593, 0.3333333333333334814, 0.3333333333333333148, 0.3333333333333333703, 0.3333333333333333703, 0.3333333333333333703, 0.3333333333333334259, 0.3333333333333334259, 0.3333333333333334814, 0.3333333333333333703, 0.3333333333333334259, 0.3333333333333333703, 0.3333333333333333703, 0.3333333333333333148, 0.3333333333333333703, 0.3333333333333334259, 0.3333333333333333148, 0.3333333333333333148, 0.3333333333333333148, 0.3333333333333334259, 0.3333333333333333148, 0.3333333333333334814, 0.3333333333333333148, 0.3333333333333334259, 0.3333333333333334259, 0.3333333333333333148, 0.3333333333333334814, 0.3333333333333333148, 0.3333333333333334814, 0.3333333333333332593, 0.3333333333333335369, 0.3333333333333333148, 0.3333333333333333703, 0.3333333333333333703, 0.3333333333333334259, 0.3333333333333333703, 0.3333333333333333703, 0.3333333333333333148, 0.3333333333333333703, 0.3333333333333332593, 0.3333333333333335369, 0.3333333333333334259, 0.3333333333333333703, 0.3333333333333334259, 0.3333333333333334259, 0.3333333333333332038, 0.3333333333333334814, 0.3333333333333333703, 0.3333333333333334259, 0.3333333333333333703, 0.3333333333333333703, 0.3333333333333333148, 0.3333333333333334814, 0.3333333333333333148, 0.3333333333333334814, 0.3333333333333334259, 0.3333333333333333148, 0.3333333333333333703, 0.3333333333333333703, 0.3333333333333333703, 0.3333333333333333703, 0.3333333333333334259, 0.3333333333333333148, 0.3333333333333334814, 0.3333333333333333148, 0.3333333333333333703, 0.3333333333333334814, 0.3333333333333332593, 0.3333333333333333148, 0.3333333333333334259, 0.3333333333333332593, 0.3333333333333335369, 0.3333333333333333703, 0.3333333333333334259, 0.3333333333333335369, 0.3333333333333333148, 0.3333333333333333703, 0.3333333333333333148, 0.3333333333333333703, 0.3333333333333333148, 0.3333333333333333148, 0.3333333333333333703, 0.3333333333333333703, 0.3333333333333333703, 0.3333333333333333148, 0.3333333333333333703, 0.3333333333333333703, 0.3333333333333334259, 0.3333333333333333703, 0.3333333333333333148, 0.3333333333333333703, 0.3333333333333333703, 0.3333333333333333703, 0.3333333333333334259, 0.3333333333333334259, 0.3333333333333334814, 0.3333333333333332593, 0.3333333333333334259, 0.3333333333333334259, 0.3333333333333333148, 0.3333333333333334259, 0.3333333333333333703, 0.3333333333333333148, 0.3333333333333334814, 0.3333333333333333703, 0.3333333333333334259, 0.3333333333333332593, 0.3333333333333334259, 0.3333333333333332593, 0.3333333333333334814, 0.3333333333333332593, 0.3333333333333334259, 0.3333333333333333148, 0.3333333333333334259, 0.3333333333333333703, 0.3333333333333334259, 0.3333333333333333703, 0.3333333333333333703, 0.3333333333333333703, 0.3333333333333333148, 0.3333333333333334259, 0.3333333333333333703, 0.3333333333333333148, 0.3333333333333334259, 0.3333333333333333148, 0.3333333333333333703, 0.3333333333333333148, 0.3333333333333334814, 0.3333333333333332593, 0.3333333333333333703, 0.3333333333333333703, 0.3333333333333334259, 0.3333333333333332593, 0.3333333333333335369, 0.3333333333333333703, 0.3333333333333333703, 0.3333333333333333703, 0.3333333333333333148, 0.3333333333333333148, 0.3333333333333334259, 0.3333333333333334814, 0.3333333333333334259, 0.3333333333333333703, 0.3333333333333334259, 0.3333333333333334259, 0.3333333333333333703, 0.3333333333333334814, 0.3333333333333333148, 0.3333333333333333148, 0.3333333333333334259, 0.3333333333333332038, 0.3333333333333334814, 0.3333333333333333148, 0.3333333333333335369, 0.3333333333333334259, 0.3333333333333333148, 0.3333333333333334814, 0.3333333333333333703, 0.3333333333333333703, 0.3333333333333334259, 0.3333333333333333703, 0.3333333333333334259, 0.3333333333333333703, 0.3333333333333334259, 0.3333333333333333148, 0.3333333333333333703, 0.3333333333333335369, 0.3333333333333332038, 0.3333333333333334814, 0.3333333333333333703, 0.3333333333333333148, 0.3333333333333334259, 0.3333333333333333703, 0.3333333333333333148, 0.3333333333333334259, 0.3333333333333333703, 0.3333333333333334259, 0.3333333333333332593, 0.3333333333333335369, 0.3333333333333334814, 0.3333333333333333148, 0.3333333333333334259, 0.3333333333333333148, 0.3333333333333335369, 0.3333333333333332593, 0.3333333333333335924, 0.3333333333333332593, 0.3333333333333333703, 0.3333333333333333703, 0.3333333333333334814, 0.3333333333333333703, 0.3333333333333334814, 0.3333333333333333703, 0.3333333333333334259, 0.3333333333333332593, 0.3333333333333334259, 0.3333333333333335369, 0.3333333333333333148, 0.3333333333333334814, 0.3333333333333333148, 0.3333333333333333703, 0.3333333333333334259, 0.3333333333333334259, 0.3333333333333332593, 0.3333333333333334259, 0.3333333333333333148, 0.3333333333333335369, 0.3333333333333332593, 0.3333333333333335369, 0.3333333333333333148, 0.3333333333333333148, 0.3333333333333333703, 0.3333333333333334814, 0.3333333333333333148, 0.3333333333333334259, 0.3333333333333333148, 0.3333333333333334259, 0.3333333333333333703, 0.3333333333333333148, 0.3333333333333334259, 0.3333333333333334814, 0.3333333333333333148, 0.3333333333333334814, 0.3333333333333333703, 0.3333333333333332593, 0.3333333333333334259, 0.3333333333333333703, 0.3333333333333334259, 0.3333333333333333703, 0.3333333333333333148, 0.3333333333333334259, 0.3333333333333333703, 0.3333333333333333148, 0.3333333333333334259, 0.3333333333333333148, 0.3333333333333333148, 0.3333333333333333703, 0.3333333333333333703, 0.3333333333333334259, 0.3333333333333333148, 0.3333333333333334259, 0.3333333333333332593, 0.3333333333333334259, 0.3333333333333333703, 0.3333333333333334259, 0.3333333333333333703, 0.3333333333333333703, 0.3333333333333333148, 0.3333333333333334814, 0.3333333333333334259, 0.3333333333333333703, 0.3333333333333333703),
 ( 0.3333333333333333703, 0.3333333333333333703, 0.3333333333333333703, 0.3333333333333335369, 0.3333333333333333148, 0.3333333333333333703, 0.3333333333333333703, 0.3333333333333333148, 0.3333333333333333148, 0.3333333333333334259, 0.3333333333333333703, 0.3333333333333333148, 0.3333333333333334259, 0.3333333333333333148, 0.3333333333333334259, 0.3333333333333333148, 0.3333333333333333703, 0.3333333333333333148, 0.3333333333333334814, 0.3333333333333333148, 0.3333333333333334814, 0.3333333333333334814, 0.3333333333333333148, 0.3333333333333334259, 0.3333333333333333148, 0.3333333333333333703, 0.3333333333333333148, 0.3333333333333334814, 0.3333333333333333703, 0.3333333333333333703, 0.3333333333333333703, 0.3333333333333334259, 0.3333333333333333148, 0.3333333333333333148, 0.3333333333333334259, 0.3333333333333333703, 0.3333333333333334259, 0.3333333333333334259, 0.3333333333333332038, 0.3333333333333334814, 0.3333333333333333703, 0.3333333333333334814, 0.3333333333333332593, 0.3333333333333334259, 0.3333333333333333703, 0.3333333333333334259, 0.3333333333333333148, 0.3333333333333333703, 0.3333333333333334259, 0.3333333333333333148, 0.3333333333333332038, 0.3333333333333335369, 0.3333333333333332593, 0.3333333333333334814, 0.3333333333333333148, 0.3333333333333333703, 0.3333333333333334259, 0.3333333333333333703, 0.3333333333333334814, 0.3333333333333333703, 0.3333333333333334259, 0.3333333333333333148, 0.3333333333333334814, 0.3333333333333332038, 0.3333333333333334259, 0.3333333333333333148, 0.3333333333333333703, 0.3333333333333333703, 0.3333333333333334259, 0.3333333333333333148, 0.3333333333333333703, 0.3333333333333334259, 0.3333333333333333148, 0.3333333333333333703, 0.3333333333333333703, 0.3333333333333335369, 0.3333333333333333148, 0.3333333333333333703, 0.3333333333333333703, 0.3333333333333333703, 0.3333333333333333148, 0.3333333333333333703, 0.3333333333333334814, 0.3333333333333333148, 0.3333333333333334814, 0.3333333333333333703, 0.3333333333333334259, 0.3333333333333333148, 0.3333333333333334259, 0.3333333333333333148, 0.3333333333333334259, 0.3333333333333333148, 0.3333333333333333703, 0.3333333333333333703, 0.3333333333333333703, 0.3333333333333334259, 0.3333333333333334259, 0.3333333333333332593, 0.3333333333333334259, 0.3333333333333333703, 0.3333333333333334259, 0.3333333333333333148, 0.3333333333333334259, 0.3333333333333333703, 0.3333333333333333703, 0.3333333333333333148, 0.3333333333333334259, 0.3333333333333333703, 0.3333333333333333148, 0.3333333333333334259, 0.3333333333333332038, 0.3333333333333334814, 0.3333333333333333148, 0.3333333333333335369, 0.3333333333333334259, 0.3333333333333332038, 0.3333333333333334814, 0.3333333333333333703, 0.3333333333333332593, 0.3333333333333333703, 0.3333333333333332593, 0.3333333333333333703, 0.3333333333333334814, 0.3333333333333333148, 0.3333333333333334814, 0.3333333333333333148, 0.3333333333333334259, 0.3333333333333334259, 0.3333333333333333148, 0.3333333333333334259, 0.3333333333333333148, 0.3333333333333334259, 0.3333333333333333703, 0.3333333333333333703, 0.3333333333333334259, 0.3333333333333332593, 0.3333333333333334814, 0.3333333333333333148, 0.3333333333333333703, 0.3333333333333333703, 0.3333333333333333703, 0.3333333333333334259, 0.3333333333333334259, 0.3333333333333334814, 0.3333333333333333703, 0.3333333333333334259, 0.3333333333333333703, 0.3333333333333333703, 0.3333333333333333148, 0.3333333333333333703, 0.3333333333333334259, 0.3333333333333333148, 0.3333333333333333148, 0.3333333333333333148, 0.3333333333333334259, 0.3333333333333333148, 0.3333333333333334814, 0.3333333333333333148, 0.3333333333333334259, 0.3333333333333334259, 0.3333333333333333148, 0.3333333333333334814, 0.3333333333333333148, 0.3333333333333334814, 0.3333333333333332593, 0.3333333333333335369, 0.3333333333333333148, 0.3333333333333333703, 0.3333333333333333703, 0.3333333333333334259, 0.3333333333333333703, 0.3333333333333333703, 0.3333333333333333148, 0.3333333333333333703, 0.3333333333333332593, 0.3333333333333335369, 0.3333333333333334259, 0.3333333333333333703, 0.3333333333333334259, 0.3333333333333334259, 0.3333333333333332038, 0.3333333333333334814, 0.3333333333333333703, 0.3333333333333334259, 0.3333333333333333703, 0.3333333333333333703, 0.3333333333333333148, 0.3333333333333334814, 0.3333333333333333148, 0.3333333333333334814, 0.3333333333333334259, 0.3333333333333333148, 0.3333333333333333703, 0.3333333333333333703, 0.3333333333333333703, 0.3333333333333333703, 0.3333333333333334259, 0.3333333333333333148, 0.3333333333333334814, 0.3333333333333333148, 0.3333333333333333703, 0.3333333333333334814, 0.3333333333333332593, 0.3333333333333333148, 0.3333333333333334259, 0.3333333333333332593, 0.3333333333333335369, 0.3333333333333333703, 0.3333333333333334259, 0.3333333333333335369, 0.3333333333333333148, 0.3333333333333333703, 0.3333333333333333148, 0.3333333333333333703, 0.3333333333333333148, 0.3333333333333333148, 0.3333333333333333703, 0.3333333333333333703, 0.3333333333333333703, 0.3333333333333333148, 0.3333333333333333703, 0.3333333333333333703, 0.3333333333333334259, 0.3333333333333333703, 0.3333333333333333148, 0.3333333333333333703, 0.3333333333333333703, 0.3333333333333333703, 0.3333333333333334259, 0.3333333333333334259, 0.3333333333333334814, 0.3333333333333332593, 0.3333333333333334259, 0.3333333333333334259, 0.3333333333333333148, 0.3333333333333334259, 0.3333333333333333703, 0.3333333333333333148, 0.3333333333333334814, 0.3333333333333333703, 0.3333333333333334259, 0.3333333333333332593, 0.3333333333333334259, 0.3333333333333332593, 0.3333333333333334814, 0.3333333333333332593, 0.3333333333333334259, 0.3333333333333333148, 0.3333333333333334259, 0.3333333333333333703, 0.3333333333333334259, 0.3333333333333333703, 0.3333333333333333703, 0.3333333333333333703, 0.3333333333333333148, 0.3333333333333334259, 0.3333333333333333703, 0.3333333333333333148, 0.3333333333333334259, 0.3333333333333333148, 0.3333333333333333703, 0.3333333333333333148, 0.3333333333333334814, 0.3333333333333332593, 0.3333333333333333703, 0.3333333333333333703, 0.3333333333333334259, 0.3333333333333332593, 0.3333333333333335369, 0.3333333333333333703, 0.3333333333333333703, 0.3333333333333333703, 0.3333333333333333148, 0.3333333333333333148, 0.3333333333333334259, 0.3333333333333334814, 0.3333333333333334259, 0.3333333333333333703, 0.3333333333333334259, 0.3333333333333334259, 0.3333333333333333703, 0.3333333333333334814, 0.3333333333333333148, 0.3333333333333333148, 0.3333333333333334259, 0.3333333333333332038, 0.3333333333333334814, 0.3333333333333333148, 0.3333333333333335369, 0.3333333333333334259, 0.3333333333333333148, 0.3333333333333334814, 0.3333333333333333703, 0.3333333333333333703, 0.3333333333333334259, 0.3333333333333333703, 0.3333333333333334259, 0.3333333333333333703, 0.3333333333333334259, 0.3333333333333333148, 0.3333333333333333703, 0.3333333333333335369, 0.3333333333333332038, 0.3333333333333334814, 0.3333333333333333703, 0.3333333333333333148, 0.3333333333333334259, 0.3333333333333333703, 0.3333333333333333148, 0.3333333333333334259, 0.3333333333333333703, 0.3333333333333334259, 0.3333333333333332593, 0.3333333333333335369, 0.3333333333333334814, 0.3333333333333333148, 0.3333333333333334259, 0.3333333333333333148, 0.3333333333333335369, 0.3333333333333332593, 0.3333333333333335924, 0.3333333333333332593, 0.3333333333333333703, 0.3333333333333333703, 0.3333333333333334814, 0.3333333333333333703, 0.3333333333333334814, 0.3333333333333333703, 0.3333333333333334259, 0.3333333333333332593, 0.3333333333333334259, 0.3333333333333335369, 0.3333333333333333148, 0.3333333333333334814, 0.3333333333333333148, 0.3333333333333333703, 0.3333333333333334259, 0.3333333333333334259, 0.3333333333333332593, 0.3333333333333334259, 0.3333333333333333148, 0.3333333333333335369, 0.3333333333333332593, 0.3333333333333335369, 0.3333333333333333148, 0.3333333333333333148, 0.3333333333333333703, 0.3333333333333334814, 0.3333333333333333148, 0.3333333333333334259, 0.3333333333333333148, 0.3333333333333334259, 0.3333333333333333703, 0.3333333333333333148, 0.3333333333333334259, 0.3333333333333334814, 0.3333333333333333148, 0.3333333333333334814, 0.3333333333333333703, 0.3333333333333332593, 0.3333333333333334259, 0.3333333333333333703, 0.3333333333333334259, 0.3333333333333333703, 0.3333333333333333148, 0.3333333333333334259, 0.3333333333333333703, 0.3333333333333333148, 0.3333333333333334259, 0.3333333333333333148, 0.3333333333333333148, 0.3333333333333333703, 0.3333333333333333703, 0.3333333333333334259, 0.3333333333333333148, 0.3333333333333334259, 0.3333333333333332593, 0.3333333333333334259, 0.3333333333333333703, 0.3333333333333334259, 0.3333333333333333703, 0.3333333333333333703, 0.3333333333333333148, 0.3333333333333334814, 0.3333333333333334259, 0.3333333333333333703, 0.3333333333333333703),
 ( 1.000000000000000000, 1.000000000000000000, 1.000000000000000000, 1.000000000000000222, 0.9999999999999996669, 1.000000000000000222, 0.9999999999999997780, 1.000000000000000000, 0.9999999999999997780, 1.000000000000000444, 1.000000000000000000, 0.9999999999999997780, 1.000000000000000222, 1.000000000000000000, 0.9999999999999997780, 1.000000000000000222, 0.9999999999999996669, 1.000000000000000000, 1.000000000000000222, 1.000000000000000000, 1.000000000000000000, 1.000000000000000444, 0.9999999999999994449, 1.000000000000000444, 0.9999999999999996669, 1.000000000000000222, 1.000000000000000000, 1.000000000000000444, 1.000000000000000000, 0.9999999999999997780, 1.000000000000000000, 1.000000000000000222, 0.9999999999999997780, 0.9999999999999997780, 1.000000000000000444, 0.9999999999999997780, 1.000000000000000444, 1.000000000000000222, 0.9999999999999996669, 1.000000000000000222, 1.000000000000000000, 1.000000000000000444, 0.9999999999999997780, 1.000000000000000222, 1.000000000000000222, 1.000000000000000222, 0.9999999999999997780, 1.000000000000000000, 1.000000000000000000, 1.000000000000000000, 0.9999999999999994449, 1.000000000000000444, 0.9999999999999997780, 1.000000000000000444, 0.9999999999999997780, 1.000000000000000000, 1.000000000000000000, 0.9999999999999997780, 1.000000000000000444, 0.9999999999999996669, 1.000000000000000444, 0.9999999999999996669, 1.000000000000000222, 0.9999999999999994449, 1.000000000000000222, 1.000000000000000000, 1.000000000000000000, 1.000000000000000000, 1.000000000000000000, 1.000000000000000222, 1.000000000000000000, 1.000000000000000222, 0.9999999999999996669, 1.000000000000000222, 1.000000000000000000, 1.000000000000000444, 1.000000000000000000, 1.000000000000000000, 0.9999999999999997780, 1.000000000000000222, 0.9999999999999997780, 0.9999999999999997780, 1.000000000000000444, 1.000000000000000000, 1.000000000000000222, 0.9999999999999996669, 1.000000000000000444, 0.9999999999999997780, 1.000000000000000222, 0.9999999999999997780, 1.000000000000000222, 1.000000000000000000, 1.000000000000000000, 1.000000000000000000, 1.000000000000000000, 1.000000000000000222, 1.000000000000000222, 0.9999999999999997780, 1.000000000000000222, 1.000000000000000000, 1.000000000000000222, 0.9999999999999997780, 1.000000000000000222, 1.000000000000000000, 1.000000000000000000, 0.9999999999999997780, 1.000000000000000000, 1.000000000000000000, 0.9999999999999997780, 1.000000000000000222, 0.9999999999999997780, 1.000000000000000222, 0.9999999999999997780, 1.000000000000000444, 1.000000000000000000, 0.9999999999999996669, 1.000000000000000444, 1.000000000000000000, 0.9999999999999997780, 1.000000000000000000, 0.9999999999999996669, 1.000000000000000000, 1.000000000000000222, 0.9999999999999996669, 1.000000000000000222, 0.9999999999999997780, 1.000000000000000000, 1.000000000000000222, 0.9999999999999997780, 1.000000000000000222, 0.9999999999999997780, 1.000000000000000222, 1.000000000000000000, 1.000000000000000000, 1.000000000000000000, 0.9999999999999997780, 1.000000000000000222, 0.9999999999999997780, 1.000000000000000222, 1.000000000000000000, 1.000000000000000000, 1.000000000000000000, 1.000000000000000000, 1.000000000000000444, 0.9999999999999997780, 1.000000000000000444, 0.9999999999999997780, 1.000000000000000222, 1.000000000000000000, 1.000000000000000000, 1.000000000000000000, 1.000000000000000000, 0.9999999999999997780, 1.000000000000000000, 1.000000000000000222, 0.9999999999999997780, 1.000000000000000222, 1.000000000000000000, 1.000000000000000000, 1.000000000000000222, 0.9999999999999997780, 1.000000000000000222, 0.9999999999999996669, 1.000000000000000444, 0.9999999999999994449, 1.000000000000000444, 0.9999999999999997780, 0.9999999999999997780, 1.000000000000000000, 1.000000000000000000, 1.000000000000000222, 1.000000000000000000, 1.000000000000000000, 1.000000000000000000, 1.000000000000000000, 1.000000000000000222, 1.000000000000000444, 0.9999999999999997780, 1.000000000000000222, 1.000000000000000000, 0.9999999999999996669, 1.000000000000000222, 1.000000000000000222, 1.000000000000000222, 1.000000000000000222, 1.000000000000000000, 1.000000000000000000, 1.000000000000000222, 1.000000000000000000, 1.000000000000000222, 1.000000000000000000, 1.000000000000000000, 1.000000000000000000, 1.000000000000000222, 0.9999999999999997780, 1.000000000000000000, 1.000000000000000222, 1.000000000000000000, 1.000000000000000222, 1.000000000000000000, 0.9999999999999997780, 1.000000000000000444, 1.000000000000000000, 0.9999999999999996669, 1.000000000000000222, 0.9999999999999997780, 1.000000000000000222, 1.000000000000000000, 1.000000000000000000, 1.000000000000000444, 0.9999999999999996669, 1.000000000000000000, 0.9999999999999997780, 1.000000000000000000, 0.9999999999999997780, 0.9999999999999997780, 1.000000000000000000, 1.000000000000000000, 1.000000000000000000, 0.9999999999999997780, 1.000000000000000000, 1.000000000000000222, 1.000000000000000222, 1.000000000000000000, 0.9999999999999997780, 1.000000000000000222, 1.000000000000000000, 1.000000000000000000, 1.000000000000000222, 1.000000000000000222, 1.000000000000000222, 1.000000000000000000, 0.9999999999999997780, 1.000000000000000444, 0.9999999999999997780, 1.000000000000000444, 0.9999999999999997780, 1.000000000000000000, 1.000000000000000222, 0.9999999999999997780, 1.000000000000000222, 0.9999999999999997780, 1.000000000000000222, 0.9999999999999997780, 1.000000000000000222, 0.9999999999999996669, 1.000000000000000222, 0.9999999999999997780, 1.000000000000000444, 1.000000000000000000, 1.000000000000000000, 0.9999999999999997780, 1.000000000000000222, 1.000000000000000000, 0.9999999999999996669, 1.000000000000000222, 0.9999999999999997780, 1.000000000000000000, 1.000000000000000222, 1.000000000000000000, 1.000000000000000222, 0.9999999999999996669, 1.000000000000000444, 0.9999999999999996669, 1.000000000000000000, 1.000000000000000000, 1.000000000000000000, 0.9999999999999997780, 1.000000000000000444, 1.000000000000000000, 1.000000000000000000, 1.000000000000000000, 1.000000000000000000, 0.9999999999999997780, 1.000000000000000222, 1.000000000000000222, 1.000000000000000222, 1.000000000000000000, 1.000000000000000222, 1.000000000000000000, 0.9999999999999997780, 1.000000000000000444, 1.000000000000000000, 0.9999999999999997780, 1.000000000000000222, 0.9999999999999996669, 1.000000000000000222, 1.000000000000000000, 1.000000000000000444, 1.000000000000000222, 0.9999999999999996669, 1.000000000000000222, 0.9999999999999997780, 1.000000000000000222, 1.000000000000000222, 0.9999999999999997780, 1.000000000000000222, 1.000000000000000000, 1.000000000000000222, 1.000000000000000222, 0.9999999999999997780, 1.000000000000000444, 0.9999999999999996669, 1.000000000000000222, 1.000000000000000222, 1.000000000000000000, 1.000000000000000000, 1.000000000000000000, 1.000000000000000222, 1.000000000000000000, 1.000000000000000000, 1.000000000000000222, 0.9999999999999996669, 1.000000000000000444, 1.000000000000000222, 0.9999999999999997780, 1.000000000000000222, 0.9999999999999997780, 1.000000000000000444, 0.9999999999999996669, 1.000000000000000666, 0.9999999999999994449, 1.000000000000000222, 0.9999999999999997780, 1.000000000000000444, 1.000000000000000000, 1.000000000000000222, 1.000000000000000222, 1.000000000000000000, 0.9999999999999997780, 0.9999999999999997780, 1.000000000000000444, 1.000000000000000000, 1.000000000000000000, 1.000000000000000000, 0.9999999999999997780, 1.000000000000000222, 1.000000000000000222, 0.9999999999999997780, 1.000000000000000222, 1.000000000000000000, 1.000000000000000444, 0.9999999999999996669, 1.000000000000000444, 0.9999999999999997780, 1.000000000000000000, 0.9999999999999997780, 1.000000000000000444, 0.9999999999999996669, 1.000000000000000444, 1.000000000000000000, 1.000000000000000000, 1.000000000000000000, 0.9999999999999997780, 1.000000000000000444, 1.000000000000000222, 0.9999999999999997780, 1.000000000000000444, 1.000000000000000000, 0.9999999999999996669, 1.000000000000000444, 1.000000000000000000, 1.000000000000000000, 1.000000000000000000, 0.9999999999999997780, 1.000000000000000222, 0.9999999999999997780, 1.000000000000000000, 1.000000000000000222, 0.9999999999999997780, 1.000000000000000000, 1.000000000000000000, 0.9999999999999997780, 1.000000000000000444, 0.9999999999999997780, 1.000000000000000444, 0.9999999999999994449, 1.000000000000000444, 0.9999999999999997780, 1.000000000000000444, 0.9999999999999997780, 1.000000000000000000, 0.9999999999999997780, 1.000000000000000222, 1.000000000000000222, 1.000000000000000000, 1.000000000000000000) ) ) 
 REPRESENTATION_ITEM ( '' )  SURFACE ( )  );
#39774=CARTESIAN_POINT ( 'NONE',  ( 3.661125528703466525, 1.714762188600306825, -1.331539952715065978 ) ) ;
#39775=CARTESIAN_POINT ( 'NONE',  ( 2.209345402013741300, -0.4006574107652469130, 1.781019818369505847 ) ) ;
#39777=CARTESIAN_POINT ( 'NONE',  ( 4.575475080723796495, 1.571334676144776621, 1.419386683734702226 ) ) ;
#39779=CARTESIAN_POINT ( 'NONE',  ( 4.722401423535961484, 2.193339426362813871, 0.6665824366990577010 ) ) ;
#39781=CARTESIAN_POINT ( 'NONE',  ( 0.07755575628181145265, 0.2276780653837663093, -2.222404768597835201 ) ) ;
#39784=CARTESIAN_POINT ( 'NONE',  ( 0.1180496341894651385, -0.5612577129426484790, 2.044807062438446454 ) ) ;
#39790=CARTESIAN_POINT ( 'NONE',  ( 5.203750078570229753, 1.864167652161516031, 0.7691231355932278690 ) ) ;
#39792=CARTESIAN_POINT ( 'NONE',  ( 3.801677422522796945, -1.558724286948458548, -1.350822056805228266 ) ) ;
#39794=CARTESIAN_POINT ( 'NONE',  ( -0.2408018239684278916, 2.008845716682732263, -2.515352618630611659 ) ) ;
#39798=CARTESIAN_POINT ( 'NONE',  ( 5.999973295341066937, -0.7855225714627244171, -2.046000194487001433 ) ) ;
#39799=CARTESIAN_POINT ( 'NONE',  ( 3.217422812353257555, 1.967887761762876941, 0.4390297752325384995 ) ) ;
#39800=CARTESIAN_POINT ( 'NONE',  ( 3.825598141381767903, 0.9817388958630569595, -1.557492293685861284 ) ) ;
#39804=CARTESIAN_POINT ( 'NONE',  ( 1.043494860557155679, 0.7046062621528689229, -1.574481895975497592 ) ) ;
#39806=CARTESIAN_POINT ( 'NONE',  ( 0.4054594355042361875, -1.236789717346518769, -1.937488090237641014 ) ) ;
#39808=CARTESIAN_POINT ( 'NONE',  ( 6.649321564832020748, -1.812311508879884459, -1.354277771019767762 ) ) ;
#39809=CARTESIAN_POINT ( 'NONE',  ( 2.262461133243711675, 0.9012960022399997273, 1.903611236745775814 ) ) ;
#39818=CARTESIAN_POINT ( 'NONE',  ( 4.201594209339031494, 1.983332154306137518, -1.000733898520693499 ) ) ;
#39819=CARTESIAN_POINT ( 'NONE',  ( 2.168174125648382411, -1.346884454587377711, 1.728604079486287137 ) ) ;
#39821=CARTESIAN_POINT ( 'NONE',  ( 0.5048604690408053930, -0.7474223562033958101, -2.076596198196341003 ) ) ;
#39823=CARTESIAN_POINT ( 'NONE',  ( 5.142999638377217408, -0.2383176028181442918, -1.947251298587366231 ) ) ;
#39829=CARTESIAN_POINT ( 'NONE',  ( 4.728832233812888752, 1.460412846248357210, -1.537820402542383169 ) ) ;
#39832=CARTESIAN_POINT ( 'NONE',  ( 5.489210439962995736, 1.908424935776025455, -1.015307555102950010 ) ) ;
#39834=CARTESIAN_POINT ( 'NONE',  ( 4.599059095968327071, -0.4863373063577690059, 1.775805238918099382 ) ) ;
#39838=CARTESIAN_POINT ( 'NONE',  ( -0.05959145049940026140, -1.342969899416647905, -1.106900597494438143 ) ) ;
#39839=CARTESIAN_POINT ( 'NONE',  ( 6.827182134110246103, 3.705739211453745074, 2.325493694733235195 ) ) ;
#39842=CARTESIAN_POINT ( 'NONE',  ( 4.540002997438313592, 0.9271085556134452954, -1.952944755896801610 ) ) ;
#39845=CARTESIAN_POINT ( 'NONE',  ( 6.415388720371407949, 0.6297814698452592896, 1.915305867393565897 ) ) ;
#39847=CARTESIAN_POINT ( 'NONE',  ( 3.467792127863758456, 2.109446376165153847, -0.4717452660116944196 ) ) ;
#39848=CARTESIAN_POINT ( 'NONE',  ( 4.481683897012714191, 1.285251931988955709, 1.494896804799286993 ) ) ;
#39849=CARTESIAN_POINT ( 'NONE',  ( 3.936634314383654853, 0.9622043370151998065, 1.442083020896669954 ) ) ;
#39851=CARTESIAN_POINT ( 'NONE',  ( 0.8201894534925309177, 1.301127354658284663, -1.763390660798454634 ) ) ;
#39852=CARTESIAN_POINT ( 'NONE',  ( 1.571738265064129836, 0.1679657064320304316, -2.301541284809864862 ) ) ;
#39853=CARTESIAN_POINT ( 'NONE',  ( 3.550122082181893290, 2.060967561582152108, 0.003633429623469893420 ) ) ;
#39854=CARTESIAN_POINT ( 'NONE',  ( 6.198774611348529362, 1.617120784385807974, 1.075137550886333004 ) ) ;
#39861=CARTESIAN_POINT ( 'NONE',  ( 3.663272223086514234, -1.945104670120747059, -1.042327912031751458 ) ) ;
#39864=CARTESIAN_POINT ( 'NONE',  ( 0.7075644152179439983, 0.5912319408809820764, -1.764584214936999684 ) ) ;
#39865=CARTESIAN_POINT ( 'NONE',  ( -0.02880301295726198432, 2.855735178999906587, -2.761736421759506399 ) ) ;
#39870=CARTESIAN_POINT ( 'NONE',  ( 6.175717916360309090, -0.9808100270635997653, 1.557957644481674730 ) ) ;
#39872=CARTESIAN_POINT ( 'NONE',  ( 1.832957655136749908, 0.2007874442899897915, 2.051070037287055392 ) ) ;
#39878=CARTESIAN_POINT ( 'NONE',  ( 1.094684877246233201, -0.5000429121475665761, -1.999180680717755898 ) ) ;
#39880=CARTESIAN_POINT ( 'NONE',  ( 4.651808992177354440, 0.7092673950449077669, 1.699362209096597187 ) ) ;
#39883=CARTESIAN_POINT ( 'NONE',  ( -0.2409995289980246258, 7.629137130509076492, -2.600476469121239198 ) ) ;
#39885=CARTESIAN_POINT ( 'NONE',  ( 4.020313978404310262, -1.133593497508533110, -1.893353337301090233 ) ) ;
#39886=CARTESIAN_POINT ( 'NONE',  ( 6.819576192995205233, -2.197070018990463502, 0.5395731105267542738 ) ) ;
#39888=CARTESIAN_POINT ( 'NONE',  ( 0.7031954830387620037, 1.685401770928725007, -0.9037484838233383888 ) ) ;
#39889=CARTESIAN_POINT ( 'NONE',  ( 1.042204282965590201, 0.8216761606248854655, 1.841732292558920570 ) ) ;
#39891=CARTESIAN_POINT ( 'NONE',  ( 1.335823321505170025, -1.456863090139989714, 1.777644367010343451 ) ) ;
#39892=CARTESIAN_POINT ( 'NONE',  ( 6.772336237553374438, -1.148929780121176414, 1.476827877338216854 ) ) ;
#39895=CARTESIAN_POINT ( 'NONE',  ( 1.340467186903429253, 0.3614942610149494695, 1.835218787103513050 ) ) ;
#39897=CARTESIAN_POINT ( 'NONE',  ( 2.290250256651988892, -0.7762311197250795214, -1.861343989391924358 ) ) ;
#39901=CARTESIAN_POINT ( 'NONE',  ( 5.074884281356676574, -1.982714853632736807, -0.7105774565657559938 ) ) ;
#39906=CARTESIAN_POINT ( 'NONE',  ( 3.990493710177836828, -1.159536886187025440, 1.653596977174769833 ) ) ;
#39909=CARTESIAN_POINT ( 'NONE',  ( 6.877413164483755281, -0.1458786163922053403, 2.030295828278828374 ) ) ;
#39911=CARTESIAN_POINT ( 'NONE',  ( 4.727887898869392203, -1.325758432718616042, -1.707240035374466114 ) ) ;
#39916=CARTESIAN_POINT ( 'NONE',  ( 2.207711330564741559, -1.742939566808225482, -1.294460726261867034 ) ) ;
#39919=CARTESIAN_POINT ( 'NONE',  ( 2.261056740009634414, 1.805359621025553363, -0.3608742708730780513 ) ) ;
#39922=CARTESIAN_POINT ( 'NONE',  ( 3.210657068901449307, 1.982179491636561819, 0.9350799695589939731 ) ) ;
#39923=CARTESIAN_POINT ( 'NONE',  ( 6.983263157960330147, 2.416677186285462575, 2.534499922921686021 ) ) ;
#39924=CARTESIAN_POINT ( 'NONE',  ( 3.503020383517113423, 1.785049946035693891, -1.390086647613536952 ) ) ;
#39929=CARTESIAN_POINT ( 'NONE',  ( 5.202326708214688900, -0.5966268589385533838, -1.666288158821194187 ) ) ;
#39930=CARTESIAN_POINT ( 'NONE',  ( 3.352200558804620645, 0.9032658637736007412, -1.799124413793075528 ) ) ;
#39932=CARTESIAN_POINT ( 'NONE',  ( 1.430846025165666280, 2.029450977514839938, 0.5621798225463514598 ) ) ;
#39935=CARTESIAN_POINT ( 'NONE',  ( 0.8714670931111346830, -0.2923345663568870378, 1.947617037577647592 ) ) ;
#39937=CARTESIAN_POINT ( 'NONE',  ( 0.4144086874100678664, 0.7473079093508437909, 1.814158889769983185 ) ) ;
#39938=CARTESIAN_POINT ( 'NONE',  ( 6.222923320161976690, 1.335851037236086558, -1.223852264422401692 ) ) ;
#39941=CARTESIAN_POINT ( 'NONE',  ( 5.137510444216992767, -1.323429205136433140, -1.322332877454430955 ) ) ;
#39945=CARTESIAN_POINT ( 'NONE',  ( 4.662978783614929235, 1.603679166536524869, -1.309313232293010776 ) ) ;
#39956=CARTESIAN_POINT ( 'NONE',  ( 4.527759979645433752, 1.903474890065796732, -0.4746247275292309609 ) ) ;
#39958=CARTESIAN_POINT ( 'NONE',  ( 1.968124833515383809, 1.674630251985644414, 1.122327857054454814 ) ) ;
#39960=CARTESIAN_POINT ( 'NONE',  ( 0.9432342461353732110, -1.730868645791438620, -1.344178957308760802 ) ) ;
#39961=CARTESIAN_POINT ( 'NONE',  ( 2.178771278573924608, -0.08713135167291724548, -1.868625915979430951 ) ) ;
#39963=CARTESIAN_POINT ( 'NONE',  ( 4.095951438411546519, 1.318107682886668242, 1.521754241968393373 ) ) ;
#39967=CARTESIAN_POINT ( 'NONE',  ( 3.005573934588702034, -2.039760842771252136, 0.5671949335201897924 ) ) ;
#39969=CARTESIAN_POINT ( 'NONE',  ( 4.510256325466165173, 2.069976601481211542, -0.04757507122059301263 ) ) ;
#39971=CARTESIAN_POINT ( 'NONE',  ( 1.189138979623612480, 1.585436599910443611, 1.363068659274695893 ) ) ;
#39972=CARTESIAN_POINT ( 'NONE',  ( 6.720655732516667591, 2.416141799769660370, 2.554522868665403568 ) ) ;
#39973=CARTESIAN_POINT ( 'NONE',  ( 6.053692819838605743, 0.5272490726609192491, -1.747765065496959869 ) ) ;
#39980=CARTESIAN_POINT ( 'NONE',  ( 5.830699381415811899, 1.280921311228696347, -1.420062396151056117 ) ) ;
#39987=CARTESIAN_POINT ( 'NONE',  ( 6.169546029190325243, 1.392557221580101423, 1.458547251757099650 ) ) ;
#39991=CARTESIAN_POINT ( 'NONE',  ( 0.1399997263886038068, 0.2431072571701595186, -2.034387401959360187 ) ) ;
#39995=CARTESIAN_POINT ( 'NONE',  ( 3.766418665963155998, -0.7939890815925625400, -1.802475468321093732 ) ) ;
#39996=CARTESIAN_POINT ( 'NONE',  ( 4.200796113533305842, 1.844717850457804120, 0.8146114232021259838 ) ) ;
#39999=CARTESIAN_POINT ( 'NONE',  ( 4.400438482046089561, 1.694813852089768869, -1.389250428430639950 ) ) ;
#40001=CARTESIAN_POINT ( 'NONE',  ( 3.276308702328960099, -1.148522560162130501, 1.546420931960400758 ) ) ;
#40003=CARTESIAN_POINT ( 'NONE',  ( -0.1294898018151836583, 2.884012836773319766, -2.415168928093185396 ) ) ;
#40004=CARTESIAN_POINT ( 'NONE',  ( 0.1331565106231329398, 0.7299000548664087429, -2.029785554894456556 ) ) ;
#40009=CARTESIAN_POINT ( 'NONE',  ( 5.706567001488551227, 1.626822141722890303, 0.8623401093873286349 ) ) ;
#40010=CARTESIAN_POINT ( 'NONE',  ( 2.754543805099545217, 1.998131736582898332, 0.2443565819899694291 ) ) ;
#40011=CARTESIAN_POINT ( 'NONE',  ( 5.062018989497997445, 1.914771916633486448, -1.271085502950035417 ) ) ;
#40013=CARTESIAN_POINT ( 'NONE',  ( 3.045584334709343644, 1.312524258565110680, 1.319513337161677846 ) ) ;
#40015=CARTESIAN_POINT ( 'NONE',  ( -0.1290005225502922348, 7.629137130509076492, -2.773995091683972625 ) ) ;
#40019=CARTESIAN_POINT ( 'NONE',  ( 5.689037021386003090, 1.583751769416761324, 1.365026519206056665 ) ) ;
#40023=CARTESIAN_POINT ( 'NONE',  ( 6.410786927598755902, 1.272630858062718584, -1.164536656126140324 ) ) ;
#40025=CARTESIAN_POINT ( 'NONE',  ( 2.408496482339622879, -0.9999731500247920346, -1.416544738438466400 ) ) ;
#40030=CARTESIAN_POINT ( 'NONE',  ( 6.842638762948665132, -2.127444276778973631, -0.4322993451541176091 ) ) ;
#40031=CARTESIAN_POINT ( 'NONE',  ( 5.391160240453525709, 1.608232483172780558, -0.8641324296934371763 ) ) ;
#40032=CARTESIAN_POINT ( 'NONE',  ( 3.010546455304231372, 0.6564385890225448161, 1.848828695667027677 ) ) ;
#40037=CARTESIAN_POINT ( 'NONE',  ( 3.615986862044855421, -0.6139777315949943581, 2.029667854546577388 ) ) ;
#40042=CARTESIAN_POINT ( 'NONE',  ( 1.780221101387355009, -1.146701191353172611, -1.723467693327894068 ) ) ;
#40043=CARTESIAN_POINT ( 'NONE',  ( 6.827182134110207024, 2.985003573113382380, 2.264833014350222662 ) ) ;
#40045=CARTESIAN_POINT ( 'NONE',  ( 4.617978872065289231, -0.5927926152728602016, 2.140694073679518805 ) ) ;
#40047=CARTESIAN_POINT ( 'NONE',  ( 1.670936656956054644, 1.588967112724626096, 1.661273962566457874 ) ) ;
#40049=CARTESIAN_POINT ( 'NONE',  ( 6.385603471572667722, -1.944119864917488893, 0.6893456996763939193 ) ) ;
#40052=CARTESIAN_POINT ( 'NONE',  ( 6.181194517112824194, 1.274813594131599226, 1.328792456347933637 ) ) ;
#40055=CARTESIAN_POINT ( 'NONE',  ( 2.935702856749936362, -1.841876368404654629, 0.5141854427313449216 ) ) ;
#40056=CARTESIAN_POINT ( 'NONE',  ( -0.1106727585416201337, 1.364743060583981649, -2.259751816641343058 ) ) ;
#40057=CARTESIAN_POINT ( 'NONE',  ( 3.979312383816283383, 1.623897443016858011, -0.5815980338331677713 ) ) ;
#40058=CARTESIAN_POINT ( 'NONE',  ( 1.903530124611974017, -1.954778955200174861, 0.4946342604733033887 ) ) ;
#40059=CARTESIAN_POINT ( 'NONE',  ( 4.289826696582184518, 1.777288211397337170, -1.457785959652138530 ) ) ;
#40060=CARTESIAN_POINT ( 'NONE',  ( 4.007294123747324299, 1.937827550919896336, 1.167430888521280963 ) ) ;
#40061=CARTESIAN_POINT ( 'NONE',  ( 6.217421135136044441, -0.2594034420708571931, 2.089956235961006659 ) ) ;
#40064=CARTESIAN_POINT ( 'NONE',  ( 4.499107683057060214, 1.420662411309661088, 1.055048638519467286 ) ) ;
#40066=CARTESIAN_POINT ( 'NONE',  ( 0.8500709472824579116, 2.289359419033740295, -0.1177234237379476411 ) ) ;
#40067=CARTESIAN_POINT ( 'NONE',  ( 5.701068745948241201, -0.4431999317857804876, 1.786873912291174538 ) ) ;
#40069=CARTESIAN_POINT ( 'NONE',  ( 6.263654578238285531, 1.123272483274835087, 1.881548979392036802 ) ) ;
#40072=CARTESIAN_POINT ( 'NONE',  ( 6.162566008723842081, -0.7415158119226210598, -1.933206815039355320 ) ) ;
#40073=CARTESIAN_POINT ( 'NONE',  ( -0.2351498743046881446, -0.1506043639611966134, -1.983733596389973597 ) ) ;
#40075=CARTESIAN_POINT ( 'NONE',  ( 4.424389683245252947, 1.183944675904605504, -1.519688292035234367 ) ) ;
#40078=CARTESIAN_POINT ( 'NONE',  ( 0.8970957097632881183, -2.168902827774013442, -0.4795612232612302961 ) ) ;
#40087=CARTESIAN_POINT ( 'NONE',  ( 1.170277241841523264, -0.8789641444944886750, -1.754005360843587047 ) ) ;
#40090=CARTESIAN_POINT ( 'NONE',  ( 6.584431417889404337, 1.130572321132311098, -1.603143135845342515 ) ) ;
#40093=CARTESIAN_POINT ( 'NONE',  ( 0.3568017664055183613, 0.8693207686717405736, 2.089032543936353736 ) ) ;
#40098=CARTESIAN_POINT ( 'NONE',  ( 1.194370141144196706, -0.4488658031855938813, -1.815784161679114384 ) ) ;
#40099=CARTESIAN_POINT ( 'NONE',  ( 6.766931417284230754, -1.733354565069046505, 0.04740994324908299334 ) ) ;
#40101=CARTESIAN_POINT ( 'NONE',  ( 4.230150181147958044, 2.149441460308566754, 0.4267382380854707336 ) ) ;
#40102=CARTESIAN_POINT ( 'NONE',  ( 4.085262347903253044, -0.2225469472450763153, -2.296823545465367822 ) ) ;
#40103=CARTESIAN_POINT ( 'NONE',  ( 0.5673477787482993362, 0.2024836561579176908, -2.050924697174760780 ) ) ;
#40104=CARTESIAN_POINT ( 'NONE',  ( 2.730336461235380430, 0.2382978201147344655, 1.927214864610910183 ) ) ;
#40108=CARTESIAN_POINT ( 'NONE',  ( 4.904590598983499916, -2.104870323260544129, -0.2570220051709286579 ) ) ;
#40110=CARTESIAN_POINT ( 'NONE',  ( 3.832657856672664565, 0.6767144645295587457, -1.899618369658891748 ) ) ;
#40114=CARTESIAN_POINT ( 'NONE',  ( 1.049113529465800054, -1.437755431736492673, -1.125068434497819680 ) ) ;
#40119=CARTESIAN_POINT ( 'NONE',  ( 5.787979943833009067, -0.9286772032993969583, 1.839872548930401974 ) ) ;
#40125=CARTESIAN_POINT ( 'NONE',  ( 5.127605754342813960, -0.2940821729933600914, 1.998008755081616572 ) ) ;
#40126=CARTESIAN_POINT ( 'NONE',  ( 5.778047442595251937, 2.188849720005956900, -0.3775064732549227586 ) ) ;
#40130=CARTESIAN_POINT ( 'NONE',  ( 4.645419472943275174, -1.591690889772362283, -1.309095959863779246 ) ) ;
#40131=CARTESIAN_POINT ( 'NONE',  ( 3.920546200773936896, -1.392545040883992336, -1.458557299768625581 ) ) ;
#40137=CARTESIAN_POINT ( 'NONE',  ( 4.411482401463855396, 0.5350073857553553358, 1.943773423102819864 ) ) ;
#40138=CARTESIAN_POINT ( 'NONE',  ( 3.925598083870453614, 0.9833751987384667936, -1.556331266066004027 ) ) ;
#40140=CARTESIAN_POINT ( 'NONE',  ( 0.9796492596481393145, -0.06170110713811990943, -2.307032891211552084 ) ) ;
#40142=CARTESIAN_POINT ( 'NONE',  ( 3.849029623751087481, -1.769594347601778361, 1.241129261558816754 ) ) ;
#40145=CARTESIAN_POINT ( 'NONE',  ( 3.550466583917981200, 2.079229874635016184, -0.9797032261932754338 ) ) ;
#40148=CARTESIAN_POINT ( 'NONE',  ( 2.887410755087606695, 1.321643875934110479, 1.324118206929347563 ) ) ;
#40149=CARTESIAN_POINT ( 'NONE',  ( 6.596557512146871360, -0.5253642993188823995, -1.900122941938019450 ) ) ;
#40154=CARTESIAN_POINT ( 'NONE',  ( 1.770444396619451632, 1.136427050704125419, 1.891651738277564831 ) ) ;
#40159=CARTESIAN_POINT ( 'NONE',  ( 5.770382930017874834, -1.251004719971451795, 1.523686133408495236 ) ) ;
#40160=CARTESIAN_POINT ( 'NONE',  ( 6.147156021580305385, -1.953063626952681542, 1.228987080356194195 ) ) ;
#40161=CARTESIAN_POINT ( 'NONE',  ( 6.760206150924522817, -1.860609546209352372, 0.04724569877399482920 ) ) ;
#40162=CARTESIAN_POINT ( 'NONE',  ( 3.186439481354142789, 1.149679979862153756, -1.712247615763124120 ) ) ;
#40169=CARTESIAN_POINT ( 'NONE',  ( 5.582552312218076018, 1.297699880476494094, -1.740541793301546347 ) ) ;
#40170=CARTESIAN_POINT ( 'NONE',  ( -0.02900071798687918478, 7.629137130509076492, -2.773797386654376584 ) ) ;
#40171=CARTESIAN_POINT ( 'NONE',  ( 5.460457653299121361, -1.667157065227730106, -0.7818181906407914994 ) ) ;
#40176=CARTESIAN_POINT ( 'NONE',  ( 0.6501784551898766029, 0.7083214130543177278, -2.148700229429708841 ) ) ;
#40181=CARTESIAN_POINT ( 'NONE',  ( 0.01216826571975513152, -1.911853497171299265, -0.04704278909201110859 ) ) ;
#40182=CARTESIAN_POINT ( 'NONE',  ( 1.639140867700689785, -1.278921918198316465, -1.223650632631252622 ) ) ;
#40184=CARTESIAN_POINT ( 'NONE',  ( 6.410797320372758179, -0.5389820150160546941, -1.939520479220447902 ) ) ;
#40186=CARTESIAN_POINT ( 'NONE',  ( 3.550306043379815257, -1.284141074626928392, 1.421643848488469031 ) ) ;
#40188=CARTESIAN_POINT ( 'NONE',  ( 3.877371502699510142, -0.1471681016796568819, 1.964127982587125398 ) ) ;
#40189=CARTESIAN_POINT ( 'NONE',  ( -0.2104748580754166598, -0.006608320950483163522, -2.103482951484026753 ) ) ;
#40191=CARTESIAN_POINT ( 'NONE',  ( 2.834663617355744680, 0.2272019944037397543, 1.856728029318695627 ) ) ;
#40192=CARTESIAN_POINT ( 'NONE',  ( 6.199779612253428773, -0.5740575353240050527, 1.626695425327763678 ) ) ;
#40194=CARTESIAN_POINT ( 'NONE',  ( 2.121956728516772639, -2.140194184088719531, 0.5379336890513550795 ) ) ;
#40198=CARTESIAN_POINT ( 'NONE',  ( 0.1685210592646404493, -0.8794871949406095624, -1.863628177300826305 ) ) ;
#40202=CARTESIAN_POINT ( 'NONE',  ( 0.1747926744264452492, 5.725295659261265158, -2.449351454080525681 ) ) ;
#40206=CARTESIAN_POINT ( 'NONE',  ( 2.066927875543830950, 1.535623996113824496, -1.388825173883188713 ) ) ;
#40210=CARTESIAN_POINT ( 'NONE',  ( 1.172527652694483669, 0.8205418800426617087, 1.845675728695548745 ) ) ;
#40214=CARTESIAN_POINT ( 'NONE',  ( 0.1749903794560592474, 0.7218944060462629819, -2.038148089257747930 ) ) ;
#40216=CARTESIAN_POINT ( 'NONE',  ( 5.712267477471262289, -1.587595409608580255, -1.242535230690837489 ) ) ;
#40217=CARTESIAN_POINT ( 'NONE',  ( 6.016788071399586713, 0.1949370894720331426, 1.905806522959735627 ) ) ;
#40219=CARTESIAN_POINT ( 'NONE',  ( 4.071962858106247474, -1.261020321617589479, 1.792237525612811355 ) ) ;
#40221=CARTESIAN_POINT ( 'NONE',  ( 2.443496805918866865, -1.782974011999260977, 0.6919810379762068031 ) ) ;
#40225=CARTESIAN_POINT ( 'NONE',  ( 6.275037739279882842, 1.841983620878117733, -1.043829292874172143 ) ) ;
#40227=CARTESIAN_POINT ( 'NONE',  ( 6.286699343557897279, 1.907799665397521105, -1.078441415684105120 ) ) ;
#40229=CARTESIAN_POINT ( 'NONE',  ( 2.801416971846592219, -0.5432927088015163664, 1.637025921142007956 ) ) ;
#40231=CARTESIAN_POINT ( 'NONE',  ( 5.994406619193555663, -1.133004004027007516, 1.792352430775605798 ) ) ;
#40235=CARTESIAN_POINT ( 'NONE',  ( 0.2210476084268316321, -1.750679471464357650, -0.8856473702157914296 ) ) ;
#40242=CARTESIAN_POINT ( 'NONE',  ( 2.736723853829028830, 1.706320744115387811, 0.6085963735071827641 ) ) ;
#40246=CARTESIAN_POINT ( 'NONE',  ( 3.316878987808123735, 1.426168316962544091, -1.116757653536442740 ) ) ;
#40250=CARTESIAN_POINT ( 'NONE',  ( 5.002340964340571183, 1.856068601349126324, 0.1372510170762584192 ) ) ;
#40252=CARTESIAN_POINT ( 'NONE',  ( 2.671383988363975170, 1.356552116283934240, 1.352788525452413237 ) ) ;
#40253=CARTESIAN_POINT ( 'NONE',  ( 0.7096328715897933792, -1.817275359149352676, 0.1739118742359047065 ) ) ;
#40263=CARTESIAN_POINT ( 'NONE',  ( 1.869195317527425404, 2.000202809997845499, -0.6082070056973082339 ) ) ;
#40264=CARTESIAN_POINT ( 'NONE',  ( 6.821331454403446237, -0.1310627394537598467, 1.896496729248610125 ) ) ;
#40266=CARTESIAN_POINT ( 'NONE',  ( 2.098414945899258033, -0.4839449910110822373, -1.760204267430766301 ) ) ;
#40267=CARTESIAN_POINT ( 'NONE',  ( 3.106307083854151774, -2.204334110825040494, 0.1085914373066959593 ) ) ;
#40269=CARTESIAN_POINT ( 'NONE',  ( 1.054777118923880597, 0.3758132965740559883, 1.874924941132802836 ) ) ;
#40270=CARTESIAN_POINT ( 'NONE',  ( 1.135132829348266092, -0.04487231981731241992, -1.969206670302141804 ) ) ;
#40271=CARTESIAN_POINT ( 'NONE',  ( 3.561997098397641448, -1.302002156301942604, 1.441148521680717387 ) ) ;
#40276=CARTESIAN_POINT ( 'NONE',  ( 0.1388275050690327694, -0.1366109201720016320, -1.830645452005694951 ) ) ;
#40281=CARTESIAN_POINT ( 'NONE',  ( 3.122796855005858241, 0.05607861761174406934, 2.191015320347329709 ) ) ;
#40282=CARTESIAN_POINT ( 'NONE',  ( 0.1399997263886003374, 7.629137130509076492, -2.599723212958489516 ) ) ;
#40286=CARTESIAN_POINT ( 'NONE',  ( 4.090329635444483358, -1.806102819543849769, -0.2658631594732660530 ) ) ;
#40290=CARTESIAN_POINT ( 'NONE',  ( 4.961713530105988923, 1.850188064717460223, -0.2750520410098392654 ) ) ;
#40292=CARTESIAN_POINT ( 'NONE',  ( 2.121591023604427306, -1.868723361717766096, 0.4677975013653943859 ) ) ;
#40293=CARTESIAN_POINT ( 'NONE',  ( 6.350445966956749899, -1.952004966925089624, -0.1956573963535559180 ) ) ;
#40302=CARTESIAN_POINT ( 'NONE',  ( 0.5447201963149818082, -1.530340168762192254, 1.463345158046714056 ) ) ;
#40306=CARTESIAN_POINT ( 'NONE',  ( 5.506714918851105089, 0.5956099481174789156, 1.982760374633622424 ) ) ;
#40307=CARTESIAN_POINT ( 'NONE',  ( 0.9602180038516641147, -1.664555262390180257, -0.7873027242753791732 ) ) ;
#40310=CARTESIAN_POINT ( 'NONE',  ( 4.782019082252658926, 1.911913310736196081, -1.275919496871528169 ) ) ;
#40315=CARTESIAN_POINT ( 'NONE',  ( 0.8324521645294904459, 2.259258938120102922, 0.3867697638584958186 ) ) ;
#40318=CARTESIAN_POINT ( 'NONE',  ( 4.734287085814634644, 0.3336016870040105498, 1.912933106389144822 ) ) ;
#40323=CARTESIAN_POINT ( 'NONE',  ( 6.521744167503259249, -0.4122283346772101509, 1.874327247564554266 ) ) ;
#40324=CARTESIAN_POINT ( 'NONE',  ( 1.066563130004109405, -1.557762288434235476, -0.7409518577887274082 ) ) ;
#40325=CARTESIAN_POINT ( 'NONE',  ( 6.139861302770143858, 2.010801613648224961, -0.1531635369260639090 ) ) ;
#40329=CARTESIAN_POINT ( 'NONE',  ( 2.326223132658828963, 2.028069097222063188, 0.5071170776438630456 ) ) ;
#40330=CARTESIAN_POINT ( 'NONE',  ( 1.252431388357349684, -1.398210551426328330, 1.084949785890441110 ) ) ;
#40332=CARTESIAN_POINT ( 'NONE',  ( 3.890815911290066875, 1.937189890886330756, -1.225201777657213498 ) ) ;
#40333=CARTESIAN_POINT ( 'NONE',  ( 2.712550014960776856, -0.1704709713557898410, 1.731945008791212270 ) ) ;
#40335=CARTESIAN_POINT ( 'NONE',  ( 3.006218798242997980, -0.8556837461295877523, 1.940463308995137526 ) ) ;
#40337=CARTESIAN_POINT ( 'NONE',  ( 2.284178307277694664, -1.682821195468919395, 0.4169209145809901762 ) ) ;
#40339=CARTESIAN_POINT ( 'NONE',  ( 2.119380567849386665, 0.3219547178687692801, -1.832826937841147252 ) ) ;
#40340=CARTESIAN_POINT ( 'NONE',  ( 1.926474581872784420, 1.115185415580312700, 1.862746952601635808 ) ) ;
#40342=CARTESIAN_POINT ( 'NONE',  ( 3.889861467948489082, -2.010801299972611478, 0.1531677096566556595 ) ) ;
#40343=CARTESIAN_POINT ( 'NONE',  ( 2.281250000000002220, 0.7852924748301068902, 1.895863743164037718 ) ) ;
#40345=CARTESIAN_POINT ( 'NONE',  ( 0.4988883441144418840, 1.603466095971857852, -1.067369714357151222 ) ) ;
#40347=CARTESIAN_POINT ( 'NONE',  ( 4.465202103771027886, -1.783222260262930181, 1.324459880397445666 ) ) ;
#40354=CARTESIAN_POINT ( 'NONE',  ( 0.2588218971089132348, 2.215798623493638875, 0.1571155685827912152 ) ) ;
#40356=CARTESIAN_POINT ( 'NONE',  ( 4.685966490639408732, -1.205361723144786845, -1.547842780461285983 ) ) ;
#40359=CARTESIAN_POINT ( 'NONE',  ( 5.343176995970949861, -1.944282970029135083, 1.156607043288411019 ) ) ;
#40361=CARTESIAN_POINT ( 'NONE',  ( 3.596185909054748553, 0.9300860933913506212, -1.841171126807969349 ) ) ;
#40366=CARTESIAN_POINT ( 'NONE',  ( 4.358574879328508622, -1.387578095181252413, 1.254630796652965730 ) ) ;
#40367=CARTESIAN_POINT ( 'NONE',  ( 3.234723362560991244, 1.734343004352358664, -0.003563068559135627086 ) ) ;
#40368=CARTESIAN_POINT ( 'NONE',  ( 2.999246388560794951, -1.738348057599903074, 0.08809733484680536131 ) ) ;
#40369=CARTESIAN_POINT ( 'NONE',  ( 0.3984806668858055789, -0.7796899918033869392, -2.155833124811225687 ) ) ;
#40370=CARTESIAN_POINT ( 'NONE',  ( 0.7982362974770088604, -0.7925503509537080715, 2.059710425106767939 ) ) ;
#40371=CARTESIAN_POINT ( 'NONE',  ( 4.476172314981810452, -2.028359691925533781, -0.5064535023821553628 ) ) ;
#40372=CARTESIAN_POINT ( 'NONE',  ( 6.017518264666532168, -1.080727962582687773, -1.613252759315900731 ) ) ;
#40376=CARTESIAN_POINT ( 'NONE',  ( 0.7564826839323666174, 1.942540863013635821, -0.5404934282097761944 ) ) ;
#40377=CARTESIAN_POINT ( 'NONE',  ( 1.248456593208754795, 1.040400552670465162, -1.847740296886036582 ) ) ;
#40382=CARTESIAN_POINT ( 'NONE',  ( 4.758326833623739205, 0.7015320795021735556, 1.685726030614169924 ) ) ;
#40388=CARTESIAN_POINT ( 'NONE',  ( 1.951431513787309724, -1.802353211750299167, 0.9118321038049399530 ) ) ;
#40389=CARTESIAN_POINT ( 'NONE',  ( 5.368293279414073638, 1.083412401764087374, 1.922438065789177308 ) ) ;
#40391=CARTESIAN_POINT ( 'NONE',  ( 2.641259143913599949, 1.703662207083409763, -0.7491738860408488909 ) ) ;
#40399=CARTESIAN_POINT ( 'NONE',  ( 5.057177669875371429, -1.544152220135000420, -0.9737345633797565014 ) ) ;
#40403=CARTESIAN_POINT ( 'NONE',  ( 0.1452960159114678740, -0.1365383601019970750, -1.704228001402931625 ) ) ;
#40404=CARTESIAN_POINT ( 'NONE',  ( 0.4975142532120572225, -0.5819891871022980778, -1.640261313346396133 ) ) ;
#40405=CARTESIAN_POINT ( 'NONE',  ( 5.338606043529401823, 2.272755431710461238, 0.3992410602531944464 ) ) ;
#40407=CARTESIAN_POINT ( 'NONE',  ( 6.854756222516505737, -1.675677847961650313, 1.365199464886861946 ) ) ;
#40409=CARTESIAN_POINT ( 'NONE',  ( 5.958471553546731414, 1.734833135700924345, 1.507719323494296937 ) ) ;
#40412=CARTESIAN_POINT ( 'NONE',  ( 5.506679003988666388, 1.415762158562785533, -1.222804595763474333 ) ) ;
#40413=CARTESIAN_POINT ( 'NONE',  ( 3.199369407753744454, 1.726971514772487559, -0.8218122705464236954 ) ) ;
#40415=CARTESIAN_POINT ( 'NONE',  ( 5.321004863918796346, 2.037934703285459115, 0.8473243778325880715 ) ) ;
#40416=CARTESIAN_POINT ( 'NONE',  ( 4.962167979565689002, -1.173633690672538865, 1.762117774576977602 ) ) ;
#40418=CARTESIAN_POINT ( 'NONE',  ( 6.883263157960366918, 2.433703524355503411, 2.428201320676713237 ) ) ;
#40421=CARTESIAN_POINT ( 'NONE',  ( 6.147156607449644206, 0.2074554230099104890, 2.110329589018632657 ) ) ;
#40422=CARTESIAN_POINT ( 'NONE',  ( 1.940857006665818174, 2.282658722630509729, 0.3375727702036589450 ) ) ;
#40423=CARTESIAN_POINT ( 'NONE',  ( 3.314850587115983238, -1.487306837207631238, 1.279512770686676681 ) ) ;
#40425=CARTESIAN_POINT ( 'NONE',  ( 6.332891742935283119, -1.956728314951971637, -0.6523575503349694493 ) ) ;
#40430=CARTESIAN_POINT ( 'NONE',  ( 5.928922775424462444, -1.700964743930567513, 1.082835439959836776 ) ) ;
#40432=CARTESIAN_POINT ( 'NONE',  ( -0.07900062026858570285, 7.629137130509076492, -2.773896239169175271 ) ) ;
#40434=CARTESIAN_POINT ( 'NONE',  ( 2.079201016916156330, 2.024566655493876155, 0.7844037353602287821 ) ) ;
#40437=CARTESIAN_POINT ( 'NONE',  ( 0.2113915902133572944, 1.759560880827226947, -1.183302968686468226 ) ) ;
#40442=CARTESIAN_POINT ( 'NONE',  ( 0.6321923500852930644, 1.061553894661429576, -1.766199267744901658 ) ) ;
#40447=CARTESIAN_POINT ( 'NONE',  ( 3.809155001108741612, 1.613891119516493777, -1.025466636117925212 ) ) ;
#40448=CARTESIAN_POINT ( 'NONE',  ( 4.979261681649114202, 1.650653357529890730, -0.6390028274257038010 ) ) ;
#40451=CARTESIAN_POINT ( 'NONE',  ( 0.4217375466794699435, -1.802849824360297060, 0.1778772001973498718 ) ) ;
#40453=CARTESIAN_POINT ( 'NONE',  ( 6.134394303309665730, 0.6061128391178214336, 1.817247008912269646 ) ) ;
#40454=CARTESIAN_POINT ( 'NONE',  ( 1.064989848632340363, 1.568927673159369762, -1.351003706900590018 ) ) ;
#40456=CARTESIAN_POINT ( 'NONE',  ( 5.981297838379462384, 1.727768277425823396, -0.7175292643646775659 ) ) ;
#40457=CARTESIAN_POINT ( 'NONE',  ( 2.719161800852238464, -0.1789327596440904167, 1.816892639718168390 ) ) ;
#40458=CARTESIAN_POINT ( 'NONE',  ( 5.883472226557855400, 2.040502603023553796, -0.8411249186189362348 ) ) ;
#40462=CARTESIAN_POINT ( 'NONE',  ( 3.174340740746087075, -1.014436240984006865, -1.795896229016210821 ) ) ;
#40468=CARTESIAN_POINT ( 'NONE',  ( 6.391088794356012848, 0.1989163192229244648, 2.060770550043041993 ) ) ;
#40470=CARTESIAN_POINT ( 'NONE',  ( 3.427187520701843404, 0.04928524951339217919, 2.161187641841005647 ) ) ;
#40471=CARTESIAN_POINT ( 'NONE',  ( 4.793620647492384812, 1.883690600511141566, -0.7290150168693364519 ) ) ;
#40472=CARTESIAN_POINT ( 'NONE',  ( 2.400770673373255448, 0.4268909467371252431, 1.914702609522442867 ) ) ;
#40473=CARTESIAN_POINT ( 'NONE',  ( 6.620655732516652847, 2.941130357193070033, 2.725706755162327966 ) ) ;
#40478=CARTESIAN_POINT ( 'NONE',  ( 2.167204200501818612, 1.841733140229084853, -0.8216742516050157263 ) ) ;
#40482=CARTESIAN_POINT ( 'NONE',  ( 6.064708884584704585, 0.6063723501847050334, 1.813766235492550560 ) ) ;
#40486=CARTESIAN_POINT ( 'NONE',  ( 4.482046101484723266, -2.016035353076811809, -0.04666016718203602753 ) ) ;
#40489=CARTESIAN_POINT ( 'NONE',  ( 6.457991230880992362, 1.719707694194565484, -0.1327171722449934921 ) ) ;
#40493=CARTESIAN_POINT ( 'NONE',  ( 4.270664716992385479, -1.744513905240049567, -0.6754176267826096369 ) ) ;
#40494=CARTESIAN_POINT ( 'NONE',  ( -0.02900071798685524560, -0.004641455105012376459, -2.173770343569726649 ) ) ;
#40496=CARTESIAN_POINT ( 'NONE',  ( 1.745070579777140418, -0.2997347613497360896, -2.048299739058518920 ) ) ;
#40501=CARTESIAN_POINT ( 'NONE',  ( 6.639320575229251453, 0.008029245381881154262, 1.796863947021019481 ) ) ;
#40509=CARTESIAN_POINT ( 'NONE',  ( 6.503544296663656077, -1.856690447402360888, 0.4709783565581044940 ) ) ;
#40517=CARTESIAN_POINT ( 'NONE',  ( 3.520547545725543515, 1.372905562624787024, -1.669742455111824508 ) ) ;
#40520=CARTESIAN_POINT ( 'NONE',  ( 0.5277791401020451856, -0.3051165123582540994, 2.098401203810342786 ) ) ;
#40521=CARTESIAN_POINT ( 'NONE',  ( 5.913091143547533513, 1.611232972626057247, 0.8583240166551918682 ) ) ;
#40522=CARTESIAN_POINT ( 'NONE',  ( 1.282427153303007605, -1.922404290768309432, -0.4359020612285709473 ) ) ;
#40523=CARTESIAN_POINT ( 'NONE',  ( 3.023589307540079041, -0.3687504995396119201, 1.876329818327879817 ) ) ;
#40525=DIRECTION ( 'NONE',  ( -1.000000000000000000, 1.014813233446432150E-15, 1.972152263052529514E-31 ) ) ;
#40526=CARTESIAN_POINT ( 'NONE',  ( 5.459413677600381654, 1.609035625656387802, 1.135536449648701041 ) ) ;
#40527=CARTESIAN_POINT ( 'NONE',  ( 0.8670093773819181893, 1.871751486835357747, -0.5171616756182734198 ) ) ;
#40533=CARTESIAN_POINT ( 'NONE',  ( 4.986922676292999235, -1.801926769106906745, -0.6406197933803285949 ) ) ;
#40536=CARTESIAN_POINT ( 'NONE',  ( 1.325528760500709780, -0.05309137938146882979, 2.206304558879538025 ) ) ;
#40538=CARTESIAN_POINT ( 'NONE',  ( 6.586586637485376983, -1.237022783311360730, 1.588989491490456762 ) ) ;
#40542=CARTESIAN_POINT ( 'NONE',  ( 2.260293373024503616, -2.069953001785612479, 0.04851313490940312168 ) ) ;
#40545=CARTESIAN_POINT ( 'NONE',  ( 0.7608789386071808103, -1.564954856162886765, 1.491513986042219297 ) ) ;
#40552=CARTESIAN_POINT ( 'NONE',  ( 6.825078400183574701, 6.039200712630649726, 2.350557101739355392 ) ) ;
#40554=CARTESIAN_POINT ( 'NONE',  ( 4.816919938037654170, 0.8852131329995099884, -1.491020713638806949 ) ) ;
#40556=CARTESIAN_POINT ( 'NONE',  ( 1.920843890195075510, -1.466934385316904565, 1.461102248941518855 ) ) ;
#40557=CARTESIAN_POINT ( 'NONE',  ( 3.497769638136785986, -2.085511745926827309, 0.3643098080348127765 ) ) ;
#40560=CARTESIAN_POINT ( 'NONE',  ( 1.446085390411493199, -0.8901679511373729037, 1.756898273940428634 ) ) ;
#40563=CARTESIAN_POINT ( 'NONE',  ( 3.820531118927258607, 2.176299813863972865, 0.7200661129266039406 ) ) ;
#40564=CARTESIAN_POINT ( 'NONE',  ( 2.262075381241589245, 0.7800679334904643270, 1.650788133108482825 ) ) ;
#40570=CARTESIAN_POINT ( 'NONE',  ( 2.584242159373177028, 1.080601423880021894, 1.698455611904861495 ) ) ;
#40571=CARTESIAN_POINT ( 'NONE',  ( 3.063279882407277999, 1.654721480355027863, 1.053479689057647217 ) ) ;
#40574=CARTESIAN_POINT ( 'NONE',  ( 0.07516593201273641389, 2.869485459350088696, -2.532657826882792840 ) ) ;
#40575=CARTESIAN_POINT ( 'NONE',  ( 5.894497796308646009, 1.709714471583067885, -1.202884697265863778 ) ) ;
#40576=CARTESIAN_POINT ( 'NONE',  ( 4.170580646280578563, -1.651567487535645640, -0.6365977468129493388 ) ) ;
#40578=CARTESIAN_POINT ( 'NONE',  ( 1.183813618819636870, -0.9825931803647185436, 1.958887836816553429 ) ) ;
#40579=CARTESIAN_POINT ( 'NONE',  ( 5.788919933143140462, 1.322006966288125085, 1.131936178618123456 ) ) ;
#40582=CARTESIAN_POINT ( 'NONE',  ( 6.117888908451988073, 0.2214900195740623634, 2.288030219478351057 ) ) ;
#40585=CARTESIAN_POINT ( 'NONE',  ( 5.184772435558752335, -0.9287019638352255191, -1.463892056132688024 ) ) ;
#40586=CARTESIAN_POINT ( 'NONE',  ( 1.770444396619451632, 1.136427050704125419, 1.891651738277564831 ) ) ;
#40587=CARTESIAN_POINT ( 'NONE',  ( 5.635278836315742446, -0.04772081403418790974, -2.170810874590335171 ) ) ;
#40589=CARTESIAN_POINT ( 'NONE',  ( 1.534521455381025801, 0.6695800964386169341, 2.008721144947374526 ) ) ;
#40590=CARTESIAN_POINT ( 'NONE',  ( 4.281250000000002665, 0.7852924748302082536, 1.895863743163987980 ) ) ;
#40592=CARTESIAN_POINT ( 'NONE',  ( 4.172816426537079515, -1.797186248846779133, -0.6940461778226751921 ) ) ;
#40593=CARTESIAN_POINT ( 'NONE',  ( 0.7334294796089964041, 2.054545164755026576, 0.8448789909778311458 ) ) ;
#40598=CARTESIAN_POINT ( 'NONE',  ( 3.334858576441266376, 1.407893888572855801, -1.718160706149525430 ) ) ;
#40605=CARTESIAN_POINT ( 'NONE',  ( 1.670546294658280084, 1.392546765991018454, 1.458555661489918442 ) ) ;
#40607=CARTESIAN_POINT ( 'NONE',  ( 0.3212321915853528220, -1.840712657873358138, -0.9308276203483353273 ) ) ;
#40610=CARTESIAN_POINT ( 'NONE',  ( -0.1121326479804653220, -0.4008509640632436088, -1.803546454093779561 ) ) ;
#40614=CARTESIAN_POINT ( 'NONE',  ( 1.018396826474694761, 1.632260513341069252, 0.6844030214382245125 ) ) ;
#40615=CARTESIAN_POINT ( 'NONE',  ( -0.1224325501351306023, -0.4448023855274513272, -1.973852191825019364 ) ) ;
#40616=CARTESIAN_POINT ( 'NONE',  ( 0.1867156058280826092, 1.363667594142993877, 1.237386390646778578 ) ) ;
#40617=CARTESIAN_POINT ( 'NONE',  ( 4.458679977242249848, -2.047270833213535202, -1.031427349252316272 ) ) ;
#40618=CARTESIAN_POINT ( 'NONE',  ( 2.255570300226293234, 0.7868700230135963203, 1.664660379391752043 ) ) ;
#40622=CARTESIAN_POINT ( 'NONE',  ( 3.504746488097260748, 1.439749907568649068, -1.122338611188322455 ) ) ;
#40623=CARTESIAN_POINT ( 'NONE',  ( 4.113907844847329187, 0.1017495355152969322, 2.013985960686740295 ) ) ;
#40625=CARTESIAN_POINT ( 'NONE',  ( 3.678848304420906601, -2.179822953419420006, -0.6058417560294343529 ) ) ;
#40627=CARTESIAN_POINT ( 'NONE',  ( 5.895568648972373538, 1.592330039046478740, 1.378332891347531231 ) ) ;
#40629=CARTESIAN_POINT ( 'NONE',  ( 3.051297593704501043, 1.777051743073382761, -1.062048545217339823 ) ) ;
#40632=CARTESIAN_POINT ( 'NONE',  ( 6.059260758684835046, -1.791542317298041365, 1.134111293253435182 ) ) ;
#40634=CARTESIAN_POINT ( 'NONE',  ( 0.8559318490590170914, 1.924348548886562815, -0.09362981192203097269 ) ) ;
#40642=CARTESIAN_POINT ( 'NONE',  ( 0.3521972369381949908, -1.576644756679127513, -1.565149006781616725 ) ) ;
#40643=CARTESIAN_POINT ( 'NONE',  ( 2.415183150638998466, 1.880743233677120818, 0.9477269459148714992 ) ) ;
#40646=CARTESIAN_POINT ( 'NONE',  ( 6.157066405694873623, 1.522017207847397469, -1.070502804743376668 ) ) ;
#40653=CARTESIAN_POINT ( 'NONE',  ( -0.05226516427493665962, -1.936187138999283297, 0.8653993394739032397 ) ) ;
#40656=CARTESIAN_POINT ( 'NONE',  ( 2.857805160684105950, -0.6180756922911297968, 1.862011555624979886 ) ) ;
#40657=CARTESIAN_POINT ( 'NONE',  ( 2.342841879718413622, 0.4729757327756216601, 2.109170662781891359 ) ) ;
#40661=CARTESIAN_POINT ( 'NONE',  ( 4.066134141799277124, -1.624876214689898957, -0.6237973674530649104 ) ) ;
#40664=CARTESIAN_POINT ( 'NONE',  ( 0.4269344243218140544, 2.069031678568326704, 0.6260965431626740463 ) ) ;
#40665=CARTESIAN_POINT ( 'NONE',  ( 1.792342068719571468, -1.899328565777322231, 0.6766080823841430503 ) ) ;
#40668=CARTESIAN_POINT ( 'NONE',  ( 2.483225996990960027, 1.803144932609510143, -0.7974705804912070040 ) ) ;
#40675=CARTESIAN_POINT ( 'NONE',  ( 2.490883850439883140, -1.933321517186505245, -0.5842891067564592866 ) ) ;
#40677=CARTESIAN_POINT ( 'NONE',  ( 6.141700272255690152, -1.665644196019906875, -1.597301777034014991 ) ) ;
#40679=CARTESIAN_POINT ( 'NONE',  ( 2.764445781119912127, -0.7462812867886670087, -1.814464804917370166 ) ) ;
#40681=CARTESIAN_POINT ( 'NONE',  ( 1.125625214514534900, 0.3961039030971892916, 1.976955501819408711 ) ) ;
#40683=CARTESIAN_POINT ( 'NONE',  ( 2.360703550434081421, -2.027734997378250359, -0.6095688489828243739 ) ) ;
#40686=CARTESIAN_POINT ( 'NONE',  ( 2.361056629804247020, 1.805642548105116596, -0.3588866333120652174 ) ) ;
#40690=CARTESIAN_POINT ( 'NONE',  ( 4.447591161967184625, -1.937652164471121763, 0.8620916771790232414 ) ) ;
#40691=CARTESIAN_POINT ( 'NONE',  ( 0.6558947131179297951, -1.335331635844772880, 1.267786537210900510 ) ) ;
#40695=CARTESIAN_POINT ( 'NONE',  ( 4.762995170230669650, -1.839058295199582638, -0.9300793793675359300 ) ) ;
#40697=CARTESIAN_POINT ( 'NONE',  ( 1.768857366986800184, 1.761637791510446860, -0.5354853023365884201 ) ) ;
#40701=CARTESIAN_POINT ( 'NONE',  ( 1.278255639411193245, 1.316999024263129092, 1.770685722221450709 ) ) ;
#40702=CARTESIAN_POINT ( 'NONE',  ( 4.095213043127944097, 1.914038588809761299, -1.205934879490217382 ) ) ;
#40704=CARTESIAN_POINT ( 'NONE',  ( 3.234412676589659252, 1.145595053071927438, -1.403395578055862902 ) ) ;
#40705=CARTESIAN_POINT ( 'NONE',  ( 2.922943415214097396, -1.687269874283424453, 0.9073053738915691779 ) ) ;
#40706=CARTESIAN_POINT ( 'NONE',  ( 4.598136200040512378, 0.8882050449813773119, -1.870312673664726644 ) ) ;
#40708=CARTESIAN_POINT ( 'NONE',  ( 2.676590784821473168, -1.886132711224804748, -0.5737105244360584111 ) ) ;
#40709=CARTESIAN_POINT ( 'NONE',  ( 1.272347295514785870, -1.224129819625971782, 1.487435282370595857 ) ) ;
#40710=CARTESIAN_POINT ( 'NONE',  ( 4.469519713540137218, 1.814478506493342191, -0.4545110902946307152 ) ) ;
#40711=CARTESIAN_POINT ( 'NONE',  ( 1.858496626375233163, 2.301273984257983241, -0.1728945724901974068 ) ) ;
#40712=CARTESIAN_POINT ( 'NONE',  ( 3.947575701020007877, 1.346737928234511106, 1.284688856454605732 ) ) ;
#40717=CARTESIAN_POINT ( 'NONE',  ( 0.8210893850928849824, 1.946682464879319729, 0.8042085006434143146 ) ) ;
#40721=CARTESIAN_POINT ( 'NONE',  ( 6.919229410208834530, -0.1638780278429008419, 2.126154539342207883 ) ) ;
#40722=CARTESIAN_POINT ( 'NONE',  ( 1.635180430577408028, 1.980530345366804834, 0.7584260845197098311 ) ) ;
#40724=CARTESIAN_POINT ( 'NONE',  ( 0.4045644467639066821, -2.005039209919571075, -0.2428365769681257724 ) ) ;
#40728=CARTESIAN_POINT ( 'NONE',  ( 0.8433209000573947955, -1.854398715148808385, 1.110445933987347367 ) ) ;
#40730=CARTESIAN_POINT ( 'NONE',  ( 6.825078400183588023, 6.037369320589220045, 2.550557596425677254 ) ) ;
#40733=CARTESIAN_POINT ( 'NONE',  ( 5.893767612163585135, -2.000732204962274441, 0.2516274335107801519 ) ) ;
#40735=CARTESIAN_POINT ( 'NONE',  ( 0.3104468679729632807, 1.506874830639578056, -1.591553791636945991 ) ) ;
#40737=CARTESIAN_POINT ( 'NONE',  ( 0.7435140528431654072, -1.938958340150579662, 1.165708873083745045 ) ) ;
#40741=CARTESIAN_POINT ( 'NONE',  ( 0.6498251619827577485, 0.9450094616851455465, 1.666218678892321226 ) ) ;
#40746=CARTESIAN_POINT ( 'NONE',  ( 3.246439759211931175, 0.4201230555563889579, 1.672790298054289693 ) ) ;
#40748=CARTESIAN_POINT ( 'NONE',  ( 0.4558546072216109191, 0.6692488815305540628, 1.638537551351123112 ) ) ;
#40749=CARTESIAN_POINT ( 'NONE',  ( 1.594390828295478402, -1.075120693119306692, 1.701777395020438899 ) ) ;
#40752=CARTESIAN_POINT ( 'NONE',  ( 4.682781310676605635, -2.139571651222616833, -0.5399477217277389718 ) ) ;
#40757=CARTESIAN_POINT ( 'NONE',  ( 4.002672028760116518, -2.097606743168555443, -0.3097674545872729501 ) ) ;
#40758=CARTESIAN_POINT ( 'NONE',  ( 3.567982607561688280, -0.9913820634350966055, 1.755780237201590488 ) ) ;
#40759=CARTESIAN_POINT ( 'NONE',  ( 3.093827002871222920, 1.152939038403834493, 1.397299590375496336 ) ) ;
#40760=VERTEX_POINT ( 'NONE', #181101 ) ;
#40764=CARTESIAN_POINT ( 'NONE',  ( 1.850267049257280139, 0.5840378008528935849, 1.777222254475477659 ) ) ;
#40767=CARTESIAN_POINT ( 'NONE',  ( 5.742758765878789085, 0.3605303665093100851, 1.789564367143759327 ) ) ;
#40777=CARTESIAN_POINT ( 'NONE',  ( 4.553055379497691568, 0.3652949536288411791, 2.088752307168060707 ) ) ;
#40778=CARTESIAN_POINT ( 'NONE',  ( -0.1294898018151837138, 2.036186877494918335, -2.343407025977122693 ) ) ;
#40780=CARTESIAN_POINT ( 'NONE',  ( 5.184826486558015368, -0.2386506126292788632, -1.956774853079599197 ) ) ;
#40782=CARTESIAN_POINT ( 'NONE',  ( 0.0002439367322616680669, -0.9454701154091667004, 1.777349279628215095 ) ) ;
#40784=CARTESIAN_POINT ( 'NONE',  ( 0.4568545718052554050, -1.995212666551810399, -0.7087754862673681933 ) ) ;
#40786=CARTESIAN_POINT ( 'NONE',  ( 1.205626512970816355, -1.630946839658468983, -1.275175305487465049 ) ) ;
#40791=CARTESIAN_POINT ( 'NONE',  ( 3.521503319566265944, -1.245636697800769355, -1.678868242315070258 ) ) ;
#40794=CARTESIAN_POINT ( 'NONE',  ( 2.414841169274529520, 1.629557050654990791, 0.8231356554938076275 ) ) ;
#40795=CARTESIAN_POINT ( 'NONE',  ( 1.224954274949443978, 1.597400116765529843, 0.8541874478597778486 ) ) ;
#40797=CARTESIAN_POINT ( 'NONE',  ( 5.514374426699260923, -0.9893691592960799364, -1.972764877262770833 ) ) ;
#40799=CARTESIAN_POINT ( 'NONE',  ( 4.542132036680512464, 0.9468659437555368985, -1.993456357439137960 ) ) ;
#40801=CARTESIAN_POINT ( 'NONE',  ( 2.859904825981678833, 0.6862549603197342085, -1.785085608301796523 ) ) ;
#40804=CARTESIAN_POINT ( 'NONE',  ( 5.195788487752976081, -1.461605715988937515, -1.466586839339318660 ) ) ;
#40806=CARTESIAN_POINT ( 'NONE',  ( 5.882419586753742102, -0.3201050945752722532, -2.167950725039065052 ) ) ;
#40816=CARTESIAN_POINT ( 'NONE',  ( 5.770397209236588942, -0.9257025293247715947, -1.851810055641222252 ) ) ;
#40817=CARTESIAN_POINT ( 'NONE',  ( 4.389231790275191614, 1.720148140252445668, -0.8676111672119514173 ) ) ;
#40818=CARTESIAN_POINT ( 'NONE',  ( 0.2808753465170962249, 1.674874268995883320, -1.122520385770640061 ) ) ;
#40822=CARTESIAN_POINT ( 'NONE',  ( 0.09403522832084068583, -2.191061582759439297, -0.04926842934906834615 ) ) ;
#40823=CARTESIAN_POINT ( 'NONE',  ( 5.092344371507952161, -1.812320225013038133, -0.2200062734805732223 ) ) ;
#40831=CARTESIAN_POINT ( 'NONE',  ( 2.313779677144182312, 1.201330555204615180, -1.395457044143719072 ) ) ;
#40832=CARTESIAN_POINT ( 'NONE',  ( 6.047140908842845164, 0.2017661761196144488, 2.003097277516131758 ) ) ;
#40833=CARTESIAN_POINT ( 'NONE',  ( 1.933413756328787869, 1.181669745456917830, 1.971221161662185528 ) ) ;
#40834=CARTESIAN_POINT ( 'NONE',  ( 0.3560157238547481118, -1.860367465765656814, -0.05377290132800408712 ) ) ;
#40840=CARTESIAN_POINT ( 'NONE',  ( 2.771125873548622831, 1.984386128312282116, -0.6585125772022564217 ) ) ;
#40841=CARTESIAN_POINT ( 'NONE',  ( 0.6373110600932235803, -1.319858442276698129, -1.325903642019378381 ) ) ;
#40842=CARTESIAN_POINT ( 'NONE',  ( 1.669295836627190610, -0.7230268306642473330, -1.882186858670406693 ) ) ;
#40846=CARTESIAN_POINT ( 'NONE',  ( 2.208218529973245303, 1.555207145793806811, 0.7814158636046761863 ) ) ;
#40851=CARTESIAN_POINT ( 'NONE',  ( 3.369487540355073030, 1.682505700701863338, -0.3791672619692722512 ) ) ;
#40852=CARTESIAN_POINT ( 'NONE',  ( 2.402122600552298870, -0.8417629408748151798, -2.023652355447076001 ) ) ;
#40854=CARTESIAN_POINT ( 'NONE',  ( 5.391335350415090488, 1.947751002805158560, -1.037606470750504828 ) ) ;
#40856=CARTESIAN_POINT ( 'NONE',  ( 2.061612764771907802, 1.803244147071264125, 1.208790786097496905 ) ) ;
#40857=CARTESIAN_POINT ( 'NONE',  ( 0.9964003531478006215, -0.4411313887022934033, -1.771462291394958255 ) ) ;
#40858=SURFACE_STYLE_USAGE ( .BOTH. , #90675 ) ;
#40859=CARTESIAN_POINT ( 'NONE',  ( 4.680926624126137803, 1.758507693093620539, -1.179036559061322542 ) ) ;
#40860=CARTESIAN_POINT ( 'NONE',  ( 6.539320575229274901, 7.629137130509072051, 2.496737603865983424 ) ) ;
#40861=EDGE_LOOP ( 'NONE', ( #136928, #49291 ) ) ;
#40863=CARTESIAN_POINT ( 'NONE',  ( 4.300488954165425426, 1.772315894223834176, -1.453880271152303116 ) ) ;
#40867=CARTESIAN_POINT ( 'NONE',  ( -0.09290056220616692284, -0.4702265987995763452, -2.075310686570643437 ) ) ;
#40873=CARTESIAN_POINT ( 'NONE',  ( 4.764296165657141202, 1.880435471729305030, -0.7283773170061805802 ) ) ;
#40875=CARTESIAN_POINT ( 'NONE',  ( 3.573143115351416377, 1.862571710426489169, 0.8863520062180642034 ) ) ;
#40877=CARTESIAN_POINT ( 'NONE',  ( -0.1411974294642202310, 0.2398548052158452348, -1.934266582396115819 ) ) ;
#40881=CARTESIAN_POINT ( 'NONE',  ( 5.666036703420031628, -1.392593631063457682, 1.692088878451535106 ) ) ;
#40882=CARTESIAN_POINT ( 'NONE',  ( 3.481092415823695774, -2.014232707597499505, -0.09613569647320965861 ) ) ;
#40883=CARTESIAN_POINT ( 'NONE',  ( 3.263068207883256466, 1.795673413606920565, -0.4063787724192802209 ) ) ;
#40886=CARTESIAN_POINT ( 'NONE',  ( 0.1469036390603413456, -1.327996847208750442, -1.100432056080926202 ) ) ;
#40888=CARTESIAN_POINT ( 'NONE',  ( 6.807534431281101028, -0.5077146954460194372, 2.213219090469565664 ) ) ;
#40889=CARTESIAN_POINT ( 'NONE',  ( 1.752698641044206251, 0.6620485714215967876, 1.999371444633216033 ) ) ;
#40898=CARTESIAN_POINT ( 'NONE',  ( 4.342156631555553759, -1.367984123109561301, -1.750111109629876260 ) ) ;
#40899=CARTESIAN_POINT ( 'NONE',  ( 2.273600812266802773, 1.349468827467028120, 1.726581335083368307 ) ) ;
#40900=CARTESIAN_POINT ( 'NONE',  ( 0.7334016978863610037, 0.1661181961954381059, 2.200687262777756725 ) ) ;
#40902=CARTESIAN_POINT ( 'NONE',  ( 4.281663391851794565, -1.878042059144067633, 0.5673916069991248312 ) ) ;
#40906=CARTESIAN_POINT ( 'NONE',  ( 6.610000000000021636, 3.695490760540712127, 2.514297579034238783 ) ) ;
#40908=VERTEX_POINT ( 'NONE', #199461 ) ;
#40909=CARTESIAN_POINT ( 'NONE',  ( 3.515986968957810266, -0.6120941298391362473, 2.030368431519948391 ) ) ;
#40911=CARTESIAN_POINT ( 'NONE',  ( 5.717692609583751029, -2.109997883074541392, 0.4692839721026839661 ) ) ;
#40912=CARTESIAN_POINT ( 'NONE',  ( 4.458453498679889826, -1.646799808365447371, -0.8236825204945983359 ) ) ;
#40915=CARTESIAN_POINT ( 'NONE',  ( 0.02830193721903468546, -1.592744100209501967, 0.7021035195741828216 ) ) ;
#40916=CARTESIAN_POINT ( 'NONE',  ( 6.727182134110201162, 1.271184308336456015, 2.025152302351560518 ) ) ;
#40919=CARTESIAN_POINT ( 'NONE',  ( 4.047864428982482110, 0.7307185629543844207, -2.034579650689218866 ) ) ;
#40922=CARTESIAN_POINT ( 'NONE',  ( 6.028672669474048007, 1.986741788447304646, -0.3418859329693338944 ) ) ;
#40926=CARTESIAN_POINT ( 'NONE',  ( 3.696290335837215668, -2.159122111672501454, -0.1082323872379290647 ) ) ;
#40927=CARTESIAN_POINT ( 'NONE',  ( 3.708241208800214572, -0.7959428688352770953, -1.803694655455597262 ) ) ;
#40929=CARTESIAN_POINT ( 'NONE',  ( 0.6050338814152752542, -0.7811975584859867094, -2.171474816401474328 ) ) ;
#40930=CARTESIAN_POINT ( 'NONE',  ( 3.180987545930415106, -0.1479678519747235910, -2.055505606019301990 ) ) ;
#40931=CARTESIAN_POINT ( 'NONE',  ( 5.495633776345048460, -1.942234966517431660, 0.004081557570839721392 ) ) ;
#40937=CARTESIAN_POINT ( 'NONE',  ( 2.678998284833411070, -2.111460168698295004, -0.6414983429729387288 ) ) ;
#40940=CARTESIAN_POINT ( 'NONE',  ( 0.6900174830311635032, 0.9632304765912635958, -1.592144255797292463 ) ) ;
#40941=CARTESIAN_POINT ( 'NONE',  ( -0.1290005225502918740, 6.946858002156244716, -2.769053915224591211 ) ) ;
#40946=CARTESIAN_POINT ( 'NONE',  ( 5.279192629422701621, 1.239228542960477242, 1.361826556748657602 ) ) ;
#40948=CARTESIAN_POINT ( 'NONE',  ( 2.272404554480491168, -1.268947053487592846, 1.623793324639089874 ) ) ;
#40954=CARTESIAN_POINT ( 'NONE',  ( 1.235309500465184396, -1.863545150897191416, 0.8803144705526543268 ) ) ;
#40956=CARTESIAN_POINT ( 'NONE',  ( 4.581507094455529838, -0.8636776874328588871, 1.626104626046148249 ) ) ;
#40959=CARTESIAN_POINT ( 'NONE',  ( -0.2409995289980003397, 0.7158067089181943121, -2.082568332340509087 ) ) ;
#40962=CARTESIAN_POINT ( 'NONE',  ( 3.967548030458594166, 0.2710504330169676845, -2.190103208553782821 ) ) ;
#40963=CARTESIAN_POINT ( 'NONE',  ( 0.2105424042340813540, -0.9235240298187572527, -1.952328634516012684 ) ) ;
#40964=CARTESIAN_POINT ( 'NONE',  ( 3.714077560468319827, 1.074663192196689376, -1.706111893292367343 ) ) ;
#40966=CARTESIAN_POINT ( 'NONE',  ( -0.07025823700084612988, -1.875094440630159065, 0.3749275819610526916 ) ) ;
#40967=CARTESIAN_POINT ( 'NONE',  ( 0.4445464637146989695, -1.457232572767804379, 1.394089106691732693 ) ) ;
#40969=CARTESIAN_POINT ( 'NONE',  ( 0.07536363704233049743, 2.002983476668462881, -2.558365315478607904 ) ) ;
#40972=CARTESIAN_POINT ( 'NONE',  ( 0.3033014811697418711, -0.5033704626738467747, 1.801585485020948951 ) ) ;
#40973=CARTESIAN_POINT ( 'NONE',  ( 2.624232735793774030, 2.001858099149746550, 0.2420302859193757539 ) ) ;
#40977=CARTESIAN_POINT ( 'NONE',  ( 3.545630178961965751, -1.594748897588176950, -1.375714639268589279 ) ) ;
#40982=CARTESIAN_POINT ( 'NONE',  ( 4.658466178349073061, 2.014666459302273616, 0.1442823096002471550 ) ) ;
#40985=CARTESIAN_POINT ( 'NONE',  ( 4.270900206319126369, -2.015198044118733822, -0.7823990653590962019 ) ) ;
#40991=CARTESIAN_POINT ( 'NONE',  ( 2.506498380571024143, 2.170641363890627229, 0.05523593993728668355 ) ) ;
#40994=CARTESIAN_POINT ( 'NONE',  ( 1.153568636672014369, 0.7464410156945017194, 1.683350060182234209 ) ) ;
#40996=CARTESIAN_POINT ( 'NONE',  ( 3.614928802375876771, -0.1595779646587774658, 2.185787688459623901 ) ) ;
#40998=CARTESIAN_POINT ( 'NONE',  ( 3.555803421180541157, 0.5519491744547943002, -2.194038648399123215 ) ) ;
#41006=CARTESIAN_POINT ( 'NONE',  ( 5.905463120178883862, -0.4284811148945049109, 1.716917210449308673 ) ) ;
#41008=CARTESIAN_POINT ( 'NONE',  ( 0.9562493570349944738, 2.103547740682055966, -0.1031677049159150372 ) ) ;
#41011=CARTESIAN_POINT ( 'NONE',  ( 1.346085547170269070, -0.8884179423524626307, 1.757888261374307870 ) ) ;
#41015=CARTESIAN_POINT ( 'NONE',  ( 5.836161222118039227, -1.013825144121174526, -1.501122385605196952 ) ) ;
#41020=CARTESIAN_POINT ( 'NONE',  ( 4.821099876132087125, -0.09137817997613774390, 1.868553921495450965 ) ) ;
#41022=CARTESIAN_POINT ( 'NONE',  ( 4.118080132427735407, 2.055207691244304691, -0.2483996215696740451 ) ) ;
#41031=CARTESIAN_POINT ( 'NONE',  ( 4.123457186961496213, 0.2424046295769199388, -1.946780420294342617 ) ) ;
#41032=CARTESIAN_POINT ( 'NONE',  ( 1.739611019359630584, -1.913509794028777522, -0.6351045200190530426 ) ) ;
#41034=CARTESIAN_POINT ( 'NONE',  ( -0.1108833634136781182, 7.629137130509072939, -2.496956624467902675 ) ) ;
#41036=CARTESIAN_POINT ( 'NONE',  ( 1.669004442688322154, 0.1428430569143137041, -1.865171992484420338 ) ) ;
#41038=CARTESIAN_POINT ( 'NONE',  ( 3.709243207436668577, 1.698441389738635676, -1.080623863572414356 ) ) ;
#41041=CARTESIAN_POINT ( 'NONE',  ( 2.847379581703746609, 0.3079039886237054935, -2.094596350150164987 ) ) ;
#41043=CARTESIAN_POINT ( 'NONE',  ( 4.615722581382986967, 0.4567890626981512270, -2.019179087418949692 ) ) ;
#41045=CARTESIAN_POINT ( 'NONE',  ( -0.1234093946873336678, -0.1598125250084568849, -2.056614676860648583 ) ) ;
#41046=CARTESIAN_POINT ( 'NONE',  ( 6.620655732516684822, 2.041257794637734602, 2.379778264366624096 ) ) ;
#41047=CARTESIAN_POINT ( 'NONE',  ( 4.911078036072877850, 1.588895129109271220, 0.8988584441092376531 ) ) ;
#41055=CARTESIAN_POINT ( 'NONE',  ( -0.005635951793048382327, -1.756493610686832740, -0.4425278525194314971 ) ) ;
#41065=CARTESIAN_POINT ( 'NONE',  ( 5.519157712072518152, -1.821736412749059397, 0.8647389720048551665 ) ) ;
#41072=CARTESIAN_POINT ( 'NONE',  ( 2.430458318764291192, -1.215629356985904685, 1.549377053225237111 ) ) ;
#41073=CARTESIAN_POINT ( 'NONE',  ( 4.868767636308747093, -0.2496254991312534810, -2.000855965115163837 ) ) ;
#41075=CARTESIAN_POINT ( 'NONE',  ( 6.827182134110196365, 7.629137130509086262, 2.689055895399253160 ) ) ;
#41076=CARTESIAN_POINT ( 'NONE',  ( 4.734432829848630675, 0.3728853646711489112, 2.159338447334692823 ) ) ;
#41078=CARTESIAN_POINT ( 'NONE',  ( 3.100521554045695627, -0.5575540177290801980, -1.843951249938739378 ) ) ;
#41081=CARTESIAN_POINT ( 'NONE',  ( 0.2060869173217265982, -0.5842117877600698783, 2.128085570573131413 ) ) ;
#41082=CARTESIAN_POINT ( 'NONE',  ( 0.1753634416057497925, 0.0001173177735149660839, -2.144164757042037017 ) ) ;
#41088=CARTESIAN_POINT ( 'NONE',  ( 6.128435733830499998, 0.1874100934057248424, 1.831705376836203936 ) ) ;
#41089=CARTESIAN_POINT ( 'NONE',  ( 2.438141639825658125, -1.160823251276057011, -1.644512180470799834 ) ) ;
#41090=CARTESIAN_POINT ( 'NONE',  ( 4.833568131691490244, -1.505864581002622105, 1.736428821378619647 ) ) ;
#41092=CARTESIAN_POINT ( 'NONE',  ( 3.502650316321722634, 0.4479755722775873861, 1.806107967122023927 ) ) ;
#41098=CARTESIAN_POINT ( 'NONE',  ( 6.110894567773135222, -0.2550301881006194482, 2.075043241552937179 ) ) ;
#41105=CARTESIAN_POINT ( 'NONE',  ( 6.076716319674939193, -1.640139352550730401, -0.5342243915677049593 ) ) ;
#41107=CARTESIAN_POINT ( 'NONE',  ( 0.8965906023701503136, -0.7780376274850349105, -1.549907966113317270 ) ) ;
#41111=CARTESIAN_POINT ( 'NONE',  ( 5.823135961761455981, -1.959396665126054815, -0.9353919727212963720 ) ) ;
#41112=CARTESIAN_POINT ( 'NONE',  ( 4.688025921862073453, -0.8580590012943272171, 1.611482198803436905 ) ) ;
#41113=CARTESIAN_POINT ( 'NONE',  ( 2.465611527742004760, -0.4346729355233552861, 1.912824223707191296 ) ) ;
#41117=CARTESIAN_POINT ( 'NONE',  ( 3.246849895443252532, 2.069243461727567013, 0.4626693848822636124 ) ) ;
#41121=CARTESIAN_POINT ( 'NONE',  ( 1.692325190600419305, 1.023896122633965566, -1.799289093316607469 ) ) ;
#41124=CARTESIAN_POINT ( 'NONE',  ( 3.598459204466686323, -1.093923138158871433, 1.933176262723006467 ) ) ;
#41126=CARTESIAN_POINT ( 'NONE',  ( 1.354533853113936814, 0.1633331948888619711, -2.292934881128176450 ) ) ;
#41128=CARTESIAN_POINT ( 'NONE',  ( 6.860222192644392258, -2.062229998417430377, 0.04471529749722201463 ) ) ;
#41136=CARTESIAN_POINT ( 'NONE',  ( -0.1102773484824119410, 4.081664357266182819, -2.758211214536327116 ) ) ;
#41137=CARTESIAN_POINT ( 'NONE',  ( 3.451896303776471608, 1.724958192144626867, 0.0007732285732166971348 ) ) ;
#41138=CARTESIAN_POINT ( 'NONE',  ( 2.606657977298726614, 1.900416011228076130, 0.6748465934659984011 ) ) ;
#41139=CARTESIAN_POINT ( 'NONE',  ( 2.532212319380182208, -1.909192193906615209, 1.279991936841210043 ) ) ;
#41140=CARTESIAN_POINT ( 'NONE',  ( 3.673342012549928981, 0.05998355446043589223, -2.261782774625902714 ) ) ;
#41141=CARTESIAN_POINT ( 'NONE',  ( 5.461587592249073531, 0.4120570304669196604, -2.065184316587692415 ) ) ;
#41143=CARTESIAN_POINT ( 'NONE',  ( 4.006921011573481906, 1.516870794648169873, 0.9113941657561406284 ) ) ;
#41146=CARTESIAN_POINT ( 'NONE',  ( 0.2348727637096776621, 0.3982709639365061838, 2.257261336973298338 ) ) ;
#41147=CARTESIAN_POINT ( 'NONE',  ( 6.017501326166345699, -1.026660802952833240, -1.528114487065170390 ) ) ;
#41150=CARTESIAN_POINT ( 'NONE',  ( 5.560537033210596114, -1.979929515673630513, -0.9395970221138388867 ) ) ;
#41153=CARTESIAN_POINT ( 'NONE',  ( 5.687960312649480876, -1.310561514506687564, -1.602779375087557412 ) ) ;
#41154=CARTESIAN_POINT ( 'NONE',  ( 0.5675926644314840397, 1.357872185771633156, 1.490966652548594285 ) ) ;
#41156=CARTESIAN_POINT ( 'NONE',  ( 3.809137074456845795, 1.652770800469059775, 0.9896037298236616264 ) ) ;
#41159=CARTESIAN_POINT ( 'NONE',  ( 6.328397690248316110, -1.000878058022572903, -1.869571840794107986 ) ) ;
#41169=CARTESIAN_POINT ( 'NONE',  ( 1.047228354049560828, 1.731870006261830408, -0.9216698261682305660 ) ) ;
#41173=CARTESIAN_POINT ( 'NONE',  ( 5.529730448059603454, 1.891198321494348633, -0.5216162335564683561 ) ) ;
#41177=CARTESIAN_POINT ( 'NONE',  ( 6.561405286136595905, 0.3748316153167965403, -2.128808860954830795 ) ) ;
#41181=CARTESIAN_POINT ( 'NONE',  ( 1.879943753831798015, -1.004885234286160722, 1.577526331995420472 ) ) ;
#41182=CARTESIAN_POINT ( 'NONE',  ( 0.1583034150156861219, 0.9959709328331721734, 1.419360398433693549 ) ) ;
#41184=CARTESIAN_POINT ( 'NONE',  ( 3.878626735558046157, -0.2160506499642600997, -2.180900317982924275 ) ) ;
#41185=CARTESIAN_POINT ( 'NONE',  ( 4.647712500454345808, -1.780663920513593013, -1.467712336591691313 ) ) ;
#41186=CARTESIAN_POINT ( 'NONE',  ( 6.872340646960426902, -1.271554428311357565, 1.622191329735128029 ) ) ;
#41187=CARTESIAN_POINT ( 'NONE',  ( 2.695178803863579997, -0.6086341500050916897, 1.844178105057793893 ) ) ;
#41190=CARTESIAN_POINT ( 'NONE',  ( 5.291314375706784645, -0.05428322906628547939, -2.120082430678168706 ) ) ;
#41192=CARTESIAN_POINT ( 'NONE',  ( 3.604138833494671346, -0.1455340571130462057, 2.011204217620660817 ) ) ;
#41196=CARTESIAN_POINT ( 'NONE',  ( 1.347985785199314668, 1.823511463271022093, 0.09156768404049858701 ) ) ;
#41201=CARTESIAN_POINT ( 'NONE',  ( 5.471578299931997513, 1.986755592664890324, -0.5475478416450995089 ) ) ;
#41206=CARTESIAN_POINT ( 'NONE',  ( 4.442060220718175856, -1.244341337028841421, -1.590709041654225553 ) ) ;
#41207=CARTESIAN_POINT ( 'NONE',  ( 5.250715360749964589, 2.188191852258320136, 0.3812115871067219275 ) ) ;
#41211=CARTESIAN_POINT ( 'NONE',  ( 4.522374016017603360, 1.269557654445327532, -1.623317902228790910 ) ) ;
#41212=CARTESIAN_POINT ( 'NONE',  ( 3.656875104409584853, 1.122498086849915921, 1.674887873639265390 ) ) ;
#41221=CARTESIAN_POINT ( 'NONE',  ( 3.567732365556259833, 1.591074578583808075, -1.238131541301431549 ) ) ;
#41222=CARTESIAN_POINT ( 'NONE',  ( 2.659893383946440260, -1.269561761542839617, 1.333649727802692198 ) ) ;
#41224=CARTESIAN_POINT ( 'NONE',  ( 0.9269276575891262082, 1.370462819911044239, -1.856556161720348763 ) ) ;
#41226=CARTESIAN_POINT ( 'NONE',  ( 3.602937629199114866, 1.706465849011790104, -1.326752773236601346 ) ) ;
#41230=CARTESIAN_POINT ( 'NONE',  ( 2.676452114398766291, -1.789519730395791486, -0.5449050523786898026 ) ) ;
#41232=CARTESIAN_POINT ( 'NONE',  ( 5.647334207030327846, -1.553848685622709835, -1.213239188487026166 ) ) ;
#41236=CARTESIAN_POINT ( 'NONE',  ( 0.8212658843103730621, 2.040464674744349338, 0.8412164853940640175 ) ) ;
#41241=CARTESIAN_POINT ( 'NONE',  ( 6.578986288830292573, -0.09655258645749519031, -1.969210242046049331 ) ) ;
#41242=CARTESIAN_POINT ( 'NONE',  ( 6.094374174207308315, -2.295927367373576722, -0.2327322904458818675 ) ) ;
#41243=CARTESIAN_POINT ( 'NONE',  ( 6.602007162813277041, 0.7109360278478898953, -1.720114357745919476 ) ) ;
#41244=CARTESIAN_POINT ( 'NONE',  ( 3.151292761600641867, 1.771340389172958441, -1.056411398746412544 ) ) ;
#41251=CARTESIAN_POINT ( 'NONE',  ( 5.793482113768906316, -1.965262051535413335, 0.9231745368859373135 ) ) ;
#41253=CARTESIAN_POINT ( 'NONE',  ( 5.671403949121008203, 1.101820082107987098, 1.475039313902235305 ) ) ;
#41255=CARTESIAN_POINT ( 'NONE',  ( 6.620655732516679493, 2.454579131793722002, 2.310038015908893350 ) ) ;
#41256=CARTESIAN_POINT ( 'NONE',  ( 6.392125918040960642, -0.5824770489515176397, -2.112646119873210271 ) ) ;
#41258=CARTESIAN_POINT ( 'NONE',  ( 6.631690487938540102, -1.471565961622269381, -1.718669407966398666 ) ) ;
#41264=CARTESIAN_POINT ( 'NONE',  ( 0.1703706300211875746, 0.7318840393725855042, 1.766877091004593225 ) ) ;
#41265=CARTESIAN_POINT ( 'NONE',  ( 1.850134630017237880, 0.5516246727584225296, 1.681758779177483287 ) ) ;
#41267=CARTESIAN_POINT ( 'NONE',  ( 6.006499477249034769, -2.003593090125683762, -0.1951834861853833925 ) ) ;
#41268=CARTESIAN_POINT ( 'NONE',  ( 5.122148429244435697, -1.124054950784241891, -1.780691527792167994 ) ) ;
#41270=CARTESIAN_POINT ( 'NONE',  ( 3.216317514422084578, 1.869562491224942224, 0.4167181705077570575 ) ) ;
#41271=CARTESIAN_POINT ( 'NONE',  ( -0.02244404828157658613, -0.004869073801674199918, -2.189079685368473527 ) ) ;
#41272=CARTESIAN_POINT ( 'NONE',  ( 4.703538277703087189, -1.521029056438701232, -1.251204274914043957 ) ) ;
#41273=CARTESIAN_POINT ( 'NONE',  ( -0.1929003719821283658, -0.4722129235960635940, -2.074948700427194481 ) ) ;
#41275=CARTESIAN_POINT ( 'NONE',  ( 2.922558825391399662, 1.760836971185793187, 0.6318509464167121337 ) ) ;
#41276=CARTESIAN_POINT ( 'NONE',  ( 5.690025311828595278, -0.7696446287084879323, 1.543740960907719950 ) ) ;
#41277=VERTEX_POINT ( 'NONE', #24368 ) ;
#41278=CARTESIAN_POINT ( 'NONE',  ( 2.209865124170300898, -0.4819264253047173541, 2.153463223375853719 ) ) ;
#41282=CARTESIAN_POINT ( 'NONE',  ( 6.074655751228532630, 1.318658252384183438, -1.452748870126779890 ) ) ;
#41290=CARTESIAN_POINT ( 'NONE',  ( 1.627480586986803868, 0.1543294891723171747, -2.064685722993148342 ) ) ;
#41294=CARTESIAN_POINT ( 'NONE',  ( 0.01237536129615121258, -2.019283296508204817, -0.04721428876065454638 ) ) ;
#41300=CARTESIAN_POINT ( 'NONE',  ( 5.624374986212743011, 0.3960386850128463920, -1.976653645673176474 ) ) ;
#41301=CARTESIAN_POINT ( 'NONE',  ( 5.260912935490944520, -0.05370519216219872549, -1.915158585242337397 ) ) ;
#41302=CARTESIAN_POINT ( 'NONE',  ( 6.539320575229230492, 2.428701779328062749, 2.485127258459709054 ) ) ;
#41303=CARTESIAN_POINT ( 'NONE',  ( 2.982162443640325122, -2.159563097825706990, -0.3721831821169723220 ) ) ;
#41305=CARTESIAN_POINT ( 'NONE',  ( 1.898553772666348394, -1.876154101037771582, -0.3696338911259658411 ) ) ;
#41307=CARTESIAN_POINT ( 'NONE',  ( 6.825078400183526739, -0.0002198122173603066763, 1.955566246027613753 ) ) ;
#41308=CARTESIAN_POINT ( 'NONE',  ( -0.03552856956758054796, -1.956598898622825766, -0.4871759670460884539 ) ) ;
#41311=CARTESIAN_POINT ( 'NONE',  ( 6.269083535738129598, 2.097726667780253074, -0.6343229546324488100 ) ) ;
#41313=CARTESIAN_POINT ( 'NONE',  ( 2.836578922267366742, 0.2088710044844780678, 1.711989638784001677 ) ) ;
#41315=CARTESIAN_POINT ( 'NONE',  ( 5.871359616481898414, -1.819694913365289768, -1.088597390283413402 ) ) ;
#41323=CARTESIAN_POINT ( 'NONE',  ( 3.017991377792153429, -1.809312282836759378, 0.09115427604276456208 ) ) ;
#41327=CARTESIAN_POINT ( 'NONE',  ( 3.352039220170324185, 0.8117645143102337757, -1.619458714540458866 ) ) ;
#41334=CARTESIAN_POINT ( 'NONE',  ( 4.721077684499490168, -1.662108436276054091, -0.8373904101051653504 ) ) ;
#41336=CARTESIAN_POINT ( 'NONE',  ( 2.847180372343278254, 0.2781937080071684720, -1.895151957576347579 ) ) ;
#41337=CARTESIAN_POINT ( 'NONE',  ( 1.237009950130557812, -1.652246606862219025, 0.7767072072360350354 ) ) ;
#41344=CARTESIAN_POINT ( 'NONE',  ( 5.594576842560746499, 1.939643975919752572, 0.3403973628498639936 ) ) ;
#41345=CARTESIAN_POINT ( 'NONE',  ( 2.536342520008515233, 0.6839386381054488595, 1.897109991223707937 ) ) ;
#41347=CARTESIAN_POINT ( 'NONE',  ( 0.1808504484964272296, -2.097240537080494516, -0.5235256853268268618 ) ) ;
#41348=CARTESIAN_POINT ( 'NONE',  ( 1.904351452098542063, 1.548259960728815665, -1.405051437006714643 ) ) ;
#41349=CARTESIAN_POINT ( 'NONE',  ( 6.668979838189343035, -1.761623494860217631, -0.7799453142821392015 ) ) ;
#41351=CARTESIAN_POINT ( 'NONE',  ( 1.887459117809231701, 1.256508940344562397, 1.324596713471258402 ) ) ;
#41352=CARTESIAN_POINT ( 'NONE',  ( 3.369938178094655346, 2.153121441420174698, -0.4834393813165636100 ) ) ;
#41354=CARTESIAN_POINT ( 'NONE',  ( 1.283307755816986528, 0.1377011610334301639, -1.907463248872851569 ) ) ;
#41355=CARTESIAN_POINT ( 'NONE',  ( 1.064831551406957511, 1.493571888342230203, -1.284017422347245807 ) ) ;
#41356=CARTESIAN_POINT ( 'NONE',  ( 2.858853853349733409, 0.2825237051190258031, -1.921275437378862305 ) ) ;
#41360=CARTESIAN_POINT ( 'NONE',  ( 6.262542430310119812, -0.6688554880303022587, -1.736790604091620560 ) ) ;
#41365=CARTESIAN_POINT ( 'NONE',  ( 2.349409277133751139, 0.5813161652389825518, -2.113004480973964760 ) ) ;
#41369=CARTESIAN_POINT ( 'NONE',  ( 2.455445036260803349, 0.4872311372507812655, -1.759406031448563557 ) ) ;
#41370=CARTESIAN_POINT ( 'NONE',  ( 5.964077395145578109, -1.074666730956087335, 1.706109649615504154 ) ) ;
#41375=B_SPLINE_CURVE_WITH_KNOTS ( 'NONE', 3,
 ( #211584, #12318, #44865, #61089, #29667, #146635, #11256, #210528, #77334, #48070 ),
 .UNSPECIFIED., .F., .F.,
 ( 4, 1, 1, 1, 1, 1, 1, 4 ),
 ( 0.000000000000000000, 0.09272347919791326665, 0.1850049962306132278, 0.2567072177207115891, 0.3610482009861257779, 0.5209239196176974618, 0.7336689415868371533, 1.000000000000000000 ),
 .UNSPECIFIED. ) ;
#41377=CARTESIAN_POINT ( 'NONE',  ( 2.051278105266049590, -1.547248087829168339, -1.147608674410576901 ) ) ;
#41378=CARTESIAN_POINT ( 'NONE',  ( 5.981297772519293510, -0.05168599705708888659, 1.961257141919122926 ) ) ;
#41385=CARTESIAN_POINT ( 'NONE',  ( 5.664915734613279241, 1.571387620024040421, -1.347999112033698266 ) ) ;
#41387=CARTESIAN_POINT ( 'NONE',  ( 5.239047776066017903, 2.296150469294107488, -0.1107920306624484569 ) ) ;
#41391=CARTESIAN_POINT ( 'NONE',  ( 0.05906008026819106055, -2.050595067678960604, -1.024705011274627431 ) ) ;
#41394=CARTESIAN_POINT ( 'NONE',  ( 5.121012332258009891, -1.843477085030984286, 0.6107378676363499626 ) ) ;
#41398=CARTESIAN_POINT ( 'NONE',  ( 6.152599605923961157, 1.892562589925715466, 0.2737767527046449101 ) ) ;
#41399=CARTESIAN_POINT ( 'NONE',  ( 0.7501351305400367764, 0.4964161116564491660, 1.651887862327553691 ) ) ;
#41400=CARTESIAN_POINT ( 'NONE',  ( 6.104703911763087909, 1.883310800321544409, 0.7212973825745233603 ) ) ;
#41404=CARTESIAN_POINT ( 'NONE',  ( 2.080132315211229876, -2.050506710900898977, -0.4067329413659624970 ) ) ;
#41405=CARTESIAN_POINT ( 'NONE',  ( 1.305125929463516909, -0.4348595813401417987, 1.715451362885108466 ) ) ;
#41406=CARTESIAN_POINT ( 'NONE',  ( 6.574846728087075931, -0.8593996854794653251, 1.822268861383633531 ) ) ;
#41409=CARTESIAN_POINT ( 'NONE',  ( 3.838036126445078633, 2.281091060459582209, 0.2259633074802695485 ) ) ;
#41410=CARTESIAN_POINT ( 'NONE',  ( 2.114833760799132989, -1.688328753782810221, 0.4216566245275765179 ) ) ;
#41412=CARTESIAN_POINT ( 'NONE',  ( 3.181995841446764839, 2.068044944583770306, -0.4684364081647199307 ) ) ;
#41414=CARTESIAN_POINT ( 'NONE',  ( 2.670900524536640841, -0.6599870735717223713, -1.603529595030905641 ) ) ;
#41416=CARTESIAN_POINT ( 'NONE',  ( 1.345918344774723163, -0.8409936141995101311, 1.660288665089631799 ) ) ;
#41417=CARTESIAN_POINT ( 'NONE',  ( 2.928372970691155430, 1.159507463759208878, 1.835456099276617570 ) ) ;
#41419=CARTESIAN_POINT ( 'NONE',  ( 3.977750132953357998, -0.7672935630990398437, 1.865046046545227654 ) ) ;
#41420=CARTESIAN_POINT ( 'NONE',  ( 3.187500000000002665, -1.451031289060985330, 1.451031289061251117 ) ) ;
#41422=CARTESIAN_POINT ( 'NONE',  ( 1.061403713111798153, 0.3786953092320010650, -1.888642112844605592 ) ) ;
#41424=CARTESIAN_POINT ( 'NONE',  ( 4.254274768897357006, 0.9481281144863746846, -2.009013624686401212 ) ) ;
#41430=CARTESIAN_POINT ( 'NONE',  ( 6.328415579541645464, -1.046111920768664660, -1.959710881125435789 ) ) ;
#41431=CARTESIAN_POINT ( 'NONE',  ( 5.002378505967389088, 1.956489882415031190, 0.1462272935644214900 ) ) ;
#41434=CARTESIAN_POINT ( 'NONE',  ( 5.659536867407776839, 0.4493550105662181271, -2.217189852095033942 ) ) ;
#41436=CARTESIAN_POINT ( 'NONE',  ( 2.752447824977616087, -2.056971473714273468, -0.1544007921008266060 ) ) ;
#41438=ADVANCED_FACE ( 'NONE', ( #208460 ), #189025, .T. ) ;
#41442=CARTESIAN_POINT ( 'NONE',  ( 4.499188554602613799, 1.501106652244098116, 1.115835331622745841 ) ) ;
#41443=CARTESIAN_POINT ( 'NONE',  ( 3.814867129904021770, 0.9234608866974923780, -1.467580195302587986 ) ) ;
#41444=CARTESIAN_POINT ( 'NONE',  ( 1.698380523978352485, 1.446983168995601199, 0.9667953101664509274 ) ) ;
#41445=CARTESIAN_POINT ( 'NONE',  ( 1.048812564444784989, -1.803156034432966681, 1.415383320267731726 ) ) ;
#41446=CARTESIAN_POINT ( 'NONE',  ( 1.009129827085092135, 1.670030910484705755, -1.442630471070925458 ) ) ;
#41447=CARTESIAN_POINT ( 'NONE',  ( 4.739831270385728601, 2.085251124590303373, 0.1521322122139453781 ) ) ;
#41448=CARTESIAN_POINT ( 'NONE',  ( 6.070255116781061666, -1.844781929399732290, -0.6067975954986597475 ) ) ;
#41451=CARTESIAN_POINT ( 'NONE',  ( 0.1939827082095749167, 1.755770691208278889, 0.9913967135185000057 ) ) ;
#41457=CARTESIAN_POINT ( 'NONE',  ( 4.529811765687052016, -1.125283923072720071, -1.437579299059896343 ) ) ;
#41458=CARTESIAN_POINT ( 'NONE',  ( 1.782535857997105566, -1.180187651135233384, 1.864495428577646274 ) ) ;
#41464=CARTESIAN_POINT ( 'NONE',  ( 1.406516720256438369, -2.010457973371252205, -0.1935789593500591155 ) ) ;
#41467=CARTESIAN_POINT ( 'NONE',  ( 2.764321045800025800, -0.7073474514263197177, -1.721481455096545377 ) ) ;
#41473=CARTESIAN_POINT ( 'NONE',  ( 4.916531288042031989, 1.256637652550334883, -1.324621001416517840 ) ) ;
#41477=CARTESIAN_POINT ( 'NONE',  ( 0.5261554912905551662, 1.716204961384654171, -0.2456527019241669663 ) ) ;
#41478=CARTESIAN_POINT ( 'NONE',  ( 6.527308116070499544, -1.206667617865687214, -1.390688675169844624 ) ) ;
#41479=CARTESIAN_POINT ( 'NONE',  ( 4.741030679083562127, 0.3911436318500530751, 2.274166950501448348 ) ) ;
#41481=CARTESIAN_POINT ( 'NONE',  ( 0.7376602057446514094, -1.455437688833590926, -1.459210590049898171 ) ) ;
#41484=CARTESIAN_POINT ( 'NONE',  ( 5.624470717464387093, 0.4563550445067353079, -2.252502686463413006 ) ) ;
#41487=CARTESIAN_POINT ( 'NONE',  ( 6.174654088403855212, -1.776896415251895789, -0.5849557326117056366 ) ) ;
#41488=CARTESIAN_POINT ( 'NONE',  ( 1.933716311909071006, -1.854087253938462521, 0.4680378644332866545 ) ) ;
#41490=CARTESIAN_POINT ( 'NONE',  ( 5.022202109028018668, -1.178465353167540197, -1.865713892744431446 ) ) ;
#41491=CARTESIAN_POINT ( 'NONE',  ( 4.979753661315234226, -0.7591050579739184734, 1.976773538454196677 ) ) ;
#41495=CARTESIAN_POINT ( 'NONE',  ( 2.397911878029312494, 1.783863880296262305, 1.463803424465635272 ) ) ;
#41496=CARTESIAN_POINT ( 'NONE',  ( 3.279693232472491893, -1.891448704997201302, 0.5207070127687256633 ) ) ;
#41498=CARTESIAN_POINT ( 'NONE',  ( 6.420768979138045118, -1.462686491410120970, 1.454469991251945649 ) ) ;
#41502=CARTESIAN_POINT ( 'NONE',  ( 5.594935472981866553, 1.780666063871166882, 0.9463038388278843804 ) ) ;
#41506=CARTESIAN_POINT ( 'NONE',  ( 1.657326198882978385, 1.776537685197575822, -1.247748726553777221 ) ) ;
#41507=DIRECTION ( 'NONE',  ( 1.014813233446432150E-15, 1.000000000000000000, -4.583713267641621330E-32 ) ) ;
#41509=B_SPLINE_CURVE_WITH_KNOTS ( 'NONE', 3,
 ( #199385, #211381, #130228, #197266, #67245, #80328, #32643, #133380, #63008, #51031 ),
 .UNSPECIFIED., .F., .F.,
 ( 4, 1, 1, 1, 1, 1, 1, 4 ),
 ( 0.000000000000000000, 0.09853459476447307130, 0.1926867929487333375, 0.2613852218134048999, 0.3629775382994345767, 0.5216635214973427415, 0.7338723600040717443, 1.000000000000000000 ),
 .UNSPECIFIED. ) ;
#41512=CARTESIAN_POINT ( 'NONE',  ( 1.124374118904346798, 1.229854006068244132, -1.653384075620732307 ) ) ;
#41514=CARTESIAN_POINT ( 'NONE',  ( 6.727182134110180733, 7.053024033604696541, 2.509100769544295950 ) ) ;
#41518=CARTESIAN_POINT ( 'NONE',  ( 3.123589223026546957, -0.3706944625661895976, 1.875830702792554483 ) ) ;
#41520=CARTESIAN_POINT ( 'NONE',  ( 5.084699950150380232, -0.2187599903600515594, -1.756180685135479091 ) ) ;
#41524=CARTESIAN_POINT ( 'NONE',  ( 6.503544296663656077, -1.856690447402360888, 0.4709783565581044940 ) ) ;
#41526=CARTESIAN_POINT ( 'NONE',  ( 0.3091450132529197647, -1.663722454078466306, 1.232067777400827069 ) ) ;
#41528=CARTESIAN_POINT ( 'NONE',  ( 6.455916552660014851, 1.865467424361374249, -0.1398750677365916961 ) ) ;
#41529=CARTESIAN_POINT ( 'NONE',  ( 2.385134503015675200, 1.669401249834654433, -0.7394980648879890817 ) ) ;
#41530=CARTESIAN_POINT ( 'NONE',  ( 5.654950187766193181, -1.741821662664808867, 1.355018943897445149 ) ) ;
#41534=CARTESIAN_POINT ( 'NONE',  ( 3.350102204537624306, -0.8385132117052511713, 1.884735577694598430 ) ) ;
#41538=CARTESIAN_POINT ( 'NONE',  ( 0.2984011986874868794, -2.161112683670802337, -0.05330630956579958390 ) ) ;
#41540=CARTESIAN_POINT ( 'NONE',  ( 5.125469573878929097, 0.2063957376101481500, -2.060066405364005426 ) ) ;
#41542=CARTESIAN_POINT ( 'NONE',  ( 3.409602121571019051, -0.4253414365745535886, 2.119164713334599881 ) ) ;
#41544=CARTESIAN_POINT ( 'NONE',  ( 3.580727245018202165, -1.354872245433702105, 1.497987768207516668 ) ) ;
#41545=CARTESIAN_POINT ( 'NONE',  ( 1.926150285298435572, 1.005797860886543660, 1.684270608208485065 ) ) ;
#41546=CARTESIAN_POINT ( 'NONE',  ( 6.620655732516684822, 2.041257794637734602, 2.379778264366624096 ) ) ;
#41553=CARTESIAN_POINT ( 'NONE',  ( 1.798064920797682653, -0.9548589541341389042, -1.776165177175797583 ) ) ;
#41557=CARTESIAN_POINT ( 'NONE',  ( 5.625241921295836889, 1.689600096388569561, 0.8957793909229804230 ) ) ;
#41561=CARTESIAN_POINT ( 'NONE',  ( 2.776970437579088014, 1.727991955821889025, -1.039012595151635354 ) ) ;
#41564=CARTESIAN_POINT ( 'NONE',  ( 6.651377187556704484, -1.389000575594327103, -1.022263415358831473 ) ) ;
#41568=CARTESIAN_POINT ( 'NONE',  ( 4.358574879328508622, -1.387578095181252413, 1.254630796652965730 ) ) ;
#41570=CARTESIAN_POINT ( 'NONE',  ( 1.639598513223254006, 1.914365469054382540, -0.7886191548351070280 ) ) ;
#41575=CARTESIAN_POINT ( 'NONE',  ( 0.3690327605676722023, -1.530577755691145958, -0.9687459989127805704 ) ) ;
#41582=CARTESIAN_POINT ( 'NONE',  ( 6.538697978567284963, -1.477089011224671955, 1.219511253712385335 ) ) ;
#41587=ADVANCED_FACE ( 'NONE', ( #8137 ), #63772, .F. ) ;
#41592=CARTESIAN_POINT ( 'NONE',  ( 3.133815226704575796, -1.450665623810345473, -1.602838778681406007 ) ) ;
#41597=CARTESIAN_POINT ( 'NONE',  ( 6.124025070245508573, -1.016541136310184390, -1.516163765885633286 ) ) ;
#41599=CARTESIAN_POINT ( 'NONE',  ( 1.352734582195244561, -1.556726207391207817, 1.209420702486432297 ) ) ;
#41600=CARTESIAN_POINT ( 'NONE',  ( 3.533378866418676711, -0.1359047358975660202, 1.907598245988059826 ) ) ;
#41603=CARTESIAN_POINT ( 'NONE',  ( 5.248484213797577347, -1.954463446003468885, -0.2428638724455249587 ) ) ;
#41604=VERTEX_POINT ( 'NONE', #31878 ) ;
#41605=CARTESIAN_POINT ( 'NONE',  ( 5.776890131463271238, 1.792767593593114439, -0.7471807142077312447 ) ) ;
#41611=CARTESIAN_POINT ( 'NONE',  ( 3.422422624566554994, -0.7774026117220147469, -1.747318718686732275 ) ) ;
#41613=CARTESIAN_POINT ( 'NONE',  ( 1.009129827085092135, 1.670030910484705755, -1.442630471070925458 ) ) ;
#41615=CARTESIAN_POINT ( 'NONE',  ( 6.111982388360997831, -0.6759622889470856544, 1.896349411511048855 ) ) ;
#41617=CARTESIAN_POINT ( 'NONE',  ( 6.481070005604858686, -0.09514881109910081070, -1.823337098959529001 ) ) ;
#41618=CARTESIAN_POINT ( 'NONE',  ( 1.680221237283368696, -1.148429780529091948, -1.722445320287042447 ) ) ;
#41621=CARTESIAN_POINT ( 'NONE',  ( -0.1296875068448159751, 0.001480089298542403009, -1.826395826379861864 ) ) ;
#41622=CARTESIAN_POINT ( 'NONE',  ( 6.789956943122251509, -0.7972922127613899512, 1.690610701080223821 ) ) ;
#41627=COLOUR_RGB ( '', 0.72549020, 0.75294118, 0.79215686) ;
#41630=CARTESIAN_POINT ( 'NONE',  ( 6.825078400183573812, 0.002648415797040087893, 1.855566311045192540 ) ) ;
#41632=CARTESIAN_POINT ( 'NONE',  ( 5.115702696222887980, 0.1348363893083539267, 1.728983578677806499 ) ) ;
#41634=CARTESIAN_POINT ( 'NONE',  ( 2.922783962489564846, -1.430918204188264875, 1.496350883549990352 ) ) ;
#41635=CARTESIAN_POINT ( 'NONE',  ( 3.884452219389774363, -0.6659801820031689967, -2.009805269316313314 ) ) ;
#41638=CARTESIAN_POINT ( 'NONE',  ( 1.235132629255174974, -0.04286028942791567098, -1.969139623717565790 ) ) ;
#41641=CARTESIAN_POINT ( 'NONE',  ( -0.1229892814952095459, -1.709044814581164973, -0.8582256167319823881 ) ) ;
#41642=CARTESIAN_POINT ( 'NONE',  ( 4.224787546089771695, 0.1105535957067731723, 2.289718640476182898 ) ) ;
#41643=CARTESIAN_POINT ( 'NONE',  ( 2.244514701088017539, 0.3993153960501935051, 1.781317584591130432 ) ) ;
#41647=CARTESIAN_POINT ( 'NONE',  ( 2.777592571122803555, 0.2913108041502753820, -1.991885045997557224 ) ) ;
#41648=CARTESIAN_POINT ( 'NONE',  ( 3.819154011256303161, -1.728040176127441985, -0.9287006429716244682 ) ) ;
#41652=CARTESIAN_POINT ( 'NONE',  ( 6.421832395068366672, 1.204883778905677216, -1.708312069947721668 ) ) ;
#41653=CARTESIAN_POINT ( 'NONE',  ( 4.996827606291168955, 1.470251540571869020, -0.9849021259363596181 ) ) ;
#41656=CARTESIAN_POINT ( 'NONE',  ( 0.9904705247469265394, -0.5356807779838267392, -2.124848333686576662 ) ) ;
#41657=CARTESIAN_POINT ( 'NONE',  ( 5.630708778567339756, -1.570753007681056079, 0.7496256940079452091 ) ) ;
#41659=CARTESIAN_POINT ( 'NONE',  ( 0.1333692844072559558, 0.7140749627707367875, -2.136770008611441618 ) ) ;
#41660=CARTESIAN_POINT ( 'NONE',  ( 6.205746375452622310, 2.143286971341977765, 0.8312943217957665665 ) ) ;
#41661=CARTESIAN_POINT ( 'NONE',  ( 0.1333692844072559003, 5.722267537706915874, -2.647605121726896105 ) ) ;
#41662=CARTESIAN_POINT ( 'NONE',  ( 5.553917692138156781, 1.528130387303320514, -0.8190655202615308994 ) ) ;
#41663=( BOUNDED_SURFACE ( )  B_SPLINE_SURFACE ( 3, 3, ( 
 ( #137683, #188543, #203704, #156056, #7644, #92145, #55351, #205854, #174457, #57486, #123647 ),
 ( #108437, #189609, #22820, #158199, #191728, #59610, #41255, #43384, #107365, #91071, #88935 ),
 ( #9789, #173386, #8723, #24969, #157132, #75863, #141970, #125766, #94274, #61748, #66764 ),
 ( #29253, #193868, #30323, #80120, #12979, #159241, #11919, #111633, #60672, #133980, #183750 ),
 ( #51636, #77992, #150205, #50556, #95345, #198910, #177644, #1777, #132905, #76915, #117760 ),
 ( #45517, #211176, #126835, #161395, #79054, #194943, #182676, #28179, #145171, #96408, #162458 ),
 ( #67834, #62802, #146225, #14034, #699, #116677, #160315, #34297, #209036, #18031, #93209 ) ),
 .UNSPECIFIED., .T., .F., .F. ) 
 B_SPLINE_SURFACE_WITH_KNOTS ( ( 4, 3, 4 ),
 ( 4, 1, 1, 1, 1, 1, 1, 1, 4 ),
 ( 0.000000000000000000, 0.5000000000000000000, 1.000000000000000000 ),
 ( 0.000000000000000000, 0.2254494161556361009, 0.3971188491599597081, 0.5240836380151728813, 0.6154273167216615104, 0.6803253696226415626, 0.7282602231486813293, 0.7688932809586735972, 1.000000000000000000 ),
 .UNSPECIFIED. ) 
 GEOMETRIC_REPRESENTATION_ITEM ( )  RATIONAL_B_SPLINE_SURFACE ( (
 ( 1.000000000000000222, 1.000000000000000222, 0.9999999999999995559, 1.000000000000000666, 0.9999999999999997780, 0.9999999999999997780, 1.000000000000000000, 1.000000000000000000, 1.000000000000000000, 1.000000000000000000, 1.000000000000000000),
 ( 0.3333333333333334259, 0.3333333333333334259, 0.3333333333333332593, 0.3333333333333335369, 0.3333333333333333148, 0.3333333333333333148, 0.3333333333333334259, 0.3333333333333333703, 0.3333333333333333148, 0.3333333333333333703, 0.3333333333333333703),
 ( 0.3333333333333334259, 0.3333333333333334259, 0.3333333333333332593, 0.3333333333333335369, 0.3333333333333333148, 0.3333333333333333148, 0.3333333333333334259, 0.3333333333333333703, 0.3333333333333333148, 0.3333333333333333703, 0.3333333333333333703),
 ( 1.000000000000000222, 1.000000000000000222, 0.9999999999999995559, 1.000000000000000666, 0.9999999999999997780, 0.9999999999999997780, 1.000000000000000000, 1.000000000000000000, 1.000000000000000000, 1.000000000000000000, 1.000000000000000000),
 ( 0.3333333333333334259, 0.3333333333333334259, 0.3333333333333332593, 0.3333333333333335369, 0.3333333333333333148, 0.3333333333333333148, 0.3333333333333334259, 0.3333333333333333703, 0.3333333333333333148, 0.3333333333333333703, 0.3333333333333333703),
 ( 0.3333333333333334259, 0.3333333333333334259, 0.3333333333333332593, 0.3333333333333335369, 0.3333333333333333148, 0.3333333333333333148, 0.3333333333333334259, 0.3333333333333333703, 0.3333333333333333148, 0.3333333333333333703, 0.3333333333333333703),
 ( 1.000000000000000222, 1.000000000000000222, 0.9999999999999995559, 1.000000000000000666, 0.9999999999999997780, 0.9999999999999997780, 1.000000000000000000, 1.000000000000000000, 1.000000000000000000, 1.000000000000000000, 1.000000000000000000) ) ) 
 REPRESENTATION_ITEM ( '' )  SURFACE ( )  );
#41665=CARTESIAN_POINT ( 'NONE',  ( 6.057114314241694331, 1.778561107892376647, -1.245054071093915304 ) ) ;
#41667=CARTESIAN_POINT ( 'NONE',  ( 0.05801502780489272565, 1.224741999009547833, 1.726997829920233540 ) ) ;
#41668=CARTESIAN_POINT ( 'NONE',  ( 3.906250000000001776, 1.895863743163997084, -0.7852924748301890467 ) ) ;
#41669=CARTESIAN_POINT ( 'NONE',  ( 6.727182134110196721, 7.051813866762763006, 2.787205683092201181 ) ) ;
#41670=CARTESIAN_POINT ( 'NONE',  ( 4.700175447307747945, -1.925963193209312418, -0.04779502591981815707 ) ) ;
#41672=CARTESIAN_POINT ( 'NONE',  ( 0.7158630905677393352, 1.819291361130066287, 1.274270043568943800 ) ) ;
#41677=CARTESIAN_POINT ( 'NONE',  ( 2.332966905468473406, 1.448476307009987307, -1.684171307209429314 ) ) ;
#41684=CARTESIAN_POINT ( 'NONE',  ( 0.7564826839323666174, 1.942540863013635821, -0.5404934282097761944 ) ) ;
#41686=CARTESIAN_POINT ( 'NONE',  ( 6.496538660071067284, 2.039668932145132008, 0.3065683105917779705 ) ) ;
#41690=CARTESIAN_POINT ( 'NONE',  ( 0.9481069621972251227, 0.5063937300482551640, 1.695761627633844304 ) ) ;
#41691=CARTESIAN_POINT ( 'NONE',  ( 0.2115648487451895210, 1.930418618556551946, 0.5826528611774861588 ) ) ;
#41692=CARTESIAN_POINT ( 'NONE',  ( 5.056098682708163317, -1.255628792201430644, 1.205468413292756669 ) ) ;
#41693=CARTESIAN_POINT ( 'NONE',  ( 3.755682109644884026, 2.274985096322924338, -0.2814536430481278662 ) ) ;
#41695=CARTESIAN_POINT ( 'NONE',  ( 2.238008233095424515, 0.4029187984595939409, 1.796341404040911804 ) ) ;
#41698=CARTESIAN_POINT ( 'NONE',  ( 2.942213871598580166, 1.811567870905493205, 0.2252638538085757203 ) ) ;
#41699=CARTESIAN_POINT ( 'NONE',  ( 3.463517678199812266, -1.944071305346905643, -0.5350885120067662148 ) ) ;
#41701=CARTESIAN_POINT ( 'NONE',  ( 3.942437297418455611, 2.251314906739984245, 0.2249487974115715883 ) ) ;
#41703=CARTESIAN_POINT ( 'NONE',  ( 4.981522283868931034, 1.966010104637575751, -0.7553895412903822715 ) ) ;
#41705=CARTESIAN_POINT ( 'NONE',  ( 2.734898984476673789, -1.980466496001157317, -0.6033880717724803278 ) ) ;
#41708=CARTESIAN_POINT ( 'NONE',  ( 4.494861206476631565, -2.057060146276223023, -0.5143016718046622415 ) ) ;
#41711=CARTESIAN_POINT ( 'NONE',  ( 0.5395173010800574653, -1.361483316988669978, -1.363248745070398726 ) ) ;
#41718=CARTESIAN_POINT ( 'NONE',  ( 0.9498388403609931974, -2.005144016916958982, 0.9564107486674018332 ) ) ;
#41719=CARTESIAN_POINT ( 'NONE',  ( 2.450341380362738075, 2.105475501793910631, 0.05272098179117353650 ) ) ;
#41722=CARTESIAN_POINT ( 'NONE',  ( 6.842638030098166624, -1.824918384715786823, -0.3633994975895912805 ) ) ;
#41727=CARTESIAN_POINT ( 'NONE',  ( -0.1929003719821283658, -0.4722129235960635940, -2.074948700427194481 ) ) ;
#41730=CARTESIAN_POINT ( 'NONE',  ( 2.928120951529111338, 1.047165451586975049, 1.658829547137883775 ) ) ;
#41731=CARTESIAN_POINT ( 'NONE',  ( 1.710078970767275885, -2.145365142986368934, 0.2646356489638818088 ) ) ;
#41735=CARTESIAN_POINT ( 'NONE',  ( 3.362975788648288944, 1.697558991927169192, -0.3826393865087075463 ) ) ;
#41740=CARTESIAN_POINT ( 'NONE',  ( 1.932970024460831882, 1.034005469613193062, 1.730602090182407959 ) ) ;
#41741=CARTESIAN_POINT ( 'NONE',  ( 6.825078400183544503, 3.684911640780349718, 2.658296617506946458 ) ) ;
#41742=CARTESIAN_POINT ( 'NONE',  ( 0.6202742476981680797, -1.157488721396517040, -1.825510493854154426 ) ) ;
#41743=CARTESIAN_POINT ( 'NONE',  ( 2.729320057108883368, -1.840128979258702557, 0.7079907272262278006 ) ) ;
#41750=CARTESIAN_POINT ( 'NONE',  ( 1.981123565540498177, -1.847491841353067210, -0.8164113852280636685 ) ) ;
#41752=CARTESIAN_POINT ( 'NONE',  ( 5.754963864978503985, -1.823789643192383014, 1.413694633616706886 ) ) ;
#41753=CARTESIAN_POINT ( 'NONE',  ( 6.865691018405424728, -0.4312029709039078007, 1.920920986087648163 ) ) ;
#41754=CARTESIAN_POINT ( 'NONE',  ( 3.010546455304231372, 0.6564385890225448161, 1.848828695667027677 ) ) ;
#41756=CARTESIAN_POINT ( 'NONE',  ( 0.8267963299631932994, 0.8146243292815741333, -1.844710905833810255 ) ) ;
#41758=CARTESIAN_POINT ( 'NONE',  ( 2.378245518041781636, -2.112004366230528785, -0.1507482023494610135 ) ) ;
#41761=CARTESIAN_POINT ( 'NONE',  ( 2.290725937607818175, 1.422998120520948984, 1.168276728405498455 ) ) ;
#41765=CARTESIAN_POINT ( 'NONE',  ( 3.199588043238619228, 1.915454767000431602, -0.9102714984489732597 ) ) ;
#41766=CARTESIAN_POINT ( 'NONE',  ( -0.02968770228140016343, 0.003472272166151618711, -1.826291111852257343 ) ) ;
#41770=CARTESIAN_POINT ( 'NONE',  ( 4.639950097937448170, 0.8846809987467202374, -1.861387103252240660 ) ) ;
#41773=CARTESIAN_POINT ( 'NONE',  ( 1.593040506729075823, -0.6195558395927207584, 1.734028948791266345 ) ) ;
#41775=CARTESIAN_POINT ( 'NONE',  ( -0.02244404828160087226, 1.323617703852699057, -2.440988974267483957 ) ) ;
#41778=CARTESIAN_POINT ( 'NONE',  ( 1.049787907720298286, -1.741764784136769162, -1.355102641770723704 ) ) ;
#41779=CARTESIAN_POINT ( 'NONE',  ( 3.796368952254399964, -2.259583311708447617, -0.1157369865004975740 ) ) ;
#41781=CARTESIAN_POINT ( 'NONE',  ( 3.357467859903106255, -1.375039365347962450, -1.179588011891503418 ) ) ;
#41783=CARTESIAN_POINT ( 'NONE',  ( 2.993272137104509678, -0.3688056758139393043, 1.879696595719517083 ) ) ;
#41784=CARTESIAN_POINT ( 'NONE',  ( 4.158688916442685013, -0.6465363538536235133, -1.966910096795893681 ) ) ;
#41787=CARTESIAN_POINT ( 'NONE',  ( 2.430492692261185805, 1.911874441976011640, 0.4805678379448170001 ) ) ;
#41788=CARTESIAN_POINT ( 'NONE',  ( 1.465712096425618949, 1.898328545170711035, -0.3267402372346754902 ) ) ;
#41789=CARTESIAN_POINT ( 'NONE',  ( 3.397188523315307407, 1.473948685399184333, 1.151750840393983344 ) ) ;
#41790=CARTESIAN_POINT ( 'NONE',  ( 2.420946758181366842, 1.505949115154591400, -1.748677306438247703 ) ) ;
#41791=CARTESIAN_POINT ( 'NONE',  ( 4.228838981530287811, -1.735973604985484142, -0.6712095357626171044 ) ) ;
#41796=CARTESIAN_POINT ( 'NONE',  ( 0.1004013553109489865, -2.105664478878019441, -0.04916207707313274139 ) ) ;
#41801=CARTESIAN_POINT ( 'NONE',  ( 1.547299434221154124, 0.2130619955753136618, 2.109896976817266179 ) ) ;
#41802=CARTESIAN_POINT ( 'NONE',  ( 0.4924518904856821089, -1.118466686806585342, 1.681619975139287515 ) ) ;
#41807=CARTESIAN_POINT ( 'NONE',  ( 1.511231465835579879, 1.905624552496063995, 1.020381674553122231 ) ) ;
#41809=CARTESIAN_POINT ( 'NONE',  ( 6.825078400183554272, 2.980425674467934272, 2.309322343017068402 ) ) ;
#41811=CARTESIAN_POINT ( 'NONE',  ( -0.2104748580754413345, 7.629137130509052511, -2.703678718140525739 ) ) ;
#41812=CARTESIAN_POINT ( 'NONE',  ( 5.313685493615880162, -1.282986534165726944, -1.555701818360885280 ) ) ;
#41816=CARTESIAN_POINT ( 'NONE',  ( 0.6380306694902828646, -1.602208245511031803, -1.597717328844779239 ) ) ;
#41820=CARTESIAN_POINT ( 'NONE',  ( 0.3158528693416655653, 0.9839445311579012587, -1.643420606830671815 ) ) ;
#41824=CARTESIAN_POINT ( 'NONE',  ( 3.439825841515719240, 0.7741550462027242396, -1.541462414610708764 ) ) ;
#41827=CARTESIAN_POINT ( 'NONE',  ( 1.071160155259534674, 1.707552549077664183, -0.4648152392626672680 ) ) ;
#41828=CARTESIAN_POINT ( 'NONE',  ( 1.488932678171340118, -1.912290114023627252, -0.6292827167945020950 ) ) ;
#41829=CARTESIAN_POINT ( 'NONE',  ( 6.983263157960366563, -0.003091553303710344557, 1.945923119799706669 ) ) ;
#41830=CARTESIAN_POINT ( 'NONE',  ( 3.645738483435243982, -1.669485028154977790, -1.443228448415982079 ) ) ;
#41834=CARTESIAN_POINT ( 'NONE',  ( 3.844477943020713440, 1.133112341739877849, -1.792160191984671691 ) ) ;
#41835=CARTESIAN_POINT ( 'NONE',  ( 2.970327539257538341, -1.987051465770898417, -0.3419137282784574516 ) ) ;
#41836=CARTESIAN_POINT ( 'NONE',  ( 3.304753640158542893, -0.3582801770840525757, -1.775609565582184191 ) ) ;
#41840=CARTESIAN_POINT ( 'NONE',  ( 1.252583056964752029, -1.476889893665521702, 1.148006582770304096 ) ) ;
#41841=CARTESIAN_POINT ( 'NONE',  ( 6.059193749186201572, -1.568369423792463024, -0.9343120793870243190 ) ) ;
#41843=CARTESIAN_POINT ( 'NONE',  ( 2.483477273924311834, -0.5967159848992757976, 1.820515277383168540 ) ) ;
#41853=CARTESIAN_POINT ( 'NONE',  ( 3.252298345715322725, 0.9499829135306799843, -1.895951488860507128 ) ) ;
#41854=CARTESIAN_POINT ( 'NONE',  ( -0.02948999725182251813, 4.092753722544117956, -2.481335295887850290 ) ) ;
#41857=CARTESIAN_POINT ( 'NONE',  ( 4.235589135538409877, -1.357111243005538759, -1.430095230664797379 ) ) ;
#41858=CARTESIAN_POINT ( 'NONE',  ( -0.1755273284492936958, -0.8636782348834280976, -1.816524446017355743 ) ) ;
#41860=CARTESIAN_POINT ( 'NONE',  ( -0.1056256405159265443, -0.9088113327815927622, -1.910082645617340757 ) ) ;
#41861=CARTESIAN_POINT ( 'NONE',  ( 1.715371797147913435, -1.774658612622433296, -1.066089629202723765 ) ) ;
#41866=CARTESIAN_POINT ( 'NONE',  ( 3.925792317461401559, 1.118293097838483074, -1.766204078809136657 ) ) ;
#41869=CARTESIAN_POINT ( 'NONE',  ( 0.2932429122153769052, 1.690905606409907058, -0.6502662643994570058 ) ) ;
#41871=CARTESIAN_POINT ( 'NONE',  ( 5.830760709146560750, 2.125890151018691832, 0.5921790101122563765 ) ) ;
#41873=CARTESIAN_POINT ( 'NONE',  ( 4.102700518754747172, -0.6894086160392081108, -2.096397988278507096 ) ) ;
#41876=CARTESIAN_POINT ( 'NONE',  ( 2.719282321824310511, 1.616554633311767297, 1.021241153818429614 ) ) ;
#41878=CARTESIAN_POINT ( 'NONE',  ( 5.564915762860970005, 1.570151797963925233, -1.349580972669261358 ) ) ;
#41880=CARTESIAN_POINT ( 'NONE',  ( 2.747127081003514881, -1.797865629537301668, 1.199965651887124896 ) ) ;
#41881=CARTESIAN_POINT ( 'NONE',  ( 5.671465802443460547, 1.304529079428708549, 1.760837017921567771 ) ) ;
#41891=CARTESIAN_POINT ( 'NONE',  ( 6.192251260771239885, 1.025525066348543568, -1.798363755310352197 ) ) ;
#41892=CARTESIAN_POINT ( 'NONE',  ( 4.090394749938445429, -1.905694808957728137, -0.2815942358586983607 ) ) ;
#41893=CARTESIAN_POINT ( 'NONE',  ( 0.5445462702219765472, -1.458543044971000402, 1.392561646250379814 ) ) ;
#41897=CARTESIAN_POINT ( 'NONE',  ( 0.6389542677898361056, -1.877638805159736579, 1.129783718924075364 ) ) ;
#41898=CARTESIAN_POINT ( 'NONE',  ( 5.479063914364931343, -0.04889757770590653918, -1.825204647902956889 ) ) ;
#41905=CARTESIAN_POINT ( 'NONE',  ( 2.559893532628489954, -1.268187297466142338, 1.335118840784771166 ) ) ;
#41906=CARTESIAN_POINT ( 'NONE',  ( 5.713144883995101786, 1.643398218655172105, -1.162588118691459949 ) ) ;
#41907=CARTESIAN_POINT ( 'NONE',  ( 0.7908558668072614983, -2.181831595417762504, 0.7228866375666581634 ) ) ;
#41908=CARTESIAN_POINT ( 'NONE',  ( 6.227397112613878960, 0.1477489091250457076, -1.956280406615627854 ) ) ;
#41914=CARTESIAN_POINT ( 'NONE',  ( 2.859016124132291115, 0.3040538821531354463, -2.068378887337805949 ) ) ;
#41915=CARTESIAN_POINT ( 'NONE',  ( 1.674454752297813265, -1.775319108138155633, -0.5897529795871117031 ) ) ;
#41916=CARTESIAN_POINT ( 'NONE',  ( 2.020861031540205133, 2.010896488828680440, -0.1455087364366919322 ) ) ;
#41920=CARTESIAN_POINT ( 'NONE',  ( 2.471852389601780331, -1.665955342129191274, -0.5037381675307306406 ) ) ;
#41924=CARTESIAN_POINT ( 'NONE',  ( 2.736579049320194468, 0.2108767276123752754, 1.711865116355310246 ) ) ;
#41925=CARTESIAN_POINT ( 'NONE',  ( 2.982162443640325566, -2.159563097825706990, -0.3721831821169723775 ) ) ;
#41926=CARTESIAN_POINT ( 'NONE',  ( 5.039771180630152614, -1.558841386063321455, -1.562417271110942307 ) ) ;
#41928=CARTESIAN_POINT ( 'NONE',  ( 2.553800759094803308, 1.675875371511101886, 1.380159786156359258 ) ) ;
#41929=CARTESIAN_POINT ( 'NONE',  ( 1.154616158753757338, -1.440623569337009968, 1.121372061650728558 ) ) ;
#41930=CARTESIAN_POINT ( 'NONE',  ( 3.925106927653505995, -1.840236814299311741, 1.047156446301507948 ) ) ;
#41931=CARTESIAN_POINT ( 'NONE',  ( 6.639320575229255006, 7.629137130509086262, 2.596737603865982624 ) ) ;
#41933=CARTESIAN_POINT ( 'NONE',  ( 4.159948666787936844, 1.080635193647750292, 2.021704573604603095 ) ) ;
#41938=CARTESIAN_POINT ( 'NONE',  ( 0.2234921222181683598, 1.847112181986635626, 1.041312259928407702 ) ) ;
#41944=CARTESIAN_POINT ( 'NONE',  ( 4.570935502227962743, -0.9480417383296577682, 1.779625852769652905 ) ) ;
#41946=CARTESIAN_POINT ( 'NONE',  ( 3.028243468416950357, 1.099549687589720826, 1.744862417660711262 ) ) ;
#41951=CARTESIAN_POINT ( 'NONE',  ( 6.175747540105122724, -1.175446681380667213, 1.849350104233343783 ) ) ;
#41952=CARTESIAN_POINT ( 'NONE',  ( 3.639296212489909532, 0.7283784247123014088, 1.880435045658496618 ) ) ;
#41953=CARTESIAN_POINT ( 'NONE',  ( 2.981803241483144351, -1.814435276338403735, -0.3121031562058202424 ) ) ;
#41955=CARTESIAN_POINT ( 'NONE',  ( 6.247073575888860475, -1.540555741078741825, 0.9791950884799265342 ) ) ;
#41957=CARTESIAN_POINT ( 'NONE',  ( 0.6853298295916141480, -0.2782767918169821164, -2.245138299566074913 ) ) ;
#41958=CARTESIAN_POINT ( 'NONE',  ( 2.086679739605776351, -2.065639965682735557, -0.4097663305358787977 ) ) ;
#41968=CARTESIAN_POINT ( 'NONE',  ( 2.109781586379317897, 1.642293606977158538, 1.341614810521203349 ) ) ;
#41969=CARTESIAN_POINT ( 'NONE',  ( 3.639129310729662503, 2.110331241038451822, 0.6939571745526812441 ) ) ;
#41970=CARTESIAN_POINT ( 'NONE',  ( 0.7092355107721182161, -0.3178641103029449244, 2.168156088950490723 ) ) ;
#41971=CARTESIAN_POINT ( 'NONE',  ( 0.7509353727821498348, 0.6442623716619542140, 2.110749664216593047 ) ) ;
#41973=CARTESIAN_POINT ( 'NONE',  ( 4.914483161888778540, 0.7490505147796695518, 1.813437088826752142 ) ) ;
#41983=CARTESIAN_POINT ( 'NONE',  ( 3.920270587443940080, -2.114697630030224929, 0.1593259359235904837 ) ) ;
#41985=CARTESIAN_POINT ( 'NONE',  ( 5.858325616802108726, 0.8718737102157668728, 1.978260574764856283 ) ) ;
#41986=CARTESIAN_POINT ( 'NONE',  ( 4.493604616018744835, -1.840970053361364656, -0.04044509776383875543 ) ) ;
#41991=CARTESIAN_POINT ( 'NONE',  ( 0.2920125592734872932, 1.448600077496174476, -0.9643754397266665057 ) ) ;
#41992=CARTESIAN_POINT ( 'NONE',  ( 6.827182134110231893, 2.454327069706051745, 2.294502690501096787 ) ) ;
#41996=CARTESIAN_POINT ( 'NONE',  ( 4.592742373648754040, -0.4705147408641910944, -2.109722102427157964 ) ) ;
#41998=CARTESIAN_POINT ( 'NONE',  ( 5.712267477471262289, -1.587595409608580255, -1.242535230690837489 ) ) ;
#42000=CARTESIAN_POINT ( 'NONE',  ( 3.573254463033649131, 0.05508235185803719847, -2.161170636208443963 ) ) ;
#42001=CARTESIAN_POINT ( 'NONE',  ( 3.514874812717229347, 1.780701125067783108, 0.8461077801947043397 ) ) ;
#42002=CARTESIAN_POINT ( 'NONE',  ( 0.2577194443907256383, 2.166829308800602316, -0.3276212646995610989 ) ) ;
#42003=CARTESIAN_POINT ( 'NONE',  ( 1.079649059555651824, -0.05968906897618533880, -2.306965765669062751 ) ) ;
#42004=CARTESIAN_POINT ( 'NONE',  ( 3.163408073613428684, 0.3057118896435347954, -2.037866251177067323 ) ) ;
#42005=CARTESIAN_POINT ( 'NONE',  ( 5.284693219347969873, 1.710810618512406789, -0.9191280305995457311 ) ) ;
#42013=CARTESIAN_POINT ( 'NONE',  ( 1.905583573826599597, 1.834846665736546756, 1.225745012653912891 ) ) ;
#42015=CARTESIAN_POINT ( 'NONE',  ( 6.332860960579021814, -1.861707940517230764, -0.6185968553879470644 ) ) ;
#42016=CARTESIAN_POINT ( 'NONE',  ( 6.539320575229258914, 2.958022083381315781, 2.556018433155104574 ) ) ;
#42021=CARTESIAN_POINT ( 'NONE',  ( 4.910013284106277354, 1.267360923890372693, -1.335742228452965863 ) ) ;
#42023=CARTESIAN_POINT ( 'NONE',  ( 2.413025777909239000, 1.840395853916647173, 0.9276406582674895374 ) ) ;
#42028=CARTESIAN_POINT ( 'NONE',  ( 0.8837498274346058391, 1.383631269908250472, 1.527543229604712893 ) ) ;
#42030=CARTESIAN_POINT ( 'NONE',  ( 5.249485218566787736, 1.838879873951341004, -0.09611505855997715120 ) ) ;
#42036=CARTESIAN_POINT ( 'NONE',  ( 4.617920694193921705, -2.164688156338661962, 0.4286357439418769788 ) ) ;
#42037=CARTESIAN_POINT ( 'NONE',  ( 6.919229411136463170, -0.1667645622517479609, 2.226262756130835463 ) ) ;
#42038=CARTESIAN_POINT ( 'NONE',  ( 3.661342437515973547, 1.897110692972364454, -0.6839366698164971448 ) ) ;
#42040=CARTESIAN_POINT ( 'NONE',  ( -0.05268457437105152075, -1.747710896673961622, 0.7768168958157274373 ) ) ;
#42041=CARTESIAN_POINT ( 'NONE',  ( -0.2409995289980038091, -0.004801160710915519658, -2.000252362011435636 ) ) ;
#42042=CARTESIAN_POINT ( 'NONE',  ( 0.07536363704233395300, 5.720741966631408104, -2.738263776839637842 ) ) ;
#42043=CARTESIAN_POINT ( 'NONE',  ( 5.988906256519172189, -1.817303134770717365, -0.5954205699960082310 ) ) ;
#42046=CARTESIAN_POINT ( 'NONE',  ( 0.6197280442463182215, -0.9970892369244135356, -1.582582228963416160 ) ) ;
#42047=CARTESIAN_POINT ( 'NONE',  ( 2.536342520008515233, 0.6839386381054488595, 1.897109991223707937 ) ) ;
#42049=CARTESIAN_POINT ( 'NONE',  ( 3.932330475907989342, 1.126754335618613379, -1.779114833428483866 ) ) ;
#42053=CARTESIAN_POINT ( 'NONE',  ( 4.517835093568582927, -0.5347929126107499043, 1.947652422195633504 ) ) ;
#42057=CARTESIAN_POINT ( 'NONE',  ( 4.358765367649009903, -1.604958417591015207, 1.448176592534822005 ) ) ;
#42062=CARTESIAN_POINT ( 'NONE',  ( 1.434277768017662824, 1.292756205793591517, 1.744237601605197252 ) ) ;
#42065=CARTESIAN_POINT ( 'NONE',  ( 0.9777802892061361328, -1.796362506263927017, -0.4033719513514141264 ) ) ;
#42067=CARTESIAN_POINT ( 'NONE',  ( 3.122796855005858241, 0.05607861761174406934, 2.191015320347329709 ) ) ;
#42068=CARTESIAN_POINT ( 'NONE',  ( 6.883263157960358924, 7.052235917045241997, 2.651962373728885325 ) ) ;
#42069=CARTESIAN_POINT ( 'NONE',  ( 3.819400769403025198, -0.1694044215128273911, 2.256236840065691585 ) ) ;
#42071=CARTESIAN_POINT ( 'NONE',  ( 4.557827498477605488, 1.164984774316142113, 1.645760986912048640 ) ) ;
#42078=CARTESIAN_POINT ( 'NONE',  ( 4.428786516960594000, 0.08554295028175006033, 1.767770697671824820 ) ) ;
#42079=CARTESIAN_POINT ( 'NONE',  ( 1.008971530259877403, 1.594680585555088292, -1.375637761830387440 ) ) ;
#42082=CARTESIAN_POINT ( 'NONE',  ( 0.9417814284814338688, 1.320271805612409421, 1.461702747868667496 ) ) ;
#42089=CARTESIAN_POINT ( 'NONE',  ( 5.032044620589739559, 0.9611010790777809731, -1.604743002217932313 ) ) ;
#42091=CARTESIAN_POINT ( 'NONE',  ( 3.977443466873981759, -0.1572589350618113779, 2.064370724987254047 ) ) ;
#42101=CARTESIAN_POINT ( 'NONE',  ( 4.193769882565239193, -1.351282707657221582, -1.422545440481419510 ) ) ;
#42103=CARTESIAN_POINT ( 'NONE',  ( 2.389999771189327937, -0.002812746694069029330, 2.016288306988550438 ) ) ;
#42106=CARTESIAN_POINT ( 'NONE',  ( 1.247088714334358972, -1.471066981041386335, -1.155250539242147045 ) ) ;
#42108=CARTESIAN_POINT ( 'NONE',  ( 2.742442218595582570, 1.114876114576800248, -1.676130933394081923 ) ) ;
#42110=CARTESIAN_POINT ( 'NONE',  ( 3.163770493730236666, 1.345063228294058000, 1.635049775249038051 ) ) ;
#42113=CARTESIAN_POINT ( 'NONE',  ( 4.668459276380106715, -0.8822503692092443783, -1.873099891353036561 ) ) ;
#42115=CARTESIAN_POINT ( 'NONE',  ( 0.5387614761330473678, -1.791220285616751173, 1.078087367808887365 ) ) ;
#42117=CARTESIAN_POINT ( 'NONE',  ( 5.297797529045338294, -0.6555159417414997414, 1.704002486358429325 ) ) ;
#42124=CARTESIAN_POINT ( 'NONE',  ( 6.164708882046985750, 0.6044385376218417427, 1.814302210532907411 ) ) ;
#42134=CARTESIAN_POINT ( 'NONE',  ( 5.185172808627552143, 1.650094130669476522, 1.158673036085342112 ) ) ;
#42139=CARTESIAN_POINT ( 'NONE',  ( 1.920693274676561924, -1.396391452584997417, 1.389085034315578060 ) ) ;
#42140=CARTESIAN_POINT ( 'NONE',  ( 2.847279977023515318, 0.2930488483154705670, -1.994874153863256172 ) ) ;
#42142=CARTESIAN_POINT ( 'NONE',  ( 6.727182134110196721, 7.629137130509074716, 2.689055895399253160 ) ) ;
#42143=CARTESIAN_POINT ( 'NONE',  ( 3.925867417771063739, 1.172880473742785812, -1.850976771919823793 ) ) ;
#42145=CARTESIAN_POINT ( 'NONE',  ( 2.450113916266524416, 1.925923877722035105, 0.04935297016485720029 ) ) ;
#42148=CARTESIAN_POINT ( 'NONE',  ( 0.1333542156527530165, 6.948072531064762636, -2.641009269961028139 ) ) ;
#42155=CARTESIAN_POINT ( 'NONE',  ( 5.864778394761136049, 0.1288883805774850844, -1.836796581567698539 ) ) ;
#42156=CARTESIAN_POINT ( 'NONE',  ( 3.176434313366371942, 0.9072602101105414762, 1.797144717478225795 ) ) ;
#42157=CARTESIAN_POINT ( 'NONE',  ( 4.042538402956846966, 2.165829419810465950, -0.7696314825454602104 ) ) ;
#42158=CARTESIAN_POINT ( 'NONE',  ( -0.1288028175206907822, 7.629137130509059617, -2.873994896247424435 ) ) ;
#42159=CARTESIAN_POINT ( 'NONE',  ( 3.027998222813840901, 0.9912708380838133326, 1.574746995948882455 ) ) ;
#42162=CARTESIAN_POINT ( 'NONE',  ( 6.451426615364327155, -1.705040744490589066, 0.8662930942644477827 ) ) ;
#42165=CARTESIAN_POINT ( 'NONE',  ( 5.987849877204276083, -2.080749957983673681, -0.2039560948884494573 ) ) ;
#42167=EDGE_LOOP ( 'NONE', ( #178880, #79817, #34951, #157819 ) ) ;
#42171=CARTESIAN_POINT ( 'NONE',  ( 6.516207646108923335, -0.8203346053292108753, -1.517322292280029350 ) ) ;
#42173=CARTESIAN_POINT ( 'NONE',  ( 1.107607643408299314, -0.04344470770747606292, 1.733769432050970449 ) ) ;
#42177=CARTESIAN_POINT ( 'NONE',  ( 6.280164127638760085, -1.199209930833704085, -1.809645864181265384 ) ) ;
#42178=CARTESIAN_POINT ( 'NONE',  ( 4.353998665852670591, 1.825246345946249571, -0.04724550102237072557 ) ) ;
#42179=CARTESIAN_POINT ( 'NONE',  ( 2.658977320520792720, 1.578554556127611530, -1.164590279592196298 ) ) ;
#42183=CARTESIAN_POINT ( 'NONE',  ( 3.932379033323248230, -1.091282289853046317, -1.817994770353311473 ) ) ;
#42188=CARTESIAN_POINT ( 'NONE',  ( 1.200149190772631158, 0.8425179731405306738, -1.891261800508976298 ) ) ;
#42191=CARTESIAN_POINT ( 'NONE',  ( 3.862163208519187929, 0.7476031731964963845, -2.091851990882629408 ) ) ;
#42193=CARTESIAN_POINT ( 'NONE',  ( 2.004881263662112723, -2.228613174808518060, 0.5628491883087839431 ) ) ;
#42195=CARTESIAN_POINT ( 'NONE',  ( 6.789892339975323488, -1.342670783288713698, -1.565829586757736758 ) ) ;
#42201=CARTESIAN_POINT ( 'NONE',  ( -0.2106725631050020975, 5.721452923065615259, -2.597767226077936087 ) ) ;
#42202=CARTESIAN_POINT ( 'NONE',  ( 2.572937677043420912, 0.08726698667262809683, -1.722694834735357894 ) ) ;
#42203=CARTESIAN_POINT ( 'NONE',  ( 2.184780103950241248, 1.616692242240840960, -1.205043568535242304 ) ) ;
#42204=CARTESIAN_POINT ( 'NONE',  ( 3.075713870353123713, 2.149355976742998831, -0.7065000242163150812 ) ) ;
#42205=CARTESIAN_POINT ( 'NONE',  ( 5.092451870646586443, -2.090052423365583500, -0.2586305528886819194 ) ) ;
#42207=CARTESIAN_POINT ( 'NONE',  ( 3.901397652722672582, -0.5159380698404272270, 1.692823668428977912 ) ) ;
#42209=CARTESIAN_POINT ( 'NONE',  ( -0.02880301295727759683, -0.006976478922920535501, -2.273770288744044521 ) ) ;
#42210=CARTESIAN_POINT ( 'NONE',  ( 5.437399513225577685, 0.7426265630364609072, -1.684910612069365321 ) ) ;
#42215=CARTESIAN_POINT ( 'NONE',  ( 5.085950966588184130, -2.174626929279792176, -0.2704268894557353975 ) ) ;
#42218=CARTESIAN_POINT ( 'NONE',  ( 5.441872305809390298, 1.387781221417656141, 1.536568222347669987 ) ) ;
#42221=CARTESIAN_POINT ( 'NONE',  ( 3.229043484313653511, 0.04796440165338172745, 1.926065231962639679 ) ) ;
#42224=CARTESIAN_POINT ( 'NONE',  ( 6.398696098476772676, -2.079943653215409416, -0.4123558718646391785 ) ) ;
#42233=CARTESIAN_POINT ( 'NONE',  ( 0.8538673084422104820, -0.7095216264049221122, 1.829241926910141203 ) ) ;
#42238=CARTESIAN_POINT ( 'NONE',  ( 5.758247127753066685, -1.962046631956643195, -0.001586170976335121285 ) ) ;
#42241=CARTESIAN_POINT ( 'NONE',  ( 0.5325469457231490900, 1.160272198634606955, -1.942242498246045113 ) ) ;
#42245=CARTESIAN_POINT ( 'NONE',  ( 0.5087955169046609605, 1.624258005607306599, 0.9276666955444978768 ) ) ;
#42246=CARTESIAN_POINT ( 'NONE',  ( 5.676976676600826721, -0.7816020568793962120, -1.547713907698013092 ) ) ;
#42248=CARTESIAN_POINT ( 'NONE',  ( 3.298540952264991777, 1.726358142885858316, -1.349911518210664241 ) ) ;
#42249=CARTESIAN_POINT ( 'NONE',  ( 4.999205796216253717, 1.921780780153565793, -1.277121366954391934 ) ) ;
#42250=CARTESIAN_POINT ( 'NONE',  ( 6.573517591324530507, 1.973370851288195338, -0.5938938365465350477 ) ) ;
#42251=CARTESIAN_POINT ( 'NONE',  ( 2.044773883198697462, -1.559800846558807130, -1.156617037343915966 ) ) ;
#42254=CARTESIAN_POINT ( 'NONE',  ( 5.344028447597857223, -1.346983732444573256, -1.637812552581649594 ) ) ;
#42257=CARTESIAN_POINT ( 'NONE',  ( 3.568982563115063567, -0.9913999084223242830, 1.755768870528086056 ) ) ;
#42261=CARTESIAN_POINT ( 'NONE',  ( 1.541335573940459058, -1.321205422867760548, -1.260230113935792318 ) ) ;
#42266=CARTESIAN_POINT ( 'NONE',  ( 5.295800851330623615, -0.7439313745516599186, 1.922114966912706224 ) ) ;
#42271=CARTESIAN_POINT ( 'NONE',  ( 4.160810511097835729, 0.5408905907967902493, 1.945810383981197544 ) ) ;
#42272=CARTESIAN_POINT ( 'NONE',  ( 5.391355351084783365, -0.05288786341082692827, -2.220837934544753089 ) ) ;
#42276=CARTESIAN_POINT ( 'NONE',  ( 4.293860741714614626, -0.7905101867788848491, 1.903454510683154188 ) ) ;
#42277=CARTESIAN_POINT ( 'NONE',  ( 4.149064681782777875, 0.9530105817698063531, 1.777011888912001014 ) ) ;
#42286=CARTESIAN_POINT ( 'NONE',  ( 3.989611116449209405, 1.913510565032714883, 0.6351021849077125303 ) ) ;
#42287=CARTESIAN_POINT ( 'NONE',  ( 2.150122221082468865, -1.423577340559305071, 1.167554138749151926 ) ) ;
#42289=CARTESIAN_POINT ( 'NONE',  ( 1.401454987343775382, 1.884297621475890416, -1.332007787593261883 ) ) ;
#42291=CARTESIAN_POINT ( 'NONE',  ( 4.042369558984196587, 2.150769235480045616, 0.2162802025119994753 ) ) ;
#42293=CARTESIAN_POINT ( 'NONE',  ( 3.234050759648151363, -2.122446487128562875, -0.8823414489649589187 ) ) ;
#42296=CARTESIAN_POINT ( 'NONE',  ( 1.305301652190330675, -0.4579020413679709689, 1.813615928118620380 ) ) ;
#42297=CARTESIAN_POINT ( 'NONE',  ( 5.172717120832922788, -1.856099020970953806, -0.6648386725634397587 ) ) ;
#42301=CARTESIAN_POINT ( 'NONE',  ( 0.6278963055918493907, -2.094311335337955882, 0.6960538111202837497 ) ) ;
#42305=CARTESIAN_POINT ( 'NONE',  ( 6.639320575229294086, -0.003630812595115453199, 2.203388474976493594 ) ) ;
#42306=CARTESIAN_POINT ( 'NONE',  ( 4.785985848584410896, -0.9303070431277806751, 1.738173387191404684 ) ) ;
#42307=CARTESIAN_POINT ( 'NONE',  ( 5.654963871297442601, -1.822634436652656342, 1.415334302069543027 ) ) ;
#42308=CARTESIAN_POINT ( 'NONE',  ( 5.705462897529653965, -1.467230705000615032, -1.144726319735862585 ) ) ;
#42309=CARTESIAN_POINT ( 'NONE',  ( 3.274340622259350742, -1.012630945124261661, -1.796778529651460898 ) ) ;
#42317=CARTESIAN_POINT ( 'NONE',  ( 5.037629062015871462, 2.027634951229041693, -0.7768168075839574360 ) ) ;
#42320=CARTESIAN_POINT ( 'NONE',  ( 4.229911503591711863, 1.806553461410321582, 0.3548724298726435022 ) ) ;
#42322=CARTESIAN_POINT ( 'NONE',  ( 6.356982542327763497, 0.3766756592470664744, -2.158781491689326426 ) ) ;
#42324=CARTESIAN_POINT ( 'NONE',  ( 0.4743659920835150978, 1.303974419552447639, 1.848657746038349092 ) ) ;
#42331=CARTESIAN_POINT ( 'NONE',  ( 0.3030915354301273457, -0.4787081777068747934, 1.703804975073195394 ) ) ;
#42333=CARTESIAN_POINT ( 'NONE',  ( 5.479157358542966705, -1.820838119324312165, -0.8587918944957111389 ) ) ;
#42335=CARTESIAN_POINT ( 'NONE',  ( 4.419037640130375699, 1.924477966361681780, 0.8556825127635151462 ) ) ;
#42336=CARTESIAN_POINT ( 'NONE',  ( 2.935058904569508353, -1.567653816607515127, -1.100626458259999385 ) ) ;
#42337=CARTESIAN_POINT ( 'NONE',  ( -0.02244404828160087226, 4.081832076214893412, -2.743766916979750281 ) ) ;
#42338=CARTESIAN_POINT ( 'NONE',  ( 4.228926779721821738, -1.836881627057206590, -0.7110872907168819257 ) ) ;
#42339=CARTESIAN_POINT ( 'NONE',  ( 5.888927314555610693, -1.919185580196127283, -0.6297945592430991280 ) ) ;
#42340=CARTESIAN_POINT ( 'NONE',  ( 2.254581950620972997, -1.447608085528677480, 1.184820545849271767 ) ) ;
#42341=CARTESIAN_POINT ( 'NONE',  ( 5.514166437991733005, -0.7808720426115691726, -1.538077146617151669 ) ) ;
#42342=CARTESIAN_POINT ( 'NONE',  ( 1.476665317443916603, -1.350161712199383413, 1.354623164920423450 ) ) ;
#42344=CARTESIAN_POINT ( 'NONE',  ( 1.893488989520499377, 1.919108310403025985, -1.089527612406354873 ) ) ;
#42347=CARTESIAN_POINT ( 'NONE',  ( 6.215287892896892430, -1.681934637451238279, -1.009743211781432670 ) ) ;
#42354=CIRCLE ( 'NONE', #31976, 0.04999999999999972522 ) ;
#42356=CARTESIAN_POINT ( 'NONE',  ( 1.979048004138800998, 1.930994533390210544, 0.7472069620131777112 ) ) ;
#42360=CARTESIAN_POINT ( 'NONE',  ( 6.305353446217972113, 1.845220813986702124, -1.044706065825385943 ) ) ;
#42366=CARTESIAN_POINT ( 'NONE',  ( 5.501327308730313170, 1.985796898448642933, 0.3474119236192701465 ) ) ;
#42367=CARTESIAN_POINT ( 'NONE',  ( 5.137857799264941683, 1.913235287650059790, -0.1005462703686579862 ) ) ;
#42368=CARTESIAN_POINT ( 'NONE',  ( 6.539320575229278454, 0.5749733277502915296, 2.156147827957733742 ) ) ;
#42369=CARTESIAN_POINT ( 'NONE',  ( 2.683357600500847262, 1.551837136583393839, 1.547750905674146971 ) ) ;
#42372=CARTESIAN_POINT ( 'NONE',  ( 5.220952493833380004, 1.521736800665099976, -1.318127947290965052 ) ) ;
#42373=CARTESIAN_POINT ( 'NONE',  ( 1.740342883905017013, 1.098329146349947827, -1.565357986077076990 ) ) ;
#42377=CARTESIAN_POINT ( 'NONE',  ( 0.05236148938883232462, -1.314980595004966002, 1.528755779884483523 ) ) ;
#42379=CARTESIAN_POINT ( 'NONE',  ( 3.333613130510120648, 0.9378223671878234136, -1.868666107883134142 ) ) ;
#42381=CARTESIAN_POINT ( 'NONE',  ( 2.379564082050821483, 1.058669913282745956, 1.361546577445968964 ) ) ;
#42383=CARTESIAN_POINT ( 'NONE',  ( 6.240501835383900797, 1.219778281852833546, -1.734492557903525300 ) ) ;
#42392=CARTESIAN_POINT ( 'NONE',  ( 3.334412561109405537, 1.147067551318830203, -1.402027596893473449 ) ) ;
#42396=CARTESIAN_POINT ( 'NONE',  ( 3.703588720873185469, 1.314418127562553940, 1.246746269480051073 ) ) ;
#42397=CARTESIAN_POINT ( 'NONE',  ( 6.539320575229270460, 2.052047842581938841, 2.303245992296603983 ) ) ;
#42401=CARTESIAN_POINT ( 'NONE',  ( 3.771788145607783527, -1.833817148065859604, 0.3161742572238452897 ) ) ;
#42403=CARTESIAN_POINT ( 'NONE',  ( 1.985809494836645817, -1.915157380443854418, 0.04907906824581054206 ) ) ;
#42404=CARTESIAN_POINT ( 'NONE',  ( 0.5690311950540331010, 0.1842100624489529104, -1.816270042949569730 ) ) ;
#42413=CARTESIAN_POINT ( 'NONE',  ( 5.330891317213126257, -1.853047821147445484, -0.6673286768130722857 ) ) ;
#42416=CARTESIAN_POINT ( 'NONE',  ( 0.3926704732973253509, 1.736993494895492152, -1.163127744158433119 ) ) ;
#42417=CARTESIAN_POINT ( 'NONE',  ( 6.071306304379397112, 0.1413743337459697769, -1.921272325444240980 ) ) ;
#42419=CARTESIAN_POINT ( 'NONE',  ( 1.799542586263824795, -0.6183211656001773582, 1.717807299235304619 ) ) ;
#42420=CARTESIAN_POINT ( 'NONE',  ( 1.858336453454629611, 2.200810804183956026, -0.1644699235988852648 ) ) ;
#42422=CARTESIAN_POINT ( 'NONE',  ( 0.6856317642073318508, 1.842354612247762091, -0.5124485439033445999 ) ) ;
#42423=ORIENTED_EDGE ( 'NONE', *, *, #99041, .F. ) ;
#42424=CARTESIAN_POINT ( 'NONE',  ( 0.2386330332824412315, -1.909482672672847992, -0.4822418261516500659 ) ) ;
#42425=CARTESIAN_POINT ( 'NONE',  ( 3.140110198738320424, 0.4743784485543530716, 1.883105278476588706 ) ) ;
#42426=ORIENTED_EDGE ( 'NONE', *, *, #79797, .T. ) ;
#42429=CARTESIAN_POINT ( 'NONE',  ( 6.912964126797830566, -1.438640208141970245, 1.180240733875538517 ) ) ;
#42433=CARTESIAN_POINT ( 'NONE',  ( 3.105210138592546798, -0.4252477525170209605, 2.149737936336936883 ) ) ;
#42434=DIRECTION ( 'NONE',  ( 1.214306433183764966E-17, 1.000000000000000000, 5.200009205990155575E-32 ) ) ;
#42437=CARTESIAN_POINT ( 'NONE',  ( 3.035583632137848653, -1.226507576337819483, -1.352503160878690380 ) ) ;
#42445=CARTESIAN_POINT ( 'NONE',  ( 0.5395173010800574653, -1.361483316988669978, -1.363248745070398726 ) ) ;
#42446=CARTESIAN_POINT ( 'NONE',  ( 5.330891710049517229, -1.845885424482188286, -0.6645199359083459045 ) ) ;
#42450=CARTESIAN_POINT ( 'NONE',  ( 4.458633810090739225, -1.957822973221786444, -0.9849130632908836835 ) ) ;
#42453=CARTESIAN_POINT ( 'NONE',  ( 4.961816271168416392, -0.5573412460852051886, 1.993729458732765858 ) ) ;
#42455=CARTESIAN_POINT ( 'NONE',  ( 4.711759750379289180, 2.199509664246365848, 0.6680300025654511975 ) ) ;
#42458=CARTESIAN_POINT ( 'NONE',  ( 0.7973255588549054140, 1.877056169618742443, 1.315483550797888812 ) ) ;
#42461=CARTESIAN_POINT ( 'NONE',  ( 4.804598357785225815, 1.690330731384475094, 0.9558792251623483560 ) ) ;
#42465=CARTESIAN_POINT ( 'NONE',  ( 5.150612376422202487, 1.885107930906554152, 0.3209214958604587054 ) ) ;
#42466=CARTESIAN_POINT ( 'NONE',  ( 6.211878148792838061, -1.711051158068075839, 0.2163953478501578487 ) ) ;
#42467=CARTESIAN_POINT ( 'NONE',  ( 5.419157771004846857, -1.820987890746316173, 0.8666037247077316152 ) ) ;
#42471=CARTESIAN_POINT ( 'NONE',  ( 1.535224857807856669, -1.515203476157600537, -1.440707689706053563 ) ) ;
#42472=CARTESIAN_POINT ( 'NONE',  ( 0.4613126893583847643, 1.751520745650859912, -0.2531317886874852041 ) ) ;
#42473=CARTESIAN_POINT ( 'NONE',  ( 5.520157785563180930, -1.821743191724470634, 0.8647220171385738841 ) ) ;
#42475=CARTESIAN_POINT ( 'NONE',  ( 3.468945898361298408, 0.05672114714776231581, -2.291715584554415930 ) ) ;
#42476=CARTESIAN_POINT ( 'NONE',  ( 1.886251080576596406, 1.515106702303461894, -0.8561229301769134326 ) ) ;
#42478=CARTESIAN_POINT ( 'NONE',  ( 3.111701630267147412, 1.674174984267240429, 1.301503359413098249 ) ) ;
#42480=CARTESIAN_POINT ( 'NONE',  ( 1.739138385086140159, -1.644397438216003593, -0.5498640316261136363 ) ) ;
#42482=CARTESIAN_POINT ( 'NONE',  ( 2.154548830654204217, -0.4927303200079625745, -1.794580903941452865 ) ) ;
#42483=CARTESIAN_POINT ( 'NONE',  ( 2.330757530436095237, -1.336968151498512336, 1.710609410560095522 ) ) ;
#42484=CARTESIAN_POINT ( 'NONE',  ( 3.239470508323912146, 0.4852670486454255250, -1.957170429962351577 ) ) ;
#42485=CARTESIAN_POINT ( 'NONE',  ( 4.312500000000001776, 1.451031289061289531, 1.451031289060941587 ) ) ;
#42487=CARTESIAN_POINT ( 'NONE',  ( 1.465712096425618949, 1.898328545170711035, -0.3267402372346754902 ) ) ;
#42489=CARTESIAN_POINT ( 'NONE',  ( 3.287547529179511319, 0.05108950329585186523, -2.220969887641692342 ) ) ;
#42491=CARTESIAN_POINT ( 'NONE',  ( -0.2108831679770960255, 0.2438762813419328990, -1.931650693707862132 ) ) ;
#42496=CARTESIAN_POINT ( 'NONE',  ( 5.678047454291774265, 2.188620968312010362, -0.3794988778502098592 ) ) ;
#42497=CARTESIAN_POINT ( 'NONE',  ( 5.125427350195786325, 0.1941421753944693185, -1.952251141935714918 ) ) ;
#42501=CARTESIAN_POINT ( 'NONE',  ( 6.204402397823557180, -0.8056473179405240215, -2.114295379420629839 ) ) ;
#42505=CARTESIAN_POINT ( 'NONE',  ( 1.785667050844968351, -1.942997710132963407, 0.6927838567832644845 ) ) ;
#42510=CARTESIAN_POINT ( 'NONE',  ( 3.831198023013999698, -1.729401117988647929, 0.7132991360168300377 ) ) ;
#42511=CARTESIAN_POINT ( 'NONE',  ( 3.023724745236521017, -1.528101708971361106, 0.8198667277116710173 ) ) ;
#42512=CARTESIAN_POINT ( 'NONE',  ( 6.286699343557897279, 1.907799665397521105, -1.078441415684105120 ) ) ;
#42513=CARTESIAN_POINT ( 'NONE',  ( 0.5345543961663907773, 1.132513062451316221, -1.893880525681296723 ) ) ;
#42514=CARTESIAN_POINT ( 'NONE',  ( 4.722262070665103728, 2.001137821747037915, 0.6055792653000735548 ) ) ;
#42515=CARTESIAN_POINT ( 'NONE',  ( 5.947205882781483766, 0.5613781043299302942, -1.859040749089553524 ) ) ;
#42517=CARTESIAN_POINT ( 'NONE',  ( 0.3437500000590538174, 1.895863741711102612, 0.7852924748299703328 ) ) ;
#42518=CARTESIAN_POINT ( 'NONE',  ( -0.01695367945527340853, -2.016028864686558730, -0.04667425414178058563 ) ) ;
#42527=CARTESIAN_POINT ( 'NONE',  ( 3.861776535121093090, 1.811678901967550326, -0.2252020330209548171 ) ) ;
#42528=CARTESIAN_POINT ( 'NONE',  ( 1.800138458411651765, -0.7431416638853625134, 2.077998897882806784 ) ) ;
#42534=CARTESIAN_POINT ( 'NONE',  ( 1.529563250702131727, -0.2428666551740152890, 2.005035470024270960 ) ) ;
#42539=CARTESIAN_POINT ( 'NONE',  ( 2.729178580549945110, 0.09652143117058623045, -1.858595261477024918 ) ) ;
#42545=CARTESIAN_POINT ( 'NONE',  ( 4.441915170580639227, 0.7783198120194650960, -1.651611053696280695 ) ) ;
#42550=CARTESIAN_POINT ( 'NONE',  ( 0.7019813383442319310, -1.220362748482771487, -1.231932065070516558 ) ) ;
#42551=CARTESIAN_POINT ( 'NONE',  ( 5.806566994037906326, 1.625791660643903791, 0.8640615347050364381 ) ) ;
#42552=CARTESIAN_POINT ( 'NONE',  ( 4.688248866636615553, -1.090845489383242883, 2.033590232148785759 ) ) ;
#42554=CARTESIAN_POINT ( 'NONE',  ( 6.538358481810655043, 2.137031053877674225, 0.3242996077847115632 ) ) ;
#42556=CARTESIAN_POINT ( 'NONE',  ( 5.817770776407988009, -1.817369610395104695, 1.406990027747441419 ) ) ;
#42559=CARTESIAN_POINT ( 'NONE',  ( 5.313307075269409374, -0.2735208697075517947, 1.850433306854900817 ) ) ;
#42561=CARTESIAN_POINT ( 'NONE',  ( 2.531394148431935776, -0.1834752923718513118, 1.903540536635806912 ) ) ;
#42563=CARTESIAN_POINT ( 'NONE',  ( 4.424592250794217030, 1.359014646446855767, -1.738718759629574118 ) ) ;
#42564=CARTESIAN_POINT ( 'NONE',  ( 4.469977352714805008, -0.9950975051371075963, 1.868896417504315677 ) ) ;
#42566=CARTESIAN_POINT ( 'NONE',  ( 6.883263157960405998, 2.961743250487959056, 2.498998094365055600 ) ) ;
#42567=CARTESIAN_POINT ( 'NONE',  ( -0.2108831679771203116, 0.7314853703891763814, -1.979988191570913880 ) ) ;
#42570=CARTESIAN_POINT ( 'NONE',  ( 1.923324260599985402, 2.153519634812319783, 0.8294600792757185204 ) ) ;
#42571=CARTESIAN_POINT ( 'NONE',  ( 2.031626174157370457, 1.878314540015123102, -0.5664888411779643862 ) ) ;
#42573=CARTESIAN_POINT ( 'NONE',  ( 6.526245194314398645, 1.055377990298064450, 1.771961156250308145 ) ) ;
#42575=CARTESIAN_POINT ( 'NONE',  ( 4.083220446344194343, 1.622485107653489633, 1.197306254465977826 ) ) ;
#42578=CARTESIAN_POINT ( 'NONE',  ( 4.399625206644591557, -1.976670321813909892, 0.3981083777728141038 ) ) ;
#42582=CARTESIAN_POINT ( 'NONE',  ( 2.501036472447940362, 0.4719354416190780777, 2.119019701963683833 ) ) ;
#42586=CARTESIAN_POINT ( 'NONE',  ( 2.055717040066493695, 1.865871300129381183, -0.1328275987748789300 ) ) ;
#42587=CARTESIAN_POINT ( 'NONE',  ( 6.204392391313840349, -0.7715976231806520591, -2.019385000091134419 ) ) ;
#42588=CARTESIAN_POINT ( 'NONE',  ( -0.02244404828160087226, 1.995160441984781041, -2.602654351998904492 ) ) ;
#42592=CARTESIAN_POINT ( 'NONE',  ( 3.721269560815092525, 1.641568950759502377, 0.9805937191851579193 ) ) ;
#42594=CARTESIAN_POINT ( 'NONE',  ( 4.258513496744737559, -1.310932089386746879, 1.189237179687177015 ) ) ;
#42595=CARTESIAN_POINT ( 'NONE',  ( 1.506358462150747091, -1.903157483220425883, -0.1863595701613318389 ) ) ;
#42597=CARTESIAN_POINT ( 'NONE',  ( -0.1181432109131977104, -1.915350881444439102, -0.04437447078771068754 ) ) ;
#42599=CARTESIAN_POINT ( 'NONE',  ( 0.9067890187421032699, 0.5993529260880943177, 1.981728858978973218 ) ) ;
#42601=CARTESIAN_POINT ( 'NONE',  ( 6.719622092096638966, -1.813896567892055112, 0.4569536213836836169 ) ) ;
#42602=CARTESIAN_POINT ( 'NONE',  ( 1.717148762710469789, -0.2249250470785572054, 1.811706739299999924 ) ) ;
#42603=CARTESIAN_POINT ( 'NONE',  ( 5.672569038193632451, -1.402732290180560337, 1.703733612381942653 ) ) ;
#42606=CARTESIAN_POINT ( 'NONE',  ( 3.543474241949475356, 1.865888119384132127, -0.8795106731672995837 ) ) ;
#42612=CARTESIAN_POINT ( 'NONE',  ( 5.828598057497599960, -1.316348130051235410, 1.597988563933512074 ) ) ;
#42614=CARTESIAN_POINT ( 'NONE',  ( 2.759224924868249662, -1.879262701025650850, -1.068020781904190253 ) ) ;
#42616=CARTESIAN_POINT ( 'NONE',  ( 2.824872690137433029, 1.461285568133148693, -1.394416722739227898 ) ) ;
#42617=CARTESIAN_POINT ( 'NONE',  ( 2.031626174157370457, 1.878314540015123102, -0.5664888411779643862 ) ) ;
#42618=CARTESIAN_POINT ( 'NONE',  ( 6.620655732516645742, 7.051964633898824886, 2.771890290588132189 ) ) ;
#42623=CARTESIAN_POINT ( 'NONE',  ( 1.745327705122714956, 0.3399549603602426417, -1.987498286102694411 ) ) ;
#42625=CARTESIAN_POINT ( 'NONE',  ( 5.829655996829377962, 1.081331853127937448, -1.906115348727636549 ) ) ;
#42627=CARTESIAN_POINT ( 'NONE',  ( 6.029550621839829816, -0.2273517531893587407, 1.898748578088353733 ) ) ;
#42632=CARTESIAN_POINT ( 'NONE',  ( 3.532827515057835654, -1.646827434736859441, 1.163287548526056980 ) ) ;
#42635=CARTESIAN_POINT ( 'NONE',  ( 4.893404818765360709, 1.279633041931761639, 1.156618277182480892 ) ) ;
#42640=CARTESIAN_POINT ( 'NONE',  ( 4.165207536865437099, 0.2314014899743311315, -1.856129391651973215 ) ) ;
#42642=CARTESIAN_POINT ( 'NONE',  ( 1.586871713678970730, 1.994102569620255228, 0.5559867524188369936 ) ) ;
#42643=CARTESIAN_POINT ( 'NONE',  ( 6.795378861676105053, -1.851214886592133846, 0.9271815693319698237 ) ) ;
#42646=CARTESIAN_POINT ( 'NONE',  ( 0.1404700283944440298, 1.733558474490008772, 0.5260085833052421389 ) ) ;
#42651=CARTESIAN_POINT ( 'NONE',  ( 1.012071980069819910, 1.959787197952606252, -0.09269708818125664551 ) ) ;
#42653=CARTESIAN_POINT ( 'NONE',  ( 5.290618452874795707, 1.447395081947447704, -1.254909122497225971 ) ) ;
#42662=CARTESIAN_POINT ( 'NONE',  ( 3.555696680978126079, 0.5271953485486252644, -2.096301903996622862 ) ) ;
#42666=CARTESIAN_POINT ( 'NONE',  ( 4.858326754937916547, 0.6996357133068829004, 1.686392194618462570 ) ) ;
#42669=CARTESIAN_POINT ( 'NONE',  ( 0.8605430240068573378, -1.430899983082928761, 1.356264857227080567 ) ) ;
#42670=CARTESIAN_POINT ( 'NONE',  ( 3.480628297764537304, -1.280852673386581264, 1.420289963180096260 ) ) ;
#42673=CARTESIAN_POINT ( 'NONE',  ( 5.213322861785598228, -1.662839039401903696, -1.055205849181278799 ) ) ;
#42675=CARTESIAN_POINT ( 'NONE',  ( 6.058146487192490603, -1.370253782545840293, 1.376481248621561182 ) ) ;
#42682=CARTESIAN_POINT ( 'NONE',  ( 3.475170734053119048, -1.687717282722025924, -0.8990902037325496643 ) ) ;
#42687=CARTESIAN_POINT ( 'NONE',  ( 4.670568766136569572, 0.7725349690445941775, 1.859148924064259356 ) ) ;
#42689=CARTESIAN_POINT ( 'NONE',  ( 6.322862864304120478, 1.705426906915354035, 0.6521430802832667295 ) ) ;
#42690=CARTESIAN_POINT ( 'NONE',  ( 5.489470343000498076, -0.4852711138302409077, 1.957169415941109047 ) ) ;
#42691=CARTESIAN_POINT ( 'NONE',  ( 6.727182134110208267, 1.290711256955964448, 1.927001067762003750 ) ) ;
#42692=CARTESIAN_POINT ( 'NONE',  ( 1.926316106172959230, 1.062450747350886848, 1.776810178100460824 ) ) ;
#42696=CARTESIAN_POINT ( 'NONE',  ( 6.684453402082996654, -1.835023323784425564, -0.3624468955198830722 ) ) ;
#42698=( NAMED_UNIT ( * ) PLANE_ANGLE_UNIT ( ) SI_UNIT ( $, .RADIAN. ) );
#42702=CARTESIAN_POINT ( 'NONE',  ( 6.825078400183556937, 1.302289051367941708, 1.872899343898648983 ) ) ;
#42704=CARTESIAN_POINT ( 'NONE',  ( 4.623498406067056088, 0.3027793956022621913, 1.707322668435699242 ) ) ;
#42706=CARTESIAN_POINT ( 'NONE',  ( 2.307561340129569150, -1.660171796135110567, -1.236610361758017973 ) ) ;
#42707=CARTESIAN_POINT ( 'NONE',  ( 3.638375168990032549, 0.7640726493506818651, 1.974712724135726516 ) ) ;
#42710=CARTESIAN_POINT ( 'NONE',  ( 1.867950311876313219, -1.955179860842346296, 0.2357939167430597172 ) ) ;
#42714=CARTESIAN_POINT ( 'NONE',  ( 3.908379099077957886, 1.621946506101832775, -1.620046465671644675 ) ) ;
#42715=CARTESIAN_POINT ( 'NONE',  ( 1.611646134362737959, -1.812087876328593916, 0.2219229778191167957 ) ) ;
#42719=CARTESIAN_POINT ( 'NONE',  ( 3.023692480417307316, -0.3885771752702297799, 1.975188976417296072 ) ) ;
#42720=CARTESIAN_POINT ( 'NONE',  ( 2.184356868638567928, 1.133688150830698627, -1.600809071968431807 ) ) ;
#42723=CARTESIAN_POINT ( 'NONE',  ( 0.07536363704230969462, 1.333366039338843789, -2.397125032416930424 ) ) ;
#42724=CARTESIAN_POINT ( 'NONE',  ( 4.927721519287828755, 1.075078395752477878, -1.792878403059654513 ) ) ;
#42725=CARTESIAN_POINT ( 'NONE',  ( 3.150976108479891735, -1.446007784402236318, -1.020181273144848744 ) ) ;
#42727=CARTESIAN_POINT ( 'NONE',  ( 6.123008101752742682, -2.160436397662615970, 0.7664941572692751670 ) ) ;
#42728=CARTESIAN_POINT ( 'NONE',  ( 6.122986541590657694, -1.636244173936936885, 0.5932577488661006093 ) ) ;
#42730=CARTESIAN_POINT ( 'NONE',  ( 5.871801794802778751, -0.3338885390306855494, -2.274238935559732333 ) ) ;
#42732=CARTESIAN_POINT ( 'NONE',  ( 5.430864382934267987, 0.8560856307190685133, 1.507619432454242681 ) ) ;
#42733=CARTESIAN_POINT ( 'NONE',  ( 6.368375356916068597, -1.978549699825098429, -0.3886382054163611821 ) ) ;
#42735=CARTESIAN_POINT ( 'NONE',  ( 5.564936049989869460, 1.647787920686558438, -1.413916910601682897 ) ) ;
#42737=CARTESIAN_POINT ( 'NONE',  ( -0.06503379110851194300, -1.696408147887063178, 1.266814603907985504 ) ) ;
#42738=CARTESIAN_POINT ( 'NONE',  ( 6.125000000000003553, -2.052068128417929849, 3.487440458529189440E-13 ) ) ;
#42741=CARTESIAN_POINT ( 'NONE',  ( 4.911117597291495329, 1.675855952751242883, 0.9498910403669177382 ) ) ;
#42743=CARTESIAN_POINT ( 'NONE',  ( -0.07508257667859614959, -0.9546805890920804227, -2.003339222774684458 ) ) ;
#42748=CARTESIAN_POINT ( 'NONE',  ( 2.192296887966191488, 1.369148959659401754, 1.749082743080948799 ) ) ;
#42750=EDGE_CURVE ( 'NONE', #70481, #65102, #71971, .T. ) ;
#42755=CARTESIAN_POINT ( 'NONE',  ( 0.2994542103806375200, 1.388483683912977495, -1.462447666687356485 ) ) ;
#42757=CARTESIAN_POINT ( 'NONE',  ( 5.037578369333176376, 1.925844591945893747, -0.7392275334625797445 ) ) ;
#42762=CARTESIAN_POINT ( 'NONE',  ( 1.299667926800106121, -1.769921777095804671, -0.007132476793576813211 ) ) ;
#42763=CARTESIAN_POINT ( 'NONE',  ( -0.06968618116158857567, -1.560424145883563929, -1.276814929289785239 ) ) ;
#42764=CARTESIAN_POINT ( 'NONE',  ( 5.935049520445493165, -1.266825670006064275, -1.193719461430408968 ) ) ;
#42765=CARTESIAN_POINT ( 'NONE',  ( 3.790815982946276641, 1.936215313137353178, -1.226956277148362862 ) ) ;
#42767=CARTESIAN_POINT ( 'NONE',  ( 1.939159035295745959, 0.7054217538491479589, -1.700835786604155242 ) ) ;
#42770=CARTESIAN_POINT ( 'NONE',  ( 3.012524388372894713, 1.323457619556423381, -1.257707024427484388 ) ) ;
#42771=CARTESIAN_POINT ( 'NONE',  ( 3.990861413484114273, -2.010826503599131065, 0.1511389102963680842 ) ) ;
#42773=CARTESIAN_POINT ( 'NONE',  ( 1.815646767810099149, -0.2761031220132881270, 2.245556248662975207 ) ) ;
#42775=CARTESIAN_POINT ( 'NONE',  ( 5.227606396355295892, -2.000638224736817516, 0.6578950869102012655 ) ) ;
#42777=CARTESIAN_POINT ( 'NONE',  ( 2.225130849662222410, -1.891980959128433781, -0.8411517639917851508 ) ) ;
#42780=CARTESIAN_POINT ( 'NONE',  ( 4.740951199079581180, 2.029406658027664623, 0.6148427566107574904 ) ) ;
#42781=CARTESIAN_POINT ( 'NONE',  ( 1.172347479525590375, -1.222655876604409553, 1.488804252732379485 ) ) ;
#42787=CARTESIAN_POINT ( 'NONE',  ( 5.801066647469003357, -0.3129311994157328303, -2.097281602037828208 ) ) ;
#42788=CARTESIAN_POINT ( 'NONE',  ( 2.432770431885710405, 2.042423857386191255, 0.5128348284264750978 ) ) ;
#42791=CARTESIAN_POINT ( 'NONE',  ( 6.315283160355378733, -1.595611397598785564, -0.9574585435550940771 ) ) ;
#42796=EDGE_LOOP ( 'NONE', ( #12763, #164484 ) ) ;
#42797=CARTESIAN_POINT ( 'NONE',  ( -0.2104748580754166598, -0.006608320950483163522, -2.103482951484026753 ) ) ;
#42800=CARTESIAN_POINT ( 'NONE',  ( 3.877359892829432386, -0.1466975079335990917, 1.956454564409334296 ) ) ;
#42801=CARTESIAN_POINT ( 'NONE',  ( 0.5323697292517782786, 1.110078392871534314, -1.854780036684190669 ) ) ;
#42806=CARTESIAN_POINT ( 'NONE',  ( 2.677380959318215847, -0.8946470780417746793, 1.492600998661142375 ) ) ;
#42810=CARTESIAN_POINT ( 'NONE',  ( 2.073592080879012478, 1.495823877299466087, -1.351946161731142126 ) ) ;
#42814=CARTESIAN_POINT ( 'NONE',  ( 2.201972163173575137, -1.971069923813788982, 0.04663598398449429056 ) ) ;
#42817=CARTESIAN_POINT ( 'NONE',  ( 5.836178160628028522, -1.067892152678026951, -1.586260290404594597 ) ) ;
#42822=CARTESIAN_POINT ( 'NONE',  ( 0.9967468350138152244, -1.970926226424707606, -0.4403189329902043037 ) ) ;
#42824=CARTESIAN_POINT ( 'NONE',  ( 5.702268328713489431, -2.307758713666784534, -0.007378162171353326235 ) ) ;
#42825=CARTESIAN_POINT ( 'NONE',  ( 6.496542546517183325, 1.940334402339534581, 0.2891159199209930031 ) ) ;
#42826=CARTESIAN_POINT ( 'NONE',  ( 2.799599750139214471, -1.450362073461785473, -1.321114446766240347 ) ) ;
#42828=CARTESIAN_POINT ( 'NONE',  ( 0.2115648487451895210, 1.930418618556551946, 0.5826528611774862698 ) ) ;
#42830=CARTESIAN_POINT ( 'NONE',  ( 0.7962977453638077074, -0.9578387366565711547, -1.888411434433327374 ) ) ;
#42833=CARTESIAN_POINT ( 'NONE',  ( 2.519273208346615611, -1.059988974693906405, -1.505194322970206944 ) ) ;
#42836=CARTESIAN_POINT ( 'NONE',  ( 2.514065211524143084, -0.6609878990531635745, 2.015050547854141172 ) ) ;
#42840=CARTESIAN_POINT ( 'NONE',  ( 4.147771190963340793, 0.6980094919085011451, -1.939086781881957933 ) ) ;
#42842=CARTESIAN_POINT ( 'NONE',  ( 0.8547319020580852467, 0.3593373433725781108, -1.805665335529122784 ) ) ;
#42847=CARTESIAN_POINT ( 'NONE',  ( 1.524350002934187653, -1.228176919886795782, -1.833354347511229498 ) ) ;
#42848=CARTESIAN_POINT ( 'NONE',  ( 2.390224264847177871, -0.9692217175977213550, 2.044435098530998474 ) ) ;
#42850=CARTESIAN_POINT ( 'NONE',  ( 2.583996913715621790, 0.9723193252555061283, 1.528341728153536305 ) ) ;
#42851=CARTESIAN_POINT ( 'NONE',  ( 2.641684811942858424, 1.906066497734011378, -0.1923337340370822046 ) ) ;
#42852=CARTESIAN_POINT ( 'NONE',  ( 3.930184216435282707, 1.147649575447948100, 1.722966636330313550 ) ) ;
#42854=CARTESIAN_POINT ( 'NONE',  ( 3.256668630020958410, -1.493913901992610205, 1.286540209188108630 ) ) ;
#42855=CARTESIAN_POINT ( 'NONE',  ( 6.639296574806412110, -1.719437650081551139, 0.8690664522189944785 ) ) ;
#42856=CARTESIAN_POINT ( 'NONE',  ( 4.487079325084206260, 1.670935625628103605, -0.8411387520786617333 ) ) ;
#42857=CARTESIAN_POINT ( 'NONE',  ( 2.508792734928457335, -0.8846401781386037388, -2.131589412884911106 ) ) ;
#42859=CARTESIAN_POINT ( 'NONE',  ( 3.385049140913086507, 0.04320281034062402326, 1.860716667189839635 ) ) ;
#42865=CARTESIAN_POINT ( 'NONE',  ( 0.8035136555551088966, 1.722860008830621847, 1.211028463478396988 ) ) ;
#42867=CARTESIAN_POINT ( 'NONE',  ( 6.397764797294555272, -0.7349420381566433846, 2.032942830986879557 ) ) ;
#42868=CARTESIAN_POINT ( 'NONE',  ( 2.549219474610735947, 0.2639673528169217964, 2.104066465523121376 ) ) ;
#42869=CARTESIAN_POINT ( 'NONE',  ( 0.07057728186875102117, 0.7769860399358395897, 1.864564603342239835 ) ) ;
#42872=CARTESIAN_POINT ( 'NONE',  ( 0.7905619602705875604, -2.145198653374354336, -0.2653712149464776959 ) ) ;
#42877=CARTESIAN_POINT ( 'NONE',  ( 5.190638768449240992, 1.523797776992100284, -1.320824044268428255 ) ) ;
#42880=CARTESIAN_POINT ( 'NONE',  ( 5.787991602622606813, -0.9759734195362681497, 1.928925553883020338 ) ) ;
#42885=CARTESIAN_POINT ( 'NONE',  ( 0.1576404624921414199, 1.103540182269863612, 1.565583644703759436 ) ) ;
#42889=CARTESIAN_POINT ( 'NONE',  ( 3.105755298912396878, -1.722902020775359144, 0.08520973767557615819 ) ) ;
#42893=CARTESIAN_POINT ( 'NONE',  ( 1.246904684444858136, -1.390570190391905658, -1.094529049636628226 ) ) ;
#42894=CARTESIAN_POINT ( 'NONE',  ( 2.068995670861985658, -1.554830924100785161, 1.278664071131753843 ) ) ;
#42896=CARTESIAN_POINT ( 'NONE',  ( 4.348781676370103710, 0.5853419563807431558, 2.127667884090424621 ) ) ;
#42900=CARTESIAN_POINT ( 'NONE',  ( 3.387459763963754700, 0.05019612904376415108, -2.120051327867578550 ) ) ;
#42901=CARTESIAN_POINT ( 'NONE',  ( 2.741814726283864800, 2.006445297011373974, -0.2004551355171620974 ) ) ;
#42902=CARTESIAN_POINT ( 'NONE',  ( 3.849720854566369255, -1.253557171431567863, -1.308061721885760198 ) ) ;
#42906=CARTESIAN_POINT ( 'NONE',  ( 0.1626889888870358680, -1.668787113083155305, -0.8454427722031019332 ) ) ;
#42908=CARTESIAN_POINT ( 'NONE',  ( 5.795480788678070816, 1.385457615097264394, 1.189071861804301466 ) ) ;
#42910=CARTESIAN_POINT ( 'NONE',  ( 2.553800400642152635, 1.028702656226655465, 1.615903109786074099 ) ) ;
#42918=CARTESIAN_POINT ( 'NONE',  ( 2.830460552442021438, -1.048868820301660953, -1.842999677239331113 ) ) ;
#42919=CARTESIAN_POINT ( 'NONE',  ( -0.1294898018151836583, 0.7212281881416956475, -2.008332099035778917 ) ) ;
#42921=CARTESIAN_POINT ( 'NONE',  ( 4.218015588379292247, -1.010805368333337562, -1.692340417948991371 ) ) ;
#42922=CARTESIAN_POINT ( 'NONE',  ( 0.2111898618733127897, 1.671471951565723035, -1.121848769376234234 ) ) ;
#42924=CARTESIAN_POINT ( 'NONE',  ( 6.210183267806027807, 1.217293573752244784, -1.732272713164469735 ) ) ;
#42926=CARTESIAN_POINT ( 'NONE',  ( 1.346235217667652417, -0.9325981557438846048, 1.848514419461377845 ) ) ;
#42927=CARTESIAN_POINT ( 'NONE',  ( 3.204954726155031963, -0.3781314774268499379, 1.904617838069742275 ) ) ;
#42931=CARTESIAN_POINT ( 'NONE',  ( 3.767594164193796669, 1.161519562870310329, 1.738068047407430816 ) ) ;
#42935=CARTESIAN_POINT ( 'NONE',  ( 0.6447925058646056806, 0.1317677938489550116, 1.806752140514777283 ) ) ;
#42937=CARTESIAN_POINT ( 'NONE',  ( 5.303435803989668074, 1.802500012205746183, 1.273053691228965389 ) ) ;
#42939=CARTESIAN_POINT ( 'NONE',  ( 2.749284697512776710, -1.835294401387000285, 1.225074929180599570 ) ) ;
#42942=CARTESIAN_POINT ( 'NONE',  ( 2.508343198132975349, -1.907285675847451234, -0.1387974571645037292 ) ) ;
#42945=CARTESIAN_POINT ( 'NONE',  ( 5.758279222819879806, -2.070544812512797428, -0.003756845764937844813 ) ) ;
#42947=CARTESIAN_POINT ( 'NONE',  ( 3.116266767097406909, -1.064116542966097922, -1.881565754655416756 ) ) ;
#42948=CARTESIAN_POINT ( 'NONE',  ( 5.302338810847701644, 1.659911028786088538, -1.431018553749352051 ) ) ;
#42960=CARTESIAN_POINT ( 'NONE',  ( 5.858279169847476098, -2.070434559870216074, -0.005763162253501209233 ) ) ;
#42961=CARTESIAN_POINT ( 'NONE',  ( 4.459546661884671970, 0.4205705884572363829, -1.879884317620848178 ) ) ;
#42962=CARTESIAN_POINT ( 'NONE',  ( 0.2632962822839111650, 1.880428227362867633, -0.7283992291491693249 ) ) ;
#42967=CARTESIAN_POINT ( 'NONE',  ( 5.489095164188675824, 0.1408790922432824055, 1.964433151921646470 ) ) ;
#42968=CARTESIAN_POINT ( 'NONE',  ( 0.1116237293282626442, -2.148295633857814746, 0.4319020730012904097 ) ) ;
#42969=CARTESIAN_POINT ( 'NONE',  ( 4.951681858558426796, 0.5695450498939165218, -1.734646904759745700 ) ) ;
#42975=CARTESIAN_POINT ( 'NONE',  ( 2.173174093899932657, 1.133995793187540180, 1.450494936146892622 ) ) ;
#42976=CARTESIAN_POINT ( 'NONE',  ( 5.976820168803962829, -1.420628428873932814, 1.426715538211227763 ) ) ;
#42977=CARTESIAN_POINT ( 'NONE',  ( 1.335823321505170025, -1.456863090139989714, 1.777644367010343451 ) ) ;
#42978=CARTESIAN_POINT ( 'NONE',  ( 6.069191303861535935, 1.728486752094375190, 0.9278679456784575397 ) ) ;
#42982=CARTESIAN_POINT ( 'NONE',  ( 0.8540665308606997241, -0.7467690478978536994, 1.931163149162813619 ) ) ;
#42984=CARTESIAN_POINT ( 'NONE',  ( 1.171554334673271303, 1.248344470866637135, 1.676987088486236566 ) ) ;
#42985=CARTESIAN_POINT ( 'NONE',  ( 1.129532124359374334, -1.183843481993757774, -1.448407549327054955 ) ) ;
#42986=CARTESIAN_POINT ( 'NONE',  ( 1.440779594245532369, 1.198675164295496920, 1.620935466883965503 ) ) ;
#42988=CARTESIAN_POINT ( 'NONE',  ( 2.137881509367345778, 0.3822841233627124469, 1.697745509426834332 ) ) ;
#42991=CARTESIAN_POINT ( 'NONE',  ( 2.965164839364425653, 0.2526306750327989015, -1.706137528056344888 ) ) ;
#42992=CARTESIAN_POINT ( 'NONE',  ( 2.876726420669137863, -0.1638259704515396820, -2.185508879517850112 ) ) ;
#42993=CARTESIAN_POINT ( 'NONE',  ( 4.670673364294657404, -1.443042178620690841, 1.669811033208345341 ) ) ;
#42995=CARTESIAN_POINT ( 'NONE',  ( 2.430757386254971841, -1.338474561058100143, 1.709278666203792652 ) ) ;
#42996=CARTESIAN_POINT ( 'NONE',  ( 0.8557438351849018243, 1.823752217391808372, -0.08689656109241167270 ) ) ;
#42997=CARTESIAN_POINT ( 'NONE',  ( 3.802059961758995854, -1.092030603714509551, -1.813900157284773496 ) ) ;
#43001=CARTESIAN_POINT ( 'NONE',  ( 3.474455725741688372, -2.209678783342132746, -0.6099929035564675139 ) ) ;
#43005=CARTESIAN_POINT ( 'NONE',  ( 6.393255305546848177, -0.1058262492604696708, -2.218914918540932035 ) ) ;
#43013=CARTESIAN_POINT ( 'NONE',  ( 3.938125092175647879, -1.678004675797317713, -1.117833462672225497 ) ) ;
#43015=CARTESIAN_POINT ( 'NONE',  ( 3.819230306994053858, -1.816680642618787145, -0.9767294869839551197 ) ) ;
#43020=CARTESIAN_POINT ( 'NONE',  ( 5.859372887940716090, 2.159598860408561194, -0.3713886045505072064 ) ) ;
#43021=CARTESIAN_POINT ( 'NONE',  ( 3.059220373557011818, -1.198860207862334049, 1.621182619130703051 ) ) ;
#43022=CARTESIAN_POINT ( 'NONE',  ( 1.628196140939692338, 0.1813696128579282696, 1.832309401408799276 ) ) ;
#43026=CARTESIAN_POINT ( 'NONE',  ( 5.895480738319402114, 1.384055093596334274, 1.190509915477963698 ) ) ;
#43027=CARTESIAN_POINT ( 'NONE',  ( -0.1042281025761494367, -0.9885194109933435058, -2.072332397174360352 ) ) ;
#43029=CARTESIAN_POINT ( 'NONE',  ( 5.963815663052111304, 2.230244011310183794, -0.3799797021378086836 ) ) ;
#43031=CARTESIAN_POINT ( 'NONE',  ( 2.297617436792959378, 1.628516202021938808, 1.335460665606647446 ) ) ;
#43041=CARTESIAN_POINT ( 'NONE',  ( 3.270003694065525046, 0.5362613544047705183, -2.155619276402853224 ) ) ;
#43042=CARTESIAN_POINT ( 'NONE',  ( -0.004863692847738298151, -0.4900785244342681368, -2.159743284330918112 ) ) ;
#43045=CARTESIAN_POINT ( 'NONE',  ( 4.211346380768822506, -1.629847038978438079, -1.091715234301626314 ) ) ;
#43053=CARTESIAN_POINT ( 'NONE',  ( 3.990573222356631256, -1.218298518170106925, 1.735533685479621502 ) ) ;
#43055=CARTESIAN_POINT ( 'NONE',  ( 4.909125497034264818, 1.879091090907711425, 1.068517025386829467 ) ) ;
#43056=CARTESIAN_POINT ( 'NONE',  ( 4.476008884455379366, -1.787108923542475525, -0.4427587100873929815 ) ) ;
#43059=CARTESIAN_POINT ( 'NONE',  ( 6.492160993672303704, -0.4719841783793111145, -1.675048763955745645 ) ) ;
#43060=CARTESIAN_POINT ( 'NONE',  ( 6.727182134110210043, 6.040083938853186396, 2.305853406558423302 ) ) ;
#43063=CARTESIAN_POINT ( 'NONE',  ( 3.749029689823797806, -1.768526636652943296, 1.242828150824742961 ) ) ;
#43065=CARTESIAN_POINT ( 'NONE',  ( 5.466172646012215530, 1.646588110366095314, 1.163089216160061001 ) ) ;
#43067=CARTESIAN_POINT ( 'NONE',  ( 3.889662759143839299, 1.564074849111227516, 1.492423382767386730 ) ) ;
#43068=CARTESIAN_POINT ( 'NONE',  ( 3.286357016390834218, -1.941589536447934972, -0.3404988550089679267 ) ) ;
#43071=CARTESIAN_POINT ( 'NONE',  ( 1.185104535163916228, -2.251984199834490052, -0.5028348148315447963 ) ) ;
#43072=CARTESIAN_POINT ( 'NONE',  ( 2.354824746187761164, -1.594966302183076667, 1.304983254080711808 ) ) ;
#43073=CARTESIAN_POINT ( 'NONE',  ( 5.601106521291020712, -0.4677194688633263264, 1.884795189151499795 ) ) ;
#43079=CARTESIAN_POINT ( 'NONE',  ( 6.610000000000006537, 0.002781820520842553934, 2.000159646111852929 ) ) ;
#43083=CARTESIAN_POINT ( 'NONE',  ( 2.485638465518677176, 2.017858404210779888, -0.8937526715337427152 ) ) ;
#43085=CARTESIAN_POINT ( 'NONE',  ( 6.157081138237819218, 1.605775322519078729, -1.126676614267435150 ) ) ;
#43088=CARTESIAN_POINT ( 'NONE',  ( 0.1749903794560384862, 2.035240947854660920, -2.372290655319588382 ) ) ;
#43090=CARTESIAN_POINT ( 'NONE',  ( 5.912015133600425187, 1.233162958052456348, -1.367321061651972869 ) ) ;
#43096=CARTESIAN_POINT ( 'NONE',  ( 6.293239850429793947, -0.1054838202379469042, -2.118119863012501991 ) ) ;
#43099=CARTESIAN_POINT ( 'NONE',  ( 0.4267267499857710367, 1.971919523859454237, 0.5989439635904010295 ) ) ;
#43101=CARTESIAN_POINT ( 'NONE',  ( 1.627181624537884286, 0.1412763417478210271, -1.855766238205541097 ) ) ;
#43102=CARTESIAN_POINT ( 'NONE',  ( 4.335397732480402055, 0.7831895168094182846, -1.666506522714307437 ) ) ;
#43107=EDGE_LOOP ( 'NONE', ( #17433, #3929, #181485, #124735 ) ) ;
#43108=CARTESIAN_POINT ( 'NONE',  ( 4.881566871873391555, 2.059980941486462047, -0.7921658822237286346 ) ) ;
#43109=CARTESIAN_POINT ( 'NONE',  ( 6.239586896912570069, -1.632293121298231675, -1.566800261409779349 ) ) ;
#43111=CARTESIAN_POINT ( 'NONE',  ( 0.3692113334803036606, -1.616751421056546789, -1.021125667832627260 ) ) ;
#43112=CARTESIAN_POINT ( 'NONE',  ( 6.245329893291753365, 0.3200292219377436354, -1.888624904781693870 ) ) ;
#43115=CARTESIAN_POINT ( 'NONE',  ( 5.461546741811521777, -1.510119879425949385, -1.173092037529008369 ) ) ;
#43117=CARTESIAN_POINT ( 'NONE',  ( 0.5494049127674709432, 0.5909524230637287490, -1.774924738581270089 ) ) ;
#43118=CARTESIAN_POINT ( 'NONE',  ( 2.061732777098632230, 1.244387006429502396, 1.586668050434843158 ) ) ;
#43120=CARTESIAN_POINT ( 'NONE',  ( 4.371769818753069359, 2.042916674203521854, -0.5113404140953855537 ) ) ;
#43126=CARTESIAN_POINT ( 'NONE',  ( 2.760026041568770072, 0.7230886973167930387, -1.886116010022680589 ) ) ;
#43129=CARTESIAN_POINT ( 'NONE',  ( 4.007220386668823409, 1.851715269821294640, 1.114988852100415651 ) ) ;
#43137=CARTESIAN_POINT ( 'NONE',  ( 1.803425971091272340, -1.834736872252432649, 1.160642024321426380 ) ) ;
#43141=CARTESIAN_POINT ( 'NONE',  ( 0.6613494997313728030, 0.9071737413179328247, 1.602200521169500957 ) ) ;
#43143=CARTESIAN_POINT ( 'NONE',  ( 1.611130907606239004, -0.2639259086049255965, 2.175532687872412829 ) ) ;
#43144=CARTESIAN_POINT ( 'NONE',  ( 6.883263157960390011, 6.036220326785228352, 2.548703601196927515 ) ) ;
#43145=CARTESIAN_POINT ( 'NONE',  ( 3.415140116862291908, 2.044469143995849780, 0.9693780919050251077 ) ) ;
#43151=CARTESIAN_POINT ( 'NONE',  ( 4.217836599137672060, -0.9083132443464863037, -1.518676986326646938 ) ) ;
#43153=CARTESIAN_POINT ( 'NONE',  ( 0.6222711621935803628, -1.126682295963852276, -1.779026129514348353 ) ) ;
#43158=CARTESIAN_POINT ( 'NONE',  ( 6.187125092307005580, 1.678016663812756937, 1.117817459622950649 ) ) ;
#43162=CARTESIAN_POINT ( 'NONE',  ( 3.696050037196423332, -1.868490534004090931, -0.09263902202472776293 ) ) ;
#43163=CARTESIAN_POINT ( 'NONE',  ( 4.539934223682924319, 1.348354173984022575, 1.571082123823979826 ) ) ;
#43172=CARTESIAN_POINT ( 'NONE',  ( 3.807043925254738781, -1.605251362286563177, 1.127602784832412386 ) ) ;
#43173=CARTESIAN_POINT ( 'NONE',  ( 1.722029606037442040, -1.727736752315935265, -1.038835718801443653 ) ) ;
#43175=CARTESIAN_POINT ( 'NONE',  ( 1.088877184111051832, 1.652420591378000791, -0.8765777015899289815 ) ) ;
#43177=CARTESIAN_POINT ( 'NONE',  ( 3.375247105954663596, -1.777387065663883714, -0.9453995415899820731 ) ) ;
#43179=CARTESIAN_POINT ( 'NONE',  ( 3.638375168990032549, 0.7640726493506818651, 1.974712724135726516 ) ) ;
#43180=CARTESIAN_POINT ( 'NONE',  ( 6.825078400183572924, 7.629137130509068498, 2.744348168701661095 ) ) ;
#43181=CARTESIAN_POINT ( 'NONE',  ( 5.318829906782316819, -1.502041817331278173, 1.425132596443792643 ) ) ;
#43183=CARTESIAN_POINT ( 'NONE',  ( 0.06416430596320726876, -1.362578676618180884, 1.585857439420575776 ) ) ;
#43185=CARTESIAN_POINT ( 'NONE',  ( 5.473610661177239933, 1.758888005172161373, -0.4887267171112125164 ) ) ;
#43192=CARTESIAN_POINT ( 'NONE',  ( 6.322915745023367506, 1.413667134151237459, -1.287952294376143447 ) ) ;
#43199=VERTEX_POINT ( 'NONE', #169066 ) ;
#43209=CARTESIAN_POINT ( 'NONE',  ( 2.869919493663297683, -1.948696178941822899, 0.2840860843679354764 ) ) ;
#43210=CARTESIAN_POINT ( 'NONE',  ( 3.075796161730546707, -0.8146103074460913085, 1.844718345957757188 ) ) ;
#43212=CARTESIAN_POINT ( 'NONE',  ( 6.727182134110195832, 3.687949058358138466, 2.603069318070629912 ) ) ;
#43213=CARTESIAN_POINT ( 'NONE',  ( 3.240350661220792183, 0.5327334615983710941, 2.125583950146384904 ) ) ;
#43214=CARTESIAN_POINT ( 'NONE',  ( 1.852440960305309137, 0.6018503411110776025, 1.830038407220703656 ) ) ;
#43217=CARTESIAN_POINT ( 'NONE',  ( 0.2331563151865486683, 0.005903526429595904942, -1.945944850731482934 ) ) ;
#43224=CARTESIAN_POINT ( 'NONE',  ( 6.392148736875968851, -0.4980823202534767624, -1.772533436741857260 ) ) ;
#43225=CARTESIAN_POINT ( 'NONE',  ( 3.352200558804620645, 0.9032658637736007412, -1.799124413793075528 ) ) ;
#43226=CARTESIAN_POINT ( 'NONE',  ( 4.604990120689349098, 0.9883660700816098155, -2.075160223314168828 ) ) ;
#43227=CARTESIAN_POINT ( 'NONE',  ( -0.1290005225502675879, -0.006633637972621592160, -2.173875058097324064 ) ) ;
#43228=CARTESIAN_POINT ( 'NONE',  ( 2.904952611580268851, -1.549997479519327648, 1.029535618745812675 ) ) ;
#43231=CARTESIAN_POINT ( 'NONE',  ( 6.328373294368253354, -0.9077179077918960948, -1.683272687665722467 ) ) ;
#43234=CARTESIAN_POINT ( 'NONE',  ( 5.478101502371197640, -2.040020603162643997, -0.4570242091310200427 ) ) ;
#43238=CARTESIAN_POINT ( 'NONE',  ( 5.707552393076498198, -0.4128270653469527374, 1.674615006835003639 ) ) ;
#43240=CARTESIAN_POINT ( 'NONE',  ( 1.230678901735713593, 1.732143722507371475, 0.08558704247295551015 ) ) ;
#43243=CARTESIAN_POINT ( 'NONE',  ( 6.069212964912024333, 1.910890531626436184, 1.030632506159581352 ) ) ;
#43244=CARTESIAN_POINT ( 'NONE',  ( 4.986841741376339066, -0.2268417095559888130, -1.811474396668552700 ) ) ;
#43245=CARTESIAN_POINT ( 'NONE',  ( 2.078885752709497492, 1.828579749420869094, 0.7109141669488158177 ) ) ;
#43249=CARTESIAN_POINT ( 'NONE',  ( 2.016421337698256711, -2.119947128278206971, 0.05498460973795551987 ) ) ;
#43254=CARTESIAN_POINT ( 'NONE',  ( 0.9364849611055334755, -1.153160888946737961, 1.719151461320179042 ) ) ;
#43258=CARTESIAN_POINT ( 'NONE',  ( 3.246955274364712540, 2.167573551356954731, 0.4849624922091085866 ) ) ;
#43260=CARTESIAN_POINT ( 'NONE',  ( 1.003029240585759263, -2.241230121681879073, 0.5102270476868026039 ) ) ;
#43262=CARTESIAN_POINT ( 'NONE',  ( 6.350444629809289587, -2.052082384739264409, -0.2080662788188895607 ) ) ;
#43266=CARTESIAN_POINT ( 'NONE',  ( 5.970224376651540155, -1.750504005202535796, -0.5711807346103907612 ) ) ;
#43268=CARTESIAN_POINT ( 'NONE',  ( -0.1102773484824119132, -0.006951161900758253548, -2.203378182130751206 ) ) ;
#43269=CARTESIAN_POINT ( 'NONE',  ( 2.748708976905740897, -1.435238111852419562, 0.9561691852014215787 ) ) ;
#43270=CARTESIAN_POINT ( 'NONE',  ( 0.6379081216283180034, 2.014007883293071899, -0.1037844182863178755 ) ) ;
#43271=CARTESIAN_POINT ( 'NONE',  ( 2.954051123917677213, -2.124883583899921824, -0.8772644825643919342 ) ) ;
#43272=CARTESIAN_POINT ( 'NONE',  ( 1.880510708721146118, -1.211181421480477693, 1.910737325309288304 ) ) ;
#43273=CARTESIAN_POINT ( 'NONE',  ( 4.951841757635310870, 0.6616352077237923623, -1.999514825752574332 ) ) ;
#43275=CARTESIAN_POINT ( 'NONE',  ( 3.795971232924668648, -1.767634583600716569, -0.08911788016389800282 ) ) ;
#43277=CARTESIAN_POINT ( 'NONE',  ( 6.216396969532355321, 2.137338928125806614, 0.8291867496624371059 ) ) ;
#43278=CARTESIAN_POINT ( 'NONE',  ( 4.857273802806507668, 1.820629801081237620, -0.2732171615176108848 ) ) ;
#43282=CARTESIAN_POINT ( 'NONE',  ( 4.752002516643937469, 0.8370584164609263800, 2.025481692006773748 ) ) ;
#43286=CARTESIAN_POINT ( 'NONE',  ( 4.439934286204096914, 1.349936692791346093, 1.569845735447549906 ) ) ;
#43287=CARTESIAN_POINT ( 'NONE',  ( 0.04025042243083893495, 0.7762349914572730381, 1.861342399428978389 ) ) ;
#43289=CARTESIAN_POINT ( 'NONE',  ( 3.316937275718701894, 1.741877725598478976, 0.8232385001258867296 ) ) ;
#43293=CARTESIAN_POINT ( 'NONE',  ( 0.5982529507728174822, 1.497540282193830841, 1.640895070279895895 ) ) ;
#43301=CARTESIAN_POINT ( 'NONE',  ( 1.451531895509536874, 1.483362660712841841, 1.284035263222626844 ) ) ;
#43304=CARTESIAN_POINT ( 'NONE',  ( 5.582460749670235423, 1.169929261559121247, -1.574690175210855747 ) ) ;
#43308=CARTESIAN_POINT ( 'NONE',  ( 6.368072262247213899, 1.106822706796772193, 1.856716078747308263 ) ) ;
#43312=CARTESIAN_POINT ( 'NONE',  ( 0.8603690976232807319, -1.359099942111790416, 1.285485254608226269 ) ) ;
#43313=CARTESIAN_POINT ( 'NONE',  ( 6.432912826982137844, 0.8947389043411910770, 1.484938929457087164 ) ) ;
#43316=CARTESIAN_POINT ( 'NONE',  ( 2.999763140970078901, -2.188934734890151113, 0.1099877568606702771 ) ) ;
#43317=CARTESIAN_POINT ( 'NONE',  ( 4.893776379751743733, 1.706213512276737232, 1.553814486356275060 ) ) ;
#43318=CARTESIAN_POINT ( 'NONE',  ( 6.239539339872155033, -1.489444859125512277, -1.424447411405028507 ) ) ;
#43319=CARTESIAN_POINT ( 'NONE',  ( 2.484236259141327618, -0.3323325037456366093, -1.913154051555246316 ) ) ;
#43322=CARTESIAN_POINT ( 'NONE',  ( 5.554972086574996304, 0.4156608669513594534, 2.079290889414136423 ) ) ;
#43324=CARTESIAN_POINT ( 'NONE',  ( 3.481092415823695774, -2.014232707597499505, -0.09613569647320965861 ) ) ;
#43328=CARTESIAN_POINT ( 'NONE',  ( 6.933263157960367629, 7.629137130509066722, 2.653810918356712900 ) ) ;
#43334=CARTESIAN_POINT ( 'NONE',  ( 5.664934882792908688, -1.862169278537370465, -0.8832596265169431193 ) ) ;
#43338=CARTESIAN_POINT ( 'NONE',  ( 4.319013676512412303, 1.559734590277090716, -1.283057401373039141 ) ) ;
#43343=CARTESIAN_POINT ( 'NONE',  ( 4.100502863055309533, -0.6448639507273239424, -1.957478828838697504 ) ) ;
#43344=CARTESIAN_POINT ( 'NONE',  ( 3.182267690267494231, 1.591318367894577701, 1.238320962759748234 ) ) ;
#43350=CARTESIAN_POINT ( 'NONE',  ( 2.671249783466634220, -0.7690017779844946499, -1.863883771055181660 ) ) ;
#43351=CARTESIAN_POINT ( 'NONE',  ( 2.027068592762204080, -1.202062398780713748, -1.394650109237540070 ) ) ;
#43352=CARTESIAN_POINT ( 'NONE',  ( 1.014821436393667398, -1.042085040243752481, -2.059081925104982336 ) ) ;
#43354=CARTESIAN_POINT ( 'NONE',  ( 3.251412196806032995, -1.765091617811213931, -1.247493029685270649 ) ) ;
#43356=CARTESIAN_POINT ( 'NONE',  ( 3.778943494763619793, -2.265100756353163103, 0.3889815702934427688 ) ) ;
#43359=CIRCLE ( 'NONE', #143731, 0.04999999999999969746 ) ;
#43360=CARTESIAN_POINT ( 'NONE',  ( 0.8482696660519238874, 0.5391449902514727777, 1.791282564952957124 ) ) ;
#43361=CARTESIAN_POINT ( 'NONE',  ( 5.875845355493965805, 1.173799634058709129, 1.583810875030462695 ) ) ;
#43365=CARTESIAN_POINT ( 'NONE',  ( 0.6630615684519860498, -1.595754342771567025, 1.524677653706180802 ) ) ;
#43370=CARTESIAN_POINT ( 'NONE',  ( 5.559438140644474835, 0.3852295531507047843, -1.933300702130675397 ) ) ;
#43371=CARTESIAN_POINT ( 'NONE',  ( 4.055530604549876017, -1.917597210323931378, -1.283581016687604270 ) ) ;
#43372=CARTESIAN_POINT ( 'NONE',  ( 6.197681965292040296, -1.348592564218813905, -1.282738352563756123 ) ) ;
#43373=CARTESIAN_POINT ( 'NONE',  ( 2.905193444429104321, -1.717358790072313957, 1.142030567362181559 ) ) ;
#43380=CARTESIAN_POINT ( 'NONE',  ( 5.459503713743925069, 1.771904602436706222, 1.254488129281390751 ) ) ;
#43382=CARTESIAN_POINT ( 'NONE',  ( 3.737712173649463399, 1.832726675769575486, 0.1767833568970395008 ) ) ;
#43384=CARTESIAN_POINT ( 'NONE',  ( 6.620655732516631531, 2.063554893983750027, 2.233578047529918287 ) ) ;
#43385=CARTESIAN_POINT ( 'NONE',  ( 5.917560222199001352, -1.216239291071326001, -1.822900893127032962 ) ) ;
#43387=CARTESIAN_POINT ( 'NONE',  ( 6.819229412991756334, -0.1648141603832406210, 2.226593352680195537 ) ) ;
#43393=CARTESIAN_POINT ( 'NONE',  ( 0.5316681593682397455, 0.9152217321290991858, -1.514687162473850490 ) ) ;
#43394=CARTESIAN_POINT ( 'NONE',  ( 5.426436493548534301, -0.9073095142285032555, -1.797119830347380542 ) ) ;
#43396=CARTESIAN_POINT ( 'NONE',  ( 3.751088088702017487, -1.722778774704723181, 1.210957861328536112 ) ) ;
#43397=CARTESIAN_POINT ( 'NONE',  ( 3.181152667880298157, 1.511915621606011007, 1.176196041047285812 ) ) ;
#43399=CARTESIAN_POINT ( 'NONE',  ( 4.404722228293363351, 0.5232710054461316984, 1.898709409516568192 ) ) ;
#43400=CARTESIAN_POINT ( 'NONE',  ( 6.011974661143067777, -0.6766988549865710079, 1.903214300750865506 ) ) ;
#43401=CARTESIAN_POINT ( 'NONE',  ( 1.586564105604048480, -0.2713065988851799393, -1.850747533123621391 ) ) ;
#43402=CARTESIAN_POINT ( 'NONE',  ( 4.758271111750849158, 0.6642134669661412527, 1.592074403417756301 ) ) ;
#43403=CARTESIAN_POINT ( 'NONE',  ( 1.459083999156213451, -1.613880964290700160, 1.025699646091532857 ) ) ;
#43405=CARTESIAN_POINT ( 'NONE',  ( 2.719571217284349363, -0.2154062111461417517, 2.196339928330424129 ) ) ;
#43408=CARTESIAN_POINT ( 'NONE',  ( 6.461383593301071926, 1.630371061775518271, 1.090930979547571456 ) ) ;
#43416=CARTESIAN_POINT ( 'NONE',  ( 1.750525128138082254, -2.060206210462053988, -0.2049951091474821463 ) ) ;
#43422=CARTESIAN_POINT ( 'NONE',  ( 0.04752895628580295490, -1.845665702319599921, 0.8205699430347112022 ) ) ;
#43427=CARTESIAN_POINT ( 'NONE',  ( 5.694685421800770087, -1.276849089899323886, -1.560260200769040706 ) ) ;
#43428=CARTESIAN_POINT ( 'NONE',  ( 4.856599191889834799, -1.806003080954875495, -0.6394761690226327122 ) ) ;
#43430=CARTESIAN_POINT ( 'NONE',  ( 3.105210138592546798, -0.4252477525170209605, 2.149737936336936883 ) ) ;
#43433=CARTESIAN_POINT ( 'NONE',  ( 5.730732165690560542, 1.348809278943388534, -1.494750323444839601 ) ) ;
#43434=CARTESIAN_POINT ( 'NONE',  ( 1.089939655121434203, 1.141396045679959004, 1.534244836814010693 ) ) ;
#43437=CARTESIAN_POINT ( 'NONE',  ( -0.1058464554703278104, -0.8645191204341062807, -1.819937883007181512 ) ) ;
#43439=CARTESIAN_POINT ( 'NONE',  ( 3.614856758894122724, -0.1514882961727741506, 2.085299387778175806 ) ) ;
#43441=CARTESIAN_POINT ( 'NONE',  ( 1.676317214473854067, -1.636236659294947104, -0.5456935059391133658 ) ) ;
#43453=CARTESIAN_POINT ( 'NONE',  ( 3.105918186854994989, -0.7317858000257486673, 1.657260211903899938 ) ) ;
#43459=CARTESIAN_POINT ( 'NONE',  ( 3.334412561109405537, 1.147067551318830203, -1.402027596893473449 ) ) ;
#43460=CARTESIAN_POINT ( 'NONE',  ( 6.539320575229245591, 2.459069921018588900, 2.280790101157427419 ) ) ;
#43464=CARTESIAN_POINT ( 'NONE',  ( 4.000341067899515046, 1.851953036565538335, 0.1839423254178795542 ) ) ;
#43466=CARTESIAN_POINT ( 'NONE',  ( 1.686979003181095615, 1.593666142434764454, 1.062572995559516009 ) ) ;
#43467=CARTESIAN_POINT ( 'NONE',  ( 1.307329191252764922, -0.4475898743878243824, 1.769731943805815222 ) ) ;
#43476=CARTESIAN_POINT ( 'NONE',  ( 5.700047960291365179, 0.8015925475840814940, -1.799137058317602067 ) ) ;
#43479=AXIS2_PLACEMENT_3D ( 'NONE', #168425, #201951, #180422 ) ;
#43480=CARTESIAN_POINT ( 'NONE',  ( 6.703104427915338448, -0.4847493572297522091, 2.145077170986497528 ) ) ;
#43482=CARTESIAN_POINT ( 'NONE',  ( 5.596683124612600757, -0.4680951147424931569, -1.868546797846575513 ) ) ;
#43484=CARTESIAN_POINT ( 'NONE',  ( 1.307329191252764922, -0.4475898743878243824, 1.769731943805815222 ) ) ;
#43485=CARTESIAN_POINT ( 'NONE',  ( 2.596532132193625664, -2.201043451360765957, -0.1612727490639675743 ) ) ;
#43487=CARTESIAN_POINT ( 'NONE',  ( 0.4746845637013075159, -1.383529810647101455, 1.320479256824915071 ) ) ;
#43488=CARTESIAN_POINT ( 'NONE',  ( 0.2913706227113096459, -1.802261421121041707, 0.7947621968238273160 ) ) ;
#43489=CARTESIAN_POINT ( 'NONE',  ( 3.175267148988625721, 1.234016112977231794, 1.499580727898646604 ) ) ;
#43491=CARTESIAN_POINT ( 'NONE',  ( 0.5442957877539145173, 1.882187304385819493, -0.7230256762977352869 ) ) ;
#43493=CARTESIAN_POINT ( 'NONE',  ( 6.965680890820083349, -0.4048625726877760900, 1.822745621051139020 ) ) ;
#43499=CARTESIAN_POINT ( 'NONE',  ( 2.279091853667324141, 2.002311374866962979, -0.8913168663882904408 ) ) ;
#43503=CARTESIAN_POINT ( 'NONE',  ( 3.123480263227970344, -1.759325740769552393, 0.4874977319994436287 ) ) ;
#43507=CARTESIAN_POINT ( 'NONE',  ( -0.02968770228137588424, 4.095675376368371090, -2.381331788581673159 ) ) ;
#43509=CARTESIAN_POINT ( 'NONE',  ( 0.4692025345035084061, 0.1902923850431673669, -1.917074784726199965 ) ) ;
#43510=CARTESIAN_POINT ( 'NONE',  ( 5.207842308544940124, 0.6190457291245822224, -1.861560318597937913 ) ) ;
#43514=CARTESIAN_POINT ( 'NONE',  ( 5.249643141573060667, 2.189086832579402842, -0.1069518675670885766 ) ) ;
#43516=CARTESIAN_POINT ( 'NONE',  ( 4.188381925097388603, 1.111774711627441681, -1.746232563387891679 ) ) ;
#43520=CARTESIAN_POINT ( 'NONE',  ( 4.412867445986612402, -1.413514171388057239, -1.812631114537610166 ) ) ;
#43526=CARTESIAN_POINT ( 'NONE',  ( 4.980387307702104138, -0.2395764092862572303, -1.927055426435628327 ) ) ;
#43531=CARTESIAN_POINT ( 'NONE',  ( 5.291234991620994421, -0.05314252713351996088, -1.911838368980276925 ) ) ;
#43532=CARTESIAN_POINT ( 'NONE',  ( 6.000961845343044665, 1.407127125985812466, -0.9971243314716814465 ) ) ;
#43533=CARTESIAN_POINT ( 'NONE',  ( 4.505092375653735992, -0.09411930587044713137, 2.014432893821124004 ) ) ;
#43537=CARTESIAN_POINT ( 'NONE',  ( 1.377023180242874068, 1.931088066391934976, -0.8015266744223081830 ) ) ;
#43538=CARTESIAN_POINT ( 'NONE',  ( 0.4789242711138582687, 1.653723610832663393, -0.6310274585415026616 ) ) ;
#43539=CARTESIAN_POINT ( 'NONE',  ( 5.783827325522512552, 1.646840809264274119, -1.163266671679111353 ) ) ;
#43541=CARTESIAN_POINT ( 'NONE',  ( 2.660454013544113927, -1.579728858233371946, 1.661220326946882375 ) ) ;
#43542=CARTESIAN_POINT ( 'NONE',  ( 2.607021377293942344, -1.721407032317923802, 0.2550150930856145970 ) ) ;
#43543=CARTESIAN_POINT ( 'NONE',  ( 3.094099843433151253, 1.348383549611749332, 1.636666742212993686 ) ) ;
#43545=CARTESIAN_POINT ( 'NONE',  ( 0.6317059331818836165, 0.1778517408326604765, -1.724704385026996079 ) ) ;
#43547=CARTESIAN_POINT ( 'NONE',  ( 2.207255083745041979, -1.492367883816644314, -1.111680554738720073 ) ) ;
#43548=( BOUNDED_CURVE ( )  B_SPLINE_CURVE ( 3, ( #3067, #100597, #50781, #147238 ),
 .UNSPECIFIED., .F., .T. ) 
 B_SPLINE_CURVE_WITH_KNOTS ( ( 4, 4 ),
 ( 0.000000000000000000, 0.4999999999999939493 ),
 .UNSPECIFIED. ) 
 CURVE ( )  GEOMETRIC_REPRESENTATION_ITEM ( )  RATIONAL_B_SPLINE_CURVE ( ( 1.000000000000000000, 0.3333333333333414195, 0.3333333333333333703, 0.9999999999999918954 ) ) 
 REPRESENTATION_ITEM ( '' )  );
#43549=CARTESIAN_POINT ( 'NONE',  ( 2.822911419172136949, -1.498817844263359067, 1.571052884911597003 ) ) ;
#43550=CARTESIAN_POINT ( 'NONE',  ( 3.046111529846948329, 0.9110102549910354952, 1.799122713138465279 ) ) ;
#43551=CARTESIAN_POINT ( 'NONE',  ( 3.593750000000001776, -1.895863743164161841, -0.7852924748297959168 ) ) ;
#43553=CARTESIAN_POINT ( 'NONE',  ( 0.3934162593667543950, 1.425226140442600098, 1.296210752655905463 ) ) ;
#43555=CARTESIAN_POINT ( 'NONE',  ( 3.902737194376978636, -2.197594379623767580, -0.3235144178719475128 ) ) ;
#43557=CARTESIAN_POINT ( 'NONE',  ( -0.2110808730067326444, 2.048707873362776599, -2.213945011526836204 ) ) ;
#43561=CARTESIAN_POINT ( 'NONE',  ( 6.029551324705815674, -0.2728526602329122142, 2.204496564233568989 ) ) ;
#43562=CARTESIAN_POINT ( 'NONE',  ( 4.228923158279327410, -1.829750178516520442, -0.7082015076659911035 ) ) ;
#43566=CARTESIAN_POINT ( 'NONE',  ( 5.677129043647218154, -0.04737763303009440846, -2.262073803551585272 ) ) ;
#43568=CARTESIAN_POINT ( 'NONE',  ( 2.488800817111187946, 2.000174138640842258, 0.5034198422354563274 ) ) ;
#43572=CARTESIAN_POINT ( 'NONE',  ( 3.672993792711932048, 0.04889617625786558258, -1.870083761627352015 ) ) ;
#43573=CARTESIAN_POINT ( 'NONE',  ( 2.373305363469370377, -0.2979590584733567971, -1.708161578628903055 ) ) ;
#43575=CARTESIAN_POINT ( 'NONE',  ( 6.339412547452306868, 0.8406370108028878851, -2.024118718474729128 ) ) ;
#43576=CARTESIAN_POINT ( 'NONE',  ( 1.272829778695073299, -1.399090282553701270, 1.706552004499435560 ) ) ;
#43577=CARTESIAN_POINT ( 'NONE',  ( 6.122988667457554435, -1.827782563270570648, 0.6563872640158885385 ) ) ;
#43582=CARTESIAN_POINT ( 'NONE',  ( 0.07093568767341934533, -0.9480374005119349690, 1.779628194860154222 ) ) ;
#43583=CARTESIAN_POINT ( 'NONE',  ( -0.01710467543277957581, -1.380256469788909035, 1.610041658517608054 ) ) ;
#43588=CARTESIAN_POINT ( 'NONE',  ( 3.598116246361187542, -1.823677485248562435, -0.08826725125678223927 ) ) ;
#43589=CARTESIAN_POINT ( 'NONE',  ( 2.503190323335769740, 1.772782541628318720, -1.313999973512294472 ) ) ;
#43594=CARTESIAN_POINT ( 'NONE',  ( 1.037374617392500031, -0.04523278242563041895, 2.019440925237799167 ) ) ;
#43595=CARTESIAN_POINT ( 'NONE',  ( 0.8914570141239013257, -0.05588796005432519753, -2.119924415460701983 ) ) ;
#43597=CARTESIAN_POINT ( 'NONE',  ( 3.151044791815108770, 1.598572158793242659, -0.9524303787414812872 ) ) ;
#43599=CARTESIAN_POINT ( 'NONE',  ( 6.293592298849588929, 1.492257802130890543, -1.356297202127904722 ) ) ;
#43603=CARTESIAN_POINT ( 'NONE',  ( 3.826616632296374831, 1.734130841282412128, 0.5711148077138239465 ) ) ;
#43608=CARTESIAN_POINT ( 'NONE',  ( 6.116564501996816894, 0.5879282371138266905, -1.928457050679150298 ) ) ;
#43609=CARTESIAN_POINT ( 'NONE',  ( 6.087831982560696353, -1.832735460234231617, -0.1757473516527594259 ) ) ;
#43611=CARTESIAN_POINT ( 'NONE',  ( 4.459805605305016130, 0.5082999457236726526, -2.250878628046268037 ) ) ;
#43613=CARTESIAN_POINT ( 'NONE',  ( 6.889893180375397996, -0.9309023296741396614, 1.948985471107896439 ) ) ;
#43615=CARTESIAN_POINT ( 'NONE',  ( 2.384236373620087335, -0.3343274798127248149, -1.912924682550071864 ) ) ;
#43616=CARTESIAN_POINT ( 'NONE',  ( 6.204520426337317929, -1.658329656736241553, -1.591615412813138564 ) ) ;
#43621=CARTESIAN_POINT ( 'NONE',  ( 4.100366707588389836, -0.5864361863821172527, -1.776433678864146382 ) ) ;
#43623=CARTESIAN_POINT ( 'NONE',  ( 2.619282413590624525, 1.617716081779559278, 1.019604094833974628 ) ) ;
#43626=CARTESIAN_POINT ( 'NONE',  ( 4.196070124731249074, -0.8457972711899945928, 2.038567251995755836 ) ) ;
#43628=CARTESIAN_POINT ( 'NONE',  ( 6.883263157960382905, 3.691751545928231959, 2.560365603790202282 ) ) ;
#43629=CARTESIAN_POINT ( 'NONE',  ( -0.2110808730066962846, 2.887681559854797797, -2.286017728802595350 ) ) ;
#43632=CARTESIAN_POINT ( 'NONE',  ( 2.038291622189229546, 1.949329857042367387, 0.2932346777646984148 ) ) ;
#43633=CARTESIAN_POINT ( 'NONE',  ( 2.784532256742262568, -1.187036312555936890, 1.978742884264461654 ) ) ;
#43634=CARTESIAN_POINT ( 'NONE',  ( 2.172246964874047670, -0.9220853831424129510, -1.731647142839589648 ) ) ;
#43636=CARTESIAN_POINT ( 'NONE',  ( 6.684441936803141360, 1.192331456891123187, -1.682829884528406428 ) ) ;
#43638=CARTESIAN_POINT ( 'NONE',  ( 3.960172920142067898, -1.157100329752266621, 1.651342637023434090 ) ) ;
#43641=CARTESIAN_POINT ( 'NONE',  ( 4.311732611912100666, -1.244383703160652610, -1.586670621409623116 ) ) ;
#43646=CARTESIAN_POINT ( 'NONE',  ( 2.342849523213458962, -2.128499089237919417, -0.4270345827348878132 ) ) ;
#43649=CARTESIAN_POINT ( 'NONE',  ( 2.917106759524803472, -0.1871779394605546654, 1.861177454839262113 ) ) ;
#43650=CARTESIAN_POINT ( 'NONE',  ( 6.151685507011436904, 0.6340151041426717038, -2.066508600247290328 ) ) ;
#43651=CARTESIAN_POINT ( 'NONE',  ( -0.02244404828157658613, 0.6916080914694566761, -2.270927585766496559 ) ) ;
#43652=CARTESIAN_POINT ( 'NONE',  ( 6.827182134110246103, 6.039869998172250121, 2.305852349323509021 ) ) ;
#43655=CARTESIAN_POINT ( 'NONE',  ( 2.895058368816882499, -0.1428820475998151540, -1.907012587803847303 ) ) ;
#43656=CARTESIAN_POINT ( 'NONE',  ( 3.608038473134207891, -0.7167157551234564217, -1.618410677222481553 ) ) ;
#43657=CARTESIAN_POINT ( 'NONE',  ( 2.104032245951466429, -0.8162354410432022256, 1.729450509904674416 ) ) ;
#43660=CARTESIAN_POINT ( 'NONE',  ( 0.1631139290103194861, 1.786460926609586330, -0.6921882798058466291 ) ) ;
#43662=CARTESIAN_POINT ( 'NONE',  ( 0.8716356842100521085, -0.3054578492302991721, 2.047597563663336118 ) ) ;
#43664=CARTESIAN_POINT ( 'NONE',  ( 6.403191318657627029, 1.556466930477506505, 1.037356966126230517 ) ) ;
#43665=CARTESIAN_POINT ( 'NONE',  ( 1.260069262837599791, 0.7379878962356714034, 1.670071910705408946 ) ) ;
#43666=CARTESIAN_POINT ( 'NONE',  ( 5.637410271038987730, -1.996576301129053377, 0.9405272304151901519 ) ) ;
#43669=CARTESIAN_POINT ( 'NONE',  ( 2.998538507119326901, 2.046783137066817027, 0.2552134970664684532 ) ) ;
#43671=CARTESIAN_POINT ( 'NONE',  ( 6.889999999999985469, 0.6064005686075202295, 1.774654002403662778 ) ) ;
#43677=CARTESIAN_POINT ( 'NONE',  ( 5.178213324540339002, -1.104578422852561914, -1.750899486206449751 ) ) ;
#43679=CARTESIAN_POINT ( 'NONE',  ( 3.075615952314793233, 2.053625483174918553, -0.6748976972978243394 ) ) ;
#43681=CARTESIAN_POINT ( 'NONE',  ( 2.596358364526121676, -1.036244631391324722, 1.733413072464027316 ) ) ;
#43688=CARTESIAN_POINT ( 'NONE',  ( 0.9718890779336667451, -0.9023411006064323558, 1.803417998987096427 ) ) ;
#43690=CARTESIAN_POINT ( 'NONE',  ( 5.548420995840112724, -1.728225626343689925, 1.347513067664840358 ) ) ;
#43692=CARTESIAN_POINT ( 'NONE',  ( 4.728717205193702533, 1.314622909153417174, -1.389140896021365368 ) ) ;
#43696=CARTESIAN_POINT ( 'NONE',  ( 3.673453983005552814, 1.462458373076291673, 1.388474078538141754 ) ) ;
#43698=CARTESIAN_POINT ( 'NONE',  ( 5.350533963330765808, 0.5041449683875122156, 1.649457517733200040 ) ) ;
#43702=CARTESIAN_POINT ( 'NONE',  ( 4.762891570102392613, -1.670096840553733752, -0.8426394062573672183 ) ) ;
#43704=CARTESIAN_POINT ( 'NONE',  ( 1.411079811451225074, -1.634442866182721277, 1.270590680402396311 ) ) ;
#43707=CARTESIAN_POINT ( 'NONE',  ( 6.633470331352866900, -0.1302952867699505302, 1.781688180685939926 ) ) ;
#43710=CARTESIAN_POINT ( 'NONE',  ( 0.6678513782990652681, 1.809512280066556400, -0.08962025572057349954 ) ) ;
#43717=CARTESIAN_POINT ( 'NONE',  ( 1.135121963537696566, -0.04462593873827064989, -1.961518378280776354 ) ) ;
#43719=CARTESIAN_POINT ( 'NONE',  ( 5.062082326478217098, -1.060395474731326448, 1.595121111449711693 ) ) ;
#43725=CARTESIAN_POINT ( 'NONE',  ( 1.463986924769441478, 2.129665692569195024, -0.3698555562515608020 ) ) ;
#43729=CARTESIAN_POINT ( 'NONE',  ( 4.946237996787820279, 1.820793779319082706, 0.1331645236858983172 ) ) ;
#43731=( BOUNDED_SURFACE ( )  B_SPLINE_SURFACE ( 3, 3, ( 
 ( #3106, #203444, #204513, #202379, #20441, #85453, #6318, #21488, #86523, #187217, #152588 ),
 ( #136359, #4175, #151538, #36695, #103851, #123393, #70244, #35627, #55098, #186142, #137425 ),
 ( #23646, #101705, #71313, #169899, #73467, #167777, #39923, #106031, #87598, #139568, #5237 ),
 ( #121247, #38846, #205595, #69177, #104929, #170971, #22570, #72392, #135297, #138492, #52951 ),
 ( #122325, #140652, #92954, #75615, #95085, #59357, #58297, #77739, #62550, #108182, #193620 ),
 ( #161133, #190412, #43144, #175265, #124453, #76670, #208791, #125514, #210924, #191476, #61491 ),
 ( #45261, #42068, #159001, #60421, #143860, #12721, #78794, #207734, #111381, #27928, #177384 ) ),
 .UNSPECIFIED., .T., .F., .T. ) 
 B_SPLINE_SURFACE_WITH_KNOTS ( ( 4, 3, 4 ),
 ( 4, 1, 1, 1, 1, 1, 1, 1, 4 ),
 ( 0.000000000000000000, 0.5000000000000000000, 1.000000000000000000 ),
 ( 0.000000000000000000, 0.2255509035172358623, 0.3975895543896152406, 0.5252637114030099807, 0.6177357421269481508, 0.6841390318922365710, 0.7334310489036851566, 0.7741974304450970346, 1.000000000000000000 ),
 .UNSPECIFIED. ) 
 GEOMETRIC_REPRESENTATION_ITEM ( )  RATIONAL_B_SPLINE_SURFACE ( (
 ( 1.000000000000000000, 1.000000000000000000, 1.000000000000000000, 1.000000000000000000, 1.000000000000000444, 0.9999999999999997780, 1.000000000000000000, 1.000000000000000000, 1.000000000000000000, 1.000000000000000000, 1.000000000000000000),
 ( 0.3333333333333333703, 0.3333333333333333703, 0.3333333333333332593, 0.3333333333333334814, 0.3333333333333334814, 0.3333333333333333148, 0.3333333333333333703, 0.3333333333333333703, 0.3333333333333333703, 0.3333333333333334259, 0.3333333333333333703),
 ( 0.3333333333333333703, 0.3333333333333333703, 0.3333333333333332593, 0.3333333333333334814, 0.3333333333333334814, 0.3333333333333333148, 0.3333333333333333703, 0.3333333333333333703, 0.3333333333333333703, 0.3333333333333334259, 0.3333333333333333703),
 ( 1.000000000000000000, 1.000000000000000000, 1.000000000000000000, 1.000000000000000000, 1.000000000000000444, 0.9999999999999997780, 1.000000000000000000, 1.000000000000000000, 1.000000000000000000, 1.000000000000000000, 1.000000000000000000),
 ( 0.3333333333333333703, 0.3333333333333333703, 0.3333333333333332593, 0.3333333333333334814, 0.3333333333333334814, 0.3333333333333333148, 0.3333333333333333703, 0.3333333333333333703, 0.3333333333333333703, 0.3333333333333334259, 0.3333333333333333703),
 ( 0.3333333333333333703, 0.3333333333333333703, 0.3333333333333332593, 0.3333333333333334814, 0.3333333333333334814, 0.3333333333333333148, 0.3333333333333333703, 0.3333333333333333703, 0.3333333333333333703, 0.3333333333333334259, 0.3333333333333333703),
 ( 1.000000000000000000, 1.000000000000000000, 1.000000000000000000, 1.000000000000000000, 1.000000000000000444, 0.9999999999999997780, 1.000000000000000000, 1.000000000000000000, 1.000000000000000000, 1.000000000000000000, 1.000000000000000000) ) ) 
 REPRESENTATION_ITEM ( '' )  SURFACE ( )  );
#43733=CARTESIAN_POINT ( 'NONE',  ( 1.300003668391478406, -1.971530339922975550, -0.004173579811568225127 ) ) ;
#43734=CARTESIAN_POINT ( 'NONE',  ( 3.269685606991072468, 0.4601866041431811327, -1.856093204100267124 ) ) ;
#43738=CARTESIAN_POINT ( 'NONE',  ( 4.281674416708352027, -1.885371899234816739, 0.5696992939150746782 ) ) ;
#43740=CARTESIAN_POINT ( 'NONE',  ( 6.040568865451770186, -1.638250791085652303, 1.042688759833640066 ) ) ;
#43746=CARTESIAN_POINT ( 'NONE',  ( 3.844317892072905973, 1.020479721125296280, -1.617037373464407457 ) ) ;
#43750=CARTESIAN_POINT ( 'NONE',  ( 5.408844923620411471, -0.4912159631041897456, -1.952115566551455572 ) ) ;
#43751=CARTESIAN_POINT ( 'NONE',  ( 6.463509179248937642, 0.3066564278407272748, -1.799597105106438777 ) ) ;
#43752=CARTESIAN_POINT ( 'NONE',  ( 5.770720322323381168, -0.3006437417610394736, -1.993894057904864514 ) ) ;
#43753=CARTESIAN_POINT ( 'NONE',  ( 6.727182134110193168, 4.701113012587437190, 2.373661997258198486 ) ) ;
#43754=CARTESIAN_POINT ( 'NONE',  ( 1.416557266959647787, 0.8372786474034592530, 1.893679232998768391 ) ) ;
#43759=CARTESIAN_POINT ( 'NONE',  ( 6.315307248462690204, -0.2269180964024133385, 1.856785020699961875 ) ) ;
#43763=FACE_OUTER_BOUND ( 'NONE', #138436, .T. ) ;
#43768=CARTESIAN_POINT ( 'NONE',  ( 4.060950141605116137, -0.9941625748171744048, 1.420652921118512602 ) ) ;
#43770=CARTESIAN_POINT ( 'NONE',  ( 2.131770371054972912, 1.982354287819853456, -0.5969549857752221023 ) ) ;
#43771=CARTESIAN_POINT ( 'NONE',  ( 3.726253221435165575, 2.107214626963071602, 0.2054869192316331195 ) ) ;
#43774=CARTESIAN_POINT ( 'NONE',  ( 0.6726246190636753219, 1.362232206854155914, -1.422558973980556418 ) ) ;
#43778=CARTESIAN_POINT ( 'NONE',  ( 0.1406777020166137260, 1.830675540527426648, 0.5531436448603862521 ) ) ;
#43779=CARTESIAN_POINT ( 'NONE',  ( 4.013863964491473979, -1.177108192605724746, -1.966824220290509961 ) ) ;
#43780=CARTESIAN_POINT ( 'NONE',  ( 0.7854531640391904102, 1.224056292049885419, 1.354719642434290439 ) ) ;
#43781=CARTESIAN_POINT ( 'NONE',  ( 2.830216799141628492, -0.9462872844297947061, -1.661813493071498726 ) ) ;
#43787=CARTESIAN_POINT ( 'NONE',  ( 1.529542846128278066, -0.2424046428922912721, 1.998471667700427057 ) ) ;
#43788=CARTESIAN_POINT ( 'NONE',  ( 2.061309051315598051, 1.628117514333087934, 1.094105149622534467 ) ) ;
#43792=CARTESIAN_POINT ( 'NONE',  ( 5.191392108680514816, -0.7531529969884572795, 1.950447244483977993 ) ) ;
#43793=CARTESIAN_POINT ( 'NONE',  ( 3.221328931188462086, -1.705978018192667811, 0.4708956190180821344 ) ) ;
#43795=CARTESIAN_POINT ( 'NONE',  ( 5.999983301813878178, -0.8195729662384824143, -2.140910441102741313 ) ) ;
#43796=CARTESIAN_POINT ( 'NONE',  ( 5.191228607790203675, -0.6215644750859107281, 1.625735776773645780 ) ) ;
#43799=CARTESIAN_POINT ( 'NONE',  ( 6.011065113327825671, 1.732079373560748481, 0.08140909068810914251 ) ) ;
#43800=CARTESIAN_POINT ( 'NONE',  ( 6.145025799957537060, -0.3124719705198654718, -2.148460482323500731 ) ) ;
#43802=CARTESIAN_POINT ( 'NONE',  ( 0.02287343425391458532, 0.3688939426326736104, 2.084831875159770753 ) ) ;
#43803=CARTESIAN_POINT ( 'NONE',  ( 4.750000000000003553, 2.703060497845378561E-13, 2.052068128417943171 ) ) ;
#43805=CARTESIAN_POINT ( 'NONE',  ( 3.680616551068579767, -1.856277683350136432, -0.5147254836462693550 ) ) ;
#43807=CARTESIAN_POINT ( 'NONE',  ( -0.1044638861024569515, -0.1585131741546479955, -2.186235582987208659 ) ) ;
#43812=CARTESIAN_POINT ( 'NONE',  ( 2.508681548337174494, -2.215532678404589007, -0.1606611847707327678 ) ) ;
#43817=CARTESIAN_POINT ( 'NONE',  ( 1.055314813143366726, -1.277040974352643854, 1.560502084637045650 ) ) ;
#43819=CARTESIAN_POINT ( 'NONE',  ( 5.547355216851989290, 1.820699215414087302, -0.9693467284541881224 ) ) ;
#43822=CARTESIAN_POINT ( 'NONE',  ( 0.4558546072216109191, 0.6692488815305540628, 1.638537551351123112 ) ) ;
#43823=CARTESIAN_POINT ( 'NONE',  ( 6.363864384548370445, -0.09514871459133207587, -1.731698918886691363 ) ) ;
#43824=CARTESIAN_POINT ( 'NONE',  ( 5.882304624916216973, -0.2641129477329319242, -1.720170474299307806 ) ) ;
#43826=CARTESIAN_POINT ( 'NONE',  ( 2.630776572171345418, 0.2838290345775448809, 2.274689434353324824 ) ) ;
#43828=CARTESIAN_POINT ( 'NONE',  ( 1.745803608711377075, 0.5764907460206626366, 1.748616612666432868 ) ) ;
#43831=CARTESIAN_POINT ( 'NONE',  ( 2.924607851032960504, 1.718362407962298333, 0.6167639819729958672 ) ) ;
#43832=CARTESIAN_POINT ( 'NONE',  ( 3.270157880292836605, 1.821742160604752137, -0.8647241845514613834 ) ) ;
#43835=CARTESIAN_POINT ( 'NONE',  ( 5.948290813881442318, 2.103388047956732620, 0.1067411848718266276 ) ) ;
#43838=CARTESIAN_POINT ( 'NONE',  ( 2.945825538390862697, 1.462269270728074222, 1.465923284304726737 ) ) ;
#43841=CARTESIAN_POINT ( 'NONE',  ( 4.969442291489525765, -1.791676405564743169, -1.133875526122554378 ) ) ;
#43844=CARTESIAN_POINT ( 'NONE',  ( 1.348133503156129454, 1.924256495421622359, 0.09534579948072999245 ) ) ;
#43852=CARTESIAN_POINT ( 'NONE',  ( 5.748313822965784858, 1.043546352714582071, -1.845953426139717246 ) ) ;
#43853=CARTESIAN_POINT ( 'NONE',  ( 1.975741970143765736, 2.015461639870301358, -0.6107432106882881850 ) ) ;
#43856=CARTESIAN_POINT ( 'NONE',  ( 5.981279135395962676, -0.04703572473597864706, 1.860536724379359574 ) ) ;
#43863=CARTESIAN_POINT ( 'NONE',  ( 2.506241959165692812, 1.961374882610424919, 0.05109738790698423877 ) ) ;
#43864=CARTESIAN_POINT ( 'NONE',  ( 1.112450467520700537, -0.9725818059473789745, -1.930612204972524282 ) ) ;
#43868=CARTESIAN_POINT ( 'NONE',  ( 2.723678392350858957, -1.506833864184083493, -0.8575499777047421723 ) ) ;
#43869=CARTESIAN_POINT ( 'NONE',  ( 2.343362483081043557, 1.739954169810492557, 0.04345107811378270263 ) ) ;
#43872=CARTESIAN_POINT ( 'NONE',  ( 1.845077155533506374, -1.080901620906085325, 1.701686244941137183 ) ) ;
#43876=CARTESIAN_POINT ( 'NONE',  ( 1.252734725572089536, -1.555569235904795011, 1.211063379650168415 ) ) ;
#43878=CARTESIAN_POINT ( 'NONE',  ( 5.308822938259078583, -0.4706598425541131947, -1.853433239416848455 ) ) ;
#43883=CARTESIAN_POINT ( 'NONE',  ( 1.242838512808578377, 1.947023393874779851, 0.5366068325038054754 ) ) ;
#43885=CARTESIAN_POINT ( 'NONE',  ( 6.001056180859140277, 1.891180833080384982, -1.322043635676501072 ) ) ;
#43886=CARTESIAN_POINT ( 'NONE',  ( 5.810985101215744741, -1.547553103248515027, 1.205733875218002238 ) ) ;
#43887=CARTESIAN_POINT ( 'NONE',  ( 3.344534541303633368, -1.931932779036081183, -0.3399374921491463142 ) ) ;
#43889=CARTESIAN_POINT ( 'NONE',  ( 0.5807041986926939625, -0.7231374404764076003, 1.882475062126743204 ) ) ;
#43891=CARTESIAN_POINT ( 'NONE',  ( 0.9368845280443529600, -1.665339089426773000, 1.307453795268032071 ) ) ;
#43894=CARTESIAN_POINT ( 'NONE',  ( 1.763359053103892293, 0.9455654613358072114, 1.579637215005654349 ) ) ;
#43897=CARTESIAN_POINT ( 'NONE',  ( 2.988655875014298857, -1.259908772670719657, 1.705623289672608678 ) ) ;
#43901=CARTESIAN_POINT ( 'NONE',  ( 3.673166697908346379, 0.05419028943656278852, -2.060251915681856616 ) ) ;
#43903=CARTESIAN_POINT ( 'NONE',  ( 0.3097736896383457839, 1.270387085892955792, -1.333027339516623888 ) ) ;
#43908=CARTESIAN_POINT ( 'NONE',  ( 2.337552072221838362, -2.021662389422747452, 1.015643474128526291 ) ) ;
#43910=CARTESIAN_POINT ( 'NONE',  ( 2.003910543607852812, -0.7718314612508870853, 1.639047433122240660 ) ) ;
#43911=CARTESIAN_POINT ( 'NONE',  ( 3.643669983026840420, 1.900603903897592595, -0.2398275428802750520 ) ) ;
#43912=CARTESIAN_POINT ( 'NONE',  ( 4.105968538015460467, 0.7004154448949986289, -1.948405661837959713 ) ) ;
#43915=CARTESIAN_POINT ( 'NONE',  ( 2.553542074257345362, 0.5272840835596946940, -1.899572117879143596 ) ) ;
#43916=CARTESIAN_POINT ( 'NONE',  ( 6.727182134110236689, 0.003007720480393410133, 1.910970182385362870 ) ) ;
#43917=CARTESIAN_POINT ( 'NONE',  ( 2.746779440450992649, -1.556306552617524597, 1.037596984913228937 ) ) ;
#43918=CARTESIAN_POINT ( 'NONE',  ( 2.157223245065964967, -1.782429894076944521, 1.465742965790328700 ) ) ;
#43920=CARTESIAN_POINT ( 'NONE',  ( 2.312761410774709425, -1.440873624601293423, 1.177899742917737358 ) ) ;
#43922=CARTESIAN_POINT ( 'NONE',  ( 6.426245203579573406, 1.057156898221789598, 1.771034054399809987 ) ) ;
#43926=CARTESIAN_POINT ( 'NONE',  ( 0.9089716955857042313, 1.593442362523834754, -1.377222155420864347 ) ) ;
#43928=CARTESIAN_POINT ( 'NONE',  ( 6.415313282229532454, -0.2716245656670859820, 2.144420208805633887 ) ) ;
#43929=CARTESIAN_POINT ( 'NONE',  ( -0.03488881496042146174, -1.619560933857542073, 1.206636643155176714 ) ) ;
#43933=CARTESIAN_POINT ( 'NONE',  ( 6.925078400183555694, 1.300159714275823664, 1.872400972051186496 ) ) ;
#43936=CARTESIAN_POINT ( 'NONE',  ( 4.364470425680367249, -1.957169923074707274, -0.4852690807995581057 ) ) ;
#43939=CARTESIAN_POINT ( 'NONE',  ( 5.577088068215094729, -0.04877400797019536272, -2.161318155665878038 ) ) ;
#43944=CARTESIAN_POINT ( 'NONE',  ( 6.609000000000036401, 0.002801690667396730238, 2.000160786441218086 ) ) ;
#43948=CARTESIAN_POINT ( 'NONE',  ( 1.224769985559545304, -0.04580521419573525821, 1.724442238450181186 ) ) ;
#43952=CARTESIAN_POINT ( 'NONE',  ( 0.5437790142346760058, 1.764394620056912055, 0.1386062191098563767 ) ) ;
#43953=CARTESIAN_POINT ( 'NONE',  ( 2.279941584743001126, 1.973825526184776580, -0.3948664393432794184 ) ) ;
#43955=CARTESIAN_POINT ( 'NONE',  ( 3.962124768131184638, 2.190450126196175074, -0.2673064950309556043 ) ) ;
#43956=CARTESIAN_POINT ( 'NONE',  ( 5.524361701572801486, 1.063745579927848794, 1.892525341434271091 ) ) ;
#43960=CARTESIAN_POINT ( 'NONE',  ( 3.141385665567609564, 0.05408136815227351790, 2.119969838212852675 ) ) ;
#43961=CARTESIAN_POINT ( 'NONE',  ( 2.566029989117986077, -1.034146858587611906, 1.730878619409223163 ) ) ;
#43962=CARTESIAN_POINT ( 'NONE',  ( 3.410248120744460376, -1.809760825414870267, -0.08362741940017533182 ) ) ;
#43967=CARTESIAN_POINT ( 'NONE',  ( 0.2857447052702493662, -0.8859512962964136706, 1.647562673099879138 ) ) ;
#43969=CARTESIAN_POINT ( 'NONE',  ( 6.375623774462673587, 1.745513195383348926, -0.5351242734627087438 ) ) ;
#43971=CARTESIAN_POINT ( 'NONE',  ( 1.376049117821566137, -1.906831126389372022, -0.1839060664316337634 ) ) ;
#43975=CARTESIAN_POINT ( 'NONE',  ( 5.295850518597075229, -0.7817450549502875656, 2.015575934489414411 ) ) ;
#43978=CARTESIAN_POINT ( 'NONE',  ( 3.058948843759463188, 0.5191580478346515815, 2.055925682384197373 ) ) ;
#43979=CARTESIAN_POINT ( 'NONE',  ( -0.02988540731099689068, 4.098597030192621560, -2.281328281275496916 ) ) ;
#43981=CARTESIAN_POINT ( 'NONE',  ( 4.305907937463241630, -1.966273716216637046, 0.1420514027590073225 ) ) ;
#43982=CARTESIAN_POINT ( 'NONE',  ( 6.521744167503259249, -0.4122283346772101509, 1.874327247564554266 ) ) ;
#43985=CARTESIAN_POINT ( 'NONE',  ( 5.296159404803077564, -0.9547103268642830320, -1.889991272064439176 ) ) ;
#43987=CARTESIAN_POINT ( 'NONE',  ( 6.795365950078042339, -1.759944107108902367, 0.8842400836535941888 ) ) ;
#43988=CARTESIAN_POINT ( 'NONE',  ( 2.290873232013816541, 1.501373485850267198, 1.231690586011934041 ) ) ;
#43992=CARTESIAN_POINT ( 'NONE',  ( 3.978531085967525360, -0.2047937889433377179, -2.080580830362771305 ) ) ;
#43995=CARTESIAN_POINT ( 'NONE',  ( 0.3459856143687444208, 0.9327069207067508749, -1.552719410179828952 ) ) ;
#43997=CARTESIAN_POINT ( 'NONE',  ( 5.039771180630152614, -1.558841386063321455, -1.562417271110942307 ) ) ;
#43999=CARTESIAN_POINT ( 'NONE',  ( 3.258999418838660400, -1.672185875938383859, 1.440126295696932068 ) ) ;
#44001=CARTESIAN_POINT ( 'NONE',  ( 2.086439996564274146, -1.175226666667992914, 1.508458442701497315 ) ) ;
#44003=CARTESIAN_POINT ( 'NONE',  ( 4.756339170418532269, -2.069830778647030023, -0.05414847147890837487 ) ) ;
#44005=CARTESIAN_POINT ( 'NONE',  ( 2.342841879718413622, 0.4729757327756216601, 2.109170662781891359 ) ) ;
#44006=CARTESIAN_POINT ( 'NONE',  ( 5.073855206572205567, -1.217758175834412260, 1.821886007100224969 ) ) ;
#44017=CARTESIAN_POINT ( 'NONE',  ( 6.227406488038683463, 0.1581931229415085571, -2.064300627111630870 ) ) ;
#44018=CARTESIAN_POINT ( 'NONE',  ( 4.723225685987796574, -0.09301374627979085152, 1.924373785979951013 ) ) ;
#44019=CARTESIAN_POINT ( 'NONE',  ( 6.310183273250552283, 1.218863855842572175, -1.731025912240143017 ) ) ;
#44023=CARTESIAN_POINT ( 'NONE',  ( 4.909022984592102290, -1.584153972474154459, 1.169931220002416339 ) ) ;
#44024=CARTESIAN_POINT ( 'NONE',  ( 0.6213436022244859247, -2.079703760468250451, 0.6910661131078955632 ) ) ;
#44025=CARTESIAN_POINT ( 'NONE',  ( 4.406759617291758246, 1.409692282476209924, -1.160130723419292131 ) ) ;
#44031=CARTESIAN_POINT ( 'NONE',  ( 3.192734241421916419, 1.453351889590439816, 1.130385295574042104 ) ) ;
#44032=CARTESIAN_POINT ( 'NONE',  ( 5.062748685862976217, 0.5883423404384033883, 1.925289297555386359 ) ) ;
#44033=CARTESIAN_POINT ( 'NONE',  ( 0.7205771127097709838, -1.942975266472912299, -1.227557580038857399 ) ) ;
#44034=CARTESIAN_POINT ( 'NONE',  ( 5.981297772519294398, -0.05168599705708888659, 1.961257141919122926 ) ) ;
#44038=CARTESIAN_POINT ( 'NONE',  ( 0.9067890187421032699, 0.5993529260880943177, 1.981728858978973218 ) ) ;
#44040=CARTESIAN_POINT ( 'NONE',  ( 1.804351596996961238, 1.546985077243122397, -1.406606537801007972 ) ) ;
#44041=CARTESIAN_POINT ( 'NONE',  ( 0.3209005354254980680, -0.09642172165634513292, 1.868300368337752815 ) ) ;
#44045=CARTESIAN_POINT ( 'NONE',  ( 1.557743604271996762, -1.230989698698783608, 1.230628217043183925 ) ) ;
#44049=CARTESIAN_POINT ( 'NONE',  ( 3.158550911874979938, -1.305529951647845355, 1.127390448682374924 ) ) ;
#44050=CARTESIAN_POINT ( 'NONE',  ( 2.630644284709309666, 0.2711686948545319886, 2.174668582101045633 ) ) ;
#44051=CARTESIAN_POINT ( 'NONE',  ( 5.110101661328442901, -2.196521081226535443, 0.2136625748923453583 ) ) ;
#44054=CARTESIAN_POINT ( 'NONE',  ( 2.870184708472456325, -2.148041568373111776, 0.3144570722862209955 ) ) ;
#44055=CARTESIAN_POINT ( 'NONE',  ( 0.7854531640391904102, 1.224056292049885419, 1.354719642434290439 ) ) ;
#44056=CARTESIAN_POINT ( 'NONE',  ( 3.520818605202329810, 0.3149718393082919232, 2.093694903831443188 ) ) ;
#44057=CARTESIAN_POINT ( 'NONE',  ( 6.539320575229251808, 0.01001626003939220556, 1.796977979958065852 ) ) ;
#44059=CARTESIAN_POINT ( 'NONE',  ( 3.421668107411596882, -1.366637645153226055, -1.840301194555084230 ) ) ;
#44061=CARTESIAN_POINT ( 'NONE',  ( 6.727182134110238465, -0.007837387828812580545, 2.289081727344749240 ) ) ;
#44064=CARTESIAN_POINT ( 'NONE',  ( 5.830790380266278383, 1.493519825859883854, -1.644436761705171612 ) ) ;
#44070=CARTESIAN_POINT ( 'NONE',  ( 3.955704058034177351, -1.882473782773282700, -0.7231407674024927790 ) ) ;
#44072=CARTESIAN_POINT ( 'NONE',  ( 1.815356060102671698, -1.766853000457936806, -1.063981086615989113 ) ) ;
#44077=CARTESIAN_POINT ( 'NONE',  ( 5.490230790444213582, -0.5297859672059505032, -2.126319610106224278 ) ) ;
#44078=CARTESIAN_POINT ( 'NONE',  ( 2.602185585689294367, -0.1948409242511044692, 2.006959980107574371 ) ) ;
#44079=CARTESIAN_POINT ( 'NONE',  ( 1.909461114401575843, -0.8690924446688346183, -1.623246667998109682 ) ) ;
#44082=CARTESIAN_POINT ( 'NONE',  ( 6.581069972421211389, -0.09314021972051110543, -1.823315219958022482 ) ) ;
#44084=CARTESIAN_POINT ( 'NONE',  ( 6.227429363453246935, -2.132905367568146637, 0.7551758973065140212 ) ) ;
#44086=CARTESIAN_POINT ( 'NONE',  ( 1.594499780405156830, -2.096077427685174577, -0.2048490792218547185 ) ) ;
#44097=CARTESIAN_POINT ( 'NONE',  ( 1.406653384705614629, -2.110883996484512970, -0.2024971186788473154 ) ) ;
#44098=CARTESIAN_POINT ( 'NONE',  ( 3.234858691920166951, 1.406421598713000432, -1.719528915531160385 ) ) ;
#44099=CARTESIAN_POINT ( 'NONE',  ( 0.4345545588612038657, 1.130843733186673639, -1.894998796914903139 ) ) ;
#44102=CARTESIAN_POINT ( 'NONE',  ( 4.738696794244872557, -1.902450960283699199, -0.4786090228221794307 ) ) ;
#44109=CARTESIAN_POINT ( 'NONE',  ( 3.779626292077961747, 0.2561244552635975058, -2.104982076983111572 ) ) ;
#44111=CARTESIAN_POINT ( 'NONE',  ( 4.627887939457571598, -1.327398817707679868, -1.706084338546076662 ) ) ;
#44112=CARTESIAN_POINT ( 'NONE',  ( 4.106863108761789505, -0.3106082297497716471, 1.814695527881895698 ) ) ;
#44115=CARTESIAN_POINT ( 'NONE',  ( 5.560439297528310121, -1.575983010118024774, -0.7385839837668640717 ) ) ;
#44119=CARTESIAN_POINT ( 'NONE',  ( 3.168983506954273999, -1.996715753333128118, -0.8287754370841573515 ) ) ;
#44120=CARTESIAN_POINT ( 'NONE',  ( 6.116564501996816894, 0.5879282371138266905, -1.928457050679150298 ) ) ;
#44122=CARTESIAN_POINT ( 'NONE',  ( 2.553791647773369089, 0.5774160426356907960, -2.083079400968433248 ) ) ;
#44125=CARTESIAN_POINT ( 'NONE',  ( 4.165272970243100836, 0.2446167658484849627, -1.956081580383911778 ) ) ;
#44126=CARTESIAN_POINT ( 'NONE',  ( 0.04676574305502099321, -1.756316032869180921, 1.310637071781264984 ) ) ;
#44127=CARTESIAN_POINT ( 'NONE',  ( 4.827648274430585751, 0.9952931021880854212, -1.667489682845281207 ) ) ;
#44135=CARTESIAN_POINT ( 'NONE',  ( 2.520803682403276902, 1.441976459853638204, -1.670562425240495363 ) ) ;
#44137=CARTESIAN_POINT ( 'NONE',  ( 6.754749089495472703, -0.5201146403621333958, -1.891512521893109700 ) ) ;
#44143=CARTESIAN_POINT ( 'NONE',  ( 5.402248404572855378, 1.391679675130308880, -1.205515946264820615 ) ) ;
#44148=CARTESIAN_POINT ( 'NONE',  ( 5.959260761812961604, -1.790568634313693730, 1.135864312162476297 ) ) ;
#44151=CARTESIAN_POINT ( 'NONE',  ( 6.204382384804184802, -0.7375479284208189545, -1.924474620761642996 ) ) ;
#44153=CARTESIAN_POINT ( 'NONE',  ( 2.470971460243949203, 1.660895280785526618, 0.8397924955986632023 ) ) ;
#44154=CARTESIAN_POINT ( 'NONE',  ( 4.247483403459266782, 1.840758003770435414, -0.04960325993209198370 ) ) ;
#44161=CARTESIAN_POINT ( 'NONE',  ( 4.073040751519330094, -2.058760688187323495, -0.7953439701907027981 ) ) ;
#44162=CARTESIAN_POINT ( 'NONE',  ( 5.905634875922824989, -0.5580066813290808225, 2.192401876011939699 ) ) ;
#44164=CARTESIAN_POINT ( 'NONE',  ( 6.222923320161976690, 1.335851037236086558, -1.223852264422401692 ) ) ;
#44165=CARTESIAN_POINT ( 'NONE',  ( -0.1179535434602772825, -2.016182236903838465, -0.04464881524945257807 ) ) ;
#44169=CARTESIAN_POINT ( 'NONE',  ( 5.496708366351358066, -1.866603419165157041, -0.4147590543357379533 ) ) ;
#44171=CARTESIAN_POINT ( 'NONE',  ( 1.059204734455133412, 0.3686402435371800013, -1.833797362824276078 ) ) ;
#44173=CARTESIAN_POINT ( 'NONE',  ( 0.8488426437929346147, -1.825078332268307513, -0.8578388575243289793 ) ) ;
#44175=CARTESIAN_POINT ( 'NONE',  ( 3.457739842999438817, 0.5116738510754537117, -2.042838612040797752 ) ) ;
#44180=CARTESIAN_POINT ( 'NONE',  ( 2.795180614130913010, -0.1526695769738794506, -2.014101982623817566 ) ) ;
#44183=CARTESIAN_POINT ( 'NONE',  ( 4.569695524216377258, 2.097929177840287540, -0.5203329012281321386 ) ) ;
#44189=CARTESIAN_POINT ( 'NONE',  ( 0.5026746641029911089, 2.165404592850531440, 0.1593437185135812284 ) ) ;
#44192=CARTESIAN_POINT ( 'NONE',  ( 1.065666191918061445, -1.167978014494171823, 1.423405568861766168 ) ) ;
#44194=CARTESIAN_POINT ( 'NONE',  ( 2.648187065138879692, 0.7411268365287645432, 2.062558662443473523 ) ) ;
#44196=CARTESIAN_POINT ( 'NONE',  ( 2.307839474932214419, -0.4956500345179111200, 2.207406129587013766 ) ) ;
#44202=CARTESIAN_POINT ( 'NONE',  ( 4.024454502147566615, 1.679793015868607409, 0.5571282570626963082 ) ) ;
#44203=CIRCLE ( 'NONE', #71834, 0.05000000000000109912 ) ;
#44204=( BOUNDED_CURVE ( )  B_SPLINE_CURVE ( 3, ( #136753, #202780, #82648, #148732 ),
 .UNSPECIFIED., .F., .T. ) 
 B_SPLINE_CURVE_WITH_KNOTS ( ( 4, 4 ),
 ( 0.000000000000000000, 0.5000000000000001110 ),
 .UNSPECIFIED. ) 
 CURVE ( )  GEOMETRIC_REPRESENTATION_ITEM ( )  RATIONAL_B_SPLINE_CURVE ( ( 1.000000000000000000, 0.3333333333333332038, 0.3333333333333333703, 1.000000000000000222 ) ) 
 REPRESENTATION_ITEM ( '' )  );
#44206=CARTESIAN_POINT ( 'NONE',  ( 1.307801118376609839, -0.5120802815330603996, 2.042612192628911139 ) ) ;
#44210=CARTESIAN_POINT ( 'NONE',  ( 5.993767587909683670, -2.000856116866961187, 0.2496242821527286382 ) ) ;
#44215=CARTESIAN_POINT ( 'NONE',  ( 4.100366707588389836, -0.5864361863821172527, -1.776433678864146382 ) ) ;
#44216=CARTESIAN_POINT ( 'NONE',  ( 4.258688845354158481, -0.6446009455991275061, -1.967446834807617506 ) ) ;
#44224=CARTESIAN_POINT ( 'NONE',  ( 4.387127823891323608, 0.09410986116351567621, 1.959716250186482434 ) ) ;
#44225=CARTESIAN_POINT ( 'NONE',  ( 1.036482258494644038, 1.943774389176852857, -0.5350038931242264706 ) ) ;
#44229=CARTESIAN_POINT ( 'NONE',  ( 1.124039026005444475, 1.118881483734196935, -1.498852260102357947 ) ) ;
#44231=CARTESIAN_POINT ( 'NONE',  ( 2.988542084594744797, -1.195720007494217585, 1.619529446093708636 ) ) ;
#44233=CARTESIAN_POINT ( 'NONE',  ( 3.374719764411674205, -0.4154235484931252942, -2.075916080105549177 ) ) ;
#44235=CARTESIAN_POINT ( 'NONE',  ( 4.861816338261779613, -0.5554421346023461492, 1.994381909410049669 ) ) ;
#44237=CARTESIAN_POINT ( 'NONE',  ( -0.09403702165171158589, -0.8981432076055823055, -1.886421477387869361 ) ) ;
#44239=CARTESIAN_POINT ( 'NONE',  ( 5.086841682847768276, -0.2248377094848166835, -1.811598703993194670 ) ) ;
#44244=CARTESIAN_POINT ( 'NONE',  ( 6.194375513154499302, -2.195555142843173879, -0.2223249613259313806 ) ) ;
#44246=CARTESIAN_POINT ( 'NONE',  ( 5.285773936917006921, 1.841837585529454202, -0.5139651673399318055 ) ) ;
#44256=CARTESIAN_POINT ( 'NONE',  ( -0.02299388927988389383, 2.039721852852835582, -2.328191723522631928 ) ) ;
#44261=CARTESIAN_POINT ( 'NONE',  ( 2.922656654487673311, -1.361644196593906342, 1.423118114318456584 ) ) ;
#44263=CARTESIAN_POINT ( 'NONE',  ( 3.884388800492278193, -0.6352171928143932611, -1.913798906059568594 ) ) ;
#44266=CARTESIAN_POINT ( 'NONE',  ( 6.727182134110227807, 1.996671600852136352, 2.590479658440256738 ) ) ;
#44268=CARTESIAN_POINT ( 'NONE',  ( 3.451304434523004172, 0.5324976444292061073, -2.125649318046138880 ) ) ;
#44270=CARTESIAN_POINT ( 'NONE',  ( 2.274328125206574569, -1.186679513062695257, 1.517402005686524280 ) ) ;
#44273=CARTESIAN_POINT ( 'NONE',  ( 0.1331565106231328843, 0.003911343561965873426, -1.946049565259087455 ) ) ;
#44279=CARTESIAN_POINT ( 'NONE',  ( 6.532758020889952277, -1.641319963461195464, 0.8346263169811756200 ) ) ;
#44280=CARTESIAN_POINT ( 'NONE',  ( 2.842442125518374496, 1.116481279481882805, -1.674925767759533723 ) ) ;
#44281=CARTESIAN_POINT ( 'NONE',  ( 4.025041230705061146, 2.281562605710918845, -0.2770438755856743929 ) ) ;
#44282=CARTESIAN_POINT ( 'NONE',  ( -0.1288028175206544224, 1.298820314038674928, -2.522219681210400744 ) ) ;
#44283=CARTESIAN_POINT ( 'NONE',  ( 1.621681814730125515, 1.834508062647151272, -0.3115270159769789604 ) ) ;
#44286=CARTESIAN_POINT ( 'NONE',  ( 6.486579876843341808, -1.171037552013409089, 1.512559164390047783 ) ) ;
#44289=CARTESIAN_POINT ( 'NONE',  ( 4.493745196466782943, -2.090321524099489903, -0.04957026750533782833 ) ) ;
#44290=CARTESIAN_POINT ( 'NONE',  ( 3.766346201128992988, -1.256895078192099335, 1.385637336983977397 ) ) ;
#44295=CARTESIAN_POINT ( 'NONE',  ( 6.182236774357948050, -0.9162642880373177423, 1.461205601097197659 ) ) ;
#44297=CARTESIAN_POINT ( 'NONE',  ( 1.511953044659793077, -1.632839461445406481, 0.5843666143663208690 ) ) ;
#44301=CARTESIAN_POINT ( 'NONE',  ( 5.331008558256671748, -2.041869270619638854, -0.7380826535893101337 ) ) ;
#44302=CARTESIAN_POINT ( 'NONE',  ( 4.336427269025699971, 1.790907886515300085, 0.3537760332646966432 ) ) ;
#44303=CARTESIAN_POINT ( 'NONE',  ( 2.237090426018002454, -0.09115598566783281176, -1.959741687340324168 ) ) ;
#44304=CARTESIAN_POINT ( 'NONE',  ( 0.6325982246286944166, 0.6188553777890459795, 2.024753282845246805 ) ) ;
#44307=CARTESIAN_POINT ( 'NONE',  ( 2.403126630736720948, -0.3650820022202577175, -2.088671427859823293 ) ) ;
#44312=CARTESIAN_POINT ( 'NONE',  ( 0.4970418144054839504, 0.3504251219754518365, 2.040211723117946629 ) ) ;
#44315=CARTESIAN_POINT ( 'NONE',  ( 3.018465837578692579, -2.218647833171137673, 0.1111532960578337226 ) ) ;
#44317=CARTESIAN_POINT ( 'NONE',  ( 0.6515572338587878320, 1.139979866233470807, 1.996073129511093169 ) ) ;
#44319=CARTESIAN_POINT ( 'NONE',  ( 5.805554948619430000, -1.622591123950654746, -1.273203187973567241 ) ) ;
#44322=CARTESIAN_POINT ( 'NONE',  ( 0.2333540202161402677, 0.7093705336200817335, -2.128223931541360248 ) ) ;
#44323=CARTESIAN_POINT ( 'NONE',  ( 5.425302022954732628, -1.172690680311109901, -1.419496581506813904 ) ) ;
#44326=CARTESIAN_POINT ( 'NONE',  ( -0.1106727585416019261, 4.087503477334416324, -2.558207815289376796 ) ) ;
#44327=CARTESIAN_POINT ( 'NONE',  ( 2.449869591326372387, 1.724352457016034457, 0.04528501180301596624 ) ) ;
#44328=CARTESIAN_POINT ( 'NONE',  ( 1.446500318503376903, -1.422605717829699579, 1.429450658469958446 ) ) ;
#44329=CARTESIAN_POINT ( 'NONE',  ( 3.059543388688467314, -1.367113599135186819, 1.847867383329027335 ) ) ;
#44330=CARTESIAN_POINT ( 'NONE',  ( 2.900009951539525677, -0.7123764238676842941, 2.147366075387107553 ) ) ;
#44331=CARTESIAN_POINT ( 'NONE',  ( 5.479168138989118475, -0.05037515785718051087, -2.105640702651077945 ) ) ;
#44333=CARTESIAN_POINT ( 'NONE',  ( 3.391635040236582022, -0.7200671834438672203, 1.616821809559340517 ) ) ;
#44335=CARTESIAN_POINT ( 'NONE',  ( 6.040627043210095692, -1.938779113641406759, 1.222911669862235096 ) ) ;
#44336=CARTESIAN_POINT ( 'NONE',  ( 4.540845788227630742, -1.424921066559198257, -1.165926479108070346 ) ) ;
#44341=CARTESIAN_POINT ( 'NONE',  ( 4.927760762764835434, 1.128268568998530563, -1.878541326455762661 ) ) ;
#44344=CARTESIAN_POINT ( 'NONE',  ( 5.248515149483167441, -2.054309126314420642, -0.2569322651706855143 ) ) ;
#44345=CARTESIAN_POINT ( 'NONE',  ( 0.1105650446291406575, 1.931126588553159884, 0.5807481968119408977 ) ) ;
#44347=CARTESIAN_POINT ( 'NONE',  ( 3.211465258343335627, -0.3752234067680487728, 1.889445157240315254 ) ) ;
#44350=CARTESIAN_POINT ( 'NONE',  ( 0.4576791451081770323, -1.901157720872756141, 1.148870853762502753 ) ) ;
#44360=CARTESIAN_POINT ( 'NONE',  ( 1.258172656280614365, -1.962046632281065461, -0.003472340283867945618 ) ) ;
#44362=CARTESIAN_POINT ( 'NONE',  ( 6.526263005029544928, 1.249015235541932167, -1.764162671312206498 ) ) ;
#44363=CARTESIAN_POINT ( 'NONE',  ( 5.547302793442128177, 1.730978599593002043, -0.9233319674036490898 ) ) ;
#44366=CARTESIAN_POINT ( 'NONE',  ( 6.192270064542984898, -2.150811787302907785, -0.2168040374768212541 ) ) ;
#44370=CARTESIAN_POINT ( 'NONE',  ( 6.626250064558294461, 1.136881752820615432, -1.610320780329032253 ) ) ;
#44371=CARTESIAN_POINT ( 'NONE',  ( 6.151638658550825589, -0.2577636348817541334, -1.714396880517143451 ) ) ;
#44373=CARTESIAN_POINT ( 'NONE',  ( 2.542740116143254792, -1.820367712357463974, 1.220030464664762393 ) ) ;
#44374=CARTESIAN_POINT ( 'NONE',  ( 4.454349891636342207, 2.307156057683857675, -0.05211387993751984832 ) ) ;
#44375=CARTESIAN_POINT ( 'NONE',  ( 5.800091581907264704, -2.060967560761736372, -0.004405934171711199318 ) ) ;
#44376=CARTESIAN_POINT ( 'NONE',  ( 0.7966981359470609592, 1.587242811699969725, 1.118599961973030021 ) ) ;
#44379=CARTESIAN_POINT ( 'NONE',  ( 4.623349522974431025, 1.846400237221163865, 1.042759738753673338 ) ) ;
#44381=CARTESIAN_POINT ( 'NONE',  ( 2.022111496571117772, -1.799922141918413487, 0.9091460122201827643 ) ) ;
#44383=CARTESIAN_POINT ( 'NONE',  ( 5.737410212107617369, -1.997324651315037780, 0.9386623957203032997 ) ) ;
#44387=CARTESIAN_POINT ( 'NONE',  ( 0.1174333910212103232, -1.791171220025630895, 0.3524246893974944395 ) ) ;
#44393=CARTESIAN_POINT ( 'NONE',  ( 5.137599278355773791, -1.455842209265911569, -1.458961989641535117 ) ) ;
#44398=CARTESIAN_POINT ( 'NONE',  ( 4.776038667982859032, 1.997392889608617716, -0.2983725866285909523 ) ) ;
#44405=CARTESIAN_POINT ( 'NONE',  ( 4.610263661134276880, -0.8792652907330700263, -1.864042625929088759 ) ) ;
#44406=CARTESIAN_POINT ( 'NONE',  ( 3.164685561777963230, 1.281361203394768111, 1.556908733426412450 ) ) ;
#44408=CARTESIAN_POINT ( 'NONE',  ( 6.727182134110178069, 2.947419669445831669, 2.641212418657997496 ) ) ;
#44410=CARTESIAN_POINT ( 'NONE',  ( 3.221888912838869690, 0.9023448338944944913, -1.803416113280359445 ) ) ;
#44413=CARTESIAN_POINT ( 'NONE',  ( 2.899767358622063806, 0.2439914025648345919, 2.001204936777578602 ) ) ;
#44414=CARTESIAN_POINT ( 'NONE',  ( 2.167674216824653222, -1.133089441918342599, 1.451089449600144521 ) ) ;
#44415=CARTESIAN_POINT ( 'NONE',  ( 1.471738413253330879, 0.1659702479998256264, -2.301786031945464828 ) ) ;
#44417=CARTESIAN_POINT ( 'NONE',  ( 2.794378387653595475, -2.155598273342887339, -0.1620501260681943834 ) ) ;
#44424=CARTESIAN_POINT ( 'NONE',  ( 1.674454752297813265, -1.775319108138155633, -0.5897529795871117031 ) ) ;
#44425=CARTESIAN_POINT ( 'NONE',  ( 5.700065208342940615, -1.971640594297157989, -0.0006100080248323812597 ) ) ;
#44429=CARTESIAN_POINT ( 'NONE',  ( 0.1005910224048736229, -2.206496634663042133, -0.04943112074598519229 ) ) ;
#44430=FACE_OUTER_BOUND ( 'NONE', #52390, .T. ) ;
#44434=CARTESIAN_POINT ( 'NONE',  ( 5.190288350601474754, -1.956472792631309909, -0.2422539641438857527 ) ) ;
#44435=CARTESIAN_POINT ( 'NONE',  ( 6.486581104273712484, -1.239329707167437622, 1.595369898402546838 ) ) ;
#44437=CARTESIAN_POINT ( 'NONE',  ( 4.354349988907435964, 2.307223249097400064, -0.05412331456603951957 ) ) ;
#44438=CARTESIAN_POINT ( 'NONE',  ( 1.955997896808071568, -0.6987562721488985717, 1.940702610317937671 ) ) ;
#44445=CARTESIAN_POINT ( 'NONE',  ( 5.125502745298136098, 0.2179265861129157655, -2.160231653469760982 ) ) ;
#44448=CARTESIAN_POINT ( 'NONE',  ( 4.458453498679889826, -1.646799808365447149, -0.8236825204945982248 ) ) ;
#44451=CARTESIAN_POINT ( 'NONE',  ( 5.952700804540857149, -1.878875186057769486, -1.127905468421293689 ) ) ;
#44453=CARTESIAN_POINT ( 'NONE',  ( 6.192268726830573833, -2.250890937568471362, -0.2291988078206678991 ) ) ;
#44460=CARTESIAN_POINT ( 'NONE',  ( 1.129378208368720271, -1.118813933885588474, -1.371354111526525754 ) ) ;
#44462=CARTESIAN_POINT ( 'NONE',  ( 4.986981296356192139, -1.896340117422308236, -0.6759883393069978652 ) ) ;
#44464=CARTESIAN_POINT ( 'NONE',  ( 4.454198790814194453, 2.105553956100237656, -0.04914431425445846269 ) ) ;
#44465=CARTESIAN_POINT ( 'NONE',  ( 2.565921762024740982, -0.9824477935329900546, 1.644319621262643638 ) ) ;
#44467=CARTESIAN_POINT ( 'NONE',  ( 3.033609518001907368, 1.871031307821906964, -0.6153852250644732402 ) ) ;
#44468=CARTESIAN_POINT ( 'NONE',  ( 5.326427914677607234, -0.9117507067677769195, -1.802394291917883473 ) ) ;
#44469=CARTESIAN_POINT ( 'NONE',  ( 1.270139834521961886, -1.189467451172643964, 1.443775233441677130 ) ) ;
#44470=CARTESIAN_POINT ( 'NONE',  ( 5.285687151129126349, 1.162661966624499277, 1.274325963116212934 ) ) ;
#44471=CARTESIAN_POINT ( 'NONE',  ( 1.195406425308798148, 1.765864799226088744, -0.7346160280939582066 ) ) ;
#44473=CARTESIAN_POINT ( 'NONE',  ( 0.8388348947251201837, 2.174866457552121268, 0.3736606161612308630 ) ) ;
#44477=CARTESIAN_POINT ( 'NONE',  ( 6.614126560844452385, -0.8839695271746010885, -1.648598838400926692 ) ) ;
#44483=CARTESIAN_POINT ( 'NONE',  ( 1.574760213118006735, 1.391939136705011348, -1.532762857463897843 ) ) ;
#44488=CARTESIAN_POINT ( 'NONE',  ( -0.09308815784560355022, -0.4424663830696302091, -1.977475021732390204 ) ) ;
#44494=CARTESIAN_POINT ( 'NONE',  ( 4.710314442360476583, -1.556670644073439913, -1.281164596596932936 ) ) ;
#44495=CARTESIAN_POINT ( 'NONE',  ( 4.505048170306029220, -0.08773398713153966744, 1.913818227509517023 ) ) ;
#44497=CARTESIAN_POINT ( 'NONE',  ( 2.419692422129790632, -1.264489869534379141, -1.789777738334753732 ) ) ;
#44498=CARTESIAN_POINT ( 'NONE',  ( 0.1335669894368864130, 4.084991946249068029, -2.708374394877795410 ) ) ;
#44500=CARTESIAN_POINT ( 'NONE',  ( 5.748296788003684377, 0.9886478197097836595, -1.753632158501418514 ) ) ;
#44503=CARTESIAN_POINT ( 'NONE',  ( 6.398082464950202386, -0.9982666083749867081, -1.867140504451180183 ) ) ;
#44505=CARTESIAN_POINT ( 'NONE',  ( 3.175413592762990067, 1.328342846777453845, 1.614508523670985740 ) ) ;
#44507=CARTESIAN_POINT ( 'NONE',  ( 2.080655396751258213, -0.08067463971387846267, -1.723007254337567407 ) ) ;
#44509=CARTESIAN_POINT ( 'NONE',  ( 6.117454236943913770, 1.763945953808215394, 1.176740244630887222 ) ) ;
#44517=CARTESIAN_POINT ( 'NONE',  ( 3.211360534488953977, 1.429591190403207035, 1.112411576641762379 ) ) ;
#44522=CARTESIAN_POINT ( 'NONE',  ( 3.017991377792153429, -1.809312282836759378, 0.09115427604276456208 ) ) ;
#44523=CARTESIAN_POINT ( 'NONE',  ( 6.639320575229294086, 0.5800432152290584398, 2.049144803211971233 ) ) ;
#44526=CARTESIAN_POINT ( 'NONE',  ( 3.613571450151699782, 0.4543224947703514149, -1.804596983994880333 ) ) ;
#44527=CARTESIAN_POINT ( 'NONE',  ( 1.177184062793021679, 1.451467631357589383, 1.250241458713635456 ) ) ;
#44528=CARTESIAN_POINT ( 'NONE',  ( 0.9733497034139363402, 1.760643049788807257, -0.4823509818385819936 ) ) ;
#44535=CARTESIAN_POINT ( 'NONE',  ( 5.682459527512692787, 1.176241607570350567, -1.579419126353029279 ) ) ;
#44537=CARTESIAN_POINT ( 'NONE',  ( 2.518767860054324625, 0.2516336668320385828, 2.000731427934741902 ) ) ;
#44540=CARTESIAN_POINT ( 'NONE',  ( 0.1114262914704557683, -2.049844763593706265, 0.4100319678014376912 ) ) ;
#44542=CARTESIAN_POINT ( 'NONE',  ( 4.928697230495170167, 1.843396615675118699, 0.5593075106890015302 ) ) ;
#44545=CARTESIAN_POINT ( 'NONE',  ( 1.008509592878764183, 1.385430265305506170, -1.188947219173806413 ) ) ;
#44546=CARTESIAN_POINT ( 'NONE',  ( 2.332911791115964473, 2.140974936812658935, 0.5348262304398290201 ) ) ;
#44548=CARTESIAN_POINT ( 'NONE',  ( -0.07025823700084612988, -1.875094440630159065, 0.3749275819610526916 ) ) ;
#44549=CARTESIAN_POINT ( 'NONE',  ( 0.6956774629466413451, -1.390297546174504850, -1.395334862655448260 ) ) ;
#44550=CARTESIAN_POINT ( 'NONE',  ( 3.157691648149099972, 0.8757969000599256093, 1.733462199761313993 ) ) ;
#44551=CARTESIAN_POINT ( 'NONE',  ( 0.9661724576192336489, 1.646585359754201061, 1.163093122096101162 ) ) ;
#44553=CARTESIAN_POINT ( 'NONE',  ( 5.893359673372067675, -1.683065101977880840, 0.7942114673132483205 ) ) ;
#44559=CARTESIAN_POINT ( 'NONE',  ( 1.699035084177059174, 1.824418957995146195, 1.213967346723361596 ) ) ;
#44564=CARTESIAN_POINT ( 'NONE',  ( 2.912524513316586461, 1.322148455168963510, -1.259233298254287536 ) ) ;
#44569=CARTESIAN_POINT ( 'NONE',  ( 0.1253635393240644380, 7.629137130509072051, -2.744100600304347104 ) ) ;
#44571=CARTESIAN_POINT ( 'NONE',  ( 1.260239703848411441, 0.7801416839768731126, 1.761649912542123664 ) ) ;
#44572=CARTESIAN_POINT ( 'NONE',  ( 5.471523917629521172, -0.2915489554583711729, 1.939870717765689534 ) ) ;
#44577=CARTESIAN_POINT ( 'NONE',  ( 5.021103811603734535, -2.081066139062941023, 0.6872292908843835590 ) ) ;
#44579=CARTESIAN_POINT ( 'NONE',  ( 4.346580092118113470, -2.046995731385771400, -0.3088174131898810959 ) ) ;
#44583=CARTESIAN_POINT ( 'NONE',  ( 4.026267332373588914, -1.999701941076356349, 1.133592428816285080 ) ) ;
#44589=CARTESIAN_POINT ( 'NONE',  ( 3.626839189636944738, -1.793926730891879151, 0.7440942006126953778 ) ) ;
#44592=CARTESIAN_POINT ( 'NONE',  ( 5.396708386617175890, -1.867154475869851504, -0.4128305108781898936 ) ) ;
#44593=CARTESIAN_POINT ( 'NONE',  ( 6.598688221398479214, -0.4661808427693337475, -1.660524940999157373 ) ) ;
#44594=CARTESIAN_POINT ( 'NONE',  ( 4.610564714392807240, 1.931124171932835809, 0.5807562064495259690 ) ) ;
#44596=CARTESIAN_POINT ( 'NONE',  ( 1.313402753022639091, 1.947697196196996217, 1.037691534346518729 ) ) ;
#44599=CARTESIAN_POINT ( 'NONE',  ( 1.306708042577527262, 1.844576602789575137, 0.9840055123579400931 ) ) ;
#44600=CARTESIAN_POINT ( 'NONE',  ( 6.503183016764070068, 1.472852356768614479, 0.9808112332466749628 ) ) ;
#44601=CARTESIAN_POINT ( 'NONE',  ( 6.047500043413473136, -1.423963828944514010, 1.427935028000301809 ) ) ;
#44603=CARTESIAN_POINT ( 'NONE',  ( 2.994356955963250133, -0.6658908676899841783, -2.193406925754942893 ) ) ;
#44604=CARTESIAN_POINT ( 'NONE',  ( 0.6381061630796550643, -1.494939029692418320, 0.8907679528266756463 ) ) ;
#44605=CARTESIAN_POINT ( 'NONE',  ( 2.566775492539817627, 0.7186216927172992541, 1.995234744298620910 ) ) ;
#44607=CARTESIAN_POINT ( 'NONE',  ( 1.528208422804043121, 1.709223377337875549, -0.2899604983128030722 ) ) ;
#44610=CARTESIAN_POINT ( 'NONE',  ( 1.170657403521972562, -0.9760459728485239017, -1.939464792355448663 ) ) ;
#44611=CARTESIAN_POINT ( 'NONE',  ( 3.854704076794239764, -1.883312302057647880, -0.7212934815618715634 ) ) ;
#44612=CARTESIAN_POINT ( 'NONE',  ( 5.250000000000002665, 2.988487650205320908E-13, 2.052068128417942283 ) ) ;
#44615=CARTESIAN_POINT ( 'NONE',  ( 6.393193437440540805, 1.674708767708126045, -0.9521171982297592651 ) ) ;
#44617=CARTESIAN_POINT ( 'NONE',  ( 3.252379014334851437, 0.9957207747773239026, -1.985791214296761087 ) ) ;
#44618=ORIENTED_EDGE ( 'NONE', *, *, #73601, .F. ) ;
#44623=CARTESIAN_POINT ( 'NONE',  ( 0.2043192855987647494, 1.601443664334546213, 0.9084302959305108338 ) ) ;
#44624=CARTESIAN_POINT ( 'NONE',  ( 4.158614545834369736, -0.6132839004606009947, -1.863630207987923226 ) ) ;
#44628=CARTESIAN_POINT ( 'NONE',  ( 6.309908665641647652, -2.246456703917932618, 0.2676860584361096529 ) ) ;
#44630=CARTESIAN_POINT ( 'NONE',  ( 2.014201374223419272, 2.057289675485386216, -0.1496214851241447485 ) ) ;
#44635=CARTESIAN_POINT ( 'NONE',  ( 3.567518508692040236, 1.825626599287116791, -0.4067673385957787380 ) ) ;
#44636=CARTESIAN_POINT ( 'NONE',  ( 2.760114697247218807, 1.645750434341390900, -0.5467383172713826678 ) ) ;
#44637=CARTESIAN_POINT ( 'NONE',  ( 0.01182134700736507844, -2.246462713633586183, 0.4557613021327082681 ) ) ;
#44638=CARTESIAN_POINT ( 'NONE',  ( 1.360703683432495259, 0.8952624662355921359, 2.017188127302282030 ) ) ;
#44639=CARTESIAN_POINT ( 'NONE',  ( 3.854492016355787420, 0.7758605394001509836, 2.017853709245204463 ) ) ;
#44640=CARTESIAN_POINT ( 'NONE',  ( 4.523342001410900259, -1.195735706813789045, -1.530077746507539027 ) ) ;
#44641=CARTESIAN_POINT ( 'NONE',  ( 6.714126539417144102, -0.8821443205445091973, -1.649434700640100226 ) ) ;
#44642=CARTESIAN_POINT ( 'NONE',  ( 0.06249170576382599707, -1.450827213159947338, -1.451031289061120777 ) ) ;
#44646=CARTESIAN_POINT ( 'NONE',  ( 5.818982467333652764, 0.9914020171761170896, -1.755767668913270407 ) ) ;
#44650=CARTESIAN_POINT ( 'NONE',  ( 3.264084022359412529, 0.8216391472936382945, 1.630427331384458833 ) ) ;
#44651=CARTESIAN_POINT ( 'NONE',  ( 2.678998284833411070, -2.111460168698295004, -0.6414983429729387288 ) ) ;
#44656=CARTESIAN_POINT ( 'NONE',  ( 1.107682413490064022, 1.532168600112630230, 1.316196929287305473 ) ) ;
#44657=CARTESIAN_POINT ( 'NONE',  ( 0.9969211937387794098, -2.069638562867767373, -0.4609060192823294932 ) ) ;
#44661=CARTESIAN_POINT ( 'NONE',  ( 1.498636204049142773, 0.3563576638296832577, 1.826325547775342173 ) ) ;
#44664=CARTESIAN_POINT ( 'NONE',  ( 0.3214396764580421118, -0.1044536432763705502, 2.159311484102262479 ) ) ;
#44665=CARTESIAN_POINT ( 'NONE',  ( 5.801407773674092105, 1.352156682446106206, -1.496049708713815374 ) ) ;
#44669=CARTESIAN_POINT ( 'NONE',  ( 4.301258635363705451, 1.467727663998198429, 1.085573330547324744 ) ) ;
#44674=CARTESIAN_POINT ( 'NONE',  ( 6.081407632663145435, 1.356090666932512789, -1.492028312255622824 ) ) ;
#44675=CARTESIAN_POINT ( 'NONE',  ( 5.999929499617846496, -0.6670042279848520383, -1.716255146773135287 ) ) ;
#44676=CARTESIAN_POINT ( 'NONE',  ( -0.02299388927987088688, 7.629137130509112907, -2.510989390717012881 ) ) ;
#44677=CARTESIAN_POINT ( 'NONE',  ( 4.705897867575262516, -0.6186405800616563422, 2.223174812903663256 ) ) ;
#44679=CARTESIAN_POINT ( 'NONE',  ( 5.606754022945427351, 1.640879930231559758, -1.407263238018638507 ) ) ;
#44681=CARTESIAN_POINT ( 'NONE',  ( 2.560020840168964806, -1.337455066581024976, 1.408356088163305042 ) ) ;
#44685=CARTESIAN_POINT ( 'NONE',  ( 4.903846967696810388, 0.3865712588492843937, 2.265520236764162920 ) ) ;
#44688=CARTESIAN_POINT ( 'NONE',  ( 4.328871119428026049, 0.09166491666120352155, 1.868520897946590598 ) ) ;
#44690=CARTESIAN_POINT ( 'NONE',  ( 2.285291272251275707, 0.09004542135446562401, -1.910373438827176251 ) ) ;
#44693=CARTESIAN_POINT ( 'NONE',  ( 4.090592613104036879, -2.182713160620152859, -0.3248913242878055385 ) ) ;
#44695=CARTESIAN_POINT ( 'NONE',  ( -0.2108831679771167866, 1.375689764684871808, -2.152500126786048185 ) ) ;
#44698=CARTESIAN_POINT ( 'NONE',  ( 1.616417101162690440, 1.326873100732330890, -1.458104111731808983 ) ) ;
#44699=CARTESIAN_POINT ( 'NONE',  ( 1.290513193724596164, -1.035378025537621927, 2.062353807931560645 ) ) ;
#44700=CARTESIAN_POINT ( 'NONE',  ( 2.805073129645048624, -1.632656238785214597, 1.087510969322850629 ) ) ;
#44702=CARTESIAN_POINT ( 'NONE',  ( 6.666849506214659549, 1.532398756413049457, -1.380780335402414849 ) ) ;
#44704=CARTESIAN_POINT ( 'NONE',  ( 3.749232653202066778, 0.2420323627391370025, -2.001857840249580800 ) ) ;
#44710=CARTESIAN_POINT ( 'NONE',  ( 1.710090495726908966, 0.6328077935687204114, -2.076762233347277053 ) ) ;
#44714=CARTESIAN_POINT ( 'NONE',  ( 2.635844295777586943, 0.8854499327175249235, -1.647724587607077629 ) ) ;
#44715=CARTESIAN_POINT ( 'NONE',  ( 6.714160596891073141, -1.012370167489636819, -1.909856561116265450 ) ) ;
#44716=FACE_OUTER_BOUND ( 'NONE', #142960, .T. ) ;
#44717=CARTESIAN_POINT ( 'NONE',  ( 6.827182134110196365, 4.700652535171166768, 2.373648650996477372 ) ) ;
#44720=CARTESIAN_POINT ( 'NONE',  ( 1.734869227892420707, 1.784761669998648381, 0.6870963898520030533 ) ) ;
#44721=CARTESIAN_POINT ( 'NONE',  ( 4.539784583036060361, 0.7555593814247036910, -1.600612801534553542 ) ) ;
#44722=CARTESIAN_POINT ( 'NONE',  ( 2.385291144485178982, 0.09204604084523880514, -1.910175020619097275 ) ) ;
#44725=CARTESIAN_POINT ( 'NONE',  ( 6.257445408045815505, 1.831477697454777953, -0.5614084181123339956 ) ) ;
#44728=CARTESIAN_POINT ( 'NONE',  ( 1.170471352854907776, -0.9292243337341490328, -1.850172451097586990 ) ) ;
#44731=CARTESIAN_POINT ( 'NONE',  ( 5.190257414508706368, -1.856628772771324210, -0.2281712211116558864 ) ) ;
#44732=CARTESIAN_POINT ( 'NONE',  ( 1.189776066567624691, -0.8228614858879386151, 1.629801898503015156 ) ) ;
#44733=CARTESIAN_POINT ( 'NONE',  ( 4.828867971087246858, 2.111205472107956282, 0.6427781511747706622 ) ) ;
#44737=CARTESIAN_POINT ( 'NONE',  ( 2.717292478832333380, -1.793364790446878798, -1.018969015592002592 ) ) ;
#44744=CARTESIAN_POINT ( 'NONE',  ( 5.301260566756325510, -1.777534899005998481, 1.061244097098137606 ) ) ;
#44746=CARTESIAN_POINT ( 'NONE',  ( 2.776834730583700228, -2.067601613962879448, -0.6303956341740593050 ) ) ;
#44748=CARTESIAN_POINT ( 'NONE',  ( 3.000653711923051414, -1.990157830909113024, -0.3430147326864175783 ) ) ;
#44749=CARTESIAN_POINT ( 'NONE',  ( 6.720655732516639169, 2.430015300743305406, 2.455394564723146100 ) ) ;
#44756=CARTESIAN_POINT ( 'NONE',  ( 1.130092623156966347, 2.014433208573155110, 0.09411304420373775570 ) ) ;
#44758=CARTESIAN_POINT ( 'NONE',  ( 5.970311429539967740, -2.080533979117826782, -0.6889730390344513955 ) ) ;
#44760=CARTESIAN_POINT ( 'NONE',  ( 4.465046277278037934, -1.532637281380120564, 1.143568071694904598 ) ) ;
#44764=CARTESIAN_POINT ( 'NONE',  ( 3.462517696756307384, -1.944077823024586538, -0.5350690621670484148 ) ) ;
#44767=CARTESIAN_POINT ( 'NONE',  ( 5.631808906544129911, -1.097478420741523575, -1.330571920265137376 ) ) ;
#44773=CARTESIAN_POINT ( 'NONE',  ( 0.6728209460903147310, 1.430239379376567976, -1.496996390900617424 ) ) ;
#44777=CARTESIAN_POINT ( 'NONE',  ( 5.795527448272657089, 1.671165027121311430, -0.6995385440057879656 ) ) ;
#44780=CARTESIAN_POINT ( 'NONE',  ( 0.5272532902790193488, -0.2650996996472804734, 1.791917353721095285 ) ) ;
#44783=CARTESIAN_POINT ( 'NONE',  ( 3.099763004921416876, -2.188912590334081809, 0.1079765428157742069 ) ) ;
#44785=CARTESIAN_POINT ( 'NONE',  ( 0.4495626703563436743, 1.451167377975391304, 1.320406988977901985 ) ) ;
#44787=CARTESIAN_POINT ( 'NONE',  ( 4.605048111083247520, -0.08973289204975383460, 1.913620015931324581 ) ) ;
#44790=CARTESIAN_POINT ( 'NONE',  ( 6.727182134110200273, -0.004969159814478123736, 2.189081792362323586 ) ) ;
#44796=CARTESIAN_POINT ( 'NONE',  ( 2.061604318190731533, 0.3698614785779800185, -2.129673623264888960 ) ) ;
#44799=CARTESIAN_POINT ( 'NONE',  ( 1.764397251013736234, -1.293498944356825664, 1.288518760371157201 ) ) ;
#44800=CARTESIAN_POINT ( 'NONE',  ( -0.2046613956954954905, -0.1581703332043625232, -2.086340352340488646 ) ) ;
#44802=CARTESIAN_POINT ( 'NONE',  ( 5.016531207907320322, 1.258010867292450152, -1.323153095230594989 ) ) ;
#44804=CARTESIAN_POINT ( 'NONE',  ( 3.111475685156277038, 1.510342251817019532, 1.173009309769344588 ) ) ;
#44806=CARTESIAN_POINT ( 'NONE',  ( 3.631270037613967716, 0.05078019485712419873, -1.969077574667767783 ) ) ;
#44808=CARTESIAN_POINT ( 'NONE',  ( 5.442900063589676485, -1.533566843616997133, -1.191469007954217618 ) ) ;
#44812=FACE_OUTER_BOUND ( 'NONE', #194151, .T. ) ;
#44814=CARTESIAN_POINT ( 'NONE',  ( 4.037688526304391345, -1.829018870347882242, 0.5580751363460645376 ) ) ;
#44818=CARTESIAN_POINT ( 'NONE',  ( 5.285796247307868789, 1.939527786139252585, -0.5389555323440149426 ) ) ;
#44819=CARTESIAN_POINT ( 'NONE',  ( 0.2333540202161603905, 0.003568502611739342648, -2.045944795905803471 ) ) ;
#44821=CARTESIAN_POINT ( 'NONE',  ( 5.619710272201024814, -1.780234218580947436, 0.4041525643716862848 ) ) ;
#44822=CARTESIAN_POINT ( 'NONE',  ( 1.064989848632340363, 1.568927673159369762, -1.351003706900590018 ) ) ;
#44826=CARTESIAN_POINT ( 'NONE',  ( 6.543822781336226413, 0.7137633992815132222, -1.729328153040734506 ) ) ;
#44829=DIRECTION ( 'NONE',  ( 1.014813233446432150E-15, 1.000000000000000000, -4.583713267641621330E-32 ) ) ;
#44834=CARTESIAN_POINT ( 'NONE',  ( 4.096141260758720648, -0.2909454306243773325, 1.709365352543093186 ) ) ;
#44836=CARTESIAN_POINT ( 'NONE',  ( 0.7782871991188352601, -1.104406889285912907, -1.750870654829151274 ) ) ;
#44837=CARTESIAN_POINT ( 'NONE',  ( 2.900141384978659698, -1.046112932010187624, -1.840686247649555796 ) ) ;
#44841=CARTESIAN_POINT ( 'NONE',  ( 6.860220180191213935, -2.069926439015772335, 0.04462916171246725239 ) ) ;
#44846=CARTESIAN_POINT ( 'NONE',  ( 3.222906779550426926, 0.05642716604136116532, 2.291727194984194860 ) ) ;
#44847=CARTESIAN_POINT ( 'NONE',  ( 0.6623940301842005107, -1.324425631624454036, 1.256838194884236204 ) ) ;
#44848=CARTESIAN_POINT ( 'NONE',  ( 3.480628297764537304, -1.280852673386581264, 1.420289963180096260 ) ) ;
#44852=CARTESIAN_POINT ( 'NONE',  ( 1.845949328209312901, -1.318067166357287379, -1.521789114188701664 ) ) ;
#44853=CARTESIAN_POINT ( 'NONE',  ( 2.201936455694650796, 0.7555380192853027310, -1.810630540845730385 ) ) ;
#44858=CARTESIAN_POINT ( 'NONE',  ( 5.437476023981094642, 0.8479630442611612029, -1.911130889300112878 ) ) ;
#44859=CARTESIAN_POINT ( 'NONE',  ( 3.186155166506371650, -1.743393047566743181, -0.3038327287053984027 ) ) ;
#44862=CARTESIAN_POINT ( 'NONE',  ( 5.912145817070847187, 1.543564834742835234, -1.694840376948128391 ) ) ;
#44863=CARTESIAN_POINT ( 'NONE',  ( 4.769343782054527026, 1.005586498893149772, 1.420189556619367410 ) ) ;
#44865=CARTESIAN_POINT ( 'NONE',  ( -0.1104750535120234134, 0.7027814200676918421, -2.185477693842474256 ) ) ;
#44866=CARTESIAN_POINT ( 'NONE',  ( 4.921093860428086941, 0.6645110682935355673, 1.601655696547391594 ) ) ;
#44867=CARTESIAN_POINT ( 'NONE',  ( 4.738842072872849087, -2.104903140973454434, -0.5318641579697135358 ) ) ;
#44870=CARTESIAN_POINT ( 'NONE',  ( 6.368375356916068597, -1.978549699825098429, -0.3886382054163611821 ) ) ;
#44871=CARTESIAN_POINT ( 'NONE',  ( 4.593750000000003553, -1.895863743164180493, -0.7852924748297412938 ) ) ;
#44873=CARTESIAN_POINT ( 'NONE',  ( 2.942313797947668785, 1.911627860423757097, 0.2376154225440275658 ) ) ;
#44875=CARTESIAN_POINT ( 'NONE',  ( 0.3467151180503316166, 1.136585144892443777, -1.908366640695156047 ) ) ;
#44877=CARTESIAN_POINT ( 'NONE',  ( -0.1409997244346088419, 5.722143553014046979, -2.594341442600463843 ) ) ;
#44880=CARTESIAN_POINT ( 'NONE',  ( 2.649351634902767483, 0.2746262237617850821, 2.204210978092531192 ) ) ;
#44886=CARTESIAN_POINT ( 'NONE',  ( 0.1588275700346117869, 1.163271727376416376, 1.646837250247008777 ) ) ;
#44888=CARTESIAN_POINT ( 'NONE',  ( 5.582507124453381486, 1.231422846540839666, -1.654610746699414214 ) ) ;
#44893=CARTESIAN_POINT ( 'NONE',  ( 0.3679306741783492929, -1.162814898748459225, 1.334192561405376676 ) ) ;
#44894=CARTESIAN_POINT ( 'NONE',  ( 5.537694164425770005, -1.361542515911953855, 1.073868356900798959 ) ) ;
#44895=CARTESIAN_POINT ( 'NONE',  ( 6.058121337783492599, -1.224224903413055010, 1.237393016278231617 ) ) ;
#44896=CARTESIAN_POINT ( 'NONE',  ( 2.507732108623667688, -2.266951094411073786, 0.3397945559272512739 ) ) ;
#44898=CARTESIAN_POINT ( 'NONE',  ( 2.642321604431462578, -1.530645349967133972, 1.022873098850234141 ) ) ;
#44900=CARTESIAN_POINT ( 'NONE',  ( 2.379681254797087586, 1.121034037677430595, 1.440765146680768272 ) ) ;
#44901=CARTESIAN_POINT ( 'NONE',  ( 2.250625165576759290, 1.976955744075848065, -0.3961026872240576702 ) ) ;
#44904=CARTESIAN_POINT ( 'NONE',  ( 4.295997052264050708, -0.8081792604435251715, 1.944918383092561376 ) ) ;
#44907=CARTESIAN_POINT ( 'NONE',  ( 1.996617168637443429, 2.047528291220417351, 0.3059219562495316125 ) ) ;
#44910=CARTESIAN_POINT ( 'NONE',  ( 5.110073233524446756, -0.7627883623938614965, 1.978724553277847464 ) ) ;
#44911=CARTESIAN_POINT ( 'NONE',  ( 6.393173274427864428, 1.585754722747900969, -0.9045919592586546543 ) ) ;
#44918=CARTESIAN_POINT ( 'NONE',  ( 6.082307721193076944, 1.091511717630256673, 1.817998432235830908 ) ) ;
#44919=CARTESIAN_POINT ( 'NONE',  ( 1.237491679122425969, -1.904027454836676014, 0.9001316648933003206 ) ) ;
#44922=CARTESIAN_POINT ( 'NONE',  ( 5.787920722453932854, -1.179413039982403433, -1.439513333959110852 ) ) ;
#44930=CARTESIAN_POINT ( 'NONE',  ( 2.523818479427087702, 1.924573107942130656, -0.3798230296482503210 ) ) ;
#44931=CARTESIAN_POINT ( 'NONE',  ( 1.217891636700708435, -2.108894920778502602, 0.4742063263511315796 ) ) ;
#44935=CARTESIAN_POINT ( 'NONE',  ( 2.776348759439921654, -1.715481723685903903, 0.2504971047874882117 ) ) ;
#44936=CARTESIAN_POINT ( 'NONE',  ( 2.747703163511563407, 0.5864964929944632699, 1.638654499222062189 ) ) ;
#44940=CARTESIAN_POINT ( 'NONE',  ( 1.950545848857932807, 1.388271641964162084, 1.462223312268404074 ) ) ;
#44943=CARTESIAN_POINT ( 'NONE',  ( 0.8132764231247009423, -0.2916495841569742842, 1.949667021961091429 ) ) ;
#44944=CARTESIAN_POINT ( 'NONE',  ( 6.258066496116281741, 0.7254575739856858885, -1.769658340881982816 ) ) ;
#44949=CARTESIAN_POINT ( 'NONE',  ( 1.506516584307997730, -2.010164795747824140, -0.1955670033209846170 ) ) ;
#44951=CARTESIAN_POINT ( 'NONE',  ( 4.419161195688524835, 2.107920515157933661, 0.9393535314214102039 ) ) ;
#44952=CARTESIAN_POINT ( 'NONE',  ( 6.373494408814909917, -0.2414686440028299685, 1.946897059556201848 ) ) ;
#44954=CARTESIAN_POINT ( 'NONE',  ( 3.414850490325722632, -1.488543670003231068, 1.277929504599809585 ) ) ;
#44958=CARTESIAN_POINT ( 'NONE',  ( 1.200578840252497947, 1.417437365323451104, -1.573097661806458936 ) ) ;
#44961=CARTESIAN_POINT ( 'NONE',  ( 1.482094074889642288, -0.2687121449159133313, -1.821302815977184686 ) ) ;
#44964=CARTESIAN_POINT ( 'NONE',  ( 3.375340920106313813, -1.871962376360849056, -0.9962781187466958066 ) ) ;
#44969=CARTESIAN_POINT ( 'NONE',  ( 3.708323652925065161, -0.8317495340520587588, -1.885651027073296904 ) ) ;
#44972=CARTESIAN_POINT ( 'NONE',  ( -0.04178991631376138827, -1.644041690304678616, -0.8291446804715857377 ) ) ;
#44976=CARTESIAN_POINT ( 'NONE',  ( 2.636292518416444075, 1.068738387235500298, -1.994089298797457666 ) ) ;
#44978=CARTESIAN_POINT ( 'NONE',  ( 2.830093135299842189, -0.8964878685940536052, -1.574152086365911529 ) ) ;
#44979=CARTESIAN_POINT ( 'NONE',  ( 2.852642732684606663, -1.771934378248109399, -0.7286688389312511172 ) ) ;
#44980=CARTESIAN_POINT ( 'NONE',  ( 4.229010956685672618, -1.930657356216297860, -0.7480826485904977785 ) ) ;
#44982=CARTESIAN_POINT ( 'NONE',  ( 2.096496217048297694, -0.5238668508756593178, -1.900535169118612755 ) ) ;
#44983=CARTESIAN_POINT ( 'NONE',  ( 6.252564000042572623, 0.6067452241035797833, 1.828529084590237774 ) ) ;
#44984=CARTESIAN_POINT ( 'NONE',  ( 2.904993682805886213, 1.579364189935757778, 1.002181356900035070 ) ) ;
#44985=CARTESIAN_POINT ( 'NONE',  ( 2.350585845863040646, 2.307203942772034111, 0.05475910514858049749 ) ) ;
#44987=CARTESIAN_POINT ( 'NONE',  ( 2.892830138475974255, 0.2247066616481566970, 1.847348555264594960 ) ) ;
#44989=CARTESIAN_POINT ( 'NONE',  ( 6.109847269609326226, 0.6021898890512421554, -1.972802226155190297 ) ) ;
#44993=CARTESIAN_POINT ( 'NONE',  ( 6.352575683687115671, 0.6571560004794211318, 2.000881423421707161 ) ) ;
#44995=CARTESIAN_POINT ( 'NONE',  ( 5.571600594950134600, 2.084881007647599205, -0.5705972643132786182 ) ) ;
#44996=CARTESIAN_POINT ( 'NONE',  ( 6.340491327343366734, 1.161156619345372842, -1.652315300818160582 ) ) ;
#44999=ADVANCED_FACE ( 'NONE', ( #56419 ), #41663, .F. ) ;
#45005=CARTESIAN_POINT ( 'NONE',  ( 4.786342355033275986, -0.6839347017603314427, -1.897111394664739326 ) ) ;
#45010=CARTESIAN_POINT ( 'NONE',  ( 5.752838164830007983, -1.706859214253673152, 1.326403591387192771 ) ) ;
#45015=CARTESIAN_POINT ( 'NONE',  ( 0.06975588353394339414, -0.9023057962903738849, 1.689756990376343859 ) ) ;
#45018=CARTESIAN_POINT ( 'NONE',  ( 2.261930500750704454, 0.7363377991795038158, 1.559957641100855330 ) ) ;
#45022=CARTESIAN_POINT ( 'NONE',  ( 0.9304724923206836307, 0.1222484634449630542, 1.765570801851876537 ) ) ;
#45023=CARTESIAN_POINT ( 'NONE',  ( 2.121741512283023656, -0.4388329339449773547, 1.964535544105987075 ) ) ;
#45025=CARTESIAN_POINT ( 'NONE',  ( 4.436686946050734548, 2.163524548302516060, 0.4339203326570104102 ) ) ;
#45026=CARTESIAN_POINT ( 'NONE',  ( 5.875877563635198975, -2.119900239643329964, 0.4680052475878637708 ) ) ;
#45030=CARTESIAN_POINT ( 'NONE',  ( 3.703867829435038228, 1.536975034498413439, 1.461131120854219700 ) ) ;
#45031=CARTESIAN_POINT ( 'NONE',  ( 2.759388848745081280, 1.913798524274639812, -0.6352183541234107667 ) ) ;
#45032=CARTESIAN_POINT ( 'NONE',  ( 2.865264419611464941, -1.483432276133073380, -1.039550242524535539 ) ) ;
#45037=CARTESIAN_POINT ( 'NONE',  ( 0.1275333129481092398, -1.147091320445620566, -1.478225367208672481 ) ) ;
#45039=CARTESIAN_POINT ( 'NONE',  ( 5.865807274569020180, 1.797851641234180509, -0.3166982042408575948 ) ) ;
#45041=CARTESIAN_POINT ( 'NONE',  ( 1.604551054648394537, 1.788909703809701712, 0.6859268596576766353 ) ) ;
#45048=CARTESIAN_POINT ( 'NONE',  ( 5.735289742212391850, -1.956171686333206816, 0.9202595734885756773 ) ) ;
#45051=CARTESIAN_POINT ( 'NONE',  ( 3.568700945156903614, 0.7666329941097769218, 1.977337035738421900 ) ) ;
#45052=FACE_OUTER_BOUND ( 'NONE', #205990, .T. ) ;
#45054=CARTESIAN_POINT ( 'NONE',  ( 4.639890180388304586, 0.8457560770286243201, -1.780867954887039417 ) ) ;
#45055=CARTESIAN_POINT ( 'NONE',  ( -0.1931356145602729502, -0.4479747710816587292, -1.970277229543435427 ) ) ;
#45057=CARTESIAN_POINT ( 'NONE',  ( 5.366459209908462036, -2.066393128712967098, -0.4610789482254721294 ) ) ;
#45059=EDGE_CURVE ( 'NONE', #39684, #124676, #89257, .T. ) ;
#45060=CARTESIAN_POINT ( 'NONE',  ( 0.7310241076574041097, -1.948878508384953356, -0.6990896207654460071 ) ) ;
#45061=CARTESIAN_POINT ( 'NONE',  ( 2.132666086734685162, -1.734545437858775463, 0.8733739462151270949 ) ) ;
#45062=EDGE_LOOP ( 'NONE', ( #48259, #139017, #66044, #104952 ) ) ;
#45065=CARTESIAN_POINT ( 'NONE',  ( 3.117214558520535306, -2.014654392230078805, 0.5582205872023697779 ) ) ;
#45068=CARTESIAN_POINT ( 'NONE',  ( 0.09988412287174981696, -0.8557525428138833545, 1.596560661436140283 ) ) ;
#45070=CARTESIAN_POINT ( 'NONE',  ( 6.094375512030342001, -2.195847865938059140, -0.2203403561373064590 ) ) ;
#45072=CARTESIAN_POINT ( 'NONE',  ( 2.819571115601596123, -0.2173934082839618365, 2.196046946737562511 ) ) ;
#45075=CARTESIAN_POINT ( 'NONE',  ( 1.857924044808876296, 0.7306008629870773818, -1.767408594711167735 ) ) ;
#45078=CARTESIAN_POINT ( 'NONE',  ( 5.406714943436663035, 0.5975561702324573288, 1.982271326387271770 ) ) ;
#45080=CARTESIAN_POINT ( 'NONE',  ( 2.729541802387557059, -2.017400560480298033, 0.7770373237434913261 ) ) ;
#45081=CARTESIAN_POINT ( 'NONE',  ( 4.739868811304373430, 2.185674081084403753, 0.1610935195608814985 ) ) ;
#45089=CARTESIAN_POINT ( 'NONE',  ( 0.7740648250077889481, 1.777010169924503558, -0.9530137779002674225 ) ) ;
#45093=CARTESIAN_POINT ( 'NONE',  ( 4.873920291170623642, -2.031351322358550870, 0.3986081187722507746 ) ) ;
#45094=CARTESIAN_POINT ( 'NONE',  ( 3.773980605468800320, 1.071039916736727937, 1.601146377209327731 ) ) ;
#45095=CARTESIAN_POINT ( 'NONE',  ( -0.08826282632121498772, -1.242921985031696153, -1.588411632956095110 ) ) ;
#45099=CARTESIAN_POINT ( 'NONE',  ( 3.625798818847306038, 1.922417080405220968, -0.4270903664440502956 ) ) ;
#45100=CARTESIAN_POINT ( 'NONE',  ( 0.5159075615763093481, -1.175655012515547160, -1.849222068403690411 ) ) ;
#45101=CARTESIAN_POINT ( 'NONE',  ( 3.668406916800326378, -1.225078373119498965, 1.353803248016254956 ) ) ;
#45107=CARTESIAN_POINT ( 'NONE',  ( 1.311775528174640604, 1.236260529797410301, -1.364685630449238740 ) ) ;
#45108=CARTESIAN_POINT ( 'NONE',  ( 5.642843092333371224, 1.941422931094261450, 0.5326616679640855390 ) ) ;
#45109=CARTESIAN_POINT ( 'NONE',  ( 0.7557052203445973060, -2.281327611594321958, -0.2792575881873406440 ) ) ;
#45110=CARTESIAN_POINT ( 'NONE',  ( 5.278158119090741174, -1.046208158741080529, -1.659298866772864534 ) ) ;
#45116=CARTESIAN_POINT ( 'NONE',  ( 0.9430502156211654219, -1.650385480578796749, -1.283440319295367615 ) ) ;
#45117=CARTESIAN_POINT ( 'NONE',  ( 6.473528777534793832, 1.692185636751794897, -0.5185713626470798143 ) ) ;
#45119=CARTESIAN_POINT ( 'NONE',  ( -0.2104748580754409182, 6.947232144882289795, -2.698723162346649662 ) ) ;
#45120=CARTESIAN_POINT ( 'NONE',  ( 1.522608870468153741, -1.638875412371978646, 0.5861679430564836757 ) ) ;
#45124=CARTESIAN_POINT ( 'NONE',  ( 1.769703478646069028, 0.8846387809394311574, 1.480598516496567152 ) ) ;
#45125=CARTESIAN_POINT ( 'NONE',  ( 1.540847765565691585, -1.849059859674206496, 1.176127931831471907 ) ) ;
#45126=CARTESIAN_POINT ( 'NONE',  ( 4.336686996305870068, 2.164023489887345164, 0.4319772483800735086 ) ) ;
#45128=CARTESIAN_POINT ( 'NONE',  ( 2.254941745292405653, -0.5755891407489240885, -2.093346358694737841 ) ) ;
#45129=CARTESIAN_POINT ( 'NONE',  ( 0.8205984872286451459, 1.685833220154912881, 0.7012733028506010768 ) ) ;
#45130=CARTESIAN_POINT ( 'NONE',  ( 3.169268314845040901, 1.912196763353574358, -0.9095376832224701946 ) ) ;
#45131=CARTESIAN_POINT ( 'NONE',  ( 6.539320575229256249, 6.039323383297771741, 2.391644441267444687 ) ) ;
#45133=CARTESIAN_POINT ( 'NONE',  ( 4.195090427499806651, 1.841111018879896477, 1.365591311898015192 ) ) ;
#45137=CARTESIAN_POINT ( 'NONE',  ( 6.094412736144367848, -1.190704872505081946, 1.875028197947399278 ) ) ;
#45143=CARTESIAN_POINT ( 'NONE',  ( 4.254529844270301453, 1.955172953530256219, -0.4926405443339901269 ) ) ;
#45145=CARTESIAN_POINT ( 'NONE',  ( 2.483324480268500611, -0.004404232681418790429, 2.062741127353195925 ) ) ;
#45150=CARTESIAN_POINT ( 'NONE',  ( 4.998067021457727854, -0.7363416341295281331, -2.064161796032103258 ) ) ;
#45151=CARTESIAN_POINT ( 'NONE',  ( 2.865861461037176205, -0.1511401116795624278, -2.010826411938296143 ) ) ;
#45152=CARTESIAN_POINT ( 'NONE',  ( 1.716098596715152746, 1.718394358364897068, 0.6617865747741287219 ) ) ;
#45154=CARTESIAN_POINT ( 'NONE',  ( 6.668987789458199700, -1.670617902683011025, -0.7365018021969899076 ) ) ;
#45155=CARTESIAN_POINT ( 'NONE',  ( 6.381482430641396419, -0.5404875331735843336, -1.942542459342583294 ) ) ;
#45157=CARTESIAN_POINT ( 'NONE',  ( 5.295900185863533061, -0.8195587353489269811, 2.109036902066116603 ) ) ;
#45159=CARTESIAN_POINT ( 'NONE',  ( 1.260533433194007236, 0.8550034467163977192, 1.924895685913818655 ) ) ;
#45170=CARTESIAN_POINT ( 'NONE',  ( 1.898838059644195386, -2.080654286433290867, -0.4088066060855889972 ) ) ;
#45171=CARTESIAN_POINT ( 'NONE',  ( 3.199698422319953384, 2.006668028495290024, -0.9531968752462171013 ) ) ;
#45175=CARTESIAN_POINT ( 'NONE',  ( 4.756279191188107269, -1.961398630904508833, -0.05015466537350299348 ) ) ;
#45182=CARTESIAN_POINT ( 'NONE',  ( 3.568700945156903614, 0.7666329941097769218, 1.977337035738421900 ) ) ;
#45184=CARTESIAN_POINT ( 'NONE',  ( 4.873979933848565871, 1.241796773192262116, 1.769252301715443565 ) ) ;
#45185=CARTESIAN_POINT ( 'NONE',  ( 4.440845869443198701, -1.426288408191313639, -1.164454570719307469 ) ) ;
#45188=CARTESIAN_POINT ( 'NONE',  ( 6.052664191884576717, -1.496297717267160765, -0.8884939375988825105 ) ) ;
#45191=STYLED_ITEM ( 'NONE', ( #57089 ), #162819 ) ;
#45193=CARTESIAN_POINT ( 'NONE',  ( 3.327187652246216931, 0.05129554954072869377, 2.161254785723889515 ) ) ;
#45194=CARTESIAN_POINT ( 'NONE',  ( 6.134138708105167481, 0.1511139231759016377, -2.010518800921741622 ) ) ;
#45196=CARTESIAN_POINT ( 'NONE',  ( 2.061604318190731533, 0.3698614785779800185, -2.129673623264888960 ) ) ;
#45197=CARTESIAN_POINT ( 'NONE',  ( 3.356668533229437923, -1.495150621271496671, 1.284956859879735402 ) ) ;
#45198=CARTESIAN_POINT ( 'NONE',  ( 2.887907956677421506, -2.014008092954455265, 0.1037802451031161477 ) ) ;
#45199=CARTESIAN_POINT ( 'NONE',  ( 0.1522426329377546128, 0.8445714516599597266, 2.022489037641273857 ) ) ;
#45200=CARTESIAN_POINT ( 'NONE',  ( 4.880387366230515944, -0.2415804104359954019, -1.926931144411721641 ) ) ;
#45208=CARTESIAN_POINT ( 'NONE',  ( 1.729795059504362076, -2.077734391967264838, 0.7439406459070623256 ) ) ;
#45210=CARTESIAN_POINT ( 'NONE',  ( 5.981297772519294398, -0.05168599705708888659, 1.961257141919122926 ) ) ;
#45215=CARTESIAN_POINT ( 'NONE',  ( 4.945164379994194448, 0.5744887182440976403, -1.749284230371531024 ) ) ;
#45220=CARTESIAN_POINT ( 'NONE',  ( 5.853796514643677007, -1.537196951383312804, -1.461068456062891041 ) ) ;
#45223=CARTESIAN_POINT ( 'NONE',  ( 6.186805567823734364, -0.2977626877682394424, -2.039013576910824632 ) ) ;
#45225=CARTESIAN_POINT ( 'NONE',  ( 1.855673809551155795, -0.6311025070286357952, 1.750906552266822569 ) ) ;
#45226=CARTESIAN_POINT ( 'NONE',  ( 3.245484093776138668, 1.841430844176932480, -0.003062914905635482320 ) ) ;
#45232=CARTESIAN_POINT ( 'NONE',  ( 3.299657469156279888, 1.739734091921738557, 1.357710657151039779 ) ) ;
#45233=CARTESIAN_POINT ( 'NONE',  ( 5.571622904855764169, 2.182566619097675797, -0.5956038432519733528 ) ) ;
#45235=CARTESIAN_POINT ( 'NONE',  ( 5.906502150075481516, -1.803732336900876421, -0.1683732622318224459 ) ) ;
#45236=CARTESIAN_POINT ( 'NONE',  ( 6.298046708350548251, -0.9096110389208410529, -1.686033347247811731 ) ) ;
#45237=CARTESIAN_POINT ( 'NONE',  ( 5.664887262500884368, -1.691755685069219695, -0.7986314380193232365 ) ) ;
#45238=CARTESIAN_POINT ( 'NONE',  ( 5.672493831469004100, 0.7790509395085333244, 1.746586765831580124 ) ) ;
#45240=CARTESIAN_POINT ( 'NONE',  ( 0.6021629784135495989, -0.6261829430146518272, -1.762877433595814614 ) ) ;
#45241=CARTESIAN_POINT ( 'NONE',  ( 1.253139057289072822, 0.1435168058863903473, -2.011451928166609893 ) ) ;
#45243=CARTESIAN_POINT ( 'NONE',  ( 4.424511703531566198, 1.296206220603330461, -1.659847191385990239 ) ) ;
#45248=CARTESIAN_POINT ( 'NONE',  ( 3.357680014348028763, -1.532128950806666445, -1.316242992507418386 ) ) ;
#45251=CARTESIAN_POINT ( 'NONE',  ( 3.444745247808535638, 0.5215555581963465803, 2.097624034931542703 ) ) ;
#45252=CARTESIAN_POINT ( 'NONE',  ( 6.620655732516659064, 6.039214117936750448, 2.421170424969817603 ) ) ;
#45256=CARTESIAN_POINT ( 'NONE',  ( 0.3444781036854955847, -1.022991162849467228, 1.915094836987745630 ) ) ;
#45260=CARTESIAN_POINT ( 'NONE',  ( 2.402122600552298870, -0.8417629408748151798, -2.023652355447076001 ) ) ;
#45261=CARTESIAN_POINT ( 'NONE',  ( 6.883263157960369583, 7.629137130509070275, 2.653810918356712900 ) ) ;
#45262=CARTESIAN_POINT ( 'NONE',  ( 3.063607368349754889, 0.3334396122402134011, -2.237705976790417939 ) ) ;
#45269=CARTESIAN_POINT ( 'NONE',  ( 4.569463179464338332, 1.716784003608927467, -0.4291735618162701438 ) ) ;
#45271=CARTESIAN_POINT ( 'NONE',  ( 0.8332068151313138937, 0.1548093300561304564, 2.100314307419436588 ) ) ;
#45274=CARTESIAN_POINT ( 'NONE',  ( 6.081657687927014777, -0.6766999560612970699, 1.899624756701682626 ) ) ;
#45277=CARTESIAN_POINT ( 'NONE',  ( 4.240975883383619305, -1.627667033997456381, 0.9218181776217827528 ) ) ;
#45278=CARTESIAN_POINT ( 'NONE',  ( 2.870052101067874339, -2.048368873657464118, 0.2992715783270774588 ) ) ;
#45285=CARTESIAN_POINT ( 'NONE',  ( 6.666866396406604167, -1.974176978123330040, -0.8811043787171415342 ) ) ;
#45287=CARTESIAN_POINT ( 'NONE',  ( 4.053139552913617827, 1.658577106941661272, -1.047563642765911185 ) ) ;
#45288=CARTESIAN_POINT ( 'NONE',  ( 0.8782795706883707032, -0.2985837142155840507, 1.993765709762222782 ) ) ;
#45292=CARTESIAN_POINT ( 'NONE',  ( 0.6494046996203367561, 0.5928216254872006319, -1.774177939146783345 ) ) ;
#45294=CARTESIAN_POINT ( 'NONE',  ( 3.269792347016476697, 0.4849277011088357070, -1.953833955329455696 ) ) ;
#45296=CARTESIAN_POINT ( 'NONE',  ( 2.425544100157220662, -1.571072031863307572, -1.419494070558358967 ) ) ;
#45298=EDGE_CURVE ( 'NONE', #35846, #106915, #44204, .T. ) ;
#45299=CARTESIAN_POINT ( 'NONE',  ( 3.437997351728830697, 1.311287738946330439, 1.602184970737066116 ) ) ;
#45301=CARTESIAN_POINT ( 'NONE',  ( 6.474567623737461197, -0.1010770918629246007, -2.088323083193554641 ) ) ;
#45303=CARTESIAN_POINT ( 'NONE',  ( 5.508770632382115728, 1.381118045931900573, -1.193960910464037850 ) ) ;
#45309=CARTESIAN_POINT ( 'NONE',  ( 5.965903178300209220, 2.175115270774199416, -0.3715683035191637562 ) ) ;
#45311=CARTESIAN_POINT ( 'NONE',  ( 4.582611755193141789, -1.246403352314252810, 1.450376384258989182 ) ) ;
#45328=CARTESIAN_POINT ( 'NONE',  ( 2.483201282919132336, -0.004963586128624993335, 1.969629312250702036 ) ) ;
#45329=CARTESIAN_POINT ( 'NONE',  ( 3.743767684670766371, 2.000855813463810140, -0.2496267151909299931 ) ) ;
#45332=CARTESIAN_POINT ( 'NONE',  ( 6.727182134110168299, 1.217656702865956397, 2.400974650093392171 ) ) ;
#45333=CARTESIAN_POINT ( 'NONE',  ( 3.890727776643727598, 1.851661642969665067, -1.171806376371389957 ) ) ;
#45335=CARTESIAN_POINT ( 'NONE',  ( 2.168856224914788466, -1.760356022852540114, -0.7827933968581005653 ) ) ;
#45337=CARTESIAN_POINT ( 'NONE',  ( -0.1296875068448125057, 2.889142263448498227, -2.315371602238533555 ) ) ;
#45338=CARTESIAN_POINT ( 'NONE',  ( 0.1333542156527295908, 5.722835866173135777, -2.639957043922738666 ) ) ;
#45345=CARTESIAN_POINT ( 'NONE',  ( 4.757273854911123756, 1.820453720981948242, -0.2752165127944474210 ) ) ;
#45346=CARTESIAN_POINT ( 'NONE',  ( 1.945949197151348509, -1.316483196816301549, -1.523026451717986784 ) ) ;
#45347=CARTESIAN_POINT ( 'NONE',  ( 3.866856096493505923, -0.6709599815711597692, 2.198256080205548635 ) ) ;
#45348=CARTESIAN_POINT ( 'NONE',  ( -0.1291982275798261026, 4.084732128465967449, -2.628654587324832814 ) ) ;
#45349=CARTESIAN_POINT ( 'NONE',  ( 2.395144146474707636, -1.664902989962243174, 0.8314883405181148213 ) ) ;
#45352=CARTESIAN_POINT ( 'NONE',  ( 5.291234991620994421, -0.05314252713351996088, -1.911838368980276925 ) ) ;
#45355=CARTESIAN_POINT ( 'NONE',  ( 4.441018442196864591, -1.617167385086373033, -1.325159661343593420 ) ) ;
#45356=CARTESIAN_POINT ( 'NONE',  ( 3.080767038946086611, -0.1360980058115155988, -1.865751385159146070 ) ) ;
#45361=CARTESIAN_POINT ( 'NONE',  ( 4.986778444009251743, -0.2158907008250054438, -1.711239743519934242 ) ) ;
#45363=CARTESIAN_POINT ( 'NONE',  ( 1.722904486866124962, 1.715286564835089456, 0.2538950934896730405 ) ) ;
#45368=CARTESIAN_POINT ( 'NONE',  ( 5.840740439281987051, -2.116473627201011620, -0.4831736825232531007 ) ) ;
#45369=CARTESIAN_POINT ( 'NONE',  ( 4.318856058802469811, 1.670182456744148336, 0.7377305746401884301 ) ) ;
#45370=CARTESIAN_POINT ( 'NONE',  ( 1.744895479173363517, -0.2825750800353257208, -1.941159045430330465 ) ) ;
#45371=CARTESIAN_POINT ( 'NONE',  ( 0.03496603831146075092, -1.697522432243668389, 1.265142316669096934 ) ) ;
#45376=CARTESIAN_POINT ( 'NONE',  ( 2.350376503035214615, 0.9972050307137376723, -1.871358364749615033 ) ) ;
#45381=CARTESIAN_POINT ( 'NONE',  ( 1.217730340897508645, 0.4076058164220326407, -2.029561569317724690 ) ) ;
#45384=CARTESIAN_POINT ( 'NONE',  ( 3.457896741714714395, -1.683011943829109791, -1.449823692882054482 ) ) ;
#45386=CARTESIAN_POINT ( 'NONE',  ( 0.7920821852162404086, 1.736045259359697335, -1.506783991232300446 ) ) ;
#45388=CARTESIAN_POINT ( 'NONE',  ( 5.383662037909134668, -1.960299721042932930, 0.6417261926762083402 ) ) ;
#45391=CARTESIAN_POINT ( 'NONE',  ( 0.2331563151865730654, 0.7315591717663977311, -2.029986209603263259 ) ) ;
#45392=CARTESIAN_POINT ( 'NONE',  ( 5.565905774130330386, -1.163279849954502287, 1.427249551226833502 ) ) ;
#45394=CARTESIAN_POINT ( 'NONE',  ( 2.924480221818404946, 1.623360404532696810, 0.5830473908832736196 ) ) ;
#45395=CARTESIAN_POINT ( 'NONE',  ( 0.8136858238772455287, -1.282993010278702606, -1.555696519147983459 ) ) ;
#45396=CARTESIAN_POINT ( 'NONE',  ( 2.620138118368781743, 0.2850873451692262361, 2.280912332010568644 ) ) ;
#45399=CARTESIAN_POINT ( 'NONE',  ( 2.741812758617673040, -1.674694146245614412, -1.521292302590461665 ) ) ;
#45400=CARTESIAN_POINT ( 'NONE',  ( 5.690091061058023314, -0.9480630415420692181, 1.880679904143019776 ) ) ;
#45402=CARTESIAN_POINT ( 'NONE',  ( 3.110363945789674123, 1.284354398739546266, -1.217803596734900573 ) ) ;
#45405=CARTESIAN_POINT ( 'NONE',  ( 0.1820931442207155415, -1.074843934555272273, 2.024655709774853207 ) ) ;
#45406=CARTESIAN_POINT ( 'NONE',  ( 4.365079047384805122, 1.785254547683400306, -0.4496667978745386152 ) ) ;
#45410=CARTESIAN_POINT ( 'NONE',  ( 5.138714532536901913, -1.880766731008373993, 1.124575086929799239 ) ) ;
#45416=CARTESIAN_POINT ( 'NONE',  ( 3.369672229528171581, 1.879407295867494554, -0.4226879870903621494 ) ) ;
#45419=CARTESIAN_POINT ( 'NONE',  ( 0.4928134435002875513, -1.227493105415909946, 1.851297100075269153 ) ) ;
#45427=CARTESIAN_POINT ( 'NONE',  ( 2.647703282711162398, 0.5884205719196273776, 1.638072370343154116 ) ) ;
#45429=CARTESIAN_POINT ( 'NONE',  ( 0.7132427667453158371, -1.655377960257615966, -1.052639099659122390 ) ) ;
#45432=CARTESIAN_POINT ( 'NONE',  ( 5.998930166150279852, 1.769978137569449883, -1.240765152474863520 ) ) ;
#45436=CARTESIAN_POINT ( 'NONE',  ( 5.243122039519461097, -1.856066598825537373, 1.107904190987746063 ) ) ;
#45437=CARTESIAN_POINT ( 'NONE',  ( -0.2104748580754201015, 7.629137130509078268, -2.703678718140526627 ) ) ;
#45440=CARTESIAN_POINT ( 'NONE',  ( 6.907508285686359883, -0.4377196890756588910, 1.929438547640258017 ) ) ;
#45441=CARTESIAN_POINT ( 'NONE',  ( 5.764916378462246804, -1.734034293797588999, 0.002837784182162239165 ) ) ;
#45443=CARTESIAN_POINT ( 'NONE',  ( 3.070069520051089906, -1.303570237086741024, 1.761582097007891923 ) ) ;
#45444=CARTESIAN_POINT ( 'NONE',  ( 3.013035845080668906, 1.672340031372629321, -1.590277441748239040 ) ) ;
#45445=CARTESIAN_POINT ( 'NONE',  ( 6.274695623702050362, -1.955332461540583600, -0.6509123137334557052 ) ) ;
#45446=CARTESIAN_POINT ( 'NONE',  ( 0.8142755762143333298, 1.794035260217427874, 0.7438321904150380082 ) ) ;
#45449=CARTESIAN_POINT ( 'NONE',  ( 4.236665939827915395, 1.302216991916404387, -1.673619383358643908 ) ) ;
#45451=CARTESIAN_POINT ( 'NONE',  ( 2.338517726396415863, 0.5350873343827439177, -1.944071628254496087 ) ) ;
#45453=CARTESIAN_POINT ( 'NONE',  ( 5.526482418920476647, 1.318621124876094397, -1.769340128416618363 ) ) ;
#45459=CARTESIAN_POINT ( 'NONE',  ( 6.825078400183572036, 7.051914997414900022, 2.742498282622223726 ) ) ;
#45461=CARTESIAN_POINT ( 'NONE',  ( 4.979397702276197712, 1.923710689106904015, -0.7398180773239333430 ) ) ;
#45463=CARTESIAN_POINT ( 'NONE',  ( 6.983263157960366563, -0.003091553303710344557, 1.945923119799706669 ) ) ;
#45466=CARTESIAN_POINT ( 'NONE',  ( 4.143226661672769318, 0.1011831993794048007, 2.017277399227022094 ) ) ;
#45472=CARTESIAN_POINT ( 'NONE',  ( 2.729428266803469061, -1.923432490405907247, 0.7405405203823824944 ) ) ;
#45473=CARTESIAN_POINT ( 'NONE',  ( 2.654922836763852878, 1.081066371885472277, 1.701947380796410059 ) ) ;
#45480=CARTESIAN_POINT ( 'NONE',  ( 2.618517346670693247, 0.5404096030681636575, -1.942243668081746311 ) ) ;
#45481=CARTESIAN_POINT ( 'NONE',  ( 1.886409237429786279, 1.602333580200336671, -0.9066872629178088783 ) ) ;
#45483=CARTESIAN_POINT ( 'NONE',  ( 0.4347317753056179623, 1.181035649988096958, -1.982462206444644437 ) ) ;
#45485=CARTESIAN_POINT ( 'NONE',  ( 2.425270691926324051, -0.002641788883844811090, 2.161773191836775521 ) ) ;
#45490=CARTESIAN_POINT ( 'NONE',  ( 0.9185735243398345240, 1.726912363944958617, 0.7195956246372691156 ) ) ;
#45491=CARTESIAN_POINT ( 'NONE',  ( 5.190288350601474754, -1.956472792631309909, -0.2422539641438857527 ) ) ;
#45496=CARTESIAN_POINT ( 'NONE',  ( 0.6806489137391663613, -1.222764829241920648, 1.836970590647703627 ) ) ;
#45497=CARTESIAN_POINT ( 'NONE',  ( 6.127406499145813257, 0.1562011534181114436, -2.064545280851529885 ) ) ;
#45500=CARTESIAN_POINT ( 'NONE',  ( 6.539320575229294441, -0.001643797937642132567, 2.203502507913539521 ) ) ;
#45501=CARTESIAN_POINT ( 'NONE',  ( 4.469576204829595945, 1.912561584401346604, -0.4778803491252373026 ) ) ;
#45502=CARTESIAN_POINT ( 'NONE',  ( 6.521752737896459706, -0.4354215942184087584, 1.979412122172687694 ) ) ;
#45504=CARTESIAN_POINT ( 'NONE',  ( 4.864078691051298975, 2.283152030527708209, -0.3349727840419229330 ) ) ;
#45505=CARTESIAN_POINT ( 'NONE',  ( 1.446217529737943153, -0.9311174319141333200, 1.840543939966767351 ) ) ;
#45512=CARTESIAN_POINT ( 'NONE',  ( 4.387298408599741961, 0.1025060220480543544, 2.168864852262440301 ) ) ;
#45515=CARTESIAN_POINT ( 'NONE',  ( 3.772867777003403589, 1.732451475078290448, -0.6238847238279123797 ) ) ;
#45517=CARTESIAN_POINT ( 'NONE',  ( 6.620655732516666170, 7.629137130509104026, 2.326260288887294969 ) ) ;
#45518=CARTESIAN_POINT ( 'NONE',  ( 5.495707582769355781, -2.191739722525353429, -0.0009102486706394352645 ) ) ;
#45520=CARTESIAN_POINT ( 'NONE',  ( 5.454102184832422928, 2.260192964246518166, -0.1051519175162188013 ) ) ;
#45526=CARTESIAN_POINT ( 'NONE',  ( 1.041466456679561059, 0.7221788661597589032, -1.615996624379830493 ) ) ;
#45528=CARTESIAN_POINT ( 'NONE',  ( 4.828775420069912450, 1.386532772215205878, -1.459704157296830784 ) ) ;
#45530=CARTESIAN_POINT ( 'NONE',  ( 4.594815077023072902, -0.4589311638903668111, -2.055181093106945855 ) ) ;
#45531=CARTESIAN_POINT ( 'NONE',  ( 2.144012975658988740, 0.8210224433658172005, 1.730898686554068311 ) ) ;
#45534=CARTESIAN_POINT ( 'NONE',  ( 2.769919614283973264, -1.948520106842245525, 0.2860871629452500509 ) ) ;
#45535=CARTESIAN_POINT ( 'NONE',  ( 5.115492516475182327, 1.653579564094692866, 1.159561630411933830 ) ) ;
#45536=CARTESIAN_POINT ( 'NONE',  ( 1.727212824277712944, -1.762453432929488528, 0.6273722324065673650 ) ) ;
#45537=CARTESIAN_POINT ( 'NONE',  ( 5.637229722410256549, -1.556708995667484441, 0.7431856355405024317 ) ) ;
#45538=CARTESIAN_POINT ( 'NONE',  ( 0.9668906521006037647, -1.505869814250645478, 1.178657042999963878 ) ) ;
#45540=CARTESIAN_POINT ( 'NONE',  ( 0.9442952520863318044, 0.8911936224933308948, -2.019119535841918278 ) ) ;
#45549=CARTESIAN_POINT ( 'NONE',  ( 0.8892259839063383353, 0.1505779921940515187, 2.064926437897919964 ) ) ;
#45554=CARTESIAN_POINT ( 'NONE',  ( -0.005205762187880831615, -1.959593580757122089, -0.4885912094437401820 ) ) ;
#45558=CARTESIAN_POINT ( 'NONE',  ( 6.830524215763060347, -1.208013408316032322, 1.546442907991877558 ) ) ;
#45560=CARTESIAN_POINT ( 'NONE',  ( 4.341172599035714619, -1.163090190446917083, 1.646587424817484324 ) ) ;
#45561=CARTESIAN_POINT ( 'NONE',  ( 4.241352010100610137, 0.4139369872660918492, -1.870304626840668893 ) ) ;
#45562=CARTESIAN_POINT ( 'NONE',  ( 3.193114300108112147, 1.729001323093733111, 1.346577201094656395 ) ) ;
#45564=CARTESIAN_POINT ( 'NONE',  ( 4.904545999335794271, -1.998481532559828189, -0.2423253454618880809 ) ) ;
#45567=CARTESIAN_POINT ( 'NONE',  ( 5.554358401905552967, -1.342484540487314026, 1.637217851860258699 ) ) ;
#45569=EDGE_CURVE ( 'NONE', #90194, #205352, #80974, .T. ) ;
#45570=CARTESIAN_POINT ( 'NONE',  ( 3.931257944464498166, -1.443263031577642463, -1.512909484191153897 ) ) ;
#45572=CARTESIAN_POINT ( 'NONE',  ( 2.256509660847346943, -1.335373073873729943, 1.091610183656815503 ) ) ;
#45574=CARTESIAN_POINT ( 'NONE',  ( 4.799148092389167175, -0.2621723519393297508, -2.104289960152181393 ) ) ;
#45583=CARTESIAN_POINT ( 'NONE',  ( 1.822642882514250218, 1.341887823972046201, -1.217030898042359643 ) ) ;
#45589=CARTESIAN_POINT ( 'NONE',  ( 2.578518618993036693, -1.248033014721174228, 1.313194663545588003 ) ) ;
#45590=CARTESIAN_POINT ( 'NONE',  ( 6.639320575229274546, 6.037277963978410433, 2.591643891269063360 ) ) ;
#45593=CARTESIAN_POINT ( 'NONE',  ( 3.789374314311170000, -1.720299746930791684, 0.7104884466354021155 ) ) ;
#45595=CARTESIAN_POINT ( 'NONE',  ( 2.056118223505171372, -1.176884799952466087, 1.511379468370318113 ) ) ;
#45596=CARTESIAN_POINT ( 'NONE',  ( 0.3053143536290473525, -0.4923201697357786344, 1.757875871163572024 ) ) ;
#45602=CARTESIAN_POINT ( 'NONE',  ( 5.893399327195629311, -1.782088370946652622, 0.8386133760364660183 ) ) ;
#45605=CARTESIAN_POINT ( 'NONE',  ( 6.685463922536254877, -0.9407050535897142352, 1.977304495687677521 ) ) ;
#45607=CARTESIAN_POINT ( 'NONE',  ( 4.858382476810707118, 0.7369543258428765675, 1.780043821814878413 ) ) ;
#45610=CARTESIAN_POINT ( 'NONE',  ( 1.729251940891060713, -1.720190037149814444, 0.6116943438041824166 ) ) ;
#45611=CARTESIAN_POINT ( 'NONE',  ( 2.086817400036289794, -2.164668306305051804, -0.4287355390964405211 ) ) ;
#45613=CARTESIAN_POINT ( 'NONE',  ( 0.4219365929402639215, -1.902980170924161385, 0.1897552588234762416 ) ) ;
#45614=CARTESIAN_POINT ( 'NONE',  ( 0.3616804892651844239, -0.5289564462071428830, 1.897103703902315530 ) ) ;
#45615=CARTESIAN_POINT ( 'NONE',  ( 2.524863302051027159, -1.811236869417539141, 0.7011504990855742525 ) ) ;
#45617=CARTESIAN_POINT ( 'NONE',  ( 0.6849224457974397717, -1.076149790962807495, -1.704679027301945649 ) ) ;
#45619=CARTESIAN_POINT ( 'NONE',  ( 5.418752549068918789, -1.349321427123598038, 1.281850857350794959 ) ) ;
#45625=CARTESIAN_POINT ( 'NONE',  ( 0.9959476074029065540, -2.191739723303194332, 0.005169097091584088505 ) ) ;
#45629=CARTESIAN_POINT ( 'NONE',  ( 3.228933428962964758, 0.04559371896543929631, 1.825288036790246204 ) ) ;
#45635=CARTESIAN_POINT ( 'NONE',  ( 1.031717895469780988, -1.221320771479022627, -1.489887157414800267 ) ) ;
#45636=CARTESIAN_POINT ( 'NONE',  ( 5.049637047142223167, 1.450995767963231264, 1.320413740667214508 ) ) ;
#45641=CARTESIAN_POINT ( 'NONE',  ( 5.091441847573507928, -0.7891374179831472935, 2.044738775321436997 ) ) ;
#45643=CARTESIAN_POINT ( 'NONE',  ( 4.118080132427735407, 2.055207691244304691, -0.2483996215696740451 ) ) ;
#45647=CARTESIAN_POINT ( 'NONE',  ( 3.885566394551481562, -0.7213347477983514944, -2.182621754721993490 ) ) ;
#45652=CARTESIAN_POINT ( 'NONE',  ( 6.620655732516649294, 4.698502813744664941, 2.488957606609870421 ) ) ;
#45654=CARTESIAN_POINT ( 'NONE',  ( 4.259667731375265554, 0.9167342216760937523, 1.711951518900257430 ) ) ;
#45658=CARTESIAN_POINT ( 'NONE',  ( 4.799029005866479736, -0.2398712174674077491, -1.897248949554980024 ) ) ;
#45660=CARTESIAN_POINT ( 'NONE',  ( 6.405283072077849305, 1.437190941405818156, 0.9532465752533066938 ) ) ;
#45661=CARTESIAN_POINT ( 'NONE',  ( 4.311732611912100666, -1.244383703160652610, -1.586670621409623116 ) ) ;
#45662=( BOUNDED_CURVE ( )  B_SPLINE_CURVE ( 3, ( #165969, #177966, #211503, #63140 ),
 .UNSPECIFIED., .F., .T. ) 
 B_SPLINE_CURVE_WITH_KNOTS ( ( 4, 4 ),
 ( 0.5000000000000006661, 1.000000000000000000 ),
 .UNSPECIFIED. ) 
 CURVE ( )  GEOMETRIC_REPRESENTATION_ITEM ( )  RATIONAL_B_SPLINE_CURVE ( ( 0.9999999999999991118, 0.3333333333333333703, 0.3333333333333342585, 1.000000000000000000 ) ) 
 REPRESENTATION_ITEM ( '' )  );
#45664=CARTESIAN_POINT ( 'NONE',  ( 1.682535984017709874, -1.178549783888741320, 1.865657194899547733 ) ) ;
#45667=CARTESIAN_POINT ( 'NONE',  ( 1.552797837233742095, -1.793874147449931344, -1.073420256486889324 ) ) ;
#45668=CARTESIAN_POINT ( 'NONE',  ( 6.819637456808122167, -1.715783256332433115, 0.4333192982870024967 ) ) ;
#45669=CARTESIAN_POINT ( 'NONE',  ( 5.590470263882489910, -0.4872053753022275169, 1.956560708789633285 ) ) ;
#45671=CARTESIAN_POINT ( 'NONE',  ( 3.012002838297692886, -1.130384021687063534, -1.994099915080405294 ) ) ;
#45673=CARTESIAN_POINT ( 'NONE',  ( 1.112787002727889885, -1.698604791339110465, 0.3779700589620417217 ) ) ;
#45675=CARTESIAN_POINT ( 'NONE',  ( 0.7195771044254402060, -1.460395948178545344, -0.9342476737749583204 ) ) ;
#45678=CARTESIAN_POINT ( 'NONE',  ( 1.662788154211870983, -0.7805772603099859763, -2.026187018951190133 ) ) ;
#45679=CARTESIAN_POINT ( 'NONE',  ( 2.307827663788959871, -1.164988201124015577, -1.645758576239789051 ) ) ;
#45680=CARTESIAN_POINT ( 'NONE',  ( 4.531250000000003553, -0.7852924748302230196, -1.895863743163982429 ) ) ;
#45683=CARTESIAN_POINT ( 'NONE',  ( 6.322878010905701451, 1.798576545740763644, 0.6907619847127777213 ) ) ;
#45685=CARTESIAN_POINT ( 'NONE',  ( 3.164521688127000854, 2.221583673635919354, -0.003682443279265367429 ) ) ;
#45693=CARTESIAN_POINT ( 'NONE',  ( 5.917484386527373630, -0.9743193633129590969, -1.441955756940280997 ) ) ;
#45694=CARTESIAN_POINT ( 'NONE',  ( 3.525789274851616639, 1.914599547803575330, -0.4273510147508317036 ) ) ;
#45698=CARTESIAN_POINT ( 'NONE',  ( 5.044316441076016844, 2.255832582719615065, 0.1735265121041371095 ) ) ;
#45699=CARTESIAN_POINT ( 'NONE',  ( 2.137244103193221889, -0.09901990427806567352, -2.060404765751827405 ) ) ;
#45703=CARTESIAN_POINT ( 'NONE',  ( 3.585083614955933307, 1.692364770286663322, -0.7970176776704935850 ) ) ;
#45704=CARTESIAN_POINT ( 'NONE',  ( 2.478840559695635548, -1.729657056378102853, -0.1252908626025364403 ) ) ;
#45705=CARTESIAN_POINT ( 'NONE',  ( 6.269083535738129598, 2.097726667780253074, -0.6343229546324488100 ) ) ;
#45706=CARTESIAN_POINT ( 'NONE',  ( 6.159233218726320125, -1.974841252017808468, -1.193533401095113300 ) ) ;
#45707=CARTESIAN_POINT ( 'NONE',  ( 3.836934241894359054, 0.3148432204054998351, 2.138525872868973998 ) ) ;
#45708=CARTESIAN_POINT ( 'NONE',  ( 4.277243253991915850, 1.269349932698702110, 1.469746654517690487 ) ) ;
#45711=CARTESIAN_POINT ( 'NONE',  ( 6.520764494017629254, 1.745421825204738431, 0.6730592012400560264 ) ) ;
#45715=CARTESIAN_POINT ( 'NONE',  ( 0.01804983835817890528, -0.5593552815991027494, 2.045460531183339814 ) ) ;
#45717=CARTESIAN_POINT ( 'NONE',  ( 5.695935454815424848, 1.779625283580280382, 0.9480427965274510482 ) ) ;
#45721=CARTESIAN_POINT ( 'NONE',  ( 3.703562413045482060, -0.5285312144065814621, 1.747510042522756990 ) ) ;
#45722=CARTESIAN_POINT ( 'NONE',  ( 2.011028756337205348, 1.635159560789069655, -1.482119803565529859 ) ) ;
#45727=CARTESIAN_POINT ( 'NONE',  ( 0.4748752182902976071, -1.459934291025711373, 1.395986992609834276 ) ) ;
#45728=CARTESIAN_POINT ( 'NONE',  ( 1.629697543846151619, -0.2563088357964183883, 2.104862515383609800 ) ) ;
#45731=CARTESIAN_POINT ( 'NONE',  ( 2.131498006616658891, 1.782543213153169548, -0.5345681993311669489 ) ) ;
#45734=CARTESIAN_POINT ( 'NONE',  ( 5.911025222378588850, 1.816451602635826612, 0.9735456368637726010 ) ) ;
#45735=CARTESIAN_POINT ( 'NONE',  ( 6.152970239395502361, 1.038990588714868490, 1.728003889287746286 ) ) ;
#45738=CARTESIAN_POINT ( 'NONE',  ( 3.439906511156048285, 0.8199118703316324863, -1.631291955839441865 ) ) ;
#45743=CARTESIAN_POINT ( 'NONE',  ( 6.556017512941495262, 1.755498886817616677, -0.9912500394320120645 ) ) ;
#45744=CARTESIAN_POINT ( 'NONE',  ( 5.349485151062911115, 1.838858031828109363, -0.09410559872920226665 ) ) ;
#45745=CARTESIAN_POINT ( 'NONE',  ( 0.07680821025391955381, 1.395885924038504644, -2.068540888291516833 ) ) ;
#45746=CARTESIAN_POINT ( 'NONE',  ( 4.178580530314169650, -1.330465218273884087, 1.885386248989364466 ) ) ;
#45748=CARTESIAN_POINT ( 'NONE',  ( 5.975883356200852425, 1.282301362320131588, 1.740048508431484953 ) ) ;
#45749=CARTESIAN_POINT ( 'NONE',  ( 1.487729058832359952, -1.932848847819462756, -0.1887428500492206451 ) ) ;
#45751=CARTESIAN_POINT ( 'NONE',  ( 5.097139630348237027, 1.187786601409031695, -1.967583100176452549 ) ) ;
#45754=CARTESIAN_POINT ( 'NONE',  ( 4.311305935566238645, -0.3199438451688824125, 1.842931056080451935 ) ) ;
#45756=CARTESIAN_POINT ( 'NONE',  ( 1.968876373762207255, -1.476028252698018628, 1.215921256797661609 ) ) ;
#45760=CARTESIAN_POINT ( 'NONE',  ( 4.178501018151202118, -1.271701901513167421, 1.803451139310302986 ) ) ;
#45761=CARTESIAN_POINT ( 'NONE',  ( 6.883263157960393563, 4.695771316066229772, 2.508818740863460572 ) ) ;
#45766=CARTESIAN_POINT ( 'NONE',  ( 1.915242260480106706, -0.2453889982298693984, 1.955985308386765542 ) ) ;
#45767=ADVANCED_FACE ( 'NONE', ( #86415 ), #152482, .T. ) ;
#45768=CARTESIAN_POINT ( 'NONE',  ( 1.396046310939329738, 1.748920304266964543, 1.505474166573782968 ) ) ;
#45769=CARTESIAN_POINT ( 'NONE',  ( 2.277722772326017608, -1.903703133612335119, 0.4737097981617058862 ) ) ;
#45771=CARTESIAN_POINT ( 'NONE',  ( 4.786014635464308498, -1.264713950826271027, -1.629283840103493253 ) ) ;
#45778=CARTESIAN_POINT ( 'NONE',  ( 1.006951398661716901, 0.6282198290366995952, 2.078224816918782025 ) ) ;
#45783=CARTESIAN_POINT ( 'NONE',  ( 2.372138566722302500, -1.154253592077842727, 1.471842878544211031 ) ) ;
#45784=CARTESIAN_POINT ( 'NONE',  ( 6.802040682177005415, -2.161276877365316818, 0.04550429416337595928 ) ) ;
#45786=CARTESIAN_POINT ( 'NONE',  ( 6.827182134110177714, 4.703275060517408512, 2.273677308227497917 ) ) ;
#45788=CARTESIAN_POINT ( 'NONE',  ( 2.209489775926488431, 1.479274643242427301, 1.211860329591994745 ) ) ;
#45789=CARTESIAN_POINT ( 'NONE',  ( 3.906921071489596997, 1.517988030950194744, 0.9097272527330434455 ) ) ;
#45790=CARTESIAN_POINT ( 'NONE',  ( 2.016128127738999076, -1.911839501640894001, 0.04842977492004740814 ) ) ;
#45792=CARTESIAN_POINT ( 'NONE',  ( 5.817977454128726578, 0.9396041113334742123, -1.669243033268079879 ) ) ;
#45794=CARTESIAN_POINT ( 'NONE',  ( 6.443809999611881167, 1.357174585993505378, 1.427557633841854967 ) ) ;
#45797=CARTESIAN_POINT ( 'NONE',  ( 5.067206508511894469, 0.1826785619755930679, -1.861722072867748823 ) ) ;
#45798=CARTESIAN_POINT ( 'NONE',  ( 1.383131112650197281, 1.687622997524572677, -0.6969523973551354779 ) ) ;
#45800=CARTESIAN_POINT ( 'NONE',  ( 4.740968412965463230, 0.3751893352213676591, 2.174603215771487630 ) ) ;
#45803=CARTESIAN_POINT ( 'NONE',  ( 2.260285141513069362, -2.062262451202213853, 0.04833688706953364472 ) ) ;
#45808=CARTESIAN_POINT ( 'NONE',  ( 0.07479286986305289098, 7.629137130509083597, -2.455503679634088776 ) ) ;
#45811=CARTESIAN_POINT ( 'NONE',  ( 5.055165704564410944, 1.723227314588217318, -1.147259442322377865 ) ) ;
#45813=CARTESIAN_POINT ( 'NONE',  ( 3.022914066069124051, 2.034213141994867247, 0.7313807043239917149 ) ) ;
#45815=CARTESIAN_POINT ( 'NONE',  ( 3.457679895445249674, -1.530724978927421986, -1.317682070945853656 ) ) ;
#45821=CARTESIAN_POINT ( 'NONE',  ( 1.850796360583713884, -1.845628094615419768, -0.8128149310912060610 ) ) ;
#45822=CARTESIAN_POINT ( 'NONE',  ( 5.794512526436308875, 1.792401445336734733, -1.260760892635464980 ) ) ;
#45824=CARTESIAN_POINT ( 'NONE',  ( 4.570513122935188299, 0.7371126809179430195, 1.764830652192488580 ) ) ;
#45828=CARTESIAN_POINT ( 'NONE',  ( 3.778922869151004171, 1.701937167235707982, -1.081084515101193633 ) ) ;
#45831=CARTESIAN_POINT ( 'NONE',  ( 5.508750344372229435, 1.303470515519134842, -1.129639352617429537 ) ) ;
#45832=CARTESIAN_POINT ( 'NONE',  ( -0.1399997263889819765, 0.7174702203470960660, -2.082715917450683740 ) ) ;
#45837=CARTESIAN_POINT ( 'NONE',  ( 0.5146170122050791607, 0.7890519337857507809, 1.914186188738425942 ) ) ;
#45839=CARTESIAN_POINT ( 'NONE',  ( 6.812946544903684121, -1.603000239855886466, 1.309962327488790157 ) ) ;
#45841=CARTESIAN_POINT ( 'NONE',  ( 4.863805359840983833, 0.5633507197577434233, -1.721726771216978369 ) ) ;
#45845=CARTESIAN_POINT ( 'NONE',  ( 6.375650462676996533, 0.3020505593925585375, -1.785944618546008833 ) ) ;
#45848=CARTESIAN_POINT ( 'NONE',  ( 2.519692321801832335, -1.262790281060278907, -1.790845962237663791 ) ) ;
#45850=CARTESIAN_POINT ( 'NONE',  ( 0.7835587076311965049, -1.864072139945194717, 0.6119401183290391621 ) ) ;
#45852=CARTESIAN_POINT ( 'NONE',  ( 4.481992950489037675, -1.915292616430896544, -0.04288535553729002497 ) ) ;
#45855=CARTESIAN_POINT ( 'NONE',  ( -0.07968760456310633455, 7.629137130509075604, -2.426417496045676803 ) ) ;
#45860=CARTESIAN_POINT ( 'NONE',  ( 1.850665834824256173, 0.6780317805383448970, 2.052694239800388676 ) ) ;
#45863=CARTESIAN_POINT ( 'NONE',  ( 1.957752326685862077, 1.820926393389955988, -0.1310869387763091420 ) ) ;
#45864=CARTESIAN_POINT ( 'NONE',  ( -0.01710467543277957581, -1.380256469788909035, 1.610041658517608054 ) ) ;
#45865=CARTESIAN_POINT ( 'NONE',  ( 4.823181420811452291, -0.08861582515604787824, 1.823562061424352621 ) ) ;
#45868=CARTESIAN_POINT ( 'NONE',  ( 3.385164793666879834, 0.04568167736355076974, 1.969186301724828336 ) ) ;
#45870=CARTESIAN_POINT ( 'NONE',  ( 5.952673665805181535, -1.667821083538678861, -0.9947414763863350329 ) ) ;
#45874=CARTESIAN_POINT ( 'NONE',  ( 5.748313822965784858, 1.043546352714582071, -1.845953426139717246 ) ) ;
#45876=CARTESIAN_POINT ( 'NONE',  ( 2.947808941170467545, -1.285945688040548207, -1.415481726668985196 ) ) ;
#45882=CARTESIAN_POINT ( 'NONE',  ( 4.776043607066285723, 1.990852085817075068, -0.2977186459587366496 ) ) ;
#45884=CARTESIAN_POINT ( 'NONE',  ( 6.111906964637446649, -1.811269838261083232, 0.2284818145076653595 ) ) ;
#45885=CARTESIAN_POINT ( 'NONE',  ( 1.188034388246852480, -1.312013912954514971, -1.601590607232979524 ) ) ;
#45889=CARTESIAN_POINT ( 'NONE',  ( 6.403191318657627029, 1.556466930477506505, 1.037356966126230517 ) ) ;
#45897=CARTESIAN_POINT ( 'NONE',  ( 3.252318870217449920, 1.690988760736945373, -0.3835568649490900817 ) ) ;
#45901=CARTESIAN_POINT ( 'NONE',  ( 1.745070579777140418, -0.2997347613497360896, -2.048299739058518920 ) ) ;
#45902=CARTESIAN_POINT ( 'NONE',  ( 1.933370326505511105, -1.702675829696152388, -1.258230627273223545 ) ) ;
#45906=CARTESIAN_POINT ( 'NONE',  ( 1.024188300031657617, 0.9657954515097492143, 1.716266578800438536 ) ) ;
#45911=CARTESIAN_POINT ( 'NONE',  ( 2.853816628688166990, 2.281129249179119078, -0.2256723309681916978 ) ) ;
#45912=CARTESIAN_POINT ( 'NONE',  ( 1.189776066567624691, -0.8228614858879386151, 1.629801898503015156 ) ) ;
#45913=CARTESIAN_POINT ( 'NONE',  ( 3.586107075002854305, 1.066394011600999780, 1.587261316105821551 ) ) ;
#45917=CARTESIAN_POINT ( 'NONE',  ( 2.302991897352596684, -0.3483681713834784199, -1.982697776695659053 ) ) ;
#45918=CARTESIAN_POINT ( 'NONE',  ( 1.621847549879053885, 1.933622029546874010, -0.3300716771732490895 ) ) ;
#45922=CARTESIAN_POINT ( 'NONE',  ( 5.068349447220681370, -1.968310418947304408, -0.7050240649949056637 ) ) ;
#45923=CARTESIAN_POINT ( 'NONE',  ( 3.854177328971124084, 0.6370089842938561064, 1.651420920916975232 ) ) ;
#45925=( LENGTH_UNIT ( ) NAMED_UNIT ( * ) SI_UNIT ( .MILLI., .METRE. ) );
#45926=CARTESIAN_POINT ( 'NONE',  ( 0.07648947921621782053, -2.126777779243053779, -0.5280787695999613618 ) ) ;
#45927=CARTESIAN_POINT ( 'NONE',  ( 4.892389968643020559, 1.444305832375993637, -0.9706037289107912747 ) ) ;
#45930=CARTESIAN_POINT ( 'NONE',  ( 4.551880008920849541, 1.548817843433186736, -0.7794160303473545159 ) ) ;
#45932=CARTESIAN_POINT ( 'NONE',  ( 4.545498338918555703, 1.941281163200560878, -0.9724488383844475115 ) ) ;
#45934=CARTESIAN_POINT ( 'NONE',  ( 6.157435431667657610, 1.928259211291092123, -0.5899821858514133766 ) ) ;
#45935=CARTESIAN_POINT ( 'NONE',  ( 4.937500000000003553, 1.451031289060916496, -1.451031289061313512 ) ) ;
#45937=CARTESIAN_POINT ( 'NONE',  ( 2.784106279807782247, -0.9919383200396988398, 1.651252367177785230 ) ) ;
#45939=CARTESIAN_POINT ( 'NONE',  ( 6.363560548480147183, -1.783403785914154049, -1.324293268510617017 ) ) ;
#45941=CARTESIAN_POINT ( 'NONE',  ( 6.883263157960402445, 0.001763689368145578400, 1.846037217754380011 ) ) ;
#45944=CARTESIAN_POINT ( 'NONE',  ( 2.965722808067718486, -1.817245444403335020, -1.277177951966218084 ) ) ;
#45948=CARTESIAN_POINT ( 'NONE',  ( 0.2115648487451895210, 1.930418618556551946, 0.5826528611774861588 ) ) ;
#45950=CARTESIAN_POINT ( 'NONE',  ( 5.687952575977194947, -1.305682642493616541, -1.596842856974973301 ) ) ;
#45955=CARTESIAN_POINT ( 'NONE',  ( 6.749288224047839790, -1.502610544577225982, -1.113804566994440970 ) ) ;
#45956=CARTESIAN_POINT ( 'NONE',  ( 6.117740286212093537, 0.1793736470585994280, 1.724862758254825712 ) ) ;
#45957=CARTESIAN_POINT ( 'NONE',  ( 5.126372767375061201, 0.1352161506754517850, 1.735264446013358608 ) ) ;
#45958=CARTESIAN_POINT ( 'NONE',  ( 3.245926457026059531, 2.292545471606484142, -0.001860936589836299044 ) ) ;
#45960=CARTESIAN_POINT ( 'NONE',  ( 1.112948326906910035, -1.796673262952220629, 0.4014371099074555693 ) ) ;
#45964=CARTESIAN_POINT ( 'NONE',  ( 1.623764174509664260, -1.011042645414115260, -1.519837739365454743 ) ) ;
#45965=CARTESIAN_POINT ( 'NONE',  ( 2.461564753630896440, -1.930417925741171103, -0.5826551686555282439 ) ) ;
#45966=CARTESIAN_POINT ( 'NONE',  ( 1.183813618819636870, -0.9825931803647185436, 1.958887836816553429 ) ) ;
#45968=CARTESIAN_POINT ( 'NONE',  ( 4.735441112814092079, -1.926550399551892001, 0.8509862954892956077 ) ) ;
#45971=CARTESIAN_POINT ( 'NONE',  ( 1.100149375694438714, 0.8407228983892693908, -1.892171374333020406 ) ) ;
#45974=CARTESIAN_POINT ( 'NONE',  ( 5.145234815219777325, 0.1564148900096741512, 2.114790009947895122 ) ) ;
#45975=CARTESIAN_POINT ( 'NONE',  ( 0.1527873662319845505, -1.548267161427993255, 1.146224303156289093 ) ) ;
#45982=CARTESIAN_POINT ( 'NONE',  ( -0.1224090711158704881, -1.988194106603015987, -0.9910323345065151779 ) ) ;
#45983=CARTESIAN_POINT ( 'NONE',  ( 1.096861832941862236, -0.5116358106188825250, -2.042740603722263515 ) ) ;
#45986=CARTESIAN_POINT ( 'NONE',  ( 5.594539833219323022, 1.833072992967394788, 0.3199324213378691439 ) ) ;
#45994=CARTESIAN_POINT ( 'NONE',  ( 2.101936620064443151, 0.7537240185569763495, -1.811501260397870405 ) ) ;
#45995=CARTESIAN_POINT ( 'NONE',  ( 1.393688021309073433, 1.637156065531343740, 1.411701162175371893 ) ) ;
#46000=CARTESIAN_POINT ( 'NONE',  ( 2.565452462605917638, 1.394811117528846900, -1.029664540377094761 ) ) ;
#46001=CARTESIAN_POINT ( 'NONE',  ( 2.782837888936703585, 1.230821076073612463, 1.230640916823136255 ) ) ;
#46004=CARTESIAN_POINT ( 'NONE',  ( 0.7728142736522191081, -2.006652962095498260, 0.1948079406639269262 ) ) ;
#46005=CARTESIAN_POINT ( 'NONE',  ( 6.925078400183578786, 0.5640289027524867382, 2.196098379985710114 ) ) ;
#46007=CARTESIAN_POINT ( 'NONE',  ( 1.481257693138532616, 1.822349276556498143, -0.7526048170787935643 ) ) ;
#46008=CARTESIAN_POINT ( 'NONE',  ( 5.660397963661894849, 1.910509065610028090, 0.08734628876111423523 ) ) ;
#46014=CARTESIAN_POINT ( 'NONE',  ( 1.084635305120797089, -1.279634344436600513, 1.562581769784775920 ) ) ;
#46017=CARTESIAN_POINT ( 'NONE',  ( 4.559805550777903171, 0.5102292677348593264, -2.250327227043275702 ) ) ;
#46018=CARTESIAN_POINT ( 'NONE',  ( 5.846142468697441252, -0.8834969228576605715, 1.751761657833034613 ) ) ;
#46019=CARTESIAN_POINT ( 'NONE',  ( 1.973419848571813073, -0.2453196125269933581, 1.946320556625024345 ) ) ;
#46023=CARTESIAN_POINT ( 'NONE',  ( 1.622414240495053672, 2.095119945234637182, 0.3050691438145485268 ) ) ;
#46026=CARTESIAN_POINT ( 'NONE',  ( 1.200829095903386046, -0.4490931065196464012, 1.785404219219708377 ) ) ;
#46029=CARTESIAN_POINT ( 'NONE',  ( 3.410498715577559015, -2.118327196165440185, -0.1003008382433126094 ) ) ;
#46032=CARTESIAN_POINT ( 'NONE',  ( 3.216142984300340846, -1.012526663717785214, -1.794778392713367587 ) ) ;
#46035=CARTESIAN_POINT ( 'NONE',  ( 0.2331563151865487238, 7.629137130509101361, -2.545728013813946866 ) ) ;
#46039=CARTESIAN_POINT ( 'NONE',  ( 0.1709339574563934483, -1.438030690398562239, 1.674123062825278563 ) ) ;
#46040=CARTESIAN_POINT ( 'NONE',  ( 2.970297248839429027, 1.207737455218102829, 1.912895951805194894 ) ) ;
#46042=CARTESIAN_POINT ( 'NONE',  ( 2.091809026493749890, 1.116998374171035424, 1.426102431979922702 ) ) ;
#46043=CARTESIAN_POINT ( 'NONE',  ( 2.114329361022151854, 1.859220375642420819, 0.4613663794279678765 ) ) ;
#46044=CARTESIAN_POINT ( 'NONE',  ( 2.629418614236479712, 0.1040367438073786233, -2.067886086930009970 ) ) ;
#46046=CARTESIAN_POINT ( 'NONE',  ( 1.973447535326333879, 1.887181058671667966, -0.5703184155462033278 ) ) ;
#46047=CARTESIAN_POINT ( 'NONE',  ( 6.182248986134903035, -1.028413017182037370, 1.628868941788450764 ) ) ;
#46048=CARTESIAN_POINT ( 'NONE',  ( 2.518242125168220102, 1.223528130051700025, -1.415109699333151561 ) ) ;
#46049=CARTESIAN_POINT ( 'NONE',  ( 0.8741376776274005778, 2.222666731570396959, -0.6204599517294244748 ) ) ;
#46051=CARTESIAN_POINT ( 'NONE',  ( 3.121387120179277996, 0.2756568158089545695, -1.840403582779404745 ) ) ;
#46053=CARTESIAN_POINT ( 'NONE',  ( 5.898899852458296955, 0.3987951208904988443, 2.023601990196000955 ) ) ;
#46057=CARTESIAN_POINT ( 'NONE',  ( 6.545935606868724221, 0.8096169477174266493, -1.944322875993751421 ) ) ;
#46059=CARTESIAN_POINT ( 'NONE',  ( 6.081358973892866615, 1.999796440023202670, -0.8210498935554910727 ) ) ;
#46060=CARTESIAN_POINT ( 'NONE',  ( 6.147130067458792091, 0.1999419896685956377, 2.009763438563259008 ) ) ;
#46065=CARTESIAN_POINT ( 'NONE',  ( 6.825078400183548055, 2.461594334264828987, 2.239602747093616841 ) ) ;
#46068=CARTESIAN_POINT ( 'NONE',  ( 5.032435514249763209, 0.5899841883351600869, 1.928258608204669766 ) ) ;
#46073=CARTESIAN_POINT ( 'NONE',  ( 5.717692609583751029, -2.109997883074541392, 0.4692839721026839661 ) ) ;
#46078=CARTESIAN_POINT ( 'NONE',  ( 6.433220217788329087, -1.621194592471734364, -1.198847091081943539 ) ) ;
#46081=CARTESIAN_POINT ( 'NONE',  ( 6.539320575229256249, 7.052319431262985105, 2.701414634427783845 ) ) ;
#46082=CARTESIAN_POINT ( 'NONE',  ( 1.488428555967473921, -0.2500744359604460954, -1.706524604440103898 ) ) ;
#46086=CARTESIAN_POINT ( 'NONE',  ( 6.098880659294531270, 1.529360415809786433, -1.076766019972655197 ) ) ;
#46088=CARTESIAN_POINT ( 'NONE',  ( 0.5045416345675997061, -1.998124945550180609, -0.2444111669489754113 ) ) ;
#46091=CARTESIAN_POINT ( 'NONE',  ( 2.854729849855553780, 0.7423848465729752100, 2.078289375090878632 ) ) ;
#46092=CARTESIAN_POINT ( 'NONE',  ( 4.926734997883643885, -1.423062915019442043, 1.639699324398981251 ) ) ;
#46096=CARTESIAN_POINT ( 'NONE',  ( 2.737105750116640923, 1.997451989420237606, 0.7121958652205606644 ) ) ;
#46097=CARTESIAN_POINT ( 'NONE',  ( 2.530875249677287719, -1.674875632724934338, 1.122518345125958383 ) ) ;
#46098=CARTESIAN_POINT ( 'NONE',  ( 1.951130291612662715, -1.617002164660426677, 0.8169817665307582688 ) ) ;
#46102=CARTESIAN_POINT ( 'NONE',  ( 0.4263524580605422276, 1.788790299270696993, 0.5473224044415525569 ) ) ;
#46105=CARTESIAN_POINT ( 'NONE',  ( 1.885809660653874120, -1.915224419731532901, 0.05109022710406836698 ) ) ;
#46111=CARTESIAN_POINT ( 'NONE',  ( 5.225516498768126183, -2.053876642077703707, 0.6744380372525200507 ) ) ;
#46114=CARTESIAN_POINT ( 'NONE',  ( 3.111701630267147856, 1.674174984267240429, 1.301503359413098249 ) ) ;
#46118=CARTESIAN_POINT ( 'NONE',  ( 4.464113681242611875, 0.9267091202830781693, 1.739933209567791073 ) ) ;
#46119=CARTESIAN_POINT ( 'NONE',  ( 5.379139070037473935, -1.731557697741787916, -0.8120211572784155063 ) ) ;
#46122=CARTESIAN_POINT ( 'NONE',  ( 0.3091450132529197647, -1.663722454078466306, 1.232067777400827069 ) ) ;
#46123=CARTESIAN_POINT ( 'NONE',  ( 2.835803868134049388, 1.927321602952759338, 0.2373744266383533696 ) ) ;
#46127=CARTESIAN_POINT ( 'NONE',  ( 2.396528757545500099, 1.678484640409601436, -1.246154833996036437 ) ) ;
#46130=CARTESIAN_POINT ( 'NONE',  ( 0.2580964568148482741, 1.806467626183925423, 0.1351022710447576103 ) ) ;
#46132=CARTESIAN_POINT ( 'NONE',  ( 4.055453297694236348, -1.834216022232620702, -1.226887332174102951 ) ) ;
#46134=CARTESIAN_POINT ( 'NONE',  ( 3.346891443098894303, 0.5343612633194516626, 2.140983517310310891 ) ) ;
#46137=CARTESIAN_POINT ( 'NONE',  ( 1.945825403448407487, -1.250168254263404277, -1.447093241409423081 ) ) ;
#46140=CARTESIAN_POINT ( 'NONE',  ( 4.158688916442684125, -0.6465363538536234023, -1.966910096795893903 ) ) ;
#46143=CARTESIAN_POINT ( 'NONE',  ( 3.344745324850742385, 0.5235245934552492653, 2.097234944377385002 ) ) ;
#46144=CARTESIAN_POINT ( 'NONE',  ( 5.056268342064010213, -1.587557771011731678, 1.511049258477934032 ) ) ;
#46153=CARTESIAN_POINT ( 'NONE',  ( 0.05336153386781630759, -1.314994204386025434, 1.528742563917218078 ) ) ;
#46155=CARTESIAN_POINT ( 'NONE',  ( 4.346580092118113470, -2.046995731385771400, -0.3088174131898810959 ) ) ;
#46156=CARTESIAN_POINT ( 'NONE',  ( 3.738824155997504395, 0.2837420414000761393, 1.905379044178076686 ) ) ;
#46157=CARTESIAN_POINT ( 'NONE',  ( 5.624650681053017465, 0.4137061758265787592, 2.076257688556768066 ) ) ;
#46160=CARTESIAN_POINT ( 'NONE',  ( 3.467590214127397541, -0.3886977184213887271, 1.930520482988388631 ) ) ;
#46161=CARTESIAN_POINT ( 'NONE',  ( 6.123008101752742682, -2.160436397662615970, 0.7664941572692751670 ) ) ;
#46162=CARTESIAN_POINT ( 'NONE',  ( 4.090329635444483358, -1.806102819543849769, -0.2658631594732660530 ) ) ;
#46168=CARTESIAN_POINT ( 'NONE',  ( 1.469984750362408388, -1.748608032326857353, -0.5769476384821782267 ) ) ;
#46169=CARTESIAN_POINT ( 'NONE',  ( 5.168231636832498310, 2.010700947019973039, -0.1031825239030410013 ) ) ;
#46170=CARTESIAN_POINT ( 'NONE',  ( 1.036931080102401426, 2.214701571188535834, -0.6144361423649072895 ) ) ;
#46171=CARTESIAN_POINT ( 'NONE',  ( 5.717619619964247946, 0.3862620380215216476, -1.923179868201368548 ) ) ;
#46176=CARTESIAN_POINT ( 'NONE',  ( 1.575843314401915496, -1.115566239278027671, 1.768056137498266844 ) ) ;
#46177=CARTESIAN_POINT ( 'NONE',  ( 6.368005316177769437, 0.9137572655052300652, 1.515547905889617519 ) ) ;
#46179=CARTESIAN_POINT ( 'NONE',  ( -0.2104748580754391973, 0.7011259924453935310, -2.185273273056092425 ) ) ;
#46180=CARTESIAN_POINT ( 'NONE',  ( 1.381927130872797838, -0.2546507840628647878, -1.721584071012570050 ) ) ;
#46184=CARTESIAN_POINT ( 'NONE',  ( 1.963112949512689553, 0.2966733001828375516, -1.698991974238444946 ) ) ;
#46185=CARTESIAN_POINT ( 'NONE',  ( 1.259612756803454525, 2.158328104161820526, -0.3793702838810895095 ) ) ;
#46186=CARTESIAN_POINT ( 'NONE',  ( 4.442132104469964204, 0.9450947508268662256, -1.994404356956205326 ) ) ;
#46188=CARTESIAN_POINT ( 'NONE',  ( 0.8312205373445592516, -2.043673001365586384, -0.7330250775806450569 ) ) ;
#46190=CARTESIAN_POINT ( 'NONE',  ( 3.643865571896960809, 2.100859469783818323, -0.2634356371126170826 ) ) ;
#46192=CARTESIAN_POINT ( 'NONE',  ( 3.843561273245421628, 0.7716866907857397040, -2.158722107141448188 ) ) ;
#46196=CARTESIAN_POINT ( 'NONE',  ( 5.725276803944279180, 1.957897222332797504, 1.049153726691682831 ) ) ;
#46204=CARTESIAN_POINT ( 'NONE',  ( 3.621720349255663773, 0.2986264320336135536, 1.994071497604548382 ) ) ;
#46206=CARTESIAN_POINT ( 'NONE',  ( 1.797792903779442009, -1.491087995953117140, -1.425289625791379411 ) ) ;
#46212=CARTESIAN_POINT ( 'NONE',  ( 5.384801694919699067, 1.933943663793664225, -1.030698541907522081 ) ) ;
#46213=CARTESIAN_POINT ( 'NONE',  ( 2.936172824561166905, -1.650081981912490336, -1.158688413653415239 ) ) ;
#46214=CARTESIAN_POINT ( 'NONE',  ( 2.507154105146496725, -1.820902139252629448, 0.2722148935128121394 ) ) ;
#46217=CARTESIAN_POINT ( 'NONE',  ( 5.051681782491273864, 0.5714109786712183725, -1.733901259708306331 ) ) ;
#46219=CARTESIAN_POINT ( 'NONE',  ( 6.522112240665402183, -1.799906897009293738, 0.9091900463213120620 ) ) ;
#46221=CARTESIAN_POINT ( 'NONE',  ( 6.121994746204825866, -1.250886037347900270, -1.885104629530814702 ) ) ;
#46223=CARTESIAN_POINT ( 'NONE',  ( 1.330846195043289493, 2.030104276556158549, 0.5602782565924493419 ) ) ;
#46233=CARTESIAN_POINT ( 'NONE',  ( 3.217226816143878398, 1.749018536054181672, -1.369387470038183396 ) ) ;
#46237=CARTESIAN_POINT ( 'NONE',  ( 2.963279974173158138, 1.655882904019840840, 1.051842618152734499 ) ) ;
#46243=CARTESIAN_POINT ( 'NONE',  ( 2.373420902723611725, -1.847293605357634982, -1.041186957106011723 ) ) ;
#46245=CARTESIAN_POINT ( 'NONE',  ( 4.961884481312108797, 2.138711985806662330, -0.3135959325617638238 ) ) ;
#46246=CARTESIAN_POINT ( 'NONE',  ( 2.612652284633736777, -0.1782932461553646819, 1.832575692395449485 ) ) ;
#46249=CARTESIAN_POINT ( 'NONE',  ( 5.982304607080743963, -0.2621144554034166574, -1.720346425911468469 ) ) ;
#46253=CARTESIAN_POINT ( 'NONE',  ( 2.835029207381420502, 0.2633842809251253358, 2.145520918749081574 ) ) ;
#46254=CARTESIAN_POINT ( 'NONE',  ( 4.604842190751081255, 0.8645911521153251122, -1.821463593394745395 ) ) ;
#46256=CARTESIAN_POINT ( 'NONE',  ( 2.659225025413253007, -1.880336703546074073, -1.066323988048665017 ) ) ;
#46257=CARTESIAN_POINT ( 'NONE',  ( 2.688696339244216915, -0.3334303690454739066, -1.942799078106532074 ) ) ;
#46259=CARTESIAN_POINT ( 'NONE',  ( 4.757337479089009058, 1.920383491809660503, -0.2886861380682907430 ) ) ;
#46269=CARTESIAN_POINT ( 'NONE',  ( 1.395868886378356821, 1.671639904693554168, 1.440724375100350008 ) ) ;
#46271=CARTESIAN_POINT ( 'NONE',  ( 5.858247074779933783, -1.961936380223072263, -0.003592477671530979431 ) ) ;
#46276=CARTESIAN_POINT ( 'NONE',  ( 0.1749903794560748460, 0.004523422195302355051, -1.955468523092759314 ) ) ;
#46277=CARTESIAN_POINT ( 'NONE',  ( 4.347483306186128438, 1.840691044367316120, -0.04759384897683878457 ) ) ;
#46286=CARTESIAN_POINT ( 'NONE',  ( 0.2333700457068142997, -1.884473515381725361, 0.8346939899398809759 ) ) ;
#46288=CARTESIAN_POINT ( 'NONE',  ( 1.996334026009699558, 1.840204857836050367, 0.2769876585018010706 ) ) ;
#46289=CARTESIAN_POINT ( 'NONE',  ( 4.018977146631536712, -1.760761141180338774, 0.5383908109771737838 ) ) ;
#46296=CARTESIAN_POINT ( 'NONE',  ( 3.141465813989018141, -1.946189201368169641, 1.040519825639886431 ) ) ;
#46297=CARTESIAN_POINT ( 'NONE',  ( 5.536487020692383076, 2.227601090660180638, 0.3946122451431322009 ) ) ;
#46299=CARTESIAN_POINT ( 'NONE',  ( 5.431847905162764611, -1.765542832439458198, 0.4050695418617160648 ) ) ;
#46300=CARTESIAN_POINT ( 'NONE',  ( 5.964071289222036221, -1.018598136897935547, 1.622275196354412419 ) ) ;
#46302=CARTESIAN_POINT ( 'NONE',  ( 5.946149726614579301, 1.868617323842229894, 0.09011704611043556967 ) ) ;
#46305=CARTESIAN_POINT ( 'NONE',  ( 5.858207189965921380, 0.7206212418228461480, 1.616676333947133504 ) ) ;
#46306=CARTESIAN_POINT ( 'NONE',  ( 1.077361674225948418, 1.530160568918725872, 1.313541346884481209 ) ) ;
#46308=CARTESIAN_POINT ( 'NONE',  ( 3.106188079018203041, -2.103647721026543405, 0.1036251941764678303 ) ) ;
#46313=CARTESIAN_POINT ( 'NONE',  ( 2.478776341996299593, -1.389826682745049835, 1.465835156725032506 ) ) ;
#46316=CARTESIAN_POINT ( 'NONE',  ( 3.304151629394710632, -2.159270932758147854, 0.1024373671053082913 ) ) ;
#46321=CARTESIAN_POINT ( 'NONE',  ( 1.276089585440323138, -2.118389508516528519, 0.4752255978458518881 ) ) ;
#46325=CARTESIAN_POINT ( 'NONE',  ( 2.314256413632868714, 1.428969747754246233, -1.661726224907192684 ) ) ;
#46327=CARTESIAN_POINT ( 'NONE',  ( 2.729655337971720552, -2.111368630554604220, 0.8135341271046038214 ) ) ;
#46329=CARTESIAN_POINT ( 'NONE',  ( 4.522672878804367969, 0.3494810548456111499, 1.985869246038343583 ) ) ;
#46335=CARTESIAN_POINT ( 'NONE',  ( 3.198275679207917666, -0.5104862868050319413, -1.694526722652128781 ) ) ;
#46336=CARTESIAN_POINT ( 'NONE',  ( 3.123692395903770347, -0.3905211382968387102, 1.974689860881967407 ) ) ;
#46338=CARTESIAN_POINT ( 'NONE',  ( 6.264705869774118696, -1.564926740429407603, 1.556175991035801287 ) ) ;
#46341=CARTESIAN_POINT ( 'NONE',  ( 5.853138716089107518, 0.1455171034051294665, -2.011206573937059261 ) ) ;
#46343=CARTESIAN_POINT ( 'NONE',  ( 3.748781033766034554, -1.529746656882627232, 1.076398355447941491 ) ) ;
#46344=CARTESIAN_POINT ( 'NONE',  ( 3.836834752522141567, -1.993853832596056197, -0.5568897355931883286 ) ) ;
#46348=SURFACE_STYLE_FILL_AREA ( #178475 ) ;
#46349=CARTESIAN_POINT ( 'NONE',  ( 6.121977807712331909, -1.196819783530624015, -1.799967629666970881 ) ) ;
#46351=CARTESIAN_POINT ( 'NONE',  ( 2.699599903323801620, -1.451799986561516764, -1.319707477925702310 ) ) ;
#46352=CARTESIAN_POINT ( 'NONE',  ( 1.159529582462547781, -0.4871260124716703666, -1.956262300040665814 ) ) ;
#46355=CARTESIAN_POINT ( 'NONE',  ( 1.141631569582121974, 0.7634220068381203372, -1.707866752806507460 ) ) ;
#46357=CARTESIAN_POINT ( 'NONE',  ( 3.533450910810581824, -0.1440131911168585910, 2.008084626805274997 ) ) ;
#46359=CARTESIAN_POINT ( 'NONE',  ( 1.722414120629287337, 2.094725599053618659, 0.3070382465363735158 ) ) ;
#46361=CARTESIAN_POINT ( 'NONE',  ( 4.141125838365485201, -0.1998502692034490602, -2.060677327190631569 ) ) ;
#46363=CARTESIAN_POINT ( 'NONE',  ( 5.683562130502735954, -0.9407222913834032418, 1.867095764824426851 ) ) ;
#46365=CARTESIAN_POINT ( 'NONE',  ( 4.664971680594516279, -1.631047870213175432, -0.8201845326444437978 ) ) ;
#46372=CARTESIAN_POINT ( 'NONE',  ( 5.426388453851806126, -0.8635988772061551355, -1.706256623820540108 ) ) ;
#46378=CARTESIAN_POINT ( 'NONE',  ( 0.6437974683802077935, 0.5340323341261629109, 1.762076181610471526 ) ) ;
#46382=CARTESIAN_POINT ( 'NONE',  ( 4.340975799156802317, -1.628549031532234403, 0.9200136957008757665 ) ) ;
#46390=CARTESIAN_POINT ( 'NONE',  ( 0.8484201349984072937, -1.953920032193863232, -0.2464512992164570593 ) ) ;
#46391=CARTESIAN_POINT ( 'NONE',  ( 2.882435586221145485, -0.5880402899147363360, -1.928746874286999979 ) ) ;
#46395=CARTESIAN_POINT ( 'NONE',  ( 4.031328258368102269, -1.510625130563835627, -1.587819133214096734 ) ) ;
#46406=CARTESIAN_POINT ( 'NONE',  ( 4.546344060013487898, -1.475942220874026489, 1.100600019281534836 ) ) ;
#46407=CARTESIAN_POINT ( 'NONE',  ( 2.121741512283023656, -0.4388329339449773547, 1.964535544105987075 ) ) ;
#46408=CARTESIAN_POINT ( 'NONE',  ( 3.743815364168050053, -2.214071480395309433, -0.6165714402358390966 ) ) ;
#46409=CARTESIAN_POINT ( 'NONE',  ( -0.02919842301641033255, 0.7163969788333038879, -2.157531187298274311 ) ) ;
#46410=CARTESIAN_POINT ( 'NONE',  ( 1.762329786688419109, -0.6638292341827031207, -1.738725725234435693 ) ) ;
#46413=CARTESIAN_POINT ( 'NONE',  ( 5.343983030329363615, -1.218012673290536974, -1.474316871017400166 ) ) ;
#46416=CARTESIAN_POINT ( 'NONE',  ( 5.267163683669145335, 2.014557126142228594, -0.5589344999666242542 ) ) ;
#46417=CARTESIAN_POINT ( 'NONE',  ( 2.904993682805886213, 1.579364189935757778, 1.002181356900035070 ) ) ;
#46419=CARTESIAN_POINT ( 'NONE',  ( 5.847170753249844033, 0.5281823367668266878, -1.763884204139199330 ) ) ;
#46422=CARTESIAN_POINT ( 'NONE',  ( 5.320820994898000755, 1.595919931443249951, 0.6549295409969541071 ) ) ;
#46424=CARTESIAN_POINT ( 'NONE',  ( 0.5274301605363295176, -1.488642097782297835, 0.8892331099567828412 ) ) ;
#46426=CARTESIAN_POINT ( 'NONE',  ( 6.210172754313918908, 1.157103754073171675, -1.651340222398114843 ) ) ;
#46428=CARTESIAN_POINT ( 'NONE',  ( 4.838842012204412235, -2.104300398676747896, -0.5337788192065362480 ) ) ;
#46429=CARTESIAN_POINT ( 'NONE',  ( 2.771877994228102882, 0.9767612972278701955, 1.542236413651025151 ) ) ;
#46430=CARTESIAN_POINT ( 'NONE',  ( 1.217545072937670225, 0.3881152535412414339, -1.922811240370206232 ) ) ;
#46431=CARTESIAN_POINT ( 'NONE',  ( 6.245324861096241520, 0.3598972253578552327, -2.086368836056912368 ) ) ;
#46432=CARTESIAN_POINT ( 'NONE',  ( 0.4281777144111223454, 1.173252442481845126, -1.969132371278771831 ) ) ;
#46436=CARTESIAN_POINT ( 'NONE',  ( 2.157031413788193852, 0.4673396547767159070, 2.068183735011968061 ) ) ;
#46440=CARTESIAN_POINT ( 'NONE',  ( 1.147426569842596722, 1.827566109494669577, -0.9725325914680116313 ) ) ;
#46441=CARTESIAN_POINT ( 'NONE',  ( 6.983263157960370116, 1.251666756963093041, 2.167287073222202931 ) ) ;
#46443=CARTESIAN_POINT ( 'NONE',  ( 2.561440534034305827, -1.845267710029829145, 1.236318238231758571 ) ) ;
#46445=CARTESIAN_POINT ( 'NONE',  ( 0.4757056697715462690, -2.282288811291408148, -0.2737132658124728501 ) ) ;
#46447=CARTESIAN_POINT ( 'NONE',  ( 5.207907603007337016, 0.6519758639490059737, -1.956853833162349066 ) ) ;
#46451=CARTESIAN_POINT ( 'NONE',  ( 0.2331563151865451988, 4.092570554693980789, -2.500672995626152861 ) ) ;
#46452=CARTESIAN_POINT ( 'NONE',  ( 5.829618728418341611, 0.9018330327132916269, -1.605192750430362025 ) ) ;
#46454=CARTESIAN_POINT ( 'NONE',  ( 1.693959787788183347, -1.716010565565774915, -0.1736237626131422462 ) ) ;
#46455=CARTESIAN_POINT ( 'NONE',  ( 1.130092623156966347, 2.014433208573155110, 0.09411304420373775570 ) ) ;
#46456=CARTESIAN_POINT ( 'NONE',  ( 2.286107107991880216, 1.843941258665306115, -1.372366127498450883 ) ) ;
#46458=CARTESIAN_POINT ( 'NONE',  ( 2.144175119285938180, 0.8672398327666650530, -2.089775168228876545 ) ) ;
#46459=CARTESIAN_POINT ( 'NONE',  ( 4.459663826605764214, 0.4620033958209149305, -2.054602365452788071 ) ) ;
#46461=CARTESIAN_POINT ( 'NONE',  ( 2.407162768383603435, -0.3926560375935496672, 1.725441652247063251 ) ) ;
#46464=CARTESIAN_POINT ( 'NONE',  ( 4.985981925524552771, -2.274816124779193593, -0.2825110863640226122 ) ) ;
#46465=CARTESIAN_POINT ( 'NONE',  ( 4.066218318298571610, -1.718653781379267276, -0.6607852518168353395 ) ) ;
#46469=CARTESIAN_POINT ( 'NONE',  ( 4.998067021457727854, -0.7363416341295281331, -2.064161796032103258 ) ) ;
#46474=CARTESIAN_POINT ( 'NONE',  ( 2.684106373981818727, -0.9902706917056921521, 1.652370099195903386 ) ) ;
#46477=CARTESIAN_POINT ( 'NONE',  ( 5.572555445586866441, 0.8612648569810870125, 1.938019255899057658 ) ) ;
#46487=CARTESIAN_POINT ( 'NONE',  ( 1.909305195714078307, -0.8207579233160157139, -1.534770245041901182 ) ) ;
#46489=CARTESIAN_POINT ( 'NONE',  ( 0.3440982351944205653, -0.9282241650855774795, 1.728402704573736903 ) ) ;
#46492=CARTESIAN_POINT ( 'NONE',  ( 5.840740251263128791, 0.4172088472891195554, 2.120894824392767664 ) ) ;
#46495=CARTESIAN_POINT ( 'NONE',  ( 6.262596564776618635, -1.532251275270900326, 1.525113613579494709 ) ) ;
#46496=CARTESIAN_POINT ( 'NONE',  ( -0.2104748580754183807, 4.084054299358617079, -2.658391380015924010 ) ) ;
#46499=CARTESIAN_POINT ( 'NONE',  ( 0.1806930697454533219, -0.1309388314422038346, -1.840455529407057256 ) ) ;
#46500=CARTESIAN_POINT ( 'NONE',  ( 6.679014442879065427, -0.8212242018711314318, -1.526972759001248514 ) ) ;
#46503=CARTESIAN_POINT ( 'NONE',  ( 2.630644284709309666, 0.2711686948545319886, 2.174668582101045633 ) ) ;
#46504=CARTESIAN_POINT ( 'NONE',  ( 3.346982425237558179, 0.5585957852003355928, 2.238849765380794832 ) ) ;
#46505=CARTESIAN_POINT ( 'NONE',  ( 6.292271403379039896, -2.050439857688883372, -0.2063938634464974886 ) ) ;
#46506=CARTESIAN_POINT ( 'NONE',  ( 0.9549039013059671399, 0.3793949951976150481, -1.904366508208689357 ) ) ;
#46511=CARTESIAN_POINT ( 'NONE',  ( 3.920270587443940080, -2.114697630030224929, 0.1593259359235904837 ) ) ;
#46513=CARTESIAN_POINT ( 'NONE',  ( 2.690077459517980163, 1.704938782060089864, 1.076316768488336351 ) ) ;
#46515=CARTESIAN_POINT ( 'NONE',  ( 4.014836333542094238, 1.562590183666902943, -1.558512549626612342 ) ) ;
#46516=PLANE ( 'NONE',  #32274 ) ;
#46519=CARTESIAN_POINT ( 'NONE',  ( 0.3635304476994546952, 1.806310985241452949, -0.2645042207462811046 ) ) ;
#46524=VERTEX_POINT ( 'NONE', #189131 ) ;
#46525=CARTESIAN_POINT ( 'NONE',  ( 4.961820856888925491, 2.038780864349061250, -0.3001439806698430468 ) ) ;
#46531=CARTESIAN_POINT ( 'NONE',  ( 3.281903422188407138, 1.969933747823931380, -0.4446889725447465413 ) ) ;
#46536=CARTESIAN_POINT ( 'NONE',  ( 3.538010501442095723, 0.9279861380482921085, -1.840221436749614803 ) ) ;
#46537=CARTESIAN_POINT ( 'NONE',  ( 3.270157880292836605, 1.821742160604752137, -0.8647241845514612724 ) ) ;
#46541=CARTESIAN_POINT ( 'NONE',  ( 2.759138561942891421, -2.010518527590241966, -0.1511176148010634768 ) ) ;
#46542=CARTESIAN_POINT ( 'NONE',  ( 1.359045109759978498, 1.814150759811587355, -0.3131490413979670651 ) ) ;
#46544=CARTESIAN_POINT ( 'NONE',  ( 0.3820104410975051490, 2.150944695799131612, -0.8364647861166041309 ) ) ;
#46546=CARTESIAN_POINT ( 'NONE',  ( 2.671339989782473001, 0.1089736159370843782, -2.158987078831893669 ) ) ;
#46548=CARTESIAN_POINT ( 'NONE',  ( 4.522735144945882801, 0.3654406173194921781, 2.085432885242066270 ) ) ;
#46550=CARTESIAN_POINT ( 'NONE',  ( 0.6900581440293825919, -1.856003987442723657, -0.2331820809091043056 ) ) ;
#46552=CARTESIAN_POINT ( 'NONE',  ( 4.803572714498323570, -0.5265354887679043472, 1.899778226852407936 ) ) ;
#46557=CARTESIAN_POINT ( 'NONE',  ( 6.006491595720174104, -0.7565722652288708883, -1.965664901909335738 ) ) ;
#46558=CARTESIAN_POINT ( 'NONE',  ( 6.478973898625433492, 1.930320082341809629, 0.7489585856828018251 ) ) ;
#46561=CARTESIAN_POINT ( 'NONE',  ( 6.539320575229276677, 6.035451701470580410, 2.698157228745074576 ) ) ;
#46562=CARTESIAN_POINT ( 'NONE',  ( 5.260604563723265237, -1.428518960016441186, 1.358918391201448417 ) ) ;
#46563=CARTESIAN_POINT ( 'NONE',  ( 6.047130097259819870, 0.2019483658235003143, 2.009690058136243351 ) ) ;
#46565=CARTESIAN_POINT ( 'NONE',  ( 4.512551404143492206, -0.9841529367882025925, -2.087457756972084244 ) ) ;
#46567=CARTESIAN_POINT ( 'NONE',  ( 1.780209297579591565, -1.142364670758776013, -1.717135550327288485 ) ) ;
#46574=CARTESIAN_POINT ( 'NONE',  ( 3.930270145471780996, 1.203169952209550919, 1.807132499170207351 ) ) ;
#46577=CARTESIAN_POINT ( 'NONE',  ( 3.966218424140379728, -1.719484690100345325, -0.6589542199007536460 ) ) ;
#46580=CARTESIAN_POINT ( 'NONE',  ( 5.970311429539967740, -2.080533979117826782, -0.6889730390344513955 ) ) ;
#46582=CARTESIAN_POINT ( 'NONE',  ( 6.086863830973287648, -0.3249354738291005407, -2.238958312302678610 ) ) ;
#46588=CARTESIAN_POINT ( 'NONE',  ( 1.164531557977426912, -1.597865870565655877, -0.7613500884297589311 ) ) ;
#46589=CARTESIAN_POINT ( 'NONE',  ( 4.723295704472612044, 1.752545568416422173, 0.9903661003969994603 ) ) ;
#46591=CARTESIAN_POINT ( 'NONE',  ( 4.049914914165038127, 0.7116930038560628224, -1.982186593211773706 ) ) ;
#46592=CARTESIAN_POINT ( 'NONE',  ( 2.231924035814872642, 1.915248681264541508, 0.04463030589317053265 ) ) ;
#46594=CARTESIAN_POINT ( 'NONE',  ( 3.402753045726066183, 0.4761229057644749130, 1.911014528907057697 ) ) ;
#46595=CARTESIAN_POINT ( 'NONE',  ( 5.924083597509600452, -2.004057273996622701, 0.2512124657789679971 ) ) ;
#46596=CARTESIAN_POINT ( 'NONE',  ( 1.990876257202532695, 1.628914321797021669, -0.9196232060951770038 ) ) ;
#46597=CARTESIAN_POINT ( 'NONE',  ( 1.890992312513404716, 0.1891058464698439912, 1.952711869325058691 ) ) ;
#46598=CARTESIAN_POINT ( 'NONE',  ( 4.107791765966132047, -1.720061694268668395, 0.1296855704675456133 ) ) ;
#46599=CARTESIAN_POINT ( 'NONE',  ( 1.529408426332915960, -0.2309274165002393187, 1.898302859121250297 ) ) ;
#46601=CARTESIAN_POINT ( 'NONE',  ( 1.243116305521356990, 0.4334984505205765060, 2.163720904216937857 ) ) ;
#46608=CARTESIAN_POINT ( 'NONE',  ( 6.543811353064236336, 1.423268159695538326, 1.503672778047180136 ) ) ;
#46609=CARTESIAN_POINT ( 'NONE',  ( 0.3618904354094238385, -0.5536326762660361833, 1.994880328902041589 ) ) ;
#46614=CARTESIAN_POINT ( 'NONE',  ( 5.637388408723053246, -0.05200288984260474645, 2.120005899716829401 ) ) ;
#46619=CARTESIAN_POINT ( 'NONE',  ( 6.725062055625550705, -1.793239977796506457, -0.7961783947641184467 ) ) ;
#46621=CARTESIAN_POINT ( 'NONE',  ( 3.919295934624257960, 0.7230291454519314209, 1.882185965797255278 ) ) ;
#46622=CARTESIAN_POINT ( 'NONE',  ( 3.098755142807321672, 1.734096097442457518, 0.8144269386064789673 ) ) ;
#46623=CARTESIAN_POINT ( 'NONE',  ( 1.347511689332027807, 0.6317163119916607839, -2.098556723903362009 ) ) ;
#46625=CARTESIAN_POINT ( 'NONE',  ( 5.238544184099147571, 1.195677241517135281, -1.619561112405358827 ) ) ;
#46628=CARTESIAN_POINT ( 'NONE',  ( 5.853141746508254251, 0.1553614259057617408, -2.111562834372962438 ) ) ;
#46630=CARTESIAN_POINT ( 'NONE',  ( 3.509396081178951743, -2.059435208860632915, 0.3595599189689518416 ) ) ;
#46632=CARTESIAN_POINT ( 'NONE',  ( 2.274029058727170316, -1.063862581237082550, 1.357477553621669442 ) ) ;
#46634=CARTESIAN_POINT ( 'NONE',  ( 5.502226937873657242, -0.9515977829631333540, 1.895136135177949877 ) ) ;
#46644=CARTESIAN_POINT ( 'NONE',  ( 1.681973674898680216, 0.9313724848135003231, 1.553549296804368707 ) ) ;
#46650=CARTESIAN_POINT ( 'NONE',  ( 2.191808917380858812, 1.115356421127197351, 1.427258924012535735 ) ) ;
#46651=CARTESIAN_POINT ( 'NONE',  ( 6.539320575229249144, 0.007148032025052972194, 1.896977914940492393 ) ) ;
#46656=CARTESIAN_POINT ( 'NONE',  ( 4.140933978860473985, -0.1807793374023874688, -1.852226635870577898 ) ) ;
#46657=CARTESIAN_POINT ( 'NONE',  ( 1.511203358410578179, -1.803099835331838818, 0.6471475864035965975 ) ) ;
#46658=CARTESIAN_POINT ( 'NONE',  ( 0.1998643617870856648, -1.825052844667142349, -0.05062755788937112200 ) ) ;
#46665=CARTESIAN_POINT ( 'NONE',  ( 5.119951519371389814, 1.948576354197928628, -0.2848888285253112218 ) ) ;
#46668=CARTESIAN_POINT ( 'NONE',  ( 6.720655732516648939, -0.004400176169771368405, 2.173773060281408487 ) ) ;
#46670=CARTESIAN_POINT ( 'NONE',  ( 5.438475939130889891, 1.897888883619626821, 0.3293186976999362137 ) ) ;
#46672=CARTESIAN_POINT ( 'NONE',  ( 1.430379662499326354, 1.758314708518812663, 0.4907259477668829972 ) ) ;
#46673=CARTESIAN_POINT ( 'NONE',  ( 2.420803835572300500, 1.440536793087299205, -1.671967039616916617 ) ) ;
#46675=CARTESIAN_POINT ( 'NONE',  ( 0.3516297456669579269, -1.353986107606550471, -1.350798769753497552 ) ) ;
#46680=CARTESIAN_POINT ( 'NONE',  ( 0.5374760852590576565, 1.839023226330655625, -0.7055796775109841601 ) ) ;
#46681=CARTESIAN_POINT ( 'NONE',  ( 1.434995430731567101, -1.407912642168735573, -1.337921467293776923 ) ) ;
#46683=CARTESIAN_POINT ( 'NONE',  ( 1.054064285791616262, 1.779355684154381834, -0.9478921834336280217 ) ) ;
#46685=CARTESIAN_POINT ( 'NONE',  ( 6.016418624437367413, 0.7528656616105857680, 1.702022903989255376 ) ) ;
#46692=CARTESIAN_POINT ( 'NONE',  ( 1.927518781310177509, -1.434474475899261581, -1.656937093973806396 ) ) ;
#46697=CARTESIAN_POINT ( 'NONE',  ( 1.189776066567624691, -0.8228614858879386151, 1.629801898503015156 ) ) ;
#46700=CARTESIAN_POINT ( 'NONE',  ( 6.509000000000014552, 2.444259026362519904, 2.383015625331697862 ) ) ;
#46703=CARTESIAN_POINT ( 'NONE',  ( 1.453605159173555705, 0.5596597320992221514, -1.843422129977128954 ) ) ;
#46705=CARTESIAN_POINT ( 'NONE',  ( 3.942202469084721272, -0.9707516781715104237, 1.704694321266352786 ) ) ;
#46708=CARTESIAN_POINT ( 'NONE',  ( 4.599289333468261631, -0.5842463895667610041, 2.112197083089427885 ) ) ;
#46712=CARTESIAN_POINT ( 'NONE',  ( 4.364170320198999420, -2.065056620294950740, 0.1471644388686063065 ) ) ;
#46715=EDGE_LOOP ( 'NONE', ( #129430, #30648, #128488, #88463 ) ) ;
#46716=CARTESIAN_POINT ( 'NONE',  ( 3.481312804724666421, -2.296076454524886845, -0.1115701876132721843 ) ) ;
#46723=CARTESIAN_POINT ( 'NONE',  ( 3.363160477839432172, 1.894460165981373789, -0.4261612883773926441 ) ) ;
#46727=CARTESIAN_POINT ( 'NONE',  ( 4.869353489999923568, -1.618680692612521455, -1.018082601613921723 ) ) ;
#46729=CARTESIAN_POINT ( 'NONE',  ( 5.684504558281781250, -1.683600953293447944, -0.3737579273616030706 ) ) ;
#46730=CARTESIAN_POINT ( 'NONE',  ( 4.628138809701114020, 2.011451458044950069, 0.1435230606586651581 ) ) ;
#46731=CARTESIAN_POINT ( 'NONE',  ( 5.168667805954368255, 1.541955118739355424, 1.704926945024546336 ) ) ;
#46733=CARTESIAN_POINT ( 'NONE',  ( 0.9091299924109221831, 1.668792687453458878, -1.444214864661397035 ) ) ;
#46736=CARTESIAN_POINT ( 'NONE',  ( 0.3030915354301273457, -0.4787081777068747934, 1.703804975073195394 ) ) ;
#46737=CARTESIAN_POINT ( 'NONE',  ( 6.065077313367789102, -1.076319894221990259, 1.704936797084610101 ) ) ;
#46739=CARTESIAN_POINT ( 'NONE',  ( 2.853816628688166990, 2.281129249179119078, -0.2256723309681916978 ) ) ;
#46740=CARTESIAN_POINT ( 'NONE',  ( 1.130330966444204277, -1.574854822160208556, 0.7409792249596267588 ) ) ;
#46742=CARTESIAN_POINT ( 'NONE',  ( 1.563399581876812716, 1.420944641023152322, -0.9932112465018216874 ) ) ;
#46745=CARTESIAN_POINT ( 'NONE',  ( 1.539757937649718800, 2.006347644133343433, -0.8302594476135690682 ) ) ;
#46746=CARTESIAN_POINT ( 'NONE',  ( 2.817592499383800853, -1.357869084745389809, -1.490969456672403881 ) ) ;
#46747=CARTESIAN_POINT ( 'NONE',  ( 4.343750000000002665, 1.895863743164175608, 0.7852924748297558377 ) ) ;
#46750=CARTESIAN_POINT ( 'NONE',  ( 6.727182134110236689, 0.003007720480393410133, 1.910970182385362870 ) ) ;
#46753=CARTESIAN_POINT ( 'NONE',  ( 3.920361760358490599, -2.215291009692350599, 0.1660125995653055075 ) ) ;
#46760=CARTESIAN_POINT ( 'NONE',  ( 5.196709787541290204, 1.427093291641279293, 0.9959802872364865722 ) ) ;
#46761=CARTESIAN_POINT ( 'NONE',  ( 3.543363863352413823, 1.774678991803163575, -0.8365776047038612218 ) ) ;
#46765=CARTESIAN_POINT ( 'NONE',  ( 4.780719109985231974, -2.192918799143634079, -0.5559354454096259168 ) ) ;
#46766=CARTESIAN_POINT ( 'NONE',  ( 1.609910828531309956, 0.6006481715085715267, -1.973267531027416810 ) ) ;
#46768=CARTESIAN_POINT ( 'NONE',  ( 2.307839474932214419, -0.4956500345179111200, 2.207406129587013766 ) ) ;
#46771=CARTESIAN_POINT ( 'NONE',  ( 3.180766902908559235, -0.1340872481324743570, -1.865776598943262199 ) ) ;
#46772=CARTESIAN_POINT ( 'NONE',  ( 2.021687164805381354, -1.548805232022354650, 0.7802212711869142003 ) ) ;
#46773=CARTESIAN_POINT ( 'NONE',  ( -0.1288028175206907822, -0.008968661790493319408, -2.273875003271645934 ) ) ;
#46774=CARTESIAN_POINT ( 'NONE',  ( 0.3060867131535297547, -0.5861141839358529060, 2.127432003918772629 ) ) ;
#46775=CARTESIAN_POINT ( 'NONE',  ( 4.540002997438313592, 0.9271085556134452954, -1.952944755896801610 ) ) ;
#46776=CARTESIAN_POINT ( 'NONE',  ( 4.997963218837587540, -0.6557800786283998207, -1.827999027568379509 ) ) ;
#46778=CARTESIAN_POINT ( 'NONE',  ( 6.696569769017397533, -0.4992639023812007193, -1.802638941973549569 ) ) ;
#46779=( NAMED_UNIT ( * ) PLANE_ANGLE_UNIT ( ) SI_UNIT ( $, .RADIAN. ) );
#46781=CARTESIAN_POINT ( 'NONE',  ( 6.983263157960365675, -0.006178392973848687020, 2.053544886540019210 ) ) ;
#46784=CARTESIAN_POINT ( 'NONE',  ( 5.643203987388664800, 0.8197706014990979728, 1.842448445624145226 ) ) ;
#46788=CARTESIAN_POINT ( 'NONE',  ( 3.650846181029033133, -1.491723252493650564, 1.052289205326197852 ) ) ;
#46793=EDGE_CURVE ( 'NONE', #126082, #92893, #1751, .T. ) ;
#46796=CARTESIAN_POINT ( 'NONE',  ( 0.4045644467639066821, -2.005039209919571075, -0.2428365769681257724 ) ) ;
#46797=CARTESIAN_POINT ( 'NONE',  ( 1.717596852896427606, 1.764750374324057347, 1.175337852406685757 ) ) ;
#46800=CARTESIAN_POINT ( 'NONE',  ( 1.445918188014534422, -0.8427435445049488161, 1.659298548423918884 ) ) ;
#46802=CARTESIAN_POINT ( 'NONE',  ( 0.09294085500742564621, -0.4768749645070144982, -2.116232079886640971 ) ) ;
#46806=CARTESIAN_POINT ( 'NONE',  ( -0.2108831679770960255, -0.001785917861228669690, -1.896958272444612792 ) ) ;
#46810=CARTESIAN_POINT ( 'NONE',  ( 6.292342264464226176, -1.899326897351862664, 0.6766127494588560776 ) ) ;
#46811=CARTESIAN_POINT ( 'NONE',  ( 6.193280126971262511, -0.6156851667328180344, 1.735278506779000640 ) ) ;
#46812=CARTESIAN_POINT ( 'NONE',  ( -0.02319159430949970999, 2.891346550825595774, -2.299931007135449512 ) ) ;
#46813=CARTESIAN_POINT ( 'NONE',  ( 3.774305527563319274, 1.280948863717756847, 1.919355958833997233 ) ) ;
#46815=CARTESIAN_POINT ( 'NONE',  ( 5.466167184710096549, 1.060119519021487378, 1.883692621652333532 ) ) ;
#46817=CARTESIAN_POINT ( 'NONE',  ( 0.8549040543346017040, 0.3774493213832031402, -1.904865965088814228 ) ) ;
#46819=ORIENTED_EDGE ( 'NONE', *, *, #142903, .F. ) ;
#46820=CARTESIAN_POINT ( 'NONE',  ( 4.956595877991936128, 1.698763664877179780, 1.548309420705455741 ) ) ;
#46824=CARTESIAN_POINT ( 'NONE',  ( 4.803500792215161574, -0.4985019455652460740, 1.802925825644098534 ) ) ;
#46826=CARTESIAN_POINT ( 'NONE',  ( 0.7559434568639655794, 0.7726834774516875282, -1.749509110286852742 ) ) ;
#46829=CARTESIAN_POINT ( 'NONE',  ( 3.510573375967055654, -0.8941257848905452832, -2.017821460644920073 ) ) ;
#46835=CARTESIAN_POINT ( 'NONE',  ( 2.161341668630599955, 0.3408821015241836894, -1.941522824740661290 ) ) ;
#46836=CARTESIAN_POINT ( 'NONE',  ( 0.9917865004017255570, 2.033541294120873033, -1.090684920485317733 ) ) ;
#46837=CARTESIAN_POINT ( 'NONE',  ( 2.101936620064443151, 0.7537240185569763495, -1.811501260397870405 ) ) ;
#46838=CARTESIAN_POINT ( 'NONE',  ( 4.944214452789121417, -0.9770834884576683477, 1.816490783314741231 ) ) ;
#46845=CARTESIAN_POINT ( 'NONE',  ( 0.9190777403676134716, -1.573854924298900615, 1.495750265368815946 ) ) ;
#46850=CARTESIAN_POINT ( 'NONE',  ( 2.126040175964475143, 1.080828230516362121, -1.526477596812993553 ) ) ;
#46851=CARTESIAN_POINT ( 'NONE',  ( 6.643834073375672666, 0.8340821395082242962, -1.994398315854857495 ) ) ;
#46853=CARTESIAN_POINT ( 'NONE',  ( 6.727182134110210043, 6.040083938853186396, 2.305853406558423302 ) ) ;
#46855=CARTESIAN_POINT ( 'NONE',  ( 2.578645926699867363, -1.317302948579327504, 1.386430337501590282 ) ) ;
#46856=CARTESIAN_POINT ( 'NONE',  ( 4.293650081035056409, -0.6766669130573493840, 1.635584247362771304 ) ) ;
#46858=CARTESIAN_POINT ( 'NONE',  ( 1.611815888142430264, -0.6431676737995162263, 1.801018335096972400 ) ) ;
#46861=CARTESIAN_POINT ( 'NONE',  ( 5.167565342116251514, 1.290006671357433632, 1.416291653197629952 ) ) ;
#46862=CARTESIAN_POINT ( 'NONE',  ( 0.1333692844072559280, 0.001398348041498076455, -2.053671342968105051 ) ) ;
#46864=CARTESIAN_POINT ( 'NONE',  ( 2.039458538997685366, 0.004855507148140979744, 2.120778211687989856 ) ) ;
#46866=CARTESIAN_POINT ( 'NONE',  ( 5.155093292349416600, -1.580716073637401076, -1.000049079914612449 ) ) ;
#46867=CARTESIAN_POINT ( 'NONE',  ( 1.523764310407935030, -1.012771255265769943, -1.518815351243132383 ) ) ;
#46869=CARTESIAN_POINT ( 'NONE',  ( 4.231241840954825584, 0.1069408422738199749, 2.204416794138922331 ) ) ;
#46872=CARTESIAN_POINT ( 'NONE',  ( 1.803259461591859347, -1.743671650923955374, 1.101644963814436329 ) ) ;
#46880=CARTESIAN_POINT ( 'NONE',  ( 3.824723168590526523, -1.392635068473629500, 1.532133406949770960 ) ) ;
#46882=CARTESIAN_POINT ( 'NONE',  ( 2.495597164219889308, 1.669172397749154380, 1.373402732410613947 ) ) ;
#46884=CARTESIAN_POINT ( 'NONE',  ( 2.367837350726550660, 0.5366352218779540939, -1.947015567076612941 ) ) ;
#46891=CARTESIAN_POINT ( 'NONE',  ( 0.1281391398850126040, 2.011452084832816123, 0.1435147193784985509 ) ) ;
#46892=CARTESIAN_POINT ( 'NONE',  ( 4.511385190476093321, -2.149204750630455241, 0.4279282578087198474 ) ) ;
#46894=CARTESIAN_POINT ( 'NONE',  ( 4.236511230858605259, 1.172298487584079396, -1.510895503047122945 ) ) ;
#46898=CARTESIAN_POINT ( 'NONE',  ( 2.407827563459669307, -1.163288551851604513, -1.646826728940099738 ) ) ;
#46902=CARTESIAN_POINT ( 'NONE',  ( 5.403229623239121260, 1.412049869051584361, 0.9901104176405839397 ) ) ;
#46903=CARTESIAN_POINT ( 'NONE',  ( -0.1399997263889819488, 4.088450529495776919, -2.555104583160577203 ) ) ;
#46907=CARTESIAN_POINT ( 'NONE',  ( 0.8134373588399683719, -1.746984811521329339, -1.110588058507409936 ) ) ;
#46909=CARTESIAN_POINT ( 'NONE',  ( 4.898965649768390662, -0.2269230896460339986, -1.797137895798770479 ) ) ;
#46912=CARTESIAN_POINT ( 'NONE',  ( 5.848286676205444401, 0.8867688175292733899, -1.579494629471886791 ) ) ;
#46915=CARTESIAN_POINT ( 'NONE',  ( 2.836070844659248191, 2.175002134116140518, 0.2674123886829762875 ) ) ;
#46916=ORIENTED_EDGE ( 'NONE', *, *, #87162, .F. ) ;
#46918=CARTESIAN_POINT ( 'NONE',  ( 6.877413160773132361, -0.1400689347856296230, 1.829862831089356545 ) ) ;
#46920=CARTESIAN_POINT ( 'NONE',  ( 5.325768798837505535, 0.7719732895165082320, -1.753353820041517741 ) ) ;
#46926=CARTESIAN_POINT ( 'NONE',  ( 1.376082401959723089, 1.288024388040419632, 1.735935173841046675 ) ) ;
#46929=CARTESIAN_POINT ( 'NONE',  ( 2.309345278970798887, -0.4025885200794159235, 1.780468244869021222 ) ) ;
#46931=CARTESIAN_POINT ( 'NONE',  ( 5.157177646623883227, -1.542991646335686973, -0.9753701268572569916 ) ) ;
#46933=CARTESIAN_POINT ( 'NONE',  ( 2.707167837304753633, 1.638089068140319071, -0.9866689735503200165 ) ) ;
#46935=CARTESIAN_POINT ( 'NONE',  ( 3.455474441396837904, 1.550956523109302543, 1.213803446622195636 ) ) ;
#46937=CARTESIAN_POINT ( 'NONE',  ( 4.933121067701986995, -1.376026015944699088, -1.370709014919595958 ) ) ;
#46941=CARTESIAN_POINT ( 'NONE',  ( 4.887034483293543730, -1.997634423138573867, -0.7120497732875651353 ) ) ;
#46943=CARTESIAN_POINT ( 'NONE',  ( 3.316961667764028121, 1.505919282548912719, -1.178437403786938731 ) ) ;
#46949=CARTESIAN_POINT ( 'NONE',  ( 4.723295704472612044, 1.752545568416422173, 0.9903661003969994603 ) ) ;
#46951=CARTESIAN_POINT ( 'NONE',  ( 5.250558533952181861, 0.5335417292645014964, 1.745990657226546894 ) ) ;
#46952=CARTESIAN_POINT ( 'NONE',  ( 1.029834584532058672, 1.995790600324919506, -0.5504719462680053299 ) ) ;
#46956=CARTESIAN_POINT ( 'NONE',  ( 6.209813078548920728, -1.856259414618817383, 0.2309603555875269776 ) ) ;
#46965=CARTESIAN_POINT ( 'NONE',  ( 1.375928118113247667, -2.020660359122231409, 0.4497719141252010111 ) ) ;
#46966=CARTESIAN_POINT ( 'NONE',  ( 2.495853057047519030, -2.093741659442478920, 0.3138373457529738397 ) ) ;
#46970=CARTESIAN_POINT ( 'NONE',  ( 0.4968415868889561882, 0.3310222599195339899, 1.941247527895247904 ) ) ;
#46975=CARTESIAN_POINT ( 'NONE',  ( 2.783473570837506017, 1.621738419858234304, 1.620254553110695772 ) ) ;
#46976=CARTESIAN_POINT ( 'NONE',  ( 0.7151340513122245168, -0.2707656271505008982, 1.805370379145049275 ) ) ;
#46977=CARTESIAN_POINT ( 'NONE',  ( 1.968876373762207255, -1.476028252698018628, 1.215921256797661609 ) ) ;
#46981=CARTESIAN_POINT ( 'NONE',  ( 1.722903956744771481, 1.489010464042400450, -1.355078301658399820 ) ) ;
#46982=CARTESIAN_POINT ( 'NONE',  ( 2.588659458060487584, 1.901619664775334728, 0.4814403318105645591 ) ) ;
#46986=CARTESIAN_POINT ( 'NONE',  ( 4.769523239323490316, 1.203412094891454842, 1.709343392706575315 ) ) ;
#46987=CARTESIAN_POINT ( 'NONE',  ( 3.274023454312132486, -1.055227348164128331, 1.420681018326484413 ) ) ;
#46990=CARTESIAN_POINT ( 'NONE',  ( 6.333931935734662844, 2.266371222927834772, 0.3428166536569366984 ) ) ;
#46991=CARTESIAN_POINT ( 'NONE',  ( 4.470479574576804005, -0.003715868306445029284, -1.740516468156935836 ) ) ;
#46994=CARTESIAN_POINT ( 'NONE',  ( 4.253097392439049607, -1.714905526014463666, -0.2545648513426115311 ) ) ;
#46995=CARTESIAN_POINT ( 'NONE',  ( 4.826735082517537023, -1.421624449711873295, 1.641102681368050487 ) ) ;
#46997=CARTESIAN_POINT ( 'NONE',  ( 5.893767612163585135, -2.000732204962274441, 0.2516274335107801519 ) ) ;
#46998=CARTESIAN_POINT ( 'NONE',  ( 5.625000000000003553, -2.052068128417940951, 3.204627906038193246E-13 ) ) ;
#47001=CARTESIAN_POINT ( 'NONE',  ( 2.731371607455813422, -1.798138232897347644, 0.6916047562727283271 ) ) ;
#47003=CARTESIAN_POINT ( 'NONE',  ( 0.5400543498376106921, -2.107395444675621121, 0.7023712877645065245 ) ) ;
#47005=CARTESIAN_POINT ( 'NONE',  ( 6.883263157960371359, 6.037760411968411844, 2.441088155713948549 ) ) ;
#47008=CARTESIAN_POINT ( 'NONE',  ( 1.506789913206330489, -2.211016841974380309, -0.2134033219785695379 ) ) ;
#47014=CARTESIAN_POINT ( 'NONE',  ( -0.03452862918938356951, -1.956592590566148093, -0.4871966601913205186 ) ) ;
#47016=CARTESIAN_POINT ( 'NONE',  ( 5.072745416573516408, 1.424789591659934684, -1.491725785151225336 ) ) ;
#47021=CARTESIAN_POINT ( 'NONE',  ( 0.2800358821246723418, -1.714356997462190835, -0.4388462949536375279 ) ) ;
#47022=CARTESIAN_POINT ( 'NONE',  ( 5.484916526786003388, -1.734343006517705676, 0.008455456694493946809 ) ) ;
#47023=CARTESIAN_POINT ( 'NONE',  ( 4.897892112245933127, -0.5929259483795108476, -1.636466244661118452 ) ) ;
#47025=CARTESIAN_POINT ( 'NONE',  ( 3.122906911094673887, 0.05843746759831092152, 2.291794357358638123 ) ) ;
#47027=CARTESIAN_POINT ( 'NONE',  ( 1.657894046870052485, -1.302874822933766774, 1.301145727299134025 ) ) ;
#47031=CARTESIAN_POINT ( 'NONE',  ( 2.291784574284541964, -0.7830779901500490858, 1.649245556672715995 ) ) ;
#47032=CARTESIAN_POINT ( 'NONE',  ( 2.338517726396415863, 0.5350873343827439177, -1.944071628254496087 ) ) ;
#47033=CARTESIAN_POINT ( 'NONE',  ( 1.746283639092637729, 0.6896231194409886411, 2.080178558289603963 ) ) ;
#47035=CARTESIAN_POINT ( 'NONE',  ( 4.190527447551747109, -2.082725220463335081, -0.3111483248238402499 ) ) ;
#47038=CARTESIAN_POINT ( 'NONE',  ( 1.416557266959647787, 0.8372786474034592530, 1.893679232998768391 ) ) ;
#47041=CARTESIAN_POINT ( 'NONE',  ( 3.844477943020713440, 1.133112341739877849, -1.792160191984671691 ) ) ;
#47042=CARTESIAN_POINT ( 'NONE',  ( 6.656878040733529289, -1.407521694628325770, 1.162499734694094844 ) ) ;
#47050=CARTESIAN_POINT ( 'NONE',  ( 6.029554895997981667, -0.2579198037528374066, 2.104758538420265168 ) ) ;
#47051=CARTESIAN_POINT ( 'NONE',  ( 0.6398468662271715734, -1.489381099377089512, -1.489160694218383485 ) ) ;
#47054=CARTESIAN_POINT ( 'NONE',  ( 4.926513725511825648, -1.217676453003987191, 1.407301474667689956 ) ) ;
#47060=CARTESIAN_POINT ( 'NONE',  ( 1.890992312513404716, 0.1891058464698439912, 1.952711869325058691 ) ) ;
#47061=CARTESIAN_POINT ( 'NONE',  ( 1.147603855448702248, -1.704515299458901012, -1.329379018566230641 ) ) ;
#47065=CARTESIAN_POINT ( 'NONE',  ( 2.846726617453724906, -0.8940771029739991160, 1.485372309294562543 ) ) ;
#47066=CARTESIAN_POINT ( 'NONE',  ( 2.202700171921621042, -0.3823900931277899318, 1.697618373880743325 ) ) ;
#47067=CARTESIAN_POINT ( 'NONE',  ( 6.727182134110239353, -0.007837387828812587484, 2.289081727344749684 ) ) ;
#47070=CARTESIAN_POINT ( 'NONE',  ( 2.337248977212981860, -1.842284197780035493, 0.9235709308827669828 ) ) ;
#47071=CARTESIAN_POINT ( 'NONE',  ( 0.6497672626537411844, -0.2439889887937417567, -2.001205234435725622 ) ) ;
#47072=CARTESIAN_POINT ( 'NONE',  ( 6.825078400183554272, 2.951006455646578264, 2.596623860847916188 ) ) ;
#47074=CARTESIAN_POINT ( 'NONE',  ( 1.305477374917118016, -0.4809445013957516779, 1.911780493352131183 ) ) ;
#47075=CARTESIAN_POINT ( 'NONE',  ( 5.625241921295836889, 1.689600096388569561, 0.8957793909229803120 ) ) ;
#47080=CARTESIAN_POINT ( 'NONE',  ( 0.6627674568651781284, 0.5885975752501994007, 1.931983969097182063 ) ) ;
#47082=CARTESIAN_POINT ( 'NONE',  ( 5.122255714018879580, -1.229368216938999003, -1.952684467508845056 ) ) ;
#47083=CARTESIAN_POINT ( 'NONE',  ( 5.512146440779991607, 1.959692598237902761, -0.09458084330612320789 ) ) ;
#47084=CARTESIAN_POINT ( 'NONE',  ( 1.657006586592904673, 1.606862555911577006, -1.125131163738995577 ) ) ;
#47088=CARTESIAN_POINT ( 'NONE',  ( 1.112693368687894369, 2.042276985739148731, 0.5586806735067056939 ) ) ;
#47091=CARTESIAN_POINT ( 'NONE',  ( 0.7789528443887736575, 1.234723402293058214, 1.365900241759879119 ) ) ;
#47093=CARTESIAN_POINT ( 'NONE',  ( 4.311506836774354312, -1.801752502381037457, -1.211023186257336404 ) ) ;
#47097=CARTESIAN_POINT ( 'NONE',  ( 1.424255164902767934, -2.103954720533041556, 0.2648648325892372646 ) ) ;
#47102=CARTESIAN_POINT ( 'NONE',  ( 3.093097461593071973, 1.769307450888421673, -1.056303779743078985 ) ) ;
#47104=CARTESIAN_POINT ( 'NONE',  ( 0.5558949066124979632, -1.334021266253348381, 1.269314063962425854 ) ) ;
#47106=CARTESIAN_POINT ( 'NONE',  ( -0.02264175331116376200, 2.864903628641465971, -2.577409799940860946 ) ) ;
#47108=CARTESIAN_POINT ( 'NONE',  ( 0.3994152196779980346, 1.832435997337564348, -1.229551327501000380 ) ) ;
#47109=CARTESIAN_POINT ( 'NONE',  ( 2.091474534086060544, 1.969063197997424686, -1.113951356575371365 ) ) ;
#47111=CARTESIAN_POINT ( 'NONE',  ( 2.302729407678519191, -0.3129977310964130455, -1.784170229015415332 ) ) ;
#47112=CARTESIAN_POINT ( 'NONE',  ( 2.395587962911712498, -1.894220731477358921, 0.2854614921951497686 ) ) ;
#47113=CARTESIAN_POINT ( 'NONE',  ( 3.332542965736586371, -1.235447621225284509, 1.661183390374972424 ) ) ;
#47115=CARTESIAN_POINT ( 'NONE',  ( 1.375784083019690351, 1.172551417808114893, 1.584734682399450145 ) ) ;
#47116=CARTESIAN_POINT ( 'NONE',  ( 6.721331456258776704, -0.1291123375851965516, 1.896827325797964869 ) ) ;
#47117=CARTESIAN_POINT ( 'NONE',  ( 2.535844406030359544, 0.8837261853790435717, -1.648756255988912400 ) ) ;
#47119=CARTESIAN_POINT ( 'NONE',  ( 0.9796492596481393145, -0.06170110713811990943, -2.307032891211552084 ) ) ;
#47121=CARTESIAN_POINT ( 'NONE',  ( 2.910441987356562787, 0.6243205138760847817, 1.753359951907756065 ) ) ;
#47124=CARTESIAN_POINT ( 'NONE',  ( 5.705554990011762584, -1.623920158085298437, -1.271698733341574350 ) ) ;
#47128=CARTESIAN_POINT ( 'NONE',  ( 6.721705546354253435, -2.043712959172855115, 0.5078683761520035311 ) ) ;
#47131=CARTESIAN_POINT ( 'NONE',  ( 5.448557382023540896, 0.6217387762853660016, 2.070273951448368788 ) ) ;
#47132=CARTESIAN_POINT ( 'NONE',  ( -0.07004771093476865051, -1.979950378243084730, 0.3982260095720979165 ) ) ;
#47139=CARTESIAN_POINT ( 'NONE',  ( 4.856657812281613751, -1.900414607462055816, -0.6748505307947461063 ) ) ;
#47143=ADVANCED_BREP_SHAPE_REPRESENTATION ( '', ( #168834, #155333, #158197, #164931, #94059, #158894, #89439, #161027, #24912, #162819, #169543, #162104, #106770, #200407 ), #124915 ) ;
#47145=CARTESIAN_POINT ( 'NONE',  ( 5.682550338946039226, -2.108058120380253087, -0.4779004524640489970 ) ) ;
#47150=CARTESIAN_POINT ( 'NONE',  ( 5.536732523015378327, -1.587826920732600122, 1.242742243127918700 ) ) ;
#47153=CARTESIAN_POINT ( 'NONE',  ( 2.279564191164831666, 1.060311948399524695, 1.360390198354200386 ) ) ;
#47158=CARTESIAN_POINT ( 'NONE',  ( 6.872336254976084469, -1.150436037642876608, 1.475500831757702969 ) ) ;
#47159=CARTESIAN_POINT ( 'NONE',  ( 0.4869769290230832048, -1.896302947978160791, -0.6760925243112311245 ) ) ;
#47161=CARTESIAN_POINT ( 'NONE',  ( 3.135963548190400019, -1.480894843444351849, -1.636267651353009223 ) ) ;
#47162=AXIS2_PLACEMENT_3D ( 'NONE', #92209, #71631, #173449 ) ;
#47163=CARTESIAN_POINT ( 'NONE',  ( 5.928641807120487606, -1.383276364288194893, 1.673324517764721575 ) ) ;
#47168=CARTESIAN_POINT ( 'NONE',  ( 2.684367718930933844, 1.136400967617630986, 1.790090880730066392 ) ) ;
#47169=CARTESIAN_POINT ( 'NONE',  ( 2.214470461757975794, 1.956567829827577931, 0.4871813834786202224 ) ) ;
#47170=CARTESIAN_POINT ( 'NONE',  ( 2.214858347191206445, 1.452946758456060250, -1.081763258146416939 ) ) ;
#47176=CARTESIAN_POINT ( 'NONE',  ( 0.9717394072371825509, -0.8581575513351351603, 1.712793540333819919 ) ) ;
#47184=CARTESIAN_POINT ( 'NONE',  ( 4.926735330553583481, 2.067573386176469796, 0.6309256262674378668 ) ) ;
#47188=CARTESIAN_POINT ( 'NONE',  ( 1.406653384705614629, -2.110883996484512970, -0.2024971186788473154 ) ) ;
#47191=CARTESIAN_POINT ( 'NONE',  ( 3.356668533229437923, -1.495150621271496671, 1.284956859879735402 ) ) ;
#47192=CARTESIAN_POINT ( 'NONE',  ( 5.677967274442059953, 1.882970570262190835, -0.3333453579756898155 ) ) ;
#47194=CARTESIAN_POINT ( 'NONE',  ( 0.1685321339487330372, -0.8835925182541467526, -1.870455940253319183 ) ) ;
#47195=CARTESIAN_POINT ( 'NONE',  ( 2.378764330827160212, 1.775374922424903801, -0.7872989649762071052 ) ) ;
#47200=CARTESIAN_POINT ( 'NONE',  ( 2.677772397998368081, -1.073972967945693080, 1.793542233829773291 ) ) ;
#47203=CARTESIAN_POINT ( 'NONE',  ( 6.445967652843097362, -1.252902786447611883, -1.444740716957277904 ) ) ;
#47205=CARTESIAN_POINT ( 'NONE',  ( 4.811249113497881424, 1.919052844561389692, 1.089612025192594258 ) ) ;
#47206=CARTESIAN_POINT ( 'NONE',  ( 2.696532018272995490, -2.200798769047443759, -0.1632673417703081331 ) ) ;
#47210=CARTESIAN_POINT ( 'NONE',  ( 1.840342752298686380, 1.099902316243700939, -1.564109231055022864 ) ) ;
#47213=CARTESIAN_POINT ( 'NONE',  ( 4.527825515032589898, 2.008996319933327612, -0.4998958796476050681 ) ) ;
#47214=CARTESIAN_POINT ( 'NONE',  ( 1.885829143180400624, 1.490600019384461072, 1.565824011241300440 ) ) ;
#47215=CARTESIAN_POINT ( 'NONE',  ( 5.337503337980974649, 0.8888059580158399475, -2.003405333693850654 ) ) ;
#47221=CARTESIAN_POINT ( 'NONE',  ( 0.7564826839323666174, 1.942540863013635821, -0.5404934282097761944 ) ) ;
#47223=CARTESIAN_POINT ( 'NONE',  ( 5.243061650278370678, -0.2479348644398685908, -2.055265572831247667 ) ) ;
#47224=CARTESIAN_POINT ( 'NONE',  ( 3.334515964829305457, 1.879714267205140565, 0.4213298384171912381 ) ) ;
#47225=CARTESIAN_POINT ( 'NONE',  ( 5.730101960677154160, 2.114805460001396575, 0.1033778851832044821 ) ) ;
#47229=CARTESIAN_POINT ( 'NONE',  ( 4.293777937636614972, -1.355062202172536034, -1.429424366026492033 ) ) ;
#47230=CARTESIAN_POINT ( 'NONE',  ( 5.543040349607136541, -1.804139640619137230, -1.413977440569001542 ) ) ;
#47231=CARTESIAN_POINT ( 'NONE',  ( 4.248545464119923842, 0.4890907236730773766, 1.758887239191930796 ) ) ;
#47239=CARTESIAN_POINT ( 'NONE',  ( 0.9953642579336658969, -1.841430844361633845, 2.783310008858119066E-05 ) ) ;
#47240=CARTESIAN_POINT ( 'NONE',  ( 5.203390118303760303, 1.773417465902687562, -0.9529421280250712778 ) ) ;
#47241=CARTESIAN_POINT ( 'NONE',  ( 6.240923344934847350, 2.292853006454723452, -0.1649963611656188323 ) ) ;
#47242=CARTESIAN_POINT ( 'NONE',  ( 5.084793414397763556, 1.876112756342168675, 0.5732009990792874543 ) ) ;
#47248=CARTESIAN_POINT ( 'NONE',  ( 1.417645169044414288, -1.164320182712182294, -1.736329362061867387 ) ) ;
#47249=CARTESIAN_POINT ( 'NONE',  ( 0.6021629784135495989, -0.6261829430146518272, -1.762877433595814614 ) ) ;
#47251=CARTESIAN_POINT ( 'NONE',  ( 5.771417317170061345, 1.158396453637217993, 1.558476049558398913 ) ) ;
#47252=CARTESIAN_POINT ( 'NONE',  ( -0.2104748580754201015, 7.629137130509078268, -2.703678718140526627 ) ) ;
#47253=CARTESIAN_POINT ( 'NONE',  ( 0.6787880507331369717, 1.167388449615349044, 1.291009837513588998 ) ) ;
#47256=CARTESIAN_POINT ( 'NONE',  ( 1.453258822912409043, 0.5037300415833938505, -1.649688963556243282 ) ) ;
#47257=CARTESIAN_POINT ( 'NONE',  ( 1.997856853652695497, -2.190977152517746163, 0.05759783203293508680 ) ) ;
#47258=CARTESIAN_POINT ( 'NONE',  ( 6.872404467231180369, -0.3655807773644218495, 1.700417682701503841 ) ) ;
#47259=CARTESIAN_POINT ( 'NONE',  ( 4.459734715955371520, 0.4851516707722826061, -2.152740496749529608 ) ) ;
#47261=CARTESIAN_POINT ( 'NONE',  ( 1.657326198882978385, 1.776537685197575822, -1.247748726553777221 ) ) ;
#47262=CARTESIAN_POINT ( 'NONE',  ( 0.4514209555319322331, 0.5758240286459560542, -1.732582669633643047 ) ) ;
#47263=CARTESIAN_POINT ( 'NONE',  ( 1.886098781581479145, -2.116736904955533571, 0.05756534462913154987 ) ) ;
#47265=CARTESIAN_POINT ( 'NONE',  ( 2.947136817621052618, -1.875550406973557349, -1.317825558608209713 ) ) ;
#47268=CARTESIAN_POINT ( 'NONE',  ( 5.057398377711723292, -1.905748072847958108, 1.140992067822230505 ) ) ;
#47277=CARTESIAN_POINT ( 'NONE',  ( 2.496720397819631732, -1.994071314890283553, 0.2986276487200872354 ) ) ;
#47279=CARTESIAN_POINT ( 'NONE',  ( 1.973554268250839350, -0.2567932339846226708, 2.046489673661837205 ) ) ;
#47285=CARTESIAN_POINT ( 'NONE',  ( 4.769572470968366673, 1.260305947291120221, 1.792593939366843303 ) ) ;
#47286=CARTESIAN_POINT ( 'NONE',  ( 2.356092462967720458, 0.09613450340887133572, -2.014232768679749430 ) ) ;
#47287=CARTESIAN_POINT ( 'NONE',  ( 2.682954136603598272, 1.303717545168959990, 1.300458928786947688 ) ) ;
#47289=CARTESIAN_POINT ( 'NONE',  ( 5.174738384962677351, -1.719472664011096219, -0.6136495084824307167 ) ) ;
#47290=CARTESIAN_POINT ( 'NONE',  ( 5.572888750952301073, -0.9041123360693378297, 1.802415994888312722 ) ) ;
#47292=CARTESIAN_POINT ( 'NONE',  ( 5.155258101147136784, -1.908469616433384086, -1.214953784003909520 ) ) ;
#47294=CARTESIAN_POINT ( 'NONE',  ( 0.8562495616285453748, 2.103569811481691865, -0.1051806538951201714 ) ) ;
#47305=CARTESIAN_POINT ( 'NONE',  ( 1.758217466200185042, 0.8068918862002281145, -1.961288232260410380 ) ) ;
#47306=CARTESIAN_POINT ( 'NONE',  ( 2.654761906407083760, 2.205155901917950967, 0.2675573109941364880 ) ) ;
#47310=CARTESIAN_POINT ( 'NONE',  ( 2.998438581075290710, 1.946722116546204306, 0.2428724957088539971 ) ) ;
#47317=CARTESIAN_POINT ( 'NONE',  ( 2.461320219219771843, -1.760565900816572826, 1.181798851529712646 ) ) ;
#47319=CARTESIAN_POINT ( 'NONE',  ( 4.381803836707322652, 1.409801062080328959, 1.638821348427916602 ) ) ;
#47320=CARTESIAN_POINT ( 'NONE',  ( 2.823586671956069605, 1.020774559177588081, -1.532180179759069283 ) ) ;
#47323=CARTESIAN_POINT ( 'NONE',  ( 5.384588317801639157, 1.532214865288351158, -0.8252546180599307224 ) ) ;
#47326=CARTESIAN_POINT ( 'NONE',  ( 2.641676655999642076, -1.601130012699041982, -1.452526871000489495 ) ) ;
#47327=CARTESIAN_POINT ( 'NONE',  ( 4.534529724472468715, 1.956261425488527106, -0.4871295050740409582 ) ) ;
#47330=CARTESIAN_POINT ( 'NONE',  ( 2.448304249002517974, 2.161202317112873139, 0.05382173394478938222 ) ) ;
#47331=CARTESIAN_POINT ( 'NONE',  ( 3.093000238167437743, 1.692540756771460764, -1.010471881233595104 ) ) ;
#47333=CARTESIAN_POINT ( 'NONE',  ( 4.933121067701986995, -1.376026015944699088, -1.370709014919595958 ) ) ;
#47336=ORIENTED_EDGE ( 'NONE', *, *, #176754, .F. ) ;
#47343=CARTESIAN_POINT ( 'NONE',  ( 1.606762454812577179, -0.7948807482080816333, -2.058825234118460745 ) ) ;
#47345=CARTESIAN_POINT ( 'NONE',  ( 4.909014596843685574, -1.577992517845404619, 1.165349624694256958 ) ) ;
#47350=CARTESIAN_POINT ( 'NONE',  ( 4.171694865975253741, -1.058263924308279424, 1.506412014522513720 ) ) ;
#47355=CARTESIAN_POINT ( 'NONE',  ( 5.291314375706784645, -0.05428322906628547939, -2.120082430678168706 ) ) ;
#47359=CARTESIAN_POINT ( 'NONE',  ( 6.380161626619829107, -1.106262522808113324, 1.738493956250926287 ) ) ;
#47361=CARTESIAN_POINT ( 'NONE',  ( 1.592022279046673816, 0.9211323807055901147, -1.617040898905151458 ) ) ;
#47362=CARTESIAN_POINT ( 'NONE',  ( 4.124425300631988200, 0.09459923933386081563, 1.838956108544815171 ) ) ;
#47365=( BOUNDED_CURVE ( )  B_SPLINE_CURVE ( 3, ( #115583, #181577, #182645, #199957 ),
 .UNSPECIFIED., .F., .T. ) 
 B_SPLINE_CURVE_WITH_KNOTS ( ( 4, 4 ),
 ( 0.4999999999999948930, 1.000000000000000000 ),
 .UNSPECIFIED. ) 
 CURVE ( )  GEOMETRIC_REPRESENTATION_ITEM ( )  RATIONAL_B_SPLINE_CURVE ( ( 1.000000000000007327, 0.3333333333333334814, 0.3333333333333266535, 1.000000000000000444 ) ) 
 REPRESENTATION_ITEM ( '' )  );
#47368=CARTESIAN_POINT ( 'NONE',  ( 3.862124860921032354, 2.190326239153097543, -0.2693113811002012525 ) ) ;
#47369=CARTESIAN_POINT ( 'NONE',  ( 6.134080777514242300, 1.123080384508338136, -1.963935940973794869 ) ) ;
#47371=CARTESIAN_POINT ( 'NONE',  ( 5.765820309002536170, 0.5175119463115984697, -1.736122601384345820 ) ) ;
#47372=CARTESIAN_POINT ( 'NONE',  ( 4.786306776965392196, -0.6515362397919061133, -1.801638605214391342 ) ) ;
#47375=CARTESIAN_POINT ( 'NONE',  ( 6.614126560844452385, -0.8839695271746010885, -1.648598838400926692 ) ) ;
#47377=CARTESIAN_POINT ( 'NONE',  ( 5.810971417242416948, -1.466730511752023958, 1.145431029696217573 ) ) ;
#47379=CARTESIAN_POINT ( 'NONE',  ( 6.772329494929559601, -1.084452473627237845, 1.399072979944876449 ) ) ;
#47380=CARTESIAN_POINT ( 'NONE',  ( 1.727750297885573882, 0.7672897036171549834, -1.865047645237365215 ) ) ;
#47382=CARTESIAN_POINT ( 'NONE',  ( 2.490967578435684615, -0.3607690000238995554, -2.074772605841824991 ) ) ;
#47387=CARTESIAN_POINT ( 'NONE',  ( 2.830336888193147882, -0.9990820879247277464, -1.755331475833141308 ) ) ;
#47390=CARTESIAN_POINT ( 'NONE',  ( 3.409602121571019051, -0.4253414365745535886, 2.119164713334599881 ) ) ;
#47395=CARTESIAN_POINT ( 'NONE',  ( 0.6960477194701603088, -1.535568182542995208, -1.535184517522319769 ) ) ;
#47400=CARTESIAN_POINT ( 'NONE',  ( 2.613028500285840661, -0.2118117899099076218, 2.181281865515646068 ) ) ;
#47402=CARTESIAN_POINT ( 'NONE',  ( 2.993345543732395697, 1.941157005910049138, -1.162047774482692697 ) ) ;
#47409=CARTESIAN_POINT ( 'NONE',  ( 2.864225066854100277, -1.223476834174407779, 1.278924851658661099 ) ) ;
#47411=CARTESIAN_POINT ( 'NONE',  ( 5.895608061265788180, 1.667329832391790667, 1.445732890734657161 ) ) ;
#47414=CARTESIAN_POINT ( 'NONE',  ( 5.343375128634678006, 0.3905785925618041610, -1.978055652833633271 ) ) ;
#47416=CARTESIAN_POINT ( 'NONE',  ( 3.889402362484274622, 1.354500474538382626, 1.290456140434749654 ) ) ;
#47417=CARTESIAN_POINT ( 'NONE',  ( 2.975506508543226847, -0.2074491501150333705, 2.059866449969804503 ) ) ;
#47424=CARTESIAN_POINT ( 'NONE',  ( 1.265713261412576562, 0.5522810963098608861, -1.830935845731461953 ) ) ;
#47425=CARTESIAN_POINT ( 'NONE',  ( 3.226955236329264398, -1.811681696138227160, -0.7532884077038404236 ) ) ;
#47426=CARTESIAN_POINT ( 'NONE',  ( 1.335314297916901927, -1.281167425915705316, 1.556668322744148014 ) ) ;
#47431=CARTESIAN_POINT ( 'NONE',  ( 6.397732417105159719, -0.6663202349154914161, 1.855440513692607540 ) ) ;
#47433=CARTESIAN_POINT ( 'NONE',  ( 2.373293634344127767, -1.753592693251155632, -0.9887173157705446691 ) ) ;
#47435=CARTESIAN_POINT ( 'NONE',  ( 2.144302737913783119, 0.9084621246772636161, 1.912570996397492618 ) ) ;
#47437=CARTESIAN_POINT ( 'NONE',  ( 3.367693471486675083, -0.4065805204805824635, 2.029877954327436118 ) ) ;
#47439=CARTESIAN_POINT ( 'NONE',  ( 5.648407305961395508, -1.648567506571393615, 1.285558710341473621 ) ) ;
#47441=CARTESIAN_POINT ( 'NONE',  ( 4.629811725094972630, -1.123643258228578024, -1.438734611599351565 ) ) ;
#47445=CARTESIAN_POINT ( 'NONE',  ( 6.598651186688741177, -0.5821561243712966016, -2.128545807824663960 ) ) ;
#47448=CARTESIAN_POINT ( 'NONE',  ( 5.531871257421491883, -1.864710570029969317, 0.4231498525801706823 ) ) ;
#47456=CARTESIAN_POINT ( 'NONE',  ( 0.3097736896383457839, 1.270387085892955792, -1.333027339516623888 ) ) ;
#47460=CARTESIAN_POINT ( 'NONE',  ( 5.132044594934622062, 0.9627672477196843603, -1.603626212978970900 ) ) ;
#47461=CARTESIAN_POINT ( 'NONE',  ( -0.02299388927988129522, 0.2517100516001030686, -1.946460665317284011 ) ) ;
#47467=CARTESIAN_POINT ( 'NONE',  ( 1.393335261261628988, -1.782783755681414117, 0.8371470673369950655 ) ) ;
#47468=CARTESIAN_POINT ( 'NONE',  ( 2.741814726283864800, 2.006445297011373974, -0.2004551355171620974 ) ) ;
#47474=CARTESIAN_POINT ( 'NONE',  ( 2.976726284633357533, -0.1618151936485581754, -2.185533650236513914 ) ) ;
#47477=CARTESIAN_POINT ( 'NONE',  ( 6.825078400183584471, 2.055285645424239416, 2.261848697290469445 ) ) ;
#47479=EDGE_CURVE ( 'NONE', #111140, #113025, #194086, .T. ) ;
#47486=CARTESIAN_POINT ( 'NONE',  ( 5.038538826285253514, -1.576363729006284187, 0.9512496309353533075 ) ) ;
#47487=CARTESIAN_POINT ( 'NONE',  ( 1.629542719884415680, -0.2443838731654828789, 1.998128341252780604 ) ) ;
#47488=CARTESIAN_POINT ( 'NONE',  ( 2.777091360721035240, -2.273647235919952880, 0.3355521655935486125 ) ) ;
#47489=CARTESIAN_POINT ( 'NONE',  ( -0.1290005225502675879, 2.860092606084875033, -2.662085506130333457 ) ) ;
#47490=CARTESIAN_POINT ( 'NONE',  ( 2.307254945994464457, -1.491077236629720248, -1.113220461199310618 ) ) ;
#47493=CARTESIAN_POINT ( 'NONE',  ( 5.818603510220927255, -0.6945032022064903110, -1.782003016414166474 ) ) ;
#47496=CARTESIAN_POINT ( 'NONE',  ( 4.739831270385728601, 2.085251124590303373, 0.1521322122139453781 ) ) ;
#47497=CARTESIAN_POINT ( 'NONE',  ( 3.414787578387419309, 1.690673485743508619, 0.8009127983473337542 ) ) ;
#47499=CARTESIAN_POINT ( 'NONE',  ( 6.409700764581637067, -0.8744420883355051854, -1.620376909479949390 ) ) ;
#47503=CARTESIAN_POINT ( 'NONE',  ( 5.531808922564334097, -1.099089406413750414, -1.329375763670269883 ) ) ;
#47505=CARTESIAN_POINT ( 'NONE',  ( 0.4395775532227184090, -1.463650450414313520, -0.9296597220836488873 ) ) ;
#47507=CARTESIAN_POINT ( 'NONE',  ( 4.311506836774354312, -1.801752502381037457, -1.211023186257336404 ) ) ;
#47508=CARTESIAN_POINT ( 'NONE',  ( 3.861776535121093090, 1.811678901967550326, -0.2252020330209548171 ) ) ;
#47509=CARTESIAN_POINT ( 'NONE',  ( 1.463640819124707004, -0.4818986642843925972, 1.901505326443528876 ) ) ;
#47510=CARTESIAN_POINT ( 'NONE',  ( 5.911343334927605220, -1.992878553188395463, 0.7155076844978009998 ) ) ;
#47511=CARTESIAN_POINT ( 'NONE',  ( 5.372717881723642286, -0.05365108595901035143, -2.291914610307096201 ) ) ;
#47515=CARTESIAN_POINT ( 'NONE',  ( 2.086737175084628859, -1.302296122868449535, 1.673399772156684895 ) ) ;
#47519=CARTESIAN_POINT ( 'NONE',  ( 6.578989008465588206, 2.022637127319019790, 0.7894149679951308896 ) ) ;
#47520=CARTESIAN_POINT ( 'NONE',  ( 6.983263157960366563, 3.694515354052980260, 2.467960814016751936 ) ) ;
#47522=CARTESIAN_POINT ( 'NONE',  ( 2.860263265526213683, 0.7972832613293324711, -2.073463298260522780 ) ) ;
#47524=CARTESIAN_POINT ( 'NONE',  ( 0.1242335807666505171, 0.4018034787525020524, 2.263199520926823638 ) ) ;
#47526=CARTESIAN_POINT ( 'NONE',  ( 5.577030875653865571, 1.903616248300431746, 0.7944661687919268855 ) ) ;
#47531=CARTESIAN_POINT ( 'NONE',  ( 0.2331563151865486683, 0.2490001740663889407, -1.980811336351681273 ) ) ;
#47532=CARTESIAN_POINT ( 'NONE',  ( 5.003375819710620398, -1.831856422778654681, 0.1858995714831001289 ) ) ;
#47535=CARTESIAN_POINT ( 'NONE',  ( 1.570901180570225542, 0.1317378181442031559, -1.719804994506502149 ) ) ;
#47536=CARTESIAN_POINT ( 'NONE',  ( 1.516814941429758701, 0.2024661778830244008, 2.006371303556075958 ) ) ;
#47537=( BOUNDED_SURFACE ( )  B_SPLINE_SURFACE ( 3, 3, ( 
 ( #81072, #146102, #93081, #63750, #26976, #10724, #159123, #126707, #95213, #195894 ),
 ( #208915, #128833, #113644, #31269, #145046, #96281, #147158, #161262, #76794, #142915 ),
 ( #192669, #160191, #44322, #211048, #97344, #194815, #163401, #64813, #62674, #213183 ),
 ( #127790, #47531, #45391, #14976, #162331, #130959, #46451, #94151, #112573, #13916 ),
 ( #79997, #209979, #110444, #176446, #12849, #212113, #28058, #196949, #111507, #109384 ),
 ( #177513, #11791, #143988, #61621, #164456, #66915, #4056, #48589, #17111, #85337 ),
 ( #133056, #83188, #148220, #136239, #152476, #16043, #184949, #50703, #201195, #118971 ) ),
 .UNSPECIFIED., .T., .F., .T. ) 
 B_SPLINE_SURFACE_WITH_KNOTS ( ( 4, 3, 4 ),
 ( 4, 1, 1, 1, 1, 1, 1, 4 ),
 ( 0.000000000000000000, 0.5000000000000000000, 1.000000000000000000 ),
 ( 0.000000000000000000, 0.09599525230796020214, 0.1893027314675523320, 0.2592390727089966540, 0.3619855251144610819, 0.5211967264240887632, 0.7336899926499302893, 1.000000000000000000 ),
 .UNSPECIFIED. ) 
 GEOMETRIC_REPRESENTATION_ITEM ( )  RATIONAL_B_SPLINE_SURFACE ( (
 ( 1.000000000000000222, 1.000000000000000222, 0.9999999999999997780, 1.000000000000000444, 1.000000000000000222, 1.000000000000000222, 1.000000000000000222, 1.000000000000000222, 1.000000000000000222, 1.000000000000000222),
 ( 0.3333333333333334259, 0.3333333333333334259, 0.3333333333333333148, 0.3333333333333335369, 0.3333333333333334259, 0.3333333333333333703, 0.3333333333333334259, 0.3333333333333333703, 0.3333333333333334259, 0.3333333333333334259),
 ( 0.3333333333333334259, 0.3333333333333334259, 0.3333333333333333148, 0.3333333333333335369, 0.3333333333333334259, 0.3333333333333333703, 0.3333333333333334259, 0.3333333333333333703, 0.3333333333333334259, 0.3333333333333334259),
 ( 1.000000000000000222, 1.000000000000000222, 0.9999999999999997780, 1.000000000000000444, 1.000000000000000222, 1.000000000000000222, 1.000000000000000222, 1.000000000000000222, 1.000000000000000222, 1.000000000000000222),
 ( 0.3333333333333334259, 0.3333333333333334259, 0.3333333333333333148, 0.3333333333333335369, 0.3333333333333334259, 0.3333333333333333703, 0.3333333333333334259, 0.3333333333333333703, 0.3333333333333334259, 0.3333333333333334259),
 ( 0.3333333333333334259, 0.3333333333333334259, 0.3333333333333333148, 0.3333333333333335369, 0.3333333333333334259, 0.3333333333333333703, 0.3333333333333334259, 0.3333333333333333703, 0.3333333333333334259, 0.3333333333333334259),
 ( 1.000000000000000222, 1.000000000000000222, 0.9999999999999997780, 1.000000000000000444, 1.000000000000000222, 1.000000000000000222, 1.000000000000000222, 1.000000000000000222, 1.000000000000000222, 1.000000000000000222) ) ) 
 REPRESENTATION_ITEM ( '' )  SURFACE ( )  );
#47538=CARTESIAN_POINT ( 'NONE',  ( 1.811588643561705680, 1.319210623403826110, -1.882327697243087350 ) ) ;
#47540=CARTESIAN_POINT ( 'NONE',  ( 2.618781011676008852, 1.479506999046651838, -1.711640912222348376 ) ) ;
#47541=CARTESIAN_POINT ( 'NONE',  ( 4.160836958300685673, -1.560740793797481318, 1.414261741400888006 ) ) ;
#47543=CARTESIAN_POINT ( 'NONE',  ( 2.161070758698178107, 0.3078950573750063313, -1.742579939182072657 ) ) ;
#47551=CARTESIAN_POINT ( 'NONE',  ( 5.994412725124051100, -1.189069957525538124, 1.876188141934010956 ) ) ;
#47552=CARTESIAN_POINT ( 'NONE',  ( 2.941561714372803671, 0.7881326131919093037, -2.044999658057600644 ) ) ;
#47555=CARTESIAN_POINT ( 'NONE',  ( 6.516280388114967792, -2.120036885061008292, 0.05137064186952475936 ) ) ;
#47560=CARTESIAN_POINT ( 'NONE',  ( 6.064709079624690524, 0.6667526090060638122, 2.013086243192941716 ) ) ;
#47565=CARTESIAN_POINT ( 'NONE',  ( 6.497600353373155002, -1.840680978339729545, 0.05264081064878384231 ) ) ;
#47569=CARTESIAN_POINT ( 'NONE',  ( 2.489492129562159484, -1.735903792773977772, -0.1261859363600649764 ) ) ;
#47573=FACE_OUTER_BOUND ( 'NONE', #24940, .T. ) ;
#47577=CARTESIAN_POINT ( 'NONE',  ( 5.524359596833869013, 1.291058806671550485, -1.733668313432787933 ) ) ;
#47581=CARTESIAN_POINT ( 'NONE',  ( 6.098895391831223201, 1.613120528903468243, -1.132937624142603905 ) ) ;
#47582=CARTESIAN_POINT ( 'NONE',  ( 5.132092517088904238, 0.1681052705169924777, -1.725677682095213994 ) ) ;
#47584=CARTESIAN_POINT ( 'NONE',  ( 1.909981697816802049, -1.036543071415759298, -1.930953618257096993 ) ) ;
#47585=CARTESIAN_POINT ( 'NONE',  ( 3.136059509142240742, -1.548504943098116593, -1.711042559064612334 ) ) ;
#47586=CARTESIAN_POINT ( 'NONE',  ( 6.450472299244985663, 0.6421947732520795205, 1.958257120725328315 ) ) ;
#47587=CARTESIAN_POINT ( 'NONE',  ( 0.9373250018651816395, 0.7876268737729983371, -1.775224631529322306 ) ) ;
#47591=CARTESIAN_POINT ( 'NONE',  ( 3.674183785563363447, 2.104178206457421485, -0.2630699042918820396 ) ) ;
#47592=CARTESIAN_POINT ( 'NONE',  ( 2.901017702322743919, -0.9963018188003970321, -1.753030416019534021 ) ) ;
#47595=CARTESIAN_POINT ( 'NONE',  ( 5.069440727656137291, 0.2206807655098403653, -2.195719112144229879 ) ) ;
#47598=CARTESIAN_POINT ( 'NONE',  ( 0.06470675514189982991, -1.629034059718449834, -0.8243793580787887043 ) ) ;
#47604=CARTESIAN_POINT ( 'NONE',  ( 4.329017481302106063, 0.09909362218092979124, 2.058626247020868494 ) ) ;
#47609=CARTESIAN_POINT ( 'NONE',  ( 3.914717006531149401, -0.6357662484684013515, -1.917053231858157236 ) ) ;
#47613=CARTESIAN_POINT ( 'NONE',  ( 2.993097573648812126, 1.768379194316849423, -1.058085006197813538 ) ) ;
#47617=CARTESIAN_POINT ( 'NONE',  ( 3.204314817619222211, 1.275555974797081049, -1.561881975048397209 ) ) ;
#47618=CARTESIAN_POINT ( 'NONE',  ( -0.2411972340276022364, 0.7381021182278154624, -1.984382818515282532 ) ) ;
#47619=CARTESIAN_POINT ( 'NONE',  ( 1.851249556194194179, 1.836288347861175785, -0.1344999175661651392 ) ) ;
#47620=CARTESIAN_POINT ( 'NONE',  ( 0.04808971849027363077, -1.788275647358487985, -1.458162290246179715 ) ) ;
#47622=CARTESIAN_POINT ( 'NONE',  ( 2.864712396292764751, -1.492883925411473856, 1.563474562115530375 ) ) ;
#47624=CARTESIAN_POINT ( 'NONE',  ( 1.762908039156896978, -0.1037823317905466058, -2.014007988105172231 ) ) ;
#47626=EDGE_CURVE ( 'NONE', #92893, #126082, #135899, .T. ) ;
#47627=CARTESIAN_POINT ( 'NONE',  ( 2.654040013917441598, -0.3913916837698909745, -2.264681309554557043 ) ) ;
#47630=CARTESIAN_POINT ( 'NONE',  ( 4.118015666179648093, -1.012585719757435498, -1.691412322542594326 ) ) ;
#47631=CARTESIAN_POINT ( 'NONE',  ( 4.716029918043215474, 1.032482702726954527, -1.731993998903176957 ) ) ;
#47635=CARTESIAN_POINT ( 'NONE',  ( 5.883451020920152708, 1.946514763749309429, -0.8046133670899023871 ) ) ;
#47636=CARTESIAN_POINT ( 'NONE',  ( 6.391088794356012848, 0.1989163192229244648, 2.060770550043041993 ) ) ;
#47640=CARTESIAN_POINT ( 'NONE',  ( 6.539320575229290000, 0.004092658091040673150, 2.003502637948690879 ) ) ;
#47641=CARTESIAN_POINT ( 'NONE',  ( 4.328955620115590541, 0.09577655398496780215, 1.969249263103334702 ) ) ;
#47642=CARTESIAN_POINT ( 'NONE',  ( -0.1577409392781377873, -1.310076727147227560, -1.668215054097483385 ) ) ;
#47644=CARTESIAN_POINT ( 'NONE',  ( 4.407023800010228420, 1.785630936674869274, -1.461832730142158088 ) ) ;
#47645=CARTESIAN_POINT ( 'NONE',  ( 1.604420861476773208, 2.060019368494928838, 0.1054051996416793119 ) ) ;
#47653=CARTESIAN_POINT ( 'NONE',  ( 3.772083221923136609, -2.139637338432040181, 0.3678540365955537128 ) ) ;
#47656=CARTESIAN_POINT ( 'NONE',  ( 3.350949008998193257, 0.4442310927498266948, -1.786741727165648497 ) ) ;
#47658=CARTESIAN_POINT ( 'NONE',  ( 5.864808805604324604, 0.1626094438406736342, -2.185560445749204828 ) ) ;
#47660=CARTESIAN_POINT ( 'NONE',  ( 5.735331106285326719, -2.048134886816056266, 0.9616036564972543221 ) ) ;
#47665=CARTESIAN_POINT ( 'NONE',  ( 6.802016525601501051, -1.769270574432443510, 0.04669485764256275928 ) ) ;
#47667=CARTESIAN_POINT ( 'NONE',  ( 3.774091158939500978, 1.997611739970482692, -0.2487840229714877727 ) ) ;
#47669=CARTESIAN_POINT ( 'NONE',  ( 2.643703295229280936, -1.559600718570711031, -1.415347570850413739 ) ) ;
#47670=CARTESIAN_POINT ( 'NONE',  ( 2.267068109148970834, 1.750504415394140922, -0.7784415599910772254 ) ) ;
#47672=CARTESIAN_POINT ( 'NONE',  ( 2.822656803168353434, -1.360269829074612469, 1.424587346448534353 ) ) ;
#47673=CARTESIAN_POINT ( 'NONE',  ( 1.252583056964752029, -1.476889893665521925, 1.148006582770304096 ) ) ;
#47674=CARTESIAN_POINT ( 'NONE',  ( 1.627322669196319849, 0.1476378700930695564, -1.956383933670035713 ) ) ;
#47675=CARTESIAN_POINT ( 'NONE',  ( 3.721100771531059781, -0.1247040890464539975, 1.720429258078775669 ) ) ;
#47676=CARTESIAN_POINT ( 'NONE',  ( 0.3164790345465406385, -0.6463921985436006379, -1.799943259716822341 ) ) ;
#47678=CARTESIAN_POINT ( 'NONE',  ( 1.120068590173186163, -2.152398693614396397, 0.4866647226241942459 ) ) ;
#47684=CARTESIAN_POINT ( 'NONE',  ( 6.649288540346695697, 1.804226486660088558, -1.015068834323729297 ) ) ;
#47685=CARTESIAN_POINT ( 'NONE',  ( 1.117730493923989599, 0.4056601665377962407, -2.030061024271647252 ) ) ;
#47690=CARTESIAN_POINT ( 'NONE',  ( 5.531924462405465981, -2.068776410037334479, 0.4646945096876684556 ) ) ;
#47694=CARTESIAN_POINT ( 'NONE',  ( 6.232861002365865488, -1.862453515449840724, -0.6167318247369477646 ) ) ;
#47696=CARTESIAN_POINT ( 'NONE',  ( 3.761092154037175117, -2.013677596940225190, -0.1017350580494805479 ) ) ;
#47698=CARTESIAN_POINT ( 'NONE',  ( 4.153473468168114913, 1.856699357379907989, -0.4712526737844865976 ) ) ;
#47700=CARTESIAN_POINT ( 'NONE',  ( 1.435386855117400717, -1.590506285900999295, -1.507976327226906443 ) ) ;
#47702=CARTESIAN_POINT ( 'NONE',  ( 4.288257209584379837, -1.849852534125648207, -0.2767368629695772797 ) ) ;
#47706=CARTESIAN_POINT ( 'NONE',  ( 5.431313658478175377, -1.669672585088026517, -1.301796502452344129 ) ) ;
#47708=CARTESIAN_POINT ( 'NONE',  ( 2.278955919255227336, 1.910372346673551602, -0.8499720230255493059 ) ) ;
#47710=CARTESIAN_POINT ( 'NONE',  ( 0.7446035987349702845, -1.482829294443729351, 0.8806902949074472131 ) ) ;
#47711=ORIENTED_EDGE ( 'NONE', *, *, #104171, .T. ) ;
#47722=CARTESIAN_POINT ( 'NONE',  ( 1.594102673003819248, -0.9688845198280521265, 1.530366366333405281 ) ) ;
#47727=CARTESIAN_POINT ( 'NONE',  ( 6.639320575229254118, 4.698690022235154196, 2.459427960261594492 ) ) ;
#47731=CARTESIAN_POINT ( 'NONE',  ( 3.297144150320669542, -1.642529969829407577, 0.8749454559845524226 ) ) ;
#47732=CARTESIAN_POINT ( 'NONE',  ( 0.9486861286592045417, -1.732399544687371229, -0.8177760133930843667 ) ) ;
#47733=CARTESIAN_POINT ( 'NONE',  ( 6.581085459773934332, -0.09550846514571986745, -1.924131155975503216 ) ) ;
#47742=CARTESIAN_POINT ( 'NONE',  ( 4.100420354389649802, 1.959567862165834562, 0.1972540966053982214 ) ) ;
#47743=CARTESIAN_POINT ( 'NONE',  ( 1.770341816056511863, 2.114587264445011883, -0.1591180397043714667 ) ) ;
#47748=CARTESIAN_POINT ( 'NONE',  ( 5.542994302928621053, -1.725804593724251657, -1.350479894307685447 ) ) ;
#47749=CARTESIAN_POINT ( 'NONE',  ( 4.752910067621118451, -1.547527511699481106, 1.147055677608086466 ) ) ;
#47751=CARTESIAN_POINT ( 'NONE',  ( 0.5338675855391886715, 0.9430634504648884864, -1.562995807167219642 ) ) ;
#47752=CARTESIAN_POINT ( 'NONE',  ( 1.436444770134176485, 1.085300811998829662, -1.921501399296850821 ) ) ;
#47759=CARTESIAN_POINT ( 'NONE',  ( 6.772316245210458163, -0.9252316606085030370, -1.738535334629727647 ) ) ;
#47760=CARTESIAN_POINT ( 'NONE',  ( 1.013109794239855699, -1.894405189233986597, 0.4268842903399574507 ) ) ;
#47761=CARTESIAN_POINT ( 'NONE',  ( 0.9134352171796227271, 0.5825640498151598567, 1.930122961472901855 ) ) ;
#47763=CARTESIAN_POINT ( 'NONE',  ( 5.436322145542998641, -1.035505548906799023, 1.546008503351968821 ) ) ;
#47770=CARTESIAN_POINT ( 'NONE',  ( 1.136565065649897344, 0.4323997850379875385, 2.148315308122191514 ) ) ;
#47774=CARTESIAN_POINT ( 'NONE',  ( 1.137010146156680834, -1.651496384925277283, 0.7785749969668461778 ) ) ;
#47778=CARTESIAN_POINT ( 'NONE',  ( 6.609000000000047947, 7.629137130509099585, 2.499999999999994227 ) ) ;
#47780=CARTESIAN_POINT ( 'NONE',  ( 6.375623774462673587, 1.745513195383348926, -0.5351242734627087438 ) ) ;
#47781=CARTESIAN_POINT ( 'NONE',  ( 4.487127722112081329, 0.09209952633786909482, 1.959694304038139379 ) ) ;
#47785=CARTESIAN_POINT ( 'NONE',  ( 4.230150181147958044, 2.149441460308566754, 0.4267382380854707336 ) ) ;
#47788=CARTESIAN_POINT ( 'NONE',  ( 3.942288228968212849, -1.024710522258945655, 1.798826465557185506 ) ) ;
#47791=CARTESIAN_POINT ( 'NONE',  ( 4.096513536321761073, -0.3929280286100769182, 2.264727396410810556 ) ) ;
#47798=CARTESIAN_POINT ( 'NONE',  ( 4.048723784538146298, -1.615201170136868924, -1.077811959465636571 ) ) ;
#47801=CARTESIAN_POINT ( 'NONE',  ( 3.832203377193269755, -0.9874410831685247469, -1.637625244210038300 ) ) ;
#47803=CARTESIAN_POINT ( 'NONE',  ( 5.754863291335100328, -1.356889945763246841, 1.064653683861387812 ) ) ;
#47804=CARTESIAN_POINT ( 'NONE',  ( 4.135954056172497673, 2.015980767636461835, -0.05432360925018697717 ) ) ;
#47805=CARTESIAN_POINT ( 'NONE',  ( 5.379591378607442742, -0.5557209876673010474, -2.230391596181950042 ) ) ;
#47807=CARTESIAN_POINT ( 'NONE',  ( 0.3115100037339203487, 1.922317768103290803, 1.083863418116323807 ) ) ;
#47810=CARTESIAN_POINT ( 'NONE',  ( 5.589024195967314590, 1.560314836579352438, -0.8350092274562578298 ) ) ;
#47812=CARTESIAN_POINT ( 'NONE',  ( 1.799181239640806007, 1.907565883177517740, 1.270813247315852879 ) ) ;
#47813=CARTESIAN_POINT ( 'NONE',  ( 1.341335103225870240, 1.738211624227633978, 0.08822054626196448868 ) ) ;
#47816=CARTESIAN_POINT ( 'NONE',  ( 0.8778075154764168886, -0.2618308253583972456, 1.713820766736633194 ) ) ;
#47820=CARTESIAN_POINT ( 'NONE',  ( 0.9245737983274513461, 1.070221580302813891, 1.888989948743382552 ) ) ;
#47821=CARTESIAN_POINT ( 'NONE',  ( 2.325407997918966796, -1.497503195670712328, -1.350734289967000512 ) ) ;
#47823=CARTESIAN_POINT ( 'NONE',  ( 0.2879446430137333479, -0.9113367411649232475, 1.697199823463049428 ) ) ;
#47825=CARTESIAN_POINT ( 'NONE',  ( 1.969254952099579459, -1.713688747078499830, 1.413451004025434665 ) ) ;
#47833=CARTESIAN_POINT ( 'NONE',  ( 5.477983384163819025, -1.699738153848131983, -0.3734572171999461232 ) ) ;
#47834=CARTESIAN_POINT ( 'NONE',  ( 3.086327779807009009, 1.092107249913790712, -1.629585102321646328 ) ) ;
#47838=CARTESIAN_POINT ( 'NONE',  ( 4.569752015286022484, 2.196007708051894269, -0.5437172964835658151 ) ) ;
#47839=CARTESIAN_POINT ( 'NONE',  ( 1.557159421845564218, 1.687539990290163772, -1.185865425756290392 ) ) ;
#47841=CARTESIAN_POINT ( 'NONE',  ( 2.008995473212730865, 1.676182761729711590, -1.519857458481475909 ) ) ;
#47844=CARTESIAN_POINT ( 'NONE',  ( 2.600682448077856090, 1.504852936121018558, -1.110837741034584436 ) ) ;
#47845=CARTESIAN_POINT ( 'NONE',  ( 1.828352651294574249, 0.6632370903016276964, -1.602517542597500455 ) ) ;
#47846=CARTESIAN_POINT ( 'NONE',  ( 5.126606437771586755, 0.1607948393855564151, 2.185736094377451089 ) ) ;
#47847=CARTESIAN_POINT ( 'NONE',  ( 6.581126798121099242, -0.1039769691308822797, -2.305377512668804751 ) ) ;
#47848=CARTESIAN_POINT ( 'NONE',  ( 4.381803836707322652, 1.409801062080328959, 1.638821348427916602 ) ) ;
#47849=CARTESIAN_POINT ( 'NONE',  ( 4.224509699451983735, 0.09670237001900212903, 1.939662488567380993 ) ) ;
#47851=CARTESIAN_POINT ( 'NONE',  ( 6.503191328365395485, 1.555263205862934983, 1.038959965768880389 ) ) ;
#47852=CARTESIAN_POINT ( 'NONE',  ( 1.750000000000001332, 1.008799782768345906E-13, 2.052068128417951165 ) ) ;
#47857=CARTESIAN_POINT ( 'NONE',  ( 5.572888750952301073, -0.9041123360693378297, 1.802415994888312722 ) ) ;
#47862=CARTESIAN_POINT ( 'NONE',  ( 2.736711336054332921, 0.2235625380298221498, 1.811883384933578256 ) ) ;
#47869=CARTESIAN_POINT ( 'NONE',  ( 0.08815677907929740653, 1.166467155405017442, 1.648690671293622012 ) ) ;
#47870=CARTESIAN_POINT ( 'NONE',  ( 0.9090200710941964690, -0.5189423241485704441, -2.055877189782874481 ) ) ;
#47871=EDGE_LOOP ( 'NONE', ( #181428, #31962, #206862, #88402 ) ) ;
#47874=CARTESIAN_POINT ( 'NONE',  ( 0.1808504484964272296, -2.097240537080494516, -0.5235256853268267507 ) ) ;
#47882=ORIENTED_EDGE ( 'NONE', *, *, #167677, .F. ) ;
#47884=CARTESIAN_POINT ( 'NONE',  ( 5.764999918528635803, -2.016288307888712161, -0.002809016773450134351 ) ) ;
#47885=CARTESIAN_POINT ( 'NONE',  ( 5.033073903806924321, -1.304366766181121573, -1.299653785596634137 ) ) ;
#47886=FACE_OUTER_BOUND ( 'NONE', #30266, .T. ) ;
#47887=CARTESIAN_POINT ( 'NONE',  ( 3.176728247877279365, -1.374524503021319344, 1.853549100471873823 ) ) ;
#47890=CARTESIAN_POINT ( 'NONE',  ( 6.292270065666691892, -2.150519007954437622, -0.2187886337903441336 ) ) ;
#47892=CARTESIAN_POINT ( 'NONE',  ( 1.276788482218065734, 1.793752796627584578, -0.7448022267775021854 ) ) ;
#47896=CARTESIAN_POINT ( 'NONE',  ( 4.991759546967353245, 2.197549137908102246, 0.6733019004761026105 ) ) ;
#47899=CARTESIAN_POINT ( 'NONE',  ( 4.276139911362797363, -1.077190196239918851, 1.529178877381555335 ) ) ;
#47902=CARTESIAN_POINT ( 'NONE',  ( 1.529408426332915960, -0.2309274165002393187, 1.898302859121250297 ) ) ;
#47905=CARTESIAN_POINT ( 'NONE',  ( 2.280145854635793334, 1.358931147977986420, 1.738775483816151768 ) ) ;
#47911=CARTESIAN_POINT ( 'NONE',  ( 2.091034261367350933, 1.717025232345986252, -0.9683794122406997884 ) ) ;
#47912=CARTESIAN_POINT ( 'NONE',  ( 1.694772972888843210, -2.296637362782745218, -0.2246623637925919403 ) ) ;
#47913=CARTESIAN_POINT ( 'NONE',  ( 0.8538673084422104820, -0.7095216264049221122, 1.829241926910141203 ) ) ;
#47914=CARTESIAN_POINT ( 'NONE',  ( 5.401261053844283566, -1.771754184838408630, 1.055722541708886020 ) ) ;
#47921=CARTESIAN_POINT ( 'NONE',  ( 0.3566018059198462486, -2.170557273582163216, -0.05455199461934338162 ) ) ;
#47923=CARTESIAN_POINT ( 'NONE',  ( 5.794452930745782382, 1.501506822132542718, -1.065412412061928160 ) ) ;
#47926=CARTESIAN_POINT ( 'NONE',  ( 1.545950201917587696, 1.868165254341861647, 0.09716206808172561660 ) ) ;
#47927=CARTESIAN_POINT ( 'NONE',  ( 5.729794944320468097, -1.366427417996706417, -1.674954217032841974 ) ) ;
#47929=CARTESIAN_POINT ( 'NONE',  ( -0.02244404828160087226, 1.323617703852699057, -2.440988974267483957 ) ) ;
#47931=CARTESIAN_POINT ( 'NONE',  ( 1.945825403448407487, -1.250168254263404277, -1.447093241409423081 ) ) ;
#47932=CARTESIAN_POINT ( 'NONE',  ( 3.063107849133941851, 0.2611542325122416797, -1.750338901227658894 ) ) ;
#47933=CARTESIAN_POINT ( 'NONE',  ( 1.154776974461441341, 0.3738248154092556064, 1.875208037630435864 ) ) ;
#47935=CARTESIAN_POINT ( 'NONE',  ( 5.431221565750523617, -1.512988070448300970, -1.174818341023081913 ) ) ;
#47936=CARTESIAN_POINT ( 'NONE',  ( 6.725064210944283971, -1.800211566667491825, -0.7994317546313032263 ) ) ;
#47938=CARTESIAN_POINT ( 'NONE',  ( 1.107859837811319581, 1.609452232531217275, 1.380942675281403353 ) ) ;
#47940=CARTESIAN_POINT ( 'NONE',  ( 4.996879044411707937, 1.554903924810165705, -1.039696167511289238 ) ) ;
#47941=CARTESIAN_POINT ( 'NONE',  ( 0.2756506080626683342, 1.048234779247591453, 1.494575289200591239 ) ) ;
#47943=CARTESIAN_POINT ( 'NONE',  ( 4.477303810882872881, 0.001702072213635372200, -2.207063162522747479 ) ) ;
#47946=CARTESIAN_POINT ( 'NONE',  ( 2.225118093709726352, -1.884898904786440177, -0.8381453960227978062 ) ) ;
#47954=CARTESIAN_POINT ( 'NONE',  ( 4.650872726564402981, -0.4503784926754761386, -2.020631409805350387 ) ) ;
#47956=CARTESIAN_POINT ( 'NONE',  ( 1.124558466181435179, 1.288545020775376804, -1.735378439385642180 ) ) ;
#47958=CARTESIAN_POINT ( 'NONE',  ( 2.402995385916364857, -0.3474029756719719808, -1.989407454614970261 ) ) ;
#47965=CARTESIAN_POINT ( 'NONE',  ( 0.2863426850727782136, -0.6839425765656822476, -1.897108587135355684 ) ) ;
#47966=CARTESIAN_POINT ( 'NONE',  ( 5.196902890030515643, 1.791362914573800369, 1.262263373074036688 ) ) ;
#47968=CARTESIAN_POINT ( 'NONE',  ( 5.133030909251353968, 1.769313487831367437, 0.7262901588861517821 ) ) ;
#47972=CARTESIAN_POINT ( 'NONE',  ( 2.126577575561945821, 0.4445254776237593242, 1.966640697269490312 ) ) ;
#47974=CARTESIAN_POINT ( 'NONE',  ( 0.7500711518760843077, 2.289381476473162369, -0.1197363719210968458 ) ) ;
#47976=CARTESIAN_POINT ( 'NONE',  ( 4.524228514566789983, 1.059873738895898310, -1.360581713153318884 ) ) ;
#47977=CARTESIAN_POINT ( 'NONE',  ( -0.1399997263889836974, 2.022132088033218533, -2.415689637818136948 ) ) ;
#47979=CARTESIAN_POINT ( 'NONE',  ( 0.1399997263886003374, 0.002789056014650820314, -1.999853399661279063 ) ) ;
#47982=CARTESIAN_POINT ( 'NONE',  ( 0.4794554595633391259, -0.1051018081165492196, 2.067734805981166435 ) ) ;
#47984=CARTESIAN_POINT ( 'NONE',  ( 5.426340414154960712, -0.8198882401838718526, -1.615393417293700784 ) ) ;
#47988=CARTESIAN_POINT ( 'NONE',  ( 5.883446949022190786, 0.1262479900229801499, -1.807133042791621458 ) ) ;
#47992=CARTESIAN_POINT ( 'NONE',  ( 2.941561714372803227, 0.7881326131919093037, -2.044999658057600644 ) ) ;
#47993=CARTESIAN_POINT ( 'NONE',  ( 5.775803124993572624, -1.815561990025884143, 0.4082129570420859888 ) ) ;
#47995=CARTESIAN_POINT ( 'NONE',  ( 3.532743792504475788, -1.564076696776861120, 1.105682177958314583 ) ) ;
#48000=CARTESIAN_POINT ( 'NONE',  ( 2.430746436576446179, 2.096607243605509208, 0.5259719050795114148 ) ) ;
#48003=CARTESIAN_POINT ( 'NONE',  ( 2.080808903162992607, -0.08653491207171599975, -1.823647505904809174 ) ) ;
#48005=CARTESIAN_POINT ( 'NONE',  ( 3.891465932158610030, 1.322013910284997262, 1.259209046625270556 ) ) ;
#48007=CARTESIAN_POINT ( 'NONE',  ( 2.812653035604309348, -0.5591599321941118639, -1.828790038765286452 ) ) ;
#48009=CARTESIAN_POINT ( 'NONE',  ( 3.877371502699510142, -0.1471681016796568819, 1.964127982587125398 ) ) ;
#48011=CARTESIAN_POINT ( 'NONE',  ( 5.372584366608633921, -0.05174306282297027465, -1.941541108160367513 ) ) ;
#48015=CARTESIAN_POINT ( 'NONE',  ( 5.115537534566190203, 1.735013203181461350, 1.219038288318145646 ) ) ;
#48018=CARTESIAN_POINT ( 'NONE',  ( 2.912652942483742180, -0.5572119909246497915, -1.829279355302193544 ) ) ;
#48023=CARTESIAN_POINT ( 'NONE',  ( 3.826817946245956392, 1.422007987377239546, -1.425180056034919041 ) ) ;
#48025=CARTESIAN_POINT ( 'NONE',  ( 5.496661139185262002, -0.4475443406098400523, -1.769863040007889410 ) ) ;
#48026=CARTESIAN_POINT ( 'NONE',  ( 1.135311898753359472, -0.04898221611688948623, -2.069941200615910581 ) ) ;
#48029=AXIS2_PLACEMENT_3D ( 'NONE', #163124, #27777, #178312 ) ;
#48032=CARTESIAN_POINT ( 'NONE',  ( 5.576977133510579776, -0.04717937999037385977, -1.870219006134994588 ) ) ;
#48042=CARTESIAN_POINT ( 'NONE',  ( 0.8837443060279138729, -1.967007789996034095, 0.6459356165888497925 ) ) ;
#48044=CARTESIAN_POINT ( 'NONE',  ( 1.898220681748989280, -1.001352587523595128, -1.865485677531570685 ) ) ;
#48047=CARTESIAN_POINT ( 'NONE',  ( 0.2390023523631857882, -0.1431304410692470219, -1.937466148627289719 ) ) ;
#48052=CARTESIAN_POINT ( 'NONE',  ( 2.379227630831231011, 2.094957926495308875, -0.9307781363587577239 ) ) ;
#48053=CARTESIAN_POINT ( 'NONE',  ( 0.8557438351849017133, 1.823752217391808150, -0.08689656109241165882 ) ) ;
#48054=CARTESIAN_POINT ( 'NONE',  ( 2.584119536544440265, 1.026460374567798484, 1.613398670029235538 ) ) ;
#48057=CARTESIAN_POINT ( 'NONE',  ( 1.336190909427417139, -1.121870850062630653, -1.671457199112064806 ) ) ;
#48058=CARTESIAN_POINT ( 'NONE',  ( 0.9714493606215730548, -0.2934177832072166758, 1.939591667560663035 ) ) ;
#48062=CARTESIAN_POINT ( 'NONE',  ( 3.363305035154311007, 2.039577031997115597, -0.4584567826917042010 ) ) ;
#48063=CARTESIAN_POINT ( 'NONE',  ( 2.043481384864866524, 0.6806142739823103360, -1.633949198972502570 ) ) ;
#48067=CARTESIAN_POINT ( 'NONE',  ( 5.560555354427807906, -2.070165260436385601, -0.9845844755148360772 ) ) ;
#48068=CARTESIAN_POINT ( 'NONE',  ( 4.277133665768851678, 1.139379310349198260, 1.315593229251702523 ) ) ;
#48070=CARTESIAN_POINT ( 'NONE',  ( -0.1104750535120248289, 7.629137130509052511, -2.703481013110929254 ) ) ;
#48071=CARTESIAN_POINT ( 'NONE',  ( 4.270605845326081784, -1.729236537505800086, 0.1267691526786636214 ) ) ;
#48072=CARTESIAN_POINT ( 'NONE',  ( 4.299414767360295819, -1.890980460948383790, 1.066717558251949471 ) ) ;
#48074=CARTESIAN_POINT ( 'NONE',  ( 6.192592252150040721, 1.490973663936447258, -1.357864438797616868 ) ) ;
#48075=CARTESIAN_POINT ( 'NONE',  ( 0.8125000000000005551, 1.451031289061154306, 1.451031289061088136 ) ) ;
#48077=CARTESIAN_POINT ( 'NONE',  ( 3.188414472400236566, -1.897621675979482614, -0.3308535721826404985 ) ) ;
#48079=CARTESIAN_POINT ( 'NONE',  ( 5.765950734523942245, 0.6451602502356535984, -2.125694943049365904 ) ) ;
#48081=CARTESIAN_POINT ( 'NONE',  ( 6.883263157960402445, -0.003972766660574957552, 2.046037087719229319 ) ) ;
#48084=CARTESIAN_POINT ( 'NONE',  ( 1.436510670779034937, -1.237796341723711002, -1.844280071174006164 ) ) ;
#48092=CARTESIAN_POINT ( 'NONE',  ( 4.562968466866096584, 1.596587869669671145, -1.305994239470360974 ) ) ;
#48096=CARTESIAN_POINT ( 'NONE',  ( 6.503191328365395485, 1.555263205862934983, 1.038959965768880389 ) ) ;
#48097=CARTESIAN_POINT ( 'NONE',  ( 5.326719796100753967, 0.6952390240965979906, -1.588890972402807966 ) ) ;
#48098=CARTESIAN_POINT ( 'NONE',  ( 4.686888010602763721, 1.293897920562389947, 1.164242640570410714 ) ) ;
#48100=CARTESIAN_POINT ( 'NONE',  ( 2.824086921994493071, 1.271197760638997254, -1.907441589200240983 ) ) ;
#48102=CARTESIAN_POINT ( 'NONE',  ( 1.007454599746326895, -0.8259622865525710900, -1.645551850779983116 ) ) ;
#48104=CARTESIAN_POINT ( 'NONE',  ( 1.588595499965880675, -0.2641367610144580991, -1.806243275932853498 ) ) ;
#48105=CARTESIAN_POINT ( 'NONE',  ( 3.199842427594956185, 1.824118962040650604, 0.8596310190432245868 ) ) ;
#48106=CARTESIAN_POINT ( 'NONE',  ( 0.8674257402763450031, 2.111068143204323455, -0.5878430487569612506 ) ) ;
#48108=CARTESIAN_POINT ( 'NONE',  ( 4.085071245346539648, -0.2040513417298230325, -2.096037468315871788 ) ) ;
#48111=CARTESIAN_POINT ( 'NONE',  ( 1.697802635435996743, -1.498143435978617877, -1.429203828351800487 ) ) ;
#48114=CARTESIAN_POINT ( 'NONE',  ( 3.246849895443252532, 2.069243461727567013, 0.4626693848822636124 ) ) ;
#48116=CARTESIAN_POINT ( 'NONE',  ( 6.551389018236878137, -1.469694460105780642, -1.082916835497591324 ) ) ;
#48123=CARTESIAN_POINT ( 'NONE',  ( 3.269790213696788683, 0.4867576797993823368, -1.960144559866239700 ) ) ;
#48124=CARTESIAN_POINT ( 'NONE',  ( 0.8683613728089655259, 1.037855563948440363, 1.832367646046024534 ) ) ;
#48127=CARTESIAN_POINT ( 'NONE',  ( 5.700015841690603935, 0.7557596558054953118, -1.700775360669419145 ) ) ;
#48132=CARTESIAN_POINT ( 'NONE',  ( 6.666874348205719336, -1.883165374045802087, -0.8376701409097894180 ) ) ;
#48136=CARTESIAN_POINT ( 'NONE',  ( 2.670900524536640841, -0.6599870735717223713, -1.603529595030905641 ) ) ;
#48137=CARTESIAN_POINT ( 'NONE',  ( 0.9369944060461411484, 0.7087284392868421490, -1.589666227069729265 ) ) ;
#48139=CARTESIAN_POINT ( 'NONE',  ( 6.340458270854060885, 2.281561288062480486, 0.3456012654466412704 ) ) ;
#48142=CARTESIAN_POINT ( 'NONE',  ( 2.266935757080061897, -1.882882732336080167, -0.8380483592859179209 ) ) ;
#48144=CARTESIAN_POINT ( 'NONE',  ( 1.036482258494644038, 1.943774389176852857, -0.5350038931242264706 ) ) ;
#48145=CARTESIAN_POINT ( 'NONE',  ( 6.925078400183531713, 7.629137130509035636, 2.644348168701659674 ) ) ;
#48147=CARTESIAN_POINT ( 'NONE',  ( 0.6902270635062581761, -1.956280663680696197, -0.2437950987402882630 ) ) ;
#48148=CARTESIAN_POINT ( 'NONE',  ( 4.254103502353132171, 0.8128351696983120434, -1.731171583500931366 ) ) ;
#48150=CARTESIAN_POINT ( 'NONE',  ( 5.777994779145079640, 1.311685685134782231, 1.774619457157788904 ) ) ;
#48155=CARTESIAN_POINT ( 'NONE',  ( 0.5221358870723510348, -2.009748826802790322, 0.2000887155638417791 ) ) ;
#48157=CARTESIAN_POINT ( 'NONE',  ( 4.647712500454345808, -1.780663920513593013, -1.467712336591691313 ) ) ;
#48158=CARTESIAN_POINT ( 'NONE',  ( 5.424254290899477304, 0.9654600744411747648, 1.707767180430696641 ) ) ;
#48159=CARTESIAN_POINT ( 'NONE',  ( 1.516376426791886445, 0.7900930292849810410, 1.795789229542772647 ) ) ;
#48161=CARTESIAN_POINT ( 'NONE',  ( -0.1224325501351306023, -0.4448023855274513272, -1.973852191825019364 ) ) ;
#48163=CARTESIAN_POINT ( 'NONE',  ( 6.350795928397162449, -1.845624747684541989, -0.8128223418941012968 ) ) ;
#48166=CARTESIAN_POINT ( 'NONE',  ( 0.7261896124251127072, 0.1329856088156805560, 1.836402230816103209 ) ) ;
#48168=CARTESIAN_POINT ( 'NONE',  ( 3.801787986034934619, -1.640574847700679628, -1.422045332411596474 ) ) ;
#48170=CARTESIAN_POINT ( 'NONE',  ( 1.529697670087664108, -0.2543295609688834835, 2.105205558366497698 ) ) ;
#48174=CARTESIAN_POINT ( 'NONE',  ( 2.970052003254409545, 1.099468894914462647, 1.742775920482849905 ) ) ;
#48176=CARTESIAN_POINT ( 'NONE',  ( 0.04610459085982108324, -1.479553692838073475, 1.095721268101347734 ) ) ;
#48181=CARTESIAN_POINT ( 'NONE',  ( 0.2412292383832773390, 0.3817025157030576321, 2.173470055567463088 ) ) ;
#48182=CARTESIAN_POINT ( 'NONE',  ( 1.529016648559086811, 2.180303969971490563, 0.6036265194416541302 ) ) ;
#48184=CARTESIAN_POINT ( 'NONE',  ( 1.529274006537587161, -0.2194501901080987971, 1.798134050542072870 ) ) ;
#48186=CARTESIAN_POINT ( 'NONE',  ( 2.360426208626884570, -1.834515764125169257, -0.5519355525325749801 ) ) ;
#48187=CARTESIAN_POINT ( 'NONE',  ( 2.699741690289765295, -1.532448122638006671, -1.392287113214360827 ) ) ;
#48189=CARTESIAN_POINT ( 'NONE',  ( 1.252734725572089536, -1.555569235904795011, 1.211063379650168415 ) ) ;
#48190=CARTESIAN_POINT ( 'NONE',  ( 5.813098442667213206, 1.700071987003290763, 0.9061822306820240813 ) ) ;
#48191=CARTESIAN_POINT ( 'NONE',  ( 1.366329765314050482, 2.272867617333930390, -0.3986118548820920537 ) ) ;
#48194=CARTESIAN_POINT ( 'NONE',  ( 5.336407798562197158, -1.148744492729685707, 1.713005319730724008 ) ) ;
#48197=CARTESIAN_POINT ( 'NONE',  ( 6.071333362910682041, 0.1583771919418910934, -2.100070647415654079 ) ) ;
#48200=CARTESIAN_POINT ( 'NONE',  ( 5.114612887932482366, 1.494710344919391476, -1.561737693111686642 ) ) ;
#48201=CARTESIAN_POINT ( 'NONE',  ( 4.986975786537023225, -1.902434985030461156, -0.6785184294546533490 ) ) ;
#48209=CARTESIAN_POINT ( 'NONE',  ( 3.186732694495420848, 1.586669336078951664, -1.244385354607212335 ) ) ;
#48214=CARTESIAN_POINT ( 'NONE',  ( 5.295850518597075229, -0.7817450549502875656, 2.015575934489414411 ) ) ;
#48219=CARTESIAN_POINT ( 'NONE',  ( 5.413685477598253470, -1.281375732037979942, -1.556898226837098331 ) ) ;
#48221=CARTESIAN_POINT ( 'NONE',  ( 1.330204427372463138, 1.661418051098985327, 0.4633224975721556005 ) ) ;
#48227=CARTESIAN_POINT ( 'NONE',  ( 6.925078400183548588, 0.0006614011395407459748, 1.855452278108092656 ) ) ;
#48228=CARTESIAN_POINT ( 'NONE',  ( 1.330727748098162078, 1.350296381755649922, -1.493239990923441951 ) ) ;
#48230=CARTESIAN_POINT ( 'NONE',  ( 3.346891443098894303, 0.5343612633194516626, 2.140983517310310891 ) ) ;
#48231=CARTESIAN_POINT ( 'NONE',  ( 5.752828983992735346, -0.5200050086436918129, -2.107789999013423454 ) ) ;
#48233=CARTESIAN_POINT ( 'NONE',  ( 2.033984416766075665, -2.056095976692096094, 0.5180656111221926263 ) ) ;
#48234=CARTESIAN_POINT ( 'NONE',  ( 1.704704067347760699, 1.882482151684254923, 0.7231221989368596947 ) ) ;
#48235=CARTESIAN_POINT ( 'NONE',  ( 1.968756957844201239, -1.398423508019512651, 1.151565528817798834 ) ) ;
#48241=CARTESIAN_POINT ( 'NONE',  ( 0.07520289192196588646, 1.421326540713454323, 1.284674935297628773 ) ) ;
#48248=CARTESIAN_POINT ( 'NONE',  ( 4.715790015261832835, -2.120648752638915724, 0.4184459369844309440 ) ) ;
#48251=CARTESIAN_POINT ( 'NONE',  ( 2.144932638433934002, 2.058100890041581810, 0.5106320605416380110 ) ) ;
#48253=CARTESIAN_POINT ( 'NONE',  ( 3.409407428336236556, -0.3879349331968630077, 1.932650128172111126 ) ) ;
#48254=CARTESIAN_POINT ( 'NONE',  ( 5.256085721135645095, 0.7693902824621422498, -1.750971482026221437 ) ) ;
#48257=CARTESIAN_POINT ( 'NONE',  ( 0.9595327444568906294, 1.691550050060253829, 1.193477315110213599 ) ) ;
#48258=CARTESIAN_POINT ( 'NONE',  ( 1.570153368812776229, -1.843976851262040029, -0.6092462720258711162 ) ) ;
#48259=ORIENTED_EDGE ( 'NONE', *, *, #11231, .F. ) ;
#48263=CARTESIAN_POINT ( 'NONE',  ( 2.326223132658828963, 2.028069097222063188, 0.5071170776438630456 ) ) ;
#48268=CARTESIAN_POINT ( 'NONE',  ( 6.111958284735683478, -0.6397702040911549259, 1.802229686255519603 ) ) ;
#48270=CARTESIAN_POINT ( 'NONE',  ( 4.090592613104036879, -2.182713160620152859, -0.3248913242878055385 ) ) ;
#48271=CARTESIAN_POINT ( 'NONE',  ( 1.729795059504362076, -2.077734391967264838, 0.7439406459070622146 ) ) ;
#48273=CARTESIAN_POINT ( 'NONE',  ( 2.121601645288184290, -0.4173985973947492711, 1.866012167355892704 ) ) ;
#48276=CARTESIAN_POINT ( 'NONE',  ( 4.211429588753928144, -1.719575573843845850, -1.152724658989822348 ) ) ;
#48278=CARTESIAN_POINT ( 'NONE',  ( 2.096749907087645415, -0.5762017740289016032, -2.083436276955972222 ) ) ;
#48279=CARTESIAN_POINT ( 'NONE',  ( 3.878626735558046157, -0.2160506499642600997, -2.180900317982924275 ) ) ;
#48286=CARTESIAN_POINT ( 'NONE',  ( 6.574911468446097196, -0.7340051069854407473, 1.570379515389648040 ) ) ;
#48288=CARTESIAN_POINT ( 'NONE',  ( 4.381733404717279790, -1.982624999272282862, 0.5960583376443123749 ) ) ;
#48289=CARTESIAN_POINT ( 'NONE',  ( 3.070836455255634423, -1.780209531678895729, -0.7368423699729318432 ) ) ;
#48290=CARTESIAN_POINT ( 'NONE',  ( 5.325823331840044084, 0.8572517883133590200, -1.936080889991494747 ) ) ;
#48293=CARTESIAN_POINT ( 'NONE',  ( 4.082825143736307005, 1.868653194780546922, 0.6220825103698603975 ) ) ;
#48294=CARTESIAN_POINT ( 'NONE',  ( 6.492113699461491194, -0.6046859696737926226, -2.211003196133090931 ) ) ;
#48295=CARTESIAN_POINT ( 'NONE',  ( 3.949673224339702138, 0.6133576713117369072, -1.719707012317383210 ) ) ;
#48302=CARTESIAN_POINT ( 'NONE',  ( 4.781498422495529255, 0.1932255103699429266, -2.003883580701450562 ) ) ;
#48303=CARTESIAN_POINT ( 'NONE',  ( 0.1580921841808444750, -0.5169658338281759580, -2.248806653996893168 ) ) ;
#48304=CARTESIAN_POINT ( 'NONE',  ( 4.205873059901494848, 0.6649649114027419428, -1.845726756006949909 ) ) ;
#48309=CARTESIAN_POINT ( 'NONE',  ( 0.7321124197560413549, 2.060462595713075995, 0.3535659584654736731 ) ) ;
#48310=CARTESIAN_POINT ( 'NONE',  ( 6.209784286858486269, -1.755916252942066436, 0.2208807251847556830 ) ) ;
#48312=CARTESIAN_POINT ( 'NONE',  ( 6.210880146794990786, -0.2354563166601444379, 1.927560789186753665 ) ) ;
#48313=FACE_OUTER_BOUND ( 'NONE', #166850, .T. ) ;
#48314=CARTESIAN_POINT ( 'NONE',  ( 1.223704041615133464, 1.677047869609141983, 0.4652235607782040372 ) ) ;
#48316=CARTESIAN_POINT ( 'NONE',  ( 0.2333690889706959148, 4.088440985731725874, -2.608190362703251441 ) ) ;
#48317=CARTESIAN_POINT ( 'NONE',  ( 2.156509779666794024, -1.334175267976490664, 1.093223185313265899 ) ) ;
#48318=CARTESIAN_POINT ( 'NONE',  ( 1.734175692058033347, 2.168326105380265378, 0.3173973903456903112 ) ) ;
#48319=CARTESIAN_POINT ( 'NONE',  ( 3.616033620774202983, -2.174319932014677548, 0.3768175846284789743 ) ) ;
#48321=CARTESIAN_POINT ( 'NONE',  ( 1.323347942641838415, -1.961697495959934479, -0.9305402519725998189 ) ) ;
#48323=CARTESIAN_POINT ( 'NONE',  ( 2.747379667311528273, 0.3059357446031922834, -2.094990568135519649 ) ) ;
#48327=CARTESIAN_POINT ( 'NONE',  ( 2.771321709476880280, 2.175846111983824382, -0.7217205603756542409 ) ) ;
#48331=CARTESIAN_POINT ( 'NONE',  ( 4.758541215226599341, 2.215266761731282674, 0.1642064029221591559 ) ) ;
#48339=CARTESIAN_POINT ( 'NONE',  ( 2.707657903872981553, 1.899618770239443366, 0.6767133375917554483 ) ) ;
#48341=CARTESIAN_POINT ( 'NONE',  ( 2.711848548736516040, 0.5542824208455496837, -1.986605816314121808 ) ) ;
#48346=CARTESIAN_POINT ( 'NONE',  ( 4.892620165872568094, 1.823077252308364482, -1.215776859382920794 ) ) ;
#48347=CARTESIAN_POINT ( 'NONE',  ( 2.215470409936692420, 1.956561601830292485, 0.4872017847364697452 ) ) ;
#48348=CARTESIAN_POINT ( 'NONE',  ( 0.9953642579336658969, -1.841430844361633845, 2.783310008858119066E-05 ) ) ;
#48351=CARTESIAN_POINT ( 'NONE',  ( 4.893472065931465664, 1.353474861756031267, 1.225258530246610134 ) ) ;
#48352=CARTESIAN_POINT ( 'NONE',  ( 6.152970239395502361, 1.038990588714868490, 1.728003889287746286 ) ) ;
#48354=CARTESIAN_POINT ( 'NONE',  ( 4.627936124501790260, -1.388401915515205198, -1.786361659577795136 ) ) ;
#48356=CARTESIAN_POINT ( 'NONE',  ( 0.3816453311432427831, 1.964265557344764712, -0.7602060659359122230 ) ) ;
#48358=CARTESIAN_POINT ( 'NONE',  ( 4.879381568908511824, -0.1049739508458477355, 2.067839077007492143 ) ) ;
#48367=CARTESIAN_POINT ( 'NONE',  ( 1.863691559860299884, -1.706161385809309650, -1.259181899442491037 ) ) ;
#48368=CARTESIAN_POINT ( 'NONE',  ( 1.775925898354186572, 0.3739997881802308299, -2.189552662180799913 ) ) ;
#48373=CARTESIAN_POINT ( 'NONE',  ( 3.771884902471400292, -1.933230903833718539, 0.3329965046865584477 ) ) ;
#48379=CARTESIAN_POINT ( 'NONE',  ( 2.197662576721173266, 1.936918166296027977, -0.8637449004969055544 ) ) ;
#48381=CARTESIAN_POINT ( 'NONE',  ( 5.635196431686764207, -0.04651148872366302894, -1.961470878453225763 ) ) ;
#48382=CARTESIAN_POINT ( 'NONE',  ( 3.309602206082487008, -0.4233974974612622066, 2.119663826602156131 ) ) ;
#48383=CARTESIAN_POINT ( 'NONE',  ( 2.841158510722852970, 0.6603703904487292498, -1.718939526767604420 ) ) ;
#48387=CARTESIAN_POINT ( 'NONE',  ( 4.611116368171574109, -1.705915267380184286, 0.3434222965797654181 ) ) ;
#48388=CARTESIAN_POINT ( 'NONE',  ( 6.727182134110209155, 1.290711256955964448, 1.927001067762003972 ) ) ;
#48391=CARTESIAN_POINT ( 'NONE',  ( 2.536181837661064087, 1.019768383293401248, -1.906060392209196763 ) ) ;
#48393=CARTESIAN_POINT ( 'NONE',  ( 4.639999869408336863, 0.002810260262744306969, -2.016288307263448321 ) ) ;
#48395=CARTESIAN_POINT ( 'NONE',  ( 1.850665834824256173, 0.6780317805383448970, 2.052694239800388676 ) ) ;
#48396=CARTESIAN_POINT ( 'NONE',  ( 2.952367129307902793, 0.6606739728568145065, 1.857499748845674370 ) ) ;
#48398=CARTESIAN_POINT ( 'NONE',  ( 3.210425159823264707, 1.756831471361683494, 0.8279855452232912638 ) ) ;
#48409=CARTESIAN_POINT ( 'NONE',  ( 1.466163881440044836, 2.173982691173735216, -0.3780781022180225159 ) ) ;
#48411=CARTESIAN_POINT ( 'NONE',  ( 5.700043108275813175, 0.7984002208856562088, -1.792138013221859394 ) ) ;
#48414=CARTESIAN_POINT ( 'NONE',  ( 0.1745949693968875116, 2.894395776691494060, -2.244452406707102110 ) ) ;
#48415=CARTESIAN_POINT ( 'NONE',  ( 4.699059028873219468, -0.4882365319774860102, 1.775153104902137624 ) ) ;
#48416=ORIENTED_EDGE ( 'NONE', *, *, #193200, .F. ) ;
#48419=CARTESIAN_POINT ( 'NONE',  ( 4.834296457332984076, -1.136628438424293508, -1.790084250976264002 ) ) ;
#48422=CARTESIAN_POINT ( 'NONE',  ( 6.731718603199120743, -1.342629487124985532, -1.563498854789405534 ) ) ;
#48424=CARTESIAN_POINT ( 'NONE',  ( 0.5900176457281476328, 0.9615612750370464701, -1.593262740414502776 ) ) ;
#48425=CARTESIAN_POINT ( 'NONE',  ( 3.473999211503727036, -1.775402473473717935, -0.4878004006634574230 ) ) ;
#48430=CARTESIAN_POINT ( 'NONE',  ( 3.158999515626020216, -1.670948785577108797, 1.441709373268922123 ) ) ;
#48431=CARTESIAN_POINT ( 'NONE',  ( 5.378307924748570557, -1.263187946576078247, 1.876752126472463367 ) ) ;
#48433=CARTESIAN_POINT ( 'NONE',  ( 5.361500737056818622, -1.433101695931580100, -1.108104203189824277 ) ) ;
#48434=CARTESIAN_POINT ( 'NONE',  ( 5.014804717692854297, 0.1473437859633792701, 1.910143238840347868 ) ) ;
#48437=CARTESIAN_POINT ( 'NONE',  ( 6.315307248462690204, -0.2269180964024133385, 1.856785020699961875 ) ) ;
#48438=CARTESIAN_POINT ( 'NONE',  ( 6.180112001919068732, -1.034620502799053599, -1.546732508075428392 ) ) ;
#48440=CARTESIAN_POINT ( 'NONE',  ( 6.385617153790816403, 1.223975321695195184, 1.278628327690333411 ) ) ;
#48441=CARTESIAN_POINT ( 'NONE',  ( 1.130092623156966347, 2.014433208573155110, 0.09411304420373775570 ) ) ;
#48443=CARTESIAN_POINT ( 'NONE',  ( 2.983145545965359080, -0.1552688264333592638, -2.100405815202969873 ) ) ;
#48449=CARTESIAN_POINT ( 'NONE',  ( 2.197526642425628118, 1.844980167888200961, -0.8223984085018556378 ) ) ;
#48453=CARTESIAN_POINT ( 'NONE',  ( 3.743588348364734752, -1.634107004491680115, -1.415051943026650161 ) ) ;
#48454=CARTESIAN_POINT ( 'NONE',  ( 6.890000000000006786, 1.992106636881568305, 2.580154195607385237 ) ) ;
#48461=CARTESIAN_POINT ( 'NONE',  ( 1.540847765565691585, -1.849059859674206496, 1.176127931831471907 ) ) ;
#48463=CARTESIAN_POINT ( 'NONE',  ( 2.202381998968961696, -2.261980054776930427, 0.05578962468580014183 ) ) ;
#48470=CARTESIAN_POINT ( 'NONE',  ( 3.567426164108201903, 1.727176351593662007, -0.3850055527321315507 ) ) ;
#48471=CARTESIAN_POINT ( 'NONE',  ( 0.1476710321905516377, -1.628112296142746995, -1.335496995165935674 ) ) ;
#48475=CARTESIAN_POINT ( 'NONE',  ( 4.622672832840883039, 0.3474877929729481840, 1.986098205159859909 ) ) ;
#48477=CARTESIAN_POINT ( 'NONE',  ( 2.113927203836548419, -0.8795192785214582809, -1.650985937663045577 ) ) ;
#48478=CARTESIAN_POINT ( 'NONE',  ( 3.784089331405198653, -1.229265877060268242, -1.665672133652921660 ) ) ;
#48480=CARTESIAN_POINT ( 'NONE',  ( 2.004032382285144021, -0.8144628449315849394, 1.730399521388835460 ) ) ;
#48484=CARTESIAN_POINT ( 'NONE',  ( 1.564566645345835338, 0.6029492335615972420, 1.814891859350221459 ) ) ;
#48485=CARTESIAN_POINT ( 'NONE',  ( 2.277722772326017608, -1.903703133612335119, 0.4737097981617058862 ) ) ;
#48486=CARTESIAN_POINT ( 'NONE',  ( 0.5091384654962345380, 2.010518347751136137, 0.1511200514899835312 ) ) ;
#48490=CARTESIAN_POINT ( 'NONE',  ( 6.380149230842863339, -1.056690401097816867, 1.664064485322758635 ) ) ;
#48492=CARTESIAN_POINT ( 'NONE',  ( 2.443610342004947533, -1.876944004186463566, 0.7284700530331960078 ) ) ;
#48494=CARTESIAN_POINT ( 'NONE',  ( 2.443091204979094044, -1.843612287508783920, -1.040880819149572201 ) ) ;
#48495=CARTESIAN_POINT ( 'NONE',  ( 4.176279081494421952, -1.061646348645030713, -1.777293304589353085 ) ) ;
#48497=CARTESIAN_POINT ( 'NONE',  ( 5.296857843117306786, 1.708683220140273740, 1.204356289764816568 ) ) ;
#48499=CARTESIAN_POINT ( 'NONE',  ( 3.803562306130504389, -0.5304149723801485639, 1.746809896627635084 ) ) ;
#48507=CARTESIAN_POINT ( 'NONE',  ( 4.740819843082155316, 1.831016553098392619, 0.5515768964349797576 ) ) ;
#48512=DIRECTION ( 'NONE',  ( 1.039099362110107450E-15, 1.000000000000000000, -4.583713267641621330E-32 ) ) ;
#48514=CARTESIAN_POINT ( 'NONE',  ( 0.3625324912872700533, 0.1813134127766780901, -1.832273687604975665 ) ) ;
#48515=ORIENTED_EDGE ( 'NONE', *, *, #6025, .F. ) ;
#48517=CARTESIAN_POINT ( 'NONE',  ( 5.079306140367803479, 1.745876537259077432, -0.6719496041647440299 ) ) ;
#48524=CARTESIAN_POINT ( 'NONE',  ( 0.9011414689646871645, -1.692011168669171672, 1.007586202480597048 ) ) ;
#48525=CARTESIAN_POINT ( 'NONE',  ( 2.319935610374638468, 0.9480221781073931986, -1.779637559903464394 ) ) ;
#48529=CARTESIAN_POINT ( 'NONE',  ( 2.062683196291382082, -2.004346222996217897, -0.8864330828558324438 ) ) ;
#48532=CARTESIAN_POINT ( 'NONE',  ( 6.825078400183548055, 3.702925343214446663, 2.370119418288775925 ) ) ;
#48540=CARTESIAN_POINT ( 'NONE',  ( 4.634224865634020141, 0.3196297827482602050, 1.813140464320086132 ) ) ;
#48541=CARTESIAN_POINT ( 'NONE',  ( 1.822903811843211264, 1.490285103888006280, -1.353523025221949450 ) ) ;
#48543=CARTESIAN_POINT ( 'NONE',  ( 3.550466583917981200, 2.079229874635016184, -0.9797032261932754338 ) ) ;
#48544=CARTESIAN_POINT ( 'NONE',  ( -0.1290005225502641184, 1.996213967822700663, -2.587563282167547385 ) ) ;
#48545=CARTESIAN_POINT ( 'NONE',  ( 1.533807339325540475, 1.103149047995868104, 1.498595216881804859 ) ) ;
#48548=CARTESIAN_POINT ( 'NONE',  ( 5.906500813101932756, -1.903809282439900219, -0.1807861040028224398 ) ) ;
#48551=CARTESIAN_POINT ( 'NONE',  ( 4.722262070665103728, 2.001137821747037915, 0.6055792653000735548 ) ) ;
#48552=CARTESIAN_POINT ( 'NONE',  ( 3.221420234344949840, -1.803205065257794004, 0.4975683872451354683 ) ) ;
#48554=CARTESIAN_POINT ( 'NONE',  ( 5.460457653299121361, -1.667157065227730106, -0.7818181906407914994 ) ) ;
#48557=CARTESIAN_POINT ( 'NONE',  ( 4.600069218058569831, -1.724633479392148949, -0.03822871362766516734 ) ) ;
#48562=CARTESIAN_POINT ( 'NONE',  ( 5.260662464746663325, -0.7247129924745611129, -2.046699161452083526 ) ) ;
#48563=CARTESIAN_POINT ( 'NONE',  ( 3.580510235063854019, -1.759844519496515325, -0.4856381957471164745 ) ) ;
#48564=CARTESIAN_POINT ( 'NONE',  ( 0.6901946996495964548, 1.013433542811643440, -1.679602092450118711 ) ) ;
#48565=CARTESIAN_POINT ( 'NONE',  ( 6.210183267806027807, 1.217293573752244784, -1.732272713164469735 ) ) ;
#48567=CARTESIAN_POINT ( 'NONE',  ( 5.829661053323575537, 1.133102282163217955, -1.992656795126966252 ) ) ;
#48572=CARTESIAN_POINT ( 'NONE',  ( 1.243013918421622455, 2.044566944090483229, 0.5621290157047582614 ) ) ;
#48574=ADVANCED_FACE ( 'NONE', ( #105267 ), #205933, .T. ) ;
#48577=CARTESIAN_POINT ( 'NONE',  ( 6.649308703871936288, 1.893188687436907047, -1.062577851937399620 ) ) ;
#48578=CARTESIAN_POINT ( 'NONE',  ( 6.983263157960363898, 3.684327263089666182, 2.667753665259400275 ) ) ;
#48580=CARTESIAN_POINT ( 'NONE',  ( 2.702056655550812980, 1.572631313784816687, 1.569006521454456848 ) ) ;
#48582=CARTESIAN_POINT ( 'NONE',  ( 5.977185442992979603, -2.006959616289708315, -0.1948445219252663840 ) ) ;
#48584=CARTESIAN_POINT ( 'NONE',  ( 5.067260671706765862, 1.791893645760339826, 1.021364248522889762 ) ) ;
#48589=CARTESIAN_POINT ( 'NONE',  ( 0.1329588055935214119, 5.724880713053031478, -2.439996743105294907 ) ) ;
#48590=CARTESIAN_POINT ( 'NONE',  ( 4.985823801847525161, -1.827980399782932697, -0.2200341325891697619 ) ) ;
#48592=CARTESIAN_POINT ( 'NONE',  ( 1.395042272690392604, 1.302445673786157831, 1.130794771346554928 ) ) ;
#48593=CARTESIAN_POINT ( 'NONE',  ( 0.2160302486270138655, 1.032475520995678853, -1.731998313101141163 ) ) ;
#48594=CARTESIAN_POINT ( 'NONE',  ( 1.899501351379283554, -1.088314401552924249, -2.024763765589305820 ) ) ;
#48596=CARTESIAN_POINT ( 'NONE',  ( 1.318052817733056825, -2.207296558944459974, 0.4957021660386366491 ) ) ;
#48597=CARTESIAN_POINT ( 'NONE',  ( 4.635441201516187881, -1.925843587088198916, 0.8528682856967207959 ) ) ;
#48599=CARTESIAN_POINT ( 'NONE',  ( 2.495042215028328236, 1.364832443287033570, 1.126547774882515673 ) ) ;
#48604=CARTESIAN_POINT ( 'NONE',  ( 6.416288448142412726, -2.220950948806613034, 0.05311210701240512422 ) ) ;
#48605=CARTESIAN_POINT ( 'NONE',  ( 3.380998015235132215, 1.981133383611884735, -0.9370748116589098231 ) ) ;
#48608=CARTESIAN_POINT ( 'NONE',  ( 6.393239817247728496, -0.1034752114322245314, -2.118097640427937911 ) ) ;
#48610=COLOUR_RGB ( '', 0.40784314, 0.44705882, 0.49803922) ;
#48614=CARTESIAN_POINT ( 'NONE',  ( 5.871359616481898414, -1.819694913365289768, -1.088597390283413402 ) ) ;
#48620=CARTESIAN_POINT ( 'NONE',  ( 6.286648950733226826, 1.598451336667701339, -0.9137711784916457969 ) ) ;
#48623=CARTESIAN_POINT ( 'NONE',  ( 1.962089020239773163, -1.591546648218734816, -0.7047476087739585893 ) ) ;
#48627=CARTESIAN_POINT ( 'NONE',  ( 6.069229152942410721, 0.1638285306290178100, -2.155560115052157055 ) ) ;
#48630=CARTESIAN_POINT ( 'NONE',  ( 5.489210439962995736, 1.908424935776025455, -1.015307555102950010 ) ) ;
#48634=CARTESIAN_POINT ( 'NONE',  ( 5.589129042188730523, 1.739749244469630529, -0.9270521019464451618 ) ) ;
#48635=CARTESIAN_POINT ( 'NONE',  ( 4.727759377455642564, -1.549208768551156190, -0.7787371415562751586 ) ) ;
#48637=CARTESIAN_POINT ( 'NONE',  ( 1.417800074541092137, -1.221294057239637576, -1.819523406426680090 ) ) ;
#48638=CARTESIAN_POINT ( 'NONE',  ( 2.907580275951544113, 1.948851909871853749, 1.235431545971882095 ) ) ;
#48639=CARTESIAN_POINT ( 'NONE',  ( 4.956353021003493176, 0.7848952607251434843, 1.905660951107574608 ) ) ;
#48640=CARTESIAN_POINT ( 'NONE',  ( 0.7439598490389126573, 0.5628818913385369438, 1.858577368155549525 ) ) ;
#48645=CARTESIAN_POINT ( 'NONE',  ( 4.324552338190708056, -0.9094542848507057853, -1.915842285305848769 ) ) ;
#48647=CARTESIAN_POINT ( 'NONE',  ( 1.494767762416524093, -2.000856930885573259, 0.2496086726550551249 ) ) ;
#48649=CARTESIAN_POINT ( 'NONE',  ( 4.612475435721691497, -0.9401552641563456492, -1.996616816212187340 ) ) ;
#48656=CARTESIAN_POINT ( 'NONE',  ( 4.205972405791720270, -2.055509729078345948, 0.1495927064073861168 ) ) ;
#48658=UNCERTAINTY_MEASURE_WITH_UNIT (LENGTH_MEASURE( 1.000000000000000082E-05 ), #131175, 'distance_accuracy_value', 'NONE');
#48661=CARTESIAN_POINT ( 'NONE',  ( 2.965494806321045562, -1.652366046825021417, -1.161084516292823832 ) ) ;
#48665=CARTESIAN_POINT ( 'NONE',  ( 3.327077596220921141, 0.04893577929474152155, 2.060475874978876298 ) ) ;
#48668=CARTESIAN_POINT ( 'NONE',  ( -0.1408020194050146334, 2.009929383927198998, -2.515281701100045009 ) ) ;
#48669=CARTESIAN_POINT ( 'NONE',  ( 0.9020086522944226193, 1.395640307904035593, -1.200911154268270664 ) ) ;
#48670=CARTESIAN_POINT ( 'NONE',  ( 0.1007806894988797913, -2.307328790448114120, -0.04970016441883937791 ) ) ;
#48672=CARTESIAN_POINT ( 'NONE',  ( 2.829541668879275829, -2.018026287816252040, 0.7751260729957698548 ) ) ;
#48675=CARTESIAN_POINT ( 'NONE',  ( 1.973842561262352469, -0.8578407463649927456, 1.825077436249371354 ) ) ;
#48676=CARTESIAN_POINT ( 'NONE',  ( 2.566106820329843163, 1.847058390165011721, -1.367687711909180148 ) ) ;
#48678=CARTESIAN_POINT ( 'NONE',  ( 0.5845639792326964290, -0.2246964894469481722, -1.857040431621145959 ) ) ;
#48680=CARTESIAN_POINT ( 'NONE',  ( 4.979350729014382360, 1.839849877434216241, -0.7087157093622028503 ) ) ;
#48681=CARTESIAN_POINT ( 'NONE',  ( 4.346888830327386266, -1.803415170841724979, -0.9023466997552240798 ) ) ;
#48685=CARTESIAN_POINT ( 'NONE',  ( 6.182269030498733997, -1.128069697684991546, 1.778281062836915449 ) ) ;
#48687=CARTESIAN_POINT ( 'NONE',  ( 6.021949436824264978, 2.040384406434097464, -0.3501103912618847014 ) ) ;
#48690=CARTESIAN_POINT ( 'NONE',  ( 6.539320575229236709, 1.252639605590207150, 2.218328189723097754 ) ) ;
#48691=CARTESIAN_POINT ( 'NONE',  ( -0.05226516427493665962, -1.936187138999283297, 0.8653993394739032397 ) ) ;
#48693=CARTESIAN_POINT ( 'NONE',  ( 3.791899867668945490, 1.670594791088287678, 1.592266751676748582 ) ) ;
#48695=CARTESIAN_POINT ( 'NONE',  ( 2.395447240195498484, -1.844268472375994339, 0.9235843863054800096 ) ) ;
#48702=CARTESIAN_POINT ( 'NONE',  ( 4.598189031992506948, 0.9324077545292840385, -1.960920063828344384 ) ) ;
#48705=CARTESIAN_POINT ( 'NONE',  ( 3.368544699895597461, 0.04196216268675251326, -1.840931771443871101 ) ) ;
#48707=CARTESIAN_POINT ( 'NONE',  ( 4.370767597569780172, -0.0006098066561242150270, -2.191739723162715592 ) ) ;
#48709=CARTESIAN_POINT ( 'NONE',  ( 5.524405971769074775, 1.352560167130362867, -1.813582142078016712 ) ) ;
#48715=CARTESIAN_POINT ( 'NONE',  ( 6.626229037604012717, 1.016508351997437165, -1.448449474740549858 ) ) ;
#48716=CARTESIAN_POINT ( 'NONE',  ( 3.738934858379244552, 1.912307379442554689, 0.6292302551485791096 ) ) ;
#48718=CARTESIAN_POINT ( 'NONE',  ( 2.907361098931018795, 1.778370309693329210, 1.127733957892971484 ) ) ;
#48719=CARTESIAN_POINT ( 'NONE',  ( 2.636237813805066388, 0.6479696587880221514, 1.802806680411846774 ) ) ;
#48721=CARTESIAN_POINT ( 'NONE',  ( 3.525798893484650254, 1.922080780809858114, -0.4290687576708405726 ) ) ;
#48722=CARTESIAN_POINT ( 'NONE',  ( 4.957288421310242832, -1.730244549199685400, 1.041802906739682566 ) ) ;
#48723=CARTESIAN_POINT ( 'NONE',  ( 0.4966798268824790252, 1.557709316500059726, -1.035497600327957235 ) ) ;
#48724=CARTESIAN_POINT ( 'NONE',  ( 1.521847698614446687, 1.933392594956625521, -0.3320675068423510345 ) ) ;
#48725=CARTESIAN_POINT ( 'NONE',  ( 0.4395310841842986482, -1.815173276516975243, 0.6020934215927520317 ) ) ;
#48730=CARTESIAN_POINT ( 'NONE',  ( 6.649288223980675205, -1.503899034092891940, -1.112267350887645945 ) ) ;
#48733=CARTESIAN_POINT ( 'NONE',  ( 6.455931442665615805, -0.7031469350025701948, 1.947301169641938223 ) ) ;
#48735=CARTESIAN_POINT ( 'NONE',  ( 0.9419464005683108043, 1.389173191389100337, 1.535309223701806447 ) ) ;
#48740=CARTESIAN_POINT ( 'NONE',  ( 5.215537505735290402, 1.733765862324820439, 1.220609238144418240 ) ) ;
#48745=CARTESIAN_POINT ( 'NONE',  ( 6.039501783790233169, 1.813256598412491982, -0.7494862575098264479 ) ) ;
#48747=CARTESIAN_POINT ( 'NONE',  ( 4.464220131058834085, 1.617570847575640736, 1.203168917025834839 ) ) ;
#48748=CARTESIAN_POINT ( 'NONE',  ( 3.292102688380782460, -0.7811219226253396375, -1.749442990535796438 ) ) ;
#48750=CARTESIAN_POINT ( 'NONE',  ( 1.470551405592795957, -2.082434148983134392, -0.6831980896230758216 ) ) ;
#48752=CARTESIAN_POINT ( 'NONE',  ( 3.180766902908559235, -0.1340872481324743570, -1.865776598943262199 ) ) ;
#48756=CARTESIAN_POINT ( 'NONE',  ( 5.150072296613558365, 1.044590698784592542, 1.841551053096659230 ) ) ;
#48759=CARTESIAN_POINT ( 'NONE',  ( 1.821934285652214935, 1.201201420651318630, -1.711045060523497030 ) ) ;
#48761=CARTESIAN_POINT ( 'NONE',  ( 0.3930057192131968802, 1.272852841813755687, 1.164116782529129868 ) ) ;
#48770=CARTESIAN_POINT ( 'NONE',  ( 1.224954274949443978, 1.597400116765529843, 0.8541874478597778486 ) ) ;
#48775=CARTESIAN_POINT ( 'NONE',  ( 6.539320575229254473, 0.5926322452488984593, 1.950287522085321301 ) ) ;
#48780=CARTESIAN_POINT ( 'NONE',  ( 3.367479257110431945, -0.3654178573793941398, 1.824635806631241808 ) ) ;
#48781=CARTESIAN_POINT ( 'NONE',  ( 0.2455189486357247652, 1.894654674652377135, -0.2817335493821241932 ) ) ;
#48782=CARTESIAN_POINT ( 'NONE',  ( 6.458035534591947346, 1.921153000004784284, -0.1426463852419664891 ) ) ;
#48783=CARTESIAN_POINT ( 'NONE',  ( 6.795378861676105053, -1.851214886592133846, 0.9271815693319698237 ) ) ;
#48788=CARTESIAN_POINT ( 'NONE',  ( 4.504722179138310523, 0.5213129852876841053, 1.899149332505256638 ) ) ;
#48789=CARTESIAN_POINT ( 'NONE',  ( 1.559403367407938390, -1.789607135292633266, 1.137164086494051096 ) ) ;
#48793=CARTESIAN_POINT ( 'NONE',  ( 6.263654578238285531, 1.123272483274835087, 1.881548979392036802 ) ) ;
#48795=CARTESIAN_POINT ( 'NONE',  ( 4.172816426537079515, -1.797186248846779133, -0.6940461778226751921 ) ) ;
#48797=CARTESIAN_POINT ( 'NONE',  ( 0.9267433102794274680, 1.311770220233858586, -1.774563083084364834 ) ) ;
#48799=CARTESIAN_POINT ( 'NONE',  ( 0.2285749388857594433, 1.317234250586714284, -1.386657971642536014 ) ) ;
#48803=CARTESIAN_POINT ( 'NONE',  ( 6.034039001082764919, 1.170257472284089717, 1.583912470002272199 ) ) ;
#48804=CARTESIAN_POINT ( 'NONE',  ( 1.241630701082994559, 1.939900434848752964, 0.09377332689292780521 ) ) ;
#48805=CARTESIAN_POINT ( 'NONE',  ( 6.626320313634256109, 0.4032262605214493312, -2.262638539848499164 ) ) ;
#48807=CARTESIAN_POINT ( 'NONE',  ( 5.647250314520869452, 1.642094101250504146, -0.8754911610409812361 ) ) ;
#48813=CARTESIAN_POINT ( 'NONE',  ( 1.558417602779540889, -1.546676288433556756, 1.552911753681482487 ) ) ;
#48818=CARTESIAN_POINT ( 'NONE',  ( 1.453431991042982041, 0.5316948868413253759, -1.746555546766684675 ) ) ;
#48821=CARTESIAN_POINT ( 'NONE',  ( 6.609000000000005315, 2.959011640422835487, 2.552823073452652913 ) ) ;
#48823=CARTESIAN_POINT ( 'NONE',  ( 6.340460056601358474, 1.806591233369018834, 0.2625940548972791611 ) ) ;
#48824=CARTESIAN_POINT ( 'NONE',  ( 4.399235598239510381, -1.708881994454291675, 0.9632455365647660805 ) ) ;
#48828=CARTESIAN_POINT ( 'NONE',  ( 4.899148033862871898, -0.2601683324335196668, -2.104413843559429065 ) ) ;
#48829=CARTESIAN_POINT ( 'NONE',  ( 3.632539538618652752, 0.3231117836275976818, 2.167502126216628522 ) ) ;
#48832=CARTESIAN_POINT ( 'NONE',  ( 3.168866831888625946, 1.502704456927813403, -1.424286459396295390 ) ) ;
#48836=CARTESIAN_POINT ( 'NONE',  ( 3.164923336591000336, 1.459680849325554197, 1.775737417650694816 ) ) ;
#48840=CARTESIAN_POINT ( 'NONE',  ( 6.720655732516647163, 0.005566325962592238996, 1.826293863978686982 ) ) ;
#48842=CARTESIAN_POINT ( 'NONE',  ( 3.257691520677992614, 0.8739490649069777684, 1.734254922796226506 ) ) ;
#48846=CARTESIAN_POINT ( 'NONE',  ( 4.341997288149157086, -1.180789491531178292, -1.504210074635865757 ) ) ;
#48848=CARTESIAN_POINT ( 'NONE',  ( 5.385687109042746279, 1.161108558237003985, 1.275598767315838211 ) ) ;
#48849=CARTESIAN_POINT ( 'NONE',  ( 3.274625289317079524, -0.3981104328964027994, -1.976669913042613747 ) ) ;
#48850=CARTESIAN_POINT ( 'NONE',  ( 5.344470762249110329, 0.4509167475243852086, -2.253899259558800772 ) ) ;
#48852=CARTESIAN_POINT ( 'NONE',  ( 0.9970219447392356660, -0.5395372827587068265, -2.139793933917451874 ) ) ;
#48854=CARTESIAN_POINT ( 'NONE',  ( 5.800005483916761406, -1.769921774263127912, 0.001416880316495658159 ) ) ;
#48856=CARTESIAN_POINT ( 'NONE',  ( 1.904612379804408118, 1.696638126304336858, -1.541566781129146912 ) ) ;
#48857=CARTESIAN_POINT ( 'NONE',  ( 0.7084657485305994040, -0.2594935844701939387, 1.720731466566546519 ) ) ;
#48863=CARTESIAN_POINT ( 'NONE',  ( 1.364001086256797945, -0.5279541034660294452, 2.105878793243611824 ) ) ;
#48864=CARTESIAN_POINT ( 'NONE',  ( 2.413296319342159713, -1.879803466158457059, 0.7303082167480907660 ) ) ;
#48866=CARTESIAN_POINT ( 'NONE',  ( 5.637312448503878137, -1.740617781635974248, 0.8259078106758013238 ) ) ;
#48868=CARTESIAN_POINT ( 'NONE',  ( 2.602056794214495650, 1.574129494629309622, 1.567664267292529612 ) ) ;
#48873=CARTESIAN_POINT ( 'NONE',  ( 5.407646374456077432, -0.7895141955979433357, -1.551160667784831748 ) ) ;
#48875=CARTESIAN_POINT ( 'NONE',  ( 3.103904542773823660, 0.7086415210641981988, -1.829580771271981154 ) ) ;
#48879=CARTESIAN_POINT ( 'NONE',  ( 4.481858567196604248, 1.473221693029845181, 1.717120190082993103 ) ) ;
#48880=CARTESIAN_POINT ( 'NONE',  ( 0.8188879582939897483, -1.495318261269963589, 1.421039783695568604 ) ) ;
#48883=CARTESIAN_POINT ( 'NONE',  ( 2.219920553356643289, -2.194584817558010936, 0.5498286310916412623 ) ) ;
#48886=CARTESIAN_POINT ( 'NONE',  ( 2.583089905966722277, 1.711919019956799737, -0.7542334906679578621 ) ) ;
#48887=CARTESIAN_POINT ( 'NONE',  ( 1.195528834012358210, 1.529115512818737699, 0.8178816217611245554 ) ) ;
#48888=CARTESIAN_POINT ( 'NONE',  ( 4.880524338131243312, -0.2681524694418158661, -2.175044001020635331 ) ) ;
#48889=CARTESIAN_POINT ( 'NONE',  ( 6.387736634265912983, 1.584785628913528699, 1.677562689604541468 ) ) ;
#48890=CARTESIAN_POINT ( 'NONE',  ( 1.674756777405971064, -1.956562173829911044, -0.6475767382677873885 ) ) ;
#48891=CARTESIAN_POINT ( 'NONE',  ( 4.593657693847520207, -1.941558278569108120, -0.04622955632663238584 ) ) ;
#48893=CARTESIAN_POINT ( 'NONE',  ( 6.415307259278708152, -0.2288938695442776505, 1.856442058181500654 ) ) ;
#48894=CARTESIAN_POINT ( 'NONE',  ( 1.062500000000000888, -1.451031289061164742, -1.451031289061077922 ) ) ;
#48896=CARTESIAN_POINT ( 'NONE',  ( 6.257185446134499784, -2.006139278912861368, -0.2004013049526700285 ) ) ;
#48900=CARTESIAN_POINT ( 'NONE',  ( 5.836564609439236939, 0.5826586670559866787, -1.930416874340326938 ) ) ;
#48904=CARTESIAN_POINT ( 'NONE',  ( 2.051128252772801641, -1.465761996925791122, -1.088229512710245261 ) ) ;
#48912=CARTESIAN_POINT ( 'NONE',  ( -0.1579319072057436268, -1.246015270063109748, -1.590120154594099278 ) ) ;
#48913=CARTESIAN_POINT ( 'NONE',  ( 0.3113914200543760336, 1.760583737686383321, -1.181573663439141830 ) ) ;
#48917=CARTESIAN_POINT ( 'NONE',  ( 6.192271402255323132, -2.050732637037344208, -0.2044092671329711397 ) ) ;
#48918=CARTESIAN_POINT ( 'NONE',  ( 5.397111353752316987, -0.9091427841607623295, -1.799923777076550824 ) ) ;
#48929=CARTESIAN_POINT ( 'NONE',  ( 4.710314442360476583, -1.556670644073439913, -1.281164596596932936 ) ) ;
#48930=CARTESIAN_POINT ( 'NONE',  ( 4.822110771479974467, 1.762745816080556915, 0.5315184756640098929 ) ) ;
#48932=CARTESIAN_POINT ( 'NONE',  ( 0.07661050522433668353, 0.008287133257128471639, -1.710863442170395432 ) ) ;
#48933=CARTESIAN_POINT ( 'NONE',  ( 3.071242857908276669, -2.132312958082840826, -0.8828933859421483898 ) ) ;
#48935=CARTESIAN_POINT ( 'NONE',  ( 6.309879873373573922, -2.146112031266556919, 0.2576265230809087758 ) ) ;
#48937=CARTESIAN_POINT ( 'NONE',  ( 1.311946287462633309, 1.302956792059128066, -1.440285294924074311 ) ) ;
#48940=CARTESIAN_POINT ( 'NONE',  ( 4.253462032731039066, -2.272626950162641268, -0.3425954598320450906 ) ) ;
#48943=CARTESIAN_POINT ( 'NONE',  ( 3.115926070338378207, -0.9207206926411042325, -1.628290677324291780 ) ) ;
#48944=CARTESIAN_POINT ( 'NONE',  ( 0.8262462788446511830, -0.8622288892402606431, -1.707089296137359158 ) ) ;
#48948=CARTESIAN_POINT ( 'NONE',  ( 2.385638622766753425, 2.017150886971270651, -0.8956362484653990208 ) ) ;
#48950=CARTESIAN_POINT ( 'NONE',  ( 6.983263157960372780, 7.052928845687945980, 2.444341994195888379 ) ) ;
#48955=CARTESIAN_POINT ( 'NONE',  ( 0.6496080044469240145, 0.6224236735355732630, -1.870565628188630702 ) ) ;
#48956=CARTESIAN_POINT ( 'NONE',  ( 1.114821240386947965, -1.040235440384199794, -2.059874970276051265 ) ) ;
#48957=CARTESIAN_POINT ( 'NONE',  ( 1.574581288703358339, 1.320057194528483135, -1.451483715152704246 ) ) ;
#48958=CARTESIAN_POINT ( 'NONE',  ( 4.996965725392733759, 0.3474287616172208604, 2.032942699294958633 ) ) ;
#48965=CARTESIAN_POINT ( 'NONE',  ( 0.9718041211803396529, -0.3205511010368928271, 2.147183668106082521 ) ) ;
#48967=CARTESIAN_POINT ( 'NONE',  ( 6.304252605626877504, 1.359535501544101077, -1.241908024382516240 ) ) ;
#48971=CARTESIAN_POINT ( 'NONE',  ( 1.458040028222376439, 0.7530789129696242590, 1.712431740859089668 ) ) ;
#48972=CARTESIAN_POINT ( 'NONE',  ( 5.202478051755599964, -0.7228594145181690411, -2.037298988101433839 ) ) ;
#48974=CARTESIAN_POINT ( 'NONE',  ( -0.02244404828160087226, 1.995160441984781041, -2.602654351998904492 ) ) ;
#48976=CARTESIAN_POINT ( 'NONE',  ( 1.682132150489405564, 0.9841149911452107268, 1.639481845682550398 ) ) ;
#48977=CARTESIAN_POINT ( 'NONE',  ( 3.397073482672040345, 1.394525624090914961, 1.089649698571172776 ) ) ;
#48978=CARTESIAN_POINT ( 'NONE',  ( 0.9086806230526077721, -0.4651930584498394916, -1.854694524013176693 ) ) ;
#48980=CARTESIAN_POINT ( 'NONE',  ( 5.308173953863717820, 1.137349973717050267, -1.541276042019421810 ) ) ;
#48982=CARTESIAN_POINT ( 'NONE',  ( 6.162556002056702731, -0.7074686763054702787, -1.838295890583282022 ) ) ;
#48984=CARTESIAN_POINT ( 'NONE',  ( 0.7738737444688469358, 0.4079195088417563730, -2.080830740624163955 ) ) ;
#48986=CARTESIAN_POINT ( 'NONE',  ( 4.293723057671197552, -0.7160966649314598476, 1.728361679364013748 ) ) ;
#48987=CARTESIAN_POINT ( 'NONE',  ( 0.6096330727367264002, -1.817201089070449971, 0.1759225495863714350 ) ) ;
#48989=CARTESIAN_POINT ( 'NONE',  ( 4.547634279845023109, -1.704780727694398479, -1.401453192282381188 ) ) ;
#48992=CARTESIAN_POINT ( 'NONE',  ( 1.609910828531309956, 0.6006481715085715267, -1.973267531027416810 ) ) ;
#49000=CARTESIAN_POINT ( 'NONE',  ( 4.141125838365485201, -0.1998502692034490602, -2.060677327190631569 ) ) ;
#49002=CARTESIAN_POINT ( 'NONE',  ( 1.229993901927586286, -1.370328181169593096, -1.671761099108048265 ) ) ;
#49004=CARTESIAN_POINT ( 'NONE',  ( 1.699873857359509799, 1.394438142870989772, 1.461265194366095033 ) ) ;
#49009=CARTESIAN_POINT ( 'NONE',  ( 6.883263157960391787, 1.253787318140922480, 2.167784446185747171 ) ) ;
#49010=CARTESIAN_POINT ( 'NONE',  ( 0.4269707148552639997, -1.727061408318403712, 1.040797348915108111 ) ) ;
#49011=CARTESIAN_POINT ( 'NONE',  ( 4.687173145698103838, 1.624054394666199830, 1.471728111018810070 ) ) ;
#49013=CARTESIAN_POINT ( 'NONE',  ( 3.673993457511486760, 1.897360377298975331, -0.2389773157873422149 ) ) ;
#49017=CARTESIAN_POINT ( 'NONE',  ( 1.862907868837269998, -0.1017702599966328891, -2.013986063733465226 ) ) ;
#49019=CARTESIAN_POINT ( 'NONE',  ( 0.6797070353673840826, 1.544897314466355143, 1.693757226825955753 ) ) ;
#49021=CARTESIAN_POINT ( 'NONE',  ( 3.926516724862822993, 1.637815149125703584, 0.5408920155725772672 ) ) ;
#49027=CARTESIAN_POINT ( 'NONE',  ( 0.1751657365761704888, 2.870293503558702497, -2.532510806204853804 ) ) ;
#49031=CARTESIAN_POINT ( 'NONE',  ( 5.127533414443554705, -0.2600442617171055404, 1.792572003776324197 ) ) ;
#49035=CARTESIAN_POINT ( 'NONE',  ( 5.602179418825736334, -0.8085942178241835032, 1.621059995222628780 ) ) ;
#49038=CARTESIAN_POINT ( 'NONE',  ( 2.765787700092982693, 1.173089151190203294, 1.850848517565194751 ) ) ;
#49040=CARTESIAN_POINT ( 'NONE',  ( 6.496546432963370421, 1.840999872533972903, 0.2716635292502044829 ) ) ;
#49042=CARTESIAN_POINT ( 'NONE',  ( 4.130425774021486696, 0.5146700378890654015, 1.845081245478853216 ) ) ;
#49048=CARTESIAN_POINT ( 'NONE',  ( 6.104719058799578768, 1.976458628850938704, 0.7599229572291065216 ) ) ;
#49049=CARTESIAN_POINT ( 'NONE',  ( 1.288190726105652217, -0.9714702286227733241, 1.931199087792371261 ) ) ;
#49052=CARTESIAN_POINT ( 'NONE',  ( 1.008509592878764183, 1.385430265305506170, -1.188947219173806413 ) ) ;
#49054=CARTESIAN_POINT ( 'NONE',  ( 3.803562306130504389, -0.5304149723801485639, 1.746809896627635084 ) ) ;
#49056=CARTESIAN_POINT ( 'NONE',  ( 2.584119536544440265, 1.026460374567798484, 1.613398670029235538 ) ) ;
#49058=CARTESIAN_POINT ( 'NONE',  ( 2.611712457634679296, 0.5281755657932221126, -1.897318813625125777 ) ) ;
#49060=CARTESIAN_POINT ( 'NONE',  ( 4.423342042002774477, -1.197376356234590933, -1.528922412636232631 ) ) ;
#49063=CARTESIAN_POINT ( 'NONE',  ( 5.836213162209912930, -1.179542664122106510, -1.762073437084572314 ) ) ;
#49065=CARTESIAN_POINT ( 'NONE',  ( 3.176317266091326807, 0.8619891151622931513, 1.707069686517001195 ) ) ;
#49071=CARTESIAN_POINT ( 'NONE',  ( 4.055341430421886884, -1.750343679372264205, 0.9943053665309193878 ) ) ;
#49073=CARTESIAN_POINT ( 'NONE',  ( 4.828627627824715773, 1.747987318788373656, 0.5269492854979712648 ) ) ;
#49074=CARTESIAN_POINT ( 'NONE',  ( 0.5200892513525963157, 2.048054262204841880, -0.3022008342252607838 ) ) ;
#49078=CARTESIAN_POINT ( 'NONE',  ( 5.612129163471575310, -0.8422657237196762292, -1.670366365510121742 ) ) ;
#49088=CARTESIAN_POINT ( 'NONE',  ( 0.8485890540621650047, -2.054197865963180547, -0.2570499307305574299 ) ) ;
#49089=CARTESIAN_POINT ( 'NONE',  ( 2.390374844762462203, -0.8132668539616545456, -1.954994498336021458 ) ) ;
#49092=CARTESIAN_POINT ( 'NONE',  ( 6.561392567526037389, 1.717850402480676664, 1.155108059606273052 ) ) ;
#49097=CARTESIAN_POINT ( 'NONE',  ( 2.115536061532933942, -2.222870945405757137, 0.5592890022133433225 ) ) ;
#49100=CARTESIAN_POINT ( 'NONE',  ( 2.214975196874233720, 1.533708969217022933, -1.142120075431733994 ) ) ;
#49103=EDGE_CURVE ( 'NONE', #30003, #35846, #65223, .T. ) ;
#49104=CARTESIAN_POINT ( 'NONE',  ( 0.4748584900105623507, -1.455329053371579695, 1.391259960792426975 ) ) ;
#49105=CARTESIAN_POINT ( 'NONE',  ( 1.252704021237858401, -0.4712815170893420724, -1.904206577484176321 ) ) ;
#49110=CARTESIAN_POINT ( 'NONE',  ( 3.662131271747073757, -1.403999256393541284, 1.549221476816674548 ) ) ;
#49111=CARTESIAN_POINT ( 'NONE',  ( 2.359889027365429826, 0.7540158325645224258, 1.601324458166239806 ) ) ;
#49114=CARTESIAN_POINT ( 'NONE',  ( 4.787240309336779909, 1.696446081987776022, 1.541789747812449818 ) ) ;
#49115=CARTESIAN_POINT ( 'NONE',  ( 4.241972025877470465, 0.4673694910880517583, 1.676319072879989047 ) ) ;
#49120=CARTESIAN_POINT ( 'NONE',  ( 4.042145929572971141, 1.632826047920731050, -0.5835893337435077433 ) ) ;
#49121=CARTESIAN_POINT ( 'NONE',  ( 5.002462566363424123, 2.165002515946230499, 0.1647018997421762776 ) ) ;
#49123=CARTESIAN_POINT ( 'NONE',  ( 6.051970301643104122, 1.040788372175960541, 1.727066800951609249 ) ) ;
#49124=CARTESIAN_POINT ( 'NONE',  ( 6.625000595499368039, -2.052053476427456502, 3.646059517245236328E-13 ) ) ;
#49126=CARTESIAN_POINT ( 'NONE',  ( 2.098540742119249458, -0.5114569845777928725, -1.857200404858405207 ) ) ;
#49128=CARTESIAN_POINT ( 'NONE',  ( 5.572587854402127228, 0.9002147710611071441, 2.031021293335387501 ) ) ;
#49130=CARTESIAN_POINT ( 'NONE',  ( 6.983263157960370116, 2.036707217602062414, 2.350489458799970066 ) ) ;
#49133=CARTESIAN_POINT ( 'NONE',  ( 1.805654246593148660, 1.930672025830199479, -1.098395813934008425 ) ) ;
#49134=CARTESIAN_POINT ( 'NONE',  ( 6.637165056451467038, -0.09505199798197358496, -1.959668910398344233 ) ) ;
#49139=CARTESIAN_POINT ( 'NONE',  ( -0.1341500063891595818, -0.1486117279969369209, -1.983907055413631992 ) ) ;
#49141=CARTESIAN_POINT ( 'NONE',  ( 4.686014676054621297, -1.266354490919174403, -1.628128356427221313 ) ) ;
#49145=CARTESIAN_POINT ( 'NONE',  ( 5.835183367072669824, -1.691281831231405963, 0.7993005984755219284 ) ) ;
#49146=CARTESIAN_POINT ( 'NONE',  ( 5.045445647265833777, -1.250780835746621245, 1.201444140469201782 ) ) ;
#49147=CARTESIAN_POINT ( 'NONE',  ( 4.036439982160089812, -1.511860617216064684, 0.8620873645008280128 ) ) ;
#49149=CARTESIAN_POINT ( 'NONE',  ( 2.349550187768103093, 0.6076851952682017499, -2.210314646808369421 ) ) ;
#49151=CARTESIAN_POINT ( 'NONE',  ( 6.040588761503070003, -1.765850204961866954, 1.119074740713212002 ) ) ;
#49152=CARTESIAN_POINT ( 'NONE',  ( 0.7261896124251127072, 0.1329856088156805560, 1.836402230816103209 ) ) ;
#49155=CARTESIAN_POINT ( 'NONE',  ( 2.285779929129946098, 1.617817622347239803, -1.203354541732377658 ) ) ;
#49156=CARTESIAN_POINT ( 'NONE',  ( 1.570551226722196381, -2.081687204081467346, -0.6850663153453034893 ) ) ;
#49159=CARTESIAN_POINT ( 'NONE',  ( 1.557173632797459684, 1.693725193156172315, -1.190412882225246438 ) ) ;
#49162=CARTESIAN_POINT ( 'NONE',  ( 4.037823014030429647, -2.028772383530423884, 0.6168223452112444605 ) ) ;
#49164=CARTESIAN_POINT ( 'NONE',  ( 6.322862864304120478, 1.705426906915354035, 0.6521430802832667295 ) ) ;
#49171=CARTESIAN_POINT ( 'NONE',  ( 3.076430314242516229, 0.9118049750012310328, 1.802366903320629765 ) ) ;
#49172=CARTESIAN_POINT ( 'NONE',  ( 1.272647984039422697, -1.336331724779236119, 1.627640044824183674 ) ) ;
#49176=CARTESIAN_POINT ( 'NONE',  ( 5.260548175522302472, -0.6249328720258572334, -1.753037815340392935 ) ) ;
#49181=CARTESIAN_POINT ( 'NONE',  ( 0.1456854043008250221, -1.672057201651616642, -1.369741535119282982 ) ) ;
#49185=CARTESIAN_POINT ( 'NONE',  ( 1.879855919261735675, -0.2174549385326445539, 1.720076089969482469 ) ) ;
#49186=CARTESIAN_POINT ( 'NONE',  ( 0.9897393536978270623, -0.4193350815317981040, -1.688907716811594240 ) ) ;
#49187=CARTESIAN_POINT ( 'NONE',  ( 6.445943507803128192, 0.8898977879068777908, -2.129411633396756098 ) ) ;
#49190=CARTESIAN_POINT ( 'NONE',  ( 2.442714938195661212, 0.4483736453565168589, 2.011251146304892767 ) ) ;
#49191=CARTESIAN_POINT ( 'NONE',  ( 1.141953626738337890, -0.04666616626641807014, -2.015725262716171695 ) ) ;
#49192=CARTESIAN_POINT ( 'NONE',  ( 6.925078400183513949, 3.679108800414055302, 2.758152782261179325 ) ) ;
#49194=CARTESIAN_POINT ( 'NONE',  ( 0.2507688454781953902, -1.584965806562924628, 1.172240258958085146 ) ) ;
#49196=CARTESIAN_POINT ( 'NONE',  ( 4.201352949932454450, 1.705870964349815333, -0.8646410313453978258 ) ) ;
#49198=CARTESIAN_POINT ( 'NONE',  ( 6.041676539500916654, -1.595688354349385607, -1.524751901930617715 ) ) ;
#49202=CARTESIAN_POINT ( 'NONE',  ( 0.5572930201490761126, -1.731111387009228952, 1.040124062761533352 ) ) ;
#49205=CARTESIAN_POINT ( 'NONE',  ( 4.630063564305310742, -1.415688044924306555, -1.822237510073132949 ) ) ;
#49206=CARTESIAN_POINT ( 'NONE',  ( 5.248475795274027078, -1.946838731704622072, -0.2419367024937419397 ) ) ;
#49207=CARTESIAN_POINT ( 'NONE',  ( 1.481223165768187355, -0.05357505548480785695, 1.961209554040027170 ) ) ;
#49209=CARTESIAN_POINT ( 'NONE',  ( -0.1048463755018592264, -0.8645036352170620830, -1.819965476435807306 ) ) ;
#49211=CARTESIAN_POINT ( 'NONE',  ( 0.2338150414605598693, 0.6575980258751003005, -2.012739700429423628 ) ) ;
#49214=CARTESIAN_POINT ( 'NONE',  ( 0.4800843290509413386, -0.2225996465644273503, -1.827572303103291551 ) ) ;
#49216=CARTESIAN_POINT ( 'NONE',  ( 4.135715461124009451, 2.046248213957535089, -0.7259774245699932571 ) ) ;
#49218=CARTESIAN_POINT ( 'NONE',  ( 1.828540510153942922, -1.004066958311781832, -1.867862179375394005 ) ) ;
#49223=CARTESIAN_POINT ( 'NONE',  ( 1.757177114327221901, -1.766000478700447074, -1.061884917490847791 ) ) ;
#49229=CARTESIAN_POINT ( 'NONE',  ( 5.092401474535850348, -1.059014397921493433, 1.592059587274458510 ) ) ;
#49232=CARTESIAN_POINT ( 'NONE',  ( 2.021152898351881166, 2.110506920502265960, 0.8154138738461161884 ) ) ;
#49234=CARTESIAN_POINT ( 'NONE',  ( 1.792921450925293536, -0.09139298786187435852, -1.809423198457478676 ) ) ;
#49235=CARTESIAN_POINT ( 'NONE',  ( 2.237376970375870577, 0.5068087052534899772, -1.847417656071285608 ) ) ;
#49236=CARTESIAN_POINT ( 'NONE',  ( 2.576698201331685922, 1.354182300986291887, -1.566139152919379107 ) ) ;
#49238=CARTESIAN_POINT ( 'NONE',  ( 1.815242386724497337, -0.2434097785052463103, 1.956328700473447979 ) ) ;
#49239=CARTESIAN_POINT ( 'NONE',  ( 5.180268977979770817, -1.068588414017849653, 1.602784418908353548 ) ) ;
#49240=CARTESIAN_POINT ( 'NONE',  ( 1.049971938256549109, -1.822247386521518298, -1.415841994891045674 ) ) ;
#49243=CARTESIAN_POINT ( 'NONE',  ( 5.266109189975630045, -2.053049664954803788, 0.1989083462991206031 ) ) ;
#49247=CARTESIAN_POINT ( 'NONE',  ( 0.01252217983070766719, -0.9030397145437498718, -1.901010321977952389 ) ) ;
#49250=CARTESIAN_POINT ( 'NONE',  ( 4.481803774187195444, 1.408218611193782221, 1.640057829624480101 ) ) ;
#49251=CARTESIAN_POINT ( 'NONE',  ( 5.584630649692731375, -1.279725605644935760, 1.562507038963067973 ) ) ;
#49258=CARTESIAN_POINT ( 'NONE',  ( 3.766814776335784209, -0.2024620155892907503, -2.006371719556559796 ) ) ;
#49263=CARTESIAN_POINT ( 'NONE',  ( 4.645497774645744649, -1.668943667408796294, -1.373881373981879594 ) ) ;
#49268=CARTESIAN_POINT ( 'NONE',  ( 5.607046053289695742, -0.04666138757647777385, 2.016035322322209389 ) ) ;
#49270=CARTESIAN_POINT ( 'NONE',  ( 0.7149654600043838792, -0.2576282674517544335, 1.705390864826474839 ) ) ;
#49272=AXIS2_PLACEMENT_3D ( 'NONE', #87423, #201136, #18120 ) ;
#49276=CARTESIAN_POINT ( 'NONE',  ( 6.731728662460410462, -1.222180481402233898, -1.416172877279207931 ) ) ;
#49277=CARTESIAN_POINT ( 'NONE',  ( 0.4342398884448725460, -1.078799894535716231, -1.699460183843485073 ) ) ;
#49280=CARTESIAN_POINT ( 'NONE',  ( 3.118423654462946892, -1.086285162511631652, -1.920806481261853493 ) ) ;
#49281=( BOUNDED_SURFACE ( )  B_SPLINE_SURFACE ( 3, 3, ( 
 ( #36285, #117618, #152190, #183611, #3759, #58953, #24293, #27516, #9135, #42733, #92310, #173553, #110422, #177490, #28032, #161236, #12823, #128808, #46426, #33867, #149768, #136722, #186515, #38146, #104219, #83678, #68483, #168143, #184375, #123756, #188655, #189718, #41370, #89045, #6686, #121611, #107482, #173506, #155102, #204877, #172672, #11210, #126127, #43752, #155344, #141274, #89293, #156420, #192087, #75165, #209399, #109866, #140190, #143403, #91434, #191023, #6926, #73004, #205132, #42690, #35810, #108096, #119264, #25698, #3289, #91806, #152769, #157864, #169014, #85632, #121421, #4350, #202555, #87768, #167952, #19555, #54207, #9457, #120345, #69357, #20612, #186321, #37956, #104029, #21662, #5415, #141640, #185249, #36872, #75529, #207649, #102955, #59269, #71493, #137605, #125425, #26769, #83491, #177159, #140428, #51424, #14634, #212838, #114362, #164116, #27931, #174211, #90817, #206668, #127659, #25784, #75618, #42071, #194687, #46329, #108185, #59360, #125517, #100385, #150222, #133997, #96156, #200003, #64685, #87343, #88416, #6062, #204254, #101451, #63121, #52201, #73231, #55938, #24479, #184843, #108678, #142213, #127087, #209283, #42575, #11094, #59859, #208227, #159495, #193050, #126011, #43638, #76109, #174706, #92396, #109753, #175763, #27356, #158434, #26282, #93458, #143292, #60930, #44704, #10035, #40964, #107071, #91860, #42038, #165350, #149099, #66746, #166417, #18010, #183730, #101417, #19085, #185300, #116108, #67269, #115054, #16397, #166946, #86751, #132344, #33730, #134476, #88905, #172787, #161874, #97944, #59567, #128921, #44410, #47617, #15063, #49717, #61187, #127347, #173901, #141421, #59047, #406, #59605, #173382, #192788, #91068, #111115, #201830, #31073, #29998, #96083, #45198, #195697, #175195, #164257, #197806, #170129, #3341, #70471, #85683, #202608, #87825, #135518, #53188, #119316, #38402, #103405, #169466, #65619, #178361, #186490, #41345, #44537, #73707, #166800, #32414, #50790, #149362, #85422, #180791, #82215, #33473, #116919, #133146, #944, #147246, #2008, #64902, #16131, #67009, #115853, #151506, #35596, #181838, #182920, #199146, #34535, #100606, #167744, #197039, #166682, #18274, #84356, #48675, #15071, #131050, #99547, #148309, #165611, #150446, #68074, #134210, #200220, #49724, #3075, #47624, #65938, #179742, #83274, #51871, #17200, #164546, #117992, #130001, #195991, #183985, #214307, #132087, #114791, #101674, #98480, #198097, #19343, #113736, #31359, #97434, #163489, #81163, #213273, #72357, #154701, #86492, #155770, #4143, #169867, #6284, #55065, #24679, #189326, #121215, #122291, #138460, #204479, #56132, #107075, #136325, #39889, #105999, #188248, #202343, #168804, #70213, #187184, #21458, #38811, #172020, #23611, #89721, #7354, #203412, #173098, #90785, #104897, #170936, #20410, #22535, #120134, #53995, #73433, #137394, #139536, #88644, #205561, #156848, #57201, #69146, #123361, #119053, #135267, #201281, #40967, #152556, #52922, #185038, #36663, #102749, #186111, #37745, #103820, #87566, #153634, #5207, #71280, #142754, #96122, #209826, #59328, #93993, #176294, #76640, #108153, #191447, #158971, #61462, #11636, #160034, #10565, #206635, #192513, #190381, #207708, #9513, #44165, #144891, #77709, #157918, #140623, #141695, #91863, #143830, #42041 ),
 ( #75585, #112415, #174179, #127628, #12692, #193592, #27898, #8432, #74520, #126552, #25750, #110285, #26821, #45236, #111351, #125485, #43112, #30036, #177356, #28970, #175237, #92925, #109227, #210898, #95053, #161104, #58266, #78768, #124423, #208763, #62525, #60388, #46300, #128687, #194656, #178427, #163241, #214062, #116662, #34280, #149103, #79840, #63598, #182660, #129752, #100353, #15885, #14823, #98241, #166421, #180541, #97188, #682, #164296, #65690, #99305, #162177, #113485, #81969, #198893, #148056, #80915, #32164, #197846, #49478, #131838, #115598, #181592, #150189, #196793, #147005, #66749, #18013, #114550, #84102, #165353, #31114, #195737, #213023, #179492, #64658, #33221, #199970, #130800, #16947, #1758, #48434, #83026, #132890, #13763, #145948, #50539, #67815, #133962, #211959, #183734, #51618, #117741, #35340, #47372, #89458, #39618, #21203, #19088, #72095, #3885, #68892, #153374, #69955, #103560, #204217, #168553, #52668, #105722, #86237, #53740, #85168, #151252, #136067, #7092, #171752, #101420, #88378, #202080, #185851, #36410, #118797, #201025, #73165, #2821, #135011, #152308, #154445, #87305, #189070, #6026, #119872, #186927, #54808, #169619, #184784, #37483, #4945, #138205, #104635, #38559, #71021, #102489, #137135, #20152, #203163, #120956, #170682, #23347, #22269, #55870, #122026, #187993, #155511, #139271, #205301, #56940, #123112, #167492, #43911, #126290, #11370, #8180, #176039, #94795, #93731, #77450, #128434, #172839, #191184, #90524, #208498, #27631, #76382, #75323, #111087, #210647, #106809, #142491, #141440, #125226, #190128, #110025, #9252, #157654, #159771, #60133, #62273, #91604, #207446, #158711, #143568, #209560, #192249, #58002, #127363, #41783, #59065, #61205, #26560, #40705, #160844, #92667, #193333, #44979, #177094, #28709, #78515, #107897, #12436, #144632, #24410, #173923, #140357, #25496, #10308, #42851, #156586, #74264, #206375, #124166, #108958, #174978, #83841, #149930, #180295, #81720, #145704, #147802, #30858, #47112, #426, #48186, #132637, #114297, #32972, #1499, #31918, #67565, #49235, #29783, #17751, #194401, #66498, #63339, #131590, #46043, #197591, #97996, #112164, #95867, #161922, #178167, #13513, #198643, #129498, #115354, #79585, #181345, #164054, #211703, #195479, #166163, #113229, #179233, #96935, #99048, #15633, #162985, #165103, #14566, #65439, #213820, #16694, #80662, #146753, #130551, #82780, #148853, #50291, #196543, #212771, #116410, #64407, #182400, #34029, #100103, #55617, #202908, #68639, #51360, #52422, #2568, #136881, #167240, #19900, #105466, #199714, #54552, #4692, #104379, #101154, #120699, #187741, #186674, #170426, #6841, #117484, #69708, #183475, #87048, #38301, #169366, #168303, #203970, #89206, #35082, #20951, #85984, #3630, #134763, #22013, #102232, #36153, #88123, #153121, #155259, #184530, #152060, #37233, #154193, #5761, #70767, #151000, #71841, #200771, #135812, #137949, #119618, #133708, #39369, #185602, #121772, #171499, #23091, #18828, #84912, #118548, #201835, #53480, #103304, #206124, #172582, #74004, #58819, #25243, #124972, #43660, #76134, #109776, #93478, #207193, #176839, #28452, #190933, #174732, #24163, #26304, #123914, #140097, #159517, #141184, #11116, #42597, #126032, #94546, #108703, #160584, #142237, #8996, #92418, #10057 ),
 ( #110834, #57754, #175785, #27377, #208249, #189881, #90266, #41524, #158457, #91343, #59883, #77192, #191995, #143312, #209305, #60952, #72919, #139024, #127109, #193074, #156333, #44725, #107636, #173668, #205048, #56691, #122858, #188819, #40453, #106555, #7919, #157404, #75071, #62027, #50033, #182144, #98794, #95619, #163800, #33775, #15376, #212517, #116158, #128183, #198393, #194144, #45792, #63084, #65190, #146500, #99854, #213568, #129253, #97741, #180042, #80403, #111913, #195224, #162736, #131344, #81470, #147547, #14308, #210386, #196289, #177913, #211449, #13263, #47935, #148606, #197339, #161669, #144386, #145453, #79335, #48980, #29527, #112974, #12191, #78262, #115099, #181095, #32712, #46861, #164848, #66242, #16440, #82519, #178986, #30600, #64159, #96687, #31664, #175, #114048, #130301, #132391, #121514, #17501, #201582, #200520, #35904, #100902, #20702, #134516, #68387, #86795, #185347, #187486, #2310, #118292, #69452, #152862, #4440, #36969, #184278, #101979, #166991, #153936, #202652, #38050, #149670, #135558, #83588, #18582, #70510, #3383, #203714, #136625, #84660, #137694, #150749, #53228, #120439, #104121, #54301, #1251, #67310, #186413, #133452, #170168, #19650, #52165, #168048, #21756, #85723, #151810, #87864, #119359, #103052, #169105, #165916, #117225, #5505, #71585, #55362, #39116, #199457, #51099, #183222, #34828, #206934, #107378, #93222, #139838, #172320, #158212, #59624, #57500, #125780, #108451, #188555, #138762, #156070, #122592, #40186, #8739, #143054, #90014, #174470, #159254, #7657, #123659, #106299, #105199, #88946, #173401, #23910, #73741, #155000, #126849, #189622, #205866, #124717, #41270, #10855, #43397, #24983, #22832, #75876, #91086, #72664, #157146, #74820, #140920, #207997, #58563, #56433, #109519, #190676, #42336, #6585, #204779, #26046, #76928, #175526, #171236, #92159, #9801, #141983, #191742, #27116, #209049, #60685, #192806, #144129, #31403, #48719, #179783, #63888, #132130, #44465, #162473, #210122, #80133, #62816, #130043, #14046, #11933, #177658, #65980, #196036, #212254, #112710, #61763, #12992, #194956, #97477, #47670, #113781, #46592, #28194, #146237, #78005, #29266, #45531, #163533, #180832, #15118, #193883, #176583, #95358, #127931, #81207, #111646, #145185, #16174, #110581, #147286, #213318, #64942, #161408, #131093, #98527, #197082, #114833, #94289, #160329, #178722, #79067, #32457, #164588, #82258, #211191, #148350, #214350, #128977, #30337, #96422, #68119, #133189, #55907, #166726, #100649, #122064, #6064, #156624, #34577, #150489, #101718, #188028, #204256, #72134, #987, #73204, #199189, #84401, #138242, #184022, #8214, #106847, #35639, #39658, #105766, #171791, #23386, #24450, #50837, #89498, #155552, #7132, #116964, #83318, #182962, #167789, #2048, #22306, #139310, #205339, #56977, #123151, #118036, #90563, #74299, #88418, #154485, #149405, #189108, #18318, #134255, #40741, #51913, #172878, #198139, #49770, #115896, #181881, #33518, #99590, #165656, #17243, #67052, #200262, #9289, #77485, #161958, #143604, #126325, #178204, #41820, #112198, #190166, #107933, #191221, #193370, #60168, #13548, #127398, #42885, #111125, #173958, #61241, #194437, #45015, #177128, #140395, #58038, #76413, #25531, #93765, #28745, #176072, #175011, #210681, #95905, #206414, #27670 ),
 ( #43944, #94829, #209597, #11408, #157691, #12476, #75362, #26598, #160881, #192284, #124202, #46078, #110060, #78551, #144668, #62310, #128469, #29821, #207481, #91639, #141474, #59101, #125261, #108994, #92699, #159804, #158745, #10339, #142523, #208532, #50324, #100134, #213854, #183509, #35118, #65475, #181383, #30895, #33006, #130587, #146790, #166196, #147837, #17787, #131625, #132673, #101189, #197624, #167278, #148889, #129533, #117516, #79620, #83874, #163020, #16728, #145739, #82812, #49268, #211739, #195514, #51396, #47150, #113267, #196577, #198679, #115389, #63377, #66531, #48219, #165137, #99085, #462, #179271, #114332, #15668, #116442, #182436, #34063, #81755, #96972, #149966, #14602, #64443, #80699, #1535, #67597, #133743, #212806, #180327, #31949, #98033, #199751, #164087, #119650, #205081, #84947, #22045, #104411, #187772, #185634, #39404, #88156, #102263, #52454, #69740, #36187, #168338, #136915, #56723, #3663, #154224, #72952, #135845, #37267, #19933, #18863, #2605, #87082, #86019, #152092, #68674, #40486, #103337, #201868, #38334, #53516, #6874, #171530, #153152, #151036, #204000, #169399, #200803, #70802, #20985, #4727, #121805, #202942, #184567, #23123, #54586, #120733, #134797, #118579, #186706, #139054, #89240, #170460, #5796, #71873, #137983, #55649, #105498, #155291, #122891, #188850, #106590, #159554, #176877, #93513, #192033, #45828, #172618, #76168, #57787, #208284, #190966, #43696, #142273, #140133, #91380, #194183, #27415, #109813, #125009, #42632, #173703, #160623, #209342, #44764, #156367, #59915, #24194, #25278, #77228, #10094, #210424, #11151, #157440, #144422, #9034, #126072, #127143, #110872, #143347, #90297, #74043, #193115, #206159, #28489, #26343, #75108, #108741, #94580, #174768, #107674, #60990, #92456, #175822, #12224, #7951, #123947, #158495, #78297, #62066, #141219, #128221, #189916, #41561, #207229, #58853, #114088, #99890, #146540, #179022, #164884, #180079, #165952, #212559, #30640, #16478, #66282, #64198, #132429, #115136, #195264, #145492, #162773, #129288, #46898, #15416, #149708, #96724, #181131, #17536, #14351, #130339, #113013, #111949, #95657, #31702, #80441, #196328, #161708, #133491, #47972, #97777, #131380, #163837, #83625, #50076, #81506, #29565, #82558, #147585, #79373, #213603, #65229, #197376, #211, #49017, #63124, #116197, #32752, #98834, #13300, #211487, #148645, #1288, #182184, #177951, #198430, #33811, #67346, #199494, #68425, #150786, #200556, #155038, #2349, #38089, #55398, #186452, #70547, #138798, #51138, #169144, #134553, #86833, #69488, #136666, #20738, #18620, #184315, #72703, #120479, #202691, #3422, #135596, #52204, #39154, #87901, #137735, #34864, #152897, #117261, #118330, #170208, #103087, #88985, #104160, #35939, #22869, #102019, #4476, #5541, #203754, #21792, #183260, #167025, #71622, #84699, #121552, #119397, #168087, #201617, #187523, #53266, #19687, #153974, #185386, #54341, #105236, #100938, #85765, #37005, #171277, #6624, #151845, #8774, #26086, #92202, #206970, #158252, #74857, #9840, #174511, #172358, #123696, #11969, #59661, #75916, #157179, #140959, #205904, #192844, #27156, #76968, #188593, #142019, #56469, #57538, #109561, #42377, #28232, #191781, #189657, #176620, #41308, #108487, #159294, #143095, #43437, #122631, #106336, #10893 ),
 ( #208034, #204818, #156111, #58600, #93260, #124755, #107416, #190715, #125820, #175565, #209088, #60723, #126886, #44503, #25020, #173441, #110620, #94325, #160366, #78043, #40225, #73777, #23947, #91120, #7694, #139873, #90052, #181922, #129017, #213353, #198173, #194994, #162512, #145223, #144167, #127969, #212291, #211228, #62854, #193921, #165691, #14083, #161448, #163574, #46628, #132167, #82295, #63924, #61800, #114869, #112751, #111684, #196074, #178763, #146279, #32491, #30376, #95396, #148388, #96462, #80173, #45567, #177691, #130079, #49806, #214389, #210159, #131129, #47706, #113821, #79105, #13028, #29302, #179820, #33552, #31439, #197118, #66018, #64975, #15157, #17280, #97518, #81243, #147325, #48756, #180870, #98565, #164626, #16211, #115932, #99625, #182997, #70291, #87642, #4222, #102827, #171016, #83356, #201358, #34614, #119135, #101755, #168882, #52999, #50875, #2085, #104975, #152635, #20486, #35677, #167822, #84435, #71359, #120214, #169946, #67088, #185115, #149441, #150524, #202423, #135344, #121288, #136407, #68158, #55142, #134292, #36741, #37821, #21532, #54078, #1023, #199228, #103899, #116997, #153713, #151587, #200297, #19422, #5282, #85500, #18357, #186188, #3154, #86572, #137475, #133222, #100684, #69225, #203489, #187264, #51950, #38890, #166762, #118072, #184059, #174248, #60458, #89800, #207770, #59397, #157990, #155845, #122370, #23690, #8510, #189399, #74591, #125553, #25820, #191514, #43179, #156921, #126615, #192578, #140694, #124493, #188326, #190452, #73512, #7431, #109292, #90857, #175302, #206710, #75655, #44233, #58337, #110354, #91930, #72433, #22613, #88721, #26888, #106074, #9578, #154780, #141762, #42110, #6364, #138535, #208828, #204558, #56206, #139615, #92991, #108223, #39967, #159036, #205637, #10629, #76704, #142821, #172097, #57275, #123437, #41041, #107150, #173175, #24755, #65754, #162239, #63662, #127694, #129816, #12756, #29038, #196855, #30098, #114612, #96188, #14882, #131901, #13825, #49537, #31174, #11702, #214125, #197908, #48494, #45296, #113550, #176357, #179553, #79899, #27965, #77776, #148125, #143896, #209890, #78830, #80976, #146008, #94058, #163301, #144951, #47435, #195798, #212018, #61528, #210957, #112479, #147066, #97247, #213087, #178488, #160099, #64717, #193654, #161170, #177420, #130859, #98300, #180603, #111416, #95121, #62584, #128746, #32228, #194720, #46359, #164363, #15948, #82031, #201095, #86308, #83092, #36483, #169689, #168620, #152379, #203237, #33283, #51690, #165420, #68962, #102560, #151322, #150259, #185922, #71098, #181657, #2890, #1827, #200038, #50603, #184856, #84170, #18082, #20222, #135082, #137216, #166491, #67886, #19160, #3958, #118870, #52736, #132957, #202159, #116728, #134031, #70025, #117812, #136141, #115663, #53817, #119947, #37557, #103637, #21277, #153451, #182728, #87383, #5024, #99368, #34347, #748, #100420, #101490, #183802, #167560, #17016, #149171, #66814, #35412, #198960, #85234, #190201, #188066, #154521, #55949, #40784, #7172, #106889, #25569, #58079, #91681, #75402, #189147, #158785, #10382, #172916, #156662, #6101, #8254, #105806, #122102, #141515, #123186, #207523, #24491, #107969, #76458, #90602, #142566, #124241, #104710, #92740, #54881, #59142, #138278, #206452, #121035, #41860, #74338, #187002, #170759 ),
 ( #23424, #139349, #204292, #72170, #39696, #171831, #38633, #89535, #173997, #125300, #157733, #140440, #22348, #88460, #9330, #155587, #191259, #73242, #42924, #109034, #205379, #57017, #175053, #26640, #49048, #111169, #177170, #11452, #33842, #245, #198463, #126367, #65260, #208573, #143647, #148677, #213634, #149744, #16508, #209641, #83654, #61282, #131407, #132461, #50107, #82590, #192326, #110103, #116228, #176114, #182219, #78590, #127443, #160924, #99923, #28787, #77526, #66317, #12518, #197407, #32787, #60206, #193414, #115168, #165984, #181163, #45057, #94870, #17570, #98863, #43985, #147616, #1321, #164915, #27714, #67382, #93808, #159849, #188778, #25205, #145141, #62769, #177611, #105429, #89171, #211147, #155223, #128933, #41491, #40416, #123879, #194910, #206086, #122819, #29223, #189844, #91310, #124937, #187704, #138988, #107603, #12945, #8961, #205009, #6804, #190900, #75036, #173634, #141151, #157367, #178676, #7881, #106519, #95313, #46548, #140064, #112668, #42564, #56656, #72880, #24130, #172545, #90232, #207160, #14005, #156297, #108666, #30291, #73969, #57721, #58783, #39332, #171465, #161362, #79025, #96377, #23053, #212208, #162428, #80089, #146193, #63844, #117718, #98220, #166396, #52645, #49455, #183708, #202056, #35316, #17987, #3859, #81947, #152285, #15862, #148030, #16922, #19064, #100329, #53716, #167468, #83002, #51594, #133940, #34257, #65666, #149078, #116640, #85142, #101394, #151229, #182635, #164272, #150165, #214040, #165329, #181569, #1733, #102464, #2798, #115573, #131814, #99281, #33198, #68870, #197823, #66723, #69932, #32140, #134990, #201000, #118775, #656, #184759, #20128, #36386, #168530, #180519, #132866, #198870, #86214, #50517, #84077, #136044, #67790, #199947, #141416, #123089, #105699, #157631, #21179, #91579, #169597, #87282, #170659, #172814, #39596, #207423, #106786, #22246, #205276, #73140, #187968, #4921, #88356, #55846, #24386, #189046, #56916, #122002, #103537, #89433, #153351, #104612, #120929, #155484, #41758, #40683, #54782, #37458, #38534, #203140, #90499, #70998, #5999, #9229, #185827, #156562, #8157, #74241, #137111, #140334, #173896, #206353, #57980, #119849, #186902, #171726, #154421, #139245, #124143, #7067, #72070, #190105, #75301, #138180, #107870, #204190, #23325, #25472, #128413, #27610, #176018, #194380, #78494, #14543, #110005, #11348, #177072, #46023, #62252, #144611, #76361, #145682, #208476, #159751, #210626, #93710, #29760, #80640, #211680, #112142, #178146, #95845, #161901, #96912, #126271, #13488, #79563, #63316, #192228, #158689, #60112, #44958, #77429, #111066, #129477, #195459, #47088, #113206, #193312, #162964, #146732, #28688, #160822, #10287, #12414, #143546, #43891, #179211, #127342, #30836, #94774, #59042, #125200, #191163, #42830, #108936, #174957, #26539, #92647, #142468, #209540, #61182, #16671, #17727, #182374, #180272, #131566, #19878, #67542, #83815, #165080, #82756, #213794, #200748, #35058, #84889, #196520, #34004, #64384, #65417, #117460, #50268, #36127, #199689, #197567, #184509, #49211, #116386, #167217, #150976, #51333, #130529, #114275, #18804, #31896, #2541, #66473, #115331, #148829, #68616, #402, #147778, #183453, #132614, #100078, #149908, #212750, #164032, #198621, #101129, #166140, #15607, #97973, #1475, #133684 ),
 ( #81694, #181322, #32950, #99024, #134741, #52397, #102212, #118524, #168277, #85961, #48163, #170401, #153097, #152037, #135789, #5737, #4672, #70745, #201813, #173646, #21989, #169344, #171478, #136858, #72895, #37208, #203947, #88098, #122833, #54530, #119595, #55594, #120675, #154171, #40430, #202882, #103282, #90244, #186653, #104356, #53457, #185578, #38279, #57734, #7894, #3608, #139001, #71816, #137926, #87025, #20928, #121749, #187717, #41502, #39346, #205023, #105442, #23068, #89184, #155236, #188794, #6817, #106532, #172558, #56669, #107615, #25219, #24142, #156310, #73982, #140076, #206100, #123891, #189857, #69685, #32421, #14009, #147249, #49731, #80095, #181844, #191974, #31364, #8975, #146199, #180796, #174709, #97440, #115859, #163496, #212213, #132093, #207172, #65944, #141164, #58796, #142216, #213281, #63850, #91323, #81169, #208230, #179746, #47631, #162433, #190913, #59862, #30296, #64907, #15079, #131056, #96381, #75049, #130006, #124951, #76112, #92399, #195997, #16137, #197044, #26285, #42578, #10038, #158437, #48681, #108681, #43641, #198102, #157381, #114797, #98488, #164551, #126014, #82222, #148313, #214312, #112673, #178683, #113742, #183989, #83282, #201287, #20416, #69152, #68082, #103825, #203417, #99553, #135272, #134217, #117999, #182925, #102757, #2013, #150452, #168812, #52928, #55073, #84361, #200226, #151514, #86498, #36668, #119062, #50798, #120140, #34541, #51877, #185044, #35603, #4150, #121222, #186118, #152563, #70221, #136332, #202352, #71287, #100611, #54002, #37751, #169873, #166687, #133151, #137400, #19349, #21463, #199153, #87572, #101680, #18278, #153642, #167750, #5212, #85429, #33480, #165618, #3082, #17206, #149367, #949, #67015, #116925, #59337, #56138, #124431, #208767, #190389, #173106, #10573, #88650, #158976, #22544, #154710, #23620, #25757, #107084, #60395, #174186, #89729, #58275, #140629, #40973, #72365, #155777, #123367, #91870, #42047, #108158, #189334, #170944, #156854, #6291, #172027, #188256, #8439, #109233, #157925, #122299, #104903, #106006, #39897, #9519, #138466, #73439, #76647, #38820, #75591, #141703, #207714, #204488, #125491, #26829, #191453, #43118, #187192, #7362, #24686, #139543, #206642, #175243, #74527, #205569, #92932, #142762, #57207, #90790, #161111, #210904, #61469, #195743, #95062, #28977, #47380, #145955, #81976, #177363, #78775, #30042, #113493, #129759, #211965, #143837, #213033, #127634, #12697, #63604, #144896, #97195, #148064, #64663, #179499, #31121, #163248, #14830, #164303, #193599, #80921, #147010, #130809, #45241, #11644, #111358, #112422, #62531, #178436, #196799, #48441, #114556, #180549, #46306, #15892, #32170, #98247, #214070, #128693, #77715, #194661, #96131, #162184, #13770, #126559, #192519, #44173, #110292, #79846, #176301, #27904, #94001, #160040, #209832, #19095, #116668, #132896, #86245, #133969, #3892, #199978, #118805, #21211, #51625, #153382, #166430, #2830, #197853, #117750, #152315, #149109, #68899, #87315, #135018, #183740, #103569, #181600, #37493, #115605, #33228, #182666, #184791, #35350, #65696, #52675, #34288, #151258, #85174, #101426, #165361, #100360, #1766, #36417, #201032, #102495, #67823, #49484, #167497, #99311, #50546, #66755, #168559, #202090, #20158, #689, #16954, #198900, #18021, #69964, #83035 ) ),
 .UNSPECIFIED., .T., .F., .T. ) 
 B_SPLINE_SURFACE_WITH_KNOTS ( ( 4, 3, 4 ),
 ( 4, 1, 1, 1, 1, 1, 1, 1, 1, 1, 1, 1, 1, 1, 1, 1, 1, 1, 1, 1, 1, 1, 1, 1, 1, 1, 1, 1, 1, 1, 1, 1, 1, 1, 1, 1, 1, 1, 1, 1, 1, 1, 1, 1, 1, 1, 1, 1, 1, 1, 1, 1, 1, 1, 1, 1, 1, 1, 1, 1, 1, 1, 1, 1, 1, 1, 1, 1, 1, 1, 1, 1, 1, 1, 1, 1, 1, 1, 1, 1, 1, 1, 1, 1, 1, 1, 1, 1, 1, 1, 1, 1, 1, 1, 1, 1, 1, 1, 1, 1, 1, 1, 1, 1, 1, 1, 1, 1, 1, 1, 1, 1, 1, 1, 1, 1, 1, 1, 1, 1, 1, 1, 1, 1, 1, 1, 1, 1, 1, 1, 1, 1, 1, 1, 1, 1, 1, 1, 1, 1, 1, 1, 1, 1, 1, 1, 1, 1, 1, 1, 1, 1, 1, 1, 1, 1, 1, 1, 1, 1, 1, 1, 1, 1, 1, 1, 1, 1, 1, 1, 1, 1, 1, 1, 1, 1, 1, 1, 1, 1, 1, 1, 1, 1, 1, 1, 1, 1, 1, 1, 1, 1, 1, 1, 1, 1, 1, 1, 1, 1, 1, 1, 1, 1, 1, 1, 1, 1, 1, 1, 1, 1, 1, 1, 1, 1, 1, 1, 1, 1, 1, 1, 1, 1, 1, 1, 1, 1, 1, 1, 1, 1, 1, 1, 1, 1, 1, 1, 1, 1, 1, 1, 1, 1, 1, 1, 1, 1, 1, 1, 1, 1, 1, 1, 1, 1, 1, 1, 1, 1, 1, 1, 1, 1, 1, 1, 1, 1, 1, 1, 1, 1, 1, 1, 1, 1, 1, 1, 1, 1, 1, 1, 1, 1, 1, 1, 1, 1, 1, 1, 1, 1, 1, 1, 1, 1, 1, 1, 1, 1, 1, 1, 1, 1, 1, 1, 1, 1, 1, 1, 1, 1, 1, 1, 1, 1, 1, 1, 1, 1, 1, 1, 1, 1, 1, 1, 1, 1, 1, 1, 1, 1, 1, 1, 1, 1, 1, 1, 1, 1, 1, 1, 1, 1, 1, 1, 1, 1, 1, 1, 1, 1, 1, 1, 1, 1, 1, 1, 1, 1, 1, 1, 1, 1, 1, 1, 1, 1, 1, 1, 1, 1, 1, 1, 1, 1, 1, 1, 1, 1, 1, 1, 1, 1, 4 ),
 ( 0.000000000000000000, 0.5000000000000000000, 1.000000000000000000 ),
 ( 0.000000000000000000, 0.002600034503794030130, 0.005208798665460326327, 0.007813183304800875098, 0.01041632952039499814, 0.01302078637366306003, 0.01562487905948694092, 0.01822913957756216313, 0.02083328395591756144, 0.02343739818322774712, 0.02604168118785421884, 0.02864568517727394958, 0.03125004130332968699, 0.03385401862675675722, 0.03645834363201481965, 0.03906241290072134942, 0.04166661303991354287, 0.04427083116291704451, 0.04687488238457573897, 0.04947921467585455341, 0.05208318889621989245, 0.05468754274347345512, 0.05729155431138267807, 0.05989582568988525285, 0.06249996760622017478, 0.06510408932096034551, 0.06770837349117478365, 0.07031237295078232585, 0.07291672927807971161, 0.07552070761765239393, 0.07812503204114096267, 0.08072910085791458468, 0.08333330089851145872, 0.08593751883178461781, 0.08854156980611090078, 0.09114590188302622298, 0.09374987588873062716, 0.09635422952249227124, 0.09895824087764454324, 0.1015625120427016276, 0.1041666537503683765, 0.1067707752516706410, 0.1093750592157429480, 0.1119790584643299974, 0.1145834145867499904, 0.1171873927198607973, 0.1197917169388799108, 0.1223957855539345302, 0.1249999853896588409, 0.1276042031245507580, 0.1302082538950744550, 0.1328125857752754935, 0.1354165595809520839, 0.1380209130188291833, 0.1406249241787864424, 0.1432291951479887082, 0.1458333366646657747, 0.1484374579699756502, 0.1510417417453218114, 0.1536457408005802994, 0.1562500967354857329, 0.1588540746797905134, 0.1614583987117299280, 0.1640624671426803571, 0.1666666667910262079, 0.1692708843450304312, 0.1718749349293641482, 0.1744792666302357464, 0.1770832402535473249, 0.1796875935129024493, 0.1822916044953091785, 0.1848958752860835608, 0.1875000166293293857, 0.1901041377562054102, 0.1927084213602507368, 0.1953124202398235920, 0.1979167760045740521, 0.2005207537777317084, 0.2031250776399721736, 0.2057291459044250093, 0.2083333453828807025, 0.2109375627734847158, 0.2135416131892344249, 0.2161459447281551538, 0.2187499181867580689, 0.2213542712849473904, 0.2239582821074418695, 0.2265625527372090720, 0.2291666939245756707, 0.2317708148905701926, 0.2343750983407339450, 0.2369790970622578097, 0.2395834526742069426, 0.2421874302938704648, 0.2447917540037867212, 0.2473958221193426621, 0.2500000214453905190, 0.2526042386900758108, 0.2552082889548416555, 0.2578126203491843960, 0.2604165936607292231, 0.2630209466151033904, 0.2656249572953180982, 0.2682292277814931625, 0.2708333688305272213, 0.2734374896531870935, 0.2760417729668830367, 0.2786457715479891406, 0.2812501270244852081, 0.2838541045083020076, 0.2864584280832634389, 0.2890624960675178268, 0.2916666952586349781, 0.2942709123748779576, 0.2968749625062547248, 0.2994792937733871119, 0.3020832669555192918, 0.3046876197834237909, 0.3072916303389863768, 0.3098959006989794318, 0.3125000416272227799, 0.3151041623240899980, 0.3177084455187270673, 0.3203124439770417831, 0.3229167993354283839, 0.3255207767010412923, 0.3281251001584127303, 0.3307291680289564662, 0.3333333671026155187, 0.3359375841078879321, 0.3385416341234662174, 0.3411459652807516951, 0.3437499383511121720, 0.3463542910698884647, 0.3489583015184220538, 0.3515625717696388985, 0.3541667125946290073, 0.3567708331832410984, 0.3593751162762241491, 0.3619791146293697692, 0.3645834698869864221, 0.3671874471520340522, 0.3697917705091763874, 0.3723958382835964032, 0.3750000372572658280, 0.3776042541690359799, 0.3802083040864021046, 0.3828126351512001757, 0.3854166081274262856, 0.3880209607544118922, 0.3906249711135359459, 0.3932292412733790488, 0.3958333820126498370, 0.3984375025105409418, 0.4010417855192715542, 0.4036457837848667074, 0.4062501389590495449, 0.4088541161411674008, 0.4114584394154381930, 0.4140625071113177014, 0.4166667060024629166, 0.4192709228381954478, 0.4218749726749327911, 0.4244793036646000717, 0.4270832765643259310, 0.4296876291168554296, 0.4322916394041865784, 0.4348959094900549660, 0.4375000501611374104, 0.4401041705858387276, 0.4427084535277153732, 0.4453124517233759683, 0.4479168068314584583, 0.4505207839482789911, 0.4531251071570330247, 0.4557291747919532399, 0.4583333736180368323, 0.4609375903951940523, 0.4635416401688834398, 0.4661459711007739370, 0.4687499439416310532, 0.4713542964370365795, 0.4739583066701890113, 0.4765625766994796009, 0.4791667173199026797, 0.4817708376889431876, 0.4843751205813623395, 0.4869791187247021202, 0.4895834737840155659, 0.4921874508531692838, 0.4947917740137594000, 0.4973958416052992049, 0.5000000403837819851, 0.5026042571198243714, 0.5052083068480445194, 0.5078126377395105751, 0.5104166105391289010, 0.5130209629947408700, 0.5156249731913270518, 0.5182292431814352618, 0.5208333837687260104, 0.5234375040996330775, 0.5260417869599895990, 0.5286457850686206994, 0.5312501400964950715, 0.5338541171356111503, 0.5364584402653888029, 0.5390625078311259699, 0.5416667065794673608, 0.5442709232918542250, 0.5468749729921829061, 0.5494793038605755298, 0.5520832766365837418, 0.5546876290697317913, 0.5572916392473630243, 0.5598959092156829964, 0.5625000497873680061, 0.5651041700976676685, 0.5677084529433557014, 0.5703124510348895893, 0.5729168060486536929, 0.5755207830753605869, 0.5781251061916765632, 0.5807291737491879768, 0.5833333724848467350, 0.5859375891910368894, 0.5885416388810509325, 0.5911459697437208005, 0.5937499425137473530, 0.5963542949417601768, 0.5989583051180477069, 0.6015625750819736384, 0.6041667156555785567, 0.6067708359627971282, 0.6093751188112106476, 0.6119791169032582356, 0.6145834719202413199, 0.6171874489521673723, 0.6197917720723722379, 0.6223958396392350600, 0.6250000383796699976, 0.6276042550971219214, 0.6302083047943985994, 0.6328126356686964993, 0.6354166084503697354, 0.6380209608905765828, 0.6406249710831318778, 0.6432292410600577437, 0.6458333816531092175, 0.6484375019747732338, 0.6510417848433065480, 0.6536457829534795261, 0.6562501379910111732, 0.6588541150457848383, 0.6614584381872300467, 0.6640625057810221055, 0.6666667045436925898, 0.6692709212898660942, 0.6718749710119833463, 0.6744793019152608426, 0.6770832747262099938, 0.6796876271959411131, 0.6822916374223763070, 0.6848959074296973037, 0.6875000480597228680, 0.6901041684133596421, 0.6927084513194080584, 0.6953124494653194487, 0.6979168045407300180, 0.7005207816359816375, 0.7031251048160196415, 0.7057291724543196532, 0.7083333712566866058, 0.7109375880490425015, 0.7135416378135795989, 0.7161459687631898108, 0.7187499416210458847, 0.7213542941376326345, 0.7239583044155618596, 0.7265625744706748490, 0.7291667151552034820, 0.7317708355583423252, 0.7343751185193033715, 0.7369791167185673064, 0.7395834718491895998, 0.7421874490025512916, 0.7447917722385364314, 0.7473958399389256657, 0.7500000387984516736, 0.7526042556544531026, 0.7552083054789914263, 0.7578126364922896929, 0.7604166094146853627, 0.7630209619954617661, 0.7656249723425013753, 0.7682292424628052174, 0.7708333832193684509, 0.7734375036895410060, 0.7760417867228139865, 0.7786457849930478181, 0.7812501401962168579, 0.7838541174253229604, 0.7864584407346123518, 0.7890625085146746320, 0.7916667074488250577, 0.7942709243859374935, 0.7968749742880611997, 0.7994793053824050810, 0.8020832783869765725, 0.8046876310492792062, 0.8072916414830481058, 0.8098959116859448804, 0.8125000525320774658, 0.8151041730868179291, 0.8177084562098055898, 0.8203124545686294455, 0.8229168098616829186, 0.8255207871841712119, 0.8281251105841250792, 0.8307291784614470043, 0.8333333774876906519, 0.8359375945233833427, 0.8385416445206798075, 0.8411459757134309712, 0.8437499488178175078, 0.8463543015789862789, 0.8489583121171074831, 0.8515625824200027116, 0.8541667233732427311, 0.8567708440300897399, 0.8593751272601987123, 0.8619791257252362726, 0.8645834811255164176, 0.8671874585590289009, 0.8697917820670107991, 0.8723958500591838527, 0.8750000491949933012, 0.8776042663467393812, 0.8802083164568000884, 0.8828126477653241988, 0.8854166209871692228, 0.8880209738645485906, 0.8906249845246493324, 0.8932292549449527552, 0.8958333960228427317, 0.8984375167993386979, 0.9010418001539796107, 0.9036457987428592187, 0.9062501542677121602, 0.9088541318298947180, 0.9114584554632734203, 0.9140625235878931942, 0.9166667228507454634, 0.9192709401360219523, 0.9218749903764450471, 0.9244793218181143191, 0.9270832951750564987, 0.9296876481859919217, 0.9322916589857459524, 0.9348959295408556525, 0.9375000707608250883, 0.9401041916746273319, 0.9427084751713679101, 0.9453124739016935951, 0.9479168295687272483, 0.9505208072738278169, 0.9531251310501845930, 0.9557291993520028450, 0.9583333987332913750, 0.9609376160454207172, 0.9635416666839513589, 0.9661459986354887786, 0.9687499708159389433, 0.9713543235632202677, 0.9739583390673558494, 0.9765626083347638264, 0.9791667417950460361, 0.9817708662416058107, 0.9843751381318576188, 0.9869792129215403387, 0.9895836736503123010, 0.9921868305638316121, 0.9947912020913856068, 0.9973999845648282569, 1.000000000000000000 ),
 .UNSPECIFIED. ) 
 GEOMETRIC_REPRESENTATION_ITEM ( )  RATIONAL_B_SPLINE_SURFACE ( (
 ( 1.000000000000000222, 1.000000000000000222, 1.000000000000000222, 1.000000000000000222, 0.9999999999999996669, 0.9999999999999997780, 1.000000000000000444, 1.000000000000000000, 1.000000000000000000, 1.000000000000000000, 0.9999999999999997780, 1.000000000000000000, 1.000000000000000000, 1.000000000000000000, 1.000000000000000000, 0.9999999999999997780, 1.000000000000000222, 0.9999999999999996669, 1.000000000000000000, 0.9999999999999997780, 1.000000000000000222, 1.000000000000000000, 1.000000000000000222, 0.9999999999999996669, 1.000000000000000000, 1.000000000000000222, 0.9999999999999996669, 1.000000000000000444, 1.000000000000000000, 0.9999999999999997780, 1.000000000000000222, 1.000000000000000222, 1.000000000000000222, 1.000000000000000000, 1.000000000000000000, 0.9999999999999997780, 1.000000000000000000, 1.000000000000000000, 1.000000000000000000, 1.000000000000000000, 1.000000000000000222, 1.000000000000000222, 1.000000000000000000, 1.000000000000000000, 1.000000000000000000, 0.9999999999999996669, 1.000000000000000222, 1.000000000000000000, 1.000000000000000000, 0.9999999999999997780, 0.9999999999999997780, 1.000000000000000000, 0.9999999999999996669, 1.000000000000000222, 0.9999999999999997780, 1.000000000000000222, 0.9999999999999997780, 0.9999999999999997780, 1.000000000000000222, 1.000000000000000222, 0.9999999999999997780, 1.000000000000000222, 1.000000000000000000, 1.000000000000000222, 1.000000000000000000, 0.9999999999999997780, 1.000000000000000000, 1.000000000000000000, 1.000000000000000222, 1.000000000000000222, 1.000000000000000000, 0.9999999999999997780, 1.000000000000000000, 1.000000000000000222, 0.9999999999999997780, 1.000000000000000444, 0.9999999999999996669, 1.000000000000000000, 1.000000000000000222, 0.9999999999999997780, 0.9999999999999997780, 0.9999999999999997780, 1.000000000000000000, 0.9999999999999997780, 1.000000000000000000, 0.9999999999999997780, 1.000000000000000222, 1.000000000000000000, 1.000000000000000222, 1.000000000000000000, 0.9999999999999997780, 1.000000000000000000, 1.000000000000000000, 0.9999999999999997780, 1.000000000000000222, 1.000000000000000000, 1.000000000000000000, 1.000000000000000000, 1.000000000000000222, 0.9999999999999996669, 1.000000000000000222, 1.000000000000000000, 1.000000000000000000, 0.9999999999999997780, 1.000000000000000000, 0.9999999999999997780, 1.000000000000000000, 1.000000000000000222, 1.000000000000000000, 0.9999999999999997780, 1.000000000000000222, 1.000000000000000222, 0.9999999999999996669, 1.000000000000000222, 1.000000000000000000, 1.000000000000000444, 0.9999999999999996669, 1.000000000000000000, 1.000000000000000222, 1.000000000000000222, 1.000000000000000222, 1.000000000000000222, 1.000000000000000000, 0.9999999999999997780, 1.000000000000000222, 1.000000000000000000, 1.000000000000000222, 0.9999999999999996669, 1.000000000000000000, 1.000000000000000000, 1.000000000000000222, 1.000000000000000222, 0.9999999999999997780, 1.000000000000000000, 0.9999999999999997780, 1.000000000000000222, 1.000000000000000000, 1.000000000000000222, 1.000000000000000000, 1.000000000000000444, 0.9999999999999996669, 1.000000000000000444, 0.9999999999999996669, 0.9999999999999997780, 0.9999999999999997780, 1.000000000000000222, 1.000000000000000000, 0.9999999999999997780, 1.000000000000000000, 0.9999999999999997780, 0.9999999999999996669, 1.000000000000000222, 1.000000000000000000, 0.9999999999999997780, 1.000000000000000000, 1.000000000000000000, 1.000000000000000222, 1.000000000000000000, 1.000000000000000000, 1.000000000000000444, 0.9999999999999997780, 1.000000000000000222, 1.000000000000000222, 0.9999999999999997780, 1.000000000000000444, 0.9999999999999996669, 1.000000000000000000, 0.9999999999999997780, 1.000000000000000222, 0.9999999999999997780, 1.000000000000000222, 1.000000000000000000, 1.000000000000000222, 0.9999999999999997780, 0.9999999999999997780, 1.000000000000000000, 1.000000000000000000, 0.9999999999999997780, 1.000000000000000222, 0.9999999999999997780, 1.000000000000000000, 1.000000000000000000, 1.000000000000000222, 1.000000000000000000, 0.9999999999999997780, 1.000000000000000222, 1.000000000000000444, 1.000000000000000000, 1.000000000000000000, 1.000000000000000000, 1.000000000000000000, 0.9999999999999997780, 1.000000000000000000, 1.000000000000000222, 1.000000000000000000, 1.000000000000000222, 0.9999999999999996669, 1.000000000000000000, 1.000000000000000000, 0.9999999999999994449, 1.000000000000000444, 1.000000000000000000, 1.000000000000000222, 0.9999999999999997780, 1.000000000000000000, 1.000000000000000222, 1.000000000000000000, 0.9999999999999996669, 1.000000000000000444, 0.9999999999999997780, 1.000000000000000444, 0.9999999999999996669, 1.000000000000000000, 0.9999999999999996669, 1.000000000000000444, 1.000000000000000000, 0.9999999999999997780, 1.000000000000000222, 1.000000000000000000, 0.9999999999999997780, 1.000000000000000444, 1.000000000000000222, 0.9999999999999997780, 1.000000000000000000, 1.000000000000000222, 0.9999999999999997780, 1.000000000000000222, 1.000000000000000222, 1.000000000000000000, 1.000000000000000000, 0.9999999999999996669, 1.000000000000000222, 0.9999999999999997780, 1.000000000000000000, 0.9999999999999997780, 1.000000000000000444, 1.000000000000000000, 1.000000000000000000, 0.9999999999999997780, 1.000000000000000444, 1.000000000000000000, 0.9999999999999997780, 1.000000000000000444, 0.9999999999999996669, 1.000000000000000444, 1.000000000000000000, 1.000000000000000444, 1.000000000000000222, 1.000000000000000222, 0.9999999999999997780, 1.000000000000000000, 0.9999999999999997780, 1.000000000000000444, 0.9999999999999996669, 1.000000000000000000, 1.000000000000000000, 1.000000000000000222, 1.000000000000000000, 1.000000000000000222, 1.000000000000000000, 1.000000000000000000, 0.9999999999999997780, 1.000000000000000000, 1.000000000000000000, 0.9999999999999997780, 1.000000000000000000, 1.000000000000000000, 0.9999999999999997780, 1.000000000000000000, 1.000000000000000222, 1.000000000000000000, 1.000000000000000000, 1.000000000000000000, 1.000000000000000000, 0.9999999999999996669, 1.000000000000000222, 1.000000000000000000, 0.9999999999999997780, 1.000000000000000000, 1.000000000000000222, 1.000000000000000000, 1.000000000000000222, 1.000000000000000222, 1.000000000000000000, 1.000000000000000222, 1.000000000000000000, 1.000000000000000000, 1.000000000000000000, 1.000000000000000222, 0.9999999999999996669, 1.000000000000000222, 0.9999999999999996669, 1.000000000000000222, 1.000000000000000222, 1.000000000000000222, 1.000000000000000222, 0.9999999999999996669, 1.000000000000000444, 1.000000000000000000, 1.000000000000000000, 1.000000000000000222, 1.000000000000000444, 0.9999999999999996669, 1.000000000000000444, 1.000000000000000222, 0.9999999999999996669, 1.000000000000000222, 0.9999999999999997780, 1.000000000000000000, 1.000000000000000000, 0.9999999999999997780, 1.000000000000000000, 0.9999999999999997780, 1.000000000000000000, 1.000000000000000000, 1.000000000000000444, 0.9999999999999997780, 1.000000000000000222, 0.9999999999999997780, 0.9999999999999997780, 1.000000000000000000, 1.000000000000000000, 0.9999999999999996669, 1.000000000000000000, 1.000000000000000222, 1.000000000000000222, 0.9999999999999997780, 1.000000000000000222, 0.9999999999999997780, 0.9999999999999997780, 1.000000000000000000, 1.000000000000000000, 1.000000000000000000, 1.000000000000000222, 1.000000000000000000, 1.000000000000000222, 1.000000000000000000, 0.9999999999999996669, 0.9999999999999997780, 1.000000000000000444, 0.9999999999999996669, 1.000000000000000444, 0.9999999999999997780, 0.9999999999999997780, 1.000000000000000222, 0.9999999999999997780, 1.000000000000000222, 1.000000000000000000, 1.000000000000000000, 0.9999999999999997780, 1.000000000000000222, 1.000000000000000222, 1.000000000000000000, 1.000000000000000222, 1.000000000000000000, 1.000000000000000000, 0.9999999999999997780, 1.000000000000000000, 1.000000000000000000, 0.9999999999999997780, 1.000000000000000000, 0.9999999999999996669, 1.000000000000000222, 0.9999999999999997780, 1.000000000000000222, 0.9999999999999997780, 1.000000000000000000, 0.9999999999999997780, 1.000000000000000222, 0.9999999999999997780, 1.000000000000000000, 1.000000000000000000, 1.000000000000000000, 1.000000000000000000, 0.9999999999999997780, 1.000000000000000222, 1.000000000000000000, 0.9999999999999997780, 1.000000000000000000, 1.000000000000000000, 1.000000000000000222, 1.000000000000000222, 1.000000000000000000, 1.000000000000000222, 1.000000000000000000, 1.000000000000000000, 1.000000000000000000),
 ( 0.3333333333333334259, 0.3333333333333334259, 0.3333333333333334259, 0.3333333333333333703, 0.3333333333333333148, 0.3333333333333333703, 0.3333333333333334259, 0.3333333333333333703, 0.3333333333333333703, 0.3333333333333334259, 0.3333333333333332593, 0.3333333333333334259, 0.3333333333333333703, 0.3333333333333333703, 0.3333333333333333703, 0.3333333333333333703, 0.3333333333333333703, 0.3333333333333333148, 0.3333333333333334259, 0.3333333333333333148, 0.3333333333333334259, 0.3333333333333333148, 0.3333333333333333703, 0.3333333333333333703, 0.3333333333333333148, 0.3333333333333334814, 0.3333333333333332593, 0.3333333333333334814, 0.3333333333333333148, 0.3333333333333333148, 0.3333333333333334259, 0.3333333333333333703, 0.3333333333333334814, 0.3333333333333332593, 0.3333333333333334259, 0.3333333333333333703, 0.3333333333333333703, 0.3333333333333333148, 0.3333333333333333703, 0.3333333333333333703, 0.3333333333333334814, 0.3333333333333333703, 0.3333333333333334259, 0.3333333333333333703, 0.3333333333333333148, 0.3333333333333333148, 0.3333333333333333703, 0.3333333333333334259, 0.3333333333333333703, 0.3333333333333333703, 0.3333333333333333148, 0.3333333333333333703, 0.3333333333333332593, 0.3333333333333334259, 0.3333333333333333148, 0.3333333333333333703, 0.3333333333333333703, 0.3333333333333333703, 0.3333333333333333703, 0.3333333333333335369, 0.3333333333333332593, 0.3333333333333334259, 0.3333333333333333703, 0.3333333333333334259, 0.3333333333333334259, 0.3333333333333333148, 0.3333333333333334259, 0.3333333333333334259, 0.3333333333333334259, 0.3333333333333334814, 0.3333333333333333703, 0.3333333333333333148, 0.3333333333333333148, 0.3333333333333333703, 0.3333333333333334259, 0.3333333333333333703, 0.3333333333333333703, 0.3333333333333333703, 0.3333333333333333703, 0.3333333333333333148, 0.3333333333333333703, 0.3333333333333332593, 0.3333333333333333703, 0.3333333333333333148, 0.3333333333333333148, 0.3333333333333333703, 0.3333333333333333703, 0.3333333333333333148, 0.3333333333333333703, 0.3333333333333333703, 0.3333333333333333703, 0.3333333333333333703, 0.3333333333333334259, 0.3333333333333332593, 0.3333333333333334259, 0.3333333333333333148, 0.3333333333333333703, 0.3333333333333333148, 0.3333333333333334814, 0.3333333333333332038, 0.3333333333333335369, 0.3333333333333332593, 0.3333333333333333703, 0.3333333333333333703, 0.3333333333333333148, 0.3333333333333333703, 0.3333333333333333148, 0.3333333333333334259, 0.3333333333333334259, 0.3333333333333332593, 0.3333333333333334814, 0.3333333333333333703, 0.3333333333333332593, 0.3333333333333334814, 0.3333333333333334259, 0.3333333333333334259, 0.3333333333333332593, 0.3333333333333333703, 0.3333333333333333703, 0.3333333333333334259, 0.3333333333333333703, 0.3333333333333334259, 0.3333333333333333703, 0.3333333333333333148, 0.3333333333333334814, 0.3333333333333333703, 0.3333333333333334259, 0.3333333333333333703, 0.3333333333333333703, 0.3333333333333333148, 0.3333333333333334259, 0.3333333333333334259, 0.3333333333333333703, 0.3333333333333333148, 0.3333333333333333148, 0.3333333333333334259, 0.3333333333333334814, 0.3333333333333333148, 0.3333333333333334259, 0.3333333333333334814, 0.3333333333333333148, 0.3333333333333334814, 0.3333333333333332038, 0.3333333333333333703, 0.3333333333333333148, 0.3333333333333333703, 0.3333333333333334259, 0.3333333333333332038, 0.3333333333333334259, 0.3333333333333333148, 0.3333333333333332038, 0.3333333333333334259, 0.3333333333333333148, 0.3333333333333334259, 0.3333333333333332593, 0.3333333333333334259, 0.3333333333333333703, 0.3333333333333334259, 0.3333333333333333703, 0.3333333333333334259, 0.3333333333333333703, 0.3333333333333333703, 0.3333333333333334814, 0.3333333333333333703, 0.3333333333333335369, 0.3333333333333332038, 0.3333333333333333703, 0.3333333333333333703, 0.3333333333333333703, 0.3333333333333333148, 0.3333333333333333703, 0.3333333333333333703, 0.3333333333333334259, 0.3333333333333333148, 0.3333333333333334259, 0.3333333333333333148, 0.3333333333333334814, 0.3333333333333332593, 0.3333333333333333703, 0.3333333333333334259, 0.3333333333333333148, 0.3333333333333333703, 0.3333333333333333148, 0.3333333333333334259, 0.3333333333333332593, 0.3333333333333333703, 0.3333333333333334814, 0.3333333333333333703, 0.3333333333333333703, 0.3333333333333333703, 0.3333333333333333703, 0.3333333333333333148, 0.3333333333333333703, 0.3333333333333333703, 0.3333333333333334259, 0.3333333333333333703, 0.3333333333333333703, 0.3333333333333333703, 0.3333333333333333703, 0.3333333333333332038, 0.3333333333333334814, 0.3333333333333333703, 0.3333333333333333703, 0.3333333333333333148, 0.3333333333333333148, 0.3333333333333334259, 0.3333333333333334259, 0.3333333333333332593, 0.3333333333333335369, 0.3333333333333332593, 0.3333333333333334814, 0.3333333333333332593, 0.3333333333333334259, 0.3333333333333332038, 0.3333333333333335369, 0.3333333333333333148, 0.3333333333333333703, 0.3333333333333334259, 0.3333333333333333148, 0.3333333333333333148, 0.3333333333333335369, 0.3333333333333334259, 0.3333333333333333703, 0.3333333333333333148, 0.3333333333333334259, 0.3333333333333333148, 0.3333333333333334259, 0.3333333333333334259, 0.3333333333333333703, 0.3333333333333333703, 0.3333333333333333148, 0.3333333333333333703, 0.3333333333333333703, 0.3333333333333334259, 0.3333333333333333703, 0.3333333333333335369, 0.3333333333333333148, 0.3333333333333333703, 0.3333333333333332593, 0.3333333333333335369, 0.3333333333333333148, 0.3333333333333333148, 0.3333333333333334814, 0.3333333333333332593, 0.3333333333333334814, 0.3333333333333333703, 0.3333333333333334259, 0.3333333333333334814, 0.3333333333333333703, 0.3333333333333333703, 0.3333333333333333148, 0.3333333333333332593, 0.3333333333333334814, 0.3333333333333333148, 0.3333333333333333703, 0.3333333333333333703, 0.3333333333333333703, 0.3333333333333333703, 0.3333333333333334259, 0.3333333333333333703, 0.3333333333333333703, 0.3333333333333333148, 0.3333333333333333703, 0.3333333333333334259, 0.3333333333333332593, 0.3333333333333334814, 0.3333333333333333703, 0.3333333333333333703, 0.3333333333333334259, 0.3333333333333333703, 0.3333333333333334259, 0.3333333333333333703, 0.3333333333333334259, 0.3333333333333332593, 0.3333333333333333703, 0.3333333333333334259, 0.3333333333333333148, 0.3333333333333333148, 0.3333333333333333703, 0.3333333333333334814, 0.3333333333333333148, 0.3333333333333333703, 0.3333333333333334259, 0.3333333333333333703, 0.3333333333333333703, 0.3333333333333333148, 0.3333333333333333703, 0.3333333333333333148, 0.3333333333333335369, 0.3333333333333332593, 0.3333333333333333703, 0.3333333333333333148, 0.3333333333333333703, 0.3333333333333334259, 0.3333333333333334259, 0.3333333333333333703, 0.3333333333333333148, 0.3333333333333334259, 0.3333333333333334259, 0.3333333333333333148, 0.3333333333333334259, 0.3333333333333335369, 0.3333333333333332593, 0.3333333333333333703, 0.3333333333333335369, 0.3333333333333332038, 0.3333333333333334259, 0.3333333333333333148, 0.3333333333333333703, 0.3333333333333333703, 0.3333333333333333703, 0.3333333333333333148, 0.3333333333333333703, 0.3333333333333333703, 0.3333333333333334259, 0.3333333333333334259, 0.3333333333333333148, 0.3333333333333334259, 0.3333333333333333148, 0.3333333333333333703, 0.3333333333333333148, 0.3333333333333334259, 0.3333333333333332038, 0.3333333333333333703, 0.3333333333333334259, 0.3333333333333335369, 0.3333333333333333148, 0.3333333333333333703, 0.3333333333333333703, 0.3333333333333333703, 0.3333333333333333703, 0.3333333333333333703, 0.3333333333333333703, 0.3333333333333334259, 0.3333333333333333703, 0.3333333333333333703, 0.3333333333333333703, 0.3333333333333332038, 0.3333333333333333703, 0.3333333333333335369, 0.3333333333333333148, 0.3333333333333334814, 0.3333333333333333703, 0.3333333333333332593, 0.3333333333333335369, 0.3333333333333333148, 0.3333333333333333703, 0.3333333333333333703, 0.3333333333333333148, 0.3333333333333333703, 0.3333333333333334259, 0.3333333333333334259, 0.3333333333333333703, 0.3333333333333334259, 0.3333333333333333148, 0.3333333333333333703, 0.3333333333333332593, 0.3333333333333333703, 0.3333333333333333703, 0.3333333333333333703, 0.3333333333333333703, 0.3333333333333333703, 0.3333333333333333703, 0.3333333333333333148, 0.3333333333333334259, 0.3333333333333333703, 0.3333333333333334259, 0.3333333333333333148, 0.3333333333333334259, 0.3333333333333333148, 0.3333333333333333703, 0.3333333333333334259, 0.3333333333333333703, 0.3333333333333333148, 0.3333333333333333148, 0.3333333333333334259, 0.3333333333333333703, 0.3333333333333333703, 0.3333333333333334259, 0.3333333333333333703, 0.3333333333333333148, 0.3333333333333334814, 0.3333333333333333703, 0.3333333333333334259, 0.3333333333333333703, 0.3333333333333333703, 0.3333333333333333703),
 ( 0.3333333333333334259, 0.3333333333333334259, 0.3333333333333334259, 0.3333333333333333703, 0.3333333333333333148, 0.3333333333333333703, 0.3333333333333334259, 0.3333333333333333703, 0.3333333333333333703, 0.3333333333333334259, 0.3333333333333332593, 0.3333333333333334259, 0.3333333333333333703, 0.3333333333333333703, 0.3333333333333333703, 0.3333333333333333703, 0.3333333333333333703, 0.3333333333333333148, 0.3333333333333334259, 0.3333333333333333148, 0.3333333333333334259, 0.3333333333333333148, 0.3333333333333333703, 0.3333333333333333703, 0.3333333333333333148, 0.3333333333333334814, 0.3333333333333332593, 0.3333333333333334814, 0.3333333333333333148, 0.3333333333333333148, 0.3333333333333334259, 0.3333333333333333703, 0.3333333333333334814, 0.3333333333333332593, 0.3333333333333334259, 0.3333333333333333703, 0.3333333333333333703, 0.3333333333333333148, 0.3333333333333333703, 0.3333333333333333703, 0.3333333333333334814, 0.3333333333333333703, 0.3333333333333334259, 0.3333333333333333703, 0.3333333333333333148, 0.3333333333333333148, 0.3333333333333333703, 0.3333333333333334259, 0.3333333333333333703, 0.3333333333333333703, 0.3333333333333333148, 0.3333333333333333703, 0.3333333333333332593, 0.3333333333333334259, 0.3333333333333333148, 0.3333333333333333703, 0.3333333333333333703, 0.3333333333333333703, 0.3333333333333333703, 0.3333333333333335369, 0.3333333333333332593, 0.3333333333333334259, 0.3333333333333333703, 0.3333333333333334259, 0.3333333333333334259, 0.3333333333333333148, 0.3333333333333334259, 0.3333333333333334259, 0.3333333333333334259, 0.3333333333333334814, 0.3333333333333333703, 0.3333333333333333148, 0.3333333333333333148, 0.3333333333333333703, 0.3333333333333334259, 0.3333333333333333703, 0.3333333333333333703, 0.3333333333333333703, 0.3333333333333333703, 0.3333333333333333148, 0.3333333333333333703, 0.3333333333333332593, 0.3333333333333333703, 0.3333333333333333148, 0.3333333333333333148, 0.3333333333333333703, 0.3333333333333333703, 0.3333333333333333148, 0.3333333333333333703, 0.3333333333333333703, 0.3333333333333333703, 0.3333333333333333703, 0.3333333333333334259, 0.3333333333333332593, 0.3333333333333334259, 0.3333333333333333148, 0.3333333333333333703, 0.3333333333333333148, 0.3333333333333334814, 0.3333333333333332038, 0.3333333333333335369, 0.3333333333333332593, 0.3333333333333333703, 0.3333333333333333703, 0.3333333333333333148, 0.3333333333333333703, 0.3333333333333333148, 0.3333333333333334259, 0.3333333333333334259, 0.3333333333333332593, 0.3333333333333334814, 0.3333333333333333703, 0.3333333333333332593, 0.3333333333333334814, 0.3333333333333334259, 0.3333333333333334259, 0.3333333333333332593, 0.3333333333333333703, 0.3333333333333333703, 0.3333333333333334259, 0.3333333333333333703, 0.3333333333333334259, 0.3333333333333333703, 0.3333333333333333148, 0.3333333333333334814, 0.3333333333333333703, 0.3333333333333334259, 0.3333333333333333703, 0.3333333333333333703, 0.3333333333333333148, 0.3333333333333334259, 0.3333333333333334259, 0.3333333333333333703, 0.3333333333333333148, 0.3333333333333333148, 0.3333333333333334259, 0.3333333333333334814, 0.3333333333333333148, 0.3333333333333334259, 0.3333333333333334814, 0.3333333333333333148, 0.3333333333333334814, 0.3333333333333332038, 0.3333333333333333703, 0.3333333333333333148, 0.3333333333333333703, 0.3333333333333334259, 0.3333333333333332038, 0.3333333333333334259, 0.3333333333333333148, 0.3333333333333332038, 0.3333333333333334259, 0.3333333333333333148, 0.3333333333333334259, 0.3333333333333332593, 0.3333333333333334259, 0.3333333333333333703, 0.3333333333333334259, 0.3333333333333333703, 0.3333333333333334259, 0.3333333333333333703, 0.3333333333333333703, 0.3333333333333334814, 0.3333333333333333703, 0.3333333333333335369, 0.3333333333333332038, 0.3333333333333333703, 0.3333333333333333703, 0.3333333333333333703, 0.3333333333333333148, 0.3333333333333333703, 0.3333333333333333703, 0.3333333333333334259, 0.3333333333333333148, 0.3333333333333334259, 0.3333333333333333148, 0.3333333333333334814, 0.3333333333333332593, 0.3333333333333333703, 0.3333333333333334259, 0.3333333333333333148, 0.3333333333333333703, 0.3333333333333333148, 0.3333333333333334259, 0.3333333333333332593, 0.3333333333333333703, 0.3333333333333334814, 0.3333333333333333703, 0.3333333333333333703, 0.3333333333333333703, 0.3333333333333333703, 0.3333333333333333148, 0.3333333333333333703, 0.3333333333333333703, 0.3333333333333334259, 0.3333333333333333703, 0.3333333333333333703, 0.3333333333333333703, 0.3333333333333333703, 0.3333333333333332038, 0.3333333333333334814, 0.3333333333333333703, 0.3333333333333333703, 0.3333333333333333148, 0.3333333333333333148, 0.3333333333333334259, 0.3333333333333334259, 0.3333333333333332593, 0.3333333333333335369, 0.3333333333333332593, 0.3333333333333334814, 0.3333333333333332593, 0.3333333333333334259, 0.3333333333333332038, 0.3333333333333335369, 0.3333333333333333148, 0.3333333333333333703, 0.3333333333333334259, 0.3333333333333333148, 0.3333333333333333148, 0.3333333333333335369, 0.3333333333333334259, 0.3333333333333333703, 0.3333333333333333148, 0.3333333333333334259, 0.3333333333333333148, 0.3333333333333334259, 0.3333333333333334259, 0.3333333333333333703, 0.3333333333333333703, 0.3333333333333333148, 0.3333333333333333703, 0.3333333333333333703, 0.3333333333333334259, 0.3333333333333333703, 0.3333333333333335369, 0.3333333333333333148, 0.3333333333333333703, 0.3333333333333332593, 0.3333333333333335369, 0.3333333333333333148, 0.3333333333333333148, 0.3333333333333334814, 0.3333333333333332593, 0.3333333333333334814, 0.3333333333333333703, 0.3333333333333334259, 0.3333333333333334814, 0.3333333333333333703, 0.3333333333333333703, 0.3333333333333333148, 0.3333333333333332593, 0.3333333333333334814, 0.3333333333333333148, 0.3333333333333333703, 0.3333333333333333703, 0.3333333333333333703, 0.3333333333333333703, 0.3333333333333334259, 0.3333333333333333703, 0.3333333333333333703, 0.3333333333333333148, 0.3333333333333333703, 0.3333333333333334259, 0.3333333333333332593, 0.3333333333333334814, 0.3333333333333333703, 0.3333333333333333703, 0.3333333333333334259, 0.3333333333333333703, 0.3333333333333334259, 0.3333333333333333703, 0.3333333333333334259, 0.3333333333333332593, 0.3333333333333333703, 0.3333333333333334259, 0.3333333333333333148, 0.3333333333333333148, 0.3333333333333333703, 0.3333333333333334814, 0.3333333333333333148, 0.3333333333333333703, 0.3333333333333334259, 0.3333333333333333703, 0.3333333333333333703, 0.3333333333333333148, 0.3333333333333333703, 0.3333333333333333148, 0.3333333333333335369, 0.3333333333333332593, 0.3333333333333333703, 0.3333333333333333148, 0.3333333333333333703, 0.3333333333333334259, 0.3333333333333334259, 0.3333333333333333703, 0.3333333333333333148, 0.3333333333333334259, 0.3333333333333334259, 0.3333333333333333148, 0.3333333333333334259, 0.3333333333333335369, 0.3333333333333332593, 0.3333333333333333703, 0.3333333333333335369, 0.3333333333333332038, 0.3333333333333334259, 0.3333333333333333148, 0.3333333333333333703, 0.3333333333333333703, 0.3333333333333333703, 0.3333333333333333148, 0.3333333333333333703, 0.3333333333333333703, 0.3333333333333334259, 0.3333333333333334259, 0.3333333333333333148, 0.3333333333333334259, 0.3333333333333333148, 0.3333333333333333703, 0.3333333333333333148, 0.3333333333333334259, 0.3333333333333332038, 0.3333333333333333703, 0.3333333333333334259, 0.3333333333333335369, 0.3333333333333333148, 0.3333333333333333703, 0.3333333333333333703, 0.3333333333333333703, 0.3333333333333333703, 0.3333333333333333703, 0.3333333333333333703, 0.3333333333333334259, 0.3333333333333333703, 0.3333333333333333703, 0.3333333333333333703, 0.3333333333333332038, 0.3333333333333333703, 0.3333333333333335369, 0.3333333333333333148, 0.3333333333333334814, 0.3333333333333333703, 0.3333333333333332593, 0.3333333333333335369, 0.3333333333333333148, 0.3333333333333333703, 0.3333333333333333703, 0.3333333333333333148, 0.3333333333333333703, 0.3333333333333334259, 0.3333333333333334259, 0.3333333333333333703, 0.3333333333333334259, 0.3333333333333333148, 0.3333333333333333703, 0.3333333333333332593, 0.3333333333333333703, 0.3333333333333333703, 0.3333333333333333703, 0.3333333333333333703, 0.3333333333333333703, 0.3333333333333333703, 0.3333333333333333148, 0.3333333333333334259, 0.3333333333333333703, 0.3333333333333334259, 0.3333333333333333148, 0.3333333333333334259, 0.3333333333333333148, 0.3333333333333333703, 0.3333333333333334259, 0.3333333333333333703, 0.3333333333333333148, 0.3333333333333333148, 0.3333333333333334259, 0.3333333333333333703, 0.3333333333333333703, 0.3333333333333334259, 0.3333333333333333703, 0.3333333333333333148, 0.3333333333333334814, 0.3333333333333333703, 0.3333333333333334259, 0.3333333333333333703, 0.3333333333333333703, 0.3333333333333333703),
 ( 1.000000000000000222, 1.000000000000000222, 1.000000000000000222, 1.000000000000000222, 0.9999999999999996669, 0.9999999999999997780, 1.000000000000000444, 1.000000000000000000, 1.000000000000000000, 1.000000000000000000, 0.9999999999999997780, 1.000000000000000000, 1.000000000000000000, 1.000000000000000000, 1.000000000000000000, 0.9999999999999997780, 1.000000000000000222, 0.9999999999999996669, 1.000000000000000000, 0.9999999999999997780, 1.000000000000000222, 1.000000000000000000, 1.000000000000000222, 0.9999999999999996669, 1.000000000000000000, 1.000000000000000222, 0.9999999999999996669, 1.000000000000000444, 1.000000000000000000, 0.9999999999999997780, 1.000000000000000222, 1.000000000000000222, 1.000000000000000222, 1.000000000000000000, 1.000000000000000000, 0.9999999999999997780, 1.000000000000000000, 1.000000000000000000, 1.000000000000000000, 1.000000000000000000, 1.000000000000000222, 1.000000000000000222, 1.000000000000000000, 1.000000000000000000, 1.000000000000000000, 0.9999999999999996669, 1.000000000000000222, 1.000000000000000000, 1.000000000000000000, 0.9999999999999997780, 0.9999999999999997780, 1.000000000000000000, 0.9999999999999996669, 1.000000000000000222, 0.9999999999999997780, 1.000000000000000222, 0.9999999999999997780, 0.9999999999999997780, 1.000000000000000222, 1.000000000000000222, 0.9999999999999997780, 1.000000000000000222, 1.000000000000000000, 1.000000000000000222, 1.000000000000000000, 0.9999999999999997780, 1.000000000000000000, 1.000000000000000000, 1.000000000000000222, 1.000000000000000222, 1.000000000000000000, 0.9999999999999997780, 1.000000000000000000, 1.000000000000000222, 0.9999999999999997780, 1.000000000000000444, 0.9999999999999996669, 1.000000000000000000, 1.000000000000000222, 0.9999999999999997780, 0.9999999999999997780, 0.9999999999999997780, 1.000000000000000000, 0.9999999999999997780, 1.000000000000000000, 0.9999999999999997780, 1.000000000000000222, 1.000000000000000000, 1.000000000000000222, 1.000000000000000000, 0.9999999999999997780, 1.000000000000000000, 1.000000000000000000, 0.9999999999999997780, 1.000000000000000222, 1.000000000000000000, 1.000000000000000000, 1.000000000000000000, 1.000000000000000222, 0.9999999999999996669, 1.000000000000000222, 1.000000000000000000, 1.000000000000000000, 0.9999999999999997780, 1.000000000000000000, 0.9999999999999997780, 1.000000000000000000, 1.000000000000000222, 1.000000000000000000, 0.9999999999999997780, 1.000000000000000222, 1.000000000000000222, 0.9999999999999996669, 1.000000000000000222, 1.000000000000000000, 1.000000000000000444, 0.9999999999999996669, 1.000000000000000000, 1.000000000000000222, 1.000000000000000222, 1.000000000000000222, 1.000000000000000222, 1.000000000000000000, 0.9999999999999997780, 1.000000000000000222, 1.000000000000000000, 1.000000000000000222, 0.9999999999999996669, 1.000000000000000000, 1.000000000000000000, 1.000000000000000222, 1.000000000000000222, 0.9999999999999997780, 1.000000000000000000, 0.9999999999999997780, 1.000000000000000222, 1.000000000000000000, 1.000000000000000222, 1.000000000000000000, 1.000000000000000444, 0.9999999999999996669, 1.000000000000000444, 0.9999999999999996669, 0.9999999999999997780, 0.9999999999999997780, 1.000000000000000222, 1.000000000000000000, 0.9999999999999997780, 1.000000000000000000, 0.9999999999999997780, 0.9999999999999996669, 1.000000000000000222, 1.000000000000000000, 0.9999999999999997780, 1.000000000000000000, 1.000000000000000000, 1.000000000000000222, 1.000000000000000000, 1.000000000000000000, 1.000000000000000444, 0.9999999999999997780, 1.000000000000000222, 1.000000000000000222, 0.9999999999999997780, 1.000000000000000444, 0.9999999999999996669, 1.000000000000000000, 0.9999999999999997780, 1.000000000000000222, 0.9999999999999997780, 1.000000000000000222, 1.000000000000000000, 1.000000000000000222, 0.9999999999999997780, 0.9999999999999997780, 1.000000000000000000, 1.000000000000000000, 0.9999999999999997780, 1.000000000000000222, 0.9999999999999997780, 1.000000000000000000, 1.000000000000000000, 1.000000000000000222, 1.000000000000000000, 0.9999999999999997780, 1.000000000000000222, 1.000000000000000444, 1.000000000000000000, 1.000000000000000000, 1.000000000000000000, 1.000000000000000000, 0.9999999999999997780, 1.000000000000000000, 1.000000000000000222, 1.000000000000000000, 1.000000000000000222, 0.9999999999999996669, 1.000000000000000000, 1.000000000000000000, 0.9999999999999994449, 1.000000000000000444, 1.000000000000000000, 1.000000000000000222, 0.9999999999999997780, 1.000000000000000000, 1.000000000000000222, 1.000000000000000000, 0.9999999999999996669, 1.000000000000000444, 0.9999999999999997780, 1.000000000000000444, 0.9999999999999996669, 1.000000000000000000, 0.9999999999999996669, 1.000000000000000444, 1.000000000000000000, 0.9999999999999997780, 1.000000000000000222, 1.000000000000000000, 0.9999999999999997780, 1.000000000000000444, 1.000000000000000222, 0.9999999999999997780, 1.000000000000000000, 1.000000000000000222, 0.9999999999999997780, 1.000000000000000222, 1.000000000000000222, 1.000000000000000000, 1.000000000000000000, 0.9999999999999996669, 1.000000000000000222, 0.9999999999999997780, 1.000000000000000000, 0.9999999999999997780, 1.000000000000000444, 1.000000000000000000, 1.000000000000000000, 0.9999999999999997780, 1.000000000000000444, 1.000000000000000000, 0.9999999999999997780, 1.000000000000000444, 0.9999999999999996669, 1.000000000000000444, 1.000000000000000000, 1.000000000000000444, 1.000000000000000222, 1.000000000000000222, 0.9999999999999997780, 1.000000000000000000, 0.9999999999999997780, 1.000000000000000444, 0.9999999999999996669, 1.000000000000000000, 1.000000000000000000, 1.000000000000000222, 1.000000000000000000, 1.000000000000000222, 1.000000000000000000, 1.000000000000000000, 0.9999999999999997780, 1.000000000000000000, 1.000000000000000000, 0.9999999999999997780, 1.000000000000000000, 1.000000000000000000, 0.9999999999999997780, 1.000000000000000000, 1.000000000000000222, 1.000000000000000000, 1.000000000000000000, 1.000000000000000000, 1.000000000000000000, 0.9999999999999996669, 1.000000000000000222, 1.000000000000000000, 0.9999999999999997780, 1.000000000000000000, 1.000000000000000222, 1.000000000000000000, 1.000000000000000222, 1.000000000000000222, 1.000000000000000000, 1.000000000000000222, 1.000000000000000000, 1.000000000000000000, 1.000000000000000000, 1.000000000000000222, 0.9999999999999996669, 1.000000000000000222, 0.9999999999999996669, 1.000000000000000222, 1.000000000000000222, 1.000000000000000222, 1.000000000000000222, 0.9999999999999996669, 1.000000000000000444, 1.000000000000000000, 1.000000000000000000, 1.000000000000000222, 1.000000000000000444, 0.9999999999999996669, 1.000000000000000444, 1.000000000000000222, 0.9999999999999996669, 1.000000000000000222, 0.9999999999999997780, 1.000000000000000000, 1.000000000000000000, 0.9999999999999997780, 1.000000000000000000, 0.9999999999999997780, 1.000000000000000000, 1.000000000000000000, 1.000000000000000444, 0.9999999999999997780, 1.000000000000000222, 0.9999999999999997780, 0.9999999999999997780, 1.000000000000000000, 1.000000000000000000, 0.9999999999999996669, 1.000000000000000000, 1.000000000000000222, 1.000000000000000222, 0.9999999999999997780, 1.000000000000000222, 0.9999999999999997780, 0.9999999999999997780, 1.000000000000000000, 1.000000000000000000, 1.000000000000000000, 1.000000000000000222, 1.000000000000000000, 1.000000000000000222, 1.000000000000000000, 0.9999999999999996669, 0.9999999999999997780, 1.000000000000000444, 0.9999999999999996669, 1.000000000000000444, 0.9999999999999997780, 0.9999999999999997780, 1.000000000000000222, 0.9999999999999997780, 1.000000000000000222, 1.000000000000000000, 1.000000000000000000, 0.9999999999999997780, 1.000000000000000222, 1.000000000000000222, 1.000000000000000000, 1.000000000000000222, 1.000000000000000000, 1.000000000000000000, 0.9999999999999997780, 1.000000000000000000, 1.000000000000000000, 0.9999999999999997780, 1.000000000000000000, 0.9999999999999996669, 1.000000000000000222, 0.9999999999999997780, 1.000000000000000222, 0.9999999999999997780, 1.000000000000000000, 0.9999999999999997780, 1.000000000000000222, 0.9999999999999997780, 1.000000000000000000, 1.000000000000000000, 1.000000000000000000, 1.000000000000000000, 0.9999999999999997780, 1.000000000000000222, 1.000000000000000000, 0.9999999999999997780, 1.000000000000000000, 1.000000000000000000, 1.000000000000000222, 1.000000000000000222, 1.000000000000000000, 1.000000000000000222, 1.000000000000000000, 1.000000000000000000, 1.000000000000000000),
 ( 0.3333333333333334259, 0.3333333333333334259, 0.3333333333333334259, 0.3333333333333333703, 0.3333333333333333148, 0.3333333333333333703, 0.3333333333333334259, 0.3333333333333333703, 0.3333333333333333703, 0.3333333333333334259, 0.3333333333333332593, 0.3333333333333334259, 0.3333333333333333703, 0.3333333333333333703, 0.3333333333333333703, 0.3333333333333333703, 0.3333333333333333703, 0.3333333333333333148, 0.3333333333333334259, 0.3333333333333333148, 0.3333333333333334259, 0.3333333333333333148, 0.3333333333333333703, 0.3333333333333333703, 0.3333333333333333148, 0.3333333333333334814, 0.3333333333333332593, 0.3333333333333334814, 0.3333333333333333148, 0.3333333333333333148, 0.3333333333333334259, 0.3333333333333333703, 0.3333333333333334814, 0.3333333333333332593, 0.3333333333333334259, 0.3333333333333333703, 0.3333333333333333703, 0.3333333333333333148, 0.3333333333333333703, 0.3333333333333333703, 0.3333333333333334814, 0.3333333333333333703, 0.3333333333333334259, 0.3333333333333333703, 0.3333333333333333148, 0.3333333333333333148, 0.3333333333333333703, 0.3333333333333334259, 0.3333333333333333703, 0.3333333333333333703, 0.3333333333333333148, 0.3333333333333333703, 0.3333333333333332593, 0.3333333333333334259, 0.3333333333333333148, 0.3333333333333333703, 0.3333333333333333703, 0.3333333333333333703, 0.3333333333333333703, 0.3333333333333335369, 0.3333333333333332593, 0.3333333333333334259, 0.3333333333333333703, 0.3333333333333334259, 0.3333333333333334259, 0.3333333333333333148, 0.3333333333333334259, 0.3333333333333334259, 0.3333333333333334259, 0.3333333333333334814, 0.3333333333333333703, 0.3333333333333333148, 0.3333333333333333148, 0.3333333333333333703, 0.3333333333333334259, 0.3333333333333333703, 0.3333333333333333703, 0.3333333333333333703, 0.3333333333333333703, 0.3333333333333333148, 0.3333333333333333703, 0.3333333333333332593, 0.3333333333333333703, 0.3333333333333333148, 0.3333333333333333148, 0.3333333333333333703, 0.3333333333333333703, 0.3333333333333333148, 0.3333333333333333703, 0.3333333333333333703, 0.3333333333333333703, 0.3333333333333333703, 0.3333333333333334259, 0.3333333333333332593, 0.3333333333333334259, 0.3333333333333333148, 0.3333333333333333703, 0.3333333333333333148, 0.3333333333333334814, 0.3333333333333332038, 0.3333333333333335369, 0.3333333333333332593, 0.3333333333333333703, 0.3333333333333333703, 0.3333333333333333148, 0.3333333333333333703, 0.3333333333333333148, 0.3333333333333334259, 0.3333333333333334259, 0.3333333333333332593, 0.3333333333333334814, 0.3333333333333333703, 0.3333333333333332593, 0.3333333333333334814, 0.3333333333333334259, 0.3333333333333334259, 0.3333333333333332593, 0.3333333333333333703, 0.3333333333333333703, 0.3333333333333334259, 0.3333333333333333703, 0.3333333333333334259, 0.3333333333333333703, 0.3333333333333333148, 0.3333333333333334814, 0.3333333333333333703, 0.3333333333333334259, 0.3333333333333333703, 0.3333333333333333703, 0.3333333333333333148, 0.3333333333333334259, 0.3333333333333334259, 0.3333333333333333703, 0.3333333333333333148, 0.3333333333333333148, 0.3333333333333334259, 0.3333333333333334814, 0.3333333333333333148, 0.3333333333333334259, 0.3333333333333334814, 0.3333333333333333148, 0.3333333333333334814, 0.3333333333333332038, 0.3333333333333333703, 0.3333333333333333148, 0.3333333333333333703, 0.3333333333333334259, 0.3333333333333332038, 0.3333333333333334259, 0.3333333333333333148, 0.3333333333333332038, 0.3333333333333334259, 0.3333333333333333148, 0.3333333333333334259, 0.3333333333333332593, 0.3333333333333334259, 0.3333333333333333703, 0.3333333333333334259, 0.3333333333333333703, 0.3333333333333334259, 0.3333333333333333703, 0.3333333333333333703, 0.3333333333333334814, 0.3333333333333333703, 0.3333333333333335369, 0.3333333333333332038, 0.3333333333333333703, 0.3333333333333333703, 0.3333333333333333703, 0.3333333333333333148, 0.3333333333333333703, 0.3333333333333333703, 0.3333333333333334259, 0.3333333333333333148, 0.3333333333333334259, 0.3333333333333333148, 0.3333333333333334814, 0.3333333333333332593, 0.3333333333333333703, 0.3333333333333334259, 0.3333333333333333148, 0.3333333333333333703, 0.3333333333333333148, 0.3333333333333334259, 0.3333333333333332593, 0.3333333333333333703, 0.3333333333333334814, 0.3333333333333333703, 0.3333333333333333703, 0.3333333333333333703, 0.3333333333333333703, 0.3333333333333333148, 0.3333333333333333703, 0.3333333333333333703, 0.3333333333333334259, 0.3333333333333333703, 0.3333333333333333703, 0.3333333333333333703, 0.3333333333333333703, 0.3333333333333332038, 0.3333333333333334814, 0.3333333333333333703, 0.3333333333333333703, 0.3333333333333333148, 0.3333333333333333148, 0.3333333333333334259, 0.3333333333333334259, 0.3333333333333332593, 0.3333333333333335369, 0.3333333333333332593, 0.3333333333333334814, 0.3333333333333332593, 0.3333333333333334259, 0.3333333333333332038, 0.3333333333333335369, 0.3333333333333333148, 0.3333333333333333703, 0.3333333333333334259, 0.3333333333333333148, 0.3333333333333333148, 0.3333333333333335369, 0.3333333333333334259, 0.3333333333333333703, 0.3333333333333333148, 0.3333333333333334259, 0.3333333333333333148, 0.3333333333333334259, 0.3333333333333334259, 0.3333333333333333703, 0.3333333333333333703, 0.3333333333333333148, 0.3333333333333333703, 0.3333333333333333703, 0.3333333333333334259, 0.3333333333333333703, 0.3333333333333335369, 0.3333333333333333148, 0.3333333333333333703, 0.3333333333333332593, 0.3333333333333335369, 0.3333333333333333148, 0.3333333333333333148, 0.3333333333333334814, 0.3333333333333332593, 0.3333333333333334814, 0.3333333333333333703, 0.3333333333333334259, 0.3333333333333334814, 0.3333333333333333703, 0.3333333333333333703, 0.3333333333333333148, 0.3333333333333332593, 0.3333333333333334814, 0.3333333333333333148, 0.3333333333333333703, 0.3333333333333333703, 0.3333333333333333703, 0.3333333333333333703, 0.3333333333333334259, 0.3333333333333333703, 0.3333333333333333703, 0.3333333333333333148, 0.3333333333333333703, 0.3333333333333334259, 0.3333333333333332593, 0.3333333333333334814, 0.3333333333333333703, 0.3333333333333333703, 0.3333333333333334259, 0.3333333333333333703, 0.3333333333333334259, 0.3333333333333333703, 0.3333333333333334259, 0.3333333333333332593, 0.3333333333333333703, 0.3333333333333334259, 0.3333333333333333148, 0.3333333333333333148, 0.3333333333333333703, 0.3333333333333334814, 0.3333333333333333148, 0.3333333333333333703, 0.3333333333333334259, 0.3333333333333333703, 0.3333333333333333703, 0.3333333333333333148, 0.3333333333333333703, 0.3333333333333333148, 0.3333333333333335369, 0.3333333333333332593, 0.3333333333333333703, 0.3333333333333333148, 0.3333333333333333703, 0.3333333333333334259, 0.3333333333333334259, 0.3333333333333333703, 0.3333333333333333148, 0.3333333333333334259, 0.3333333333333334259, 0.3333333333333333148, 0.3333333333333334259, 0.3333333333333335369, 0.3333333333333332593, 0.3333333333333333703, 0.3333333333333335369, 0.3333333333333332038, 0.3333333333333334259, 0.3333333333333333148, 0.3333333333333333703, 0.3333333333333333703, 0.3333333333333333703, 0.3333333333333333148, 0.3333333333333333703, 0.3333333333333333703, 0.3333333333333334259, 0.3333333333333334259, 0.3333333333333333148, 0.3333333333333334259, 0.3333333333333333148, 0.3333333333333333703, 0.3333333333333333148, 0.3333333333333334259, 0.3333333333333332038, 0.3333333333333333703, 0.3333333333333334259, 0.3333333333333335369, 0.3333333333333333148, 0.3333333333333333703, 0.3333333333333333703, 0.3333333333333333703, 0.3333333333333333703, 0.3333333333333333703, 0.3333333333333333703, 0.3333333333333334259, 0.3333333333333333703, 0.3333333333333333703, 0.3333333333333333703, 0.3333333333333332038, 0.3333333333333333703, 0.3333333333333335369, 0.3333333333333333148, 0.3333333333333334814, 0.3333333333333333703, 0.3333333333333332593, 0.3333333333333335369, 0.3333333333333333148, 0.3333333333333333703, 0.3333333333333333703, 0.3333333333333333148, 0.3333333333333333703, 0.3333333333333334259, 0.3333333333333334259, 0.3333333333333333703, 0.3333333333333334259, 0.3333333333333333148, 0.3333333333333333703, 0.3333333333333332593, 0.3333333333333333703, 0.3333333333333333703, 0.3333333333333333703, 0.3333333333333333703, 0.3333333333333333703, 0.3333333333333333703, 0.3333333333333333148, 0.3333333333333334259, 0.3333333333333333703, 0.3333333333333334259, 0.3333333333333333148, 0.3333333333333334259, 0.3333333333333333148, 0.3333333333333333703, 0.3333333333333334259, 0.3333333333333333703, 0.3333333333333333148, 0.3333333333333333148, 0.3333333333333334259, 0.3333333333333333703, 0.3333333333333333703, 0.3333333333333334259, 0.3333333333333333703, 0.3333333333333333148, 0.3333333333333334814, 0.3333333333333333703, 0.3333333333333334259, 0.3333333333333333703, 0.3333333333333333703, 0.3333333333333333703),
 ( 0.3333333333333334259, 0.3333333333333334259, 0.3333333333333334259, 0.3333333333333333703, 0.3333333333333333148, 0.3333333333333333703, 0.3333333333333334259, 0.3333333333333333703, 0.3333333333333333703, 0.3333333333333334259, 0.3333333333333332593, 0.3333333333333334259, 0.3333333333333333703, 0.3333333333333333703, 0.3333333333333333703, 0.3333333333333333703, 0.3333333333333333703, 0.3333333333333333148, 0.3333333333333334259, 0.3333333333333333148, 0.3333333333333334259, 0.3333333333333333148, 0.3333333333333333703, 0.3333333333333333703, 0.3333333333333333148, 0.3333333333333334814, 0.3333333333333332593, 0.3333333333333334814, 0.3333333333333333148, 0.3333333333333333148, 0.3333333333333334259, 0.3333333333333333703, 0.3333333333333334814, 0.3333333333333332593, 0.3333333333333334259, 0.3333333333333333703, 0.3333333333333333703, 0.3333333333333333148, 0.3333333333333333703, 0.3333333333333333703, 0.3333333333333334814, 0.3333333333333333703, 0.3333333333333334259, 0.3333333333333333703, 0.3333333333333333148, 0.3333333333333333148, 0.3333333333333333703, 0.3333333333333334259, 0.3333333333333333703, 0.3333333333333333703, 0.3333333333333333148, 0.3333333333333333703, 0.3333333333333332593, 0.3333333333333334259, 0.3333333333333333148, 0.3333333333333333703, 0.3333333333333333703, 0.3333333333333333703, 0.3333333333333333703, 0.3333333333333335369, 0.3333333333333332593, 0.3333333333333334259, 0.3333333333333333703, 0.3333333333333334259, 0.3333333333333334259, 0.3333333333333333148, 0.3333333333333334259, 0.3333333333333334259, 0.3333333333333334259, 0.3333333333333334814, 0.3333333333333333703, 0.3333333333333333148, 0.3333333333333333148, 0.3333333333333333703, 0.3333333333333334259, 0.3333333333333333703, 0.3333333333333333703, 0.3333333333333333703, 0.3333333333333333703, 0.3333333333333333148, 0.3333333333333333703, 0.3333333333333332593, 0.3333333333333333703, 0.3333333333333333148, 0.3333333333333333148, 0.3333333333333333703, 0.3333333333333333703, 0.3333333333333333148, 0.3333333333333333703, 0.3333333333333333703, 0.3333333333333333703, 0.3333333333333333703, 0.3333333333333334259, 0.3333333333333332593, 0.3333333333333334259, 0.3333333333333333148, 0.3333333333333333703, 0.3333333333333333148, 0.3333333333333334814, 0.3333333333333332038, 0.3333333333333335369, 0.3333333333333332593, 0.3333333333333333703, 0.3333333333333333703, 0.3333333333333333148, 0.3333333333333333703, 0.3333333333333333148, 0.3333333333333334259, 0.3333333333333334259, 0.3333333333333332593, 0.3333333333333334814, 0.3333333333333333703, 0.3333333333333332593, 0.3333333333333334814, 0.3333333333333334259, 0.3333333333333334259, 0.3333333333333332593, 0.3333333333333333703, 0.3333333333333333703, 0.3333333333333334259, 0.3333333333333333703, 0.3333333333333334259, 0.3333333333333333703, 0.3333333333333333148, 0.3333333333333334814, 0.3333333333333333703, 0.3333333333333334259, 0.3333333333333333703, 0.3333333333333333703, 0.3333333333333333148, 0.3333333333333334259, 0.3333333333333334259, 0.3333333333333333703, 0.3333333333333333148, 0.3333333333333333148, 0.3333333333333334259, 0.3333333333333334814, 0.3333333333333333148, 0.3333333333333334259, 0.3333333333333334814, 0.3333333333333333148, 0.3333333333333334814, 0.3333333333333332038, 0.3333333333333333703, 0.3333333333333333148, 0.3333333333333333703, 0.3333333333333334259, 0.3333333333333332038, 0.3333333333333334259, 0.3333333333333333148, 0.3333333333333332038, 0.3333333333333334259, 0.3333333333333333148, 0.3333333333333334259, 0.3333333333333332593, 0.3333333333333334259, 0.3333333333333333703, 0.3333333333333334259, 0.3333333333333333703, 0.3333333333333334259, 0.3333333333333333703, 0.3333333333333333703, 0.3333333333333334814, 0.3333333333333333703, 0.3333333333333335369, 0.3333333333333332038, 0.3333333333333333703, 0.3333333333333333703, 0.3333333333333333703, 0.3333333333333333148, 0.3333333333333333703, 0.3333333333333333703, 0.3333333333333334259, 0.3333333333333333148, 0.3333333333333334259, 0.3333333333333333148, 0.3333333333333334814, 0.3333333333333332593, 0.3333333333333333703, 0.3333333333333334259, 0.3333333333333333148, 0.3333333333333333703, 0.3333333333333333148, 0.3333333333333334259, 0.3333333333333332593, 0.3333333333333333703, 0.3333333333333334814, 0.3333333333333333703, 0.3333333333333333703, 0.3333333333333333703, 0.3333333333333333703, 0.3333333333333333148, 0.3333333333333333703, 0.3333333333333333703, 0.3333333333333334259, 0.3333333333333333703, 0.3333333333333333703, 0.3333333333333333703, 0.3333333333333333703, 0.3333333333333332038, 0.3333333333333334814, 0.3333333333333333703, 0.3333333333333333703, 0.3333333333333333148, 0.3333333333333333148, 0.3333333333333334259, 0.3333333333333334259, 0.3333333333333332593, 0.3333333333333335369, 0.3333333333333332593, 0.3333333333333334814, 0.3333333333333332593, 0.3333333333333334259, 0.3333333333333332038, 0.3333333333333335369, 0.3333333333333333148, 0.3333333333333333703, 0.3333333333333334259, 0.3333333333333333148, 0.3333333333333333148, 0.3333333333333335369, 0.3333333333333334259, 0.3333333333333333703, 0.3333333333333333148, 0.3333333333333334259, 0.3333333333333333148, 0.3333333333333334259, 0.3333333333333334259, 0.3333333333333333703, 0.3333333333333333703, 0.3333333333333333148, 0.3333333333333333703, 0.3333333333333333703, 0.3333333333333334259, 0.3333333333333333703, 0.3333333333333335369, 0.3333333333333333148, 0.3333333333333333703, 0.3333333333333332593, 0.3333333333333335369, 0.3333333333333333148, 0.3333333333333333148, 0.3333333333333334814, 0.3333333333333332593, 0.3333333333333334814, 0.3333333333333333703, 0.3333333333333334259, 0.3333333333333334814, 0.3333333333333333703, 0.3333333333333333703, 0.3333333333333333148, 0.3333333333333332593, 0.3333333333333334814, 0.3333333333333333148, 0.3333333333333333703, 0.3333333333333333703, 0.3333333333333333703, 0.3333333333333333703, 0.3333333333333334259, 0.3333333333333333703, 0.3333333333333333703, 0.3333333333333333148, 0.3333333333333333703, 0.3333333333333334259, 0.3333333333333332593, 0.3333333333333334814, 0.3333333333333333703, 0.3333333333333333703, 0.3333333333333334259, 0.3333333333333333703, 0.3333333333333334259, 0.3333333333333333703, 0.3333333333333334259, 0.3333333333333332593, 0.3333333333333333703, 0.3333333333333334259, 0.3333333333333333148, 0.3333333333333333148, 0.3333333333333333703, 0.3333333333333334814, 0.3333333333333333148, 0.3333333333333333703, 0.3333333333333334259, 0.3333333333333333703, 0.3333333333333333703, 0.3333333333333333148, 0.3333333333333333703, 0.3333333333333333148, 0.3333333333333335369, 0.3333333333333332593, 0.3333333333333333703, 0.3333333333333333148, 0.3333333333333333703, 0.3333333333333334259, 0.3333333333333334259, 0.3333333333333333703, 0.3333333333333333148, 0.3333333333333334259, 0.3333333333333334259, 0.3333333333333333148, 0.3333333333333334259, 0.3333333333333335369, 0.3333333333333332593, 0.3333333333333333703, 0.3333333333333335369, 0.3333333333333332038, 0.3333333333333334259, 0.3333333333333333148, 0.3333333333333333703, 0.3333333333333333703, 0.3333333333333333703, 0.3333333333333333148, 0.3333333333333333703, 0.3333333333333333703, 0.3333333333333334259, 0.3333333333333334259, 0.3333333333333333148, 0.3333333333333334259, 0.3333333333333333148, 0.3333333333333333703, 0.3333333333333333148, 0.3333333333333334259, 0.3333333333333332038, 0.3333333333333333703, 0.3333333333333334259, 0.3333333333333335369, 0.3333333333333333148, 0.3333333333333333703, 0.3333333333333333703, 0.3333333333333333703, 0.3333333333333333703, 0.3333333333333333703, 0.3333333333333333703, 0.3333333333333334259, 0.3333333333333333703, 0.3333333333333333703, 0.3333333333333333703, 0.3333333333333332038, 0.3333333333333333703, 0.3333333333333335369, 0.3333333333333333148, 0.3333333333333334814, 0.3333333333333333703, 0.3333333333333332593, 0.3333333333333335369, 0.3333333333333333148, 0.3333333333333333703, 0.3333333333333333703, 0.3333333333333333148, 0.3333333333333333703, 0.3333333333333334259, 0.3333333333333334259, 0.3333333333333333703, 0.3333333333333334259, 0.3333333333333333148, 0.3333333333333333703, 0.3333333333333332593, 0.3333333333333333703, 0.3333333333333333703, 0.3333333333333333703, 0.3333333333333333703, 0.3333333333333333703, 0.3333333333333333703, 0.3333333333333333148, 0.3333333333333334259, 0.3333333333333333703, 0.3333333333333334259, 0.3333333333333333148, 0.3333333333333334259, 0.3333333333333333148, 0.3333333333333333703, 0.3333333333333334259, 0.3333333333333333703, 0.3333333333333333148, 0.3333333333333333148, 0.3333333333333334259, 0.3333333333333333703, 0.3333333333333333703, 0.3333333333333334259, 0.3333333333333333703, 0.3333333333333333148, 0.3333333333333334814, 0.3333333333333333703, 0.3333333333333334259, 0.3333333333333333703, 0.3333333333333333703, 0.3333333333333333703),
 ( 1.000000000000000222, 1.000000000000000222, 1.000000000000000222, 1.000000000000000222, 0.9999999999999996669, 0.9999999999999997780, 1.000000000000000444, 1.000000000000000000, 1.000000000000000000, 1.000000000000000000, 0.9999999999999997780, 1.000000000000000000, 1.000000000000000000, 1.000000000000000000, 1.000000000000000000, 0.9999999999999997780, 1.000000000000000222, 0.9999999999999996669, 1.000000000000000000, 0.9999999999999997780, 1.000000000000000222, 1.000000000000000000, 1.000000000000000222, 0.9999999999999996669, 1.000000000000000000, 1.000000000000000222, 0.9999999999999996669, 1.000000000000000444, 1.000000000000000000, 0.9999999999999997780, 1.000000000000000222, 1.000000000000000222, 1.000000000000000222, 1.000000000000000000, 1.000000000000000000, 0.9999999999999997780, 1.000000000000000000, 1.000000000000000000, 1.000000000000000000, 1.000000000000000000, 1.000000000000000222, 1.000000000000000222, 1.000000000000000000, 1.000000000000000000, 1.000000000000000000, 0.9999999999999996669, 1.000000000000000222, 1.000000000000000000, 1.000000000000000000, 0.9999999999999997780, 0.9999999999999997780, 1.000000000000000000, 0.9999999999999996669, 1.000000000000000222, 0.9999999999999997780, 1.000000000000000222, 0.9999999999999997780, 0.9999999999999997780, 1.000000000000000222, 1.000000000000000222, 0.9999999999999997780, 1.000000000000000222, 1.000000000000000000, 1.000000000000000222, 1.000000000000000000, 0.9999999999999997780, 1.000000000000000000, 1.000000000000000000, 1.000000000000000222, 1.000000000000000222, 1.000000000000000000, 0.9999999999999997780, 1.000000000000000000, 1.000000000000000222, 0.9999999999999997780, 1.000000000000000444, 0.9999999999999996669, 1.000000000000000000, 1.000000000000000222, 0.9999999999999997780, 0.9999999999999997780, 0.9999999999999997780, 1.000000000000000000, 0.9999999999999997780, 1.000000000000000000, 0.9999999999999997780, 1.000000000000000222, 1.000000000000000000, 1.000000000000000222, 1.000000000000000000, 0.9999999999999997780, 1.000000000000000000, 1.000000000000000000, 0.9999999999999997780, 1.000000000000000222, 1.000000000000000000, 1.000000000000000000, 1.000000000000000000, 1.000000000000000222, 0.9999999999999996669, 1.000000000000000222, 1.000000000000000000, 1.000000000000000000, 0.9999999999999997780, 1.000000000000000000, 0.9999999999999997780, 1.000000000000000000, 1.000000000000000222, 1.000000000000000000, 0.9999999999999997780, 1.000000000000000222, 1.000000000000000222, 0.9999999999999996669, 1.000000000000000222, 1.000000000000000000, 1.000000000000000444, 0.9999999999999996669, 1.000000000000000000, 1.000000000000000222, 1.000000000000000222, 1.000000000000000222, 1.000000000000000222, 1.000000000000000000, 0.9999999999999997780, 1.000000000000000222, 1.000000000000000000, 1.000000000000000222, 0.9999999999999996669, 1.000000000000000000, 1.000000000000000000, 1.000000000000000222, 1.000000000000000222, 0.9999999999999997780, 1.000000000000000000, 0.9999999999999997780, 1.000000000000000222, 1.000000000000000000, 1.000000000000000222, 1.000000000000000000, 1.000000000000000444, 0.9999999999999996669, 1.000000000000000444, 0.9999999999999996669, 0.9999999999999997780, 0.9999999999999997780, 1.000000000000000222, 1.000000000000000000, 0.9999999999999997780, 1.000000000000000000, 0.9999999999999997780, 0.9999999999999996669, 1.000000000000000222, 1.000000000000000000, 0.9999999999999997780, 1.000000000000000000, 1.000000000000000000, 1.000000000000000222, 1.000000000000000000, 1.000000000000000000, 1.000000000000000444, 0.9999999999999997780, 1.000000000000000222, 1.000000000000000222, 0.9999999999999997780, 1.000000000000000444, 0.9999999999999996669, 1.000000000000000000, 0.9999999999999997780, 1.000000000000000222, 0.9999999999999997780, 1.000000000000000222, 1.000000000000000000, 1.000000000000000222, 0.9999999999999997780, 0.9999999999999997780, 1.000000000000000000, 1.000000000000000000, 0.9999999999999997780, 1.000000000000000222, 0.9999999999999997780, 1.000000000000000000, 1.000000000000000000, 1.000000000000000222, 1.000000000000000000, 0.9999999999999997780, 1.000000000000000222, 1.000000000000000444, 1.000000000000000000, 1.000000000000000000, 1.000000000000000000, 1.000000000000000000, 0.9999999999999997780, 1.000000000000000000, 1.000000000000000222, 1.000000000000000000, 1.000000000000000222, 0.9999999999999996669, 1.000000000000000000, 1.000000000000000000, 0.9999999999999994449, 1.000000000000000444, 1.000000000000000000, 1.000000000000000222, 0.9999999999999997780, 1.000000000000000000, 1.000000000000000222, 1.000000000000000000, 0.9999999999999996669, 1.000000000000000444, 0.9999999999999997780, 1.000000000000000444, 0.9999999999999996669, 1.000000000000000000, 0.9999999999999996669, 1.000000000000000444, 1.000000000000000000, 0.9999999999999997780, 1.000000000000000222, 1.000000000000000000, 0.9999999999999997780, 1.000000000000000444, 1.000000000000000222, 0.9999999999999997780, 1.000000000000000000, 1.000000000000000222, 0.9999999999999997780, 1.000000000000000222, 1.000000000000000222, 1.000000000000000000, 1.000000000000000000, 0.9999999999999996669, 1.000000000000000222, 0.9999999999999997780, 1.000000000000000000, 0.9999999999999997780, 1.000000000000000444, 1.000000000000000000, 1.000000000000000000, 0.9999999999999997780, 1.000000000000000444, 1.000000000000000000, 0.9999999999999997780, 1.000000000000000444, 0.9999999999999996669, 1.000000000000000444, 1.000000000000000000, 1.000000000000000444, 1.000000000000000222, 1.000000000000000222, 0.9999999999999997780, 1.000000000000000000, 0.9999999999999997780, 1.000000000000000444, 0.9999999999999996669, 1.000000000000000000, 1.000000000000000000, 1.000000000000000222, 1.000000000000000000, 1.000000000000000222, 1.000000000000000000, 1.000000000000000000, 0.9999999999999997780, 1.000000000000000000, 1.000000000000000000, 0.9999999999999997780, 1.000000000000000000, 1.000000000000000000, 0.9999999999999997780, 1.000000000000000000, 1.000000000000000222, 1.000000000000000000, 1.000000000000000000, 1.000000000000000000, 1.000000000000000000, 0.9999999999999996669, 1.000000000000000222, 1.000000000000000000, 0.9999999999999997780, 1.000000000000000000, 1.000000000000000222, 1.000000000000000000, 1.000000000000000222, 1.000000000000000222, 1.000000000000000000, 1.000000000000000222, 1.000000000000000000, 1.000000000000000000, 1.000000000000000000, 1.000000000000000222, 0.9999999999999996669, 1.000000000000000222, 0.9999999999999996669, 1.000000000000000222, 1.000000000000000222, 1.000000000000000222, 1.000000000000000222, 0.9999999999999996669, 1.000000000000000444, 1.000000000000000000, 1.000000000000000000, 1.000000000000000222, 1.000000000000000444, 0.9999999999999996669, 1.000000000000000444, 1.000000000000000222, 0.9999999999999996669, 1.000000000000000222, 0.9999999999999997780, 1.000000000000000000, 1.000000000000000000, 0.9999999999999997780, 1.000000000000000000, 0.9999999999999997780, 1.000000000000000000, 1.000000000000000000, 1.000000000000000444, 0.9999999999999997780, 1.000000000000000222, 0.9999999999999997780, 0.9999999999999997780, 1.000000000000000000, 1.000000000000000000, 0.9999999999999996669, 1.000000000000000000, 1.000000000000000222, 1.000000000000000222, 0.9999999999999997780, 1.000000000000000222, 0.9999999999999997780, 0.9999999999999997780, 1.000000000000000000, 1.000000000000000000, 1.000000000000000000, 1.000000000000000222, 1.000000000000000000, 1.000000000000000222, 1.000000000000000000, 0.9999999999999996669, 0.9999999999999997780, 1.000000000000000444, 0.9999999999999996669, 1.000000000000000444, 0.9999999999999997780, 0.9999999999999997780, 1.000000000000000222, 0.9999999999999997780, 1.000000000000000222, 1.000000000000000000, 1.000000000000000000, 0.9999999999999997780, 1.000000000000000222, 1.000000000000000222, 1.000000000000000000, 1.000000000000000222, 1.000000000000000000, 1.000000000000000000, 0.9999999999999997780, 1.000000000000000000, 1.000000000000000000, 0.9999999999999997780, 1.000000000000000000, 0.9999999999999996669, 1.000000000000000222, 0.9999999999999997780, 1.000000000000000222, 0.9999999999999997780, 1.000000000000000000, 0.9999999999999997780, 1.000000000000000222, 0.9999999999999997780, 1.000000000000000000, 1.000000000000000000, 1.000000000000000000, 1.000000000000000000, 0.9999999999999997780, 1.000000000000000222, 1.000000000000000000, 0.9999999999999997780, 1.000000000000000000, 1.000000000000000000, 1.000000000000000222, 1.000000000000000222, 1.000000000000000000, 1.000000000000000222, 1.000000000000000000, 1.000000000000000000, 1.000000000000000000) ) ) 
 REPRESENTATION_ITEM ( '' )  SURFACE ( )  );
#49286=CARTESIAN_POINT ( 'NONE',  ( 2.016421337698256711, -2.119947128278206971, 0.05498460973795551987 ) ) ;
#49287=CARTESIAN_POINT ( 'NONE',  ( 1.616814774554303780, 0.2004563524992293566, 2.006445175307514095 ) ) ;
#49288=CARTESIAN_POINT ( 'NONE',  ( 2.285178059325339461, 0.08539987017499665878, -1.809671756684204214 ) ) ;
#49291=ORIENTED_EDGE ( 'NONE', *, *, #4355, .T. ) ;
#49295=CARTESIAN_POINT ( 'NONE',  ( 0.3740639818887542267, -1.901581053304630675, -0.2314239742453021165 ) ) ;
#49302=CARTESIAN_POINT ( 'NONE',  ( 4.627887939457571598, -1.327398817707679868, -1.706084338546076662 ) ) ;
#49305=CARTESIAN_POINT ( 'NONE',  ( 1.635180430577408028, 1.980530345366804834, 0.7584260845197099421 ) ) ;
#49306=CARTESIAN_POINT ( 'NONE',  ( 6.651389018303578204, -1.468406013062272475, -1.084454090978362428 ) ) ;
#49307=CARTESIAN_POINT ( 'NONE',  ( 3.198462767114045313, -0.5687421903855809369, -1.887558129442780341 ) ) ;
#49309=CARTESIAN_POINT ( 'NONE',  ( 5.793399386127640049, -1.781339898235247077, 0.8404781526112365952 ) ) ;
#49310=CARTESIAN_POINT ( 'NONE',  ( 1.974458820771322953, -0.09541523299517583323, -1.939727210137192737 ) ) ;
#49315=CARTESIAN_POINT ( 'NONE',  ( 2.994169869935947137, -0.6075897704641713970, -2.000389221998987832 ) ) ;
#49319=CARTESIAN_POINT ( 'NONE',  ( 6.586579894266018975, -1.172543786506787145, 1.511232097859278367 ) ) ;
#49321=CARTESIAN_POINT ( 'NONE',  ( 4.617920694193921705, -2.164688156338661962, 0.4286357439418769788 ) ) ;
#49323=CARTESIAN_POINT ( 'NONE',  ( 1.501302152069685647, 1.803625081967351829, -1.271268654958551014 ) ) ;
#49325=CARTESIAN_POINT ( 'NONE',  ( 0.6098336241119780565, -0.6879379538977903330, 1.784437680087819666 ) ) ;
#49328=CARTESIAN_POINT ( 'NONE',  ( 3.789561645344252216, -1.914057400617325211, 0.7896510022299549902 ) ) ;
#49330=CARTESIAN_POINT ( 'NONE',  ( 1.639762333045853726, -1.565812861550972324, -1.490595759849028035 ) ) ;
#49331=CARTESIAN_POINT ( 'NONE',  ( 3.650093349144762023, 0.7902683543556283663, 2.044282924279612779 ) ) ;
#49338=CARTESIAN_POINT ( 'NONE',  ( 0.8092204703840089053, 1.198858234535697065, -1.621184076614573533 ) ) ;
#49340=CARTESIAN_POINT ( 'NONE',  ( 4.416890754593222113, -1.537527071031305814, 1.386575359339572655 ) ) ;
#49341=CARTESIAN_POINT ( 'NONE',  ( 5.976184116172984950, -2.107040639921609504, -0.2072291863110999888 ) ) ;
#49344=CARTESIAN_POINT ( 'NONE',  ( 4.469560827962531846, -0.3407972494764506810, 1.939574385640041809 ) ) ;
#49345=CARTESIAN_POINT ( 'NONE',  ( 6.158190107012026182, -1.625331280325162053, 1.616661686624631944 ) ) ;
#49346=CARTESIAN_POINT ( 'NONE',  ( 3.141029808440584326, -1.609794727316344209, 0.8612202190056221784 ) ) ;
#49352=CARTESIAN_POINT ( 'NONE',  ( 3.709243207436668577, 1.698441389738635676, -1.080623863572414356 ) ) ;
#49353=CARTESIAN_POINT ( 'NONE',  ( 0.2284049197783468987, -2.054502581980635956, -1.030649272238814085 ) ) ;
#49354=CARTESIAN_POINT ( 'NONE',  ( 4.610177715184628155, 1.961415711727178213, -0.04403062578262756377 ) ) ;
#49358=CARTESIAN_POINT ( 'NONE',  ( 0.5739142741672832448, -1.158190483201524179, 1.740425096305434183 ) ) ;
#49359=CARTESIAN_POINT ( 'NONE',  ( 5.840640841166978348, 0.3488620263497018703, 1.734928340252988033 ) ) ;
#49360=CARTESIAN_POINT ( 'NONE',  ( 1.535386672163775668, -1.589036399888818618, -1.509351277865833563 ) ) ;
#49361=CARTESIAN_POINT ( 'NONE',  ( 1.188542350144041304, 1.317171145998846216, 1.137751157100845623 ) ) ;
#49364=CARTESIAN_POINT ( 'NONE',  ( 1.154464490038846547, -1.361941861570209467, 1.058318063114448648 ) ) ;
#49365=CARTESIAN_POINT ( 'NONE',  ( 1.118978350340808614, -0.04878210919301298465, 2.191179638975069732 ) ) ;
#49366=CARTESIAN_POINT ( 'NONE',  ( 3.545738602337618506, -1.670889076328873069, -1.441789439710974063 ) ) ;
#49368=CARTESIAN_POINT ( 'NONE',  ( 1.059715561420447205, 1.773747297294786307, 1.251667063311131312 ) ) ;
#49370=CARTESIAN_POINT ( 'NONE',  ( 2.835287003684193508, -1.733785568389034193, -1.215143187034111838 ) ) ;
#49371=CARTESIAN_POINT ( 'NONE',  ( 6.827182134110198142, 6.033542260787205791, 2.783941933017803905 ) ) ;
#49374=CARTESIAN_POINT ( 'NONE',  ( 2.542860532589632960, -1.904047414228837942, 1.276277502183044810 ) ) ;
#49377=CARTESIAN_POINT ( 'NONE',  ( 4.389451384964074165, 0.0001031656717501855256, -2.221473415372441806 ) ) ;
#49384=CARTESIAN_POINT ( 'NONE',  ( 3.129529892704606464, 0.4926417352555876872, 1.955172657653013957 ) ) ;
#49386=CARTESIAN_POINT ( 'NONE',  ( 0.6200784347700560861, 2.040642744413103671, -0.2990284185609564105 ) ) ;
#49392=CARTESIAN_POINT ( 'NONE',  ( 4.136819237485493517, -1.907179771870757268, 1.079280405373375773 ) ) ;
#49393=CARTESIAN_POINT ( 'NONE',  ( 1.354138928560550292, 0.1455316553338575902, -2.011204400906742240 ) ) ;
#49394=CARTESIAN_POINT ( 'NONE',  ( 1.188719773494644860, 1.394467456127197025, 1.202481090285527632 ) ) ;
#49396=CARTESIAN_POINT ( 'NONE',  ( 4.752862199841776381, -1.465721779273346792, 1.088108411805274622 ) ) ;
#49397=CARTESIAN_POINT ( 'NONE',  ( 6.451795992440088057, -1.844709169062180409, -0.8146298745319994206 ) ) ;
#49399=CARTESIAN_POINT ( 'NONE',  ( 4.944316486460487603, 2.256077187801101669, 0.1715336590100754455 ) ) ;
#49401=CARTESIAN_POINT ( 'NONE',  ( 1.190214010286832602, -0.9452824899213798648, 1.882083610947625107 ) ) ;
#49403=CARTESIAN_POINT ( 'NONE',  ( 4.352052382902608763, -0.7952921280917917279, 1.911720769834825973 ) ) ;
#49411=CARTESIAN_POINT ( 'NONE',  ( 0.2641366190093488164, 0.6592694798918593557, -2.015615888626711705 ) ) ;
#49412=CARTESIAN_POINT ( 'NONE',  ( 1.582608957317205522, 1.147345939325004283, 1.902073548153013327 ) ) ;
#49417=CARTESIAN_POINT ( 'NONE',  ( 3.490630252122446375, 1.913478943654752129, 0.4322817992908413176 ) ) ;
#49423=CARTESIAN_POINT ( 'NONE',  ( 2.408575119285644384, -2.115224228095522907, -0.1514441693673748146 ) ) ;
#49425=CARTESIAN_POINT ( 'NONE',  ( 4.017981030900905637, 1.947309607215493621, -0.2378496960543720617 ) ) ;
#49426=CARTESIAN_POINT ( 'NONE',  ( 2.799875798528407511, -0.6792266858460673795, 2.052276964324008635 ) ) ;
#49427=CARTESIAN_POINT ( 'NONE',  ( 2.876309626556411203, -0.1380247437976732383, -1.836149222064882514 ) ) ;
#49430=CARTESIAN_POINT ( 'NONE',  ( 4.558407276396470920, -1.556374654738747587, -0.7788941851257675797 ) ) ;
#49434=CARTESIAN_POINT ( 'NONE',  ( 1.780366757100563913, -1.156431984057613827, 1.826190802295484472 ) ) ;
#49436=CARTESIAN_POINT ( 'NONE',  ( 4.516953773913958692, 2.015725170860783066, -0.04666989112152990921 ) ) ;
#49438=CARTESIAN_POINT ( 'NONE',  ( 0.9366540776252421097, 2.129889809250965271, 0.3686189752144660714 ) ) ;
#49440=CARTESIAN_POINT ( 'NONE',  ( 2.266812238764161158, -1.800804572728794239, -0.8025143323158872022 ) ) ;
#49442=CARTESIAN_POINT ( 'NONE',  ( 3.808095655114822176, 1.371164123868431117, -1.375570907105559293 ) ) ;
#49450=CARTESIAN_POINT ( 'NONE',  ( 1.044295067165665669, 0.8929887407379886177, -2.018210024696056148 ) ) ;
#49453=CARTESIAN_POINT ( 'NONE',  ( 5.295737746731337126, -1.384591195607473235, -1.390005841682784959 ) ) ;
#49455=CARTESIAN_POINT ( 'NONE',  ( 3.960252432329254724, -1.215859836287141116, 1.733281388416860525 ) ) ;
#49457=CARTESIAN_POINT ( 'NONE',  ( 0.07479286986305369589, 4.095183424177953668, -2.410510762676120411 ) ) ;
#49458=CARTESIAN_POINT ( 'NONE',  ( 4.189278935350455590, -0.7026162016144417155, 1.701997885059022497 ) ) ;
#49462=CARTESIAN_POINT ( 'NONE',  ( 5.467072749063267345, -1.670387955228332277, 1.306269166133757986 ) ) ;
#49467=CARTESIAN_POINT ( 'NONE',  ( 5.483688661837972766, 1.380929853543419128, 1.529855004671219820 ) ) ;
#49468=CARTESIAN_POINT ( 'NONE',  ( 0.6427239283240515633, -0.2220358882154548907, -1.847681390136299839 ) ) ;
#49469=CARTESIAN_POINT ( 'NONE',  ( 4.177188522404684079, 1.205947341878073287, 1.391433828303423326 ) ) ;
#49474=CARTESIAN_POINT ( 'NONE',  ( 2.948105999307056635, 0.7938017206191756436, -2.059354589195587337 ) ) ;
#49475=CARTESIAN_POINT ( 'NONE',  ( 4.411571241670419141, -0.3925092328114428986, 2.227967001921112633 ) ) ;
#49477=CARTESIAN_POINT ( 'NONE',  ( 4.746265919983247983, 0.9249516081627707775, -1.557494045171695651 ) ) ;
#49478=CARTESIAN_POINT ( 'NONE',  ( 5.401554078093819378, -1.867474805896391032, 0.4264384668619321528 ) ) ;
#49479=CARTESIAN_POINT ( 'NONE',  ( 6.727182134110201162, 0.003007720480356954919, 1.910970182385363980 ) ) ;
#49480=CARTESIAN_POINT ( 'NONE',  ( 5.576977133510579776, -0.04717937999037385977, -1.870219006134994588 ) ) ;
#49481=CARTESIAN_POINT ( 'NONE',  ( 5.951566935816642534, 1.409582436273165706, 1.215217600354216554 ) ) ;
#49483=CARTESIAN_POINT ( 'NONE',  ( 6.121911923048983795, -0.9866791243483238327, -1.469064191006617337 ) ) ;
#49484=CARTESIAN_POINT ( 'NONE',  ( -0.03006412033006514162, -0.9462945741195265548, 1.780671068589256834 ) ) ;
#49486=CARTESIAN_POINT ( 'NONE',  ( 2.385502688336095911, 1.925211662925530254, -0.8542917040773172488 ) ) ;
#49490=DIRECTION ( 'NONE',  ( -1.000000000000000000, 0.000000000000000000, 0.000000000000000000 ) ) ;
#49491=CARTESIAN_POINT ( 'NONE',  ( 2.215108757275308982, 1.619595947845490436, -1.206587912388109141 ) ) ;
#49494=CARTESIAN_POINT ( 'NONE',  ( 3.339309863714147397, -1.908069850993234340, 1.015702806061814734 ) ) ;
#49495=CARTESIAN_POINT ( 'NONE',  ( 6.620655732516649294, 2.985444497229528871, 2.280274006979409407 ) ) ;
#49503=CARTESIAN_POINT ( 'NONE',  ( 1.277182604683280598, 2.023070758711601691, -0.8431670391453591762 ) ) ;
#49505=CARTESIAN_POINT ( 'NONE',  ( 1.182923723612337774, -2.207873014618145113, -0.4935663919954368373 ) ) ;
#49512=CARTESIAN_POINT ( 'NONE',  ( 2.881836681058600913, -0.9132262334808398663, 1.515770159524139515 ) ) ;
#49513=CARTESIAN_POINT ( 'NONE',  ( 6.088949818052607377, -0.3178892970779038096, -2.183640257897196513 ) ) ;
#49517=CARTESIAN_POINT ( 'NONE',  ( 4.833611329963474645, 0.6298591494234163646, -1.915606498650752831 ) ) ;
#49519=CARTESIAN_POINT ( 'NONE',  ( 2.571000202304725590, 0.09389976206976291540, -1.868427151830873267 ) ) ;
#49520=CARTESIAN_POINT ( 'NONE',  ( 2.764580022184208730, -0.7881864689132519475, -1.914544693583389634 ) ) ;
#49522=CARTESIAN_POINT ( 'NONE',  ( 2.408343312057196872, -1.907530749141531423, -0.1368029246449145864 ) ) ;
#49527=CARTESIAN_POINT ( 'NONE',  ( 0.8789968191965717992, -1.730013457311157188, -0.8152767527440167861 ) ) ;
#49529=CARTESIAN_POINT ( 'NONE',  ( 2.787496613063783713, -1.831585881375777713, 0.7034878451678548972 ) ) ;
#49533=CARTESIAN_POINT ( 'NONE',  ( 6.573508854753547404, 1.887220770608761589, -0.5698601248695351895 ) ) ;
#49535=CARTESIAN_POINT ( 'NONE',  ( 1.881109812905419343, -1.842300511448742739, -0.8121059663154740482 ) ) ;
#49537=CARTESIAN_POINT ( 'NONE',  ( 2.530995666134610911, -1.758555926239983691, 1.178765877976214016 ) ) ;
#49539=CARTESIAN_POINT ( 'NONE',  ( 3.244645865714153032, -2.039272935636734285, -0.3565889006169955522 ) ) ;
#49541=CARTESIAN_POINT ( 'NONE',  ( 6.105435528804215473, -2.075010666747591159, 0.2545828925317530911 ) ) ;
#49543=CARTESIAN_POINT ( 'NONE',  ( 4.612205747861584548, -0.7811881352849485705, -1.650120847746315622 ) ) ;
#49548=CARTESIAN_POINT ( 'NONE',  ( 5.895608061265788180, 1.667329832391790667, 1.445732890734657161 ) ) ;
#49551=CARTESIAN_POINT ( 'NONE',  ( 4.143145976665215002, 0.09703654569752531711, 1.909951782607082427 ) ) ;
#49556=CARTESIAN_POINT ( 'NONE',  ( 6.614806895146394972, -0.1608752592793839531, 2.155998228907447523 ) ) ;
#49559=CARTESIAN_POINT ( 'NONE',  ( 0.08126746489400815676, -0.8690269180096841239, 1.623235155968821841 ) ) ;
#49563=CARTESIAN_POINT ( 'NONE',  ( 4.393722961847310593, -0.7179090532695198146, 1.727491627791829742 ) ) ;
#49570=CARTESIAN_POINT ( 'NONE',  ( 1.235132629255174974, -0.04286028942791567098, -1.969139623717565790 ) ) ;
#49571=CARTESIAN_POINT ( 'NONE',  ( 1.880482680076976720, -0.5405129038237622696, -1.942536604102131026 ) ) ;
#49575=CARTESIAN_POINT ( 'NONE',  ( 1.974822964535282610, -0.1094934731284517848, -2.188836591978132518 ) ) ;
#49587=CARTESIAN_POINT ( 'NONE',  ( 5.478019777291557979, -1.797689181224306321, -0.3974485807837144224 ) ) ;
#49588=CARTESIAN_POINT ( 'NONE',  ( 1.260403266252381416, 2.010875322206317151, 0.09671919503399273310 ) ) ;
#49589=CARTESIAN_POINT ( 'NONE',  ( 3.163697234774452305, -0.6641558444393131921, -2.200356767709225725 ) ) ;
#49591=CARTESIAN_POINT ( 'NONE',  ( 1.217372920688150506, 0.3700031967454868176, -1.823611282344459239 ) ) ;
#49595=CARTESIAN_POINT ( 'NONE',  ( 4.623256175466385010, 1.666654777633369555, 0.9376445158523971646 ) ) ;
#49598=CARTESIAN_POINT ( 'NONE',  ( 4.247661304151585604, 2.090252499381782147, -0.05307422152340918187 ) ) ;
#49599=CARTESIAN_POINT ( 'NONE',  ( 1.832664747978371533, 0.1804508633567840359, 1.861920966532565336 ) ) ;
#49602=CARTESIAN_POINT ( 'NONE',  ( 6.093280168761200599, -0.6138376400152152357, 1.736067454429328416 ) ) ;
#49605=CARTESIAN_POINT ( 'NONE',  ( 4.951616564603428472, 0.5366251361543332710, -1.639350107105986831 ) ) ;
#49610=CARTESIAN_POINT ( 'NONE',  ( 4.926734997883643885, -1.423062915019442043, 1.639699324398981251 ) ) ;
#49611=CARTESIAN_POINT ( 'NONE',  ( 2.982817717652554101, -0.1347461720548545627, -1.820777111243766733 ) ) ;
#49612=CARTESIAN_POINT ( 'NONE',  ( 1.006607400890747295, 0.5640878064397096825, 1.878940696355746454 ) ) ;
#49613=CARTESIAN_POINT ( 'NONE',  ( 5.419199134695255715, -1.912947687149676668, 0.9079543477103575455 ) ) ;
#49614=CARTESIAN_POINT ( 'NONE',  ( 6.304234482382112148, 1.701787343685069009, -1.536020108501337855 ) ) ;
#49618=CARTESIAN_POINT ( 'NONE',  ( 1.383610671357866639, 0.1525377206293351273, -2.115047022047947589 ) ) ;
#49622=CARTESIAN_POINT ( 'NONE',  ( 6.825048293896172957, -1.981324744236719004, -0.8880960284254543202 ) ) ;
#49623=FACE_OUTER_BOUND ( 'NONE', #42167, .T. ) ;
#49625=CARTESIAN_POINT ( 'NONE',  ( 2.350487294161308860, 1.044453463271700633, -1.960417310804033031 ) ) ;
#49627=CARTESIAN_POINT ( 'NONE',  ( -0.03393210605391345364, -2.232032725161440023, -0.5493522527948471179 ) ) ;
#49629=CARTESIAN_POINT ( 'NONE',  ( 4.346570391463054683, -2.039393746373055372, -0.3077390332135512829 ) ) ;
#49636=CARTESIAN_POINT ( 'NONE',  ( 0.2344723086637650333, 0.3594713984965206000, 2.059332689821891105 ) ) ;
#49637=CARTESIAN_POINT ( 'NONE',  ( 4.810013364240863787, 1.265987717737980134, -1.337210144835267345 ) ) ;
#49641=CARTESIAN_POINT ( 'NONE',  ( 1.307153468561640164, -0.4245502288011630543, 1.671566548543522268 ) ) ;
#49642=CARTESIAN_POINT ( 'NONE',  ( 0.4093891192313535710, -1.913260280790154866, 0.6371585790938688598 ) ) ;
#49643=CARTESIAN_POINT ( 'NONE',  ( 1.864337758866913441, -0.1181282521124735752, -2.295782230965204285 ) ) ;
#49645=CARTESIAN_POINT ( 'NONE',  ( 1.370828697373091432, -1.435183881573602216, 1.748884408748638597 ) ) ;
#49646=CARTESIAN_POINT ( 'NONE',  ( 4.336618311946851101, 2.065336219181472366, 0.4112933666130594301 ) ) ;
#49648=CARTESIAN_POINT ( 'NONE',  ( 2.934531203469164851, 0.2125141484592401875, 1.756833830538252483 ) ) ;
#49656=CARTESIAN_POINT ( 'NONE',  ( 5.168325547630102434, 2.218848025724213802, -0.1096118590232265239 ) ) ;
#49657=CARTESIAN_POINT ( 'NONE',  ( 3.257961296797746265, 0.9855263100190698733, 1.957416934251283935 ) ) ;
#49660=CARTESIAN_POINT ( 'NONE',  ( 5.479186192515411946, -1.917069751554843160, -0.9065152316691318379 ) ) ;
#49663=CARTESIAN_POINT ( 'NONE',  ( 6.889999999999985469, 0.6064005686075202295, 1.774654002403662778 ) ) ;
#49665=CARTESIAN_POINT ( 'NONE',  ( 5.414351406770180120, -2.120778210838507150, 0.002142078463891750485 ) ) ;
#49671=CARTESIAN_POINT ( 'NONE',  ( 5.917501325027624937, -1.028386522942719816, -1.527094029191010893 ) ) ;
#49673=CARTESIAN_POINT ( 'NONE',  ( 1.645671328968565605, 0.5460171089132167532, 1.652615436037402130 ) ) ;
#49675=CARTESIAN_POINT ( 'NONE',  ( 0.3616705494772323726, -0.5269360983083425376, 1.889693748445469224 ) ) ;
#49678=CARTESIAN_POINT ( 'NONE',  ( 5.629794960336353071, -1.368038101806166029, -1.673757646710342550 ) ) ;
#49681=CARTESIAN_POINT ( 'NONE',  ( 4.575171270262055501, 0.003154952768896768234, -2.161883445794945846 ) ) ;
#49685=CARTESIAN_POINT ( 'NONE',  ( 5.712177144062582812, -0.8841330711255364072, -1.762019952394773936 ) ) ;
#49686=CARTESIAN_POINT ( 'NONE',  ( 5.290307710256559659, -1.645723771949607173, 0.5459688634881465497 ) ) ;
#49688=CARTESIAN_POINT ( 'NONE',  ( 2.419692422129790632, -1.264489869534379141, -1.789777738334753732 ) ) ;
#49689=CARTESIAN_POINT ( 'NONE',  ( 2.837322237161111094, 0.2816050128923338058, 2.290267077920715710 ) ) ;
#49690=CARTESIAN_POINT ( 'NONE',  ( 5.272755944101470860, -1.938957023840400362, -0.6983732565980956819 ) ) ;
#49691=CARTESIAN_POINT ( 'NONE',  ( -0.02948999725180690215, 0.001137248348246927814, -1.926291057026579656 ) ) ;
#49695=CARTESIAN_POINT ( 'NONE',  ( 4.430007776716601953, -2.079114408633813582, 0.4165480963118637914 ) ) ;
#49697=CARTESIAN_POINT ( 'NONE',  ( 1.705704151892040832, 1.882474636155605507, 0.7231385473688843879 ) ) ;
#49699=CARTESIAN_POINT ( 'NONE',  ( 4.137865722265689605, -1.519559189622637252, -1.600479987451455699 ) ) ;
#49701=CARTESIAN_POINT ( 'NONE',  ( -0.1288028175206361037, 4.078893953557697571, -2.828657143142800034 ) ) ;
#49705=CARTESIAN_POINT ( 'NONE',  ( 6.825078400183575589, -0.005632053428735600553, 2.144262460745151255 ) ) ;
#49708=CARTESIAN_POINT ( 'NONE',  ( 3.590745217537123057, -0.4003831998886059340, -2.021439917362640504 ) ) ;
#49711=CARTESIAN_POINT ( 'NONE',  ( 3.088540408894335787, -1.201353318763114020, 1.623377594596470352 ) ) ;
#49714=CARTESIAN_POINT ( 'NONE',  ( 3.625900526125751089, -1.226333045360414653, -1.656161981788171200 ) ) ;
#49717=CARTESIAN_POINT ( 'NONE',  ( 3.169157936054858293, 1.820986098869777470, -0.8666075021629695563 ) ) ;
#49718=CARTESIAN_POINT ( 'NONE',  ( -0.2409995289980245703, 0.2355275985303668385, -2.034371242098035548 ) ) ;
#49719=CARTESIAN_POINT ( 'NONE',  ( 1.587592257565925813, -1.832131100469553520, -0.1817911664281982032 ) ) ;
#49720=CARTESIAN_POINT ( 'NONE',  ( 6.217417563691929772, -0.2743312036321900460, 2.189694890431858276 ) ) ;
#49722=CARTESIAN_POINT ( 'NONE',  ( 1.704591423195594535, -0.7763021076895926242, -2.017573427605146907 ) ) ;
#49724=CARTESIAN_POINT ( 'NONE',  ( 1.798064920797682653, -0.9548589541341389042, -1.776165177175797583 ) ) ;
#49725=CARTESIAN_POINT ( 'NONE',  ( 2.109147326763362695, 0.8800818102412102384, -2.123382460422203355 ) ) ;
#49727=CARTESIAN_POINT ( 'NONE',  ( 0.5142528298564854605, 1.293200884458247657, -1.351890787750304135 ) ) ;
#49730=CARTESIAN_POINT ( 'NONE',  ( 4.838727080925394830, 0.3361901323847040213, 1.942436603694275510 ) ) ;
#49731=CARTESIAN_POINT ( 'NONE',  ( 5.155482549980198392, 1.942097955248718533, -0.5424665614216088727 ) ) ;
#49735=CARTESIAN_POINT ( 'NONE',  ( 6.551405291548149101, -1.690254494844857014, -1.256206543278805876 ) ) ;
#49737=CARTESIAN_POINT ( 'NONE',  ( 5.318829906782316819, -1.502041817331278173, 1.425132596443792643 ) ) ;
#49741=CARTESIAN_POINT ( 'NONE',  ( 5.115492516475182327, 1.653579564094692866, 1.159561630411933830 ) ) ;
#49743=CARTESIAN_POINT ( 'NONE',  ( 3.545847025713305012, -1.747029255069532550, -1.507864240153370172 ) ) ;
#49745=CARTESIAN_POINT ( 'NONE',  ( 0.4794367124230074495, -0.1050040150484717050, 2.060039547518006664 ) ) ;
#49752=CARTESIAN_POINT ( 'NONE',  ( 3.983024850003999973, 2.060528110339276520, 0.6844299113566986170 ) ) ;
#49756=CARTESIAN_POINT ( 'NONE',  ( 2.682954136603598272, 1.303717545168959990, 1.300458928786947688 ) ) ;
#49759=CARTESIAN_POINT ( 'NONE',  ( 4.687173145698103838, 1.624054394666199830, 1.471728111018810070 ) ) ;
#49761=CARTESIAN_POINT ( 'NONE',  ( 5.137693465899466183, -1.596169073733178845, -1.603756505840604918 ) ) ;
#49766=CARTESIAN_POINT ( 'NONE',  ( 0.1976571007769452604, -1.769309276362411643, -0.05040135802934773979 ) ) ;
#49767=CARTESIAN_POINT ( 'NONE',  ( 4.055341430421886884, -1.750343679372264205, 0.9943053665309193878 ) ) ;
#49769=CARTESIAN_POINT ( 'NONE',  ( 3.346800460960248191, 0.5101267414385314281, 2.043117269239830947 ) ) ;
#49770=CARTESIAN_POINT ( 'NONE',  ( 0.5795164177304649167, -0.6885740665637375413, 1.787764417203549172 ) ) ;
#49772=CARTESIAN_POINT ( 'NONE',  ( 1.750388463564346075, -1.959780499145358679, -0.1960735186044142708 ) ) ;
#49773=CARTESIAN_POINT ( 'NONE',  ( 0.3736316133628528879, 1.073300769168658908, 1.531925686032776124 ) ) ;
#49774=CARTESIAN_POINT ( 'NONE',  ( 1.416376618315864144, 0.7919773292732554815, 1.795081228748253377 ) ) ;
#49775=CARTESIAN_POINT ( 'NONE',  ( 0.1055216070770526038, 1.418477292093557329, 1.282857148695019989 ) ) ;
#49780=CARTESIAN_POINT ( 'NONE',  ( 6.473518811298506037, 1.789458955665638396, -0.5451884755478533240 ) ) ;
#49782=CARTESIAN_POINT ( 'NONE',  ( 6.157099584139436033, 1.695871835526874483, -1.187180358042688511 ) ) ;
#49785=CARTESIAN_POINT ( 'NONE',  ( 0.8013346216862862192, -1.776568573310655985, 1.062853015585236482 ) ) ;
#49790=CARTESIAN_POINT ( 'NONE',  ( 5.022192282182047940, -2.110239842997441606, 0.2083548542347323507 ) ) ;
#49795=CARTESIAN_POINT ( 'NONE',  ( 5.863715402168388380, -0.4781514528688200483, 1.902565108626976809 ) ) ;
#49797=CARTESIAN_POINT ( 'NONE',  ( 3.093124880496417983, 1.122326866504215426, -1.674630914042275709 ) ) ;
#49798=CARTESIAN_POINT ( 'NONE',  ( 3.362411380332845035, -1.847649188899632255, -0.5059680389012406465 ) ) ;
#49800=CARTESIAN_POINT ( 'NONE',  ( 1.663894474538109236, 1.130263417742288112, 1.877492182091732076 ) ) ;
#49801=CARTESIAN_POINT ( 'NONE',  ( 0.2335667940002632559, 2.006215057630795773, -2.568298294197084886 ) ) ;
#49802=CARTESIAN_POINT ( 'NONE',  ( 3.110468855859845672, 1.357358932127524120, -1.287316363804760888 ) ) ;
#49806=CARTESIAN_POINT ( 'NONE',  ( 5.501600788752927684, -2.065472302299308893, 0.4645820118519652930 ) ) ;
#49809=CARTESIAN_POINT ( 'NONE',  ( 2.208638616728377357, 1.868957087031404285, 0.9372459875717062960 ) ) ;
#49810=CARTESIAN_POINT ( 'NONE',  ( 6.620655732516645742, 7.051964633898824886, 2.771890290588132189 ) ) ;
#49811=CARTESIAN_POINT ( 'NONE',  ( 0.2699429432127123385, -1.132711312255540115, 1.300796998575669772 ) ) ;
#49822=CARTESIAN_POINT ( 'NONE',  ( 1.084272394670304118, -1.149816064065724230, 1.399778539804387822 ) ) ;
#49832=CARTESIAN_POINT ( 'NONE',  ( 3.244433657958167849, -1.833057675465451730, -0.3206290368645177136 ) ) ;
#49833=CARTESIAN_POINT ( 'NONE',  ( -0.1060672704247594272, -0.8202269080865699502, -1.729793120397028927 ) ) ;
#49834=CARTESIAN_POINT ( 'NONE',  ( 6.088885551643496541, -0.2832829338282101261, -1.905325039026314560 ) ) ;
#49840=CARTESIAN_POINT ( 'NONE',  ( 5.049637312653283416, 1.456549282395647849, 1.325737238711437893 ) ) ;
#49841=CARTESIAN_POINT ( 'NONE',  ( 1.401209248766785542, -0.3145075555085960484, -2.096923750572597722 ) ) ;
#49845=CARTESIAN_POINT ( 'NONE',  ( 5.912113082354764515, 1.474260358680115068, -1.621598248542432064 ) ) ;
#49847=CARTESIAN_POINT ( 'NONE',  ( 4.155238220467009747, -1.601147421941846227, -1.070839854175157813 ) ) ;
#49849=CARTESIAN_POINT ( 'NONE',  ( 0.08272424614634911466, -0.1293432359340887239, -1.795996506534849546 ) ) ;
#49850=CARTESIAN_POINT ( 'NONE',  ( 1.383733252933561086, 2.037972573443189717, -0.8472329510355591786 ) ) ;
#49854=SURFACE_SIDE_STYLE ('',( #159609 ) ) ;
#49856=CARTESIAN_POINT ( 'NONE',  ( 6.174653332693735841, 1.325436276047034179, -1.456821488112548080 ) ) ;
#49857=CARTESIAN_POINT ( 'NONE',  ( 1.979929434068830929, -1.904991468646766606, -0.3768183752349169580 ) ) ;
#49858=CARTESIAN_POINT ( 'NONE',  ( 6.362725135800558540, -0.7832434641057796076, 2.160938040253687742 ) ) ;
#49860=CARTESIAN_POINT ( 'NONE',  ( 4.258551055683129860, -0.5805891344777401875, -1.768159363456432764 ) ) ;
#49866=CARTESIAN_POINT ( 'NONE',  ( 0.6619992422990974568, 1.085049530943157148, 1.904046507712559455 ) ) ;
#49871=CARTESIAN_POINT ( 'NONE',  ( 2.068725586703868746, -1.668841220716179130, -0.7407507213199536755 ) ) ;
#49875=CARTESIAN_POINT ( 'NONE',  ( 3.955468362790943715, -1.619900715620861131, -0.6195580815930351593 ) ) ;
#49877=CARTESIAN_POINT ( 'NONE',  ( 6.609000000000012420, 2.052634316153336691, 2.306727925381938604 ) ) ;
#49879=CARTESIAN_POINT ( 'NONE',  ( -0.01707793031917748464, -0.1336475082493841504, -1.895772241332476682 ) ) ;
#49880=CARTESIAN_POINT ( 'NONE',  ( 4.522284091987982535, 0.9210895807079204634, 1.732038000912524467 ) ) ;
#49883=CARTESIAN_POINT ( 'NONE',  ( 4.881546266219149999, 0.2071824046101199135, -2.110321684233848583 ) ) ;
#49884=CIRCLE ( 'NONE', #184681, 0.05000000000000056483 ) ;
#49887=CARTESIAN_POINT ( 'NONE',  ( 3.116144222688784549, 2.060704436481402890, -0.1983081510379124945 ) ) ;
#49892=CARTESIAN_POINT ( 'NONE',  ( 2.655266180633470086, 1.232652804806773528, 1.940110688254999438 ) ) ;
#49902=CARTESIAN_POINT ( 'NONE',  ( 3.990413957267644474, -1.096855775730350757, 1.566394476586838724 ) ) ;
#49904=CARTESIAN_POINT ( 'NONE',  ( 4.823137214860290456, -0.08221903636504260260, 1.722948775904736385 ) ) ;
#49905=CARTESIAN_POINT ( 'NONE',  ( 3.380092458137720968, -2.014432998692190058, -0.09411721906785883163 ) ) ;
#49906=CARTESIAN_POINT ( 'NONE',  ( 5.221416903470996296, 2.264307454851313572, 0.3953409806420198347 ) ) ;
#49908=CARTESIAN_POINT ( 'NONE',  ( 0.4170028235400899397, 1.518763190251697370, -1.601383572969114599 ) ) ;
#49910=CARTESIAN_POINT ( 'NONE',  ( 6.432837487460982828, 0.1759369732093341021, 1.760927613267867953 ) ) ;
#49912=CARTESIAN_POINT ( 'NONE',  ( 2.396762456488350956, 1.839990291603439632, -1.366890742103431755 ) ) ;
#49913=CARTESIAN_POINT ( 'NONE',  ( 0.2689661900789627746, 0.9977586965290600185, 1.425695987021274647 ) ) ;
#49915=CARTESIAN_POINT ( 'NONE',  ( 6.492125937493531396, -0.5805207454109837517, -2.113085764653479082 ) ) ;
#49919=CARTESIAN_POINT ( 'NONE',  ( 0.4323793472312524311, 1.250547990301904111, 1.774695861279996567 ) ) ;
#49920=CARTESIAN_POINT ( 'NONE',  ( 1.903530124611974017, -1.954778955200174861, 0.4946342604733033887 ) ) ;
#49922=CARTESIAN_POINT ( 'NONE',  ( 5.373632986646971865, 1.856140760046654403, -0.5156676092323666527 ) ) ;
#49924=CARTESIAN_POINT ( 'NONE',  ( 2.742673093864269163, 1.230450920196803022, -1.849320754654346866 ) ) ;
#49930=CARTESIAN_POINT ( 'NONE',  ( 4.388070221843799246, -0.3869516340575751001, -1.696700118790330558 ) ) ;
#49931=CARTESIAN_POINT ( 'NONE',  ( 3.648837080137564470, -0.3802854374791163616, -1.924481129451253603 ) ) ;
#49935=CARTESIAN_POINT ( 'NONE',  ( 4.587383588223284292, 2.023586100481920447, -1.011833202457941283 ) ) ;
#49936=CARTESIAN_POINT ( 'NONE',  ( 1.398963405728241183, 0.4003750237208941742, 2.023287731994154015 ) ) ;
#49939=CARTESIAN_POINT ( 'NONE',  ( 0.7083710243460902278, -2.251296572208848712, 0.2248925466769024495 ) ) ;
#49942=CARTESIAN_POINT ( 'NONE',  ( 2.758895227446885645, -1.625506345271657604, -0.9254698705311248386 ) ) ;
#49943=CARTESIAN_POINT ( 'NONE',  ( 1.406441466896314996, -0.9629721463089849776, -1.441941353469172293 ) ) ;
#49944=CARTESIAN_POINT ( 'NONE',  ( 5.284801750429747536, 1.933107837519608685, -1.032524723389722787 ) ) ;
#49945=CARTESIAN_POINT ( 'NONE',  ( 6.247156018452869830, -1.954037266989640420, 1.227234044731172036 ) ) ;
#49946=CARTESIAN_POINT ( 'NONE',  ( 1.692332502075646783, -2.050886281836623581, -0.2028688129896583647 ) ) ;
#49947=CARTESIAN_POINT ( 'NONE',  ( 3.011592816664434569, -0.9578117005206161494, -1.689242170645321339 ) ) ;
#49950=CARTESIAN_POINT ( 'NONE',  ( 5.342975940791072631, -1.604858128155508101, 0.9606422304059699657 ) ) ;
#49951=CARTESIAN_POINT ( 'NONE',  ( 1.531250000000001110, -0.7852924748300684765, -1.895863743164053927 ) ) ;
#49953=CARTESIAN_POINT ( 'NONE',  ( 6.450546045330813882, 1.388275245401158431, 1.462219883709668045 ) ) ;
#49956=CARTESIAN_POINT ( 'NONE',  ( 4.272111401563948085, 1.799923229630392640, -0.9091438646662284295 ) ) ;
#49960=CARTESIAN_POINT ( 'NONE',  ( 2.437895498511342574, 0.8609710149188254391, -1.609920059450341778 ) ) ;
#49968=CARTESIAN_POINT ( 'NONE',  ( 0.03542360567958083295, -0.09470281839311225913, 2.017672626582614814 ) ) ;
#49969=CARTESIAN_POINT ( 'NONE',  ( 6.340512354315207766, 1.281540423541355223, -1.814176132805396691 ) ) ;
#49973=CARTESIAN_POINT ( 'NONE',  ( 6.157116169989634180, -1.766321488544853935, -1.061543263526150138 ) ) ;
#49974=CARTESIAN_POINT ( 'NONE',  ( 5.449842333688053486, -1.824117940560719298, -0.8596331684956671770 ) ) ;
#49984=CARTESIAN_POINT ( 'NONE',  ( 4.938827285099913311, 1.158512636183751665, 1.649828125244500843 ) ) ;
#49985=CARTESIAN_POINT ( 'NONE',  ( 4.365079047384805122, 1.785254547683400306, -0.4496667978745386152 ) ) ;
#49986=CARTESIAN_POINT ( 'NONE',  ( -0.02319159430949970999, 2.891346550825595774, -2.299931007135449512 ) ) ;
#49987=CARTESIAN_POINT ( 'NONE',  ( 2.965757426574578304, 0.3381026970978153745, -2.282680038778000853 ) ) ;
#49989=CARTESIAN_POINT ( 'NONE',  ( 4.938837616837212785, 0.3641351946921667082, 2.130543054529559832 ) ) ;
#49991=CARTESIAN_POINT ( 'NONE',  ( 0.6791179963998601465, 1.305170301278056444, 1.438240348306470739 ) ) ;
#49996=CARTESIAN_POINT ( 'NONE',  ( 3.449935675575486638, 1.870836310073907827, 0.001118452434160921221 ) ) ;
#49997=CARTESIAN_POINT ( 'NONE',  ( 1.195406425308798148, 1.765864799226088744, -0.7346160280939582066 ) ) ;
#50000=CARTESIAN_POINT ( 'NONE',  ( 2.684424123961434816, -1.133677649706768431, 1.893296980138805097 ) ) ;
#50001=CARTESIAN_POINT ( 'NONE',  ( 0.07755575628184004089, 7.629137130509076492, -2.788902932953695846 ) ) ;
#50006=CARTESIAN_POINT ( 'NONE',  ( 0.7726555735236986244, -1.854786837065467653, -0.6681536526091761408 ) ) ;
#50007=CARTESIAN_POINT ( 'NONE',  ( 0.3589920806752691096, 0.8874099113769757796, 2.130322803234908857 ) ) ;
#50008=CARTESIAN_POINT ( 'NONE',  ( 1.873419974815058842, -0.2433403713097622156, 1.946663811685337420 ) ) ;
#50009=CARTESIAN_POINT ( 'NONE',  ( 5.418824339757763120, -1.497735668165665723, 1.418348116948890736 ) ) ;
#50017=CARTESIAN_POINT ( 'NONE',  ( 1.024573611315128252, 1.068414711107899429, 1.889872971959544401 ) ) ;
#50019=CARTESIAN_POINT ( 'NONE',  ( 6.269096963164666469, 1.759884223096353173, -0.5412972069449849544 ) ) ;
#50022=CARTESIAN_POINT ( 'NONE',  ( 1.510794437334112672, 1.647127454408814362, 0.8865631655482277829 ) ) ;
#50023=CARTESIAN_POINT ( 'NONE',  ( 5.852838158510675015, -1.708014377640250991, 1.324763891615586386 ) ) ;
#50026=CARTESIAN_POINT ( 'NONE',  ( -0.02264175331115856477, -0.002534049983802035520, -2.089079740194145440 ) ) ;
#50029=CARTESIAN_POINT ( 'NONE',  ( 1.576665144504853400, -1.351504567317940664, 1.353124384123285839 ) ) ;
#50030=CARTESIAN_POINT ( 'NONE',  ( 2.940057854958120220, 1.756256042272446694, 0.2183286820098342407 ) ) ;
#50031=CARTESIAN_POINT ( 'NONE',  ( 1.066890508724306130, -1.507026839618429426, 1.177014404800474479 ) ) ;
#50033=CARTESIAN_POINT ( 'NONE',  ( 6.028903631427566800, -1.615475894945080926, 1.029159534634891626 ) ) ;
#50035=CARTESIAN_POINT ( 'NONE',  ( 6.180130249528606790, -1.092802789126966934, -1.638350696670291651 ) ) ;
#50037=CARTESIAN_POINT ( 'NONE',  ( 1.529697670087664108, -0.2543295609688834835, 2.105205558366497698 ) ) ;
#50040=CARTESIAN_POINT ( 'NONE',  ( 4.451927283622527654, 1.870250842541102410, -0.04591718433973044494 ) ) ;
#50041=CARTESIAN_POINT ( 'NONE',  ( 0.4514209555319322331, 0.5758240286459560542, -1.732582669633643047 ) ) ;
#50043=CARTESIAN_POINT ( 'NONE',  ( 3.088704478669739295, -2.174299887604825177, -0.3769171259565203269 ) ) ;
#50046=CARTESIAN_POINT ( 'NONE',  ( 1.539586554034046539, 1.906627302964102988, -0.7874849336161419133 ) ) ;
#50055=CARTESIAN_POINT ( 'NONE',  ( 4.756339170418532269, -2.069830778647030023, -0.05414847147890837487 ) ) ;
#50058=CARTESIAN_POINT ( 'NONE',  ( 1.687033600898584895, -0.3153356727807927751, -2.138329785107299319 ) ) ;
#50060=CARTESIAN_POINT ( 'NONE',  ( 2.174478703267632707, 0.8655064541149575241, 1.824978016274068082 ) ) ;
#50066=CARTESIAN_POINT ( 'NONE',  ( -0.2409995289980038091, -0.004801160710915519658, -2.000252362011435636 ) ) ;
#50067=CARTESIAN_POINT ( 'NONE',  ( 6.639320575229257670, 2.957073754255258535, 2.555924021811271096 ) ) ;
#50068=CARTESIAN_POINT ( 'NONE',  ( 5.073855206572205567, -1.217758175834412260, 1.821886007100224969 ) ) ;
#50072=CARTESIAN_POINT ( 'NONE',  ( 3.586107075002854305, 1.066394011600999780, 1.587261316105821551 ) ) ;
#50076=CARTESIAN_POINT ( 'NONE',  ( 2.038685622454153190, -1.556895902704044765, 1.281378572682637218 ) ) ;
#50078=CARTESIAN_POINT ( 'NONE',  ( 0.8555022099123296142, 0.4403784002881392379, -2.249529875239093979 ) ) ;
#50080=CARTESIAN_POINT ( 'NONE',  ( 3.715580044805122384, -1.699234090967314259, 0.2946211727567394911 ) ) ;
#50084=CARTESIAN_POINT ( 'NONE',  ( 0.7132427667453158371, -1.655377960257615966, -1.052639099659122390 ) ) ;
#50085=CARTESIAN_POINT ( 'NONE',  ( 0.2505829665140328899, -1.505242420826727656, 1.110479572284161831 ) ) ;
#50086=CARTESIAN_POINT ( 'NONE',  ( 0.1751657365761885576, 5.722053558346082092, -2.638081460773045617 ) ) ;
#50090=CARTESIAN_POINT ( 'NONE',  ( 4.951724851890283219, -1.284874556838147219, -1.277195305962516292 ) ) ;
#50095=CARTESIAN_POINT ( 'NONE',  ( 5.742768220754598474, 1.747532268389985433, 0.4768009125176131957 ) ) ;
#50099=CARTESIAN_POINT ( 'NONE',  ( 6.162542460989155479, -0.6707643300355231597, -1.736165932305182125 ) ) ;
#50101=CARTESIAN_POINT ( 'NONE',  ( 4.183139505431884508, 1.540756628010631735, 1.138051695910688998 ) ) ;
#50107=CARTESIAN_POINT ( 'NONE',  ( 5.753141757616087482, 0.1533694674813860792, -2.111807561841658742 ) ) ;
#50108=CARTESIAN_POINT ( 'NONE',  ( 0.9366540776252419986, 2.129889809250965271, 0.3686189752144660159 ) ) ;
#50112=CARTESIAN_POINT ( 'NONE',  ( 0.6744773098602949712, -1.717252091951677384, -0.6198786263262797691 ) ) ;
#50114=CARTESIAN_POINT ( 'NONE',  ( 3.944226942909400346, 1.816763600636053688, 0.1792749827478901103 ) ) ;
#50118=CARTESIAN_POINT ( 'NONE',  ( 2.734760313433327372, -1.883857982319175450, -0.5745676990022812181 ) ) ;
#50119=CARTESIAN_POINT ( 'NONE',  ( 4.687022505062548916, 1.441580155910677785, 1.301524815871560214 ) ) ;
#50122=CARTESIAN_POINT ( 'NONE',  ( 4.904590598983499916, -2.104870323260544129, -0.2570220051709286579 ) ) ;
#50124=CARTESIAN_POINT ( 'NONE',  ( 2.684119430630255820, 1.024705199231435993, 1.614373862881289590 ) ) ;
#50131=CARTESIAN_POINT ( 'NONE',  ( 5.074738461036464088, -1.720261882950037124, -0.6118011564382742629 ) ) ;
#50135=CARTESIAN_POINT ( 'NONE',  ( 5.858239598252557911, 0.7595784280203803362, 1.709674162104061645 ) ) ;
#50144=CARTESIAN_POINT ( 'NONE',  ( 6.508646264616319677, 0.6728166153291449403, 2.064291235436790384 ) ) ;
#50145=CARTESIAN_POINT ( 'NONE',  ( 2.759486767256282391, 2.009531813720342175, -0.6668115938158604150 ) ) ;
#50148=CARTESIAN_POINT ( 'NONE',  ( 6.139524545372063713, 1.915082402702467101, -0.7868883245659707981 ) ) ;
#50153=CARTESIAN_POINT ( 'NONE',  ( 2.994356955963250133, -0.6658908676899841783, -2.193406925754942893 ) ) ;
#50155=CARTESIAN_POINT ( 'NONE',  ( 0.2333690889706925564, 2.018283468528142777, -2.468684669820114586 ) ) ;
#50157=CARTESIAN_POINT ( 'NONE',  ( 2.285291272251275707, 0.09004542135446562401, -1.910373438827176251 ) ) ;
#50161=CARTESIAN_POINT ( 'NONE',  ( 1.054940647564650336, 0.3968280277809080880, 1.973547778087578308 ) ) ;
#50162=CARTESIAN_POINT ( 'NONE',  ( 0.7429250141685154185, -0.2344385519315282107, -1.947609053799495005 ) ) ;
#50166=CARTESIAN_POINT ( 'NONE',  ( 4.013684974745008738, -1.074646439955847965, -1.793145193944564175 ) ) ;
#50167=CARTESIAN_POINT ( 'NONE',  ( 2.447821898584545242, 1.769419436591600725, 0.04612135499031978086 ) ) ;
#50171=CARTESIAN_POINT ( 'NONE',  ( 5.595737365542901465, -2.292435212557204949, -0.004933362929348399616 ) ) ;
#50172=CARTESIAN_POINT ( 'NONE',  ( 2.800428594868603405, 1.470281860783069439, 0.9307988129052218174 ) ) ;
#50175=CARTESIAN_POINT ( 'NONE',  ( 3.303724397909554078, -1.530444925530007216, 0.8147494179842218465 ) ) ;
#50176=CARTESIAN_POINT ( 'NONE',  ( 4.000555764329702946, 2.160365084594504381, 0.2165898760093481201 ) ) ;
#50178=CARTESIAN_POINT ( 'NONE',  ( 5.190638768449240992, 1.523797776992100284, -1.320824044268428255 ) ) ;
#50179=CARTESIAN_POINT ( 'NONE',  ( 6.687508294236179651, -1.450827213159664675, 1.451031289061379681 ) ) ;
#50181=CARTESIAN_POINT ( 'NONE',  ( 2.520427876150105995, 1.259661825572227167, -1.457548065151576200 ) ) ;
#50183=CARTESIAN_POINT ( 'NONE',  ( 5.695613681701293451, 2.052597959444299125, -0.8498680618601384129 ) ) ;
#50185=CARTESIAN_POINT ( 'NONE',  ( 6.983263157960370116, 6.036630394911544073, 2.541087343977180613 ) ) ;
#50189=CARTESIAN_POINT ( 'NONE',  ( 1.928696271399105600, -1.050554081124959183, -1.957186058178138399 ) ) ;
#50197=CARTESIAN_POINT ( 'NONE',  ( 4.088373676034792403, 1.106037789618707912, -1.740905279395239758 ) ) ;
#50202=CARTESIAN_POINT ( 'NONE',  ( 6.081297793977560318, 1.728434112010367674, -0.7156336962577531935 ) ) ;
#50203=CARTESIAN_POINT ( 'NONE',  ( 4.394945383863869459, -0.7467295182301251222, -1.565304230221546300 ) ) ;
#50204=CARTESIAN_POINT ( 'NONE',  ( 4.915436192723389830, -0.9368120511010556983, -1.466610992562596527 ) ) ;
#50206=CARTESIAN_POINT ( 'NONE',  ( 1.769451523944377769, 2.192225184321832554, -0.6701302238534474487 ) ) ;
#50208=CARTESIAN_POINT ( 'NONE',  ( 5.970280646434825478, -1.985518398909513982, -0.6551979098984096472 ) ) ;
#50209=CARTESIAN_POINT ( 'NONE',  ( 0.6207436649305307919, -1.749090901066195691, 0.5750481222980761142 ) ) ;
#50212=CARTESIAN_POINT ( 'NONE',  ( 1.670546294658280084, 1.392546765991018454, 1.458555661489918442 ) ) ;
#50213=CARTESIAN_POINT ( 'NONE',  ( 0.6038064816080711550, -2.180521553291506986, 0.2185767975278959385 ) ) ;
#50218=CARTESIAN_POINT ( 'NONE',  ( 3.739029402251158984, 2.014021593674422572, 0.6637135986873595739 ) ) ;
#50220=CARTESIAN_POINT ( 'NONE',  ( 5.883392091387671385, 1.685093539698417242, -0.7030590484573000509 ) ) ;
#50226=CARTESIAN_POINT ( 'NONE',  ( 3.322525440707891242, -0.8223705904544276191, -1.844992516297422780 ) ) ;
#50227=CARTESIAN_POINT ( 'NONE',  ( 0.3937647135470741522, 1.560644430845319119, 1.414193795423605904 ) ) ;
#50229=CARTESIAN_POINT ( 'NONE',  ( 4.838624485402447384, -1.804320056961044694, -0.4549315660777561443 ) ) ;
#50234=CARTESIAN_POINT ( 'NONE',  ( 0.1632417891470130944, -1.931755829615459996, -0.9703963252955111196 ) ) ;
#50239=CARTESIAN_POINT ( 'NONE',  ( 1.721629994271107744, -1.484111423267266527, -0.8961763045370867431 ) ) ;
#50240=CARTESIAN_POINT ( 'NONE',  ( 0.7259949354544228406, 0.1236639744153274628, 1.736007293746767655 ) ) ;
#50241=CARTESIAN_POINT ( 'NONE',  ( 6.498638929175646339, -0.6082784835782985011, -2.226023345802934372 ) ) ;
#50244=CARTESIAN_POINT ( 'NONE',  ( 2.759116376063870391, -1.791426917979478395, -1.018529149919424892 ) ) ;
#50246=CARTESIAN_POINT ( 'NONE',  ( 1.054064285791616262, 1.779355684154381834, -0.9478921834336280217 ) ) ;
#50249=CARTESIAN_POINT ( 'NONE',  ( 0.3035114269093022732, -0.5280327476409033549, 1.899365994968700955 ) ) ;
#50252=CARTESIAN_POINT ( 'NONE',  ( 4.781465250580236415, 0.1816826923375300662, -1.903719681147630016 ) ) ;
#50254=CARTESIAN_POINT ( 'NONE',  ( 6.691986956589398794, -0.9478133180038283978, 1.990996264204819122 ) ) ;
#50259=CARTESIAN_POINT ( 'NONE',  ( 6.533838320793388554, -2.056994387304663885, 0.5145578593022880343 ) ) ;
#50261=CARTESIAN_POINT ( 'NONE',  ( 3.030630200643165573, 1.283085264563757599, -1.917795831646688320 ) ) ;
#50262=CARTESIAN_POINT ( 'NONE',  ( 4.439869198996494681, 1.279870211898268550, 1.486999339763886097 ) ) ;
#50264=CARTESIAN_POINT ( 'NONE',  ( 1.867943658074404434, -1.947550630801861526, 0.2349073745619503772 ) ) ;
#50268=CARTESIAN_POINT ( 'NONE',  ( 0.3216855292715998793, -1.502087118449943137, -1.492529068308690920 ) ) ;
#50270=CARTESIAN_POINT ( 'NONE',  ( 0.3922017905241963476, 1.532332584989907653, -1.020347975915262939 ) ) ;
#50271=CARTESIAN_POINT ( 'NONE',  ( 4.153319900303814372, 1.837149938469440302, -1.156618460589062813 ) ) ;
#50273=CARTESIAN_POINT ( 'NONE',  ( 1.318772358905948794, -0.7683209907942339933, -1.976687055281033611 ) ) ;
#50279=CARTESIAN_POINT ( 'NONE',  ( 2.425137330123087853, -0.003247232972201920167, 2.060967562036238210 ) ) ;
#50286=CARTESIAN_POINT ( 'NONE',  ( 4.494721087910215296, -1.855708629272670551, -0.4612273479895278583 ) ) ;
#50288=CARTESIAN_POINT ( 'NONE',  ( 1.405971756114566595, -0.5497231165422427068, 2.194469222715933476 ) ) ;
#50290=CARTESIAN_POINT ( 'NONE',  ( 0.8260602286952464235, -0.8153974433127196830, -1.617802387155008681 ) ) ;
#50291=CARTESIAN_POINT ( 'NONE',  ( 1.534256617913127174, 0.6047330867673149646, 1.817800723622571057 ) ) ;
#50292=CARTESIAN_POINT ( 'NONE',  ( 3.139188941651628539, -0.1496422021231707811, -2.064996656166856237 ) ) ;
#50295=CARTESIAN_POINT ( 'NONE',  ( 0.9890677962714401472, 1.739647146885098694, -0.9275093368027197416 ) ) ;
#50296=CARTESIAN_POINT ( 'NONE',  ( 5.039640240021522999, -1.363685002003648616, -1.361047059521299785 ) ) ;
#50297=CARTESIAN_POINT ( 'NONE',  ( 0.6280632297508845774, -2.189494644770412890, 0.7293192972532935858 ) ) ;
#50300=CARTESIAN_POINT ( 'NONE',  ( 5.441865409415975741, 1.382631645094612338, 1.530856317113358678 ) ) ;
#50304=CARTESIAN_POINT ( 'NONE',  ( 5.262764605058766421, -1.527415466006694533, 1.450107492850923441 ) ) ;
#50307=CARTESIAN_POINT ( 'NONE',  ( 5.343121995983710626, -1.856993961526328007, 1.106124453333141577 ) ) ;
#50308=CARTESIAN_POINT ( 'NONE',  ( 5.619787797283516184, -0.4887302510508689801, 1.959527308111078669 ) ) ;
#50315=CARTESIAN_POINT ( 'NONE',  ( 3.169157936054858293, 1.820986098869777470, -0.8666075021629695563 ) ) ;
#50319=CARTESIAN_POINT ( 'NONE',  ( 4.961884481312108797, 2.138711985806662330, -0.3135959325617638238 ) ) ;
#50322=CARTESIAN_POINT ( 'NONE',  ( 6.720655732516641834, 7.051887106169240305, 2.771889904330120391 ) ) ;
#50324=CARTESIAN_POINT ( 'NONE',  ( 6.099232498865051255, -0.2440123228986730841, 2.001514574626765075 ) ) ;
#50326=CARTESIAN_POINT ( 'NONE',  ( 0.5919146312290176626, -1.711225830157696137, -0.2159481953097255325 ) ) ;
#50331=CARTESIAN_POINT ( 'NONE',  ( 6.468025801952650866, 0.9617254617904011926, 1.604207369834034669 ) ) ;
#50332=CARTESIAN_POINT ( 'NONE',  ( 0.6979027206182022436, 1.353502529517286446, 1.490303647139071153 ) ) ;
#50337=CARTESIAN_POINT ( 'NONE',  ( 2.174623584685225541, 0.9092215167782154994, 1.915816808323366871 ) ) ;
#50338=CARTESIAN_POINT ( 'NONE',  ( 2.196888872880573551, 1.802427395782604247, 0.9040921628407010413 ) ) ;
#50339=CARTESIAN_POINT ( 'NONE',  ( 2.021461901335448896, -0.3940331753463456321, 1.768040416340182608 ) ) ;
#50341=CARTESIAN_POINT ( 'NONE',  ( 6.438358464623771482, 2.137424745569570295, 0.3223339197731683869 ) ) ;
#50345=CARTESIAN_POINT ( 'NONE',  ( 0.3037315811481311467, -1.027229472348114347, -1.616837036282785078 ) ) ;
#50353=CARTESIAN_POINT ( 'NONE',  ( 4.663041391408608405, -1.929494027986548232, -0.9748474430888447451 ) ) ;
#50356=CARTESIAN_POINT ( 'NONE',  ( 1.547299434221154124, 0.2130619955753136618, 2.109896976817266179 ) ) ;
#50357=CARTESIAN_POINT ( 'NONE',  ( 6.739283625173963621, -1.628968703954777553, 0.8242606506234579911 ) ) ;
#50359=CARTESIAN_POINT ( 'NONE',  ( 3.040257615459122320, 1.956033444698499268, 0.2450028794991568337 ) ) ;
#50362=CARTESIAN_POINT ( 'NONE',  ( 5.828554260932977904, -1.250890888562717684, 1.521285551415082482 ) ) ;
#50363=CARTESIAN_POINT ( 'NONE',  ( 1.798672962244704410, 1.614485480382701565, 1.078883064099228628 ) ) ;
#50371=CARTESIAN_POINT ( 'NONE',  ( 6.006500814222540008, -1.903516144586704151, -0.1827706444143817055 ) ) ;
#50373=CARTESIAN_POINT ( 'NONE',  ( 4.705825944637973990, -0.5905853116198942487, 2.126329296355852883 ) ) ;
#50374=CARTESIAN_POINT ( 'NONE',  ( 2.011028756337205348, 1.635159560789069655, -1.482119803565529859 ) ) ;
#50376=CARTESIAN_POINT ( 'NONE',  ( 0.8735180803765253410, 0.3724630581584260081, -1.875478908130092215 ) ) ;
#50379=CARTESIAN_POINT ( 'NONE',  ( 3.648938843998358106, -0.4010542052625790110, -2.030977206718207473 ) ) ;
#50383=CARTESIAN_POINT ( 'NONE',  ( 1.516726440323381331, 1.451591637995581996, -1.601975981646540426 ) ) ;
#50384=CARTESIAN_POINT ( 'NONE',  ( 3.597391730528697540, -0.6346259394694170330, 2.097678010650514402 ) ) ;
#50391=CARTESIAN_POINT ( 'NONE',  ( 6.029869095562110815, -1.459853974539515153, 0.9356793305193217281 ) ) ;
#50392=STYLED_ITEM ( 'NONE', ( #26911 ), #89439 ) ;
#50394=CARTESIAN_POINT ( 'NONE',  ( 3.924723049676182018, -1.394041313093749457, 1.530695986988837021 ) ) ;
#50395=CARTESIAN_POINT ( 'NONE',  ( 5.817987567751313982, 1.043164272916985214, -1.842315021624504778 ) ) ;
#50398=CARTESIAN_POINT ( 'NONE',  ( 3.362113288959746704, -1.967404159762261795, 0.09189030742163574461 ) ) ;
#50399=CARTESIAN_POINT ( 'NONE',  ( 6.281209671116547710, 1.576043917979405684, 1.664718807710400705 ) ) ;
#50400=CARTESIAN_POINT ( 'NONE',  ( 2.420285107995377327, 1.192830232448302441, -1.382225081888274643 ) ) ;
#50408=CARTESIAN_POINT ( 'NONE',  ( 3.603774441610514412, 1.461153639754816824, 1.385179026781646394 ) ) ;
#50409=CARTESIAN_POINT ( 'NONE',  ( 3.907043859180459933, -1.606318986283063799, 1.125903821926607318 ) ) ;
#50413=EDGE_CURVE ( 'NONE', #57833, #185672, #70710, .T. ) ;
#50414=CARTESIAN_POINT ( 'NONE',  ( -0.05888619351396630341, -1.618772603580875158, -1.322922665863958125 ) ) ;
#50415=CARTESIAN_POINT ( 'NONE',  ( 5.541803865142582275, 0.7143684798897788069, -1.619465043896466616 ) ) ;
#50417=CARTESIAN_POINT ( 'NONE',  ( 1.605704095283020605, -2.174604996184846595, 0.2706701637196773369 ) ) ;
#50418=CARTESIAN_POINT ( 'NONE',  ( 0.5381063436600447281, -1.494009556959356999, 0.8925505203737462701 ) ) ;
#50420=CARTESIAN_POINT ( 'NONE',  ( 0.6797846375097577054, -0.9621480743811950953, 1.431375779520219549 ) ) ;
#50421=CARTESIAN_POINT ( 'NONE',  ( 0.6854589470919645322, -1.231871052372325526, -1.940221060253940699 ) ) ;
#50422=CARTESIAN_POINT ( 'NONE',  ( 0.3983070667218471805, -0.7439898890007863308, -2.061537379893277677 ) ) ;
#50423=CARTESIAN_POINT ( 'NONE',  ( 6.222016520869273926, -1.489155408782488088, -0.8877787665630013647 ) ) ;
#50424=CARTESIAN_POINT ( 'NONE',  ( 3.229339687698820072, 0.05429069646168545316, 2.206380697113208722 ) ) ;
#50425=CARTESIAN_POINT ( 'NONE',  ( 1.674930785650229792, 1.460053457903678131, -1.606915656648603141 ) ) ;
#50426=CARTESIAN_POINT ( 'NONE',  ( 0.2756506080626683342, 1.048234779247591453, 1.494575289200591239 ) ) ;
#50427=CARTESIAN_POINT ( 'NONE',  ( 2.272804288956633112, -0.3671671630497001515, -2.085132402650377248 ) ) ;
#50428=CARTESIAN_POINT ( 'NONE',  ( 6.727182134110194056, 3.682851444631680682, 2.702965647100654234 ) ) ;
#50429=CARTESIAN_POINT ( 'NONE',  ( 5.614262457756467484, -0.8664596825185383322, -1.720589126903127264 ) ) ;
#50431=CARTESIAN_POINT ( 'NONE',  ( 2.806493257264990326, 1.658461721128750677, -1.582772817771603169 ) ) ;
#50435=CARTESIAN_POINT ( 'NONE',  ( 5.233148740271514221, 2.051824077619863296, 0.8514482647801949744 ) ) ;
#50443=CARTESIAN_POINT ( 'NONE',  ( 2.619767714365705658, 0.2496074646863334634, 2.000857082853441327 ) ) ;
#50445=CARTESIAN_POINT ( 'NONE',  ( 0.9892170606862679128, 0.1480104381128030111, 2.057284718974061288 ) ) ;
#50450=CARTESIAN_POINT ( 'NONE',  ( 4.470767510317084970, 0.001397387737574890204, -2.191629466793604930 ) ) ;
#50451=CARTESIAN_POINT ( 'NONE',  ( 1.688125190044654556, 1.678006053171029688, 1.117831401076685660 ) ) ;
#50452=CARTESIAN_POINT ( 'NONE',  ( 0.5382993156314471728, -1.579489783069366604, 0.9460463261394758128 ) ) ;
#50453=CARTESIAN_POINT ( 'NONE',  ( 5.689115845898126800, 1.733752489355618875, 1.499825188574270607 ) ) ;
#50454=CARTESIAN_POINT ( 'NONE',  ( 4.874869531740305462, 1.716800804850382223, -0.6655867697097294089 ) ) ;
#50456=CARTESIAN_POINT ( 'NONE',  ( 4.330939430599492823, 0.08983702179986638447, 1.823481399301421169 ) ) ;
#50457=CARTESIAN_POINT ( 'NONE',  ( 4.518204034511161815, -1.842447959940773705, 0.8197716922626956393 ) ) ;
#50459=CARTESIAN_POINT ( 'NONE',  ( 4.030342351814687696, 1.213150246598847293, -1.909612865279747052 ) ) ;
#50461=CARTESIAN_POINT ( 'NONE',  ( 6.387733883603046614, 1.449543625446013673, 1.527951702703828074 ) ) ;
#50463=CARTESIAN_POINT ( 'NONE',  ( 5.072747062355987602, 1.430223858385268665, -1.497173470029027120 ) ) ;
#50468=CARTESIAN_POINT ( 'NONE',  ( 1.910648867733771850, 1.427813452364127045, -1.293523827780170166 ) ) ;
#50473=CARTESIAN_POINT ( 'NONE',  ( 0.6332531790259123827, 1.961634380476449335, 0.8060562103610890983 ) ) ;
#50474=CARTESIAN_POINT ( 'NONE',  ( 1.547463978342083157, 0.2240547868478468541, 2.210115929984892258 ) ) ;
#50475=CARTESIAN_POINT ( 'NONE',  ( 2.872209793879555217, 1.125368584265328264, 1.779858853945482489 ) ) ;
#50478=CARTESIAN_POINT ( 'NONE',  ( 3.525789274851616639, 1.914599547803575330, -0.4273510147508317591 ) ) ;
#50485=CARTESIAN_POINT ( 'NONE',  ( 1.951583061186522583, -1.892041120407188304, 0.9578705467366486204 ) ) ;
#50488=CARTESIAN_POINT ( 'NONE',  ( 4.984793487045196869, 1.876812866478014596, 0.5713181500588762063 ) ) ;
#50489=CARTESIAN_POINT ( 'NONE',  ( 3.836934241894359054, 0.3148432204054998351, 2.138525872868973998 ) ) ;
#50490=CARTESIAN_POINT ( 'NONE',  ( 2.946635061770471076, -1.506786691049965432, -1.057933238436038925 ) ) ;
#50493=CARTESIAN_POINT ( 'NONE',  ( 4.259493880088534468, 0.8231460567260719952, 1.533345966155388540 ) ) ;
#50497=CARTESIAN_POINT ( 'NONE',  ( 1.692469166403000491, -2.151312531270420436, -0.2117842694067117448 ) ) ;
#50499=CARTESIAN_POINT ( 'NONE',  ( 3.954453749441131816, 1.458333106491338960, 1.392332789497241263 ) ) ;
#50501=CARTESIAN_POINT ( 'NONE',  ( 1.428841412761387986, 2.083414371474631377, 0.5762002773818803991 ) ) ;
#50502=CARTESIAN_POINT ( 'NONE',  ( 3.309407512850143451, -0.3859909667141645517, 1.933149248684182808 ) ) ;
#50504=CARTESIAN_POINT ( 'NONE',  ( 3.263160552478797882, 1.894124000634039851, -0.4281397233536556879 ) ) ;
#50512=CARTESIAN_POINT ( 'NONE',  ( 1.061882456046374434, 0.4290601450722114074, -2.164491299336705588 ) ) ;
#50514=CARTESIAN_POINT ( 'NONE',  ( 5.576992410575341452, 1.811172876804711507, 0.7542287045681006497 ) ) ;
#50515=CARTESIAN_POINT ( 'NONE',  ( 2.479138880926802901, -2.011204309026824344, -0.1455328587063598189 ) ) ;
#50517=CARTESIAN_POINT ( 'NONE',  ( 2.993478482863177081, -0.4084587893785693868, 2.077413892881809776 ) ) ;
#50519=CARTESIAN_POINT ( 'NONE',  ( 0.07459516483345089710, 0.2549822845471191868, -1.790622017744479155 ) ) ;
#50521=CARTESIAN_POINT ( 'NONE',  ( 4.417794048288587128, 1.130693009273657124, -1.452954439256304520 ) ) ;
#50524=CARTESIAN_POINT ( 'NONE',  ( 4.887034483293543730, -1.997634423138573867, -0.7120497732875651353 ) ) ;
#50527=CARTESIAN_POINT ( 'NONE',  ( 5.167286647625595641, 0.2060095241231186813, -2.050478191761321956 ) ) ;
#50529=CARTESIAN_POINT ( 'NONE',  ( 1.293147247811817779, -1.684623093139308025, 0.7912131235938785201 ) ) ;
#50530=CARTESIAN_POINT ( 'NONE',  ( 2.893917256732419396, -0.5369380550670297403, -1.761199466696103499 ) ) ;
#50535=CARTESIAN_POINT ( 'NONE',  ( 2.614145488985010424, -2.182733025630137824, 0.3247920039054427721 ) ) ;
#50536=CARTESIAN_POINT ( 'NONE',  ( 4.727936083913598431, -1.386761530526101405, -1.787517356406182811 ) ) ;
#50538=CARTESIAN_POINT ( 'NONE',  ( 4.377109366116209266, -1.621248278760094363, -0.8084319655582442588 ) ) ;
#50539=CARTESIAN_POINT ( 'NONE',  ( 4.926915384452605018, -1.639780065798799757, 0.9903009516807855794 ) ) ;
#50542=CARTESIAN_POINT ( 'NONE',  ( 4.733189744967194024, -1.710186631362722531, 0.7584244158565585092 ) ) ;
#50543=CARTESIAN_POINT ( 'NONE',  ( 4.545250530879026307, 1.662896905596674468, -0.8357390809586220382 ) ) ;
#50545=CARTESIAN_POINT ( 'NONE',  ( 6.244957947127046438, -1.492741346086885024, 0.9504933407481640506 ) ) ;
#50546=CARTESIAN_POINT ( 'NONE',  ( -0.08279552664090458758, -1.841734517378278424, 0.8216794407479923734 ) ) ;
#50548=CARTESIAN_POINT ( 'NONE',  ( 2.860102072500060544, 2.095886770163409185, -0.2068341903323153708 ) ) ;
#50553=CARTESIAN_POINT ( 'NONE',  ( 2.355728564803623915, -1.499445635549499389, -1.353443481924651470 ) ) ;
#50556=CARTESIAN_POINT ( 'NONE',  ( 6.720655732516679137, 4.703287744343486843, 2.289001594030832365 ) ) ;
#50559=CARTESIAN_POINT ( 'NONE',  ( 2.179201376995115513, -0.1036959380565916911, -2.159207860300814463 ) ) ;
#50560=FACE_OUTER_BOUND ( 'NONE', #204987, .T. ) ;
#50565=CARTESIAN_POINT ( 'NONE',  ( 6.491432910188612126, -0.4373703761123280964, 1.975813455233149218 ) ) ;
#50567=CARTESIAN_POINT ( 'NONE',  ( 1.470551405592795957, -2.082434148983134392, -0.6831980896230758216 ) ) ;
#50569=CARTESIAN_POINT ( 'NONE',  ( 2.026610535765199561, 1.302222112816675326, -1.850007447375429104 ) ) ;
#50576=CARTESIAN_POINT ( 'NONE',  ( 2.723612921674794407, -1.015349471937683656, -1.449289906420585305 ) ) ;
#50577=CARTESIAN_POINT ( 'NONE',  ( 3.176434313366371942, 0.9072602101105414762, 1.797144717478225795 ) ) ;
#50578=CARTESIAN_POINT ( 'NONE',  ( 6.721690211428396289, -2.142211831252617493, 0.5295551626897446740 ) ) ;
#50582=CARTESIAN_POINT ( 'NONE',  ( 5.378529868213833609, -0.4926607797600784378, -1.955169007017331317 ) ) ;
#50583=ORIENTED_EDGE ( 'NONE', *, *, #134927, .T. ) ;
#50584=CARTESIAN_POINT ( 'NONE',  ( 2.781945002432617997, -0.9632652739061452474, 1.603442845774772474 ) ) ;
#50585=CARTESIAN_POINT ( 'NONE',  ( 2.114207291064807759, 2.064986537539798661, -0.1480984254652456533 ) ) ;
#50587=CARTESIAN_POINT ( 'NONE',  ( 2.496234081663367022, -0.9796988711565941532, 1.642222327643327873 ) ) ;
#50591=CARTESIAN_POINT ( 'NONE',  ( -0.08783152977152529350, -1.912005390248720627, -0.04503566501021933483 ) ) ;
#50593=CARTESIAN_POINT ( 'NONE',  ( 2.558977423257744022, 1.577441344615847951, -1.166261179026031325 ) ) ;
#50596=CARTESIAN_POINT ( 'NONE',  ( 5.045234882716379765, 0.1584239314957915090, 2.114765283346302205 ) ) ;
#50599=CARTESIAN_POINT ( 'NONE',  ( 6.854760797074392897, -1.525272977149809694, 1.248552938341955798 ) ) ;
#50601=CARTESIAN_POINT ( 'NONE',  ( 1.529542846128278066, -0.2424046428922912721, 1.998471667700427057 ) ) ;
#50603=CARTESIAN_POINT ( 'NONE',  ( 1.282980312568120951, 1.728570797422763095, -1.222324810828350428 ) ) ;
#50605=CARTESIAN_POINT ( 'NONE',  ( 2.611853368047814872, 0.5545374748289233491, -1.994631108499920646 ) ) ;
#50610=CARTESIAN_POINT ( 'NONE',  ( 5.999963288868293887, -0.7514721766869683073, -1.951089947871258001 ) ) ;
#50612=CARTESIAN_POINT ( 'NONE',  ( 3.750846114953470867, -1.492790808496821775, 1.050590184284278861 ) ) ;
#50613=CARTESIAN_POINT ( 'NONE',  ( 3.176200218816268350, 0.8167180202140277290, 1.616994655555709981 ) ) ;
#50618=CARTESIAN_POINT ( 'NONE',  ( 4.840968367003476658, 0.3731960759543617168, 2.174832070070693568 ) ) ;
#50621=CARTESIAN_POINT ( 'NONE',  ( 4.213462193461685601, 1.537813053725526569, 1.136448645172025262 ) ) ;
#50628=CARTESIAN_POINT ( 'NONE',  ( 0.1164230846485321547, -0.09151219166612066525, 1.839079034809627755 ) ) ;
#50631=CARTESIAN_POINT ( 'NONE',  ( 3.760894150569486616, -1.648321677062795976, -0.8843367818652316803 ) ) ;
#50638=CARTESIAN_POINT ( 'NONE',  ( 1.059349595761612584, 1.606854154984382443, 1.138435182648824373 ) ) ;
#50639=CARTESIAN_POINT ( 'NONE',  ( 2.706657832681820697, 1.899625987897411772, 0.6766965020792228280 ) ) ;
#50643=CARTESIAN_POINT ( 'NONE',  ( 2.800927341068761844, 1.851789894747071008, 1.171597702228709181 ) ) ;
#50644=CARTESIAN_POINT ( 'NONE',  ( 6.428339884752385380, 1.046657586246093175, -1.495688092090129873 ) ) ;
#50653=CARTESIAN_POINT ( 'NONE',  ( 4.352959896991869471, 0.3989296284454147412, -1.797357466088687961 ) ) ;
#50654=CARTESIAN_POINT ( 'NONE',  ( 0.6803381722274345345, 0.9942335676262317179, 1.750384451323853785 ) ) ;
#50655=CARTESIAN_POINT ( 'NONE',  ( 2.741952636841408442, -2.198962954702073702, -0.6686182857488265352 ) ) ;
#50657=CARTESIAN_POINT ( 'NONE',  ( 0.6724161089360582988, 1.288989887148813018, -1.342485977130857711 ) ) ;
#50661=CARTESIAN_POINT ( 'NONE',  ( 4.640819915729988310, 1.831716588661407963, 0.5496940206762624959 ) ) ;
#50665=CARTESIAN_POINT ( 'NONE',  ( 3.843375017719421916, 0.7025675959630849343, -1.969317001441653670 ) ) ;
#50666=CARTESIAN_POINT ( 'NONE',  ( 2.113927203836548419, -0.8795192785214582809, -1.650985937663045577 ) ) ;
#50669=CARTESIAN_POINT ( 'NONE',  ( 5.565905774130330386, -1.163279849954502287, 1.427249551226833502 ) ) ;
#50672=CARTESIAN_POINT ( 'NONE',  ( 4.371539443043367612, 1.672179000890521516, -0.4225743650863537648 ) ) ;
#50674=CARTESIAN_POINT ( 'NONE',  ( 6.428370569364434850, 1.274405893209800356, -1.801548588985131039 ) ) ;
#50678=CARTESIAN_POINT ( 'NONE',  ( 4.909118719746323301, -1.747747579089290237, 1.287847701716714255 ) ) ;
#50679=CARTESIAN_POINT ( 'NONE',  ( 3.756323439517950558, 0.6585720284536450420, 1.702948436616057881 ) ) ;
#50680=CARTESIAN_POINT ( 'NONE',  ( 1.270277045833507312, -0.8771146801004360283, -1.754798696806989078 ) ) ;
#50681=CARTESIAN_POINT ( 'NONE',  ( 5.225823379661913570, 0.8554599082026111967, -1.936989086107894664 ) ) ;
#50683=CARTESIAN_POINT ( 'NONE',  ( 6.462434034201492317, -2.093801447487374734, -0.9336288876484639676 ) ) ;
#50686=CARTESIAN_POINT ( 'NONE',  ( 1.489100733002651555, -2.014586327357254181, -0.6619970261998938676 ) ) ;
#50691=CARTESIAN_POINT ( 'NONE',  ( 6.526262532640958902, 1.108799689610693751, 1.866440817598405966 ) ) ;
#50692=CARTESIAN_POINT ( 'NONE',  ( 6.983263157960330147, 2.017328405816510628, 2.456467998350126525 ) ) ;
#50694=CARTESIAN_POINT ( 'NONE',  ( 2.526306204038858194, -2.196730012672935661, 0.3287970392919815632 ) ) ;
#50696=CARTESIAN_POINT ( 'NONE',  ( 6.399064592084179992, -0.9530083391863402031, -1.777013033299412292 ) ) ;
#50698=CARTESIAN_POINT ( 'NONE',  ( 4.452046733557501135, -0.7940950990443145230, 1.903769949380555770 ) ) ;
#50703=CARTESIAN_POINT ( 'NONE',  ( 0.1331565106231606399, 5.723858289613107608, -2.539976893513963052 ) ) ;
#50704=CARTESIAN_POINT ( 'NONE',  ( 0.8672654471616656480, 2.014311826519481929, -0.5594637955527237416 ) ) ;
#50705=CARTESIAN_POINT ( 'NONE',  ( 4.395157833011634096, -0.8647231026696032830, -1.821742675176166060 ) ) ;
#50706=CARTESIAN_POINT ( 'NONE',  ( 4.054132754448328768, -1.361571661076573792, 1.239656203754435193 ) ) ;
#50708=CARTESIAN_POINT ( 'NONE',  ( 2.098289149679245735, -0.4564329974444079618, -1.663208130003128948 ) ) ;
#50709=CARTESIAN_POINT ( 'NONE',  ( 0.5851731681005939434, 1.651346252830317551, 1.157095189655330092 ) ) ;
#50710=CARTESIAN_POINT ( 'NONE',  ( 2.356409458221408126, 0.1091249688820790792, -2.296199191736052025 ) ) ;
#50712=CARTESIAN_POINT ( 'NONE',  ( 1.511376755312091591, 1.995097771225157635, 1.066857341152693373 ) ) ;
#50713=CARTESIAN_POINT ( 'NONE',  ( 4.371769818753069359, 2.042916674203521854, -0.5113404140953855537 ) ) ;
#50718=CARTESIAN_POINT ( 'NONE',  ( 6.739650031034449817, -0.2601230917362121753, 2.000000000000034639 ) ) ;
#50722=CARTESIAN_POINT ( 'NONE',  ( 5.379204547434111028, -2.008251482569714419, -0.9497353344293004707 ) ) ;
#50723=CARTESIAN_POINT ( 'NONE',  ( 3.345827479060593301, 2.191629467292684819, -0.0001215010576177677764 ) ) ;
#50727=CARTESIAN_POINT ( 'NONE',  ( 6.889999999999967706, 3.707772630975701311, 2.234475054783117809 ) ) ;
#50729=CARTESIAN_POINT ( 'NONE',  ( 5.836213162209912930, -1.179542664122106510, -1.762073437084572314 ) ) ;
#50733=CARTESIAN_POINT ( 'NONE',  ( 6.526263005029544928, 1.249015235541932167, -1.764162671312206498 ) ) ;
#50735=CARTESIAN_POINT ( 'NONE',  ( 6.532758020889952277, -1.641319963461195464, 0.8346263169811756200 ) ) ;
#50738=CARTESIAN_POINT ( 'NONE',  ( 0.7139227764019463462, 1.607345104371117772, 0.6680024673673248259 ) ) ;
#50743=CARTESIAN_POINT ( 'NONE',  ( 4.979442225389012933, 2.018306902694905425, -0.7746836383674888804 ) ) ;
#50746=CARTESIAN_POINT ( 'NONE',  ( 4.873979933848565871, 1.241796773192262116, 1.769252301715443565 ) ) ;
#50749=CARTESIAN_POINT ( 'NONE',  ( 6.134049847598044281, 0.9739642658876453973, -1.713909437456696105 ) ) ;
#50750=CARTESIAN_POINT ( 'NONE',  ( 4.780456778825039166, -1.700172319169111157, 0.3389010404759411621 ) ) ;
#50752=CARTESIAN_POINT ( 'NONE',  ( 2.296645709751913955, 1.758124065145909798, -1.308193547052277861 ) ) ;
#50753=CARTESIAN_POINT ( 'NONE',  ( 2.556097155687846900, 0.6156694008866661072, -2.223864192518353544 ) ) ;
#50754=CARTESIAN_POINT ( 'NONE',  ( 4.569639033146696505, 1.999850647628642175, -0.4969485059727016263 ) ) ;
#50755=CARTESIAN_POINT ( 'NONE',  ( 0.5857530202744161141, -1.927162159831939503, -0.2386530530817491391 ) ) ;
#50759=CARTESIAN_POINT ( 'NONE',  ( 3.445663904809421307, -1.957918079443463855, 0.8150281543025169606 ) ) ;
#50760=CARTESIAN_POINT ( 'NONE',  ( 1.336564801266389990, 0.5826540126645517459, -1.930418273149013153 ) ) ;
#50762=CARTESIAN_POINT ( 'NONE',  ( 4.419099417909471583, 2.016199240759775524, 0.8975180220924662278 ) ) ;
#50765=CARTESIAN_POINT ( 'NONE',  ( 1.955673630663162132, -0.6329532555123269510, 1.750116298748620958 ) ) ;
#50770=CARTESIAN_POINT ( 'NONE',  ( 6.825078400183546279, 2.419143596098617621, 2.525240329153962904 ) ) ;
#50774=CARTESIAN_POINT ( 'NONE',  ( 3.854412985283267368, 0.7401793164230722200, 1.923571582979522798 ) ) ;
#50777=CARTESIAN_POINT ( 'NONE',  ( 3.404948832191158736, -0.3961486058311721736, -1.980257767865372109 ) ) ;
#50780=CARTESIAN_POINT ( 'NONE',  ( 1.657177242756900926, -1.767118338917167852, -1.060216354352721435 ) ) ;
#50781=CARTESIAN_POINT ( 'NONE',  ( 6.983263157960363010, -0.003310164959547157865, 1.953544951557646403 ) ) ;
#50784=CARTESIAN_POINT ( 'NONE',  ( -0.1409997244346088141, 2.874455162768466909, -2.488748179275114492 ) ) ;
#50785=CARTESIAN_POINT ( 'NONE',  ( 1.130510352786683326, -1.665311210022573540, 0.7854980884962547982 ) ) ;
#50786=CARTESIAN_POINT ( 'NONE',  ( 5.619807753665406302, -2.153844256707802440, 0.4802137346974973409 ) ) ;
#50788=CARTESIAN_POINT ( 'NONE',  ( 1.440939128517594758, 0.4201678954103040819, 2.120193794684998245 ) ) ;
#50790=CARTESIAN_POINT ( 'NONE',  ( 2.448454179885679149, -1.387098808145654560, 1.463928423225707931 ) ) ;
#50791=CARTESIAN_POINT ( 'NONE',  ( 2.056460162951703197, 1.999754300726686029, -1.132793482217157033 ) ) ;
#50796=CARTESIAN_POINT ( 'NONE',  ( 4.961777154302105863, 1.950117994852887282, -0.2885197095366370257 ) ) ;
#50798=CARTESIAN_POINT ( 'NONE',  ( 3.643767777461913493, 2.000731686840724333, -0.2516315899964287617 ) ) ;
#50802=CARTESIAN_POINT ( 'NONE',  ( 6.709622069694824553, -0.4604308047033068840, 2.062537096560501659 ) ) ;
#50803=CARTESIAN_POINT ( 'NONE',  ( 5.195788487752976081, -1.461605715988937515, -1.466586839339318882 ) ) ;
#50806=CARTESIAN_POINT ( 'NONE',  ( 6.539320575229251808, 7.629137130509035636, 2.603262396134010892 ) ) ;
#50807=CARTESIAN_POINT ( 'NONE',  ( 5.027605771429075610, -0.2921156310390393140, 1.998402611621821423 ) ) ;
#50810=CARTESIAN_POINT ( 'NONE',  ( 0.3915631436273382948, -1.887207296038289961, 0.8326094146433449250 ) ) ;
#50816=CARTESIAN_POINT ( 'NONE',  ( 6.827182134110161726, 7.629137130509067610, 2.310944104600751281 ) ) ;
#50818=CARTESIAN_POINT ( 'NONE',  ( 2.664704904736223234, -0.8290184881076659851, -2.006861667775594160 ) ) ;
#50822=CARTESIAN_POINT ( 'NONE',  ( 3.069684041021227827, -1.094477399149307306, 1.480508570315848482 ) ) ;
#50824=CARTESIAN_POINT ( 'NONE',  ( 4.862908538974716421, 0.2148362657848035262, -2.180980218048253150 ) ) ;
#50826=CARTESIAN_POINT ( 'NONE',  ( 4.645576076348203465, -1.746196445045271606, -1.438666788099978389 ) ) ;
#50832=CARTESIAN_POINT ( 'NONE',  ( 6.661408102931688724, 0.2994711133218473931, -1.744046391327475964 ) ) ;
#50834=CARTESIAN_POINT ( 'NONE',  ( 3.633450831153079541, -0.1460068579729571769, 2.007839618615501642 ) ) ;
#50836=CARTESIAN_POINT ( 'NONE',  ( 2.555815334374893943, 0.5629295958425766244, -2.029244372067032565 ) ) ;
#50837=CARTESIAN_POINT ( 'NONE',  ( 1.054133004535224849, -1.214278006866207571, 1.481595424536867656 ) ) ;
#50841=CARTESIAN_POINT ( 'NONE',  ( 2.225000061332568890, -1.799552404990023113, -0.8009105870329900068 ) ) ;
#50842=CARTESIAN_POINT ( 'NONE',  ( 0.3033014811697418711, -0.5033704626738467747, 1.801585485020948951 ) ) ;
#50843=CARTESIAN_POINT ( 'NONE',  ( 1.029656018189710309, 1.891699080040713410, -0.5197978237033785698 ) ) ;
#50844=CARTESIAN_POINT ( 'NONE',  ( 6.539320575229251808, 0.01001626003939220556, 1.796977979958065852 ) ) ;
#50849=CARTESIAN_POINT ( 'NONE',  ( 6.086763352761943580, -0.2763008855245497331, -1.850001521387992565 ) ) ;
#50852=CARTESIAN_POINT ( 'NONE',  ( 6.561392567526037389, 1.717850402480676664, 1.155108059606273052 ) ) ;
#50864=CARTESIAN_POINT ( 'NONE',  ( 5.758247127753066685, -1.962046631956643195, -0.001586170976335121285 ) ) ;
#50866=CARTESIAN_POINT ( 'NONE',  ( 2.987657498945671453, 1.897406709466815444, 0.6818930838706840358 ) ) ;
#50867=CARTESIAN_POINT ( 'NONE',  ( 3.380013747803870316, -1.913774515330651127, -0.08860483629866824917 ) ) ;
#50869=CARTESIAN_POINT ( 'NONE',  ( 1.997856853652695497, -2.190977152517746163, 0.05759783203293508680 ) ) ;
#50870=CARTESIAN_POINT ( 'NONE',  ( 0.1333692844072802142, 0.2389375359408679178, -2.087895146362698906 ) ) ;
#50871=CARTESIAN_POINT ( 'NONE',  ( 2.881944908259078453, -0.9649329312324153030, 1.602325162460143559 ) ) ;
#50875=CARTESIAN_POINT ( 'NONE',  ( 4.798512230019831293, 1.459014486584905956, -1.534486623482501644 ) ) ;
#50877=CARTESIAN_POINT ( 'NONE',  ( 6.338344951546218908, -1.110931056888088353, 1.746890944850580052 ) ) ;
#50878=CARTESIAN_POINT ( 'NONE',  ( 2.138330579027637679, 0.4610650599585190967, 2.039099516977191495 ) ) ;
#50879=CARTESIAN_POINT ( 'NONE',  ( 6.620655732516651071, -0.002413161512292844035, 2.173887093218453082 ) ) ;
#50880=CARTESIAN_POINT ( 'NONE',  ( 0.9555556167152472469, 1.723134239262851475, -0.07815038326265508206 ) ) ;
#50885=( LENGTH_UNIT ( ) NAMED_UNIT ( * ) SI_UNIT ( .MILLI., .METRE. ) );
#50890=CARTESIAN_POINT ( 'NONE',  ( 1.119438638434491429, -0.4408070000805932032, 1.756890142956100576 ) ) ;
#50895=CARTESIAN_POINT ( 'NONE',  ( 6.539320575229234933, 1.301352213286063320, 1.914891792149053140 ) ) ;
#50900=CARTESIAN_POINT ( 'NONE',  ( 3.103785861066649776, 0.6724651444435655323, -1.735490194124859054 ) ) ;
#50901=CARTESIAN_POINT ( 'NONE',  ( 0.2103571609669597775, 1.833310535235525673, 0.5554914372104239328 ) ) ;
#50902=CARTESIAN_POINT ( 'NONE',  ( 0.3641364058636682999, 0.6611385597973111761, -2.014868753213174823 ) ) ;
#50908=CARTESIAN_POINT ( 'NONE',  ( 4.346514977827297344, -1.947402357529237626, -0.2931004117151541633 ) ) ;
#50909=CARTESIAN_POINT ( 'NONE',  ( 1.858217301831434964, 0.8087058978607818416, -1.960417502992222838 ) ) ;
#50913=CARTESIAN_POINT ( 'NONE',  ( 5.999973295341066937, -0.7855225714627244171, -2.046000194487001433 ) ) ;
#50915=CARTESIAN_POINT ( 'NONE',  ( 4.401339437636656804, 1.546884307994823793, 1.147896415085915667 ) ) ;
#50918=CARTESIAN_POINT ( 'NONE',  ( 0.8915962724085277902, 1.944627461026976034, -1.043433064090833140 ) ) ;
#50923=CARTESIAN_POINT ( 'NONE',  ( 5.823099318722479545, -1.778931037738925802, -0.8454068362369684397 ) ) ;
#50924=CARTESIAN_POINT ( 'NONE',  ( 1.522887052880964598, -1.828065777178315532, 0.6558840488102948285 ) ) ;
#50926=CARTESIAN_POINT ( 'NONE',  ( 0.1927366488196740335, -1.238295061544148812, -1.591656064170659191 ) ) ;
#50928=CARTESIAN_POINT ( 'NONE',  ( 4.803460451949028709, -1.436610920757129817, -1.182842806638328526 ) ) ;
#50934=CARTESIAN_POINT ( 'NONE',  ( 6.720655732516647163, 0.5950723047917580999, 1.879543361893110109 ) ) ;
#50935=CARTESIAN_POINT ( 'NONE',  ( 0.7850416839378616674, 1.930235501049954339, -1.037882601892345713 ) ) ;
#50939=CARTESIAN_POINT ( 'NONE',  ( 1.101864800459760207, -1.825872481749410525, -0.002338443969775172437 ) ) ;
#50941=CARTESIAN_POINT ( 'NONE',  ( 3.164447786964882603, 1.103041557463914524, 1.338080049202054145 ) ) ;
#50945=CARTESIAN_POINT ( 'NONE',  ( 0.04732232356348483465, -1.488192626783080952, -1.223051670295220994 ) ) ;
#50946=CARTESIAN_POINT ( 'NONE',  ( 4.785966450049039089, -1.203721183051874810, -1.548998264137561254 ) ) ;
#50949=CARTESIAN_POINT ( 'NONE',  ( 4.371814246616528621, 0.4635510597098577712, -2.069045912693792566 ) ) ;
#50954=CARTESIAN_POINT ( 'NONE',  ( 3.010663864534826928, 0.6931938328994196041, 1.950912564768356727 ) ) ;
#50958=CARTESIAN_POINT ( 'NONE',  ( 2.532212319380182208, -1.909192193906615209, 1.279991936841210043 ) ) ;
#50967=CARTESIAN_POINT ( 'NONE',  ( 4.007995338699682719, -0.7271224857151190601, 1.768968726348684406 ) ) ;
#50969=CARTESIAN_POINT ( 'NONE',  ( 5.245002492778637837, -1.477622881800463306, 0.8893561077145789584 ) ) ;
#50970=CARTESIAN_POINT ( 'NONE',  ( 3.081267818761534105, 1.592661989535900435, 1.236799713577160009 ) ) ;
#50971=CARTESIAN_POINT ( 'NONE',  ( 4.817139702178411476, 1.183121084409150425, -1.970709701559998805 ) ) ;
#50973=CARTESIAN_POINT ( 'NONE',  ( 0.4697016844467936103, 0.2121168557088908557, -2.196667960996725011 ) ) ;
#50975=CARTESIAN_POINT ( 'NONE',  ( 6.221911924188020748, -0.9849534058487903199, -1.470084644806458174 ) ) ;
#50977=CARTESIAN_POINT ( 'NONE',  ( 1.535548486519675571, -1.662869323620078665, -1.577994866025609566 ) ) ;
#50978=CARTESIAN_POINT ( 'NONE',  ( 0.4623611518889169103, 0.1752324854824957590, -1.731468860160074952 ) ) ;
#50979=B_SPLINE_CURVE_WITH_KNOTS ( 'NONE', 3,
 ( #99693, #17348, #25, #180937, #148455, #1096, #165763, #67157, #83430, #16280 ),
 .UNSPECIFIED., .F., .F.,
 ( 4, 1, 1, 1, 1, 1, 1, 4 ),
 ( 0.000000000000000000, 0.09599525230796020214, 0.1893027314675523320, 0.2592390727089966540, 0.3619855251144610819, 0.5211967264240887632, 0.7336899926499302893, 1.000000000000000000 ),
 .UNSPECIFIED. ) ;
#50981=CARTESIAN_POINT ( 'NONE',  ( 6.562441972333600937, -2.001882313047067985, -0.8919867065708479981 ) ) ;
#50985=CARTESIAN_POINT ( 'NONE',  ( 6.443811375169310907, 1.424792453395683500, 1.502365266013883538 ) ) ;
#50986=CARTESIAN_POINT ( 'NONE',  ( 0.6906390985809904848, 1.523792322931913468, -1.320830384837400118 ) ) ;
#50989=CARTESIAN_POINT ( 'NONE',  ( 5.338475953816137931, 1.898335173771143580, 0.3273637156304096130 ) ) ;
#50991=CARTESIAN_POINT ( 'NONE',  ( 2.197798511016679335, 2.028856164703813025, -0.9050913924920337417 ) ) ;
#50999=CARTESIAN_POINT ( 'NONE',  ( 4.792390001771311248, 1.443284891743993770, -0.9723301709525405956 ) ) ;
#51001=CARTESIAN_POINT ( 'NONE',  ( 2.295295855072278624, -1.753792786583353580, 0.8793850528211948347 ) ) ;
#51006=CARTESIAN_POINT ( 'NONE',  ( 0.6606829430093235089, -0.6931630328321845003, -1.942862509804524906 ) ) ;
#51009=CARTESIAN_POINT ( 'NONE',  ( 1.077466299836680630, -0.05792418700063763082, -2.261926406141855583 ) ) ;
#51012=CARTESIAN_POINT ( 'NONE',  ( 2.108475139129362574, 1.389272611029747750, -1.252756881873963168 ) ) ;
#51013=CARTESIAN_POINT ( 'NONE',  ( 1.564674090997038025, -0.9275931817575002736, 1.464960531123546961 ) ) ;
#51014=CARTESIAN_POINT ( 'NONE',  ( 4.985950990042907094, -2.174969566330759996, -0.2684501861200879747 ) ) ;
#51015=CARTESIAN_POINT ( 'NONE',  ( 5.368347952151684588, 1.131674353116480569, 2.010972138180310065 ) ) ;
#51016=CARTESIAN_POINT ( 'NONE',  ( 1.323197370116558469, -0.05141181009169673577, 2.060424651611890479 ) ) ;
#51017=CARTESIAN_POINT ( 'NONE',  ( 3.749888610702892144, 0.6998405808875374223, 1.811630882863373149 ) ) ;
#51019=CARTESIAN_POINT ( 'NONE',  ( 5.589076619078012342, 1.650032040524500143, -0.8810306647013476100 ) ) ;
#51020=CARTESIAN_POINT ( 'NONE',  ( 1.281250000000000444, 0.7852924748300526003, 1.895863743164061255 ) ) ;
#51022=CARTESIAN_POINT ( 'NONE',  ( 6.538435458278026857, 1.930121188254026787, -0.5825698962980339068 ) ) ;
#51025=CARTESIAN_POINT ( 'NONE',  ( 4.940077362011475515, -1.704937458037486531, -1.076318853994034930 ) ) ;
#51029=CARTESIAN_POINT ( 'NONE',  ( 1.980809073483770000, -0.08854697198140694392, -1.823669195971427071 ) ) ;
#51031=CARTESIAN_POINT ( 'NONE',  ( -0.1296875068448137269, 7.629137130509075604, -2.426516348560475045 ) ) ;
#51033=EDGE_LOOP ( 'NONE', ( #47336, #166064, #214265, #31989 ) ) ;
#51037=CARTESIAN_POINT ( 'NONE',  ( 6.375650237155517708, 0.3431015828706286408, -1.990142738341105000 ) ) ;
#51038=CARTESIAN_POINT ( 'NONE',  ( 6.463560548549353690, -1.782115098378980855, -1.325830300435285825 ) ) ;
#51042=CARTESIAN_POINT ( 'NONE',  ( 5.735248378139378822, -1.864208485850331609, 0.8789154904798938128 ) ) ;
#51043=CARTESIAN_POINT ( 'NONE',  ( 4.781875055470904634, 1.674888562130649960, -1.122497055794105414 ) ) ;
#51052=CARTESIAN_POINT ( 'NONE',  ( 4.991564454312596766, 1.928456700051227379, 0.5879293935868237231 ) ) ;
#51053=CARTESIAN_POINT ( 'NONE',  ( 4.997927640213790212, -0.6233917918176261619, -1.732523409203725606 ) ) ;
#51054=CARTESIAN_POINT ( 'NONE',  ( 0.07661050522435489119, 4.099791711901569435, -2.265836654070508605 ) ) ;
#51055=CARTESIAN_POINT ( 'NONE',  ( 3.580997583313150212, -2.223846063185720645, -0.6162045312432282707 ) ) ;
#51057=CARTESIAN_POINT ( 'NONE',  ( 5.097027542433036018, 1.800287743887505343, -1.196142203056582920 ) ) ;
#51059=CARTESIAN_POINT ( 'NONE',  ( 0.02871324022350740107, -1.775192216153992808, 0.7880070256306227483 ) ) ;
#51061=CARTESIAN_POINT ( 'NONE',  ( 3.919517222396780909, 0.8229245375931023565, 2.146178768164926254 ) ) ;
#51064=CARTESIAN_POINT ( 'NONE',  ( 3.608139902456270143, -0.7572706533398064765, -1.710698989992056607 ) ) ;
#51066=CARTESIAN_POINT ( 'NONE',  ( 1.494246876672610025, -1.020364814108923213, 1.617233793950809906 ) ) ;
#51069=CARTESIAN_POINT ( 'NONE',  ( 2.825073394047578734, 2.078234123670623212, 0.7428476018367863309 ) ) ;
#51074=CARTESIAN_POINT ( 'NONE',  ( 0.2453084554022276487, -1.520975263078115258, -1.253778558530042053 ) ) ;
#51075=CARTESIAN_POINT ( 'NONE',  ( 6.691963835194851384, -0.9925954392468823162, 2.080958020993000979 ) ) ;
#51076=CARTESIAN_POINT ( 'NONE',  ( 1.275752070009423367, -1.914805681740685106, 0.4264308320794732432 ) ) ;
#51078=CARTESIAN_POINT ( 'NONE',  ( 4.241124981676721362, -0.1973008666005781619, -2.053083420615212429 ) ) ;
#51086=CARTESIAN_POINT ( 'NONE',  ( 6.373493056145338009, -0.2723341383174918695, 2.153988726128319264 ) ) ;
#51088=CARTESIAN_POINT ( 'NONE',  ( 6.444863656277017405, -1.483217659742748218, -1.090817886357238198 ) ) ;
#51091=CARTESIAN_POINT ( 'NONE',  ( 1.774454573425466863, -1.774572579973210384, -0.5916213571805841731 ) ) ;
#51095=CARTESIAN_POINT ( 'NONE',  ( 1.523922206041250949, -1.897707704667614736, 0.2351830868887184178 ) ) ;
#51096=CARTESIAN_POINT ( 'NONE',  ( 3.379546851323252721, 1.122120933264129539, 1.368648242959294992 ) ) ;
#51097=CARTESIAN_POINT ( 'NONE',  ( 1.242663310189826564, 1.843194135250892707, 0.5091577964371830634 ) ) ;
#51099=CARTESIAN_POINT ( 'NONE',  ( 3.849167162397474140, 0.2308054593076276639, -1.901561516516042660 ) ) ;
#51101=CARTESIAN_POINT ( 'NONE',  ( 5.687944394218412469, -1.248225810400976465, -1.523521433493113308 ) ) ;
#51102=CARTESIAN_POINT ( 'NONE',  ( 1.266058358664986949, 0.6103625328083387425, -2.030891291126469600 ) ) ;
#51104=CARTESIAN_POINT ( 'NONE',  ( 3.520239479114236403, 1.187513476551487424, -1.445374034619356207 ) ) ;
#51105=CARTESIAN_POINT ( 'NONE',  ( 1.119449510670032177, -1.781678707675336870, 0.3977030049751931196 ) ) ;
#51107=CARTESIAN_POINT ( 'NONE',  ( 3.492985898914053866, -0.4302566696539159574, -2.164365734511737305 ) ) ;
#51110=CARTESIAN_POINT ( 'NONE',  ( 0.7837256325555241876, -1.959260395640700203, 0.6451903852672227213 ) ) ;
#51119=CARTESIAN_POINT ( 'NONE',  ( 4.281733463571851139, -1.982135700070002615, 0.5980053909793592304 ) ) ;
#51121=CARTESIAN_POINT ( 'NONE',  ( 1.810078809455554438, -2.145489296895970011, 0.2626290421628638128 ) ) ;
#51123=CARTESIAN_POINT ( 'NONE',  ( 1.963541569377712959, -1.623395098231813494, -1.201329681988633657 ) ) ;
#51131=CARTESIAN_POINT ( 'NONE',  ( 0.4797043241997685503, -0.7212876333932433104, 1.883314553594167107 ) ) ;
#51132=CARTESIAN_POINT ( 'NONE',  ( 6.539320575229280230, 7.629137130509070275, 2.703262396134015866 ) ) ;
#51133=CARTESIAN_POINT ( 'NONE',  ( 4.458633810090739225, -1.957822973221786667, -0.9849130632908837946 ) ) ;
#51135=CARTESIAN_POINT ( 'NONE',  ( 3.621269620730773298, 1.642686141288721480, 0.9789267784374030557 ) ) ;
#51138=CARTESIAN_POINT ( 'NONE',  ( 1.423454079394898875, -1.462460055423294047, -1.388472309132340321 ) ) ;
#51140=CARTESIAN_POINT ( 'NONE',  ( 0.1348729467166914497, 0.4002676433968958558, 2.257031873882467732 ) ) ;
#51142=CARTESIAN_POINT ( 'NONE',  ( 4.506709144069167117, 1.332172526941363344, -1.095522069602150372 ) ) ;
#51143=CARTESIAN_POINT ( 'NONE',  ( 0.1405533004714253908, 5.720147882271004569, -2.873730252010114228 ) ) ;
#51145=CARTESIAN_POINT ( 'NONE',  ( -0.02244404828157658613, -0.004869073801674199918, -2.189079685368473527 ) ) ;
#51146=CARTESIAN_POINT ( 'NONE',  ( 1.644895634054041933, -0.2845770130874228365, -1.940982728367894206 ) ) ;
#51149=CARTESIAN_POINT ( 'NONE',  ( 0.07536363704237906969, 4.084105538841027894, -2.698926661290324880 ) ) ;
#51153=( BOUNDED_SURFACE ( )  B_SPLINE_SURFACE ( 3, 3, ( 
 ( #210147, #8765, #61790, #127957, #45558, #29292, #95384, #123685, #113808, #80162, #46619, #82282, #114858, #179809, #66006, #146267, #31428, #212279, #96451, #145212, #163562, #181909, #162502, #97505, #15146, #81232, #63913, #133211, #33541, #17268, #129006, #180858, #132156, #147314, #211219, #130069, #196064, #213341, #47694, #64964, #131117, #32480, #100671, #62845, #198161, #14072, #194983, #197105, #99614, #48745, #98554, #164615, #16200, #148375, #199217, #165680, #83344, #112740, #214376, #49795, #115921, #178751, #149429, #1011, #67076, #50864, #116986, #182986, #34603, #166749, #30364, #18344, #2074, #200286, #38879, #51937, #171005, #152623, #85489, #20474, #104963, #102815, #19411, #52986, #202410, #86561, #106063, #84424, #35664, #4210, #121276, #151576, #201346, #204547, #172086, #186176, #70278, #37810, #136394, #118061, #184046, #56196, #3144, #103886, #120201, #137463, #154768, #167811, #101743, #135332, #69213, #119122, #54066, #122358, #185102, #169934, #36728, #21518, #87629, #168870, #150513, #68148, #153701, #134281, #138524, #188315, #5269, #203478, #71346, #55131, #187252, #22602, #88709, #6351, #72422, #39956, #140685, #205627, #75647, #192569, #206701, #90847, #189389, #44224, #76696, #77766, #74582, #7419, #73501, #58328, #143887, #124484, #156911, #190442, #42101, #108215, #139603, #174239, #41031, #10621, #25812, #141754, #45287, #91922, #173167, #57265, #175294, #207761, #157982, #159028, #24746, #9570, #8501, #59388, #125544, #191506, #43172, #92983, #109284, #26880, #142812, #208818, #193645, #60449, #126606, #110346, #123427, #176349, #27956, #94049, #160089, #11692, #209880, #61519, #127685, #111407, #23678, #89789, #155835, #107141, #98292, #114603, #112469, #214117, #78820, #99359, #144942, #62575, #162230, #47425, #163292, #129808, #14873, #148113, #180594, #65744, #197899, #97238, #17006, #181648, #13817, #164354, #128737, #130850, #79890, #30089, #149160, #15938, #95111, #212010, #12747, #131891, #82022, #210949, #49529, #146000, #738, #165410, #115653, #46351, #32219, #198951, #63653, #161160, #96179, #195787, #33274, #50593, #113540, #83081, #66804, #80965, #177411, #132946, #179544, #29028, #194711, #178478, #31165, #147057, #213077, #64707, #196847, #48485, #203227, #70015, #117800, #54871, #91400, #167549, #67874, #200027, #19149, #186992, #3948, #168610, #184845, #100411, #185913, #157460, #68951, #202146, #119937, #53807, #87372, #84160, #37547, #173721, #169679, #153442, #103627, #21267, #36474, #182718, #35400, #135072, #150247, #9055, #207248, #75130, #141239, #116718, #134020, #102546, #5014, #183792, #85223, #25298, #34336, #136131, #118859, #71087, #20212, #1816, #51679, #166480, #101478, #137204, #152370, #121025, #38623, #151312, #2880, #201085, #52726, #86300, #107695, #18072, #43717, #176898, #93532, #193137, #12243, #59936, #58874, #42651, #127166, #146560, #113036, #179042, #108761, #111970, #175843, #94601, #109833, #126091, #143366, #125030, #45850, #29586, #27434, #26361, #110891, #13320, #159576, #192052, #10113, #79393, #177973, #30660, #11173, #174786, #92475, #77249, #96744, #209363, #61009, #44785, #28511, #160643, #158515, #78318, #76188, #95674, #144442, #210445, #80461, #62083, #208306, #142296, #128241, #194205, #161728, #145511, #211510, #63146, #129308 ),
 ( #195286, #46918, #162794, #14371, #190987, #64220, #131400, #16501, #180100, #35966, #85792, #168113, #19713, #197397, #32777, #82582, #147607, #67372, #181154, #115160, #133514, #17560, #212580, #49040, #164906, #116220, #31726, #148668, #132455, #99915, #213626, #84721, #165976, #65251, #150809, #184343, #98855, #163858, #81527, #235, #68451, #83646, #50099, #66308, #196350, #199520, #102044, #198454, #149732, #1310, #51165, #183284, #97799, #117287, #52228, #34889, #100961, #167050, #18642, #182211, #130361, #33835, #2373, #15438, #47993, #114108, #134580, #200580, #118356, #186481, #21819, #86859, #6652, #120506, #54366, #72729, #171303, #107442, #202715, #104185, #55424, #119423, #170235, #71646, #39178, #23973, #152924, #38114, #89011, #155064, #70572, #123719, #121577, #204844, #138824, #56497, #122655, #4502, #188618, #53290, #73804, #185410, #37028, #136690, #87924, #137760, #153999, #203780, #40250, #106361, #172385, #90075, #187548, #205929, #156138, #5567, #7721, #103114, #105262, #22895, #139898, #189682, #57562, #69513, #41334, #201643, #173467, #25046, #169171, #151872, #3446, #135622, #20765, #177719, #174534, #28257, #112777, #142041, #74878, #158274, #9863, #29328, #178789, #208056, #111710, #144193, #10917, #91147, #78067, #75940, #157202, #127992, #129047, #211256, #59683, #195023, #191800, #46656, #193947, #95422, #140984, #60750, #210186, #125843, #8799, #43464, #109584, #159321, #175589, #27179, #93284, #126912, #206994, #58625, #61825, #124778, #190737, #45593, #42401, #161475, #76993, #92223, #143120, #13053, #209112, #26111, #192870, #44526, #110644, #108509, #176645, #94350, #160391, #79133, #11992, #145250, #62879, #34639, #164653, #197142, #16237, #48780, #146302, #212314, #199254, #47731, #82321, #98590, #49832, #149466, #196098, #63950, #97541, #130105, #113848, #32516, #50900, #163599, #148414, #81269, #114895, #166411, #179844, #30402, #14109, #180894, #96488, #117026, #183022, #31467, #181947, #147348, #66046, #15181, #213375, #132189, #80198, #115957, #99649, #64998, #131151, #198197, #17306, #33576, #165717, #83384, #1050, #67114, #100710, #133248, #162538, #207696, #44153, #129742, #192502, #76628, #60377, #110274, #126540, #59317, #176283, #175226, #210887, #160024, #127617, #31104, #27885, #158959, #125474, #161092, #193581, #93982, #144881, #10554, #11623, #142743, #26811, #9502, #77697, #46288, #92913, #143818, #209815, #61450, #208751, #211950, #97177, #45225, #191434, #111340, #177345, #162167, #75574, #28957, #30026, #62512, #95042, #141683, #128677, #12681, #43101, #112405, #47361, #195725, #78757, #113475, #194646, #179482, #178416, #96111, #13754, #79828, #145938, #109215, #63585, #114537, #32153, #214052, #19077, #50529, #672, #16936, #146995, #18002, #201012, #115587, #34271, #166407, #100343, #133953, #130788, #84092, #2810, #1747, #199960, #150179, #67804, #83017, #14813, #81959, #181581, #196783, #52659, #36399, #118787, #184773, #148044, #197836, #33210, #98231, #51608, #131827, #65680, #117732, #182649, #163231, #49468, #99294, #66738, #48424, #165341, #149090, #116652, #35330, #164286, #132881, #183721, #101409, #198883, #135001, #167482, #85158, #151241, #68882, #80904, #15874, #213012, #64648, #180531, #91174, #155090, #22920, #75967, #72753, #89035, #40276, #6676 ),
 ( #57589, #77018, #43493, #109613, #39196, #42429, #106386, #25072, #188645, #56522, #73833, #55447, #190765, #174564, #172409, #171324, #138850, #124806, #175618, #108534, #26140, #141013, #92253, #123746, #121599, #122682, #7746, #204867, #27205, #203801, #159347, #10944, #23997, #90100, #139929, #156165, #58652, #205956, #189707, #158299, #8828, #187571, #41360, #107470, #173496, #157233, #74905, #207021, #9890, #142070, #208084, #59711, #125871, #191830, #93312, #105288, #46685, #196125, #146327, #63983, #80229, #78093, #179872, #44553, #65026, #98619, #210214, #110669, #197171, #129076, #95451, #195047, #113877, #212342, #31497, #163629, #62906, #48807, #147378, #164680, #14136, #144220, #143147, #126940, #211283, #16265, #114924, #180923, #192897, #47763, #45619, #178816, #128017, #61850, #13081, #209142, #130136, #97572, #111736, #176669, #112803, #15210, #177742, #193971, #94375, #81301, #213405, #32544, #29357, #28281, #160416, #161501, #60781, #79161, #145277, #30429, #96515, #162564, #12021, #131181, #33606, #69274, #18408, #200348, #103950, #50928, #17332, #198224, #19471, #51997, #117053, #3205, #83413, #183050, #149495, #99676, #82349, #100735, #119181, #165746, #34665, #166814, #84484, #150574, #148440, #67143, #133277, #2136, #199285, #1078, #68212, #118123, #37873, #8, #135388, #66073, #49860, #36791, #115987, #168934, #134343, #184108, #35728, #102876, #101804, #167873, #85548, #151638, #201409, #169992, #132215, #53048, #185167, #20537, #86619, #152687, #202474, #181975, #4269, #70339, #136456, #54127, #120264, #186238, #141816, #22659, #123487, #187313, #55191, #108274, #105024, #121338, #72484, #38941, #171062, #139665, #59447, #6412, #9625, #41092, #191564, #107200, #88770, #21579, #5328, #89845, #109345, #75702, #207819, #71409, #74639, #138585, #57322, #204608, #154827, #106124, #87684, #8559, #206757, #56259, #203538, #73564, #190501, #122416, #188375, #40013, #42159, #140745, #125604, #172147, #137521, #23739, #155894, #43228, #7482, #205686, #189450, #173224, #24804, #90906, #156969, #58388, #124544, #174295, #25870, #153758, #91980, #158038, #76753, #112526, #145004, #143946, #96238, #176408, #209942, #28014, #126666, #175355, #193705, #212070, #192631, #127748, #45349, #111468, #94112, #163357, #63709, #47490, #159085, #211009, #162288, #177474, #160153, #14932, #129866, #113600, #10682, #62632, #13876, #61580, #26935, #11750, #77825, #29088, #95172, #161221, #12808, #128792, #130913, #93043, #79954, #142874, #208876, #195849, #60506, #179603, #78881, #194773, #46410, #31224, #178539, #110404, #30149, #146057, #97298, #196905, #44283, #81027, #147115, #213141, #64771, #48545, #20277, #136195, #1876, #116783, #67936, #182780, #82082, #214177, #86361, #115715, #134081, #65804, #148175, #201150, #197962, #131951, #165471, #49591, #181705, #18133, #152432, #99417, #102618, #200089, #70081, #51738, #33335, #114663, #98347, #34398, #202213, #168673, #4011, #164413, #167612, #17067, #150310, #83146, #149224, #199012, #180657, #101543, #85289, #799, #66867, #166545, #69016, #133012, #50657, #100470, #135133, #19210, #32282, #84222, #15997, #117861, #183853, #35465, #151375, #2944, #52788, #118927, #184907, #36531, #6150, #5074, #40834, #204343, #171882, #75450, #22403, #203286, #169740, #205430, #23479 ),
 ( #72220, #88512, #170812, #189197, #73294, #9379, #104763, #138327, #89586, #21329, #56001, #188120, #155635, #140490, #54933, #154574, #57068, #123232, #187052, #25618, #7220, #106943, #172966, #24545, #90653, #121085, #156714, #87436, #190250, #141563, #38684, #153504, #108019, #39751, #122152, #105856, #8305, #74389, #206501, #58132, #139397, #91730, #124291, #157781, #41908, #71149, #174045, #53867, #120000, #185977, #37610, #103691, #137266, #42978, #95993, #128558, #175103, #29908, #44034, #179362, #195607, #79709, #76506, #144762, #14693, #110152, #191310, #60259, #126416, #145824, #80788, #176165, #13636, #46171, #127495, #207571, #194523, #192379, #59192, #162046, #30984, #113357, #27765, #97059, #93861, #163112, #208625, #211829, #160973, #159899, #63466, #125347, #11506, #158837, #142617, #77577, #129621, #94924, #45110, #61336, #109088, #62393, #26690, #143700, #78637, #210773, #112285, #178301, #92792, #47242, #10434, #209692, #193466, #111220, #177223, #28836, #12563, #65561, #165221, #114415, #184649, #20015, #102347, #168418, #131708, #181465, #16813, #81840, #1621, #146878, #197712, #167360, #199837, #66610, #212898, #133824, #49354, #64530, #183594, #36270, #52532, #115472, #130675, #33094, #196663, #147924, #18948, #100218, #213940, #85032, #118666, #99168, #98119, #15756, #82898, #2686, #34148, #198760, #545, #48304, #67680, #180415, #148971, #17875, #150049, #83960, #117602, #32033, #51479, #200886, #35201, #101276, #151120, #68759, #132757, #164171, #50409, #116528, #182518, #166286, #134879, #41648, #107762, #4805, #120814, #170543, #21066, #155369, #54666, #203024, #6954, #105581, #173788, #136997, #38419, #204079, #53601, #104499, #5882, #187856, #172700, #87164, #186791, #23209, #89322, #70886, #57869, #55732, #139133, #73035, #205161, #56803, #153234, #122973, #201945, #8038, #86103, #22127, #119735, #140223, #71956, #88240, #138066, #188932, #40571, #106677, #24278, #121886, #124032, #90384, #189998, #156453, #37347, #39483, #154310, #171615, #152175, #74128, #3744, #206244, #135927, #69819, #185713, #103421, #169482, #76256, #211573, #13383, #112037, #108828, #176966, #46982, #142365, #9120, #92542, #158582, #178039, #25364, #191055, #93603, #62151, #10182, #208374, #145575, #113098, #127237, #27503, #193206, #159648, #207319, #125097, #63207, #26432, #44853, #42720, #58940, #29655, #174854, #60006, #126159, #192122, #43788, #143436, #129371, #109900, #79459, #110959, #195350, #28583, #175912, #91464, #75195, #11245, #157525, #141307, #77323, #209433, #78388, #61077, #94671, #160713, #12307, #144508, #210516, #128310, #194273, #45918, #95741, #161792, #133581, #81588, #31791, #130428, #199585, #17626, #18703, #15501, #162858, #14436, #213690, #84786, #147673, #97865, #65312, #131461, #197462, #80526, #49105, #196413, #166042, #115226, #82647, #203575, #181216, #114171, #146623, #116283, #148731, #32842, #99977, #180165, #98919, #163926, #48058, #179104, #164972, #1375, #16564, #299, #66370, #132518, #198516, #167116, #67436, #51228, #212640, #50162, #83711, #182274, #30726, #33898, #149801, #117352, #183350, #34954, #101025, #150874, #137557, #96809, #5363, #64282, #71445, #55226, #22691, #207856, #189485, #122453, #57358, #141851, #139700, #56293, #89879, #24842, #123521, #142912, #23774, #26973 ),
 ( #175387, #107240, #73598, #173261, #92016, #124578, #158074, #59482, #41128, #159120, #125639, #93078, #42195, #72523, #74675, #172184, #188412, #10721, #108310, #38976, #155931, #171100, #9662, #174330, #88804, #75738, #7516, #76790, #109380, #191600, #204642, #58425, #208912, #205723, #105062, #40049, #106158, #43262, #121372, #90941, #187347, #25906, #157007, #154863, #6445, #8593, #138619, #140778, #206793, #190539, #111504, #164451, #161258, #16038, #61617, #147153, #13911, #127787, #213178, #32319, #177510, #11788, #143985, #29122, #130954, #162327, #112568, #128829, #44319, #129904, #98387, #12845, #146097, #63745, #212108, #31264, #28055, #195888, #114700, #113639, #97338, #47526, #179644, #194811, #126704, #193742, #78919, #94148, #82121, #148214, #60546, #192665, #45388, #95209, #145041, #209976, #163396, #211044, #62670, #14970, #79993, #110441, #46447, #178579, #30187, #160187, #96277, #81067, #64807, #196944, #48584, #180694, #176443, #77862, #133050, #151414, #199052, #186015, #117900, #52829, #2988, #135175, #69055, #149266, #36571, #115754, #136232, #169780, #66910, #181745, #53906, #200130, #166588, #51783, #184944, #201190, #102657, #20318, #134121, #37651, #4051, #103729, #118966, #165513, #167650, #50698, #116822, #21369, #168714, #131994, #34440, #49629, #86404, #152471, #33375, #70121, #182824, #87477, #202255, #120041, #83183, #214216, #65845, #100513, #198003, #18177, #84264, #99456, #17105, #150349, #845, #1919, #183893, #67978, #35505, #101582, #19251, #85331, #191350, #59226, #204385, #43015, #39792, #109128, #154612, #25656, #106980, #6191, #91766, #125384, #56041, #104805, #22440, #122197, #9418, #40875, #205473, #7259, #137306, #8344, #175142, #105899, #24586, #156755, #90693, #124329, #121126, #74429, #207607, #206541, #190289, #140529, #58171, #73335, #5112, #72260, #171923, #187090, #26728, #153543, #71189, #203323, #138368, #188159, #23519, #88551, #41946, #89625, #155677, #108059, #173005, #54974, #139438, #57105, #123274, #38724, #189236, #174084, #157822, #75489, #141600, #170850, #29946, #180451, #48341, #114452, #11544, #127532, #177260, #27802, #162082, #61374, #209731, #13671, #112322, #92830, #143737, #45145, #210807, #60296, #111257, #12602, #194561, #179400, #93900, #193504, #96031, #79743, #77614, #64567, #62432, #145860, #211866, #63505, #129659, #159939, #195643, #208665, #14731, #158874, #28874, #126454, #146913, #78674, #94959, #144800, #47279, #113391, #31020, #97094, #128595, #130710, #163147, #196701, #80823, #44072, #46206, #161007, #178337, #10470, #212931, #76544, #142655, #192417, #110191, #176201, #213974, #68794, #82933, #3780, #20051, #118700, #115505, #183632, #53636, #149006, #15791, #99208, #165257, #184686, #119769, #582, #52569, #85067, #166322, #32068, #18986, #16850, #98157, #134914, #69854, #152210, #66648, #135964, #132793, #201980, #33128, #36306, #199872, #198796, #102385, #164204, #50445, #197748, #181500, #116564, #168452, #133865, #83997, #100253, #81877, #101314, #147961, #182557, #117640, #35239, #167395, #2722, #65594, #151153, #86139, #200921, #131743, #49386, #34181, #17911, #150086, #1657, #67714, #51515, #9154, #57904, #120853, #71993, #123013, #188965, #104534, #157561, #89358, #24314, #40607, #106712, #172738, #186827, #8078, #87203, #107797 ),
 ( #105620, #75231, #190033, #141341, #90420, #137033, #139168, #22163, #38457, #207355, #156489, #103457, #5921, #21100, #74166, #140259, #153268, #206281, #88278, #58975, #173822, #124068, #54703, #41686, #185749, #154343, #169519, #170580, #138105, #25400, #37382, #204115, #91500, #4843, #171649, #70922, #203060, #55767, #121925, #187892, #39520, #23246, #155406, #6989, #73069, #205199, #56840, #211606, #78421, #126193, #63242, #96841, #175943, #76289, #208406, #27539, #195384, #12341, #176999, #193241, #108861, #194309, #162889, #77357, #210550, #128343, #62186, #95772, #92576, #45950, #179138, #178071, #161829, #112070, #29689, #44888, #191088, #43819, #143470, #158618, #14471, #212673, #80560, #146659, #109934, #159676, #209467, #60040, #13416, #93634, #11278, #79491, #144543, #125130, #61110, #127270, #28615, #10215, #110994, #94705, #145610, #160746, #129404, #192156, #47016, #30761, #42757, #113131, #174887, #26467, #142398, #31824, #163959, #184444, #65347, #166075, #15537, #97900, #150910, #147705, #81621, #115257, #213724, #131494, #182307, #102143, #49141, #52328, #83748, #19809, #149840, #197498, #64314, #48092, #132550, #151970, #118458, #36062, #114204, #117390, #181250, #100010, #32877, #98954, #148763, #130459, #51266, #34992, #165005, #16599, #116316, #18738, #82680, #332, #66405, #84822, #183386, #168210, #198549, #180202, #50197, #33936, #85895, #17663, #1410, #67470, #133618, #199620, #101064, #167151, #2472, #68549, #134676, #200679, #196449, #186585, #153029, #119523, #155169, #187649, #38213, #138931, #4602, #104286, #70677, #169275, #3543, #21918, #40361, #20861, #170334, #88027, #154099, #136787, #206031, #106464, #90182, #201746, #39275, #204952, #5668, #69614, #202815, #54464, #71747, #120608, #137863, #203883, #105370, #173579, #135723, #56600, #53387, #185510, #172490, #37133, #156245, #55527, #121682, #171407, #24077, #22997, #89114, #6752, #72828, #122764, #25149, #103215, #86960, #188723, #7823, #73915, #140008, #57666, #123824, #189786, #41436, #107545, #91250, #125949, #9967, #208160, #191905, #59792, #141089, #109687, #108611, #144297, #93387, #60856, #178892, #43568, #92332, #58728, #94454, #127018, #175690, #78168, #158374, #27281, #76044, #174638, #157310, #159423, #194047, #26215, #11023, #77100, #143225, #142146, #145359, #45699, #29435, #207100, #192977, #210290, #209215, #8900, #44630, #110746, #176744, #28358, #160492, #12099, #61931, #112878, #74981, #128089, #124879, #190843, #111817, #42505, #95526, #177819, #161576, #13163, #79241, #211359, #62984, #129153, #195128, #46766, #30506, #96587, #47839, #164752, #133353, #163703, #213474, #2213, #118198, #198295, #98694, #49936, #16342, #64059, #196196, #68289, #97644, #116057, #113950, #130202, #183129, #179946, #31569, #147451, #15284, #81370, #79, #134422, #65097, #84561, #182047, #52071, #33677, #131254, #162636, #80305, #82423, #184185, #150651, #200425, #146405, #149571, #197241, #132289, #48880, #114998, #180997, #14210, #83488, #67217, #32616, #148512, #66144, #51006, #99751, #1155, #199359, #165821, #117127, #17404, #212417, #34735, #100807, #166893, #18485, #123563, #205769, #57398, #169011, #70416, #120342, #185246, #105104, #4347, #152766, #171143, #55270, #35807, #86697, #202552, #153841, #3286, #54203, #170073, #137602 ),
 ( #187389, #36869, #72567, #151716, #172228, #101884, #102952, #69353, #89922, #21659, #186318, #87765, #6492, #39021, #138665, #56337, #5411, #73646, #40090, #7560, #22735, #201485, #203619, #136532, #20609, #139745, #88852, #167949, #37953, #85629, #204687, #154908, #135463, #122498, #104025, #19552, #23817, #188459, #119260, #106202, #53130, #71490, #121417, #155973, #108351, #130747, #214014, #25952, #210022, #28095, #109424, #65636, #176485, #174373, #189526, #11830, #15830, #98194, #92058, #81916, #75783, #148003, #190580, #64607, #142955, #42238, #196741, #164242, #158115, #140822, #58468, #9707, #48381, #76835, #27015, #43304, #173302, #44363, #41173, #141890, #60590, #192707, #126748, #160231, #157050, #110486, #32109, #107281, #207899, #94191, #77907, #144027, #114494, #8638, #180490, #24882, #90987, #74718, #206835, #124622, #175429, #59522, #125682, #191640, #93123, #159162, #10761, #208957, #87250, #50488, #166365, #1704, #66690, #200966, #100298, #34226, #52613, #151196, #153315, #182602, #84043, #35284, #99250, #150131, #51562, #19030, #3826, #132837, #17956, #68838, #134958, #116609, #103504, #101360, #184726, #118742, #36350, #102428, #198841, #168497, #33168, #53683, #4890, #67758, #165298, #185794, #117687, #133909, #183679, #20096, #86184, #152253, #69899, #167438, #169564, #136010, #21146, #202023, #82974, #85110, #199915, #2767, #131784, #119814, #49425, #37427, #181540, #197788, #115545, #16893, #149047, #623, #42800, #59017, #157605, #154389, #8126, #92620, #121969, #54748, #138150, #204159, #9201, #158662, #187935, #91547, #124115, #205243, #70968, #57950, #55814, #137078, #107839, #108908, #191134, #39565, #174931, #171694, #26511, #72037, #75273, #24358, #105667, #141388, #203103, #23293, #22212, #5967, #89403, #207398, #172785, #123059, #139212, #120898, #140307, #186871, #125173, #38503, #104581, #190078, #155452, #106757, #7035, #73112, #56884, #170626, #41730, #173866, #189013, #88325, #40656, #25441, #90468, #156535, #74212, #206325, #29732, #113177, #77400, #208449, #142442, #61153, #179181, #209512, #93681, #143516, #127315, #193285, #60082, #44930, #43863, #178117, #111038, #12386, #14514, #177045, #27583, #126239, #194352, #78465, #28661, #95814, #159723, #94747, #11321, #109979, #10260, #160794, #79536, #144584, #210598, #62227, #128384, #45994, #30804, #145654, #63287, #192201, #112114, #161872, #13460, #76335, #211650, #129448, #195430, #47060, #96884, #162933, #80607, #175989, #54351, #169155, #2357, #103096, #183268, #117270, #135607, #19697, #170219, #51146, #167033, #118341, #182192, #18628, #134563, #102029, #86843, #149716, #100946, #151856, #3432, #133499, #186463, #184325, #53276, #69499, #201627, #119407, #1296, #37014, #116205, #136676, #21803, #67354, #33820, #120490, #200566, #84707, #52212, #185396, #20748, #152909, #4486, #35950, #38099, #70557, #104170, #202701, #165960, #168098, #34872, #199502, #17544, #219, #150794, #87910, #83634, #68433, #85775, #66291, #132437, #198438, #50084, #99899, #137745, #123705, #140969, #122641, #5550, #138809, #204828, #7705, #56479, #72713, #188603, #189666, #109570, #71632, #106346, #187533, #203765, #208042, #55409, #26096, #73788, #155048, #90061, #174520, #172368, #88995, #40235, #57547, #156122, #175574, #153983, #105247, #139882 ) ),
 .UNSPECIFIED., .T., .F., .T. ) 
 B_SPLINE_SURFACE_WITH_KNOTS ( ( 4, 3, 4 ),
 ( 4, 1, 1, 1, 1, 1, 1, 1, 1, 1, 1, 1, 1, 1, 1, 1, 1, 1, 1, 1, 1, 1, 1, 1, 1, 1, 1, 1, 1, 1, 1, 1, 1, 1, 1, 1, 1, 1, 1, 1, 1, 1, 1, 1, 1, 1, 1, 1, 1, 1, 1, 1, 1, 1, 1, 1, 1, 1, 1, 1, 1, 1, 1, 1, 1, 1, 1, 1, 1, 1, 1, 1, 1, 1, 1, 1, 1, 1, 1, 1, 1, 1, 1, 1, 1, 1, 1, 1, 1, 1, 1, 1, 1, 1, 1, 1, 1, 1, 1, 1, 1, 1, 1, 1, 1, 1, 1, 1, 1, 1, 1, 1, 1, 1, 1, 1, 1, 1, 1, 1, 1, 1, 1, 1, 1, 1, 1, 1, 1, 1, 1, 1, 1, 1, 1, 1, 1, 1, 1, 1, 1, 1, 1, 1, 1, 1, 1, 1, 1, 1, 1, 1, 1, 1, 1, 1, 1, 1, 1, 1, 1, 1, 1, 1, 1, 1, 1, 1, 1, 1, 1, 1, 1, 1, 1, 1, 1, 1, 1, 1, 1, 1, 1, 1, 1, 1, 1, 1, 1, 1, 1, 1, 1, 1, 1, 1, 1, 1, 1, 1, 1, 1, 1, 1, 1, 1, 1, 1, 1, 1, 1, 1, 1, 1, 1, 1, 1, 1, 1, 1, 1, 1, 1, 1, 1, 1, 1, 1, 1, 1, 1, 1, 1, 1, 1, 1, 1, 1, 1, 1, 1, 1, 1, 1, 1, 1, 1, 1, 1, 1, 1, 1, 1, 1, 1, 1, 1, 1, 1, 1, 1, 1, 1, 1, 1, 1, 1, 1, 1, 1, 1, 1, 1, 1, 1, 1, 1, 1, 1, 1, 1, 1, 1, 1, 1, 1, 1, 1, 1, 1, 1, 1, 1, 1, 1, 1, 1, 1, 1, 1, 1, 1, 1, 1, 1, 1, 1, 1, 1, 1, 1, 1, 1, 1, 1, 1, 1, 1, 1, 1, 1, 1, 1, 1, 1, 1, 1, 1, 1, 1, 1, 1, 1, 1, 1, 1, 1, 1, 1, 1, 1, 1, 1, 1, 1, 1, 1, 1, 1, 1, 1, 1, 1, 1, 1, 1, 1, 1, 1, 1, 1, 1, 1, 1, 1, 1, 1, 1, 1, 1, 1, 1, 1, 1, 1, 1, 1, 1, 1, 1, 1, 1, 1, 1, 4 ),
 ( 0.000000000000000000, 0.5000000000000000000, 1.000000000000000000 ),
 ( 0.000000000000000000, 0.002600063085273907840, 0.005208809393482579861, 0.007813201938950280895, 0.01041611862257568050, 0.01302098276518856741, 0.01562474632808895890, 0.01822919105953027183, 0.02083324087635668453, 0.02343728507989274734, 0.02604173773626635227, 0.02864548761524753420, 0.03125016255115702773, 0.03385383280295282959, 0.03645844125268089125, 0.03906229690237970897, 0.04166656525949016115, 0.04427081591349327910, 0.04687468903198145631, 0.04947928942627017462, 0.05208296534865054783, 0.05468764290212216328, 0.05729137561078536528, 0.05989584521530456201, 0.06249987723257615507, 0.06510392926424246607, 0.06770838613806146045, 0.07031213076997053224, 0.07291680575263978503, 0.07552047744215656389, 0.07812508546332513903, 0.08072894086165181837, 0.08333320924388483431, 0.08593745993457323207, 0.08854133291633270453, 0.09114593330519306369, 0.09374960916840779923, 0.09635428668231969807, 0.09895801939011879267, 0.1015624889210437753, 0.1041665209728785957, 0.1067705729027476208, 0.1093750297965602747, 0.1119787743537518920, 0.1145834493281674554, 0.1171871210017138010, 0.1197917289818775377, 0.1223955844170728779, 0.1249998527215379351, 0.1276041034591044177, 0.1302079763611066199, 0.1328125767709825433, 0.1354162526020633861, 0.1380209301064295735, 0.1406246628425296130, 0.1432291323291436380, 0.1458331644451768827, 0.1484372163025670099, 0.1510416732455448496, 0.1536454177576472568, 0.1562500927529001105, 0.1588537644400710158, 0.1614583724083656635, 0.1640622279099430147, 0.1666664961659596600, 0.1692707469797122277, 0.1718746198314790308, 0.1744792202914958457, 0.1770828961200470730, 0.1796875736439581817, 0.1822913064379278192, 0.1848957759094348730, 0.1874998081190861754, 0.1901038599334289314, 0.1927083169547665342, 0.1953120614513534081, 0.1979167364965291054, 0.2005204082269216870, 0.2031250162124720871, 0.2057288718099357372, 0.2083331400468157457, 0.2109373909660553770, 0.2135412637971000893, 0.2161458643363758370, 0.2187495401919937743, 0.2213542177645327069, 0.2239579506459335456, 0.2265624201315297737, 0.2291664524642116896, 0.2317705042649303715, 0.2343749613938155840, 0.2369787059044528299, 0.2395833810286300269, 0.2421870528318344207, 0.2447916608637582536, 0.2473955165866061623, 0.2499997848336539263, 0.2526040358876752157, 0.2552079087275039293, 0.2578125093751503782, 0.2604161852874245509, 0.2630208629376679097, 0.2656245959360551967, 0.2682290654649299166, 0.2708330979500496172, 0.2734371497665608608, 0.2760416070321756732, 0.2786453515864226738, 0.2812500268186742258, 0.2838536987242743503, 0.2864583068316831627, 0.2890621627094078216, 0.2916664309959213219, 0.2942706822140139789, 0.2968745550921262355, 0.2994791558772498252, 0.3020828318757637354, 0.3046875096327826826, 0.3072912427777066413, 0.3098957123790437307, 0.3124997450460035853, 0.3151037969077182255, 0.3177082543392401592, 0.3203119989666507461, 0.3229166743360447622, 0.3255203463736199843, 0.3281249545856204097, 0.3307288106477103140, 0.3333330790029824242, 0.3359373304144318562, 0.3385412033603223403, 0.3411458043120255135, 0.3437494804263583337, 0.3463541583192197293, 0.3489578916402267250, 0.3515623613432052874, 0.3541663942214042238, 0.3567704461577280162, 0.3593749037843310123, 0.3619786485144548260, 0.3645833240500557237, 0.3671869962491814965, 0.3697916045948764219, 0.3723954608708167080, 0.3749997293241361662, 0.3776039809582251716, 0.3802078540013843488, 0.3828124551487663840, 0.3854161314084936785, 0.3880208094662612184, 0.3906245429928945634, 0.3932290128266905938, 0.3958330459455252637, 0.3984370979858605777, 0.4010415558367163569, 0.4036453006990994852, 0.4062499764299690730, 0.4088536488202184072, 0.4114582573287078326, 0.4140621138479816388, 0.4166663824286341855, 0.4192706343146435644, 0.4218745074845589027, 0.4244791088567174686, 0.4270827852914125256, 0.4296874635431477407, 0.4322911973049493040, 0.4348956672987361882, 0.4374997006876018557, 0.4401037528613486738, 0.4427082109656274023, 0.4453119559898139901, 0.4479166319450127998, 0.4505203045559570407, 0.4531249132563394122, 0.4557287700484292658, 0.4583330387856985322, 0.4609372909529084184, 0.4635411642790657205, 0.4661457659050973201, 0.4687494425443319290, 0.4713541210190953512, 0.4739578550456061690, 0.4765623252285562383, 0.4791663589168480009, 0.4817704112534048067, 0.4843748696402766507, 0.4869786148558097882, 0.4895832910643978519, 0.4921869639256079565, 0.4947915728469811647, 0.4973954299413693159, 0.4999996988645384333, 0.5026039513422294602, 0.5052078248541136407, 0.5078124267631153321, 0.5104161036364611714, 0.5130207823633133879, 0.5156245166840751626, 0.5182289870853604707, 0.5208330211024742029, 0.5234370736312391470, 0.5260415323298749390, 0.5286452777662975500, 0.5312499542573357880, 0.5338536273983837122, 0.5364582365698458144, 0.5390620939960163449, 0.5416663631343685559, 0.5442706159518226894, 0.5468744896789192733, 0.5494790918999890028, 0.5520827690370186946, 0.5546874480450217915, 0.5572911826895774468, 0.5598956533383712131, 0.5624996877137050655, 0.5651037404640770756, 0.5677081995036498130, 0.5703119451905063197, 0.5729166219930570403, 0.5755202954435161278, 0.5781249048941674573, 0.5807287626816063364, 0.5833330320644263267, 0.5859372852509285856, 0.5885411592227242084, 0.5911457617849628088, 0.5937494392152512512, 0.5963541185334689798, 0.5989578535313645480, 0.6015623244568418793, 0.6041663592197970001, 0.6067704122211770024, 0.6093748716308627911, 0.6119786175976995590, 0.6145832947408284008, 0.6171869685302752151, 0.6197915782892181591, 0.6223954364674153528, 0.6249997061239902507, 0.6276039597088286515, 0.6302078339548128350, 0.6328124368873246919, 0.6354161146404495586, 0.6380207942979494451, 0.6406245296787346222, 0.6432290009100736228, 0.6458330360900554901, 0.6484370893718474083, 0.6510415491808263511, 0.6536452954571934093, 0.6562499729699700080, 0.6588536471279848872, 0.6614582572243260516, 0.6640621158227759668, 0.6666663857823964534, 0.6692706397948642305, 0.6718745143445301604, 0.6744791176764239893, 0.6770827957819672838, 0.6796874758078212952, 0.6822912116010506622, 0.6848956831674339885, 0.6874997187938534093, 0.6901037723854651640, 0.6927082326229228038, 0.6953119792383747333, 0.6979166571498732763, 0.7005203317060422208, 0.7031249421688929857, 0.7057288012170955804, 0.7083330715090569996, 0.7109373259784533827, 0.7135412008612989077, 0.7161458046216893081, 0.7187494831092385850, 0.7213541635325240176, 0.7239578997677582617, 0.7265623716983737879, 0.7291664078006476757, 0.7317704617314926274, 0.7343749224266207243, 0.7369786694107173242, 0.7395833477500189934, 0.7421870227339337767, 0.7447916335924112952, 0.7473954931198736329, 0.7499997637734774347, 0.7526040187291080930, 0.7552078939746372788, 0.7578124981926457338, 0.7604161770917949870, 0.7630208579415957981, 0.7656245946484027121, 0.7682290669724446408, 0.7708331035799980135, 0.7734371578794957403, 0.7760416190614934928, 0.7786453664438016675, 0.7812500452399944173, 0.7838537206812543623, 0.7864583319644831150, 0.7890621920007202528, 0.7916664630452742157, 0.7942707185164536998, 0.7968745941541772737, 0.7994791988589329268, 0.8020828781992835887, 0.8046875595046918406, 0.8072912967126475436, 0.8098957694593176271, 0.8124998066015838294, 0.8151038612991610144, 0.8177083229972362810, 0.8203120708073305956, 0.8229167500895105958, 0.8255204260177235742, 0.8281250377548363684, 0.8307288983293719120, 0.8333331697941922522, 0.8359374258102438837, 0.8385413018696807885, 0.8411459070903221091, 0.8437495869014844940, 0.8463542686916004643, 0.8489580064302900686, 0.8515624796287988296, 0.8541665173352209761, 0.8567705724603134065, 0.8593750347036837045, 0.8619787829711476057, 0.8645834627684209073, 0.8671871392132045608, 0.8697917514333429745, 0.8723956125757112989, 0.8749998844901232253, 0.8776041410803804288, 0.8802080175910590443, 0.8828126233567346048, 0.8854163036683286858, 0.8880209859722626442, 0.8906247242712825862, 0.8932291979508502067, 0.8958332362508822921, 0.8984372918329353030, 0.9010417546508288078, 0.9036455034052560675, 0.9062501837467389354, 0.9088538607377212308, 0.9114584734700372781, 0.9140623352097841936, 0.9166666076031229071, 0.9192708647969299873, 0.9218747417883903505, 0.9244793481282622682, 0.9270830289699085736, 0.9296877118167798937, 0.9322914507057830091, 0.9348959248956096868, 0.9374999638185942397, 0.9401040198872741005, 0.9427084833090058069, 0.9453122325795346725, 0.9479169134952544207, 0.9505205910598265584, 0.9531252043308329203, 0.9557290667238423909, 0.9583333396063040688, 0.9609375973010293448, 0.9635414750455153499, 0.9661460823481272664, 0.9687497623469286667, 0.9713544456720903941, 0.9739581901020435417, 0.9765626606554614897, 0.9791666924408860551, 0.9817707657828746992, 0.9843752055175947202, 0.9869789906880002128, 0.9895838567146432174, 0.9921867690109741345, 0.9947911791560083428, 0.9973999138825643263, 0.9999999999999998890 ),
 .UNSPECIFIED. ) 
 GEOMETRIC_REPRESENTATION_ITEM ( )  RATIONAL_B_SPLINE_SURFACE ( (
 ( 1.000000000000000222, 1.000000000000000222, 1.000000000000000222, 1.000000000000000222, 1.000000000000000444, 1.000000000000000444, 1.000000000000000222, 1.000000000000000444, 1.000000000000000222, 1.000000000000000444, 1.000000000000000444, 1.000000000000000000, 1.000000000000000222, 1.000000000000000000, 1.000000000000000222, 1.000000000000000222, 1.000000000000000444, 1.000000000000000000, 1.000000000000000444, 1.000000000000000444, 1.000000000000000222, 1.000000000000000222, 1.000000000000000000, 1.000000000000000222, 1.000000000000000000, 1.000000000000000444, 1.000000000000000000, 1.000000000000000444, 1.000000000000000222, 1.000000000000000000, 1.000000000000000666, 1.000000000000000000, 1.000000000000000222, 1.000000000000000666, 1.000000000000000222, 1.000000000000000444, 1.000000000000000222, 1.000000000000000444, 1.000000000000000000, 1.000000000000000444, 1.000000000000000000, 1.000000000000000444, 1.000000000000000000, 1.000000000000000444, 1.000000000000000000, 1.000000000000000222, 1.000000000000000444, 1.000000000000000000, 1.000000000000000444, 1.000000000000000222, 1.000000000000000222, 1.000000000000000444, 1.000000000000000222, 1.000000000000000444, 1.000000000000000222, 1.000000000000000222, 1.000000000000000444, 1.000000000000000444, 1.000000000000000222, 1.000000000000000222, 1.000000000000000444, 1.000000000000000222, 1.000000000000000444, 1.000000000000000000, 1.000000000000000222, 1.000000000000000222, 1.000000000000000222, 1.000000000000000222, 1.000000000000000444, 1.000000000000000000, 0.9999999999999997780, 1.000000000000000444, 1.000000000000000444, 1.000000000000000222, 1.000000000000000222, 1.000000000000000444, 0.9999999999999997780, 1.000000000000000666, 1.000000000000000000, 1.000000000000000000, 1.000000000000000444, 1.000000000000000222, 1.000000000000000222, 0.9999999999999997780, 1.000000000000000222, 1.000000000000000444, 0.9999999999999997780, 1.000000000000000444, 1.000000000000000000, 1.000000000000000000, 1.000000000000000444, 1.000000000000000000, 1.000000000000000444, 1.000000000000000444, 0.9999999999999997780, 1.000000000000000444, 1.000000000000000444, 1.000000000000000444, 1.000000000000000444, 1.000000000000000000, 1.000000000000000444, 1.000000000000000222, 1.000000000000000000, 1.000000000000000444, 1.000000000000000444, 1.000000000000000222, 1.000000000000000000, 1.000000000000000444, 1.000000000000000444, 1.000000000000000000, 1.000000000000000222, 1.000000000000000000, 1.000000000000000444, 1.000000000000000222, 1.000000000000000444, 1.000000000000000222, 1.000000000000000444, 1.000000000000000444, 1.000000000000000000, 1.000000000000000666, 1.000000000000000222, 1.000000000000000222, 1.000000000000000000, 1.000000000000000222, 1.000000000000000222, 1.000000000000000222, 1.000000000000000444, 1.000000000000000222, 1.000000000000000222, 1.000000000000000444, 0.9999999999999997780, 1.000000000000000666, 0.9999999999999997780, 1.000000000000000222, 1.000000000000000000, 1.000000000000000444, 1.000000000000000000, 1.000000000000000444, 1.000000000000000000, 1.000000000000000222, 1.000000000000000222, 1.000000000000000444, 1.000000000000000444, 1.000000000000000222, 1.000000000000000444, 1.000000000000000444, 1.000000000000000000, 1.000000000000000666, 1.000000000000000222, 1.000000000000000222, 1.000000000000000444, 1.000000000000000000, 1.000000000000000222, 1.000000000000000444, 1.000000000000000000, 1.000000000000000222, 1.000000000000000222, 1.000000000000000444, 1.000000000000000222, 1.000000000000000222, 1.000000000000000444, 1.000000000000000000, 1.000000000000000222, 1.000000000000000000, 1.000000000000000444, 1.000000000000000222, 1.000000000000000444, 1.000000000000000222, 1.000000000000000222, 1.000000000000000444, 1.000000000000000000, 1.000000000000000222, 1.000000000000000444, 1.000000000000000000, 1.000000000000000444, 1.000000000000000222, 1.000000000000000444, 1.000000000000000444, 1.000000000000000222, 1.000000000000000222, 1.000000000000000000, 1.000000000000000444, 1.000000000000000444, 1.000000000000000000, 1.000000000000000444, 1.000000000000000222, 1.000000000000000444, 1.000000000000000444, 1.000000000000000222, 1.000000000000000000, 1.000000000000000444, 1.000000000000000222, 1.000000000000000444, 1.000000000000000000, 1.000000000000000444, 1.000000000000000222, 1.000000000000000222, 1.000000000000000444, 1.000000000000000222, 1.000000000000000222, 1.000000000000000222, 1.000000000000000222, 1.000000000000000444, 1.000000000000000000, 1.000000000000000666, 1.000000000000000000, 1.000000000000000222, 1.000000000000000444, 1.000000000000000000, 1.000000000000000222, 1.000000000000000444, 1.000000000000000000, 1.000000000000000666, 0.9999999999999997780, 1.000000000000000222, 1.000000000000000444, 1.000000000000000000, 1.000000000000000444, 1.000000000000000222, 1.000000000000000444, 1.000000000000000000, 1.000000000000000444, 1.000000000000000222, 1.000000000000000222, 1.000000000000000000, 1.000000000000000444, 1.000000000000000222, 1.000000000000000000, 1.000000000000000222, 1.000000000000000222, 1.000000000000000222, 1.000000000000000444, 1.000000000000000000, 1.000000000000000444, 1.000000000000000222, 1.000000000000000222, 1.000000000000000222, 1.000000000000000000, 1.000000000000000666, 1.000000000000000000, 1.000000000000000000, 1.000000000000000222, 1.000000000000000444, 1.000000000000000222, 1.000000000000000444, 0.9999999999999997780, 1.000000000000000444, 1.000000000000000444, 0.9999999999999997780, 1.000000000000000444, 1.000000000000000444, 1.000000000000000444, 1.000000000000000222, 1.000000000000000444, 1.000000000000000444, 1.000000000000000000, 1.000000000000000444, 0.9999999999999997780, 1.000000000000000444, 0.9999999999999997780, 1.000000000000000444, 1.000000000000000000, 1.000000000000000444, 1.000000000000000444, 1.000000000000000444, 1.000000000000000222, 1.000000000000000444, 1.000000000000000444, 1.000000000000000222, 1.000000000000000222, 1.000000000000000000, 1.000000000000000222, 1.000000000000000444, 0.9999999999999997780, 1.000000000000000666, 0.9999999999999997780, 1.000000000000000444, 1.000000000000000222, 1.000000000000000222, 1.000000000000000000, 1.000000000000000222, 1.000000000000000222, 1.000000000000000000, 1.000000000000000000, 1.000000000000000444, 1.000000000000000222, 1.000000000000000444, 0.9999999999999997780, 1.000000000000000444, 1.000000000000000444, 1.000000000000000222, 1.000000000000000444, 1.000000000000000000, 1.000000000000000444, 1.000000000000000444, 0.9999999999999997780, 1.000000000000000444, 1.000000000000000222, 1.000000000000000444, 1.000000000000000222, 1.000000000000000222, 1.000000000000000444, 1.000000000000000000, 1.000000000000000000, 1.000000000000000444, 1.000000000000000444, 1.000000000000000444, 0.9999999999999997780, 1.000000000000000444, 1.000000000000000222, 1.000000000000000222, 1.000000000000000444, 1.000000000000000000, 1.000000000000000444, 1.000000000000000222, 1.000000000000000444, 1.000000000000000000, 1.000000000000000444, 1.000000000000000444, 1.000000000000000444, 1.000000000000000000, 1.000000000000000444, 1.000000000000000000, 1.000000000000000222, 1.000000000000000444, 1.000000000000000444, 1.000000000000000000, 1.000000000000000444, 1.000000000000000444, 1.000000000000000000, 1.000000000000000444, 1.000000000000000222, 1.000000000000000000, 1.000000000000000444, 1.000000000000000222, 1.000000000000000222, 1.000000000000000444, 1.000000000000000444, 1.000000000000000000, 1.000000000000000000, 1.000000000000000444, 1.000000000000000000, 1.000000000000000222, 1.000000000000000444, 1.000000000000000000, 1.000000000000000222, 1.000000000000000444, 0.9999999999999997780, 1.000000000000000444, 1.000000000000000222, 1.000000000000000000, 1.000000000000000444, 1.000000000000000000, 1.000000000000000444, 1.000000000000000444, 1.000000000000000000, 1.000000000000000222, 1.000000000000000222, 1.000000000000000222, 1.000000000000000444, 1.000000000000000222, 1.000000000000000000, 1.000000000000000222, 1.000000000000000444, 1.000000000000000444, 1.000000000000000222, 1.000000000000000444, 1.000000000000000444, 1.000000000000000000, 1.000000000000000000, 1.000000000000000666, 0.9999999999999997780, 1.000000000000000444, 0.9999999999999997780, 1.000000000000000222, 0.9999999999999997780, 1.000000000000000444, 1.000000000000000000, 1.000000000000000222, 1.000000000000000222, 1.000000000000000444, 1.000000000000000000, 1.000000000000000000, 1.000000000000000444, 1.000000000000000000, 1.000000000000000222, 1.000000000000000222),
 ( 0.3333333333333334259, 0.3333333333333334259, 0.3333333333333334814, 0.3333333333333333703, 0.3333333333333335369, 0.3333333333333335369, 0.3333333333333334259, 0.3333333333333334259, 0.3333333333333334259, 0.3333333333333334814, 0.3333333333333334259, 0.3333333333333334259, 0.3333333333333334259, 0.3333333333333334259, 0.3333333333333333148, 0.3333333333333334259, 0.3333333333333334814, 0.3333333333333333703, 0.3333333333333335369, 0.3333333333333335924, 0.3333333333333334259, 0.3333333333333334814, 0.3333333333333333703, 0.3333333333333334259, 0.3333333333333333703, 0.3333333333333334814, 0.3333333333333333703, 0.3333333333333334259, 0.3333333333333333703, 0.3333333333333333703, 0.3333333333333335369, 0.3333333333333334259, 0.3333333333333333703, 0.3333333333333335924, 0.3333333333333334259, 0.3333333333333334259, 0.3333333333333333703, 0.3333333333333334814, 0.3333333333333333703, 0.3333333333333334814, 0.3333333333333333703, 0.3333333333333335369, 0.3333333333333333148, 0.3333333333333334814, 0.3333333333333333703, 0.3333333333333334814, 0.3333333333333334259, 0.3333333333333333703, 0.3333333333333334259, 0.3333333333333334259, 0.3333333333333334814, 0.3333333333333333703, 0.3333333333333335369, 0.3333333333333334259, 0.3333333333333334259, 0.3333333333333334814, 0.3333333333333334259, 0.3333333333333334259, 0.3333333333333333703, 0.3333333333333333703, 0.3333333333333335924, 0.3333333333333334259, 0.3333333333333335369, 0.3333333333333333703, 0.3333333333333333703, 0.3333333333333333703, 0.3333333333333334814, 0.3333333333333333703, 0.3333333333333335369, 0.3333333333333332593, 0.3333333333333333703, 0.3333333333333334259, 0.3333333333333335369, 0.3333333333333334259, 0.3333333333333333703, 0.3333333333333334814, 0.3333333333333333703, 0.3333333333333335369, 0.3333333333333334259, 0.3333333333333333148, 0.3333333333333334814, 0.3333333333333334814, 0.3333333333333334259, 0.3333333333333333148, 0.3333333333333333703, 0.3333333333333334814, 0.3333333333333333703, 0.3333333333333334814, 0.3333333333333333148, 0.3333333333333334259, 0.3333333333333334814, 0.3333333333333333703, 0.3333333333333335369, 0.3333333333333334814, 0.3333333333333333148, 0.3333333333333335369, 0.3333333333333334814, 0.3333333333333334259, 0.3333333333333334814, 0.3333333333333333703, 0.3333333333333334814, 0.3333333333333334259, 0.3333333333333333703, 0.3333333333333334259, 0.3333333333333335369, 0.3333333333333334259, 0.3333333333333334259, 0.3333333333333334814, 0.3333333333333335369, 0.3333333333333333148, 0.3333333333333334259, 0.3333333333333333148, 0.3333333333333335924, 0.3333333333333334259, 0.3333333333333334814, 0.3333333333333333703, 0.3333333333333334814, 0.3333333333333334259, 0.3333333333333333703, 0.3333333333333335924, 0.3333333333333334259, 0.3333333333333334259, 0.3333333333333333703, 0.3333333333333334259, 0.3333333333333333703, 0.3333333333333333703, 0.3333333333333335369, 0.3333333333333334259, 0.3333333333333333703, 0.3333333333333334814, 0.3333333333333333148, 0.3333333333333335924, 0.3333333333333333148, 0.3333333333333334259, 0.3333333333333333148, 0.3333333333333335924, 0.3333333333333333703, 0.3333333333333335369, 0.3333333333333333148, 0.3333333333333334259, 0.3333333333333334814, 0.3333333333333334259, 0.3333333333333334259, 0.3333333333333334259, 0.3333333333333334259, 0.3333333333333334259, 0.3333333333333334259, 0.3333333333333334814, 0.3333333333333334259, 0.3333333333333333703, 0.3333333333333334814, 0.3333333333333333148, 0.3333333333333334259, 0.3333333333333334814, 0.3333333333333334259, 0.3333333333333333703, 0.3333333333333334259, 0.3333333333333334814, 0.3333333333333333703, 0.3333333333333334259, 0.3333333333333334814, 0.3333333333333333703, 0.3333333333333333703, 0.3333333333333333703, 0.3333333333333335369, 0.3333333333333333703, 0.3333333333333334814, 0.3333333333333334259, 0.3333333333333333703, 0.3333333333333334814, 0.3333333333333333703, 0.3333333333333334259, 0.3333333333333335369, 0.3333333333333333703, 0.3333333333333334259, 0.3333333333333334814, 0.3333333333333334259, 0.3333333333333335924, 0.3333333333333333703, 0.3333333333333334259, 0.3333333333333333148, 0.3333333333333335369, 0.3333333333333334259, 0.3333333333333334259, 0.3333333333333334259, 0.3333333333333333703, 0.3333333333333335369, 0.3333333333333334259, 0.3333333333333333703, 0.3333333333333334259, 0.3333333333333334259, 0.3333333333333333703, 0.3333333333333335369, 0.3333333333333333703, 0.3333333333333335369, 0.3333333333333333703, 0.3333333333333334814, 0.3333333333333334259, 0.3333333333333333703, 0.3333333333333334259, 0.3333333333333333703, 0.3333333333333334814, 0.3333333333333334259, 0.3333333333333333703, 0.3333333333333335369, 0.3333333333333333703, 0.3333333333333333703, 0.3333333333333334814, 0.3333333333333333703, 0.3333333333333333148, 0.3333333333333335924, 0.3333333333333333148, 0.3333333333333335924, 0.3333333333333332593, 0.3333333333333334814, 0.3333333333333334814, 0.3333333333333334259, 0.3333333333333334259, 0.3333333333333334814, 0.3333333333333334259, 0.3333333333333333703, 0.3333333333333335369, 0.3333333333333334259, 0.3333333333333334814, 0.3333333333333333703, 0.3333333333333334259, 0.3333333333333333703, 0.3333333333333334814, 0.3333333333333333703, 0.3333333333333335369, 0.3333333333333333148, 0.3333333333333335924, 0.3333333333333333703, 0.3333333333333334259, 0.3333333333333333703, 0.3333333333333334259, 0.3333333333333333703, 0.3333333333333333703, 0.3333333333333335924, 0.3333333333333334259, 0.3333333333333333148, 0.3333333333333334814, 0.3333333333333335369, 0.3333333333333333703, 0.3333333333333334814, 0.3333333333333333703, 0.3333333333333334259, 0.3333333333333335369, 0.3333333333333333148, 0.3333333333333334814, 0.3333333333333334814, 0.3333333333333333703, 0.3333333333333334259, 0.3333333333333334259, 0.3333333333333335369, 0.3333333333333333148, 0.3333333333333335369, 0.3333333333333333148, 0.3333333333333335369, 0.3333333333333332593, 0.3333333333333335924, 0.3333333333333333148, 0.3333333333333335369, 0.3333333333333335369, 0.3333333333333334814, 0.3333333333333334259, 0.3333333333333334814, 0.3333333333333334814, 0.3333333333333334259, 0.3333333333333334259, 0.3333333333333334259, 0.3333333333333334814, 0.3333333333333334259, 0.3333333333333333703, 0.3333333333333334814, 0.3333333333333333703, 0.3333333333333335369, 0.3333333333333333703, 0.3333333333333334259, 0.3333333333333333148, 0.3333333333333334259, 0.3333333333333334259, 0.3333333333333333703, 0.3333333333333333703, 0.3333333333333335924, 0.3333333333333334259, 0.3333333333333335369, 0.3333333333333333148, 0.3333333333333335369, 0.3333333333333334814, 0.3333333333333334259, 0.3333333333333334814, 0.3333333333333334259, 0.3333333333333333703, 0.3333333333333335369, 0.3333333333333333148, 0.3333333333333335369, 0.3333333333333333703, 0.3333333333333335369, 0.3333333333333333703, 0.3333333333333334814, 0.3333333333333334259, 0.3333333333333333703, 0.3333333333333334259, 0.3333333333333333703, 0.3333333333333335924, 0.3333333333333334259, 0.3333333333333333148, 0.3333333333333334259, 0.3333333333333334259, 0.3333333333333334259, 0.3333333333333335924, 0.3333333333333333703, 0.3333333333333334259, 0.3333333333333334259, 0.3333333333333335369, 0.3333333333333333703, 0.3333333333333334814, 0.3333333333333334814, 0.3333333333333334814, 0.3333333333333333703, 0.3333333333333334814, 0.3333333333333333148, 0.3333333333333335369, 0.3333333333333334259, 0.3333333333333334814, 0.3333333333333333703, 0.3333333333333334259, 0.3333333333333334259, 0.3333333333333334259, 0.3333333333333334259, 0.3333333333333333703, 0.3333333333333333703, 0.3333333333333334814, 0.3333333333333333703, 0.3333333333333334259, 0.3333333333333334814, 0.3333333333333334259, 0.3333333333333334259, 0.3333333333333333703, 0.3333333333333334814, 0.3333333333333333703, 0.3333333333333334259, 0.3333333333333335369, 0.3333333333333333148, 0.3333333333333333703, 0.3333333333333334814, 0.3333333333333333148, 0.3333333333333334259, 0.3333333333333333703, 0.3333333333333333703, 0.3333333333333334814, 0.3333333333333333703, 0.3333333333333334259, 0.3333333333333334814, 0.3333333333333333703, 0.3333333333333334259, 0.3333333333333334259, 0.3333333333333334259, 0.3333333333333335369, 0.3333333333333334259, 0.3333333333333334259, 0.3333333333333333703, 0.3333333333333334259, 0.3333333333333334259, 0.3333333333333334259, 0.3333333333333334814, 0.3333333333333335369, 0.3333333333333333148, 0.3333333333333333703, 0.3333333333333335924, 0.3333333333333333148, 0.3333333333333334259, 0.3333333333333334259, 0.3333333333333333703, 0.3333333333333333148, 0.3333333333333335369, 0.3333333333333334259, 0.3333333333333333703, 0.3333333333333334814, 0.3333333333333334259, 0.3333333333333334259, 0.3333333333333333148, 0.3333333333333335369, 0.3333333333333333703, 0.3333333333333334259, 0.3333333333333334259),
 ( 0.3333333333333334259, 0.3333333333333334259, 0.3333333333333334814, 0.3333333333333333703, 0.3333333333333335369, 0.3333333333333335369, 0.3333333333333334259, 0.3333333333333334259, 0.3333333333333334259, 0.3333333333333334814, 0.3333333333333334259, 0.3333333333333334259, 0.3333333333333334259, 0.3333333333333334259, 0.3333333333333333148, 0.3333333333333334259, 0.3333333333333334814, 0.3333333333333333703, 0.3333333333333335369, 0.3333333333333335924, 0.3333333333333334259, 0.3333333333333334814, 0.3333333333333333703, 0.3333333333333334259, 0.3333333333333333703, 0.3333333333333334814, 0.3333333333333333703, 0.3333333333333334259, 0.3333333333333333703, 0.3333333333333333703, 0.3333333333333335369, 0.3333333333333334259, 0.3333333333333333703, 0.3333333333333335924, 0.3333333333333334259, 0.3333333333333334259, 0.3333333333333333703, 0.3333333333333334814, 0.3333333333333333703, 0.3333333333333334814, 0.3333333333333333703, 0.3333333333333335369, 0.3333333333333333148, 0.3333333333333334814, 0.3333333333333333703, 0.3333333333333334814, 0.3333333333333334259, 0.3333333333333333703, 0.3333333333333334259, 0.3333333333333334259, 0.3333333333333334814, 0.3333333333333333703, 0.3333333333333335369, 0.3333333333333334259, 0.3333333333333334259, 0.3333333333333334814, 0.3333333333333334259, 0.3333333333333334259, 0.3333333333333333703, 0.3333333333333333703, 0.3333333333333335924, 0.3333333333333334259, 0.3333333333333335369, 0.3333333333333333703, 0.3333333333333333703, 0.3333333333333333703, 0.3333333333333334814, 0.3333333333333333703, 0.3333333333333335369, 0.3333333333333332593, 0.3333333333333333703, 0.3333333333333334259, 0.3333333333333335369, 0.3333333333333334259, 0.3333333333333333703, 0.3333333333333334814, 0.3333333333333333703, 0.3333333333333335369, 0.3333333333333334259, 0.3333333333333333148, 0.3333333333333334814, 0.3333333333333334814, 0.3333333333333334259, 0.3333333333333333148, 0.3333333333333333703, 0.3333333333333334814, 0.3333333333333333703, 0.3333333333333334814, 0.3333333333333333148, 0.3333333333333334259, 0.3333333333333334814, 0.3333333333333333703, 0.3333333333333335369, 0.3333333333333334814, 0.3333333333333333148, 0.3333333333333335369, 0.3333333333333334814, 0.3333333333333334259, 0.3333333333333334814, 0.3333333333333333703, 0.3333333333333334814, 0.3333333333333334259, 0.3333333333333333703, 0.3333333333333334259, 0.3333333333333335369, 0.3333333333333334259, 0.3333333333333334259, 0.3333333333333334814, 0.3333333333333335369, 0.3333333333333333148, 0.3333333333333334259, 0.3333333333333333148, 0.3333333333333335924, 0.3333333333333334259, 0.3333333333333334814, 0.3333333333333333703, 0.3333333333333334814, 0.3333333333333334259, 0.3333333333333333703, 0.3333333333333335924, 0.3333333333333334259, 0.3333333333333334259, 0.3333333333333333703, 0.3333333333333334259, 0.3333333333333333703, 0.3333333333333333703, 0.3333333333333335369, 0.3333333333333334259, 0.3333333333333333703, 0.3333333333333334814, 0.3333333333333333148, 0.3333333333333335924, 0.3333333333333333148, 0.3333333333333334259, 0.3333333333333333148, 0.3333333333333335924, 0.3333333333333333703, 0.3333333333333335369, 0.3333333333333333148, 0.3333333333333334259, 0.3333333333333334814, 0.3333333333333334259, 0.3333333333333334259, 0.3333333333333334259, 0.3333333333333334259, 0.3333333333333334259, 0.3333333333333334259, 0.3333333333333334814, 0.3333333333333334259, 0.3333333333333333703, 0.3333333333333334814, 0.3333333333333333148, 0.3333333333333334259, 0.3333333333333334814, 0.3333333333333334259, 0.3333333333333333703, 0.3333333333333334259, 0.3333333333333334814, 0.3333333333333333703, 0.3333333333333334259, 0.3333333333333334814, 0.3333333333333333703, 0.3333333333333333703, 0.3333333333333333703, 0.3333333333333335369, 0.3333333333333333703, 0.3333333333333334814, 0.3333333333333334259, 0.3333333333333333703, 0.3333333333333334814, 0.3333333333333333703, 0.3333333333333334259, 0.3333333333333335369, 0.3333333333333333703, 0.3333333333333334259, 0.3333333333333334814, 0.3333333333333334259, 0.3333333333333335924, 0.3333333333333333703, 0.3333333333333334259, 0.3333333333333333148, 0.3333333333333335369, 0.3333333333333334259, 0.3333333333333334259, 0.3333333333333334259, 0.3333333333333333703, 0.3333333333333335369, 0.3333333333333334259, 0.3333333333333333703, 0.3333333333333334259, 0.3333333333333334259, 0.3333333333333333703, 0.3333333333333335369, 0.3333333333333333703, 0.3333333333333335369, 0.3333333333333333703, 0.3333333333333334814, 0.3333333333333334259, 0.3333333333333333703, 0.3333333333333334259, 0.3333333333333333703, 0.3333333333333334814, 0.3333333333333334259, 0.3333333333333333703, 0.3333333333333335369, 0.3333333333333333703, 0.3333333333333333703, 0.3333333333333334814, 0.3333333333333333703, 0.3333333333333333148, 0.3333333333333335924, 0.3333333333333333148, 0.3333333333333335924, 0.3333333333333332593, 0.3333333333333334814, 0.3333333333333334814, 0.3333333333333334259, 0.3333333333333334259, 0.3333333333333334814, 0.3333333333333334259, 0.3333333333333333703, 0.3333333333333335369, 0.3333333333333334259, 0.3333333333333334814, 0.3333333333333333703, 0.3333333333333334259, 0.3333333333333333703, 0.3333333333333334814, 0.3333333333333333703, 0.3333333333333335369, 0.3333333333333333148, 0.3333333333333335924, 0.3333333333333333703, 0.3333333333333334259, 0.3333333333333333703, 0.3333333333333334259, 0.3333333333333333703, 0.3333333333333333703, 0.3333333333333335924, 0.3333333333333334259, 0.3333333333333333148, 0.3333333333333334814, 0.3333333333333335369, 0.3333333333333333703, 0.3333333333333334814, 0.3333333333333333703, 0.3333333333333334259, 0.3333333333333335369, 0.3333333333333333148, 0.3333333333333334814, 0.3333333333333334814, 0.3333333333333333703, 0.3333333333333334259, 0.3333333333333334259, 0.3333333333333335369, 0.3333333333333333148, 0.3333333333333335369, 0.3333333333333333148, 0.3333333333333335369, 0.3333333333333332593, 0.3333333333333335924, 0.3333333333333333148, 0.3333333333333335369, 0.3333333333333335369, 0.3333333333333334814, 0.3333333333333334259, 0.3333333333333334814, 0.3333333333333334814, 0.3333333333333334259, 0.3333333333333334259, 0.3333333333333334259, 0.3333333333333334814, 0.3333333333333334259, 0.3333333333333333703, 0.3333333333333334814, 0.3333333333333333703, 0.3333333333333335369, 0.3333333333333333703, 0.3333333333333334259, 0.3333333333333333148, 0.3333333333333334259, 0.3333333333333334259, 0.3333333333333333703, 0.3333333333333333703, 0.3333333333333335924, 0.3333333333333334259, 0.3333333333333335369, 0.3333333333333333148, 0.3333333333333335369, 0.3333333333333334814, 0.3333333333333334259, 0.3333333333333334814, 0.3333333333333334259, 0.3333333333333333703, 0.3333333333333335369, 0.3333333333333333148, 0.3333333333333335369, 0.3333333333333333703, 0.3333333333333335369, 0.3333333333333333703, 0.3333333333333334814, 0.3333333333333334259, 0.3333333333333333703, 0.3333333333333334259, 0.3333333333333333703, 0.3333333333333335924, 0.3333333333333334259, 0.3333333333333333148, 0.3333333333333334259, 0.3333333333333334259, 0.3333333333333334259, 0.3333333333333335924, 0.3333333333333333703, 0.3333333333333334259, 0.3333333333333334259, 0.3333333333333335369, 0.3333333333333333703, 0.3333333333333334814, 0.3333333333333334814, 0.3333333333333334814, 0.3333333333333333703, 0.3333333333333334814, 0.3333333333333333148, 0.3333333333333335369, 0.3333333333333334259, 0.3333333333333334814, 0.3333333333333333703, 0.3333333333333334259, 0.3333333333333334259, 0.3333333333333334259, 0.3333333333333334259, 0.3333333333333333703, 0.3333333333333333703, 0.3333333333333334814, 0.3333333333333333703, 0.3333333333333334259, 0.3333333333333334814, 0.3333333333333334259, 0.3333333333333334259, 0.3333333333333333703, 0.3333333333333334814, 0.3333333333333333703, 0.3333333333333334259, 0.3333333333333335369, 0.3333333333333333148, 0.3333333333333333703, 0.3333333333333334814, 0.3333333333333333148, 0.3333333333333334259, 0.3333333333333333703, 0.3333333333333333703, 0.3333333333333334814, 0.3333333333333333703, 0.3333333333333334259, 0.3333333333333334814, 0.3333333333333333703, 0.3333333333333334259, 0.3333333333333334259, 0.3333333333333334259, 0.3333333333333335369, 0.3333333333333334259, 0.3333333333333334259, 0.3333333333333333703, 0.3333333333333334259, 0.3333333333333334259, 0.3333333333333334259, 0.3333333333333334814, 0.3333333333333335369, 0.3333333333333333148, 0.3333333333333333703, 0.3333333333333335924, 0.3333333333333333148, 0.3333333333333334259, 0.3333333333333334259, 0.3333333333333333703, 0.3333333333333333148, 0.3333333333333335369, 0.3333333333333334259, 0.3333333333333333703, 0.3333333333333334814, 0.3333333333333334259, 0.3333333333333334259, 0.3333333333333333148, 0.3333333333333335369, 0.3333333333333333703, 0.3333333333333334259, 0.3333333333333334259),
 ( 1.000000000000000222, 1.000000000000000222, 1.000000000000000222, 1.000000000000000222, 1.000000000000000444, 1.000000000000000444, 1.000000000000000222, 1.000000000000000444, 1.000000000000000222, 1.000000000000000444, 1.000000000000000444, 1.000000000000000000, 1.000000000000000222, 1.000000000000000000, 1.000000000000000222, 1.000000000000000222, 1.000000000000000444, 1.000000000000000000, 1.000000000000000444, 1.000000000000000444, 1.000000000000000222, 1.000000000000000222, 1.000000000000000000, 1.000000000000000222, 1.000000000000000000, 1.000000000000000444, 1.000000000000000000, 1.000000000000000444, 1.000000000000000222, 1.000000000000000000, 1.000000000000000666, 1.000000000000000000, 1.000000000000000222, 1.000000000000000666, 1.000000000000000222, 1.000000000000000444, 1.000000000000000222, 1.000000000000000444, 1.000000000000000000, 1.000000000000000444, 1.000000000000000000, 1.000000000000000444, 1.000000000000000000, 1.000000000000000444, 1.000000000000000000, 1.000000000000000222, 1.000000000000000444, 1.000000000000000000, 1.000000000000000444, 1.000000000000000222, 1.000000000000000222, 1.000000000000000444, 1.000000000000000222, 1.000000000000000444, 1.000000000000000222, 1.000000000000000222, 1.000000000000000444, 1.000000000000000444, 1.000000000000000222, 1.000000000000000222, 1.000000000000000444, 1.000000000000000222, 1.000000000000000444, 1.000000000000000000, 1.000000000000000222, 1.000000000000000222, 1.000000000000000222, 1.000000000000000222, 1.000000000000000444, 1.000000000000000000, 0.9999999999999997780, 1.000000000000000444, 1.000000000000000444, 1.000000000000000222, 1.000000000000000222, 1.000000000000000444, 0.9999999999999997780, 1.000000000000000666, 1.000000000000000000, 1.000000000000000000, 1.000000000000000444, 1.000000000000000222, 1.000000000000000222, 0.9999999999999997780, 1.000000000000000222, 1.000000000000000444, 0.9999999999999997780, 1.000000000000000444, 1.000000000000000000, 1.000000000000000000, 1.000000000000000444, 1.000000000000000000, 1.000000000000000444, 1.000000000000000444, 0.9999999999999997780, 1.000000000000000444, 1.000000000000000444, 1.000000000000000444, 1.000000000000000444, 1.000000000000000000, 1.000000000000000444, 1.000000000000000222, 1.000000000000000000, 1.000000000000000444, 1.000000000000000444, 1.000000000000000222, 1.000000000000000000, 1.000000000000000444, 1.000000000000000444, 1.000000000000000000, 1.000000000000000222, 1.000000000000000000, 1.000000000000000444, 1.000000000000000222, 1.000000000000000444, 1.000000000000000222, 1.000000000000000444, 1.000000000000000444, 1.000000000000000000, 1.000000000000000666, 1.000000000000000222, 1.000000000000000222, 1.000000000000000000, 1.000000000000000222, 1.000000000000000222, 1.000000000000000222, 1.000000000000000444, 1.000000000000000222, 1.000000000000000222, 1.000000000000000444, 0.9999999999999997780, 1.000000000000000666, 0.9999999999999997780, 1.000000000000000222, 1.000000000000000000, 1.000000000000000444, 1.000000000000000000, 1.000000000000000444, 1.000000000000000000, 1.000000000000000222, 1.000000000000000222, 1.000000000000000444, 1.000000000000000444, 1.000000000000000222, 1.000000000000000444, 1.000000000000000444, 1.000000000000000000, 1.000000000000000666, 1.000000000000000222, 1.000000000000000222, 1.000000000000000444, 1.000000000000000000, 1.000000000000000222, 1.000000000000000444, 1.000000000000000000, 1.000000000000000222, 1.000000000000000222, 1.000000000000000444, 1.000000000000000222, 1.000000000000000222, 1.000000000000000444, 1.000000000000000000, 1.000000000000000222, 1.000000000000000000, 1.000000000000000444, 1.000000000000000222, 1.000000000000000444, 1.000000000000000222, 1.000000000000000222, 1.000000000000000444, 1.000000000000000000, 1.000000000000000222, 1.000000000000000444, 1.000000000000000000, 1.000000000000000444, 1.000000000000000222, 1.000000000000000444, 1.000000000000000444, 1.000000000000000222, 1.000000000000000222, 1.000000000000000000, 1.000000000000000444, 1.000000000000000444, 1.000000000000000000, 1.000000000000000444, 1.000000000000000222, 1.000000000000000444, 1.000000000000000444, 1.000000000000000222, 1.000000000000000000, 1.000000000000000444, 1.000000000000000222, 1.000000000000000444, 1.000000000000000000, 1.000000000000000444, 1.000000000000000222, 1.000000000000000222, 1.000000000000000444, 1.000000000000000222, 1.000000000000000222, 1.000000000000000222, 1.000000000000000222, 1.000000000000000444, 1.000000000000000000, 1.000000000000000666, 1.000000000000000000, 1.000000000000000222, 1.000000000000000444, 1.000000000000000000, 1.000000000000000222, 1.000000000000000444, 1.000000000000000000, 1.000000000000000666, 0.9999999999999997780, 1.000000000000000222, 1.000000000000000444, 1.000000000000000000, 1.000000000000000444, 1.000000000000000222, 1.000000000000000444, 1.000000000000000000, 1.000000000000000444, 1.000000000000000222, 1.000000000000000222, 1.000000000000000000, 1.000000000000000444, 1.000000000000000222, 1.000000000000000000, 1.000000000000000222, 1.000000000000000222, 1.000000000000000222, 1.000000000000000444, 1.000000000000000000, 1.000000000000000444, 1.000000000000000222, 1.000000000000000222, 1.000000000000000222, 1.000000000000000000, 1.000000000000000666, 1.000000000000000000, 1.000000000000000000, 1.000000000000000222, 1.000000000000000444, 1.000000000000000222, 1.000000000000000444, 0.9999999999999997780, 1.000000000000000444, 1.000000000000000444, 0.9999999999999997780, 1.000000000000000444, 1.000000000000000444, 1.000000000000000444, 1.000000000000000222, 1.000000000000000444, 1.000000000000000444, 1.000000000000000000, 1.000000000000000444, 0.9999999999999997780, 1.000000000000000444, 0.9999999999999997780, 1.000000000000000444, 1.000000000000000000, 1.000000000000000444, 1.000000000000000444, 1.000000000000000444, 1.000000000000000222, 1.000000000000000444, 1.000000000000000444, 1.000000000000000222, 1.000000000000000222, 1.000000000000000000, 1.000000000000000222, 1.000000000000000444, 0.9999999999999997780, 1.000000000000000666, 0.9999999999999997780, 1.000000000000000444, 1.000000000000000222, 1.000000000000000222, 1.000000000000000000, 1.000000000000000222, 1.000000000000000222, 1.000000000000000000, 1.000000000000000000, 1.000000000000000444, 1.000000000000000222, 1.000000000000000444, 0.9999999999999997780, 1.000000000000000444, 1.000000000000000444, 1.000000000000000222, 1.000000000000000444, 1.000000000000000000, 1.000000000000000444, 1.000000000000000444, 0.9999999999999997780, 1.000000000000000444, 1.000000000000000222, 1.000000000000000444, 1.000000000000000222, 1.000000000000000222, 1.000000000000000444, 1.000000000000000000, 1.000000000000000000, 1.000000000000000444, 1.000000000000000444, 1.000000000000000444, 0.9999999999999997780, 1.000000000000000444, 1.000000000000000222, 1.000000000000000222, 1.000000000000000444, 1.000000000000000000, 1.000000000000000444, 1.000000000000000222, 1.000000000000000444, 1.000000000000000000, 1.000000000000000444, 1.000000000000000444, 1.000000000000000444, 1.000000000000000000, 1.000000000000000444, 1.000000000000000000, 1.000000000000000222, 1.000000000000000444, 1.000000000000000444, 1.000000000000000000, 1.000000000000000444, 1.000000000000000444, 1.000000000000000000, 1.000000000000000444, 1.000000000000000222, 1.000000000000000000, 1.000000000000000444, 1.000000000000000222, 1.000000000000000222, 1.000000000000000444, 1.000000000000000444, 1.000000000000000000, 1.000000000000000000, 1.000000000000000444, 1.000000000000000000, 1.000000000000000222, 1.000000000000000444, 1.000000000000000000, 1.000000000000000222, 1.000000000000000444, 0.9999999999999997780, 1.000000000000000444, 1.000000000000000222, 1.000000000000000000, 1.000000000000000444, 1.000000000000000000, 1.000000000000000444, 1.000000000000000444, 1.000000000000000000, 1.000000000000000222, 1.000000000000000222, 1.000000000000000222, 1.000000000000000444, 1.000000000000000222, 1.000000000000000000, 1.000000000000000222, 1.000000000000000444, 1.000000000000000444, 1.000000000000000222, 1.000000000000000444, 1.000000000000000444, 1.000000000000000000, 1.000000000000000000, 1.000000000000000666, 0.9999999999999997780, 1.000000000000000444, 0.9999999999999997780, 1.000000000000000222, 0.9999999999999997780, 1.000000000000000444, 1.000000000000000000, 1.000000000000000222, 1.000000000000000222, 1.000000000000000444, 1.000000000000000000, 1.000000000000000000, 1.000000000000000444, 1.000000000000000000, 1.000000000000000222, 1.000000000000000222),
 ( 0.3333333333333334259, 0.3333333333333334259, 0.3333333333333334814, 0.3333333333333333703, 0.3333333333333335369, 0.3333333333333335369, 0.3333333333333334259, 0.3333333333333334259, 0.3333333333333334259, 0.3333333333333334814, 0.3333333333333334259, 0.3333333333333334259, 0.3333333333333334259, 0.3333333333333334259, 0.3333333333333333148, 0.3333333333333334259, 0.3333333333333334814, 0.3333333333333333703, 0.3333333333333335369, 0.3333333333333335924, 0.3333333333333334259, 0.3333333333333334814, 0.3333333333333333703, 0.3333333333333334259, 0.3333333333333333703, 0.3333333333333334814, 0.3333333333333333703, 0.3333333333333334259, 0.3333333333333333703, 0.3333333333333333703, 0.3333333333333335369, 0.3333333333333334259, 0.3333333333333333703, 0.3333333333333335924, 0.3333333333333334259, 0.3333333333333334259, 0.3333333333333333703, 0.3333333333333334814, 0.3333333333333333703, 0.3333333333333334814, 0.3333333333333333703, 0.3333333333333335369, 0.3333333333333333148, 0.3333333333333334814, 0.3333333333333333703, 0.3333333333333334814, 0.3333333333333334259, 0.3333333333333333703, 0.3333333333333334259, 0.3333333333333334259, 0.3333333333333334814, 0.3333333333333333703, 0.3333333333333335369, 0.3333333333333334259, 0.3333333333333334259, 0.3333333333333334814, 0.3333333333333334259, 0.3333333333333334259, 0.3333333333333333703, 0.3333333333333333703, 0.3333333333333335924, 0.3333333333333334259, 0.3333333333333335369, 0.3333333333333333703, 0.3333333333333333703, 0.3333333333333333703, 0.3333333333333334814, 0.3333333333333333703, 0.3333333333333335369, 0.3333333333333332593, 0.3333333333333333703, 0.3333333333333334259, 0.3333333333333335369, 0.3333333333333334259, 0.3333333333333333703, 0.3333333333333334814, 0.3333333333333333703, 0.3333333333333335369, 0.3333333333333334259, 0.3333333333333333148, 0.3333333333333334814, 0.3333333333333334814, 0.3333333333333334259, 0.3333333333333333148, 0.3333333333333333703, 0.3333333333333334814, 0.3333333333333333703, 0.3333333333333334814, 0.3333333333333333148, 0.3333333333333334259, 0.3333333333333334814, 0.3333333333333333703, 0.3333333333333335369, 0.3333333333333334814, 0.3333333333333333148, 0.3333333333333335369, 0.3333333333333334814, 0.3333333333333334259, 0.3333333333333334814, 0.3333333333333333703, 0.3333333333333334814, 0.3333333333333334259, 0.3333333333333333703, 0.3333333333333334259, 0.3333333333333335369, 0.3333333333333334259, 0.3333333333333334259, 0.3333333333333334814, 0.3333333333333335369, 0.3333333333333333148, 0.3333333333333334259, 0.3333333333333333148, 0.3333333333333335924, 0.3333333333333334259, 0.3333333333333334814, 0.3333333333333333703, 0.3333333333333334814, 0.3333333333333334259, 0.3333333333333333703, 0.3333333333333335924, 0.3333333333333334259, 0.3333333333333334259, 0.3333333333333333703, 0.3333333333333334259, 0.3333333333333333703, 0.3333333333333333703, 0.3333333333333335369, 0.3333333333333334259, 0.3333333333333333703, 0.3333333333333334814, 0.3333333333333333148, 0.3333333333333335924, 0.3333333333333333148, 0.3333333333333334259, 0.3333333333333333148, 0.3333333333333335924, 0.3333333333333333703, 0.3333333333333335369, 0.3333333333333333148, 0.3333333333333334259, 0.3333333333333334814, 0.3333333333333334259, 0.3333333333333334259, 0.3333333333333334259, 0.3333333333333334259, 0.3333333333333334259, 0.3333333333333334259, 0.3333333333333334814, 0.3333333333333334259, 0.3333333333333333703, 0.3333333333333334814, 0.3333333333333333148, 0.3333333333333334259, 0.3333333333333334814, 0.3333333333333334259, 0.3333333333333333703, 0.3333333333333334259, 0.3333333333333334814, 0.3333333333333333703, 0.3333333333333334259, 0.3333333333333334814, 0.3333333333333333703, 0.3333333333333333703, 0.3333333333333333703, 0.3333333333333335369, 0.3333333333333333703, 0.3333333333333334814, 0.3333333333333334259, 0.3333333333333333703, 0.3333333333333334814, 0.3333333333333333703, 0.3333333333333334259, 0.3333333333333335369, 0.3333333333333333703, 0.3333333333333334259, 0.3333333333333334814, 0.3333333333333334259, 0.3333333333333335924, 0.3333333333333333703, 0.3333333333333334259, 0.3333333333333333148, 0.3333333333333335369, 0.3333333333333334259, 0.3333333333333334259, 0.3333333333333334259, 0.3333333333333333703, 0.3333333333333335369, 0.3333333333333334259, 0.3333333333333333703, 0.3333333333333334259, 0.3333333333333334259, 0.3333333333333333703, 0.3333333333333335369, 0.3333333333333333703, 0.3333333333333335369, 0.3333333333333333703, 0.3333333333333334814, 0.3333333333333334259, 0.3333333333333333703, 0.3333333333333334259, 0.3333333333333333703, 0.3333333333333334814, 0.3333333333333334259, 0.3333333333333333703, 0.3333333333333335369, 0.3333333333333333703, 0.3333333333333333703, 0.3333333333333334814, 0.3333333333333333703, 0.3333333333333333148, 0.3333333333333335924, 0.3333333333333333148, 0.3333333333333335924, 0.3333333333333332593, 0.3333333333333334814, 0.3333333333333334814, 0.3333333333333334259, 0.3333333333333334259, 0.3333333333333334814, 0.3333333333333334259, 0.3333333333333333703, 0.3333333333333335369, 0.3333333333333334259, 0.3333333333333334814, 0.3333333333333333703, 0.3333333333333334259, 0.3333333333333333703, 0.3333333333333334814, 0.3333333333333333703, 0.3333333333333335369, 0.3333333333333333148, 0.3333333333333335924, 0.3333333333333333703, 0.3333333333333334259, 0.3333333333333333703, 0.3333333333333334259, 0.3333333333333333703, 0.3333333333333333703, 0.3333333333333335924, 0.3333333333333334259, 0.3333333333333333148, 0.3333333333333334814, 0.3333333333333335369, 0.3333333333333333703, 0.3333333333333334814, 0.3333333333333333703, 0.3333333333333334259, 0.3333333333333335369, 0.3333333333333333148, 0.3333333333333334814, 0.3333333333333334814, 0.3333333333333333703, 0.3333333333333334259, 0.3333333333333334259, 0.3333333333333335369, 0.3333333333333333148, 0.3333333333333335369, 0.3333333333333333148, 0.3333333333333335369, 0.3333333333333332593, 0.3333333333333335924, 0.3333333333333333148, 0.3333333333333335369, 0.3333333333333335369, 0.3333333333333334814, 0.3333333333333334259, 0.3333333333333334814, 0.3333333333333334814, 0.3333333333333334259, 0.3333333333333334259, 0.3333333333333334259, 0.3333333333333334814, 0.3333333333333334259, 0.3333333333333333703, 0.3333333333333334814, 0.3333333333333333703, 0.3333333333333335369, 0.3333333333333333703, 0.3333333333333334259, 0.3333333333333333148, 0.3333333333333334259, 0.3333333333333334259, 0.3333333333333333703, 0.3333333333333333703, 0.3333333333333335924, 0.3333333333333334259, 0.3333333333333335369, 0.3333333333333333148, 0.3333333333333335369, 0.3333333333333334814, 0.3333333333333334259, 0.3333333333333334814, 0.3333333333333334259, 0.3333333333333333703, 0.3333333333333335369, 0.3333333333333333148, 0.3333333333333335369, 0.3333333333333333703, 0.3333333333333335369, 0.3333333333333333703, 0.3333333333333334814, 0.3333333333333334259, 0.3333333333333333703, 0.3333333333333334259, 0.3333333333333333703, 0.3333333333333335924, 0.3333333333333334259, 0.3333333333333333148, 0.3333333333333334259, 0.3333333333333334259, 0.3333333333333334259, 0.3333333333333335924, 0.3333333333333333703, 0.3333333333333334259, 0.3333333333333334259, 0.3333333333333335369, 0.3333333333333333703, 0.3333333333333334814, 0.3333333333333334814, 0.3333333333333334814, 0.3333333333333333703, 0.3333333333333334814, 0.3333333333333333148, 0.3333333333333335369, 0.3333333333333334259, 0.3333333333333334814, 0.3333333333333333703, 0.3333333333333334259, 0.3333333333333334259, 0.3333333333333334259, 0.3333333333333334259, 0.3333333333333333703, 0.3333333333333333703, 0.3333333333333334814, 0.3333333333333333703, 0.3333333333333334259, 0.3333333333333334814, 0.3333333333333334259, 0.3333333333333334259, 0.3333333333333333703, 0.3333333333333334814, 0.3333333333333333703, 0.3333333333333334259, 0.3333333333333335369, 0.3333333333333333148, 0.3333333333333333703, 0.3333333333333334814, 0.3333333333333333148, 0.3333333333333334259, 0.3333333333333333703, 0.3333333333333333703, 0.3333333333333334814, 0.3333333333333333703, 0.3333333333333334259, 0.3333333333333334814, 0.3333333333333333703, 0.3333333333333334259, 0.3333333333333334259, 0.3333333333333334259, 0.3333333333333335369, 0.3333333333333334259, 0.3333333333333334259, 0.3333333333333333703, 0.3333333333333334259, 0.3333333333333334259, 0.3333333333333334259, 0.3333333333333334814, 0.3333333333333335369, 0.3333333333333333148, 0.3333333333333333703, 0.3333333333333335924, 0.3333333333333333148, 0.3333333333333334259, 0.3333333333333334259, 0.3333333333333333703, 0.3333333333333333148, 0.3333333333333335369, 0.3333333333333334259, 0.3333333333333333703, 0.3333333333333334814, 0.3333333333333334259, 0.3333333333333334259, 0.3333333333333333148, 0.3333333333333335369, 0.3333333333333333703, 0.3333333333333334259, 0.3333333333333334259),
 ( 0.3333333333333334259, 0.3333333333333334259, 0.3333333333333334814, 0.3333333333333333703, 0.3333333333333335369, 0.3333333333333335369, 0.3333333333333334259, 0.3333333333333334259, 0.3333333333333334259, 0.3333333333333334814, 0.3333333333333334259, 0.3333333333333334259, 0.3333333333333334259, 0.3333333333333334259, 0.3333333333333333148, 0.3333333333333334259, 0.3333333333333334814, 0.3333333333333333703, 0.3333333333333335369, 0.3333333333333335924, 0.3333333333333334259, 0.3333333333333334814, 0.3333333333333333703, 0.3333333333333334259, 0.3333333333333333703, 0.3333333333333334814, 0.3333333333333333703, 0.3333333333333334259, 0.3333333333333333703, 0.3333333333333333703, 0.3333333333333335369, 0.3333333333333334259, 0.3333333333333333703, 0.3333333333333335924, 0.3333333333333334259, 0.3333333333333334259, 0.3333333333333333703, 0.3333333333333334814, 0.3333333333333333703, 0.3333333333333334814, 0.3333333333333333703, 0.3333333333333335369, 0.3333333333333333148, 0.3333333333333334814, 0.3333333333333333703, 0.3333333333333334814, 0.3333333333333334259, 0.3333333333333333703, 0.3333333333333334259, 0.3333333333333334259, 0.3333333333333334814, 0.3333333333333333703, 0.3333333333333335369, 0.3333333333333334259, 0.3333333333333334259, 0.3333333333333334814, 0.3333333333333334259, 0.3333333333333334259, 0.3333333333333333703, 0.3333333333333333703, 0.3333333333333335924, 0.3333333333333334259, 0.3333333333333335369, 0.3333333333333333703, 0.3333333333333333703, 0.3333333333333333703, 0.3333333333333334814, 0.3333333333333333703, 0.3333333333333335369, 0.3333333333333332593, 0.3333333333333333703, 0.3333333333333334259, 0.3333333333333335369, 0.3333333333333334259, 0.3333333333333333703, 0.3333333333333334814, 0.3333333333333333703, 0.3333333333333335369, 0.3333333333333334259, 0.3333333333333333148, 0.3333333333333334814, 0.3333333333333334814, 0.3333333333333334259, 0.3333333333333333148, 0.3333333333333333703, 0.3333333333333334814, 0.3333333333333333703, 0.3333333333333334814, 0.3333333333333333148, 0.3333333333333334259, 0.3333333333333334814, 0.3333333333333333703, 0.3333333333333335369, 0.3333333333333334814, 0.3333333333333333148, 0.3333333333333335369, 0.3333333333333334814, 0.3333333333333334259, 0.3333333333333334814, 0.3333333333333333703, 0.3333333333333334814, 0.3333333333333334259, 0.3333333333333333703, 0.3333333333333334259, 0.3333333333333335369, 0.3333333333333334259, 0.3333333333333334259, 0.3333333333333334814, 0.3333333333333335369, 0.3333333333333333148, 0.3333333333333334259, 0.3333333333333333148, 0.3333333333333335924, 0.3333333333333334259, 0.3333333333333334814, 0.3333333333333333703, 0.3333333333333334814, 0.3333333333333334259, 0.3333333333333333703, 0.3333333333333335924, 0.3333333333333334259, 0.3333333333333334259, 0.3333333333333333703, 0.3333333333333334259, 0.3333333333333333703, 0.3333333333333333703, 0.3333333333333335369, 0.3333333333333334259, 0.3333333333333333703, 0.3333333333333334814, 0.3333333333333333148, 0.3333333333333335924, 0.3333333333333333148, 0.3333333333333334259, 0.3333333333333333148, 0.3333333333333335924, 0.3333333333333333703, 0.3333333333333335369, 0.3333333333333333148, 0.3333333333333334259, 0.3333333333333334814, 0.3333333333333334259, 0.3333333333333334259, 0.3333333333333334259, 0.3333333333333334259, 0.3333333333333334259, 0.3333333333333334259, 0.3333333333333334814, 0.3333333333333334259, 0.3333333333333333703, 0.3333333333333334814, 0.3333333333333333148, 0.3333333333333334259, 0.3333333333333334814, 0.3333333333333334259, 0.3333333333333333703, 0.3333333333333334259, 0.3333333333333334814, 0.3333333333333333703, 0.3333333333333334259, 0.3333333333333334814, 0.3333333333333333703, 0.3333333333333333703, 0.3333333333333333703, 0.3333333333333335369, 0.3333333333333333703, 0.3333333333333334814, 0.3333333333333334259, 0.3333333333333333703, 0.3333333333333334814, 0.3333333333333333703, 0.3333333333333334259, 0.3333333333333335369, 0.3333333333333333703, 0.3333333333333334259, 0.3333333333333334814, 0.3333333333333334259, 0.3333333333333335924, 0.3333333333333333703, 0.3333333333333334259, 0.3333333333333333148, 0.3333333333333335369, 0.3333333333333334259, 0.3333333333333334259, 0.3333333333333334259, 0.3333333333333333703, 0.3333333333333335369, 0.3333333333333334259, 0.3333333333333333703, 0.3333333333333334259, 0.3333333333333334259, 0.3333333333333333703, 0.3333333333333335369, 0.3333333333333333703, 0.3333333333333335369, 0.3333333333333333703, 0.3333333333333334814, 0.3333333333333334259, 0.3333333333333333703, 0.3333333333333334259, 0.3333333333333333703, 0.3333333333333334814, 0.3333333333333334259, 0.3333333333333333703, 0.3333333333333335369, 0.3333333333333333703, 0.3333333333333333703, 0.3333333333333334814, 0.3333333333333333703, 0.3333333333333333148, 0.3333333333333335924, 0.3333333333333333148, 0.3333333333333335924, 0.3333333333333332593, 0.3333333333333334814, 0.3333333333333334814, 0.3333333333333334259, 0.3333333333333334259, 0.3333333333333334814, 0.3333333333333334259, 0.3333333333333333703, 0.3333333333333335369, 0.3333333333333334259, 0.3333333333333334814, 0.3333333333333333703, 0.3333333333333334259, 0.3333333333333333703, 0.3333333333333334814, 0.3333333333333333703, 0.3333333333333335369, 0.3333333333333333148, 0.3333333333333335924, 0.3333333333333333703, 0.3333333333333334259, 0.3333333333333333703, 0.3333333333333334259, 0.3333333333333333703, 0.3333333333333333703, 0.3333333333333335924, 0.3333333333333334259, 0.3333333333333333148, 0.3333333333333334814, 0.3333333333333335369, 0.3333333333333333703, 0.3333333333333334814, 0.3333333333333333703, 0.3333333333333334259, 0.3333333333333335369, 0.3333333333333333148, 0.3333333333333334814, 0.3333333333333334814, 0.3333333333333333703, 0.3333333333333334259, 0.3333333333333334259, 0.3333333333333335369, 0.3333333333333333148, 0.3333333333333335369, 0.3333333333333333148, 0.3333333333333335369, 0.3333333333333332593, 0.3333333333333335924, 0.3333333333333333148, 0.3333333333333335369, 0.3333333333333335369, 0.3333333333333334814, 0.3333333333333334259, 0.3333333333333334814, 0.3333333333333334814, 0.3333333333333334259, 0.3333333333333334259, 0.3333333333333334259, 0.3333333333333334814, 0.3333333333333334259, 0.3333333333333333703, 0.3333333333333334814, 0.3333333333333333703, 0.3333333333333335369, 0.3333333333333333703, 0.3333333333333334259, 0.3333333333333333148, 0.3333333333333334259, 0.3333333333333334259, 0.3333333333333333703, 0.3333333333333333703, 0.3333333333333335924, 0.3333333333333334259, 0.3333333333333335369, 0.3333333333333333148, 0.3333333333333335369, 0.3333333333333334814, 0.3333333333333334259, 0.3333333333333334814, 0.3333333333333334259, 0.3333333333333333703, 0.3333333333333335369, 0.3333333333333333148, 0.3333333333333335369, 0.3333333333333333703, 0.3333333333333335369, 0.3333333333333333703, 0.3333333333333334814, 0.3333333333333334259, 0.3333333333333333703, 0.3333333333333334259, 0.3333333333333333703, 0.3333333333333335924, 0.3333333333333334259, 0.3333333333333333148, 0.3333333333333334259, 0.3333333333333334259, 0.3333333333333334259, 0.3333333333333335924, 0.3333333333333333703, 0.3333333333333334259, 0.3333333333333334259, 0.3333333333333335369, 0.3333333333333333703, 0.3333333333333334814, 0.3333333333333334814, 0.3333333333333334814, 0.3333333333333333703, 0.3333333333333334814, 0.3333333333333333148, 0.3333333333333335369, 0.3333333333333334259, 0.3333333333333334814, 0.3333333333333333703, 0.3333333333333334259, 0.3333333333333334259, 0.3333333333333334259, 0.3333333333333334259, 0.3333333333333333703, 0.3333333333333333703, 0.3333333333333334814, 0.3333333333333333703, 0.3333333333333334259, 0.3333333333333334814, 0.3333333333333334259, 0.3333333333333334259, 0.3333333333333333703, 0.3333333333333334814, 0.3333333333333333703, 0.3333333333333334259, 0.3333333333333335369, 0.3333333333333333148, 0.3333333333333333703, 0.3333333333333334814, 0.3333333333333333148, 0.3333333333333334259, 0.3333333333333333703, 0.3333333333333333703, 0.3333333333333334814, 0.3333333333333333703, 0.3333333333333334259, 0.3333333333333334814, 0.3333333333333333703, 0.3333333333333334259, 0.3333333333333334259, 0.3333333333333334259, 0.3333333333333335369, 0.3333333333333334259, 0.3333333333333334259, 0.3333333333333333703, 0.3333333333333334259, 0.3333333333333334259, 0.3333333333333334259, 0.3333333333333334814, 0.3333333333333335369, 0.3333333333333333148, 0.3333333333333333703, 0.3333333333333335924, 0.3333333333333333148, 0.3333333333333334259, 0.3333333333333334259, 0.3333333333333333703, 0.3333333333333333148, 0.3333333333333335369, 0.3333333333333334259, 0.3333333333333333703, 0.3333333333333334814, 0.3333333333333334259, 0.3333333333333334259, 0.3333333333333333148, 0.3333333333333335369, 0.3333333333333333703, 0.3333333333333334259, 0.3333333333333334259),
 ( 1.000000000000000222, 1.000000000000000222, 1.000000000000000222, 1.000000000000000222, 1.000000000000000444, 1.000000000000000444, 1.000000000000000222, 1.000000000000000444, 1.000000000000000222, 1.000000000000000444, 1.000000000000000444, 1.000000000000000000, 1.000000000000000222, 1.000000000000000000, 1.000000000000000222, 1.000000000000000222, 1.000000000000000444, 1.000000000000000000, 1.000000000000000444, 1.000000000000000444, 1.000000000000000222, 1.000000000000000222, 1.000000000000000000, 1.000000000000000222, 1.000000000000000000, 1.000000000000000444, 1.000000000000000000, 1.000000000000000444, 1.000000000000000222, 1.000000000000000000, 1.000000000000000666, 1.000000000000000000, 1.000000000000000222, 1.000000000000000666, 1.000000000000000222, 1.000000000000000444, 1.000000000000000222, 1.000000000000000444, 1.000000000000000000, 1.000000000000000444, 1.000000000000000000, 1.000000000000000444, 1.000000000000000000, 1.000000000000000444, 1.000000000000000000, 1.000000000000000222, 1.000000000000000444, 1.000000000000000000, 1.000000000000000444, 1.000000000000000222, 1.000000000000000222, 1.000000000000000444, 1.000000000000000222, 1.000000000000000444, 1.000000000000000222, 1.000000000000000222, 1.000000000000000444, 1.000000000000000444, 1.000000000000000222, 1.000000000000000222, 1.000000000000000444, 1.000000000000000222, 1.000000000000000444, 1.000000000000000000, 1.000000000000000222, 1.000000000000000222, 1.000000000000000222, 1.000000000000000222, 1.000000000000000444, 1.000000000000000000, 0.9999999999999997780, 1.000000000000000444, 1.000000000000000444, 1.000000000000000222, 1.000000000000000222, 1.000000000000000444, 0.9999999999999997780, 1.000000000000000666, 1.000000000000000000, 1.000000000000000000, 1.000000000000000444, 1.000000000000000222, 1.000000000000000222, 0.9999999999999997780, 1.000000000000000222, 1.000000000000000444, 0.9999999999999997780, 1.000000000000000444, 1.000000000000000000, 1.000000000000000000, 1.000000000000000444, 1.000000000000000000, 1.000000000000000444, 1.000000000000000444, 0.9999999999999997780, 1.000000000000000444, 1.000000000000000444, 1.000000000000000444, 1.000000000000000444, 1.000000000000000000, 1.000000000000000444, 1.000000000000000222, 1.000000000000000000, 1.000000000000000444, 1.000000000000000444, 1.000000000000000222, 1.000000000000000000, 1.000000000000000444, 1.000000000000000444, 1.000000000000000000, 1.000000000000000222, 1.000000000000000000, 1.000000000000000444, 1.000000000000000222, 1.000000000000000444, 1.000000000000000222, 1.000000000000000444, 1.000000000000000444, 1.000000000000000000, 1.000000000000000666, 1.000000000000000222, 1.000000000000000222, 1.000000000000000000, 1.000000000000000222, 1.000000000000000222, 1.000000000000000222, 1.000000000000000444, 1.000000000000000222, 1.000000000000000222, 1.000000000000000444, 0.9999999999999997780, 1.000000000000000666, 0.9999999999999997780, 1.000000000000000222, 1.000000000000000000, 1.000000000000000444, 1.000000000000000000, 1.000000000000000444, 1.000000000000000000, 1.000000000000000222, 1.000000000000000222, 1.000000000000000444, 1.000000000000000444, 1.000000000000000222, 1.000000000000000444, 1.000000000000000444, 1.000000000000000000, 1.000000000000000666, 1.000000000000000222, 1.000000000000000222, 1.000000000000000444, 1.000000000000000000, 1.000000000000000222, 1.000000000000000444, 1.000000000000000000, 1.000000000000000222, 1.000000000000000222, 1.000000000000000444, 1.000000000000000222, 1.000000000000000222, 1.000000000000000444, 1.000000000000000000, 1.000000000000000222, 1.000000000000000000, 1.000000000000000444, 1.000000000000000222, 1.000000000000000444, 1.000000000000000222, 1.000000000000000222, 1.000000000000000444, 1.000000000000000000, 1.000000000000000222, 1.000000000000000444, 1.000000000000000000, 1.000000000000000444, 1.000000000000000222, 1.000000000000000444, 1.000000000000000444, 1.000000000000000222, 1.000000000000000222, 1.000000000000000000, 1.000000000000000444, 1.000000000000000444, 1.000000000000000000, 1.000000000000000444, 1.000000000000000222, 1.000000000000000444, 1.000000000000000444, 1.000000000000000222, 1.000000000000000000, 1.000000000000000444, 1.000000000000000222, 1.000000000000000444, 1.000000000000000000, 1.000000000000000444, 1.000000000000000222, 1.000000000000000222, 1.000000000000000444, 1.000000000000000222, 1.000000000000000222, 1.000000000000000222, 1.000000000000000222, 1.000000000000000444, 1.000000000000000000, 1.000000000000000666, 1.000000000000000000, 1.000000000000000222, 1.000000000000000444, 1.000000000000000000, 1.000000000000000222, 1.000000000000000444, 1.000000000000000000, 1.000000000000000666, 0.9999999999999997780, 1.000000000000000222, 1.000000000000000444, 1.000000000000000000, 1.000000000000000444, 1.000000000000000222, 1.000000000000000444, 1.000000000000000000, 1.000000000000000444, 1.000000000000000222, 1.000000000000000222, 1.000000000000000000, 1.000000000000000444, 1.000000000000000222, 1.000000000000000000, 1.000000000000000222, 1.000000000000000222, 1.000000000000000222, 1.000000000000000444, 1.000000000000000000, 1.000000000000000444, 1.000000000000000222, 1.000000000000000222, 1.000000000000000222, 1.000000000000000000, 1.000000000000000666, 1.000000000000000000, 1.000000000000000000, 1.000000000000000222, 1.000000000000000444, 1.000000000000000222, 1.000000000000000444, 0.9999999999999997780, 1.000000000000000444, 1.000000000000000444, 0.9999999999999997780, 1.000000000000000444, 1.000000000000000444, 1.000000000000000444, 1.000000000000000222, 1.000000000000000444, 1.000000000000000444, 1.000000000000000000, 1.000000000000000444, 0.9999999999999997780, 1.000000000000000444, 0.9999999999999997780, 1.000000000000000444, 1.000000000000000000, 1.000000000000000444, 1.000000000000000444, 1.000000000000000444, 1.000000000000000222, 1.000000000000000444, 1.000000000000000444, 1.000000000000000222, 1.000000000000000222, 1.000000000000000000, 1.000000000000000222, 1.000000000000000444, 0.9999999999999997780, 1.000000000000000666, 0.9999999999999997780, 1.000000000000000444, 1.000000000000000222, 1.000000000000000222, 1.000000000000000000, 1.000000000000000222, 1.000000000000000222, 1.000000000000000000, 1.000000000000000000, 1.000000000000000444, 1.000000000000000222, 1.000000000000000444, 0.9999999999999997780, 1.000000000000000444, 1.000000000000000444, 1.000000000000000222, 1.000000000000000444, 1.000000000000000000, 1.000000000000000444, 1.000000000000000444, 0.9999999999999997780, 1.000000000000000444, 1.000000000000000222, 1.000000000000000444, 1.000000000000000222, 1.000000000000000222, 1.000000000000000444, 1.000000000000000000, 1.000000000000000000, 1.000000000000000444, 1.000000000000000444, 1.000000000000000444, 0.9999999999999997780, 1.000000000000000444, 1.000000000000000222, 1.000000000000000222, 1.000000000000000444, 1.000000000000000000, 1.000000000000000444, 1.000000000000000222, 1.000000000000000444, 1.000000000000000000, 1.000000000000000444, 1.000000000000000444, 1.000000000000000444, 1.000000000000000000, 1.000000000000000444, 1.000000000000000000, 1.000000000000000222, 1.000000000000000444, 1.000000000000000444, 1.000000000000000000, 1.000000000000000444, 1.000000000000000444, 1.000000000000000000, 1.000000000000000444, 1.000000000000000222, 1.000000000000000000, 1.000000000000000444, 1.000000000000000222, 1.000000000000000222, 1.000000000000000444, 1.000000000000000444, 1.000000000000000000, 1.000000000000000000, 1.000000000000000444, 1.000000000000000000, 1.000000000000000222, 1.000000000000000444, 1.000000000000000000, 1.000000000000000222, 1.000000000000000444, 0.9999999999999997780, 1.000000000000000444, 1.000000000000000222, 1.000000000000000000, 1.000000000000000444, 1.000000000000000000, 1.000000000000000444, 1.000000000000000444, 1.000000000000000000, 1.000000000000000222, 1.000000000000000222, 1.000000000000000222, 1.000000000000000444, 1.000000000000000222, 1.000000000000000000, 1.000000000000000222, 1.000000000000000444, 1.000000000000000444, 1.000000000000000222, 1.000000000000000444, 1.000000000000000444, 1.000000000000000000, 1.000000000000000000, 1.000000000000000666, 0.9999999999999997780, 1.000000000000000444, 0.9999999999999997780, 1.000000000000000222, 0.9999999999999997780, 1.000000000000000444, 1.000000000000000000, 1.000000000000000222, 1.000000000000000222, 1.000000000000000444, 1.000000000000000000, 1.000000000000000000, 1.000000000000000444, 1.000000000000000000, 1.000000000000000222, 1.000000000000000222) ) ) 
 REPRESENTATION_ITEM ( '' )  SURFACE ( )  );
#51155=CARTESIAN_POINT ( 'NONE',  ( 4.055163089163640322, -1.574157218682000758, 0.8962264629079966793 ) ) ;
#51159=CARTESIAN_POINT ( 'NONE',  ( 5.356058406599743194, 0.7285399314688314476, -1.658701577940960847 ) ) ;
#51165=CARTESIAN_POINT ( 'NONE',  ( 6.021894344906984387, 1.833355594513026876, -0.3188260975769128813 ) ) ;
#51167=CARTESIAN_POINT ( 'NONE',  ( 4.042530882030176187, -1.416877165883747125, 1.289359272694647451 ) ) ;
#51173=CARTESIAN_POINT ( 'NONE',  ( 0.6905621207787122628, -2.145541755201633372, -0.2633910710312590275 ) ) ;
#51176=CARTESIAN_POINT ( 'NONE',  ( 0.4108170757193031486, 1.585627777896590151, 0.9046078287104839522 ) ) ;
#51178=CARTESIAN_POINT ( 'NONE',  ( 3.153144192703428939, -1.491587519860730460, -1.052284964708279258 ) ) ;
#51180=CARTESIAN_POINT ( 'NONE',  ( 1.687617486097678476, 1.829050272730630144, -0.5582976189952293389 ) ) ;
#51182=CARTESIAN_POINT ( 'NONE',  ( 2.945709429406599966, 1.390870048597905084, 1.394762357610879855 ) ) ;
#51183=CARTESIAN_POINT ( 'NONE',  ( 5.161643714676827699, 0.9607356898342777063, 1.687723941809249117 ) ) ;
#51186=CARTESIAN_POINT ( 'NONE',  ( 3.674183785563363447, 2.104178206457421485, -0.2630699042918820396 ) ) ;
#51193=CIRCLE ( 'NONE', #172263, 0.04999999999999969746 ) ;
#51198=CARTESIAN_POINT ( 'NONE',  ( 4.512205841073367196, -0.7830535718562798841, -1.649371741558727678 ) ) ;
#51203=CARTESIAN_POINT ( 'NONE',  ( 5.541831131927607679, 0.7570117910807551143, -1.710825945835430462 ) ) ;
#51212=CARTESIAN_POINT ( 'NONE',  ( 0.4618902312403838639, -0.5555351291045197426, 1.994226918997483500 ) ) ;
#51213=CARTESIAN_POINT ( 'NONE',  ( 0.6677574575255783573, 1.425215384571768551, 1.565850431965072787 ) ) ;
#51216=CARTESIAN_POINT ( 'NONE',  ( 5.840704046183605946, -2.018525344099521668, -0.4591754850708437696 ) ) ;
#51217=CARTESIAN_POINT ( 'NONE',  ( 1.944624168438695566, -1.479605912621816621, -1.095697124569312564 ) ) ;
#51222=CARTESIAN_POINT ( 'NONE',  ( 1.306998621393583138, 2.023524796797530723, 1.076953482639223747 ) ) ;
#51227=CARTESIAN_POINT ( 'NONE',  ( 0.8967405870976161708, -1.965081358092489516, -0.4369277762777488139 ) ) ;
#51228=CARTESIAN_POINT ( 'NONE',  ( 0.7780835697005837881, -1.044612314895682292, -1.660310580060719188 ) ) ;
#51229=CARTESIAN_POINT ( 'NONE',  ( 6.503150282362620160, -0.1410805869419759218, 1.984311032119711715 ) ) ;
#51233=CARTESIAN_POINT ( 'NONE',  ( 3.486350522754261494, -0.4081323730865527577, -2.050228346494194831 ) ) ;
#51234=CARTESIAN_POINT ( 'NONE',  ( 1.867668082833298993, 0.9064309091474114233, 1.519949287764200685 ) ) ;
#51237=CARTESIAN_POINT ( 'NONE',  ( 4.945436657225622312, 0.7223393070586077158, -2.175551854680431330 ) ) ;
#51238=CARTESIAN_POINT ( 'NONE',  ( 3.679424820307465538, -0.8558964687110992564, 1.515225693578539978 ) ) ;
#51241=CARTESIAN_POINT ( 'NONE',  ( 3.497127502780640107, 1.691016411901521854, 0.3820211100199251697 ) ) ;
#51242=CARTESIAN_POINT ( 'NONE',  ( 3.033805354627703288, 2.062495667156949430, -0.6785788507157832772 ) ) ;
#51244=CARTESIAN_POINT ( 'NONE',  ( 4.382046175016578005, -2.016188710442788246, -0.04465648322755921829 ) ) ;
#51245=CARTESIAN_POINT ( 'NONE',  ( 1.031250000000000888, -0.7852924748300426083, -1.895863743164066584 ) ) ;
#51248=CARTESIAN_POINT ( 'NONE',  ( 1.905176762840081528, 1.600281962709374062, 1.072135106281972616 ) ) ;
#51250=CARTESIAN_POINT ( 'NONE',  ( 5.502238596801645620, -0.9988962762179309784, 1.984187878789472892 ) ) ;
#51252=CARTESIAN_POINT ( 'NONE',  ( -0.1108833634136767443, 0.0002062650063822807356, -1.896853557917008271 ) ) ;
#51258=CARTESIAN_POINT ( 'NONE',  ( 1.348599501924132804, 1.090831829848055046, -1.934932191954039427 ) ) ;
#51259=CARTESIAN_POINT ( 'NONE',  ( 6.848121815800094936, -0.8396676627679277027, 1.771385694100804598 ) ) ;
#51262=CARTESIAN_POINT ( 'NONE',  ( 6.679017863784723730, -0.1010099541198590523, -2.260277599329813647 ) ) ;
#51265=CARTESIAN_POINT ( 'NONE',  ( -0.1224325501351306023, -0.4448023855274513272, -1.973852191825019364 ) ) ;
#51266=CARTESIAN_POINT ( 'NONE',  ( 4.334473715658632820, -1.190102281996632261, 1.684540188307581010 ) ) ;
#51270=CARTESIAN_POINT ( 'NONE',  ( 6.362560269511371658, -1.322780316340057549, 1.322825847358683138 ) ) ;
#51271=CARTESIAN_POINT ( 'NONE',  ( 4.500456895562253479, -1.699381082468238713, 0.3444616058281315119 ) ) ;
#51272=CARTESIAN_POINT ( 'NONE',  ( 4.563825558218141509, -1.132311722701891510, 1.321849635945840706 ) ) ;
#51274=CARTESIAN_POINT ( 'NONE',  ( 2.015536172832455897, -2.222481616396556170, 0.5612588729206613447 ) ) ;
#51276=CARTESIAN_POINT ( 'NONE',  ( 5.987849877204276083, -2.080749957983673681, -0.2039560948884494573 ) ) ;
#51277=CARTESIAN_POINT ( 'NONE',  ( 6.386669098100576036, 1.688287130807873293, -0.9594923298414399504 ) ) ;
#51280=CARTESIAN_POINT ( 'NONE',  ( 1.477185633673218534, -2.006960102380969779, -0.1948397147320118372 ) ) ;
#51281=CARTESIAN_POINT ( 'NONE',  ( 0.5510472016944796270, -1.853416330350022179, -1.169031858332982177 ) ) ;
#51285=CARTESIAN_POINT ( 'NONE',  ( 3.334745777049468618, 1.343786929377327466, -1.640352557257473309 ) ) ;
#51287=CARTESIAN_POINT ( 'NONE',  ( 5.391160240453525709, 1.608232483172780558, -0.8641324296934371763 ) ) ;
#51294=CARTESIAN_POINT ( 'NONE',  ( 2.830336888193147882, -0.9990820879247277464, -1.755331475833141308 ) ) ;
#51295=CARTESIAN_POINT ( 'NONE',  ( 6.352570083819033542, 0.6862697483850827007, 2.097430819677794656 ) ) ;
#51297=CARTESIAN_POINT ( 'NONE',  ( 3.537814430808595922, 1.177328839734363308, 1.441218929277183536 ) ) ;
#51306=CARTESIAN_POINT ( 'NONE',  ( 1.897353599431324866, 0.1640088499204050976, 1.726041979094733447 ) ) ;
#51307=CARTESIAN_POINT ( 'NONE',  ( 1.042430265417312985, -1.369658564370433540, -1.073568199598630146 ) ) ;
#51308=CARTESIAN_POINT ( 'NONE',  ( 6.656845493208900955, -1.788705722188275837, 1.457663220358196732 ) ) ;
#51311=CARTESIAN_POINT ( 'NONE',  ( 0.9310180319365793933, 0.1487380178207615700, 2.055447871051790720 ) ) ;
#51313=CARTESIAN_POINT ( 'NONE',  ( 6.556073970538053075, 2.004588421764907036, -1.124284452974108950 ) ) ;
#51316=CARTESIAN_POINT ( 'NONE',  ( 6.807498166657679484, -0.4075194142965676836, 1.832415718333743282 ) ) ;
#51317=CARTESIAN_POINT ( 'NONE',  ( 4.675980034926481288, 1.890745994642643479, -0.2862527531290667837 ) ) ;
#51319=CARTESIAN_POINT ( 'NONE',  ( 6.076841795016812320, -2.094286673724785164, -0.6961510500591641115 ) ) ;
#51324=CARTESIAN_POINT ( 'NONE',  ( 0.4166731193052671256, -0.6827031231213858131, -1.900913249881502232 ) ) ;
#51326=CARTESIAN_POINT ( 'NONE',  ( 3.909432592967517550, 1.977442543354444249, 1.189201670975383429 ) ) ;
#51327=CARTESIAN_POINT ( 'NONE',  ( 5.125427350195786325, 0.1941421753944693185, -1.952251141935714696 ) ) ;
#51329=CARTESIAN_POINT ( 'NONE',  ( 0.5144084716053355377, 0.7454083195421266073, 1.814826383214888983 ) ) ;
#51333=CARTESIAN_POINT ( 'NONE',  ( 0.1634790396850393235, 1.973143002845114458, -0.7684359545688070892 ) ) ;
#51338=CARTESIAN_POINT ( 'NONE',  ( 3.977515510703835133, -0.1653560672004051324, 2.164858251032927061 ) ) ;
#51340=CARTESIAN_POINT ( 'NONE',  ( 1.406653384705614629, -2.110883996484512970, -0.2024971186788473154 ) ) ;
#51347=CARTESIAN_POINT ( 'NONE',  ( 2.565760370094140264, 2.021647365152558606, -0.3987750144259157858 ) ) ;
#51351=CARTESIAN_POINT ( 'NONE',  ( 0.07775346131143417994, 7.629137130509094256, -2.888902737517151209 ) ) ;
#51355=CARTESIAN_POINT ( 'NONE',  ( 4.916621234345090130, -0.6478637630910142331, -1.799314785492410529 ) ) ;
#51357=CARTESIAN_POINT ( 'NONE',  ( 1.388340239569575640, -1.017395381511316810, 2.020837998375684563 ) ) ;
#51359=CARTESIAN_POINT ( 'NONE',  ( 1.775370306292364031, 0.3070917902865456517, -1.785173024263370101 ) ) ;
#51360=CARTESIAN_POINT ( 'NONE',  ( 1.340887447446635017, -1.644988140609974225, -0.9815275998622545739 ) ) ;
#51362=CARTESIAN_POINT ( 'NONE',  ( 1.715371797147913435, -1.774658612622433296, -1.066089629202723765 ) ) ;
#51364=CARTESIAN_POINT ( 'NONE',  ( 0.3562423511419475775, 0.7522458758148011793, 1.822497947957350428 ) ) ;
#51365=CARTESIAN_POINT ( 'NONE',  ( 6.024042007596412063, -1.072333998858214343, -1.600281699052849893 ) ) ;
#51366=CARTESIAN_POINT ( 'NONE',  ( 6.481111342790009999, -0.1036386110354891726, -2.204582208980155222 ) ) ;
#51369=CARTESIAN_POINT ( 'NONE',  ( 4.756332342268011715, -2.062141065897259207, -0.05393103437261077132 ) ) ;
#51374=CARTESIAN_POINT ( 'NONE',  ( 4.788165231579453618, -0.9949995658048852443, 1.856088619770781989 ) ) ;
#51376=CARTESIAN_POINT ( 'NONE',  ( 0.6257148180217129152, 0.2125798311119214690, -2.160765367999056608 ) ) ;
#51378=CARTESIAN_POINT ( 'NONE',  ( 4.938837616837212785, 0.3641351946921667082, 2.130543054529559832 ) ) ;
#51379=CARTESIAN_POINT ( 'NONE',  ( 5.953772690328709594, -1.464304757327790973, -1.391265315224277099 ) ) ;
#51387=CARTESIAN_POINT ( 'NONE',  ( 3.661342437515973547, 1.897110692972364454, -0.6839366698164971448 ) ) ;
#51391=CARTESIAN_POINT ( 'NONE',  ( 5.190363053866647647, -2.144918610114197488, -0.2683968819863768451 ) ) ;
#51393=SURFACE_SIDE_STYLE ('',( #98030 ) ) ;
#51396=CARTESIAN_POINT ( 'NONE',  ( 5.554314605481814660, -1.277030258849481736, 1.560512323070535112 ) ) ;
#51398=CARTESIAN_POINT ( 'NONE',  ( 1.084105852307458040, -1.681943224540465964, -0.3816912691657590728 ) ) ;
#51403=CARTESIAN_POINT ( 'NONE',  ( 5.712129104542990277, -0.8404194184173617854, -1.671158263034502767 ) ) ;
#51404=CARTESIAN_POINT ( 'NONE',  ( 5.959245303985257536, -1.698412939339728700, 1.080668751846917797 ) ) ;
#51409=CARTESIAN_POINT ( 'NONE',  ( 2.455864667332839257, -1.573010975769023601, -1.422207447652395373 ) ) ;
#51410=CARTESIAN_POINT ( 'NONE',  ( 1.792592436991577109, 1.492242793082170227, -1.356315429364700176 ) ) ;
#51411=CARTESIAN_POINT ( 'NONE',  ( 1.300706311995255771, -0.2675212335121620599, -1.791602419159578519 ) ) ;
#51413=CARTESIAN_POINT ( 'NONE',  ( 5.893488898593548520, 1.633865717575968546, 1.415524914074948404 ) ) ;
#51416=CARTESIAN_POINT ( 'NONE',  ( 0.5849901852424718163, 1.567898511244028459, 1.100480585720535087 ) ) ;
#51424=CARTESIAN_POINT ( 'NONE',  ( 4.768767694835816862, -0.2516295123269947642, -2.000731945836851544 ) ) ;
#51425=CARTESIAN_POINT ( 'NONE',  ( 4.645497774645743760, -1.668943667408796294, -1.373881373981879817 ) ) ;
#51428=CARTESIAN_POINT ( 'NONE',  ( 1.723052270212792836, 1.567896913533245229, -1.427966198690698851 ) ) ;
#51430=CARTESIAN_POINT ( 'NONE',  ( 3.796128654474308028, -1.968949637145664955, -0.1001596523246932047 ) ) ;
#51431=CARTESIAN_POINT ( 'NONE',  ( 4.412309042748480792, -1.912102599942141268, -0.04143165621695726192 ) ) ;
#51434=CARTESIAN_POINT ( 'NONE',  ( 5.846149472147661896, -0.8869723270901458401, 1.758618239599341937 ) ) ;
#51435=CARTESIAN_POINT ( 'NONE',  ( 1.464679669172624488, 0.1433081720705318696, -1.936712990118959032 ) ) ;
#51443=CARTESIAN_POINT ( 'NONE',  ( 6.340485057729076779, 1.096952271789692901, -1.566184530335120950 ) ) ;
#51445=CARTESIAN_POINT ( 'NONE',  ( 3.246891520140795517, 0.5363302883765566076, 2.140594385818309409 ) ) ;
#51446=CARTESIAN_POINT ( 'NONE',  ( 2.257103711190447282, -1.706036888594957723, 1.399758388914617013 ) ) ;
#51448=CARTESIAN_POINT ( 'NONE',  ( 0.9438406676962156627, -1.213610516764839664, -1.477797202995428938 ) ) ;
#51451=CARTESIAN_POINT ( 'NONE',  ( 2.893098739488662030, 0.2508700648995808025, 2.055025655848155886 ) ) ;
#51455=CARTESIAN_POINT ( 'NONE',  ( 1.815512348505427642, -0.2646426633909418347, 2.145385951886819242 ) ) ;
#51456=CARTESIAN_POINT ( 'NONE',  ( 4.089532599075940134, -0.8378280566024614018, 2.025282237563410526 ) ) ;
#51462=CARTESIAN_POINT ( 'NONE',  ( 5.555191991570319843, -1.093772777934084894, 1.345723482730563525 ) ) ;
#51464=CARTESIAN_POINT ( 'NONE',  ( 3.942288228968212849, -1.024710522258945655, 1.798826465557185506 ) ) ;
#51465=CARTESIAN_POINT ( 'NONE',  ( 4.306348207420813701, 1.301105652591315387, -1.670210365991892987 ) ) ;
#51468=CARTESIAN_POINT ( 'NONE',  ( 2.658990959838656742, 1.584636853462956685, -1.169278883008363135 ) ) ;
#51469=CARTESIAN_POINT ( 'NONE',  ( 1.248149539447914735, 0.9399939672071171426, -1.665319807275446706 ) ) ;
#51470=CARTESIAN_POINT ( 'NONE',  ( 4.312625044126452423, 2.094834666918590216, 0.9310453638207391025 ) ) ;
#51471=CARTESIAN_POINT ( 'NONE',  ( 3.070728972534173096, -1.687097908962056803, -0.6982200720766564839 ) ) ;
#51478=CARTESIAN_POINT ( 'NONE',  ( 3.498294685330126441, -0.9886941555459362041, 1.753605845479579095 ) ) ;
#51479=CARTESIAN_POINT ( 'NONE',  ( 4.047668389856577065, 1.417901948909123799, 1.355967163993692992 ) ) ;
#51482=CARTESIAN_POINT ( 'NONE',  ( 0.1751657365761521701, 0.7240325161481726557, -2.128694924679303213 ) ) ;
#51483=CARTESIAN_POINT ( 'NONE',  ( 0.6266517258138035729, 0.1575598857218879489, 2.084883927750030175 ) ) ;
#51484=CARTESIAN_POINT ( 'NONE',  ( 5.190226478415982392, -1.756784752911320302, -0.2140884780794347908 ) ) ;
#51486=CARTESIAN_POINT ( 'NONE',  ( 2.256057974219495499, 0.9384471748680022207, 1.980482673072603284 ) ) ;
#51487=CARTESIAN_POINT ( 'NONE',  ( 0.2920125592734872932, 1.448600077496174476, -0.9643754397266665057 ) ) ;
#51490=CARTESIAN_POINT ( 'NONE',  ( 0.2335667940003021970, 4.085521407782252368, -2.708192491817535075 ) ) ;
#51491=CARTESIAN_POINT ( 'NONE',  ( 0.1875851866701295223, -0.8181552731707610882, 1.518483014795414032 ) ) ;
#51492=CARTESIAN_POINT ( 'NONE',  ( 0.6795420635867071013, 1.475991390215245058, 1.620154534501851096 ) ) ;
#51493=CARTESIAN_POINT ( 'NONE',  ( 2.877765823869771644, 2.095344539500657799, -0.6929138170133213315 ) ) ;
#51494=CARTESIAN_POINT ( 'NONE',  ( 6.795391773274086944, -1.942485666075419060, 0.9701230550103381312 ) ) ;
#51496=CARTESIAN_POINT ( 'NONE',  ( 2.325544253341553347, -1.572509993196508971, -1.418087145738779808 ) ) ;
#51498=CARTESIAN_POINT ( 'NONE',  ( 5.209954918934378121, -1.917094737882633959, 0.1888984193934347133 ) ) ;
#51501=CARTESIAN_POINT ( 'NONE',  ( 1.998001414424467104, -2.291734237260790952, 0.06083037064899367297 ) ) ;
#51506=CARTESIAN_POINT ( 'NONE',  ( 4.336746411289113645, 1.366526421497065824, -1.751164563135388041 ) ) ;
#51513=CARTESIAN_POINT ( 'NONE',  ( 2.918592439375994552, -1.356299846568160827, -1.492255409411530120 ) ) ;
#51515=CARTESIAN_POINT ( 'NONE',  ( 0.5146022356567416800, 0.7859572577839054608, 1.907140732884365697 ) ) ;
#51520=CARTESIAN_POINT ( 'NONE',  ( 4.277398745584213735, 1.430588233724191083, 1.660156109410643177 ) ) ;
#51521=CARTESIAN_POINT ( 'NONE',  ( 1.863907939170056149, -0.1017519224979606118, -2.013985838549677609 ) ) ;
#51522=CARTESIAN_POINT ( 'NONE',  ( 1.206327419354651820, 1.623952629372883427, 0.8676893986077349741 ) ) ;
#51523=CARTESIAN_POINT ( 'NONE',  ( 4.775077868145559457, 2.139425163340304525, -0.8237163094031977328 ) ) ;
#51524=CARTESIAN_POINT ( 'NONE',  ( 3.591602706507342369, -1.839109287420921834, -0.08896477992388628075 ) ) ;
#51526=CARTESIAN_POINT ( 'NONE',  ( 2.375000000000001776, 2.052068128417950277, -1.362642298365709419E-13 ) ) ;
#51528=CARTESIAN_POINT ( 'NONE',  ( 4.172732250082421324, -1.703408510751417193, -0.6570589383413026896 ) ) ;
#51529=CARTESIAN_POINT ( 'NONE',  ( 5.432267593368638181, -1.591316862017605471, -1.238322901282742805 ) ) ;
#51531=CARTESIAN_POINT ( 'NONE',  ( 5.067353023127458833, 0.2270735253321141400, -2.251102950005756220 ) ) ;
#51533=CARTESIAN_POINT ( 'NONE',  ( 0.1179828827667589730, -2.064941173381201978, 0.4132506003948192563 ) ) ;
#51535=CARTESIAN_POINT ( 'NONE',  ( 3.279797552538410876, -1.996039814156633785, 0.5495672325947635883 ) ) ;
#51540=CARTESIAN_POINT ( 'NONE',  ( 1.857912668630396169, 1.921361403365331677, -0.1415498456752254663 ) ) ;
#51543=CARTESIAN_POINT ( 'NONE',  ( 0.1683113222354900018, -0.8393015767643360325, -1.780324559216818425 ) ) ;
#51547=CARTESIAN_POINT ( 'NONE',  ( 0.6156802735862785259, 1.737094954450137285, 1.216079458918501333 ) ) ;
#51548=CARTESIAN_POINT ( 'NONE',  ( 1.863841412593499003, -1.787636906239049805, -1.318573911375673369 ) ) ;
#51549=CARTESIAN_POINT ( 'NONE',  ( 3.012826026228847098, 1.526343371991075948, -1.451234828553144673 ) ) ;
#51552=CARTESIAN_POINT ( 'NONE',  ( 0.6427239283240515633, -0.2220358882154548907, -1.847681390136299839 ) ) ;
#51559=CARTESIAN_POINT ( 'NONE',  ( 1.002369745560643510, -0.9483682245385971488, 1.896766750748935415 ) ) ;
#51562=CARTESIAN_POINT ( 'NONE',  ( 4.721123852359588646, -1.751549048416237486, -0.8839179009662299080 ) ) ;
#51563=CARTESIAN_POINT ( 'NONE',  ( 3.784175263432405956, -1.067420458145739826, 1.879713924940962677 ) ) ;
#51564=CARTESIAN_POINT ( 'NONE',  ( 2.155570461979210428, 0.7887370375637430264, 1.663910549085621415 ) ) ;
#51567=CARTESIAN_POINT ( 'NONE',  ( 4.189205958701418986, -0.6631863921694808317, 1.609220651327713414 ) ) ;
#51571=CARTESIAN_POINT ( 'NONE',  ( 2.413140945657660907, 1.930630709398067246, 0.9725960170764782475 ) ) ;
#51572=CARTESIAN_POINT ( 'NONE',  ( 3.075545897833771747, 1.462222457232667416, -1.388272539953112839 ) ) ;
#51575=CARTESIAN_POINT ( 'NONE',  ( 0.9542513359644848592, 2.159166806557303531, -0.1069676271590186134 ) ) ;
#51576=CARTESIAN_POINT ( 'NONE',  ( 3.362146542844654196, 0.8852860682435258477, 1.761578244261922332 ) ) ;
#51577=CARTESIAN_POINT ( 'NONE',  ( 6.609000000000038177, 0.002801690667396730672, 2.000160786441218530 ) ) ;
#51578=CARTESIAN_POINT ( 'NONE',  ( 3.087376005906359744, -0.7846555324184587565, 1.776656735299622980 ) ) ;
#51588=CARTESIAN_POINT ( 'NONE',  ( 0.3763673390903346516, 1.272619870141003418, 1.802674353332263335 ) ) ;
#51591=CARTESIAN_POINT ( 'NONE',  ( 4.821123798404616245, -1.750560105953799184, -0.8856655065374097191 ) ) ;
#51592=CARTESIAN_POINT ( 'NONE',  ( 1.547500230860882287, -1.423960469535384465, 1.427938386157491246 ) ) ;
#51593=ORIENTED_EDGE ( 'NONE', *, *, #120271, .F. ) ;
#51594=CARTESIAN_POINT ( 'NONE',  ( 3.679011075472499392, 1.786488794941149871, -1.136238802782759238 ) ) ;
#51598=CARTESIAN_POINT ( 'NONE',  ( 2.730204174461122069, 0.2256132759956077649, 1.827196471909063202 ) ) ;
#51602=CARTESIAN_POINT ( 'NONE',  ( 4.799148092389167175, -0.2621723519393297508, -2.104289960152181393 ) ) ;
#51605=CARTESIAN_POINT ( 'NONE',  ( 5.079397637315079983, 1.924335792300538861, -0.7379084467255945246 ) ) ;
#51608=CARTESIAN_POINT ( 'NONE',  ( 0.7482324461028444507, -1.846328264857381996, -0.2332022352751206007 ) ) ;
#51609=CARTESIAN_POINT ( 'NONE',  ( 2.735704033801298785, 1.827604811068459956, 0.2230458208379028362 ) ) ;
#51614=CARTESIAN_POINT ( 'NONE',  ( 2.561379550486083012, -1.920685204893451292, -1.086737900330703166 ) ) ;
#51615=CARTESIAN_POINT ( 'NONE',  ( 4.341306091576823789, -1.971171287362062818, 1.110239852968941232 ) ) ;
#51617=CARTESIAN_POINT ( 'NONE',  ( 4.623216614435611937, 1.579690555364177351, 0.8866180403494609008 ) ) ;
#51618=CARTESIAN_POINT ( 'NONE',  ( 4.839036869973236676, -1.621808105726432414, -1.019334933273335242 ) ) ;
#51620=CARTESIAN_POINT ( 'NONE',  ( 4.364113771024707766, 0.9285358673545366370, 1.739096546318192882 ) ) ;
#51621=CARTESIAN_POINT ( 'NONE',  ( 5.313307075269409374, -0.2735208697075517947, 1.850433306854900817 ) ) ;
#51623=CARTESIAN_POINT ( 'NONE',  ( 5.353892109531869004, -0.6699537489362316078, 1.736457084658560079 ) ) ;
#51625=CARTESIAN_POINT ( 'NONE',  ( 0.5500180045474002410, 0.9981291480291035745, 1.752136972055001518 ) ) ;
#51627=CARTESIAN_POINT ( 'NONE',  ( 1.313257463657933055, 1.858222661572891621, 0.9912184023134795741 ) ) ;
#51631=CARTESIAN_POINT ( 'NONE',  ( 3.357788437482766675, -1.608272433257527556, -1.382313803475518244 ) ) ;
#51633=CARTESIAN_POINT ( 'NONE',  ( 2.162373415809074828, 2.019440163517810749, 0.04526320522070524655 ) ) ;
#51636=CARTESIAN_POINT ( 'NONE',  ( 6.720655732516660485, 7.629137130509104914, 2.326260288887294969 ) ) ;
#51639=CARTESIAN_POINT ( 'NONE',  ( 2.073706595668877384, 2.069181010895416950, -0.6253580070983978390 ) ) ;
#51640=CARTESIAN_POINT ( 'NONE',  ( 6.609999999999973674, 0.5530568637619069916, 2.330679033986877258 ) ) ;
#51648=CARTESIAN_POINT ( 'NONE',  ( 0.6268464039562298140, 0.1668571106153530770, 2.185281662807083691 ) ) ;
#51650=CARTESIAN_POINT ( 'NONE',  ( 1.288340396327339432, -1.015645312862264227, 2.021827887327799722 ) ) ;
#51658=CARTESIAN_POINT ( 'NONE',  ( 4.459404883141235842, 0.3742951803532655330, -1.683599696842478677 ) ) ;
#51660=CARTESIAN_POINT ( 'NONE',  ( 2.038023431533928509, 1.749628755847471018, 0.2652362932685590757 ) ) ;
#51661=CARTESIAN_POINT ( 'NONE',  ( 4.911249081476436018, 1.917979745144289261, 1.091307337132418454 ) ) ;
#51664=CARTESIAN_POINT ( 'NONE',  ( 4.482678814652188315, -1.316266026504675057, 1.532109124154117596 ) ) ;
#51666=CARTESIAN_POINT ( 'NONE',  ( 5.448842280278080707, -1.824126957265741256, -0.8596167168879662590 ) ) ;
#51669=CARTESIAN_POINT ( 'NONE',  ( 2.184254540302111636, -1.834043650784190405, -0.3674020703766099905 ) ) ;
#51672=CARTESIAN_POINT ( 'NONE',  ( 1.775505761281343631, 0.3235837346332003372, -1.884644527778083001 ) ) ;
#51677=CARTESIAN_POINT ( 'NONE',  ( 0.2110004604562870645, 1.588762659912812403, -1.064147093309028680 ) ) ;
#51679=CARTESIAN_POINT ( 'NONE',  ( 1.381223342121252085, -0.05156877537583307025, 1.961363007973878858 ) ) ;
#51680=CARTESIAN_POINT ( 'NONE',  ( 0.1399997263886003374, 0.002789056014650820314, -1.999853399661279063 ) ) ;
#51682=CARTESIAN_POINT ( 'NONE',  ( 5.344028447597857223, -1.346983732444573256, -1.637812552581649594 ) ) ;
#51685=CARTESIAN_POINT ( 'NONE',  ( 0.2802489257003986656, -1.812731005579379051, -0.4610361243657657981 ) ) ;
#51687=CARTESIAN_POINT ( 'NONE',  ( 1.740491373288379995, 1.155656410672186496, -1.648304894270665510 ) ) ;
#51690=CARTESIAN_POINT ( 'NONE',  ( 1.493934562436026292, -2.100767169153750391, 0.2631679424494152153 ) ) ;
#51692=CARTESIAN_POINT ( 'NONE',  ( 3.139188941651628539, -0.1496422021231707811, -2.064996656166856237 ) ) ;
#51696=CARTESIAN_POINT ( 'NONE',  ( 5.208965158259858619, -0.3072975092734456237, 2.067794563079519143 ) ) ;
#51698=CARTESIAN_POINT ( 'NONE',  ( 3.241029684393876842, -1.610631872634618933, 0.8593927405577477252 ) ) ;
#51699=CARTESIAN_POINT ( 'NONE',  ( 2.719172733320520674, 1.531317187073286901, 0.9673847807401686483 ) ) ;
#51703=CARTESIAN_POINT ( 'NONE',  ( 5.508869005905306260, 1.674340917344345536, -1.437622030140395912 ) ) ;
#51706=CARTESIAN_POINT ( 'NONE',  ( 4.090413894173472009, -1.098427525215146749, 1.565146720495188104 ) ) ;
#51711=B_SPLINE_CURVE_WITH_KNOTS ( 'NONE', 3,
 ( #57882, #173799, #106689, #124044, #125109, #174865, #104512, #41661, #58951, #108839 ),
 .UNSPECIFIED., .F., .F.,
 ( 4, 1, 1, 1, 1, 1, 1, 4 ),
 ( 0.000000000000000000, 0.09373397616858752945, 0.1863105892815605236, 0.2574079725677296260, 0.3612190813870841954, 0.5208938042821120717, 0.7336009914826546741, 1.000000000000000000 ),
 .UNSPECIFIED. ) ;
#51718=CARTESIAN_POINT ( 'NONE',  ( 3.479631686803522417, 1.184185218286455621, 1.448006030947253331 ) ) ;
#51722=CARTESIAN_POINT ( 'NONE',  ( 0.3562224712859492493, -1.968894089644295686, -0.05400687454796929826 ) ) ;
#51723=CARTESIAN_POINT ( 'NONE',  ( 2.829704019156009220, 0.7231233381281775285, -1.882481713119791067 ) ) ;
#51727=CARTESIAN_POINT ( 'NONE',  ( 2.308753661914957345, 1.958203289975643191, 0.9839491227633669901 ) ) ;
#51734=CARTESIAN_POINT ( 'NONE',  ( 3.544333174469185721, -1.503253232081468216, 1.062929765333266108 ) ) ;
#51735=CARTESIAN_POINT ( 'NONE',  ( 0.5396978354115729015, -1.910900059352708125, 0.6334021227705748380 ) ) ;
#51736=CARTESIAN_POINT ( 'NONE',  ( 3.462589497157672724, 1.809959297682335100, 1.416443637550690804 ) ) ;
#51738=CARTESIAN_POINT ( 'NONE',  ( 1.076741303291447460, 1.716668495539741324, 0.7189669686299257068 ) ) ;
#51742=CARTESIAN_POINT ( 'NONE',  ( 5.045129621168108258, 0.1466893748028277877, 1.906852434080000824 ) ) ;
#51746=CARTESIAN_POINT ( 'NONE',  ( 4.071883345936186060, -1.202257327942996445, 1.710302118368298707 ) ) ;
#51747=CARTESIAN_POINT ( 'NONE',  ( 2.430351462470367707, 1.813921419787648315, 0.4566771774890953095 ) ) ;
#51750=CARTESIAN_POINT ( 'NONE',  ( 2.841039829263870775, 0.6241981022326682504, -1.624847995071764917 ) ) ;
#51755=CARTESIAN_POINT ( 'NONE',  ( 4.072648179469573471, -1.610461668677556801, -0.6182406629154230115 ) ) ;
#51758=CARTESIAN_POINT ( 'NONE',  ( 6.111994396789379280, -2.190734547077430872, 0.2660306753756238041 ) ) ;
#51761=CARTESIAN_POINT ( 'NONE',  ( 4.065408448962204879, 1.859168595270783042, 1.121007083124803572 ) ) ;
#51762=CARTESIAN_POINT ( 'NONE',  ( 1.998415063578623085, -0.4859047700337820741, -1.759764234465097221 ) ) ;
#51764=CARTESIAN_POINT ( 'NONE',  ( 5.137957784024314911, 2.114781318005181099, -0.1070058694263714694 ) ) ;
#51766=CARTESIAN_POINT ( 'NONE',  ( 5.390252792638895230, -0.5542908586613685129, -2.224220739628431254 ) ) ;
#51770=CARTESIAN_POINT ( 'NONE',  ( 1.770341816056511863, 2.114587264445011883, -0.1591180397043714667 ) ) ;
#51776=CARTESIAN_POINT ( 'NONE',  ( 6.438351068470751670, -1.168633322568404243, 1.829565972870864865 ) ) ;
#51779=CARTESIAN_POINT ( 'NONE',  ( 1.172868535947855673, 0.9048325283492463234, 2.028842389263245227 ) ) ;
#51780=EDGE_LOOP ( 'NONE', ( #179641, #126856, #72963, #923 ) ) ;
#51781=CARTESIAN_POINT ( 'NONE',  ( 6.363907750917786821, -0.1017471579566435469, -2.013986097687201049 ) ) ;
#51783=CARTESIAN_POINT ( 'NONE',  ( 4.662968416576672048, 1.597784760895196721, -1.304382716673627707 ) ) ;
#51789=CARTESIAN_POINT ( 'NONE',  ( 0.1290073198303761104, -1.910558061381230521, 0.8492679875119947264 ) ) ;
#51790=CARTESIAN_POINT ( 'NONE',  ( 4.852185490356213826, 0.1948433276699329531, -2.006959737079899497 ) ) ;
#51791=CARTESIAN_POINT ( 'NONE',  ( 4.581507094455529838, -0.8636776874328588871, 1.626104626046148249 ) ) ;
#51793=CARTESIAN_POINT ( 'NONE',  ( 0.6040130627208201153, -0.5744563726430768069, -1.626443300898507305 ) ) ;
#51794=CARTESIAN_POINT ( 'NONE',  ( 0.3566581422463632189, -1.900417414521380133, -0.6748426577906709856 ) ) ;
#51795=CARTESIAN_POINT ( 'NONE',  ( 0.4230186368967851496, -1.631317381931682631, -1.619748931356496113 ) ) ;
#51797=CARTESIAN_POINT ( 'NONE',  ( 1.634417699101225585, 1.115656568974830343, -1.968152581808318757 ) ) ;
#51798=CARTESIAN_POINT ( 'NONE',  ( 3.528042858452341335, -1.254676591636105121, -1.691379958841844111 ) ) ;
#51802=CARTESIAN_POINT ( 'NONE',  ( 6.562500042754934704, -1.451030237095789266, -1.451031289060847440 ) ) ;
#51807=CARTESIAN_POINT ( 'NONE',  ( 4.869482922584397855, -1.877140712267670430, -1.187567259214457271 ) ) ;
#51808=CARTESIAN_POINT ( 'NONE',  ( 3.468858241077877214, 0.05382521638562161315, -2.190950023606648145 ) ) ;
#51811=CARTESIAN_POINT ( 'NONE',  ( 5.353941776413853937, -0.7077614321437855072, 1.829919609802006741 ) ) ;
#51815=CARTESIAN_POINT ( 'NONE',  ( 4.447591161967184625, -1.937652164471121763, 0.8620916771790232414 ) ) ;
#51819=CARTESIAN_POINT ( 'NONE',  ( 6.825078400183575589, -0.005632053428735600553, 2.144262460745151255 ) ) ;
#51821=CARTESIAN_POINT ( 'NONE',  ( 4.581507094455529838, -0.8636776874328588871, 1.626104626046148249 ) ) ;
#51824=CARTESIAN_POINT ( 'NONE',  ( 0.6963323360776455528, 1.421588922443246084, 1.003805163531448441 ) ) ;
#51828=CARTESIAN_POINT ( 'NONE',  ( 5.664953204072169513, -1.952404353424816774, -0.9282482345986733385 ) ) ;
#51831=CARTESIAN_POINT ( 'NONE',  ( 4.891577088959510711, 1.599438101461609918, 1.454397306527709155 ) ) ;
#51833=CARTESIAN_POINT ( 'NONE',  ( 6.432890565879505473, 0.1910017811236862373, 1.962057160394870881 ) ) ;
#51834=CARTESIAN_POINT ( 'NONE',  ( 4.569544190834089470, 1.339882265830975694, -1.100422448201631820 ) ) ;
#51835=CARTESIAN_POINT ( 'NONE',  ( 1.822082775007987543, 1.258534617508931586, -1.793986466278547853 ) ) ;
#51836=CARTESIAN_POINT ( 'NONE',  ( 2.731810774274369802, -2.153386645068070759, 0.8298372035008163561 ) ) ;
#51837=CARTESIAN_POINT ( 'NONE',  ( 5.026665581557772100, 1.970771621317930045, 0.6023086073758465719 ) ) ;
#51838=CARTESIAN_POINT ( 'NONE',  ( 0.2166051034824221788, -0.09641855276349860226, 1.939669501089319015 ) ) ;
#51843=CARTESIAN_POINT ( 'NONE',  ( 1.652970434142877920, 1.038994816082598804, 1.728001345923817267 ) ) ;
#51845=CARTESIAN_POINT ( 'NONE',  ( 3.258999418838660400, -1.672185875938383859, 1.440126295696932068 ) ) ;
#51847=CARTESIAN_POINT ( 'NONE',  ( 1.973285428892736171, -0.2338459910692871346, 1.846151439588203935 ) ) ;
#51852=CARTESIAN_POINT ( 'NONE',  ( 6.925078400183582339, 6.034855204486058611, 2.639235227498262670 ) ) ;
#51855=CARTESIAN_POINT ( 'NONE',  ( 3.502855024581267518, 1.625569291660882598, -1.266701038991333572 ) ) ;
#51858=CARTESIAN_POINT ( 'NONE',  ( 2.420574729456357765, -0.7750317791199374806, -1.865254733019072297 ) ) ;
#51861=CARTESIAN_POINT ( 'NONE',  ( 2.114203836804037007, -0.9703286663178596338, -1.818149309968750016 ) ) ;
#51866=CARTESIAN_POINT ( 'NONE',  ( -0.2411972340276282434, 2.878796387150697633, -2.389097370654146513 ) ) ;
#51867=CARTESIAN_POINT ( 'NONE',  ( 5.162800556355915838, -1.600310254184673431, 1.519886962452212664 ) ) ;
#51869=CARTESIAN_POINT ( 'NONE',  ( 1.194844697948213463, -0.5240009448631496314, -2.097013730318515456 ) ) ;
#51871=CARTESIAN_POINT ( 'NONE',  ( 1.692592581891849912, 1.490968054865527304, -1.357870634957742961 ) ) ;
#51872=CARTESIAN_POINT ( 'NONE',  ( 1.898275044819753621, 0.2256094754716081452, 2.287263704067198145 ) ) ;
#51876=CARTESIAN_POINT ( 'NONE',  ( 1.867826558377215118, 0.9591755677602131769, 1.605880698980370225 ) ) ;
#51877=CARTESIAN_POINT ( 'NONE',  ( 3.591030000661588062, 1.731995077137841843, 1.032480907900306111 ) ) ;
#51881=CARTESIAN_POINT ( 'NONE',  ( 4.881522348829672175, 1.965384978258335247, -0.7572991678025364770 ) ) ;
#51885=CARTESIAN_POINT ( 'NONE',  ( 5.379167904621746210, -1.827783419154908273, -0.8597544005511729148 ) ) ;
#51887=CARTESIAN_POINT ( 'NONE',  ( 1.059521212928912881, 1.683986000210126788, 1.190688086201870499 ) ) ;
#51895=CARTESIAN_POINT ( 'NONE',  ( 3.525983582677540085, 2.118976886349494659, -0.4726038967238275212 ) ) ;
#51898=CARTESIAN_POINT ( 'NONE',  ( 2.436835438956724165, -1.365703447793526371, -1.235134912642745775 ) ) ;
#51901=CARTESIAN_POINT ( 'NONE',  ( 4.001666433686186686, -2.185622478633037602, 0.1623105178310546570 ) ) ;
#51903=CARTESIAN_POINT ( 'NONE',  ( 4.944316486460487603, 2.256077187801101669, 0.1715336590100754455 ) ) ;
#51909=CARTESIAN_POINT ( 'NONE',  ( 6.380137019068807369, -0.9445444496645590826, 1.496399839161892897 ) ) ;
#51910=CARTESIAN_POINT ( 'NONE',  ( 3.897138702661524956, -0.1997049427340416294, -2.003176435020975088 ) ) ;
#51912=CARTESIAN_POINT ( 'NONE',  ( 3.399542317941701253, 1.658995184361473196, 1.297097526815289115 ) ) ;
#51913=CARTESIAN_POINT ( 'NONE',  ( 0.6322731411384452382, 0.5572298914768618605, 1.832739050869176101 ) ) ;
#51916=CARTESIAN_POINT ( 'NONE',  ( 2.119528921591812498, 0.3396393280722594388, -1.939881811770089115 ) ) ;
#51917=CARTESIAN_POINT ( 'NONE',  ( 4.939715878566554252, -1.916525930768823383, 0.6376727893300809802 ) ) ;
#51918=CARTESIAN_POINT ( 'NONE',  ( 0.8658264364783776479, 0.9185255527898968930, 1.629538061279064642 ) ) ;
#51919=CARTESIAN_POINT ( 'NONE',  ( 1.346068015636435522, -0.8851805579040676886, 1.750911360861057142 ) ) ;
#51920=CARTESIAN_POINT ( 'NONE',  ( 0.7031954830387620037, 1.685401770928725007, -0.9037484838233383888 ) ) ;
#51924=CARTESIAN_POINT ( 'NONE',  ( 5.401189721097995111, 1.529905263132097071, 1.076157610686766075 ) ) ;
#51926=CARTESIAN_POINT ( 'NONE',  ( 5.225469540725330653, 0.2083811790645866135, -2.059773418507819365 ) ) ;
#51937=CARTESIAN_POINT ( 'NONE',  ( 5.582460749670235423, 1.169929261559121247, -1.574690175210855747 ) ) ;
#51939=CARTESIAN_POINT ( 'NONE',  ( 2.671249783466634220, -0.7690017779844946499, -1.863883771055181660 ) ) ;
#51940=CARTESIAN_POINT ( 'NONE',  ( 1.973720722908858249, -0.8152147109428582450, 1.733722481544483163 ) ) ;
#51942=CARTESIAN_POINT ( 'NONE',  ( -0.1232117409455633916, -0.1621322592461546530, -2.156395338765437764 ) ) ;
#51945=CARTESIAN_POINT ( 'NONE',  ( 3.602682612693074660, 1.476495159181415939, -1.148357684351591912 ) ) ;
#51950=CARTESIAN_POINT ( 'NONE',  ( 3.989952538763715140, -2.111419002029162328, 0.1578513319024783257 ) ) ;
#51952=CARTESIAN_POINT ( 'NONE',  ( 5.547352688424546763, 1.827615396715172258, -0.9727077141251788683 ) ) ;
#51953=CARTESIAN_POINT ( 'NONE',  ( 2.806283438348840420, 1.512464495701435929, -1.443730951476623670 ) ) ;
#51954=CARTESIAN_POINT ( 'NONE',  ( 6.620655732516655512, 0.5568428858156619921, 2.325336003765938742 ) ) ;
#51955=CARTESIAN_POINT ( 'NONE',  ( 0.5336903687956630060, 0.8928529924820073349, -1.475541649381803433 ) ) ;
#51964=CARTESIAN_POINT ( 'NONE',  ( 0.5920784091685951100, -1.007499442088593211, 1.505216462368397234 ) ) ;
#51973=CARTESIAN_POINT ( 'NONE',  ( 6.556263154800559434, -1.238474754573845038, 1.591913907798309991 ) ) ;
#51974=CARTESIAN_POINT ( 'NONE',  ( 0.6277789859737945566, -0.3070864893036719945, 2.098006834332386994 ) ) ;
#51980=CARTESIAN_POINT ( 'NONE',  ( 3.397268178914572889, -1.739110600408208196, 0.9241587964883835049 ) ) ;
#51981=CARTESIAN_POINT ( 'NONE',  ( 1.928540351845555056, -1.002238520345886785, -1.868699319572619366 ) ) ;
#51984=CARTESIAN_POINT ( 'NONE',  ( 6.883263157960374912, 7.629137130509066722, 2.546189081643289942 ) ) ;
#51985=CARTESIAN_POINT ( 'NONE',  ( 5.876942531769460132, 2.026063101133714461, -0.8356547683932225024 ) ) ;
#51987=CARTESIAN_POINT ( 'NONE',  ( 4.383760159432283032, 1.257691660000469058, 1.459273733648867699 ) ) ;
#51989=CARTESIAN_POINT ( 'NONE',  ( -0.02968770228137588424, 5.725071598255107475, -2.420367217772397606 ) ) ;
#51990=CARTESIAN_POINT ( 'NONE',  ( 1.067327838873022516, -1.996528553209110379, -0.9406146916221403975 ) ) ;
#51993=CARTESIAN_POINT ( 'NONE',  ( 6.104353324094977218, 1.967046249225043342, 0.1001853051637753428 ) ) ;
#51994=CARTESIAN_POINT ( 'NONE',  ( 0.7494335824394976475, 1.939781244166354002, -0.09678450214786055161 ) ) ;
#51995=CARTESIAN_POINT ( 'NONE',  ( 6.134147193249257946, 0.1786779444946043904, -2.291516319396588397 ) ) ;
#51997=CARTESIAN_POINT ( 'NONE',  ( 4.733164070488131259, 0.002922519798398153738, -1.861131630917359336 ) ) ;
#52003=CARTESIAN_POINT ( 'NONE',  ( 0.06437606466144081552, -1.426665095847098330, 1.663708609037084951 ) ) ;
#52008=CARTESIAN_POINT ( 'NONE',  ( 1.066719475142905216, -1.649486405746130258, -0.7827983987617056494 ) ) ;
#52010=CARTESIAN_POINT ( 'NONE',  ( 2.021687164805381354, -1.548805232022354650, 0.7802212711869142003 ) ) ;
#52014=CARTESIAN_POINT ( 'NONE',  ( 6.498675964634617941, -0.4922777150685350156, -1.758009983081544991 ) ) ;
#52015=CARTESIAN_POINT ( 'NONE',  ( 3.414850490325722632, -1.488543670003230845, 1.277929504599809585 ) ) ;
#52020=CARTESIAN_POINT ( 'NONE',  ( 5.074906250706387567, -1.535530725987072298, 1.462626433913247093 ) ) ;
#52023=CARTESIAN_POINT ( 'NONE',  ( 2.905202624773518316, -1.723727875341171778, 1.146311801414557241 ) ) ;
#52026=CARTESIAN_POINT ( 'NONE',  ( 5.074942145771424329, -1.609735135204511280, 1.530878986171863687 ) ) ;
#52028=CARTESIAN_POINT ( 'NONE',  ( 2.743178873131403961, 2.287300171779807378, -0.2288005476599272447 ) ) ;
#52035=CARTESIAN_POINT ( 'NONE',  ( 3.920094060441734030, -1.906919942518231936, 0.1457910263855527466 ) ) ;
#52037=CARTESIAN_POINT ( 'NONE',  ( 4.137519252912919221, -1.190027120290118257, -1.248710780074323567 ) ) ;
#52038=CARTESIAN_POINT ( 'NONE',  ( 3.573454097414618946, 1.463926983822515293, 1.387100322000796027 ) ) ;
#52039=CARTESIAN_POINT ( 'NONE',  ( 4.518391418568163509, -2.101855750862766659, 0.9310765106353561249 ) ) ;
#52041=CARTESIAN_POINT ( 'NONE',  ( 6.270163029207718175, 1.081028068854476665, 1.807315287263556280 ) ) ;
#52044=CARTESIAN_POINT ( 'NONE',  ( 4.903428802837151324, -0.4723676116331463892, 1.705421244663980263 ) ) ;
#52046=CARTESIAN_POINT ( 'NONE',  ( 2.273717984289443717, 1.411852697042052185, 1.805783550510152935 ) ) ;
#52047=CARTESIAN_POINT ( 'NONE',  ( 0.2513753182956691146, 0.6612109069651134208, 1.610038921780505339 ) ) ;
#52052=CARTESIAN_POINT ( 'NONE',  ( 0.5554291532160166023, 1.804893407318912901, -1.206520995182088329 ) ) ;
#52053=CARTESIAN_POINT ( 'NONE',  ( 1.551970632248239612, 1.040795554343958429, 1.727062486439542965 ) ) ;
#52055=CARTESIAN_POINT ( 'NONE',  ( 4.986905038743431717, -0.2377927182869009337, -1.911709049817163164 ) ) ;
#52057=CARTESIAN_POINT ( 'NONE',  ( 2.145073868429191677, 2.156049884074415779, 0.5345358195362903686 ) ) ;
#52066=CARTESIAN_POINT ( 'NONE',  ( 3.860698480431251411, 0.2083224649859614919, -1.727840645513075923 ) ) ;
#52067=CARTESIAN_POINT ( 'NONE',  ( 2.137090596337941406, -0.09316805448006217072, -1.959763546484971197 ) ) ;
#52071=CARTESIAN_POINT ( 'NONE',  ( 1.047418773927465629, 1.819938098697634343, -0.9707658663142370026 ) ) ;
#52074=CARTESIAN_POINT ( 'NONE',  ( 1.675094374204841419, -2.148779999652763895, -0.7084808733194192243 ) ) ;
#52078=CARTESIAN_POINT ( 'NONE',  ( 2.811613793402362393, -1.850737340378521223, 0.2705540153197931730 ) ) ;
#52079=CARTESIAN_POINT ( 'NONE',  ( 1.160356219728400307, 1.032376606561947741, 1.393149478428891364 ) ) ;
#52080=CARTESIAN_POINT ( 'NONE',  ( 4.898067072109578035, -0.7382639882421681010, -2.063579870930781546 ) ) ;
#52081=CARTESIAN_POINT ( 'NONE',  ( 5.192513718098597408, -2.289403112372697890, -0.2887273360754892826 ) ) ;
#52082=CARTESIAN_POINT ( 'NONE',  ( 1.393510596882661989, 1.559873972335079184, 1.346953478171313057 ) ) ;
#52083=CARTESIAN_POINT ( 'NONE',  ( 3.767467431601259076, 1.079656630588815780, 1.613968600252370322 ) ) ;
#52085=CARTESIAN_POINT ( 'NONE',  ( 5.923093557443567470, -0.04637014295935314168, 1.870147476527424635 ) ) ;
#52087=CARTESIAN_POINT ( 'NONE',  ( 0.4207071466195873022, 0.6554624660736629860, 1.605403739708724631 ) ) ;
#52090=CARTESIAN_POINT ( 'NONE',  ( 4.957657809308734898, -1.899617967926207740, -0.6767155953601932117 ) ) ;
#52094=CARTESIAN_POINT ( 'NONE',  ( 2.508196354075361789, -0.6984789837382252564, -1.686990664346368796 ) ) ;
#52103=CARTESIAN_POINT ( 'NONE',  ( 5.654946514622759324, 0.3960909877551482827, 1.980269227310478275 ) ) ;
#52104=CARTESIAN_POINT ( 'NONE',  ( 6.639320575229294086, -0.003630812595115453199, 2.203388474976493594 ) ) ;
#52110=CARTESIAN_POINT ( 'NONE',  ( 4.786040499707863383, -0.9732044846940243188, 1.816634495032407814 ) ) ;
#52111=CARTESIAN_POINT ( 'NONE',  ( 5.660779783930850684, 1.203351582566011047, 1.617819807990819481 ) ) ;
#52119=CARTESIAN_POINT ( 'NONE',  ( 4.604842190751081255, 0.8645911521153251122, -1.821463593394745395 ) ) ;
#52120=CARTESIAN_POINT ( 'NONE',  ( 3.995923475689294513, -0.5793754966058572986, -1.747668199984537152 ) ) ;
#52121=CARTESIAN_POINT ( 'NONE',  ( -0.02319159430947368913, 6.948789054712430691, -2.406029888528108618 ) ) ;
#52122=CARTESIAN_POINT ( 'NONE',  ( 1.805729983942544026, 1.920404770136320716, 1.279379207282659969 ) ) ;
#52124=CARTESIAN_POINT ( 'NONE',  ( 5.325516461952285674, -2.054413220456321909, 0.6725034809518318779 ) ) ;
#52126=CARTESIAN_POINT ( 'NONE',  ( 0.4505971019186795212, -1.641227270844529018, -1.037965677199135017 ) ) ;
#52131=CARTESIAN_POINT ( 'NONE',  ( 3.854256360616271415, 0.6726810918341770140, 1.745705178215435582 ) ) ;
#52134=CARTESIAN_POINT ( 'NONE',  ( 1.295869073816724226, 1.673045085319382119, 1.439284050222865652 ) ) ;
#52139=CARTESIAN_POINT ( 'NONE',  ( 0.2277241186354854174, -1.209499947282626220, -1.557479245376863330 ) ) ;
#52140=CARTESIAN_POINT ( 'NONE',  ( 6.340458270854060885, 2.281561288062480486, 0.3456012654466412704 ) ) ;
#52141=CARTESIAN_POINT ( 'NONE',  ( 1.047228354049560828, 1.731870006261830630, -0.9216698261682305660 ) ) ;
#52142=CARTESIAN_POINT ( 'NONE',  ( 4.100476343641854093, 2.052162271747024924, 0.2072667206600986300 ) ) ;
#52150=CARTESIAN_POINT ( 'NONE',  ( 6.566846207931698487, 1.613421326539933531, -1.453093050198107861 ) ) ;
#52152=CARTESIAN_POINT ( 'NONE',  ( 6.128435733830499998, 0.1874100934057248424, 1.831705376836203936 ) ) ;
#52156=CARTESIAN_POINT ( 'NONE',  ( 0.9131076777311696313, -0.2804849920042574718, 1.849292663789033009 ) ) ;
#52161=CARTESIAN_POINT ( 'NONE',  ( 0.6098336241119780565, -0.6879379538977903330, 1.784437680087819666 ) ) ;
#52162=CARTESIAN_POINT ( 'NONE',  ( 3.274023454312132486, -1.055227348164128331, 1.420681018326484413 ) ) ;
#52163=CARTESIAN_POINT ( 'NONE',  ( 0.3285747216504387724, 1.318609938922534530, -1.385187620709791512 ) ) ;
#52165=CARTESIAN_POINT ( 'NONE',  ( 4.130425774021486696, 0.5146700378890654015, 1.845081245478853216 ) ) ;
#52168=CARTESIAN_POINT ( 'NONE',  ( 4.879337363741727884, -0.09859167047137314122, 1.967224067494575346 ) ) ;
#52169=CARTESIAN_POINT ( 'NONE',  ( 0.4223351350958382544, -2.109807164369668087, 0.2139620856976830743 ) ) ;
#52171=CARTESIAN_POINT ( 'NONE',  ( 3.660894226558962128, -1.649352935060313552, -0.8826137995501317501 ) ) ;
#52172=CARTESIAN_POINT ( 'NONE',  ( 0.2932112110246976044, 1.350478442433366677, 1.228755397233910696 ) ) ;
#52174=CARTESIAN_POINT ( 'NONE',  ( 4.002700589841681200, -0.6913439845411989415, -2.095861086919461602 ) ) ;
#52178=CARTESIAN_POINT ( 'NONE',  ( 0.4497679408741364071, 1.527348849510310247, 1.386460675282843447 ) ) ;
#52185=CARTESIAN_POINT ( 'NONE',  ( 3.561042923925850978, 1.633862107263984065, -1.271492733312264090 ) ) ;
#52187=CARTESIAN_POINT ( 'NONE',  ( 1.862795570070171713, -1.530026953448139659, 1.527182012981804560 ) ) ;
#52189=CARTESIAN_POINT ( 'NONE',  ( 0.4869804533438352734, -1.902474711392083684, -0.6784070981462678729 ) ) ;
#52192=CARTESIAN_POINT ( 'NONE',  ( 0.07499057489264347731, 2.883324855518037300, -2.444194386608829372 ) ) ;
#52195=CARTESIAN_POINT ( 'NONE',  ( 6.421099303836709460, -1.707838190419972424, 0.8681067396549295712 ) ) ;
#52196=CARTESIAN_POINT ( 'NONE',  ( 6.539320575229247368, 1.232987345766973775, 2.316458022558224972 ) ) ;
#52197=CARTESIAN_POINT ( 'NONE',  ( 3.808297599986898430, 1.548825491099754315, -1.550762550882843094 ) ) ;
#52199=CARTESIAN_POINT ( 'NONE',  ( 3.023589307540079041, -0.3687504995396119201, 1.876329818327879817 ) ) ;
#52201=CARTESIAN_POINT ( 'NONE',  ( 4.241422899474024177, 0.4370803545316758743, -1.968444674787086512 ) ) ;
#52204=CARTESIAN_POINT ( 'NONE',  ( 1.177361486786612899, 1.528755565978222819, 1.314981834344926437 ) ) ;
#52206=CARTESIAN_POINT ( 'NONE',  ( -0.02329727741511803188, -2.225753042794619496, -0.5483686822410521744 ) ) ;
#52208=CARTESIAN_POINT ( 'NONE',  ( 4.207791664195513093, -1.720086916870446236, 0.1276756817342617201 ) ) ;
#52209=CARTESIAN_POINT ( 'NONE',  ( -0.1399997263889663501, 0.2375346743129815030, -2.034463206964792548 ) ) ;
#52212=CARTESIAN_POINT ( 'NONE',  ( 1.135121963537696566, -0.04462593873827064989, -1.961518378280776354 ) ) ;
#52214=CARTESIAN_POINT ( 'NONE',  ( 0.07516593201273635838, 7.629137130509072939, -2.644199648255764590 ) ) ;
#52218=CARTESIAN_POINT ( 'NONE',  ( 4.178215122889179511, 0.8575144648667647473, 1.595655492163786437 ) ) ;
#52223=CARTESIAN_POINT ( 'NONE',  ( 4.811091142047322577, 1.503129720864199381, -1.010622461758519552 ) ) ;
#52228=CARTESIAN_POINT ( 'NONE',  ( 5.951566935816642534, 1.409582436273165706, 1.215217600354216554 ) ) ;
#52230=CARTESIAN_POINT ( 'NONE',  ( 3.409697593026795204, -1.143712931967875601, -1.536527803759838662 ) ) ;
#52237=CARTESIAN_POINT ( 'NONE',  ( 0.3566080023540800781, 0.8287714912002723811, 1.996717379258300840 ) ) ;
#52240=CARTESIAN_POINT ( 'NONE',  ( 0.4283665542385572955, 1.745377284433462295, 0.5351633580037706839 ) ) ;
#52242=CARTESIAN_POINT ( 'NONE',  ( 3.328933297416610593, 0.04358344136132231289, 1.825221112333124340 ) ) ;
#52244=CARTESIAN_POINT ( 'NONE',  ( 1.898553772666348394, -1.876154101037771582, -0.3696338911259658411 ) ) ;
#52245=CARTESIAN_POINT ( 'NONE',  ( 2.260148812482842828, -1.969196485324760326, 0.04527702327579082725 ) ) ;
#52246=CARTESIAN_POINT ( 'NONE',  ( 4.194824786304445219, 1.561856751782536135, 1.154042840620983057 ) ) ;
#52250=CARTESIAN_POINT ( 'NONE',  ( 4.289387122732970958, -0.003046686910593982868, -2.120778211268215419 ) ) ;
#52260=CARTESIAN_POINT ( 'NONE',  ( 4.441915170580639227, 0.7783198120194650960, -1.651611053696280695 ) ) ;
#52261=CARTESIAN_POINT ( 'NONE',  ( 0.1392002015415672034, -0.1474423581745692435, -2.037351525059682977 ) ) ;
#52265=CARTESIAN_POINT ( 'NONE',  ( 4.574985519202336981, -0.0001439422951596270033, -1.870836309977530920 ) ) ;
#52267=CARTESIAN_POINT ( 'NONE',  ( 3.580616652426432012, -1.856930023900615456, -0.5128254122194577658 ) ) ;
#52277=CARTESIAN_POINT ( 'NONE',  ( 1.072038591870585700, -0.9482746200860227015, 1.893052406114493769 ) ) ;
#52280=CARTESIAN_POINT ( 'NONE',  ( 6.825056245572477032, -1.890314563506745316, -0.8446596084958692963 ) ) ;
#52281=CARTESIAN_POINT ( 'NONE',  ( 1.874305484616908934, -0.09156810461483089192, -1.839108553062768214 ) ) ;
#52286=CARTESIAN_POINT ( 'NONE',  ( 1.078551950277906402, -2.237456700407819632, -0.4976139165283523513 ) ) ;
#52288=CARTESIAN_POINT ( 'NONE',  ( 6.263619209540105537, 1.000520857970560895, 1.664240579554799648 ) ) ;
#52292=CARTESIAN_POINT ( 'NONE',  ( 1.002198536899261860, -0.9015652438304004868, 1.800089726458251826 ) ) ;
#52297=CARTESIAN_POINT ( 'NONE',  ( 4.066417572287989834, -1.950679019168543471, -0.7525511210752598990 ) ) ;
#52298=CARTESIAN_POINT ( 'NONE',  ( 2.711481306777110412, -1.750889404861367460, 0.2573583090697410536 ) ) ;
#52301=CARTESIAN_POINT ( 'NONE',  ( 5.824266732648851530, 2.207754452112113075, 0.6165074292824882507 ) ) ;
#52302=CARTESIAN_POINT ( 'NONE',  ( 3.415673062852276232, 1.103011313415346306, -1.346137666936922717 ) ) ;
#52305=CARTESIAN_POINT ( 'NONE',  ( 3.286226705615200139, -1.671546763608670272, 0.4602933761382789202 ) ) ;
#52306=CARTESIAN_POINT ( 'NONE',  ( 3.947858391199970285, 1.570127341852745273, 1.499791163327832466 ) ) ;
#52308=CARTESIAN_POINT ( 'NONE',  ( 4.540250091716044878, 0.7762272601403925609, 1.861345588084816871 ) ) ;
#52309=CARTESIAN_POINT ( 'NONE',  ( 1.312500000000000888, 1.451031289061174734, 1.451031289061067486 ) ) ;
#52311=CARTESIAN_POINT ( 'NONE',  ( 2.063383741992553144, 0.3316209358346365876, -1.897488084917675843 ) ) ;
#52313=CARTESIAN_POINT ( 'NONE',  ( 6.152596803620836496, 2.197069216644991663, 0.3270334163130541594 ) ) ;
#52315=CARTESIAN_POINT ( 'NONE',  ( -0.2108831679771168421, 7.629137130509075604, -2.497154329497493386 ) ) ;
#52321=CARTESIAN_POINT ( 'NONE',  ( 0.7861345822535183991, 2.139302153856616151, -0.5977261144227277168 ) ) ;
#52322=CARTESIAN_POINT ( 'NONE',  ( 5.600043156098196917, 0.7966083592686535875, -1.793046234938546979 ) ) ;
#52325=CARTESIAN_POINT ( 'NONE',  ( 6.362609103649501385, -1.606607173180201187, 1.593162483179947575 ) ) ;
#52328=CARTESIAN_POINT ( 'NONE',  ( 4.668458352237446540, -0.8791470107305986437, -1.866060610730088332 ) ) ;
#52334=CARTESIAN_POINT ( 'NONE',  ( 5.800035319642947051, -1.870726058474009079, -0.0005997126256013227737 ) ) ;
#52335=CARTESIAN_POINT ( 'NONE',  ( 5.115702696222887980, 0.1348363893083539267, 1.728983578677806499 ) ) ;
#52336=CARTESIAN_POINT ( 'NONE',  ( 3.825523041098664034, 0.9271419989833797892, -1.472723941875812237 ) ) ;
#52338=CARTESIAN_POINT ( 'NONE',  ( 2.208868952076637804, 2.049428429192188705, 1.027153634429162743 ) ) ;
#52340=CARTESIAN_POINT ( 'NONE',  ( 5.442948297640814559, -1.648798800320664615, -1.285478093666903687 ) ) ;
#52341=CARTESIAN_POINT ( 'NONE',  ( 6.509718631618705231, -0.9178700960432868428, -1.711342201762585002 ) ) ;
#52344=CARTESIAN_POINT ( 'NONE',  ( 1.512342498431101134, -1.897697209584522815, 0.6819976561535444626 ) ) ;
#52345=CARTESIAN_POINT ( 'NONE',  ( 0.3928598746986839974, 1.819701785225702473, -1.220828600141062203 ) ) ;
#52350=CARTESIAN_POINT ( 'NONE',  ( 2.086737175084628859, -1.302296122868449535, 1.673399772156684895 ) ) ;
#52352=CARTESIAN_POINT ( 'NONE',  ( 5.760330229460346452, 0.7440287100829169331, 1.667389206893993725 ) ) ;
#52358=CARTESIAN_POINT ( 'NONE',  ( 2.865494903669623117, -1.653614387114977990, -1.159512146270498478 ) ) ;
#52359=CARTESIAN_POINT ( 'NONE',  ( 6.581111309608331794, -0.1016299978719436697, -2.204559905201553427 ) ) ;
#52361=CARTESIAN_POINT ( 'NONE',  ( 4.311269015108330827, -1.545260327404588852, -1.036625270625696205 ) ) ;
#52363=( BOUNDED_SURFACE ( )  B_SPLINE_SURFACE ( 3, 3, ( 
 ( #175735, #205258, #179994, #11068, #27328, #46812, #129202, #28405, #189029, #77147 ),
 ( #14261, #64110, #143268, #127062, #193024, #94499, #80352, #112926, #196243, #44676 ),
 ( #160537, #212466, #31618, #78216, #178939, #194096, #146451, #144339, #210339, #30553 ),
 ( #161621, #61978, #95571, #45745, #111863, #177868, #13214, #145405, #211405, #116104 ),
 ( #48932, #166942, #18535, #182095, #33726, #99804, #51054, #19605, #200475, #84612 ),
 ( #36920, #65144, #165869, #199409, #198346, #135512, #100858, #164801, #117178, #183179 ),
 ( #115050, #53182, #16393, #150701, #1203, #49986, #213521, #34783, #52121, #131300 ) ),
 .UNSPECIFIED., .T., .F., .F. ) 
 B_SPLINE_SURFACE_WITH_KNOTS ( ( 4, 3, 4 ),
 ( 4, 1, 1, 1, 1, 1, 1, 4 ),
 ( 0.000000000000000000, 0.5000000000000000000, 1.000000000000000000 ),
 ( 0.000000000000000000, 0.09884949474608377418, 0.1930937302289311708, 0.2616037862002966730, 0.3630310524065313849, 0.5216543902990324888, 0.7338513509102306820, 0.9999999999999998890 ),
 .UNSPECIFIED. ) 
 GEOMETRIC_REPRESENTATION_ITEM ( )  RATIONAL_B_SPLINE_SURFACE ( (
 ( 1.000000000000000222, 1.000000000000000222, 1.000000000000000000, 1.000000000000000222, 1.000000000000000444, 1.000000000000000222, 1.000000000000000222, 1.000000000000000222, 1.000000000000000222, 1.000000000000000222),
 ( 0.3333333333333334259, 0.3333333333333334259, 0.3333333333333334814, 0.3333333333333333703, 0.3333333333333334814, 0.3333333333333333703, 0.3333333333333334814, 0.3333333333333333703, 0.3333333333333334259, 0.3333333333333334259),
 ( 0.3333333333333334259, 0.3333333333333334259, 0.3333333333333334814, 0.3333333333333333703, 0.3333333333333334814, 0.3333333333333333703, 0.3333333333333334814, 0.3333333333333333703, 0.3333333333333334259, 0.3333333333333334259),
 ( 1.000000000000000222, 1.000000000000000222, 1.000000000000000000, 1.000000000000000222, 1.000000000000000444, 1.000000000000000222, 1.000000000000000222, 1.000000000000000222, 1.000000000000000222, 1.000000000000000222),
 ( 0.3333333333333334259, 0.3333333333333334259, 0.3333333333333334814, 0.3333333333333333703, 0.3333333333333334814, 0.3333333333333333703, 0.3333333333333334814, 0.3333333333333333703, 0.3333333333333334259, 0.3333333333333334259),
 ( 0.3333333333333334259, 0.3333333333333334259, 0.3333333333333334814, 0.3333333333333333703, 0.3333333333333334814, 0.3333333333333333703, 0.3333333333333334814, 0.3333333333333333703, 0.3333333333333334259, 0.3333333333333334259),
 ( 1.000000000000000222, 1.000000000000000222, 1.000000000000000000, 1.000000000000000222, 1.000000000000000444, 1.000000000000000222, 1.000000000000000222, 1.000000000000000222, 1.000000000000000222, 1.000000000000000222) ) ) 
 REPRESENTATION_ITEM ( '' )  SURFACE ( )  );
#52371=CARTESIAN_POINT ( 'NONE',  ( 2.020412548985677681, 1.729603159991144556, -0.1218859752038989053 ) ) ;
#52372=CARTESIAN_POINT ( 'NONE',  ( 1.604977476713872697, -1.727474156022209328, 0.2105546776469246206 ) ) ;
#52373=CARTESIAN_POINT ( 'NONE',  ( 5.408889320884306073, 1.750735854880939746, -1.503546334452151134 ) ) ;
#52376=CARTESIAN_POINT ( 'NONE',  ( 1.845067233098520942, -1.742569257963645146, 1.099794920586109725 ) ) ;
#52378=CARTESIAN_POINT ( 'NONE',  ( 0.1399997263886003374, 0.002789056014650820314, -1.999853399661279063 ) ) ;
#52381=CARTESIAN_POINT ( 'NONE',  ( 6.737182200980119440, -1.669782060861616291, 0.8434366901180423426 ) ) ;
#52382=CARTESIAN_POINT ( 'NONE',  ( 4.289254230599209627, -0.005406649120142519548, -1.912571728590661380 ) ) ;
#52384=CARTESIAN_POINT ( 'NONE',  ( 6.059228469117068805, -1.890744221452178353, -1.137928576693452820 ) ) ;
#52389=CARTESIAN_POINT ( 'NONE',  ( 6.358074577831472673, 0.8120454629646983724, -1.959034198684066697 ) ) ;
#52390=EDGE_LOOP ( 'NONE', ( #38370, #99596, #141126, #163541 ) ) ;
#52391=CARTESIAN_POINT ( 'NONE',  ( 3.628207509315328760, -1.372338424813070556, -1.855037849730954091 ) ) ;
#52392=CARTESIAN_POINT ( 'NONE',  ( 4.914483161888778540, 0.7490505147796695518, 1.813437088826752142 ) ) ;
#52393=CARTESIAN_POINT ( 'NONE',  ( 0.4265131056294459433, -1.285834093136655643, 1.481649512794058543 ) ) ;
#52397=CARTESIAN_POINT ( 'NONE',  ( 6.438686429976131720, -1.555646628146038157, 1.282773817382940384 ) ) ;
#52401=CARTESIAN_POINT ( 'NONE',  ( 2.817415258179640336, -1.886890863808653007, -1.073800027038468219 ) ) ;
#52403=CARTESIAN_POINT ( 'NONE',  ( 1.160570123509139906, 2.118417766304943495, 0.09849428607798524360 ) ) ;
#52408=CARTESIAN_POINT ( 'NONE',  ( 2.249358885376837591, -1.653154358101496246, -1.230164295365917537 ) ) ;
#52416=CARTESIAN_POINT ( 'NONE',  ( 4.231050068913538631, 1.749697241329374098, 0.7720063087622434095 ) ) ;
#52419=CARTESIAN_POINT ( 'NONE',  ( 1.282923566313122210, -2.207321063319432231, -0.4954982646878171582 ) ) ;
#52421=CARTESIAN_POINT ( 'NONE',  ( 1.037045679623523897, -0.04297598538225732429, 1.811226269459820903 ) ) ;
#52422=CARTESIAN_POINT ( 'NONE',  ( 1.323292448300671165, -1.390094005022534773, -1.318457861805687914 ) ) ;
#52423=CARTESIAN_POINT ( 'NONE',  ( 1.732962091629593804, -1.965256999408044436, -0.6514315320021792921 ) ) ;
#52426=CARTESIAN_POINT ( 'NONE',  ( 0.6550726410136185063, -1.664185259661060234, -1.056694852926373773 ) ) ;
#52427=CARTESIAN_POINT ( 'NONE',  ( 5.584577364790731302, -1.880054400457907171, -0.4198111936028568469 ) ) ;
#52428=CARTESIAN_POINT ( 'NONE',  ( 0.5050340691590156084, -0.7831231796689057667, -2.170891709475693876 ) ) ;
#52431=CARTESIAN_POINT ( 'NONE',  ( 4.562968466866096584, 1.596587869669671145, -1.305994239470360974 ) ) ;
#52436=CARTESIAN_POINT ( 'NONE',  ( 5.438542061945497608, 2.074265116652589391, 0.3630613376124564584 ) ) ;
#52438=CARTESIAN_POINT ( 'NONE',  ( 6.285608408418759119, -1.950803066209889636, 0.6937918898708083093 ) ) ;
#52440=CARTESIAN_POINT ( 'NONE',  ( 4.516967039858135635, 1.974289957696921949, 0.8805908171375662619 ) ) ;
#52441=CARTESIAN_POINT ( 'NONE',  ( 5.057288377774205479, -1.731171949422895651, 1.040023186547271328 ) ) ;
#52442=CARTESIAN_POINT ( 'NONE',  ( -0.1399997263889597998, 7.629137130509076492, -2.600276787041354787 ) ) ;
#52447=CARTESIAN_POINT ( 'NONE',  ( 4.030482632556767975, 0.5424685788828055300, 1.942097399793737633 ) ) ;
#52452=CARTESIAN_POINT ( 'NONE',  ( 6.720655732516622294, 7.629137130509072051, 2.773739711112707340 ) ) ;
#52454=CARTESIAN_POINT ( 'NONE',  ( 4.798453934790239295, 1.388474963651475269, -1.462457531588717830 ) ) ;
#52456=CARTESIAN_POINT ( 'NONE',  ( 1.066563130004109405, -1.557762288434235476, -0.7409518577887274082 ) ) ;
#52461=CARTESIAN_POINT ( 'NONE',  ( 5.202362286721474050, -0.6290170809866748591, -1.761763226176292996 ) ) ;
#52462=CARTESIAN_POINT ( 'NONE',  ( 6.469000937953021335, -1.553436082622870140, 1.280157488742767136 ) ) ;
#52467=CARTESIAN_POINT ( 'NONE',  ( 0.1578276607246929530, 1.163290555716024244, 1.646825313395771762 ) ) ;
#52468=CARTESIAN_POINT ( 'NONE',  ( 1.494102799026775008, -0.9672467274632718937, 1.531528279607297094 ) ) ;
#52470=CARTESIAN_POINT ( 'NONE',  ( 5.911032513020412438, 1.904272706209766630, 1.023102869888978361 ) ) ;
#52474=CARTESIAN_POINT ( 'NONE',  ( 0.7783702408986278298, -0.4687143430282306733, -1.857332652546606733 ) ) ;
#52480=CARTESIAN_POINT ( 'NONE',  ( 3.766626874709140704, -1.453462046928340579, 1.600284095077113333 ) ) ;
#52483=CARTESIAN_POINT ( 'NONE',  ( 0.4750491441844888474, -1.531729482103380224, 1.466773057065169139 ) ) ;
#52485=CARTESIAN_POINT ( 'NONE',  ( 1.967984887604894206, 1.010138386605848426, 1.692741100060575210 ) ) ;
#52486=CARTESIAN_POINT ( 'NONE',  ( 4.886922752366290368, -1.802716094696995786, -0.6387714794457154399 ) ) ;
#52489=CARTESIAN_POINT ( 'NONE',  ( 6.549268392505379843, 1.714383406945050980, -0.9693629108104614422 ) ) ;
#52490=CARTESIAN_POINT ( 'NONE',  ( 2.079929315299507753, -1.904492180933140322, -0.3787631973139488073 ) ) ;
#52498=CARTESIAN_POINT ( 'NONE',  ( 3.457846583235091753, 0.5364296187198510646, -2.140574738106671759 ) ) ;
#52499=CARTESIAN_POINT ( 'NONE',  ( 2.415298318263587873, 1.970979330149217335, 0.9926799514654093270 ) ) ;
#52501=CARTESIAN_POINT ( 'NONE',  ( 1.014147342612067737, -1.912461472154961539, 0.0006945104691555297090 ) ) ;
#52502=CARTESIAN_POINT ( 'NONE',  ( -0.02319159430947542733, 0.7471999394491578572, -1.895068635927643630 ) ) ;
#52505=CARTESIAN_POINT ( 'NONE',  ( 3.244645865714153032, -2.039272935636734285, -0.3565889006169955522 ) ) ;
#52509=CARTESIAN_POINT ( 'NONE',  ( 0.9190830904215805397, 1.997680973563022544, 0.8264451868333838602 ) ) ;
#52510=CARTESIAN_POINT ( 'NONE',  ( 3.017305944477025825, -2.111434807548946857, 0.5868732223921411251 ) ) ;
#52516=CARTESIAN_POINT ( 'NONE',  ( 6.399014502872731214, -0.8263350558326795214, -1.524632933908439902 ) ) ;
#52519=CARTESIAN_POINT ( 'NONE',  ( 3.643477671580112709, 1.873648065284461817, -0.8808079623299628347 ) ) ;
#52520=CARTESIAN_POINT ( 'NONE',  ( 4.253586407750776566, 2.053249321966661434, -0.5160394917872836995 ) ) ;
#52523=CARTESIAN_POINT ( 'NONE',  ( 2.412896334679739851, -1.525488895468416706, 1.245673054583651407 ) ) ;
#52524=CARTESIAN_POINT ( 'NONE',  ( 0.3340484552533556362, -1.024938778295768849, -1.614363347046356756 ) ) ;
#52525=CARTESIAN_POINT ( 'NONE',  ( 4.769621702613293657, 1.317199799690757178, 1.875844486027035574 ) ) ;
#52526=CARTESIAN_POINT ( 'NONE',  ( 3.176193443437186126, -1.086901434622984830, 1.466744820640853320 ) ) ;
#52531=CARTESIAN_POINT ( 'NONE',  ( 4.306893573823011856, -0.4451576889303583418, -1.963212451998196606 ) ) ;
#52532=CARTESIAN_POINT ( 'NONE',  ( 4.539869136473917877, 1.278287603951251183, 1.488235606430035274 ) ) ;
#52535=CARTESIAN_POINT ( 'NONE',  ( 0.07556134207193415664, 4.081186479400328082, -2.798928192855642649 ) ) ;
#52536=CARTESIAN_POINT ( 'NONE',  ( 0.7145361118556601276, 1.933244891618046024, 0.7966077499205433954 ) ) ;
#52537=CARTESIAN_POINT ( 'NONE',  ( 5.401144703012512593, 1.448466425555764658, 1.016686210146000358 ) ) ;
#52539=CARTESIAN_POINT ( 'NONE',  ( 1.500213180713722450, -0.7911926984936793472, -2.043816727864488314 ) ) ;
#52540=CARTESIAN_POINT ( 'NONE',  ( 0.3271923042600047848, 0.8970799620377118977, -1.491255180049656071 ) ) ;
#52544=CARTESIAN_POINT ( 'NONE',  ( 0.6094340267816320544, -1.717071606940338446, 0.1640370458491739458 ) ) ;
#52545=CARTESIAN_POINT ( 'NONE',  ( 1.265469760322552206, -2.298542322993640141, 0.001328286606278733300 ) ) ;
#52546=CARTESIAN_POINT ( 'NONE',  ( 0.3280006606478855224, 1.121390616443746602, -1.882787531365101685 ) ) ;
#52548=CARTESIAN_POINT ( 'NONE',  ( 6.837244271306878396, -1.062160112102826126, 1.370476690187643731 ) ) ;
#52549=CARTESIAN_POINT ( 'NONE',  ( 2.455956380646412196, 0.5873987694336445520, -2.127207350628975924 ) ) ;
#52550=CARTESIAN_POINT ( 'NONE',  ( 0.4444779246538512751, -1.024716592377757696, 1.914062593285012603 ) ) ;
#52552=CARTESIAN_POINT ( 'NONE',  ( 0.7786901736592425349, -0.5205582433389954744, -2.052224243718490992 ) ) ;
#52553=CARTESIAN_POINT ( 'NONE',  ( 6.620655732516651071, -0.002413161512292844035, 2.173887093218453082 ) ) ;
#52554=CARTESIAN_POINT ( 'NONE',  ( 5.895520149318425496, 1.459072380863110530, 1.257889585189754023 ) ) ;
#52556=CARTESIAN_POINT ( 'NONE',  ( 1.910137617552462030, -1.084854587848137708, -2.019442561568355110 ) ) ;
#52560=CARTESIAN_POINT ( 'NONE',  ( 3.721504678736448302, 1.905620783811642571, 1.141157194635911365 ) ) ;
#52567=CARTESIAN_POINT ( 'NONE',  ( 1.758435621656749603, 1.928751379572872571, -0.5880216644931559600 ) ) ;
#52569=CARTESIAN_POINT ( 'NONE',  ( 1.340767248851399307, -2.011434839998844204, -0.4557168523060088905 ) ) ;
#52574=CARTESIAN_POINT ( 'NONE',  ( 3.978626637211603700, -0.2140425413966473567, -2.180973779111646138 ) ) ;
#52575=CARTESIAN_POINT ( 'NONE',  ( 0.7916389524552720491, 1.525042296397002284, -1.319230309296010928 ) ) ;
#52576=CARTESIAN_POINT ( 'NONE',  ( 0.7492455685023796663, 1.839184785914184994, -0.09005233288367914257 ) ) ;
#52577=CARTESIAN_POINT ( 'NONE',  ( 5.372717881723642286, -0.05365108595901035143, -2.291914610307096201 ) ) ;
#52578=CARTESIAN_POINT ( 'NONE',  ( 2.835703941817575569, 1.827261480098177682, 0.2250241719141123087 ) ) ;
#52579=ADVANCED_FACE ( 'NONE', ( #65457 ), #99067, .T. ) ;
#52581=CARTESIAN_POINT ( 'NONE',  ( 4.612205747861584548, -0.7811881352849485705, -1.650120847746315622 ) ) ;
#52582=CARTESIAN_POINT ( 'NONE',  ( 4.588517629802620235, -0.5350896943857390564, 1.944070981013111155 ) ) ;
#52584=CARTESIAN_POINT ( 'NONE',  ( 4.223666230214691453, -2.166182250408314580, 0.6532043330096364286 ) ) ;
#52586=CARTESIAN_POINT ( 'NONE',  ( 6.493207903183886742, 1.834288230482609583, -1.034473908808232201 ) ) ;
#52589=CARTESIAN_POINT ( 'NONE',  ( 3.666520218671379450, -0.8364210039109070127, -1.894060025281426807 ) ) ;
#52594=CARTESIAN_POINT ( 'NONE',  ( 1.664548039484465614, -1.362698257634049614, 1.362033803609383531 ) ) ;
#52596=CARTESIAN_POINT ( 'NONE',  ( 0.2386330332824412315, -1.909482672672847992, -0.4822418261516500659 ) ) ;
#52601=CARTESIAN_POINT ( 'NONE',  ( 2.004415182159818176, -0.9449143528836713157, 2.010537586115124231 ) ) ;
#52602=CARTESIAN_POINT ( 'NONE',  ( 3.153452123856602896, -1.720715631468725526, -1.213874241417127298 ) ) ;
#52605=CARTESIAN_POINT ( 'NONE',  ( 0.7130641938532373825, -1.569203791704287809, -1.000260708767531481 ) ) ;
#52610=CARTESIAN_POINT ( 'NONE',  ( 0.8090202166558431163, -0.5209130535433897924, -2.055487714681260236 ) ) ;
#52613=CARTESIAN_POINT ( 'NONE',  ( 4.861744986159981075, -0.5251177144562025889, 1.890194517805739771 ) ) ;
#52614=CARTESIAN_POINT ( 'NONE',  ( 3.379894511112140787, 1.369989894601089775, 1.672159933133889442 ) ) ;
#52615=CARTESIAN_POINT ( 'NONE',  ( 1.434833617064284805, -1.334073193498284793, -1.269287082821937584 ) ) ;
#52618=PLANE ( 'NONE',  #54099 ) ;
#52619=CARTESIAN_POINT ( 'NONE',  ( 4.628681372238307112, -1.589566819310319845, 0.7089629299102307991 ) ) ;
#52623=CARTESIAN_POINT ( 'NONE',  ( 2.290102563249151402, -0.9248296759884739870, 1.954025333243500917 ) ) ;
#52624=CARTESIAN_POINT ( 'NONE',  ( 2.934922540206805319, 1.076151813804010926, 1.704677747124828446 ) ) ;
#52626=CARTESIAN_POINT ( 'NONE',  ( 1.235488887756378551, -1.954010380348418119, 0.9248176494114216384 ) ) ;
#52627=CARTESIAN_POINT ( 'NONE',  ( 2.940257707442377022, 1.956376729411358095, 0.2430245213203632293 ) ) ;
#52628=CARTESIAN_POINT ( 'NONE',  ( 6.509000000000053632, 6.037921079186737927, 2.494901127718162304 ) ) ;
#52629=CARTESIAN_POINT ( 'NONE',  ( 3.403789896209925114, -0.7897705758606025084, -1.774406015287466332 ) ) ;
#52634=CARTESIAN_POINT ( 'NONE',  ( -0.1110810684432777806, 1.403644835841436400, -2.056232460864733103 ) ) ;
#52639=CARTESIAN_POINT ( 'NONE',  ( 6.616287922300326585, -1.079552588663035051, -2.039509185488725951 ) ) ;
#52641=CARTESIAN_POINT ( 'NONE',  ( 4.311346321947408633, -1.628642355029306987, -1.093319670275281652 ) ) ;
#52643=CARTESIAN_POINT ( 'NONE',  ( 1.283827520628720187, 1.646837967535810021, -1.163270716046126196 ) ) ;
#52645=CARTESIAN_POINT ( 'NONE',  ( 3.977823109611013930, -0.8067237889231733128, 1.957824063906116407 ) ) ;
#52649=CARTESIAN_POINT ( 'NONE',  ( 2.923586578878138109, 1.022379729796508041, -1.530975008504284141 ) ) ;
#52653=CARTESIAN_POINT ( 'NONE',  ( 4.148766697842418694, 2.080301416381886703, 0.4105806053946169376 ) ) ;
#52657=CARTESIAN_POINT ( 'NONE',  ( 5.114554592455347048, 1.424167462454002608, -1.489711086068323587 ) ) ;
#52659=CARTESIAN_POINT ( 'NONE',  ( 0.8888279104573212352, 0.1313983060258062385, 1.856467483602406432 ) ) ;
#52660=CARTESIAN_POINT ( 'NONE',  ( 2.278628554356322500, 1.682734121078124812, -0.7478279864501293783 ) ) ;
#52664=CARTESIAN_POINT ( 'NONE',  ( 2.455956380646412196, 0.5873987694336445520, -2.127207350628975924 ) ) ;
#52665=CARTESIAN_POINT ( 'NONE',  ( 5.308033872091713512, -2.252217787711635388, 0.2143866227288723780 ) ) ;
#52667=CARTESIAN_POINT ( 'NONE',  ( 4.816585706611137496, -0.6173935602037239345, -1.703258737839604242 ) ) ;
#52668=CARTESIAN_POINT ( 'NONE',  ( 4.557778266838360182, 1.108094384514320963, 1.562507240529472874 ) ) ;
#52670=CARTESIAN_POINT ( 'NONE',  ( 4.258636414635104117, -1.461677231104720143, 1.323132448414195528 ) ) ;
#52671=CARTESIAN_POINT ( 'NONE',  ( 4.680451076648031616, -1.814532364864028136, -0.4542276060127621862 ) ) ;
#52672=CARTESIAN_POINT ( 'NONE',  ( 4.967181581899757781, 1.619035083845013157, 0.9176225028624994673 ) ) ;
#52675=CARTESIAN_POINT ( 'NONE',  ( 0.1808755166769344669, 1.673851406602990366, -1.124249698880399162 ) ) ;
#52677=CARTESIAN_POINT ( 'NONE',  ( 1.752698641044206251, 0.6620485714215967876, 1.999371444633216033 ) ) ;
#52681=CARTESIAN_POINT ( 'NONE',  ( 3.076547362214879566, 0.9570632234598417387, 1.892448740577145738 ) ) ;
#52683=CARTESIAN_POINT ( 'NONE',  ( 2.267837486342203057, 0.5347344578308220742, -1.947668537691170876 ) ) ;
#52688=CARTESIAN_POINT ( 'NONE',  ( 1.845224345143604561, -1.827161268409679407, 1.154667503900350445 ) ) ;
#52689=CARTESIAN_POINT ( 'NONE',  ( 6.890000000000015667, 0.5768591945385994624, 2.052260346930290247 ) ) ;
#52695=CARTESIAN_POINT ( 'NONE',  ( 0.6092356648998223934, -0.3158941238240610128, 2.168550393043596536 ) ) ;
#52697=CARTESIAN_POINT ( 'NONE',  ( 1.657462679512666348, -1.941143012291703940, -1.162103002166763988 ) ) ;
#52705=CARTESIAN_POINT ( 'NONE',  ( 3.580403817701179658, -1.662759015092404535, -0.4584509792747801793 ) ) ;
#52707=CARTESIAN_POINT ( 'NONE',  ( 2.231405582217013794, -1.152036887248751862, -1.343533879150171861 ) ) ;
#52708=CARTESIAN_POINT ( 'NONE',  ( 2.807291710112637340, 1.725400251052783052, -1.036881053028392508 ) ) ;
#52710=CARTESIAN_POINT ( 'NONE',  ( 5.684669477433477169, -2.151827843693389308, -0.4886931181809702207 ) ) ;
#52712=CARTESIAN_POINT ( 'NONE',  ( 4.271743411778946786, 0.4384756098019436665, -1.971458303354764352 ) ) ;
#52714=CARTESIAN_POINT ( 'NONE',  ( 4.025017672583341977, -1.753021876717888006, 0.9963191169995513352 ) ) ;
#52717=CARTESIAN_POINT ( 'NONE',  ( 3.010468980803046257, 1.356049738124785353, -1.288842618233053683 ) ) ;
#52718=EDGE_CURVE ( 'NONE', #168104, #55444, #8040, .T. ) ;
#52719=CARTESIAN_POINT ( 'NONE',  ( 1.494246876672610025, -1.020364814108923213, 1.617233793950809906 ) ) ;
#52724=CARTESIAN_POINT ( 'NONE',  ( 0.3867804997886997720, -1.801505969789623629, -0.6421655129100201087 ) ) ;
#52726=CARTESIAN_POINT ( 'NONE',  ( 1.205434515183744226, -1.544416933936803904, -1.209700862059132964 ) ) ;
#52729=CARTESIAN_POINT ( 'NONE',  ( 5.379186226027963258, -1.918017450862268714, -0.9047448674902383026 ) ) ;
#52732=CARTESIAN_POINT ( 'NONE',  ( 5.940691962724923059, 0.3820465716247494758, 1.933821394355714096 ) ) ;
#52734=CARTESIAN_POINT ( 'NONE',  ( 1.353772324478102584, -1.461116690358499337, -1.385217879419877951 ) ) ;
#52736=CARTESIAN_POINT ( 'NONE',  ( 1.072038591870585700, -0.9482746200860227015, 1.893052406114493769 ) ) ;
#52738=CARTESIAN_POINT ( 'NONE',  ( 2.875506610227479332, -0.2054619808779626633, 2.060159609288146232 ) ) ;
#52742=CARTESIAN_POINT ( 'NONE',  ( 4.435544174077206137, 0.8940267830384877046, -1.889970096008020128 ) ) ;
#52744=CARTESIAN_POINT ( 'NONE',  ( 3.399243825379614226, 1.438455020490635450, 1.123966471122700650 ) ) ;
#52745=CARTESIAN_POINT ( 'NONE',  ( 1.154613445820645845, 0.3528100842024176620, 1.776585200675658172 ) ) ;
#52750=CARTESIAN_POINT ( 'NONE',  ( 5.403435775159438847, 1.801252639416499601, 1.274624607731331905 ) ) ;
#52753=CARTESIAN_POINT ( 'NONE',  ( 4.547458224165379370, -1.746952781796942133, 0.7782266863690868730 ) ) ;
#52757=CARTESIAN_POINT ( 'NONE',  ( 6.514133371570012265, 2.065101995627930620, -0.1482383472809906122 ) ) ;
#52764=CARTESIAN_POINT ( 'NONE',  ( 3.092876253348992410, 1.606159189733218140, -0.9584765265276545820 ) ) ;
#52770=CARTESIAN_POINT ( 'NONE',  ( 0.2331713839410576583, 0.005725554726919174046, -1.953566683266183102 ) ) ;
#52771=CARTESIAN_POINT ( 'NONE',  ( 1.019157904985489305, -1.821734318179563106, 0.8647433871810317196 ) ) ;
#52775=CARTESIAN_POINT ( 'NONE',  ( 1.781448188194576066, 1.512826363221421833, 1.585725795389548942 ) ) ;
#52776=CARTESIAN_POINT ( 'NONE',  ( 6.674438497507635404, -1.118711561685633349, 1.443368817030561635 ) ) ;
#52784=CARTESIAN_POINT ( 'NONE',  ( 3.772867777003403589, 1.732451475078290448, -0.6238847238279123797 ) ) ;
#52785=CARTESIAN_POINT ( 'NONE',  ( 0.8561085696928095734, 0.8139254773164643630, -1.841379974997810143 ) ) ;
#52786=CARTESIAN_POINT ( 'NONE',  ( 1.915759298113205666, 0.7205626639651928622, 2.182595962359680897 ) ) ;
#52788=CARTESIAN_POINT ( 'NONE',  ( 0.4614603993745093891, -0.5041695895235782654, 1.791261842318598863 ) ) ;
#52792=CARTESIAN_POINT ( 'NONE',  ( 4.236511230858605259, 1.172298487584079396, -1.510895503047122945 ) ) ;
#52796=CARTESIAN_POINT ( 'NONE',  ( 4.194928683902748645, 1.680244682056671879, 1.243991948001839543 ) ) ;
#52797=CARTESIAN_POINT ( 'NONE',  ( 2.799504582125960095, -0.5885537693137884441, 1.775713401224961574 ) ) ;
#52800=CARTESIAN_POINT ( 'NONE',  ( 3.262975863287612466, 1.697222826579761534, -0.3846178214849705901 ) ) ;
#52805=CARTESIAN_POINT ( 'NONE',  ( 4.037519343584392573, -1.191552764850771995, -1.247402213628981293 ) ) ;
#52807=CARTESIAN_POINT ( 'NONE',  ( 4.335597073515660149, 0.9364531651635084053, -1.981528385891350386 ) ) ;
#52808=CARTESIAN_POINT ( 'NONE',  ( 6.445939570963194143, 0.8488519614954292969, -2.037301952897092594 ) ) ;
#52809=CARTESIAN_POINT ( 'NONE',  ( 6.983263157960365675, 7.052158404629149224, 2.651961988451009944 ) ) ;
#52810=CARTESIAN_POINT ( 'NONE',  ( 3.643588050499571018, 1.964860050422628124, -0.9237357390106512023 ) ) ;
#52811=CARTESIAN_POINT ( 'NONE',  ( 2.508196354075361789, -0.6984789837382252564, -1.686990664346368796 ) ) ;
#52813=CARTESIAN_POINT ( 'NONE',  ( 5.085217855557687905, 1.732777129288827656, 1.216576597717359931 ) ) ;
#52815=CARTESIAN_POINT ( 'NONE',  ( 4.985981925524552771, -2.274816124779193593, -0.2825110863640226122 ) ) ;
#52817=CARTESIAN_POINT ( 'NONE',  ( 6.720655732516645386, 3.710664525043025019, 2.240930934554703491 ) ) ;
#52819=CARTESIAN_POINT ( 'NONE',  ( 1.155114678095255254, 0.4172207117813032662, 2.078868179971034902 ) ) ;
#52824=CARTESIAN_POINT ( 'NONE',  ( 6.883263157960364254, 2.431740398616466070, 2.435552827938294751 ) ) ;
#52827=CARTESIAN_POINT ( 'NONE',  ( 5.854138739207011888, 0.1455364397412381439, -2.011204036175239018 ) ) ;
#52829=CARTESIAN_POINT ( 'NONE',  ( 4.909062464502076395, -1.659793021533024548, 1.224303311577365161 ) ) ;
#52836=CARTESIAN_POINT ( 'NONE',  ( 0.6387612955554131666, -1.792149412372344042, 1.076304641864724410 ) ) ;
#52837=CARTESIAN_POINT ( 'NONE',  ( 4.957657809308734898, -1.899617967926207740, -0.6767155953601932117 ) ) ;
#52838=CARTESIAN_POINT ( 'NONE',  ( 4.933073973922719624, -1.305863698873997780, -1.298312775753200699 ) ) ;
#52840=CARTESIAN_POINT ( 'NONE',  ( 1.219288043345586159, -1.683946549099228029, 0.3722564037182389818 ) ) ;
#52842=CARTESIAN_POINT ( 'NONE',  ( 0.4972802279516430057, -0.2910764605805628014, 1.995268990643041640 ) ) ;
#52843=CARTESIAN_POINT ( 'NONE',  ( 0.8799778958844242105, -0.5652253508772618895, -2.228020342328890901 ) ) ;
#52845=CARTESIAN_POINT ( 'NONE',  ( 0.8786447689848001508, -1.256089115395578659, 1.881495417452299312 ) ) ;
#52846=CARTESIAN_POINT ( 'NONE',  ( 2.701903229428818776, -0.6601559168808753819, 2.000001591751764618 ) ) ;
#52851=CARTESIAN_POINT ( 'NONE',  ( 5.750000000000004441, 3.273043269275614537E-13, 2.052068128417940951 ) ) ;
#52858=CARTESIAN_POINT ( 'NONE',  ( 4.746434557108095476, 1.141014917558682340, -1.905822037654863133 ) ) ;
#52859=CARTESIAN_POINT ( 'NONE',  ( 1.939652437182255662, 0.8368340126228106524, -2.025574644071465258 ) ) ;
#52862=CARTESIAN_POINT ( 'NONE',  ( 5.934033239752055877, 1.167398200610193282, 1.576599764842034457 ) ) ;
#52864=CARTESIAN_POINT ( 'NONE',  ( 6.890000000000014779, 6.038692643467888921, 2.314896014905319266 ) ) ;
#52866=CARTESIAN_POINT ( 'NONE',  ( 5.080389167821143026, 1.047295930500062866, 1.843893106414703054 ) ) ;
#52872=CARTESIAN_POINT ( 'NONE',  ( 5.302248432823610358, 1.390444127666954355, -1.207098008268410183 ) ) ;
#52874=CARTESIAN_POINT ( 'NONE',  ( 1.346757998634398712, 0.5060278187854657661, -1.665264516905233361 ) ) ;
#52878=CARTESIAN_POINT ( 'NONE',  ( 5.594645800149128156, -0.5210773734287167391, -2.097845705497362712 ) ) ;
#52882=CARTESIAN_POINT ( 'NONE',  ( 4.733375416736937069, -1.977748744329570263, 0.8730265686548792647 ) ) ;
#52884=CARTESIAN_POINT ( 'NONE',  ( 5.132083838642755858, 1.015972595308231474, -1.689280876731833470 ) ) ;
#52885=CARTESIAN_POINT ( 'NONE',  ( 3.532318661231689916, 1.691930322982236667, -0.3780173437282279281 ) ) ;
#52886=CARTESIAN_POINT ( 'NONE',  ( 0.5740950506661415265, -1.212703583203307511, 1.825263377225619266 ) ) ;
#52887=CARTESIAN_POINT ( 'NONE',  ( 2.433052891977859566, 2.238319448195260186, 0.5606502339033142546 ) ) ;
#52888=CARTESIAN_POINT ( 'NONE',  ( 5.325487547722469905, -1.958136382931666031, 0.6425617224121594750 ) ) ;
#52889=CARTESIAN_POINT ( 'NONE',  ( -0.01194524340117873729, -0.4266214822964596309, -1.901745140312367521 ) ) ;
#52893=CARTESIAN_POINT ( 'NONE',  ( 0.9322677863709986079, -1.591319861332978425, -1.238319039483272599 ) ) ;
#52895=CARTESIAN_POINT ( 'NONE',  ( 3.206306947805489305, -2.204311952916749640, 0.1065802224688369715 ) ) ;
#52897=CARTESIAN_POINT ( 'NONE',  ( 0.6021283177516533192, 1.855420301818105910, 0.1446146731104556993 ) ) ;
#52898=CARTESIAN_POINT ( 'NONE',  ( -0.1290005225502433017, 0.6921039065478848951, -2.255494067288220439 ) ) ;
#52902=CARTESIAN_POINT ( 'NONE',  ( 6.925078400183577010, 2.950057911518182419, 2.596529392604688180 ) ) ;
#52903=CARTESIAN_POINT ( 'NONE',  ( 6.035073252477260120, -1.336788798515762489, -1.266260169258619284 ) ) ;
#52906=CARTESIAN_POINT ( 'NONE',  ( 3.414965445803084254, 1.862500966792278057, 0.8825600945957471355 ) ) ;
#52909=CARTESIAN_POINT ( 'NONE',  ( 1.770181643375926317, 2.014124636562672155, -0.1506882416659905133 ) ) ;
#52912=CARTESIAN_POINT ( 'NONE',  ( 2.483339057139447803, 1.884786786457379737, -0.8339860623947179530 ) ) ;
#52919=CARTESIAN_POINT ( 'NONE',  ( 5.092482806099829062, -2.189899077852827780, -0.2726905915074183673 ) ) ;
#52920=CARTESIAN_POINT ( 'NONE',  ( 1.581558009922879204, 1.997867266642009643, -0.8257073301623578665 ) ) ;
#52922=CARTESIAN_POINT ( 'NONE',  ( 0.4093891192313535710, -1.913260280790154866, 0.6371585790938688598 ) ) ;
#52923=CARTESIAN_POINT ( 'NONE',  ( 2.144337281971959719, -0.1124944508365255252, -2.295720847718041746 ) ) ;
#52927=CARTESIAN_POINT ( 'NONE',  ( 2.289737743334671283, -0.8020533187339595749, 1.690132462187944107 ) ) ;
#52928=CARTESIAN_POINT ( 'NONE',  ( 3.784388871581423786, -0.6371526190629381858, -1.913262240507591416 ) ) ;
#52932=CARTESIAN_POINT ( 'NONE',  ( 5.268238656634978589, 1.036954370284940419, 1.833022835974008613 ) ) ;
#52936=CARTESIAN_POINT ( 'NONE',  ( 4.957288421310242832, -1.730244549199685400, 1.041802906739682566 ) ) ;
#52938=CARTESIAN_POINT ( 'NONE',  ( 0.6552251538811122433, 1.716912266053271408, -1.142698840430116602 ) ) ;
#52945=CARTESIAN_POINT ( 'NONE',  ( 3.156845524303863559, -0.6275973837717390147, -2.078511276010074127 ) ) ;
#52948=CARTESIAN_POINT ( 'NONE',  ( 2.348939331405873077, 0.4892633877765646400, -1.774999737812533063 ) ) ;
#52950=CARTESIAN_POINT ( 'NONE',  ( 4.405938146338868933, -0.9375679901368579872, -1.981035393479456008 ) ) ;
#52951=CARTESIAN_POINT ( 'NONE',  ( 6.983263157960365675, -0.006178392973848687020, 2.053544886540019210 ) ) ;
#52952=CARTESIAN_POINT ( 'NONE',  ( 4.627936124501790260, -1.388401915515205198, -1.786361659577795136 ) ) ;
#52959=CARTESIAN_POINT ( 'NONE',  ( 5.518734381310105519, 1.635532185772445857, 0.6765044976165290880 ) ) ;
#52961=CARTESIAN_POINT ( 'NONE',  ( 2.362460971492767570, 0.8994288142968703825, 1.904360703123770149 ) ) ;
#52964=CARTESIAN_POINT ( 'NONE',  ( 2.383201438719654064, -0.002954665228930426248, 1.969739564733210324 ) ) ;
#52965=CARTESIAN_POINT ( 'NONE',  ( 0.9009904985227291663, 1.526999960511504772, 1.080287613699250304 ) ) ;
#52966=CARTESIAN_POINT ( 'NONE',  ( 1.152704166800899932, -0.4732522875653189520, -1.903817266927515961 ) ) ;
#52967=CARTESIAN_POINT ( 'NONE',  ( 6.293201719952925544, -0.09848415459409513850, -1.809066888985458199 ) ) ;
#52972=CARTESIAN_POINT ( 'NONE',  ( 5.629731426258720361, -1.187751674602673058, -1.445209747047627946 ) ) ;
#52975=CARTESIAN_POINT ( 'NONE',  ( 5.559458666840932928, 1.689222788819956245, 1.196583256836199149 ) ) ;
#52986=CARTESIAN_POINT ( 'NONE',  ( 5.441838459065293065, 1.316327937319297758, 1.454900926449454124 ) ) ;
#52988=CARTESIAN_POINT ( 'NONE',  ( 3.585314394424500062, 1.281165535658060239, -1.556669873624405120 ) ) ;
#52989=CARTESIAN_POINT ( 'NONE',  ( 2.465921856196826134, -0.9807800477944830231, 1.645437157327357180 ) ) ;
#52992=CARTESIAN_POINT ( 'NONE',  ( 0.7850416839378616674, 1.930235501049954339, -1.037882601892345491 ) ) ;
#52993=CARTESIAN_POINT ( 'NONE',  ( 0.2331713839410758105, 2.878356536703096324, -2.442089366404568640 ) ) ;
#52994=CARTESIAN_POINT ( 'NONE',  ( 2.231529376059933956, -1.218349341866202362, -1.419469154777988296 ) ) ;
#52996=CARTESIAN_POINT ( 'NONE',  ( 4.306893573823011856, -0.4451576889303583418, -1.963212451998196606 ) ) ;
#52999=CARTESIAN_POINT ( 'NONE',  ( 4.816069135992575134, 1.087346734782314472, -1.816536155142484121 ) ) ;
#53001=CARTESIAN_POINT ( 'NONE',  ( 6.408651866624735405, 0.6456447432892989946, 1.967203394946090977 ) ) ;
#53002=CARTESIAN_POINT ( 'NONE',  ( 0.6793770918060678676, 1.407085465964125204, 1.546551842177671166 ) ) ;
#53004=CARTESIAN_POINT ( 'NONE',  ( 6.598675984083053336, -0.4903212918116289787, -1.758449130657411263 ) ) ;
#53014=CARTESIAN_POINT ( 'NONE',  ( 1.101899038012419174, -0.8149344392366760781, 1.617857622727811862 ) ) ;
#53021=CARTESIAN_POINT ( 'NONE',  ( 5.923453886551514280, -1.462456689723025782, -1.388475849216065372 ) ) ;
#53022=CARTESIAN_POINT ( 'NONE',  ( -0.1104750535120025967, -0.004616138082884357029, -2.103378236956429337 ) ) ;
#53024=CARTESIAN_POINT ( 'NONE',  ( 0.1405533004714800693, 1.287645162063441928, -2.525240623925705474 ) ) ;
#53028=CARTESIAN_POINT ( 'NONE',  ( 3.731269929808676000, 0.05278475387572807015, -1.968924232409387409 ) ) ;
#53029=CARTESIAN_POINT ( 'NONE',  ( 4.288685525864014636, 1.556897452430844320, -1.281376678550147474 ) ) ;
#53031=CARTESIAN_POINT ( 'NONE',  ( 6.727182134110196721, 6.033756510516266935, 2.783943001041962795 ) ) ;
#53032=CARTESIAN_POINT ( 'NONE',  ( 4.752002516643937469, 0.8370584164609263800, 2.025481692006773748 ) ) ;
#53034=CARTESIAN_POINT ( 'NONE',  ( 2.625899107431714175, -1.107553820047700199, -1.575994028688005644 ) ) ;
#53036=CARTESIAN_POINT ( 'NONE',  ( -0.1294898018152226826, 6.948707995275583471, -2.521562306467279857 ) ) ;
#53037=CARTESIAN_POINT ( 'NONE',  ( 0.1533209562146371774, -1.769702838771534559, 1.318327933512997152 ) ) ;
#53038=DIRECTION ( 'NONE',  ( 1.214306433183764966E-17, 1.000000000000000000, 5.200010849845536803E-32 ) ) ;
#53043=CARTESIAN_POINT ( 'NONE',  ( 5.102387438446081447, 1.963913563476852309, 0.1487572088093111478 ) ) ;
#53044=CARTESIAN_POINT ( 'NONE',  ( 0.6791179963998601465, 1.305170301278056444, 1.438240348306470739 ) ) ;
#53045=CARTESIAN_POINT ( 'NONE',  ( 4.248693477488805215, 1.974695210492120045, 0.3904942472512766827 ) ) ;
#53046=CARTESIAN_POINT ( 'NONE',  ( 5.782642724008081103, -2.244312133422786015, 0.4951331349164668216 ) ) ;
#53048=CARTESIAN_POINT ( 'NONE',  ( 3.994834637159989654, 0.2691826048217076384, 1.841218289905453664 ) ) ;
#53054=CARTESIAN_POINT ( 'NONE',  ( 0.4334776158547505864, -1.553986563932317377, -1.545601477622601472 ) ) ;
#53058=CARTESIAN_POINT ( 'NONE',  ( 0.4162703231485806454, 1.261427835099769634, -1.320066674804179385 ) ) ;
#53061=CARTESIAN_POINT ( 'NONE',  ( 2.478840559695635548, -1.729657056378102853, -0.1252908626025364403 ) ) ;
#53066=CARTESIAN_POINT ( 'NONE',  ( 5.022008369909983116, -0.9795521577263366364, -1.540466923627185292 ) ) ;
#53067=CARTESIAN_POINT ( 'NONE',  ( 2.957805016080543137, -0.6199431972748243869, 1.861265166911832081 ) ) ;
#53071=CARTESIAN_POINT ( 'NONE',  ( 4.600305182625006317, -0.9987976242244798186, 1.870504488178956759 ) ) ;
#53075=CARTESIAN_POINT ( 'NONE',  ( 2.711853232431875593, 0.5564382603544039130, -1.993978196652478996 ) ) ;
#53078=CARTESIAN_POINT ( 'NONE',  ( 4.336746411289113645, 1.366526421497065824, -1.751164563135388041 ) ) ;
#53080=CARTESIAN_POINT ( 'NONE',  ( 3.323114718373169740, 1.032193166631629078, -2.053959190227053533 ) ) ;
#53084=ADVANCED_FACE ( 'NONE', ( #53501 ), #195363, .F. ) ;
#53089=CARTESIAN_POINT ( 'NONE',  ( 2.918110517850933672, -1.910018876965378309, 0.09814724848770939314 ) ) ;
#53091=CARTESIAN_POINT ( 'NONE',  ( 4.295721138614797319, -0.6590762262537721572, 1.594082981517078945 ) ) ;
#53092=CARTESIAN_POINT ( 'NONE',  ( 2.887907956677421062, -2.014008092954455265, 0.1037802451031161616 ) ) ;
#53093=CARTESIAN_POINT ( 'NONE',  ( 4.500793239850611194, -2.254531372669385636, 0.4477389049844481272 ) ) ;
#53095=CARTESIAN_POINT ( 'NONE',  ( 6.076811011874215573, -1.999271364452784638, -0.6623750905550094270 ) ) ;
#53098=CARTESIAN_POINT ( 'NONE',  ( 4.885902211565920972, -0.8344178305333300738, 1.560695085661115922 ) ) ;
#53101=CARTESIAN_POINT ( 'NONE',  ( 0.7621917111494004304, 1.134545731666029011, 1.991736209811171054 ) ) ;
#53102=CARTESIAN_POINT ( 'NONE',  ( 0.05802509242504564485, -1.552030147408272054, -0.7874549631982865616 ) ) ;
#53104=CARTESIAN_POINT ( 'NONE',  ( 6.386699327874667098, 1.908680410311427433, -1.076638258889956345 ) ) ;
#53108=CARTESIAN_POINT ( 'NONE',  ( 6.777786256569462431, -2.009253640576996514, 0.4989836931604470505 ) ) ;
#53109=CARTESIAN_POINT ( 'NONE',  ( 1.639861632979456418, 2.010800986640928656, -0.1531718788195315928 ) ) ;
#53111=CARTESIAN_POINT ( 'NONE',  ( 4.951747152513418904, 0.6024649636334912239, -1.829943702413504791 ) ) ;
#53113=CARTESIAN_POINT ( 'NONE',  ( 1.354101172232239580, -1.613524214714330940, -1.527088627841047375 ) ) ;
#53122=CARTESIAN_POINT ( 'NONE',  ( 4.616618505336416156, -0.07905358554981949115, 1.738770568734932853 ) ) ;
#53123=CARTESIAN_POINT ( 'NONE',  ( 1.996468121258226924, 1.940055844723225009, 0.2909814450420752929 ) ) ;
#53130=CARTESIAN_POINT ( 'NONE',  ( 6.197705743426439540, -1.420020466879829302, -1.353909852041992767 ) ) ;
#53134=CARTESIAN_POINT ( 'NONE',  ( 1.499281897245376527, 1.848817473390499844, -1.303928773892924609 ) ) ;
#53136=VERTEX_POINT ( 'NONE', #131367 ) ;
#53138=CARTESIAN_POINT ( 'NONE',  ( 1.809613641711980359, -1.857008771552502768, 0.2239427725650791623 ) ) ;
#53139=CARTESIAN_POINT ( 'NONE',  ( 0.2989044949552251418, 1.198067244415670141, -1.254020425504979164 ) ) ;
#53141=CARTESIAN_POINT ( 'NONE',  ( 4.704715985517350596, 1.906866092115505840, 1.080010033982371498 ) ) ;
#53142=CARTESIAN_POINT ( 'NONE',  ( 5.034332918631054810, 1.191367258472323831, -1.976142064534849307 ) ) ;
#53143=CARTESIAN_POINT ( 'NONE',  ( 1.463821189631772990, 2.030551501382936497, -0.3513165408277911794 ) ) ;
#53144=CARTESIAN_POINT ( 'NONE',  ( 3.152217820003437421, -1.470166820979129207, 1.268861441860974049 ) ) ;
#53146=CARTESIAN_POINT ( 'NONE',  ( 5.395714598229544023, -0.6742385858747660388, 1.744967798948720228 ) ) ;
#53148=CARTESIAN_POINT ( 'NONE',  ( 6.556017512941495262, 1.755498886817616677, -0.9912500394320120645 ) ) ;
#53152=CARTESIAN_POINT ( 'NONE',  ( 4.430314669760617718, -1.560499787156752971, -1.277043788614096176 ) ) ;
#53156=CARTESIAN_POINT ( 'NONE',  ( 1.646812808029130215, -1.543121136568927243, 0.9753659028155501343 ) ) ;
#53166=CARTESIAN_POINT ( 'NONE',  ( 5.795571226005820087, 1.865288689459403848, -0.7749498061812712946 ) ) ;
#53167=CARTESIAN_POINT ( 'NONE',  ( 0.5398874254142792539, -2.012210497580559476, 0.6691108114003360141 ) ) ;
#53171=CARTESIAN_POINT ( 'NONE',  ( 5.084866380259029484, -0.2499542577577648639, -2.045595823183245621 ) ) ;
#53172=CARTESIAN_POINT ( 'NONE',  ( 4.606092368833686557, -0.09613688574180989654, 2.014232646917232916 ) ) ;
#53173=VERTEX_POINT ( 'NONE', #197362 ) ;
#53174=ORIENTED_EDGE ( 'NONE', *, *, #185954, .T. ) ;
#53178=ORIENTED_EDGE ( 'NONE', *, *, #151345, .F. ) ;
#53180=CARTESIAN_POINT ( 'NONE',  ( 5.518907608433407219, 2.013924273726455549, -0.09612181791086168992 ) ) ;
#53181=CARTESIAN_POINT ( 'NONE',  ( 3.960763856159645879, 0.2235175650571289141, -1.827449369368571386 ) ) ;
#53182=CARTESIAN_POINT ( 'NONE',  ( -0.02319159430947542386, 0.2540490248266329965, -1.846305437520213477 ) ) ;
#53183=CARTESIAN_POINT ( 'NONE',  ( 1.647554839532150872, -1.947651944554330772, 1.237524531948221096 ) ) ;
#53185=CARTESIAN_POINT ( 'NONE',  ( 4.376362478467909156, -1.248523626585487989, 1.764366501186130698 ) ) ;
#53187=CARTESIAN_POINT ( 'NONE',  ( -0.05917297228825654093, -1.501800262597710267, -1.231000148999121357 ) ) ;
#53188=CARTESIAN_POINT ( 'NONE',  ( 2.676970549635893537, 1.727063564601112100, -1.040793759654296213 ) ) ;
#53192=CARTESIAN_POINT ( 'NONE',  ( 3.819104250046548632, -0.1383300533824398659, 1.865606469731183825 ) ) ;
#53193=CARTESIAN_POINT ( 'NONE',  ( 6.631714602856194851, -1.287423518921044341, -1.493153376739835947 ) ) ;
#53196=CARTESIAN_POINT ( 'NONE',  ( 1.541937560865791479, -1.600244427420342896, -1.519961040588948986 ) ) ;
#53202=CARTESIAN_POINT ( 'NONE',  ( 6.789933821422706295, -0.8420773930338676383, 1.780570074765168043 ) ) ;
#53203=CARTESIAN_POINT ( 'NONE',  ( 0.3765545373161778286, 1.332373789618445770, 1.883912488508274752 ) ) ;
#53204=CARTESIAN_POINT ( 'NONE',  ( 0.4671467121175364445, 1.705069321186868159, 0.9702857188121425391 ) ) ;
#53205=CARTESIAN_POINT ( 'NONE',  ( 4.522371018022923295, 0.9678747400500853360, 1.821345444039919270 ) ) ;
#53214=CARTESIAN_POINT ( 'NONE',  ( 6.602019255160630706, 0.8372048429528687885, -2.003470777635954381 ) ) ;
#53216=CARTESIAN_POINT ( 'NONE',  ( 5.618664544990171095, -0.03892770779775727580, 1.841008343696965310 ) ) ;
#53224=CARTESIAN_POINT ( 'NONE',  ( 1.629408300089077111, -0.2329066467734331181, 1.897959532673603844 ) ) ;
#53225=CARTESIAN_POINT ( 'NONE',  ( 1.709447022217532641, -1.756973726300320449, 0.2123998563456699906 ) ) ;
#53226=CARTESIAN_POINT ( 'NONE',  ( 5.883453010584854148, 0.1459518013421389204, -2.007843741401983184 ) ) ;
#53228=CARTESIAN_POINT ( 'NONE',  ( 4.306187113567048641, 1.175507255964372222, -1.512451795395561405 ) ) ;
#53231=CARTESIAN_POINT ( 'NONE',  ( 5.125436402459787821, 0.1948648891074710732, -1.959901157258244098 ) ) ;
#53232=CARTESIAN_POINT ( 'NONE',  ( 0.3871773095200456982, -1.998849835692744659, -0.7086421328065874992 ) ) ;
#53234=CARTESIAN_POINT ( 'NONE',  ( 4.240975883383619305, -1.627667033997456381, 0.9218181776217827528 ) ) ;
#53235=CARTESIAN_POINT ( 'NONE',  ( 6.340463942928090901, 1.707257656261139234, 0.2451334271395839426 ) ) ;
#53237=CARTESIAN_POINT ( 'NONE',  ( 3.651171877326536030, -1.804458330144659950, 1.270265763067345066 ) ) ;
#53241=CARTESIAN_POINT ( 'NONE',  ( 0.8188879582939897483, -1.495318261269963589, 1.421039783695568604 ) ) ;
#53247=ORIENTED_EDGE ( 'NONE', *, *, #910, .F. ) ;
#53248=CARTESIAN_POINT ( 'NONE',  ( 2.945825538390862697, 1.462269270728074222, 1.465923284304726737 ) ) ;
#53252=CARTESIAN_POINT ( 'NONE',  ( 0.9088601047923352549, -0.4930153254206064428, -1.958433058913966018 ) ) ;
#53255=CARTESIAN_POINT ( 'NONE',  ( 0.07499057489264349119, 0.2503043380940940810, -1.990932473338621778 ) ) ;
#53257=CARTESIAN_POINT ( 'NONE',  ( 6.626327358740755180, 0.3474107405085808953, -1.985797104380654376 ) ) ;
#53258=CARTESIAN_POINT ( 'NONE',  ( 5.577321932364699641, 1.455147452656019524, 1.246156846922679584 ) ) ;
#53259=CARTESIAN_POINT ( 'NONE',  ( 6.539320575229251808, 6.034535422585679321, 2.798157489527762554 ) ) ;
#53260=CARTESIAN_POINT ( 'NONE',  ( 4.212563348414651188, 2.004022095860341413, 0.8874167208733558798 ) ) ;
#53262=CARTESIAN_POINT ( 'NONE',  ( 3.129067941553372645, 1.730785544086024696, 0.8136490247460312908 ) ) ;
#53266=CARTESIAN_POINT ( 'NONE',  ( 0.6851730022342136239, 1.650096953764205399, 1.158669022729153175 ) ) ;
#53268=CARTESIAN_POINT ( 'NONE',  ( 5.776942576169182608, 2.025397260235710206, -0.8375503648087383457 ) ) ;
#53270=CARTESIAN_POINT ( 'NONE',  ( 3.311258828109595154, -0.3375135790737812114, 1.691226829923969666 ) ) ;
#53272=CARTESIAN_POINT ( 'NONE',  ( -0.1405533004718313439, 1.431097497908106808, -1.984188993888830632 ) ) ;
#53276=CARTESIAN_POINT ( 'NONE',  ( 1.381223342121252085, -0.05156877537583307025, 1.961363007973878858 ) ) ;
#53278=CARTESIAN_POINT ( 'NONE',  ( 0.1755611466353291517, 1.991966693188641280, -2.657903234774192658 ) ) ;
#53282=CARTESIAN_POINT ( 'NONE',  ( 4.336430608486574911, 1.111010274217393956, -1.430681851146862416 ) ) ;
#53286=CARTESIAN_POINT ( 'NONE',  ( 5.197853184559683370, 1.220981990389960581, 1.338314830865680261 ) ) ;
#53290=CARTESIAN_POINT ( 'NONE',  ( 5.160548226176637776, -0.6268552802725676498, -1.752456121274186263 ) ) ;
#53292=CARTESIAN_POINT ( 'NONE',  ( 2.653800294728881681, 1.026947457930127872, 1.616878242289141676 ) ) ;
#53301=CARTESIAN_POINT ( 'NONE',  ( 0.08116279290028630133, -0.1557560750096824431, -2.127278773206460638 ) ) ;
#53303=CARTESIAN_POINT ( 'NONE',  ( 2.572312895708084302, -2.000810251872984225, -0.6062274732134291799 ) ) ;
#53305=CARTESIAN_POINT ( 'NONE',  ( 0.4635302585514287088, 1.806487598472360956, -0.2625014351145052438 ) ) ;
#53307=CARTESIAN_POINT ( 'NONE',  ( 2.309345278970798887, -0.4025885200794159235, 1.780468244869021222 ) ) ;
#53309=CARTESIAN_POINT ( 'NONE',  ( 1.986440140746603911, -1.173720106059353396, 1.509789020923378189 ) ) ;
#53310=CARTESIAN_POINT ( 'NONE',  ( 2.242574321144190641, -1.930940592676654965, -0.3871509593617681322 ) ) ;
#53311=CARTESIAN_POINT ( 'NONE',  ( 4.265135581495039574, 1.882949608596860669, -0.4750026310351186387 ) ) ;
#53314=CARTESIAN_POINT ( 'NONE',  ( 4.236665939827915395, 1.302216991916404387, -1.673619383358643908 ) ) ;
#53322=CARTESIAN_POINT ( 'NONE',  ( 3.527797039230845311, -1.088449851438414218, -1.465592618984489670 ) ) ;
#53327=CARTESIAN_POINT ( 'NONE',  ( 4.873830839387755631, 1.077430855447782942, 1.529020332772989210 ) ) ;
#53329=CARTESIAN_POINT ( 'NONE',  ( 1.770020429662170658, 0.9901332625182661662, 1.652458556229096320 ) ) ;
#53330=CARTESIAN_POINT ( 'NONE',  ( 6.297705697576845729, -1.418553083497756884, -1.355282376159852475 ) ) ;
#53336=CARTESIAN_POINT ( 'NONE',  ( 1.388444276177196235, -0.7657061372807508759, -1.974083799386998406 ) ) ;
#53340=CARTESIAN_POINT ( 'NONE',  ( 6.069205674026176389, 1.823072449729469247, 0.9810699074010442722 ) ) ;
#53341=CARTESIAN_POINT ( 'NONE',  ( 0.8898994657863326108, -0.4472179738511591895, -1.785967584704901912 ) ) ;
#53343=CARTESIAN_POINT ( 'NONE',  ( 6.223268877717999636, 2.273007049229976761, 0.3419319510214839930 ) ) ;
#53347=CARTESIAN_POINT ( 'NONE',  ( 1.289493641233057319, 1.738593318175378766, 1.494007209952723958 ) ) ;
#53350=CARTESIAN_POINT ( 'NONE',  ( 5.876890087061106271, 1.793433424740819904, -0.7452851482259108540 ) ) ;
#53353=CARTESIAN_POINT ( 'NONE',  ( 0.2990880961862537601, -0.2507095357664780866, -1.997497332983847906 ) ) ;
#53357=CARTESIAN_POINT ( 'NONE',  ( 3.029325995398450821, -1.404573224648179242, -1.548692548079745546 ) ) ;
#53358=CARTESIAN_POINT ( 'NONE',  ( 0.9183970251232485005, 1.633131562045697649, 0.6825882272994202582 ) ) ;
#53362=CARTESIAN_POINT ( 'NONE',  ( 3.996227152750064349, -0.7175114184741685497, -2.177131142417339849 ) ) ;
#53363=CARTESIAN_POINT ( 'NONE',  ( 3.644249385861945800, -1.421566135898670646, 1.003629588703761621 ) ) ;
#53366=CARTESIAN_POINT ( 'NONE',  ( 3.426783358884141428, 0.7772304037446680081, 1.549921577765429825 ) ) ;
#53367=CARTESIAN_POINT ( 'NONE',  ( 4.106061665437168884, 0.7349691374628541940, -2.043110004675054103 ) ) ;
#53369=CARTESIAN_POINT ( 'NONE',  ( 4.874232570624013050, -2.001857581374043349, -0.2420344392276354561 ) ) ;
#53370=CARTESIAN_POINT ( 'NONE',  ( 3.437500000000002665, 1.451031289060976448, -1.451031289061255780 ) ) ;
#53372=CARTESIAN_POINT ( 'NONE',  ( 1.975490806028988633, 1.844176287694970995, -0.5568081592420818238 ) ) ;
#53374=CARTESIAN_POINT ( 'NONE',  ( 4.359788498249434596, -1.718402401499378840, -1.407797849641032828 ) ) ;
#53376=CARTESIAN_POINT ( 'NONE',  ( -0.2108831679770961920, 2.882544375557041239, -2.385815782126240236 ) ) ;
#53381=CARTESIAN_POINT ( 'NONE',  ( 0.4521970297205242240, -1.575145348204033180, -1.566492488853583387 ) ) ;
#53382=CARTESIAN_POINT ( 'NONE',  ( 5.547302793442128177, 1.730978599593002043, -0.9233319674036490898 ) ) ;
#53384=CARTESIAN_POINT ( 'NONE',  ( 6.643838010208884981, 0.8751278368869718216, -2.086507859592637626 ) ) ;
#53387=CARTESIAN_POINT ( 'NONE',  ( 3.174340740746087075, -1.014436240984006865, -1.795896229016210821 ) ) ;
#53391=CARTESIAN_POINT ( 'NONE',  ( 5.536355731483205922, 1.842701317132239724, 0.3206550288221421963 ) ) ;
#53392=CARTESIAN_POINT ( 'NONE',  ( 4.183993884235046146, 1.395953275470160682, 1.028640563475995640 ) ) ;
#53393=CARTESIAN_POINT ( 'NONE',  ( 3.245385237338119566, 1.740626721681370670, -0.003331538806947489072 ) ) ;
#53394=CARTESIAN_POINT ( 'NONE',  ( 2.173718093399327422, 1.413494431062709333, 1.804626757829434380 ) ) ;
#53396=CARTESIAN_POINT ( 'NONE',  ( 5.267163683669145335, 2.014557126142228594, -0.5589344999666242542 ) ) ;
#53397=CARTESIAN_POINT ( 'NONE',  ( 6.492136518976993287, -0.5202676277693082385, -1.870896455867506747 ) ) ;
#53400=CARTESIAN_POINT ( 'NONE',  ( 1.406875202279284753, -1.122500148236497575, -1.674886495921081631 ) ) ;
#53401=CARTESIAN_POINT ( 'NONE',  ( 0.2874129202556953144, 1.626693421326959710, 1.468627725614686463 ) ) ;
#53405=CARTESIAN_POINT ( 'NONE',  ( 2.737105750116640923, 1.997451989420237606, 0.7121958652205606644 ) ) ;
#53407=CARTESIAN_POINT ( 'NONE',  ( 5.672426548614882158, -1.154804106291613675, 1.414059844683832834 ) ) ;
#53414=CARTESIAN_POINT ( 'NONE',  ( 2.092062652781300880, 1.246029564253118282, 1.589516146451919631 ) ) ;
#53415=CARTESIAN_POINT ( 'NONE',  ( 0.2179827029432715169, -2.065224962065722369, 0.4112614876821736321 ) ) ;
#53417=CARTESIAN_POINT ( 'NONE',  ( 4.135495018730405370, 1.753490048523008049, -0.6236645969141580981 ) ) ;
#53423=CARTESIAN_POINT ( 'NONE',  ( 5.531824841778981927, -1.161409778037244100, -1.408645805323349487 ) ) ;
#53427=CARTESIAN_POINT ( 'NONE',  ( 1.317307599089176939, -1.370793471230176808, 1.061547382435957587 ) ) ;
#53428=CARTESIAN_POINT ( 'NONE',  ( 6.439398882927052981, 0.6998097629446423662, -1.703160347957879850 ) ) ;
#53429=CARTESIAN_POINT ( 'NONE',  ( 6.041700318104039624, -1.667111694969125368, -1.595929347687746747 ) ) ;
#53432=CARTESIAN_POINT ( 'NONE',  ( 1.106794710556399997, 1.562239816646590285, -1.344093658231941824 ) ) ;
#53434=CARTESIAN_POINT ( 'NONE',  ( 0.5970295589228531430, 1.038836743281198238, -1.727736137786803461 ) ) ;
#53438=CARTESIAN_POINT ( 'NONE',  ( 0.1277242839827036902, -1.211146277544056460, -1.556326691921037675 ) ) ;
#53440=CARTESIAN_POINT ( 'NONE',  ( 3.392734571251673881, -1.844325299564765652, -0.5055192353106837677 ) ) ;
#53442=CARTESIAN_POINT ( 'NONE',  ( 5.373716497573798101, 2.127666891504222058, -0.5857064233696291922 ) ) ;
#53447=CARTESIAN_POINT ( 'NONE',  ( 5.988958055669808545, -2.013456733998910231, -0.6654305520411086805 ) ) ;
#53449=CARTESIAN_POINT ( 'NONE',  ( 3.118547318853508887, -1.136067310315771905, -2.008477146686512782 ) ) ;
#53450=CARTESIAN_POINT ( 'NONE',  ( 4.228923158279327410, -1.829750178516520442, -0.7082015076659909925 ) ) ;
#53452=CARTESIAN_POINT ( 'NONE',  ( 0.6374591745182572877, 1.832550977151351290, -0.7006947966294306829 ) ) ;
#53457=CARTESIAN_POINT ( 'NONE',  ( 5.823453932400854960, -1.463924103857511039, -1.387103351090559711 ) ) ;
#53461=CARTESIAN_POINT ( 'NONE',  ( 3.661125528703466525, 1.714762188600306825, -1.331539952715065978 ) ) ;
#53463=CARTESIAN_POINT ( 'NONE',  ( 0.5805319366703353134, 1.050441701016215923, 1.842106252469346117 ) ) ;
#53468=CARTESIAN_POINT ( 'NONE',  ( 1.634131612217240681, 1.018193428692963698, -1.791617596397138801 ) ) ;
#53474=CARTESIAN_POINT ( 'NONE',  ( 4.951771945676144426, -1.355037094400749487, -1.349591858340569717 ) ) ;
#53478=CARTESIAN_POINT ( 'NONE',  ( -0.1407840215364779823, -1.400018645128609629, -1.149511601580233577 ) ) ;
#53480=CARTESIAN_POINT ( 'NONE',  ( 0.3037315811481311467, -1.027229472348114347, -1.616837036282785078 ) ) ;
#53481=CARTESIAN_POINT ( 'NONE',  ( 1.891162872569674080, 0.2007839719405465906, 2.060584128686280714 ) ) ;
#53483=CARTESIAN_POINT ( 'NONE',  ( 0.3738188115672124168, 1.133047686669987675, 1.613170723887060065 ) ) ;
#53484=CARTESIAN_POINT ( 'NONE',  ( 2.965264444195826243, 0.2674972279559268973, -1.805858685475017378 ) ) ;
#53485=CARTESIAN_POINT ( 'NONE',  ( 0.1535068347273665368, -1.849414538273885578, 1.380102022147772667 ) ) ;
#53489=CARTESIAN_POINT ( 'NONE',  ( 4.229007335028351910, -1.923526752047514110, -0.7451934795693700986 ) ) ;
#53494=CARTESIAN_POINT ( 'NONE',  ( 5.596739085487917542, -0.5086175864091507792, -2.043493955398622219 ) ) ;
#53497=CARTESIAN_POINT ( 'NONE',  ( 0.2214384409217939054, -1.939739064610836339, -0.9756505802681545436 ) ) ;
#53499=CARTESIAN_POINT ( 'NONE',  ( 3.444745247808535638, 0.5215555581963465803, 2.097624034931542703 ) ) ;
#53500=CARTESIAN_POINT ( 'NONE',  ( 4.336585317048437638, 1.240917556630851237, -1.593414756171371183 ) ) ;
#53501=FACE_OUTER_BOUND ( 'NONE', #213478, .T. ) ;
#53508=CARTESIAN_POINT ( 'NONE',  ( 1.956267901341804283, -1.236798062192035363, 1.592663274815858676 ) ) ;
#53513=SURFACE_STYLE_USAGE ( .BOTH. , #51393 ) ;
#53516=CARTESIAN_POINT ( 'NONE',  ( 4.411732571322396268, -1.242743209197882059, -1.587826168943158089 ) ) ;
#53518=CARTESIAN_POINT ( 'NONE',  ( 0.2402810872906081530, 0.2891477966728701610, 1.700304936625576024 ) ) ;
#53523=CARTESIAN_POINT ( 'NONE',  ( 5.800035319642947051, -1.870726058474009079, -0.0005997126256013227737 ) ) ;
#53524=CARTESIAN_POINT ( 'NONE',  ( 0.1178376421791422907, -0.5346926475991298222, 1.940734443874014836 ) ) ;
#53529=CARTESIAN_POINT ( 'NONE',  ( 1.194935658704935566, 1.779638138761422628, 0.9480210990304924756 ) ) ;
#53531=CARTESIAN_POINT ( 'NONE',  ( 1.705023097204850346, 1.575028893885391579, -0.8949447657340557916 ) ) ;
#53537=CARTESIAN_POINT ( 'NONE',  ( 6.450803866275835574, -1.753708343991422502, -0.7711757456045026382 ) ) ;
#53546=CARTESIAN_POINT ( 'NONE',  ( 4.610339536224768331, -0.9213992672730474398, -1.955631277330005968 ) ) ;
#53550=CARTESIAN_POINT ( 'NONE',  ( 0.2816890862925770511, 0.2015970107726860194, -2.110973810222869229 ) ) ;
#53551=CARTESIAN_POINT ( 'NONE',  ( 5.754876975610782708, -1.437719105923901841, 1.124948175183659638 ) ) ;
#53552=CARTESIAN_POINT ( 'NONE',  ( 1.985558396190547858, 1.356547016436062014, 1.430631702862941168 ) ) ;
#53553=CARTESIAN_POINT ( 'NONE',  ( 4.166199421025416960, 1.911861072351704882, -0.05224187775455800542 ) ) ;
#53556=CARTESIAN_POINT ( 'NONE',  ( 6.092246201825009422, 0.9720536035879873138, -1.712898845271645820 ) ) ;
#53557=CARTESIAN_POINT ( 'NONE',  ( 0.3923911919363164413, 1.615042221312415371, -1.078049841609552306 ) ) ;
#53564=CARTESIAN_POINT ( 'NONE',  ( 4.705663775918221603, 1.419457463540532816, 1.281590252682027087 ) ) ;
#53566=CARTESIAN_POINT ( 'NONE',  ( 0.9564373720404686363, 2.204146663617879476, -0.1098798544595935567 ) ) ;
#53568=CARTESIAN_POINT ( 'NONE',  ( 6.498696042004469930, -1.974701156420979542, -0.3904368389309967324 ) ) ;
#53570=CARTESIAN_POINT ( 'NONE',  ( -0.02338929933911031503, 1.420967854922173368, -1.971839201816010911 ) ) ;
#53573=CARTESIAN_POINT ( 'NONE',  ( 3.209495720308676248, -1.691010085789945716, -1.194244797349801157 ) ) ;
#53577=CARTESIAN_POINT ( 'NONE',  ( 1.042116488573753497, 0.8753402851892390091, -1.976733581976031218 ) ) ;
#53582=CARTESIAN_POINT ( 'NONE',  ( 6.825078400183573812, 0.002648415797040087893, 1.855566311045192540 ) ) ;
#53585=CARTESIAN_POINT ( 'NONE',  ( 5.590364566445758854, -0.4131642248683431440, 1.684076740667529881 ) ) ;
#53587=CARTESIAN_POINT ( 'NONE',  ( 3.291909242638372923, -1.386922682245657734, -1.537212927083357217 ) ) ;
#53588=CARTESIAN_POINT ( 'NONE',  ( 4.464542613241986757, -2.054094600764106548, -0.5127786416893320709 ) ) ;
#53592=CARTESIAN_POINT ( 'NONE',  ( 2.694150338025066205, 0.9325801345280826382, -1.734679099899273824 ) ) ;
#53593=CARTESIAN_POINT ( 'NONE',  ( 0.4922593472763935329, -1.060406550076501642, 1.591262010887870115 ) ) ;
#53594=CARTESIAN_POINT ( 'NONE',  ( 5.191491443341288203, -0.8287821522852161227, 2.137368679509048963 ) ) ;
#53595=CARTESIAN_POINT ( 'NONE',  ( 3.193790821891542286, -0.7392406677243366087, 1.669511829839696038 ) ) ;
#53599=CARTESIAN_POINT ( 'NONE',  ( 4.324480843662709795, -0.8647720088908043001, -1.818167814553457884 ) ) ;
#53601=CARTESIAN_POINT ( 'NONE',  ( 3.555471618195928496, 1.543666060651678551, 1.210462546525910010 ) ) ;
#53605=CARTESIAN_POINT ( 'NONE',  ( 6.193323979940683621, -0.7056316722037699884, 1.968093674265839477 ) ) ;
#53606=CARTESIAN_POINT ( 'NONE',  ( 4.908955397393719444, 1.540865433829426090, 0.8705488387463419242 ) ) ;
#53609=CARTESIAN_POINT ( 'NONE',  ( 0.3752731597879420677, 2.043270790221253908, -0.7926104125151807178 ) ) ;
#53610=CARTESIAN_POINT ( 'NONE',  ( 6.316323101372843141, 1.626595589989995982, 0.6193309307870945579 ) ) ;
#53612=CARTESIAN_POINT ( 'NONE',  ( 0.1333692844072559280, 6.947498546895843674, -2.648624074793118233 ) ) ;
#53613=CARTESIAN_POINT ( 'NONE',  ( 0.5040132504689893711, -0.5763820916803040761, -1.625860608634047244 ) ) ;
#53614=( BOUNDED_CURVE ( )  B_SPLINE_CURVE ( 3, ( #181139, #169154, #100945, #51145 ),
 .UNSPECIFIED., .F., .T. ) 
 B_SPLINE_CURVE_WITH_KNOTS ( ( 4, 4 ),
 ( 0.4999999999999957812, 1.000000000000000000 ),
 .UNSPECIFIED. ) 
 CURVE ( )  GEOMETRIC_REPRESENTATION_ITEM ( )  RATIONAL_B_SPLINE_CURVE ( ( 1.000000000000005773, 0.3333333333333334259, 0.3333333333333278192, 1.000000000000000222 ) ) 
 REPRESENTATION_ITEM ( '' )  );
#53615=CARTESIAN_POINT ( 'NONE',  ( 0.9959476074029065540, -2.191739723303194332, 0.005169097091584088505 ) ) ;
#53616=CARTESIAN_POINT ( 'NONE',  ( 2.684424123961434816, -1.133677649706768431, 1.893296980138805097 ) ) ;
#53617=CARTESIAN_POINT ( 'NONE',  ( 6.707499178395360140, -1.739742505839674047, -1.298780901186733505 ) ) ;
#53619=CARTESIAN_POINT ( 'NONE',  ( 1.147838861943322630, 2.084982156806517661, -0.3680304603586990742 ) ) ;
#53620=CARTESIAN_POINT ( 'NONE',  ( 3.625000000000002665, -2.052068128417946280, 2.068584262981140017E-13 ) ) ;
#53622=CARTESIAN_POINT ( 'NONE',  ( 6.727182134110178069, 2.947419669445831669, 2.641212418657997496 ) ) ;
#53623=CARTESIAN_POINT ( 'NONE',  ( 5.438475939130889891, 1.897888883619626821, 0.3293186976999362137 ) ) ;
#53625=CARTESIAN_POINT ( 'NONE',  ( 1.066458480799619135, -1.449176446249898831, 1.776219484066744903 ) ) ;
#53629=CARTESIAN_POINT ( 'NONE',  ( 4.055513949679364849, -1.932427950605047018, 1.095304516859375799 ) ) ;
#53634=CARTESIAN_POINT ( 'NONE',  ( 1.529922885524274134, -1.701946718671920600, 1.081067414773040802 ) ) ;
#53636=CARTESIAN_POINT ( 'NONE',  ( 1.481379835429663228, -0.05473030402166743219, 2.062018025990194126 ) ) ;
#53639=CARTESIAN_POINT ( 'NONE',  ( 0.1515692981730529243, 0.7036590017722235135, 1.701685288394996665 ) ) ;
#53642=CARTESIAN_POINT ( 'NONE',  ( 2.741159958678766717, -1.308340514575502045, -1.191892431489706805 ) ) ;
#53643=CARTESIAN_POINT ( 'NONE',  ( 1.318982659667154334, 0.9913977828604101372, -1.755770081111128977 ) ) ;
#53644=CARTESIAN_POINT ( 'NONE',  ( -0.05938221139379848412, -1.422385081007140117, -1.168950373246782526 ) ) ;
#53645=CARTESIAN_POINT ( 'NONE',  ( 5.126663105998436443, 0.1666055143465100530, 2.286395203598155845 ) ) ;
#53646=CARTESIAN_POINT ( 'NONE',  ( 3.732213890823964597, 0.2717154217161937280, 1.820854149191558635 ) ) ;
#53649=CARTESIAN_POINT ( 'NONE',  ( 3.645350208285046634, -1.381898811119431691, -1.193016960613018096 ) ) ;
#53650=CARTESIAN_POINT ( 'NONE',  ( 5.467422714486909641, -1.967887220244109558, -0.4390321945699494632 ) ) ;
#53652=CARTESIAN_POINT ( 'NONE',  ( 3.432755235230527280, 2.206939294067700619, 0.4977334550177249795 ) ) ;
#53654=CARTESIAN_POINT ( 'NONE',  ( 0.1004013553109489865, -2.105664478878019441, -0.04916207707313274139 ) ) ;
#53656=CARTESIAN_POINT ( 'NONE',  ( 3.332542965736586371, -1.235447621225284509, 1.661183390374972424 ) ) ;
#53659=CARTESIAN_POINT ( 'NONE',  ( 5.514351353798126354, -2.120667953778174741, 0.0001357579994532010219 ) ) ;
#53662=CARTESIAN_POINT ( 'NONE',  ( 2.016120517293042536, -0.9081000056256024466, -1.699051532819460197 ) ) ;
#53663=B_SPLINE_CURVE_WITH_KNOTS ( 'NONE', 3,
 ( #34844, #148624, #191, #66260, #132408, #150766, #198410, #33790, #165932, #64177, #17517, #67326, #205077, #207225, #154220, #170457, #57783, #56719, #122887, #54582, #105494, #139050, #25274, #75104, #104408, #24190, #9030, #141215, #40482, #140129, #42627, #188846, #58849, #6869, #155287, #38331, #7948, #5792, #125005, #71869, #74038, #190962, #91376, #206155, #123944, #108737, #186703, #23119, #174765, #189912, #26338, #106585, #187768, #41557, #70799, #89236, #156363, #171526, #120730, #22042, #172614, #90293, #107670, #173698, #157436, #88152, #92452, #4724, #55645, #136912, #137978, #202939, #203996, #121801, #39399, #72948, #63119, #146536, #30635, #62062, #143343, #47968, #59911, #158491, #110868, #196324, #144418, #60986, #210420, #160619, #192029, #80437, #145488, #128217, #211483, #208280, #113009, #78292, #29561, #10090, #176873, #114084, #28485, #127139, #43692, #31698, #180075, #126067, #76164, #94576, #142269, #194179, #193111, #45824, #12220, #109809, #212555, #129284, #111945, #44760, #64194, #177947, #95653, #209337, #77224, #161703, #175818, #27411, #93509, #13296, #79369, #195259, #46894, #159550, #11147, #179018, #96720, #162769, #14347, #130335, #99886, #181127, #147581, #66277, #67342, #65225, #149703, #185381, #201613, #85761, #17532, #1284, #133487, #148641, #168083, #132425, #198426, #84695, #97773, #213599, #165948, #83621, #151841, #32748, #49013, #150782, #199490, #51135, #131375, #50072, #3418, #182179, #98830, #200552, #163833, #16474, #102014, #15412, #115132, #164880, #197371, #69484, #117257, #33807, #82554, #100934, #207, #19683, #116193, #167021, #183256, #135592, #118325, #18615, #2345, #53262, #34860, #68421, #119393, #134548, #81502, #52199, #184311, #35935, #157177, #56465, #4472, #153970, #152893, #120475, #156106, #6619, #72699, #204814, #122627, #70543, #206967, #57535, #87897, #55394, #173437, #155034, #137730, #71618, #172353, #5537, #8771, #188589, #136662, #203750, #202687, #186448, #7691, #138794, #40221, #106332, #23943, #54336, #58597, #123693, #121549, #189654, #38084, #187520, #124752, #37001, #39151, #73774, #140956, #105232, #171273, #104156, #103083, #169139, #170204, #20734, #22866, #74854, #88980, #90047, #139870, #21788, #86829, #205901, #25016, #41305, #107413, #91118, #14872, #159291, #175562, #109558, #93257, #75913, #42373, #9837, #76965, #27153, #143092, #10890, #92199, #66802, #163290, #130849, #48484, #158249, #142016, #65743, #59659, #26084, #209084, #80964, #208031, #31164, #190712, #83079, #181645, #113539, #97237, #147055, #63652, #47424, #129807, #131890, #108484, #179543, #195786, #191778, #213076, #33272, #125816, #43434, #32217, #64706, #196846, #114602, #180593, #99357, #98291, #164352, #82021, #15937, #197898, #49527, #148112, #214116, #17004, #115650, #165407, #149158, #736, #174508, #136129, #134018, #137202, #200025, #202144, #150245, #38620, #153440, #53804, #121022, #100409, #182716, #101476, #102544, #166478, #184842, #6088, #22334, #186989, #52724, #36471, #168608, #183790, #203225, #167547, #19146, #119934, #132943, #34334, #51677, #118857, #104697, #67871, #84158, #185910, #20210, #86298, #18070, #85221, #170748, #2878, #1813, #21264, #198948, #117798, #54869, #50591, #35398, #151310, #152367, #88448, #135070, #68948, #201083, #37545 ),
 .UNSPECIFIED., .F., .F.,
 ( 4, 1, 1, 1, 1, 1, 1, 1, 1, 1, 1, 1, 1, 1, 1, 1, 1, 1, 1, 1, 1, 1, 1, 1, 1, 1, 1, 1, 1, 1, 1, 1, 1, 1, 1, 1, 1, 1, 1, 1, 1, 1, 1, 1, 1, 1, 1, 1, 1, 1, 1, 1, 1, 1, 1, 1, 1, 1, 1, 1, 1, 1, 1, 1, 1, 1, 1, 1, 1, 1, 1, 1, 1, 1, 1, 1, 1, 1, 1, 1, 1, 1, 1, 1, 1, 1, 1, 1, 1, 1, 1, 1, 1, 1, 1, 1, 1, 1, 1, 1, 1, 1, 1, 1, 1, 1, 1, 1, 1, 1, 1, 1, 1, 1, 1, 1, 1, 1, 1, 1, 1, 1, 1, 1, 1, 1, 1, 1, 1, 1, 1, 1, 1, 1, 1, 1, 1, 1, 1, 1, 1, 1, 1, 1, 1, 1, 1, 1, 1, 1, 1, 1, 1, 1, 1, 1, 1, 1, 1, 1, 1, 1, 1, 1, 1, 1, 1, 1, 1, 1, 1, 1, 1, 1, 1, 1, 1, 1, 1, 1, 1, 1, 1, 1, 1, 1, 1, 1, 1, 1, 1, 1, 1, 1, 1, 1, 1, 1, 1, 1, 1, 1, 1, 1, 1, 1, 1, 1, 1, 1, 1, 1, 1, 1, 1, 1, 1, 1, 1, 1, 1, 1, 1, 1, 1, 1, 1, 1, 1, 1, 1, 1, 1, 1, 1, 1, 1, 1, 1, 1, 1, 1, 1, 1, 1, 1, 1, 1, 1, 1, 1, 1, 1, 1, 1, 1, 1, 1, 1, 1, 1, 1, 1, 1, 1, 1, 1, 1, 1, 1, 1, 1, 1, 1, 1, 1, 1, 1, 1, 1, 1, 1, 1, 1, 1, 1, 1, 1, 1, 1, 1, 1, 1, 1, 1, 1, 1, 1, 1, 1, 1, 1, 1, 1, 1, 1, 1, 1, 1, 1, 1, 1, 1, 1, 1, 1, 1, 1, 1, 1, 1, 1, 1, 1, 1, 1, 1, 1, 1, 1, 1, 1, 1, 1, 1, 1, 1, 1, 1, 1, 1, 1, 1, 1, 1, 1, 1, 1, 1, 1, 1, 1, 1, 1, 1, 1, 1, 1, 1, 1, 1, 1, 1, 1, 1, 1, 1, 1, 1, 1, 1, 1, 1, 1, 1, 1, 1, 1, 1, 1, 1, 1, 1, 1, 4 ),
 ( 0.000000000000000000, 0.002600137934918278840, 0.005208846947063642402, 0.007813284371963545236, 0.01041597565644012714, 0.01302123463190214131, 0.01562472912267370319, 0.01822934229245065652, 0.02083335053635077330, 0.02343730581734793095, 0.02604195799539401474, 0.02864545692284610826, 0.03125045498156164142, 0.03385385361191795006, 0.03645873261014952182, 0.03906243010681619693, 0.04166674480109257978, 0.04427107247243720900, 0.04687475664952634596, 0.04947964045798968619, 0.05208303702386667122, 0.05468803228817373241, 0.05729153353077973132, 0.05989618223844375006, 0.06250015876865079589, 0.06510412050499821135, 0.06770877833268285073, 0.07031227041168378045, 0.07291726700687002627, 0.07552066596874357218, 0.07812554330212571896, 0.08072923942118487295, 0.08333355289058355653, 0.08593787945419822938, 0.08854156225015286097, 0.09114644488045960113, 0.09374984019314609729, 0.09635483420994474246, 0.09895833431534489799, 0.1015629817166532611, 0.1041669571688737805, 0.1067709175595765864, 0.1093755742645453749, 0.1119790650618166516, 0.1145840604711090005, 0.1171874582687142119, 0.1197923343547293018, 0.1223960294069747767, 0.1250003415701952669, 0.1276046670722256471, 0.1302083485727723866, 0.1328132300777099817, 0.1354166241949035232, 0.1380216170238739992, 0.1406251160503516617, 0.1432297622036773077, 0.1458337366370238142, 0.1484376957407889386, 0.1510423513813509144, 0.1536458409560605698, 0.1562508352375901466, 0.1588542319300798034, 0.1614591068269417562, 0.1640628008713490293, 0.1666671117869774343, 0.1692714362859856492, 0.1718751165501164191, 0.1744799969878772505, 0.1770833899687347668, 0.1796883816679979429, 0.1822918796746371972, 0.1848965246383280081, 0.1875004981115827030, 0.1901044559872153150, 0.1927091106216977379, 0.1953125990329364348, 0.1979175922448092595, 0.2005209878913200294, 0.2031258616572126918, 0.2057295547527302204, 0.2083338644793258920, 0.2109381880338489224, 0.2135418671205281671, 0.2161467465492790951, 0.2187501384529311477, 0.2213551290805818306, 0.2239586261264417955, 0.2265632699588193688, 0.2291672425307399730, 0.2317711992370185270, 0.2343758529237242316, 0.2369793402305566954, 0.2395843324308542799, 0.2421877270904984059, 0.2447925997835804779, 0.2473962919891333490, 0.2500006005852301039, 0.2526049232537817546, 0.2552086012219486610, 0.2578134796998332035, 0.2604168705853860954, 0.2630218601994954719, 0.2656253563436123954, 0.2682299991029740149, 0.2708339708322964334, 0.2734379264279751531, 0.2760425792251849364, 0.2786460654866522724, 0.2812510567334335909, 0.2838544504653006673, 0.2864593221437078951, 0.2890630135181997962, 0.2916673210423081364, 0.2942716428833813125, 0.2968753197919519748, 0.2994801973770923054, 0.3020835873036303854, 0.3046885759622478540, 0.3072920712636373342, 0.3098967130082584398, 0.3125006839536987324, 0.3151046384975096371, 0.3177092904634842285, 0.3203127757386058927, 0.3229177660899096303, 0.3255211589530693228, 0.3281260296749167193, 0.3307297202772326306, 0.3333340267878420748, 0.3359383478599109463, 0.3385420237677806976, 0.3411469005182800607, 0.3437502895448679152, 0.3463552773060237788, 0.3489587718236830116, 0.3515634126118191150, 0.3541673828320756612, 0.3567713363827305639, 0.3593759875757128741, 0.3619794719234893932, 0.3645844614373360826, 0.3671878534908398217, 0.3697927233142242476, 0.3723964132032320795, 0.3750007187588132451, 0.3776050391203355505, 0.3802087140863810166, 0.3828135900603256703, 0.3854169782460106219, 0.3880219651677176973, 0.3906254589606275029, 0.3932300988505167960, 0.3958340684042725433, 0.3984380210204655492, 0.4010426714986830565, 0.4036461549780977487, 0.4062511437124918245, 0.4088545350153757196, 0.4114594039983773821, 0.4140630932329303349, 0.4166673978919369636, 0.4192717176013560643, 0.4218753916844373286, 0.4244802669398990425, 0.4270836543437129262, 0.4296886404839689866, 0.4322921336110964741, 0.4348967726609613837, 0.4375007416068860122, 0.4401046933472957945, 0.4427093431689624881, 0.4453128258389836835, 0.4479178138519160357, 0.4505212044632024293, 0.4531260726638874359, 0.4557297613028266636, 0.4583340651236982866, 0.4609383842394453867, 0.4635420574984087105, 0.4661469320934465421, 0.4687503187744080368, 0.4713553041911981989, 0.4739587967114984313, 0.4765634349795482838, 0.4791674033763006491, 0.4817713542995921694, 0.4843760035229108252, 0.4869794854424946973, 0.4895844727919445583, 0.4921878627706443576, 0.4947927302470669919, 0.4973964183492232127, 0.5000007213903868708, 0.5026050399708832384, 0.5052087124645624483, 0.5078135864572254077, 0.5104169724743423675, 0.5130219572256408123, 0.5156254491980594157, 0.5182300867424926016, 0.5208340546487225664, 0.5234380048135498509, 0.5260426534967141965, 0.5286461347248060383, 0.5312511214687432037, 0.5338545108738584899, 0.5364593776840630435, 0.5390630653082590928, 0.5416673676281316130, 0.5442716857317909662, 0.5468753575190105076, 0.5494802309673390006, 0.5520836163796108975, 0.5546886005233833128, 0.5572920920068584749, 0.5598967288858642810, 0.5625006963602153798, 0.5651046458252231286, 0.5677092940264200083, 0.5703127746219572858, 0.5729177608183441128, 0.5755211497088699169, 0.5781260159108934094, 0.5807297031159460721, 0.5833340047729366207, 0.5859383224581667937, 0.5885419935977430628, 0.5911468665597719996, 0.5937502514261915332, 0.5963552350203973340, 0.5989587260738620245, 0.6015633623456233536, 0.6041673294467342359, 0.6067712782705607655, 0.6093759260479724160, 0.6119794060698863225, 0.6145843917766802278, 0.6171877802116071399, 0.6197926458634805957, 0.6223963327082033814, 0.6250006337607152407, 0.6276049510859208480, 0.6302086216366651339, 0.6328134941704254279, 0.6354168785499811900, 0.6380218616525755726, 0.6406253523349600965, 0.6432299880576550777, 0.6458339548441623945, 0.6484379030854412473, 0.6510425504972472410, 0.6536460300044655281, 0.6562510152796211527, 0.6588544033179367654, 0.6614592684776883225, 0.6640629550208935195, 0.6666672555273263079, 0.6692715725509107427, 0.6718752425716313370, 0.6744801147351520143, 0.6770834986868305982, 0.6796884813557668714, 0.6822919717260003125, 0.6848966069578048543, 0.6875005734883452568, 0.6901045212057073108, 0.6927091683100871089, 0.6953126473615357517, 0.6979176322630067375, 0.7005210199636988655, 0.7031258846893556624, 0.7057295709898557812, 0.7083338710086078960, 0.7109381877889758838, 0.7135418573384794128, 0.7161467291897904985, 0.7187501127725786088, 0.7213550950658099703, 0.7239585851828231888, 0.7265632199819130888, 0.7291671863151253374, 0.7317711335672014705, 0.7343757804223364216, 0.7369792590769420615, 0.7395842436626837157, 0.7421876310847422831, 0.7447924954343322357, 0.7473961815509432283, 0.7500004811404139549, 0.7526047977359727748, 0.7552084668730677519, 0.7578133384702019359, 0.7604167217430886083, 0.7630217037185706985, 0.7656251936412983294, 0.7682298280658512724, 0.7708337942603785686, 0.7734377411058018792, 0.7760423877698768846, 0.7786458660865690495, 0.7812508504145402322, 0.7838542376169586046, 0.7864591016485131814, 0.7890627876400562180, 0.7916670868586475063, 0.7942714033278103214, 0.7968750721113085911, 0.7994799435123028930, 0.8020833265342820484, 0.8046883082499752815, 0.8072917980373575109, 0.8098964321455554005, 0.8125003982600473851, 0.8151043447574546352, 0.8177089912886614798, 0.8203124693263749156, 0.8229174534545398156, 0.8255208404963184643, 0.8281257042678743518, 0.8307293901931780411, 0.8333336890992975032, 0.8359380055004849153, 0.8385416739892034288, 0.8411465452521027508, 0.8437499280821748604, 0.8463549095960458679, 0.8489583993070312085, 0.8515630331570626099, 0.8541669992501779163, 0.8567709454582125295, 0.8593755919147509914, 0.8619790697324273276, 0.8645840537187589048, 0.8671874406589066275, 0.8697923042285079509, 0.8723959901464106714, 0.8750002887984731359, 0.8776046051901155165, 0.8802082734428797739, 0.8828131446257380111, 0.8854165273229123168, 0.8880215086929368340, 0.8906249983864840125, 0.8932296320365455955, 0.8958335981669537373, 0.8984375441442679078, 0.9010421905843485346, 0.9036456682409392815, 0.9062506521434200435, 0.9088540390409564074, 0.9114589024666573946, 0.9140625884360091824, 0.9166668868924389146, 0.9192712033329777377, 0.9218748714086243412, 0.9244797425695093773, 0.9270831251927963423, 0.9296881064769593195, 0.9322915962120889022, 0.9348962297203436966, 0.9375001959466012780, 0.9401041417521586174, 0.9427087882339971747, 0.9453122657876905643, 0.9479172496658602176, 0.9505206365780075606, 0.9531254999124115779, 0.9557291860198475764, 0.9583334843266348990, 0.9609378007344983041, 0.9635414689593263526, 0.9661463405142474148, 0.9687497214891268582, 0.9713547029754164841, 0.9739581985331400293, 0.9765628250748574768, 0.9791667834374845336, 0.9817707607320566021, 0.9843753697534296521, 0.9869788348889786400, 0.9895840831931937975, 0.9921867700316038263, 0.9947911815772807476, 0.9973998924267860611, 1.000000000000000000 ),
 .UNSPECIFIED. ) ;
#53666=CARTESIAN_POINT ( 'NONE',  ( 6.473500209388782345, -0.2444377345085078923, 1.954170833970412913 ) ) ;
#53670=CARTESIAN_POINT ( 'NONE',  ( 0.4576791451081770323, -1.901157720872756141, 1.148870853762502753 ) ) ;
#53671=CARTESIAN_POINT ( 'NONE',  ( 2.942513229011092690, 2.089901898437613870, 0.2590637233205703716 ) ) ;
#53674=CARTESIAN_POINT ( 'NONE',  ( 0.8185401059354965314, -1.351722143400556631, 1.279475349031534259 ) ) ;
#53680=CARTESIAN_POINT ( 'NONE',  ( 1.476976393720278002, -1.495863523836362896, 1.503369785937097136 ) ) ;
#53683=CARTESIAN_POINT ( 'NONE',  ( 4.422284181769401634, 0.9229163912191931107, 1.731201473044993167 ) ) ;
#53684=CARTESIAN_POINT ( 'NONE',  ( 2.008865009297224447, 1.601992838228694316, -1.451600824242594845 ) ) ;
#53685=CARTESIAN_POINT ( 'NONE',  ( 1.329379181053941483, 0.9071106928158387817, -1.602193565413398746 ) ) ;
#53688=CARTESIAN_POINT ( 'NONE',  ( 3.538731034799988073, -1.318886434843706601, -1.135564254951209273 ) ) ;
#53692=CARTESIAN_POINT ( 'NONE',  ( 2.325270847726228940, -0.0006328605136555342939, 2.161883445422786654 ) ) ;
#53695=CARTESIAN_POINT ( 'NONE',  ( 3.093124880496417983, 1.122326866504215426, -1.674630914042275709 ) ) ;
#53698=CARTESIAN_POINT ( 'NONE',  ( 3.467610927914951624, 1.923740664667829225, -0.4305075535177785295 ) ) ;
#53700=CARTESIAN_POINT ( 'NONE',  ( 2.401813893259804100, -0.7453968187615340746, -1.793506507769267788 ) ) ;
#53710=CARTESIAN_POINT ( 'NONE',  ( 0.4642757356001780966, 2.182421439735841684, -0.3260586787675948117 ) ) ;
#53712=CARTESIAN_POINT ( 'NONE',  ( 4.100408672059585591, 1.951911038179511726, 0.1965976633130430695 ) ) ;
#53714=CARTESIAN_POINT ( 'NONE',  ( 1.740861508391436274, 2.010826320759526720, -0.1511413081683593562 ) ) ;
#53716=CARTESIAN_POINT ( 'NONE',  ( 3.731751022097353321, 0.7093996228057770637, -1.995120430414954349 ) ) ;
#53720=CARTESIAN_POINT ( 'NONE',  ( 3.591602706507342369, -1.839109287420921834, -0.08896477992388628075 ) ) ;
#53724=CARTESIAN_POINT ( 'NONE',  ( 3.533539421053989660, -0.1523460092780377639, 2.115156586662121363 ) ) ;
#53728=CARTESIAN_POINT ( 'NONE',  ( 5.378222296270031677, -1.148346438381561363, 1.710960936357192264 ) ) ;
#53730=CARTESIAN_POINT ( 'NONE',  ( 2.243484787601189634, 1.840893492186860492, 0.04347913094143729396 ) ) ;
#53736=CARTESIAN_POINT ( 'NONE',  ( 2.350463684150871035, 2.206416367115513477, 0.05273732197710182673 ) ) ;
#53737=CARTESIAN_POINT ( 'NONE',  ( 4.288523069895104456, -2.236996925053718055, -0.3375187357864944393 ) ) ;
#53739=CARTESIAN_POINT ( 'NONE',  ( 4.781432078664868079, 0.1701398743050798745, -1.803555781593807250 ) ) ;
#53740=CARTESIAN_POINT ( 'NONE',  ( 4.505048170306029220, -0.08773398713153966744, 1.913818227509517023 ) ) ;
#53742=CARTESIAN_POINT ( 'NONE',  ( 3.678557393866654923, -1.899675168901427513, -0.5269097987367215019 ) ) ;
#53743=CARTESIAN_POINT ( 'NONE',  ( 4.574985519202336981, -0.0001439422951596270033, -1.870836309977530920 ) ) ;
#53744=CARTESIAN_POINT ( 'NONE',  ( 3.282123524285113003, 1.463787882210180191, 1.784030387633539938 ) ) ;
#53745=CARTESIAN_POINT ( 'NONE',  ( 4.861673063681271501, -0.4970775243713953517, 1.793344219904927206 ) ) ;
#53750=CARTESIAN_POINT ( 'NONE',  ( 1.981218818260335413, -0.1044028718686483975, -2.103608768903475035 ) ) ;
#53755=CARTESIAN_POINT ( 'NONE',  ( 3.129257641292593650, 1.918792544363761454, 0.9031103230835100248 ) ) ;
#53758=CARTESIAN_POINT ( 'NONE',  ( 0.7561249178302269502, 0.8145892717734238841, -1.848413388458100215 ) ) ;
#53764=CARTESIAN_POINT ( 'NONE',  ( 2.513140823169751847, 1.929641211675875878, 0.9743453106897670413 ) ) ;
#53765=CARTESIAN_POINT ( 'NONE',  ( 6.610000000000011866, 2.967812824040619191, 2.453181572820534395 ) ) ;
#53767=CARTESIAN_POINT ( 'NONE',  ( 6.925078400183546812, 3.702220002068328242, 2.370079373711677206 ) ) ;
#53770=CARTESIAN_POINT ( 'NONE',  ( 5.805875103277515770, -1.124240986939632592, -1.673857227857282082 ) ) ;
#53772=CARTESIAN_POINT ( 'NONE',  ( 0.2049558871960316941, 1.909868400323280424, 1.074723926240577221 ) ) ;
#53774=CARTESIAN_POINT ( 'NONE',  ( 0.9719599696450488269, 2.179858136331577434, -0.6057951801161051142 ) ) ;
#53781=CARTESIAN_POINT ( 'NONE',  ( 4.371539443043367612, 1.672179000890521516, -0.4225743650863537648 ) ) ;
#53783=CARTESIAN_POINT ( 'NONE',  ( 2.565387841970759197, 1.736461783412158955, -0.3405875811831828859 ) ) ;
#53784=CARTESIAN_POINT ( 'NONE',  ( 3.018229385809416687, -2.010681777978724494, 0.1011178238035769505 ) ) ;
#53786=CARTESIAN_POINT ( 'NONE',  ( 4.823365732668142947, -0.1123398232194070118, 2.204042774474362254 ) ) ;
#53789=CARTESIAN_POINT ( 'NONE',  ( 3.885024839820313325, -1.886105071096555230, -0.7231171000243222791 ) ) ;
#53791=CARTESIAN_POINT ( 'NONE',  ( 5.496778590849229040, -2.068848325035842706, -0.4644329061709790429 ) ) ;
#53792=CARTESIAN_POINT ( 'NONE',  ( 4.288685525864014636, 1.556897452430844320, -1.281376678550147474 ) ) ;
#53795=CARTESIAN_POINT ( 'NONE',  ( 1.533845512228737551, 0.9248708299973290581, -1.625957014461040906 ) ) ;
#53797=CARTESIAN_POINT ( 'NONE',  ( 6.024035747493574178, -1.796918165027236780, 0.2286857708345239326 ) ) ;
#53804=CARTESIAN_POINT ( 'NONE',  ( 0.5801457039020865292, 0.9447208859736742070, 1.662703529197881558 ) ) ;
#53807=CARTESIAN_POINT ( 'NONE',  ( 1.926150285298435572, 1.005797860886543660, 1.684270608208485065 ) ) ;
#53811=CARTESIAN_POINT ( 'NONE',  ( 3.797228045176269440, -0.2112621354826669517, -2.110076569278092062 ) ) ;
#53813=CARTESIAN_POINT ( 'NONE',  ( 5.677018108359257020, -0.04579235393691384604, -1.970973552702318443 ) ) ;
#53815=CARTESIAN_POINT ( 'NONE',  ( 0.8439947366445134103, -1.280256340399921200, -1.553649900018534202 ) ) ;
#53817=CARTESIAN_POINT ( 'NONE',  ( 0.9138395863287234189, -1.346417975848941406, -1.633941036375158973 ) ) ;
#53819=CARTESIAN_POINT ( 'NONE',  ( 2.313015868914463091, -1.601887806243259771, 1.311650804931147274 ) ) ;
#53823=CARTESIAN_POINT ( 'NONE',  ( 5.244118971382810912, 0.6063552182394044143, 2.000762070341703502 ) ) ;
#53825=CARTESIAN_POINT ( 'NONE',  ( 3.575057022766346737, 0.04566639709948847742, -1.825179878808772305 ) ) ;
#53826=CARTESIAN_POINT ( 'NONE',  ( 2.051130129875160968, -1.617795175136220509, 0.8151331081446986371 ) ) ;
#53831=CARTESIAN_POINT ( 'NONE',  ( 5.315527377757141458, -0.3284926246858720922, 2.182075488366498117 ) ) ;
#53834=CARTESIAN_POINT ( 'NONE',  ( 4.529883686416775745, -1.874680353417649492, 0.3764776581506729114 ) ) ;
#53839=CARTESIAN_POINT ( 'NONE',  ( 6.427279137517246888, -1.429865906218323435, -1.660902671979214595 ) ) ;
#53844=CARTESIAN_POINT ( 'NONE',  ( 3.549935554046261821, 1.870726058081632504, 0.003126486288931861444 ) ) ;
#53845=CARTESIAN_POINT ( 'NONE',  ( -0.02319159430947542039, 5.725354828811364705, -2.405035539666657840 ) ) ;
#53850=CARTESIAN_POINT ( 'NONE',  ( 0.4792732452305690782, -0.1022114018467655538, 1.966944630885968603 ) ) ;
#53851=CARTESIAN_POINT ( 'NONE',  ( 0.8082205221912192039, 1.198841770460257194, -1.621197638953228548 ) ) ;
#53855=CARTESIAN_POINT ( 'NONE',  ( 0.8498829323080080433, 2.188760582993890313, -0.1110106097068005726 ) ) ;
#53856=CARTESIAN_POINT ( 'NONE',  ( 6.721331454403435934, -0.1262074967819451221, 1.796610827203233063 ) ) ;
#53863=CARTESIAN_POINT ( 'NONE',  ( 4.265079090171526310, 1.784866007061826298, -0.4516350764028759235 ) ) ;
#53864=CARTESIAN_POINT ( 'NONE',  ( 0.6275903186243469989, -0.2933333519314991755, 1.991482607974030206 ) ) ;
#53865=CARTESIAN_POINT ( 'NONE',  ( 2.214639623771569088, -1.845710301178200119, -1.369457037089250484 ) ) ;
#53867=CARTESIAN_POINT ( 'NONE',  ( 6.174655700867183405, 1.320063289540554408, -1.451312704123429498 ) ) ;
#53871=CARTESIAN_POINT ( 'NONE',  ( 4.922078805074791674, -1.902621863305080430, 0.1933406509087298719 ) ) ;
#53875=CARTESIAN_POINT ( 'NONE',  ( 3.720331632570073932, 1.985922124624572627, 0.6539709493295197129 ) ) ;
#53876=CARTESIAN_POINT ( 'NONE',  ( 2.535844406030359544, 0.8837261853790435717, -1.648756255988912400 ) ) ;
#53879=CARTESIAN_POINT ( 'NONE',  ( 3.614586527008158523, -0.1238012486478034802, 1.736083139875769676 ) ) ;
#53882=CARTESIAN_POINT ( 'NONE',  ( 4.494587217144647262, -0.3816326207147257010, -1.681953545215847168 ) ) ;
#53883=CARTESIAN_POINT ( 'NONE',  ( 4.212563348414651188, 2.004022095860341413, 0.8874167208733558798 ) ) ;
#53884=CARTESIAN_POINT ( 'NONE',  ( 6.639307388351803674, -1.973492857608965423, 0.9879489342229507143 ) ) ;
#53886=CARTESIAN_POINT ( 'NONE',  ( 3.168971741543443077, 1.575705016696099081, -1.493804678357780524 ) ) ;
#53887=CARTESIAN_POINT ( 'NONE',  ( 2.068725586703868746, -1.668841220716179130, -0.7407507213199536755 ) ) ;
#53888=CARTESIAN_POINT ( 'NONE',  ( 0.3913574919355842785, -1.795980968407092426, 0.7896611536716554580 ) ) ;
#53889=CARTESIAN_POINT ( 'NONE',  ( 4.241493788847498614, 0.4602237217972443561, -2.066584722733503909 ) ) ;
#53891=CARTESIAN_POINT ( 'NONE',  ( 4.282983983471492451, 2.047787327626307441, -1.030491903107624951 ) ) ;
#53893=CARTESIAN_POINT ( 'NONE',  ( 6.720655732516655156, 7.629137130509086262, 2.526260288887293814 ) ) ;
#53895=CARTESIAN_POINT ( 'NONE',  ( 0.3641364058636682999, 0.6611385597973111761, -2.014868753213174823 ) ) ;
#53904=CARTESIAN_POINT ( 'NONE',  ( 5.361953999179126740, -0.05229508359532940298, -2.015913028294749942 ) ) ;
#53906=CARTESIAN_POINT ( 'NONE',  ( 4.715719689075464238, 0.4568931354213046636, -2.011171341922016076 ) ) ;
#53908=CARTESIAN_POINT ( 'NONE',  ( -0.2409995289980245703, 0.2355275985303668385, -2.034371242098035548 ) ) ;
#53911=CARTESIAN_POINT ( 'NONE',  ( 0.4454078864507329816, 0.6539998520847762897, -1.985780399853773526 ) ) ;
#53912=CARTESIAN_POINT ( 'NONE',  ( 4.377577386359387646, -0.4445010797573499817, -1.966645064109616481 ) ) ;
#53913=CARTESIAN_POINT ( 'NONE',  ( 3.491602800004707241, -1.839307750763185645, -0.08696504193297231733 ) ) ;
#53916=CARTESIAN_POINT ( 'NONE',  ( 0.7270763493693053192, -1.639898566368836130, 0.5346300883638678281 ) ) ;
#53918=CARTESIAN_POINT ( 'NONE',  ( 0.6866852740153045476, 1.883736933065732533, 1.317207514508748734 ) ) ;
#53920=CARTESIAN_POINT ( 'NONE',  ( 6.526273518496622295, 1.309208030111205900, -1.845092234498114658 ) ) ;
#53921=CARTESIAN_POINT ( 'NONE',  ( 2.772209899791327370, 1.127123820452385017, 1.778883819610539208 ) ) ;
#53925=CARTESIAN_POINT ( 'NONE',  ( 5.781250000000004441, 0.7852924748302878566, 1.895863743163952453 ) ) ;
#53931=CARTESIAN_POINT ( 'NONE',  ( 2.496466685713152334, -1.086271176545396067, 1.821091972856798913 ) ) ;
#53932=CARTESIAN_POINT ( 'NONE',  ( 3.762163318865581640, 0.7457541186767223662, -2.092641825391368560 ) ) ;
#53933=CARTESIAN_POINT ( 'NONE',  ( 1.851786237446376049, 2.185420115623282200, -0.1633297828415938846 ) ) ;
#53936=CARTESIAN_POINT ( 'NONE',  ( 5.969191311310417802, 1.729517061547349632, 0.9261464158661563140 ) ) ;
#53940=CARTESIAN_POINT ( 'NONE',  ( 4.043311264919998038, 0.1072909356813686182, 2.118029240109862155 ) ) ;
#53944=CARTESIAN_POINT ( 'NONE',  ( 6.666866396406604167, -1.974176978123330040, -0.8811043787171415342 ) ) ;
#53946=CARTESIAN_POINT ( 'NONE',  ( 5.196754805642953556, 1.508532920973480795, 1.055450849767838539 ) ) ;
#53948=CARTESIAN_POINT ( 'NONE',  ( 1.417106933825535986, -0.9663644154882103932, -1.447271084069596370 ) ) ;
#53953=CARTESIAN_POINT ( 'NONE',  ( 5.313408243115379292, -0.3210861823062813314, 2.137610926513198617 ) ) ;
#53956=CARTESIAN_POINT ( 'NONE',  ( 4.083022661009271914, -0.2092679848491978134, -2.151539631373246220 ) ) ;
#53957=CARTESIAN_POINT ( 'NONE',  ( 4.868415619454742327, -1.289772430030609707, 1.490937899079747497 ) ) ;
#53958=CARTESIAN_POINT ( 'NONE',  ( 4.006995869149078793, 1.725434352394356052, 0.1705419362300845121 ) ) ;
#53959=CARTESIAN_POINT ( 'NONE',  ( 1.048660896456204528, -1.724490848714568259, 1.352309724062021878 ) ) ;
#53960=CARTESIAN_POINT ( 'NONE',  ( 2.222082089356589130, -2.238238103340572049, 0.5610464132631690637 ) ) ;
#53961=CARTESIAN_POINT ( 'NONE',  ( 4.095036773856917556, 1.742982576809920303, -1.099142878725319239 ) ) ;
#53962=CARTESIAN_POINT ( 'NONE',  ( 6.532770933798597746, -1.732582191135303651, 0.8775855664264734513 ) ) ;
#53970=CARTESIAN_POINT ( 'NONE',  ( 3.522699392456357881, 1.401646575410384843, -1.704459333586107794 ) ) ;
#53973=CARTESIAN_POINT ( 'NONE',  ( 0.2680791809135505410, -0.7890318081985218113, -1.684091100025336463 ) ) ;
#53974=CARTESIAN_POINT ( 'NONE',  ( -0.1288028175206621384, 0.6694653996850441491, -2.353626493485785343 ) ) ;
#53978=CARTESIAN_POINT ( 'NONE',  ( 6.825078400183552496, 6.035069422732725286, 2.639236294420511442 ) ) ;
#53981=CARTESIAN_POINT ( 'NONE',  ( 3.520434746236697610, 1.308796515248649817, -1.591936018771279659 ) ) ;
#53986=CARTESIAN_POINT ( 'NONE',  ( 1.586866656640874451, -0.3012919939810917436, -2.038609575755165437 ) ) ;
#53992=CARTESIAN_POINT ( 'NONE',  ( 6.111994396789379280, -2.190734547077430872, 0.2660306753756238041 ) ) ;
#53993=CARTESIAN_POINT ( 'NONE',  ( 0.9487563388480976245, 0.6265645459165304354, 2.068816658077163861 ) ) ;
#53995=CARTESIAN_POINT ( 'NONE',  ( 0.6730650033222317363, 1.776164188848127878, -0.9548607967814757291 ) ) ;
#53996=CARTESIAN_POINT ( 'NONE',  ( 1.915759298113205666, 0.7205626639651928622, 2.182595962359680897 ) ) ;
#54001=CARTESIAN_POINT ( 'NONE',  ( 1.990876257202532695, 1.628914321797021669, -0.9196232060951770038 ) ) ;
#54002=CARTESIAN_POINT ( 'NONE',  ( 3.380092458137720968, -2.014432998692190058, -0.09411721906785883163 ) ) ;
#54004=CARTESIAN_POINT ( 'NONE',  ( 6.639320575229258559, 7.052241914652472410, 2.701414248926166994 ) ) ;
#54006=CARTESIAN_POINT ( 'NONE',  ( 4.600280035732231987, -2.105589688358105782, -0.05227242994678206467 ) ) ;
#54011=CARTESIAN_POINT ( 'NONE',  ( 3.603775140268844712, 1.465814181579458753, 1.389848736882649094 ) ) ;
#54013=CARTESIAN_POINT ( 'NONE',  ( 1.041928790383022774, 1.382269897723470642, 1.531051681482889393 ) ) ;
#54016=CARTESIAN_POINT ( 'NONE',  ( 5.536455037250767930, 2.128579029500421438, 0.3755436860354774420 ) ) ;
#54020=CARTESIAN_POINT ( 'NONE',  ( -0.2106854629475244101, -0.004120941679102127324, -1.996958217618934661 ) ) ;
#54022=CARTESIAN_POINT ( 'NONE',  ( 2.752568609338637895, -2.165203543660359387, -0.1620229588487445971 ) ) ;
#54025=CARTESIAN_POINT ( 'NONE',  ( 1.716098596715152746, 1.718394358364897068, 0.6617865747741287219 ) ) ;
#54028=CARTESIAN_POINT ( 'NONE',  ( 3.773127072069931032, 2.063069237518061705, -0.7396954945804237180 ) ) ;
#54030=CARTESIAN_POINT ( 'NONE',  ( 4.364347144703619286, 1.063191675971109307, 1.997143021516068595 ) ) ;
#54038=CARTESIAN_POINT ( 'NONE',  ( 4.921055611120458195, -0.08698325021493956422, 1.767741905644197642 ) ) ;
#54039=CARTESIAN_POINT ( 'NONE',  ( 3.475247029965710777, -1.776355867393118126, -0.9471225605895690070 ) ) ;
#54041=CARTESIAN_POINT ( 'NONE',  ( 2.344876439239967247, 0.4604487725310001389, 2.054841016598129233 ) ) ;
#54044=CARTESIAN_POINT ( 'NONE',  ( 2.014047288863869412, 1.964499257916036079, -0.1416769614510370867 ) ) ;
#54047=CARTESIAN_POINT ( 'NONE',  ( 5.994382934279598452, -0.9612500426990595592, 1.535330125949084135 ) ) ;
#54052=CARTESIAN_POINT ( 'NONE',  ( 6.034044788248046132, 0.9204803733943857091, -1.628451883209979689 ) ) ;
#54054=CARTESIAN_POINT ( 'NONE',  ( 5.682505902380680318, 1.237739610710281823, -1.659335868388504220 ) ) ;
#54066=CARTESIAN_POINT ( 'NONE',  ( 4.932062528313536198, 1.127988425013145779, 1.604980062286972542 ) ) ;
#54069=CARTESIAN_POINT ( 'NONE',  ( 3.163435312993330140, -0.5825663732807913053, -1.930122257003751063 ) ) ;
#54070=CARTESIAN_POINT ( 'NONE',  ( 2.131924177892559058, 1.915402082336896461, 0.04262488632780260522 ) ) ;
#54071=CARTESIAN_POINT ( 'NONE',  ( 0.2577194443907256383, 2.166829308800602316, -0.3276212646995610989 ) ) ;
#54072=CARTESIAN_POINT ( 'NONE',  ( 0.1333692844072316419, 7.629137130509075604, -2.653547345224521514 ) ) ;
#54073=CARTESIAN_POINT ( 'NONE',  ( 1.686563950722594685, -0.2693046698774223535, -1.850923959389898288 ) ) ;
#54075=CARTESIAN_POINT ( 'NONE',  ( 4.500248159151196248, -0.9453760218497176959, 1.777399672076788617 ) ) ;
#54078=CARTESIAN_POINT ( 'NONE',  ( 4.359064374566766986, -0.001685027751544953406, -2.117403152337670846 ) ) ;
#54080=CARTESIAN_POINT ( 'NONE',  ( 6.144996677366851401, -0.2998803957653916608, -2.048400609436632269 ) ) ;
#54081=CARTESIAN_POINT ( 'NONE',  ( 0.6442209307526406414, 0.6107738465899931191, 1.999526160293135568 ) ) ;
#54083=CARTESIAN_POINT ( 'NONE',  ( 6.475623784153278883, 1.746001614453606576, -0.5331787911772439825 ) ) ;
#54091=CARTESIAN_POINT ( 'NONE',  ( 1.031567638852897373, -1.767431343716918013, 0.3961611186833951526 ) ) ;
#54099=AXIS2_PLACEMENT_3D ( 'NONE', #183683, #66695, #118746 ) ;
#54100=CARTESIAN_POINT ( 'NONE',  ( 5.888296041240274725, -0.7283935311428509918, -1.880430420734761965 ) ) ;
#54101=CARTESIAN_POINT ( 'NONE',  ( 0.8914570141239013257, -0.05588796005432519753, -2.119924415460701983 ) ) ;
#54107=CARTESIAN_POINT ( 'NONE',  ( 3.573067284968055812, 1.778583338327298646, 0.8461400097728142278 ) ) ;
#54108=CARTESIAN_POINT ( 'NONE',  ( 4.798453934790239295, 1.388474963651475269, -1.462457531588717830 ) ) ;
#54111=CARTESIAN_POINT ( 'NONE',  ( 6.727182134110194944, 2.413774403037728167, 2.569658639860139093 ) ) ;
#54113=CARTESIAN_POINT ( 'NONE',  ( 5.033237522093748417, -1.548190877955179179, -1.551241237171486098 ) ) ;
#54115=CARTESIAN_POINT ( 'NONE',  ( 3.082943253306829057, -0.1403151614269258773, -1.921328324580730440 ) ) ;
#54117=CARTESIAN_POINT ( 'NONE',  ( -0.1294898018151836583, 0.7212281881416956475, -2.008332099035778917 ) ) ;
#54118=CARTESIAN_POINT ( 'NONE',  ( 0.1331565106231571705, 2.881392620029461504, -2.434650611646618223 ) ) ;
#54121=CARTESIAN_POINT ( 'NONE',  ( 4.698083300297758669, 0.8457734583860087030, -1.778757171186759134 ) ) ;
#54123=CARTESIAN_POINT ( 'NONE',  ( 0.6263844939735198070, 0.1443197301355322315, 1.936771776935701794 ) ) ;
#54124=CARTESIAN_POINT ( 'NONE',  ( 3.527992865196138972, -1.982922396879973626, 0.3464002264041438073 ) ) ;
#54125=CARTESIAN_POINT ( 'NONE',  ( 5.923294579110739200, 0.9235710928677911546, 2.104827929701275302 ) ) ;
#54127=CARTESIAN_POINT ( 'NONE',  ( 3.819077715518546690, -1.639399709636097713, -0.8806717989592935947 ) ) ;
#54134=CARTESIAN_POINT ( 'NONE',  ( 0.5916818631664167993, -0.7834642122952638621, 2.046923429677327100 ) ) ;
#54138=CARTESIAN_POINT ( 'NONE',  ( 0.09986456629675066754, -1.825204794925545881, -0.04862044751281074939 ) ) ;
#54140=CARTESIAN_POINT ( 'NONE',  ( 2.900671442982618142, -0.8568821622233543378, -1.507568437789049032 ) ) ;
#54142=CARTESIAN_POINT ( 'NONE',  ( 6.609000000000012420, 2.456927087449762404, 2.283703893460458989 ) ) ;
#54145=CARTESIAN_POINT ( 'NONE',  ( 6.059193749186201572, -1.568369423792463024, -0.9343120793870243190 ) ) ;
#54146=CARTESIAN_POINT ( 'NONE',  ( 3.713678095275750657, 0.4809820416172749802, -1.901733992618503066 ) ) ;
#54150=CARTESIAN_POINT ( 'NONE',  ( 3.281995766809755466, 2.068381274212594878, -0.4664580258975092875 ) ) ;
#54153=CARTESIAN_POINT ( 'NONE',  ( 2.026315959858393967, 1.060668813445601044, 1.777738962378045295 ) ) ;
#54156=CARTESIAN_POINT ( 'NONE',  ( 4.705860574468672120, 1.645629519818484932, 1.492201155203516150 ) ) ;
#54158=CARTESIAN_POINT ( 'NONE',  ( 1.512731952202387653, -2.162554957723664462, 0.7796286979407650586 ) ) ;
#54165=CARTESIAN_POINT ( 'NONE',  ( 2.759904966095374501, 0.6844231338998980618, -1.785916880244736715 ) ) ;
#54167=CARTESIAN_POINT ( 'NONE',  ( 4.436358534413815669, 1.691719876958649227, 0.3350348670820638142 ) ) ;
#54168=CARTESIAN_POINT ( 'NONE',  ( 1.868375392651611122, -1.978555653031977446, -0.3886301775877995524 ) ) ;
#54169=CARTESIAN_POINT ( 'NONE',  ( 3.463815647965732936, -2.215898795117266840, -0.6112515151598179042 ) ) ;
#54170=CARTESIAN_POINT ( 'NONE',  ( 6.533818191484063398, -1.374270492279753286, -1.595981979862278077 ) ) ;
#54172=CARTESIAN_POINT ( 'NONE',  ( 5.307753102408475421, -1.761140305208692913, 0.1738094965475830145 ) ) ;
#54174=CARTESIAN_POINT ( 'NONE',  ( 1.166458296791187621, -1.450650017800562575, 1.774850106915156100 ) ) ;
#54175=CARTESIAN_POINT ( 'NONE',  ( 0.3041415704291222100, 1.511679331021776207, 0.8621369596173468208 ) ) ;
#54177=CARTESIAN_POINT ( 'NONE',  ( 5.455090197064776270, 0.4301712223657681022, -2.148646160378755443 ) ) ;
#54181=CARTESIAN_POINT ( 'NONE',  ( 6.672334155782003506, -0.9722939650993901450, -1.827837255792996718 ) ) ;
#54182=CARTESIAN_POINT ( 'NONE',  ( 0.7609543035823238544, -0.05432987398422234326, -2.015980609757315190 ) ) ;
#54184=CARTESIAN_POINT ( 'NONE',  ( 4.231024032915966515, 0.09596189134018082156, 1.924231256547383362 ) ) ;
#54186=CARTESIAN_POINT ( 'NONE',  ( 0.8619570425896695420, -1.755772037458620316, -1.360811342731186979 ) ) ;
#54194=CARTESIAN_POINT ( 'NONE',  ( 0.1831564129048668388, 7.629137130509052511, -2.545826866328745997 ) ) ;
#54195=CARTESIAN_POINT ( 'NONE',  ( 3.807932448155851191, 1.227607710457185197, -1.234010206841095636 ) ) ;
#54196=CARTESIAN_POINT ( 'NONE',  ( 2.910546574502240968, 0.6583626327048962557, 1.848246418561696913 ) ) ;
#54203=CARTESIAN_POINT ( 'NONE',  ( 0.1509074155349584279, -0.4535863444464246497, -2.019966333402842817 ) ) ;
#54205=( BOUNDED_SURFACE ( )  B_SPLINE_SURFACE ( 3, 3, ( 
 ( #99450, #131988, #214210, #31258, #16031, #83177, #181738, #97332, #115748, #195882, #33369 ),
 ( #165507, #79987, #211038, #78913, #161252, #194805, #180688, #34434, #62664, #30180, #199045 ),
 ( #82115, #163390, #197997, #66904, #48578, #14964, #32313, #50692, #17099, #98381, #130947 ),
 ( #164444, #149260, #838, #81061, #148208, #96271, #145035, #116816, #46441, #129897, #162321 ),
 ( #133044, #128823, #147146, #112560, #47520, #182818, #113633, #146091, #213172, #212102, #64801 ),
 ( #63739, #179638, #196938, #114694, #22436, #18171, #2983, #103724, #20313, #203319, #153539 ),
 ( #84258, #69050, #101576, #21364, #88546, #102652, #52824, #135170, #122193, #36566, #168709 ) ),
 .UNSPECIFIED., .T., .F., .T. ) 
 B_SPLINE_SURFACE_WITH_KNOTS ( ( 4, 3, 4 ),
 ( 4, 1, 1, 1, 1, 1, 1, 1, 4 ),
 ( 0.000000000000000000, 0.5000000000000000000, 1.000000000000000000 ),
 ( 0.000000000000000000, 0.2255509035172358623, 0.3975895543896152406, 0.5252637114030099807, 0.6177357421269481508, 0.6841390318922365710, 0.7334310489036851566, 0.7741974304450970346, 1.000000000000000000 ),
 .UNSPECIFIED. ) 
 GEOMETRIC_REPRESENTATION_ITEM ( )  RATIONAL_B_SPLINE_SURFACE ( (
 ( 1.000000000000000000, 1.000000000000000000, 1.000000000000000000, 1.000000000000000000, 1.000000000000000444, 0.9999999999999997780, 1.000000000000000000, 1.000000000000000000, 1.000000000000000000, 1.000000000000000000, 1.000000000000000000),
 ( 0.3333333333333333703, 0.3333333333333333703, 0.3333333333333332593, 0.3333333333333334814, 0.3333333333333334814, 0.3333333333333333148, 0.3333333333333333703, 0.3333333333333333703, 0.3333333333333333703, 0.3333333333333334259, 0.3333333333333333703),
 ( 0.3333333333333333703, 0.3333333333333333703, 0.3333333333333332593, 0.3333333333333334814, 0.3333333333333334814, 0.3333333333333333148, 0.3333333333333333703, 0.3333333333333333703, 0.3333333333333333703, 0.3333333333333334259, 0.3333333333333333703),
 ( 1.000000000000000000, 1.000000000000000000, 1.000000000000000000, 1.000000000000000000, 1.000000000000000444, 0.9999999999999997780, 1.000000000000000000, 1.000000000000000000, 1.000000000000000000, 1.000000000000000000, 1.000000000000000000),
 ( 0.3333333333333333703, 0.3333333333333333703, 0.3333333333333332593, 0.3333333333333334814, 0.3333333333333334814, 0.3333333333333333148, 0.3333333333333333703, 0.3333333333333333703, 0.3333333333333333703, 0.3333333333333334259, 0.3333333333333333703),
 ( 0.3333333333333333703, 0.3333333333333333703, 0.3333333333333332593, 0.3333333333333334814, 0.3333333333333334814, 0.3333333333333333148, 0.3333333333333333703, 0.3333333333333333703, 0.3333333333333333703, 0.3333333333333334259, 0.3333333333333333703),
 ( 1.000000000000000000, 1.000000000000000000, 1.000000000000000000, 1.000000000000000000, 1.000000000000000444, 0.9999999999999997780, 1.000000000000000000, 1.000000000000000000, 1.000000000000000000, 1.000000000000000000, 1.000000000000000000) ) ) 
 REPRESENTATION_ITEM ( '' )  SURFACE ( )  );
#54207=CARTESIAN_POINT ( 'NONE',  ( 5.190638768449240992, 1.523797776992100284, -1.320824044268428255 ) ) ;
#54208=CARTESIAN_POINT ( 'NONE',  ( 0.7962373781299083575, -0.8115885651059464578, 2.112105989495225877 ) ) ;
#54212=CARTESIAN_POINT ( 'NONE',  ( 1.669004442688322154, 0.1428430569143137041, -1.865171992484420338 ) ) ;
#54213=CARTESIAN_POINT ( 'NONE',  ( 0.6329805529394582075, 0.5017471949167272571, 1.659931108299773639 ) ) ;
#54215=CARTESIAN_POINT ( 'NONE',  ( 4.546525781634036534, -1.759932548463913671, 1.305750774140898685 ) ) ;
#54216=CARTESIAN_POINT ( 'NONE',  ( 5.596783072813162896, -0.5536939349623200002, -2.240073236831362280 ) ) ;
#54217=CARTESIAN_POINT ( 'NONE',  ( 0.4091470207043126917, 1.792883176943863122, 1.016159331636699470 ) ) ;
#54218=CARTESIAN_POINT ( 'NONE',  ( 3.380740619721524620, 1.755215216048062521, -0.8311813869739079763 ) ) ;
#54224=CARTESIAN_POINT ( 'NONE',  ( 4.746720300533005421, 1.994071680685698400, -0.2986252114312442640 ) ) ;
#54228=CARTESIAN_POINT ( 'NONE',  ( 1.330379832379691818, 1.758967509726565792, 0.4888242021733391618 ) ) ;
#54234=CARTESIAN_POINT ( 'NONE',  ( 0.09294085500742564621, -0.4768749645070144982, -2.116232079886640971 ) ) ;
#54238=CARTESIAN_POINT ( 'NONE',  ( 5.865880358592049149, 0.5843737978505449959, -1.933295926576389379 ) ) ;
#54239=CARTESIAN_POINT ( 'NONE',  ( 5.654997643673960184, 0.4312606369310955645, 2.178877383265501066 ) ) ;
#54243=CARTESIAN_POINT ( 'NONE',  ( 5.383688703920392449, 1.382483038487541283, 1.528581890270568122 ) ) ;
#54244=CARTESIAN_POINT ( 'NONE',  ( 4.043592392309851569, -1.492256208629010761, 1.356298961253152413 ) ) ;
#54253=CARTESIAN_POINT ( 'NONE',  ( 4.165388622617651748, -0.6297791189726584804, -1.915306643112117291 ) ) ;
#54254=CARTESIAN_POINT ( 'NONE',  ( 3.908013947242465314, 1.300727540704300633, -1.303293010247716488 ) ) ;
#54256=CARTESIAN_POINT ( 'NONE',  ( 2.596638674903679167, -2.301597171833298372, -0.1684899434626195847 ) ) ;
#54258=CARTESIAN_POINT ( 'NONE',  ( 5.202478051755599964, -0.7228594145181690411, -2.037298988101433839 ) ) ;
#54260=CARTESIAN_POINT ( 'NONE',  ( 6.497600353373155002, -1.840680978339729545, 0.05264081064878384231 ) ) ;
#54265=CARTESIAN_POINT ( 'NONE',  ( 2.799504582125960095, -0.5885537693137884441, 1.775713401224961574 ) ) ;
#54266=CARTESIAN_POINT ( 'NONE',  ( 6.684453674706574589, -1.933370886519528264, -0.3848441959667763257 ) ) ;
#54269=CARTESIAN_POINT ( 'NONE',  ( 1.946200625105892312, 0.8427435547867198062, -2.039832142532324255 ) ) ;
#54275=CARTESIAN_POINT ( 'NONE',  ( 6.526250059115050739, 1.135311405967744935, -1.611567521105742751 ) ) ;
#54276=CARTESIAN_POINT ( 'NONE',  ( 0.5875216112017033199, -0.2866185507822028855, -2.289643093864159429 ) ) ;
#54277=CARTESIAN_POINT ( 'NONE',  ( 0.4847190467827041105, 1.876267867961832980, 0.5731238010058882226 ) ) ;
#54278=CARTESIAN_POINT ( 'NONE',  ( 3.731348124473393479, 0.05553323764710679095, -2.061997793915891553 ) ) ;
#54287=CARTESIAN_POINT ( 'NONE',  ( 5.934065736658769019, 1.288437188380668452, 1.747434731901863936 ) ) ;
#54289=CARTESIAN_POINT ( 'NONE',  ( 5.583513413114173041, -0.8223277247318347971, 1.647484189299788682 ) ) ;
#54292=CARTESIAN_POINT ( 'NONE',  ( 0.3154175708385241750, -1.835744252435017598, 0.3582649291258357960 ) ) ;
#54298=CARTESIAN_POINT ( 'NONE',  ( 2.430210232679584248, 1.715968397599322737, 0.4327865170333042300 ) ) ;
#54299=CARTESIAN_POINT ( 'NONE',  ( 6.129547061768469085, -0.2442746830248194168, 1.998141925448652989 ) ) ;
#54301=CARTESIAN_POINT ( 'NONE',  ( 4.253473425383147877, 1.857088099111468216, -0.4692844457289280236 ) ) ;
#54302=CARTESIAN_POINT ( 'NONE',  ( -0.1409997244346088141, -0.002808977843308038680, -2.000147647483838220 ) ) ;
#54303=CARTESIAN_POINT ( 'NONE',  ( 5.846149472147661896, -0.8869723270901458401, 1.758618239599341937 ) ) ;
#54304=CARTESIAN_POINT ( 'NONE',  ( -0.1049925189658337810, -2.058569791948822392, -0.5088776734372552069 ) ) ;
#54306=CARTESIAN_POINT ( 'NONE',  ( 3.045614982896325262, 0.6747646648952825288, -1.744891315567910439 ) ) ;
#54307=CARTESIAN_POINT ( 'NONE',  ( 6.674431755534494748, -1.054235620458108702, 1.365612558063566073 ) ) ;
#54309=CARTESIAN_POINT ( 'NONE',  ( 3.510573375967055654, -0.8941257848905452832, -2.017821460644920073 ) ) ;
#54312=CARTESIAN_POINT ( 'NONE',  ( 0.2739786698724961944, -2.023204396000506833, 0.4007670430965051822 ) ) ;
#54319=CARTESIAN_POINT ( 'NONE',  ( 2.770052221688572125, -2.048192801557855436, 0.3012726569043902569 ) ) ;
#54323=CARTESIAN_POINT ( 'NONE',  ( 1.031905740238812097, -1.969920897724128483, 0.4447463068311637846 ) ) ;
#54329=CARTESIAN_POINT ( 'NONE',  ( 0.1745949693968328886, 2.059235863126197774, -2.173049245862024303 ) ) ;
#54332=CARTESIAN_POINT ( 'NONE',  ( 6.087116770962817114, 1.596809997336025022, 1.058066368194489959 ) ) ;
#54334=CARTESIAN_POINT ( 'NONE',  ( 3.861010967126534688, 0.2669419790740577558, -2.175157288012785184 ) ) ;
#54336=CARTESIAN_POINT ( 'NONE',  ( 2.390748813209525814, -1.831196095803063528, -0.5514187292172747501 ) ) ;
#54341=CARTESIAN_POINT ( 'NONE',  ( 0.6148615108944045504, 0.1511614643284354409, 2.010825953887733775 ) ) ;
#54343=CARTESIAN_POINT ( 'NONE',  ( 5.794512526436308875, 1.792401445336734733, -1.260760892635464980 ) ) ;
#54345=CARTESIAN_POINT ( 'NONE',  ( 2.924480221818404946, 1.623360404532696810, 0.5830473908832736196 ) ) ;
#54347=CARTESIAN_POINT ( 'NONE',  ( 0.1394461523057136665, 6.947783040739019533, -2.314776707679897516 ) ) ;
#54351=CARTESIAN_POINT ( 'NONE',  ( 1.803102349535959714, -1.659081995624330563, 1.046767247423967095 ) ) ;
#54358=CARTESIAN_POINT ( 'NONE',  ( 4.037629478943724592, -1.732251659483119433, 0.5297805909155322013 ) ) ;
#54362=CARTESIAN_POINT ( 'NONE',  ( 4.564998375345614257, -1.451947166338814377, 1.082946968254307585 ) ) ;
#54366=CARTESIAN_POINT ( 'NONE',  ( 5.600015889513015210, 0.7539677941885476464, -1.701683582386106952 ) ) ;
#54368=CARTESIAN_POINT ( 'NONE',  ( 2.495587842290597713, -1.894396863028270594, 0.2834604161582406356 ) ) ;
#54377=CARTESIAN_POINT ( 'NONE',  ( 1.429752723428807215, 1.029013270877369379, -1.819774963352964292 ) ) ;
#54379=CARTESIAN_POINT ( 'NONE',  ( 0.1295496576057716120, -1.118478952742516519, -1.443350188048427851 ) ) ;
#54381=CARTESIAN_POINT ( 'NONE',  ( 2.748829393344632166, -1.518919317350690967, 1.012417160375630898 ) ) ;
#54383=CARTESIAN_POINT ( 'NONE',  ( 2.179812656587180264, 1.874749209517186710, -0.3766967574026017229 ) ) ;
#54384=CARTESIAN_POINT ( 'NONE',  ( 1.820693447614455618, -1.395048584331352703, 1.390583823087336857 ) ) ;
#54385=CARTESIAN_POINT ( 'NONE',  ( 4.300292543067584461, 1.499173285595749583, -1.234514081855079048 ) ) ;
#54390=CARTESIAN_POINT ( 'NONE',  ( 3.867525618572264623, -1.764951123045129577, -1.175235903013646332 ) ) ;
#54398=CARTESIAN_POINT ( 'NONE',  ( 3.773894676421325478, 1.015518775504126614, 1.516979517045339509 ) ) ;
#54404=CARTESIAN_POINT ( 'NONE',  ( 4.416781281874038179, 1.710313510141375115, 0.7581657270378170388 ) ) ;
#54406=CARTESIAN_POINT ( 'NONE',  ( 2.244641533702110614, 0.4219287677580378926, 1.879577339372063838 ) ) ;
#54407=CARTESIAN_POINT ( 'NONE',  ( 6.912952593004608737, -1.518390278170888230, 1.241885805282372912 ) ) ;
#54412=CARTESIAN_POINT ( 'NONE',  ( 1.230240178466317724, 2.114980979692267393, 0.09988113581482771508 ) ) ;
#54414=CARTESIAN_POINT ( 'NONE',  ( 5.260626886859606444, -0.6923115906582855139, -1.951227211109484383 ) ) ;
#54415=CARTESIAN_POINT ( 'NONE',  ( 0.3273695209934923689, 0.9472894719858866441, -1.578709817245539604 ) ) ;
#54418=CARTESIAN_POINT ( 'NONE',  ( 6.399114681295562157, -1.079681622539971464, -2.029393132690388235 ) ) ;
#54422=CARTESIAN_POINT ( 'NONE',  ( 1.605870876717029549, -2.274517881136278508, 0.2841979012723067077 ) ) ;
#54426=CARTESIAN_POINT ( 'NONE',  ( 6.070255116781061666, -1.844781929399732290, -0.6067975954986597475 ) ) ;
#54430=CARTESIAN_POINT ( 'NONE',  ( -0.1579526903544171412, -1.242116785587377592, -1.585096312452577205 ) ) ;
#54435=CARTESIAN_POINT ( 'NONE',  ( 3.011755509560889443, -1.030818127458534184, -1.818759449385324078 ) ) ;
#54436=CARTESIAN_POINT ( 'NONE',  ( 1.111743784240331712, -0.7909239834335696218, -1.583357840528883287 ) ) ;
#54439=CARTESIAN_POINT ( 'NONE',  ( 3.855682016854941274, 2.275109001451373292, -0.2794487578934058969 ) ) ;
#54440=CARTESIAN_POINT ( 'NONE',  ( 2.976183818757103250, -0.1284355763333933920, -1.735648432857107126 ) ) ;
#54443=CARTESIAN_POINT ( 'NONE',  ( 3.778401656274816389, -1.708383637232064878, 0.2947856008331130040 ) ) ;
#54444=CARTESIAN_POINT ( 'NONE',  ( 3.736941271748619009, -2.091586689864731063, -0.5821943698010292323 ) ) ;
#54446=CARTESIAN_POINT ( 'NONE',  ( 4.803922858132807505, -1.082837210388952309, -1.700963621564715700 ) ) ;
#54447=CARTESIAN_POINT ( 'NONE',  ( 2.218750000000001332, -0.7852924748298697466, 1.895863743164134974 ) ) ;
#54449=CARTESIAN_POINT ( 'NONE',  ( 1.518447027862340093, 1.295632655171574665, -1.425748867336932513 ) ) ;
#54451=CARTESIAN_POINT ( 'NONE',  ( 5.010122972300034228, -0.7987708819462059351, 2.073016528135694703 ) ) ;
#54453=CARTESIAN_POINT ( 'NONE',  ( -0.2106854629475244378, -0.004120941679102134263, -1.996958217618934661 ) ) ;
#54457=CARTESIAN_POINT ( 'NONE',  ( 0.9268046190927975436, -1.003647134691580289, -1.981720526202688015 ) ) ;
#54458=CARTESIAN_POINT ( 'NONE',  ( 5.406682003534418079, 0.5678430586343993225, 1.877905798087247335 ) ) ;
#54462=CARTESIAN_POINT ( 'NONE',  ( 6.854744688279930998, -1.755419801747569286, 1.426855864884185809 ) ) ;
#54464=CARTESIAN_POINT ( 'NONE',  ( 3.332538901969614553, -1.230775513943611399, 1.655089866650825581 ) ) ;
#54468=CARTESIAN_POINT ( 'NONE',  ( 5.290257391050456448, -1.856285702826396156, -0.2301478561287788605 ) ) ;
#54469=CARTESIAN_POINT ( 'NONE',  ( 3.586273015720359503, -0.4996269028240771237, 1.660617844614233674 ) ) ;
#54470=CARTESIAN_POINT ( 'NONE',  ( 3.016877700344788416, -1.676514204431644783, 0.4670218299706177523 ) ) ;
#54471=CARTESIAN_POINT ( 'NONE',  ( 1.206998765908244176, 2.024556473040285187, 1.075228724532976132 ) ) ;
#54473=CARTESIAN_POINT ( 'NONE',  ( 4.054300615058183510, -1.547851416709244310, 1.405648825684354897 ) ) ;
#54474=CARTESIAN_POINT ( 'NONE',  ( 6.615187027077672255, -1.883050660437551205, 0.4742715046822160718 ) ) ;
#54476=CARTESIAN_POINT ( 'NONE',  ( 1.881482635453747720, -0.5404922439061732309, -1.942541187959702764 ) ) ;
#54480=( BOUNDED_SURFACE ( )  B_SPLINE_SURFACE ( 3, 3, ( 
 ( #115703, #149213, #15986, #62621, #48532, #99406, #165459, #66855, #128782, #17054, #53582 ),
 ( #119716, #37329, #212059, #63699, #103403, #194761, #195837, #47477, #57850, #90366, #125079 ),
 ( #136981, #71938, #154291, #141287, #6937, #54648, #189978, #153218, #120797, #108809, #25345 ),
 ( #56785, #24260, #156433, #186774, #203008, #173768, #170526, #38400, #55714, #122953, #104480 ),
 ( #174832, #191035, #75177, #73018, #205143, #188913, #138048, #157505, #121867, #187838, #74109 ),
 ( #22109, #89303, #40552, #124011, #8018, #88221, #5866, #9101, #42702, #172683, #204062 ),
 ( #139115, #107744, #207296, #39465, #106656, #91444, #58920, #140202, #206224, #87146, #41630 ) ),
 .UNSPECIFIED., .T., .F., .T. ) 
 B_SPLINE_SURFACE_WITH_KNOTS ( ( 4, 3, 4 ),
 ( 4, 1, 1, 1, 1, 1, 1, 1, 4 ),
 ( 0.000000000000000000, 0.5000000000000000000, 1.000000000000000000 ),
 ( 0.000000000000000000, 0.2254179815473072723, 0.3971144120416517653, 0.5241699701252212629, 0.6156743509408303394, 0.6807935377546089351, 0.7289379548928518471, 0.7696256121123346006, 1.000000000000000000 ),
 .UNSPECIFIED. ) 
 GEOMETRIC_REPRESENTATION_ITEM ( )  RATIONAL_B_SPLINE_SURFACE ( (
 ( 1.000000000000000000, 1.000000000000000000, 1.000000000000000222, 0.9999999999999997780, 0.9999999999999997780, 1.000000000000000222, 0.9999999999999997780, 1.000000000000000222, 0.9999999999999992228, 1.000000000000000000, 1.000000000000000000),
 ( 0.3333333333333333703, 0.3333333333333334259, 0.3333333333333334259, 0.3333333333333332593, 0.3333333333333333703, 0.3333333333333334259, 0.3333333333333333703, 0.3333333333333334814, 0.3333333333333332038, 0.3333333333333333703, 0.3333333333333333703),
 ( 0.3333333333333333703, 0.3333333333333334259, 0.3333333333333334259, 0.3333333333333332593, 0.3333333333333333703, 0.3333333333333334259, 0.3333333333333333703, 0.3333333333333334814, 0.3333333333333332038, 0.3333333333333333703, 0.3333333333333333703),
 ( 1.000000000000000000, 1.000000000000000000, 1.000000000000000222, 0.9999999999999997780, 0.9999999999999997780, 1.000000000000000222, 0.9999999999999997780, 1.000000000000000222, 0.9999999999999992228, 1.000000000000000000, 1.000000000000000000),
 ( 0.3333333333333333703, 0.3333333333333334259, 0.3333333333333334259, 0.3333333333333332593, 0.3333333333333333703, 0.3333333333333334259, 0.3333333333333333703, 0.3333333333333334814, 0.3333333333333332038, 0.3333333333333333703, 0.3333333333333333703),
 ( 0.3333333333333333703, 0.3333333333333334259, 0.3333333333333334259, 0.3333333333333332593, 0.3333333333333333703, 0.3333333333333334259, 0.3333333333333333703, 0.3333333333333334814, 0.3333333333333332038, 0.3333333333333333703, 0.3333333333333333703),
 ( 1.000000000000000000, 1.000000000000000000, 1.000000000000000222, 0.9999999999999997780, 0.9999999999999997780, 1.000000000000000222, 0.9999999999999997780, 1.000000000000000222, 0.9999999999999992228, 1.000000000000000000, 1.000000000000000000) ) ) 
 REPRESENTATION_ITEM ( '' )  SURFACE ( )  );
#54482=CARTESIAN_POINT ( 'NONE',  ( 2.262495435604610527, 2.120074037919957632, 0.04929290001921824566 ) ) ;
#54484=CARTESIAN_POINT ( 'NONE',  ( 6.059193749186201572, -1.568369423792463024, -0.9343120793870243190 ) ) ;
#54491=CARTESIAN_POINT ( 'NONE',  ( 2.144791408438687430, 1.960151896008819117, 0.4867283015469162644 ) ) ;
#54492=CARTESIAN_POINT ( 'NONE',  ( 6.721690211428396289, -2.142211831252617493, 0.5295551626897446740 ) ) ;
#54494=CARTESIAN_POINT ( 'NONE',  ( 4.153051346612735450, 1.574026050290713963, -0.9924080308383613769 ) ) ;
#54499=CARTESIAN_POINT ( 'NONE',  ( 4.775911370473768791, 1.053640644303525331, 1.490772598166143048 ) ) ;
#54503=CARTESIAN_POINT ( 'NONE',  ( 0.8250588069352093878, -1.261192405561472274, 1.190076739608906697 ) ) ;
#54504=CARTESIAN_POINT ( 'NONE',  ( 0.1107398820658512667, -1.707777377628461046, 0.3340355821882161069 ) ) ;
#54505=CARTESIAN_POINT ( 'NONE',  ( 5.971339433669736962, 0.1760496889521658836, -2.301030538967073991 ) ) ;
#54507=CARTESIAN_POINT ( 'NONE',  ( 1.968112693492467979, 1.056634718301739717, 1.769108711375965148 ) ) ;
#54509=CARTESIAN_POINT ( 'NONE',  ( 0.2806244687772480040, -1.977743564115455932, 0.3905345501400147024 ) ) ;
#54512=CARTESIAN_POINT ( 'NONE',  ( 5.858239598252557911, 0.7595784280203803362, 1.709674162104061645 ) ) ;
#54514=CARTESIAN_POINT ( 'NONE',  ( 3.656429697474584017, 1.903630103707624865, 0.1825790434749063051 ) ) ;
#54516=CARTESIAN_POINT ( 'NONE',  ( 5.531908139154323223, -1.397534428995873546, -1.707979418440738195 ) ) ;
#54521=CARTESIAN_POINT ( 'NONE',  ( 6.006510593949522026, -2.110231943656666331, -0.2080817731764383061 ) ) ;
#54523=CARTESIAN_POINT ( 'NONE',  ( 3.364621831457567769, 1.035725732715401470, 2.062151656813861145 ) ) ;
#54524=CARTESIAN_POINT ( 'NONE',  ( 4.123457186961496213, 0.2424046295769199388, -1.946780420294342617 ) ) ;
#54526=CARTESIAN_POINT ( 'NONE',  ( 0.6023038706522118035, 1.956103482322549825, 0.1501044349687257751 ) ) ;
#54530=CARTESIAN_POINT ( 'NONE',  ( 6.016814611094169152, 0.2024578496369993375, 2.006372135924570088 ) ) ;
#54533=CARTESIAN_POINT ( 'NONE',  ( 3.256845431185355633, -0.6256494993409821292, -2.079000826131827129 ) ) ;
#54534=CARTESIAN_POINT ( 'NONE',  ( 1.002369745560643510, -0.9483682245385971488, 1.896766750748935415 ) ) ;
#54539=CARTESIAN_POINT ( 'NONE',  ( 0.4915707408097417797, 1.525207926881542830, 1.386002245639144981 ) ) ;
#54541=CARTESIAN_POINT ( 'NONE',  ( 6.827182134110238110, 6.038038905730811479, 2.505852844092556264 ) ) ;
#54545=CARTESIAN_POINT ( 'NONE',  ( 3.967365900211225593, -1.591558630706500832, -1.059764132600553355 ) ) ;
#54547=CARTESIAN_POINT ( 'NONE',  ( 5.717594842608604289, -1.725906139129701478, 0.3911541089357990497 ) ) ;
#54550=CARTESIAN_POINT ( 'NONE',  ( 0.7381712907078247232, 1.078401568856072412, -1.455492281976622504 ) ) ;
#54552=CARTESIAN_POINT ( 'NONE',  ( 1.200237320533149799, 1.284028115529710190, -1.421911532115504029 ) ) ;
#54553=CARTESIAN_POINT ( 'NONE',  ( 1.486871883557450369, 1.994755712061954123, 0.5540851298423480342 ) ) ;
#54555=AXIS2_PLACEMENT_3D ( 'NONE', #180088, #196338, #14361 ) ;
#54556=CARTESIAN_POINT ( 'NONE',  ( 0.8308620510419548744, 0.1428995296039961560, 1.966335887032538032 ) ) ;
#54557=CARTESIAN_POINT ( 'NONE',  ( 3.299243935302543118, 1.439784963707075649, 1.122460502641378755 ) ) ;
#54558=CARTESIAN_POINT ( 'NONE',  ( 0.3996046210705077595, 1.915144275937111340, -1.287252092841030260 ) ) ;
#54561=CARTESIAN_POINT ( 'NONE',  ( 4.404768648179163471, 0.5469982912414109721, 1.988780625590305329 ) ) ;
#54566=CARTESIAN_POINT ( 'NONE',  ( 5.491282870796595716, 1.858858430755592428, -0.9897807336930256605 ) ) ;
#54568=CARTESIAN_POINT ( 'NONE',  ( 5.986797818411375260, 1.994257276370488219, 0.5558945855626205024 ) ) ;
#54570=CARTESIAN_POINT ( 'NONE',  ( 3.989662644735529451, 1.562606173494068829, 1.493797087085822373 ) ) ;
#54571=CARTESIAN_POINT ( 'NONE',  ( 3.949871522956601932, -1.394395303408175080, -1.461305941245706119 ) ) ;
#54577=CARTESIAN_POINT ( 'NONE',  ( 2.342982756445275427, -1.756855002775299379, -0.9896843009072553432 ) ) ;
#54582=CARTESIAN_POINT ( 'NONE',  ( 6.222915752822945734, 1.412394824171304908, -1.289504995239741714 ) ) ;
#54586=CARTESIAN_POINT ( 'NONE',  ( 4.148064665909578785, 0.9530284220014314522, 1.777003606838889915 ) ) ;
#54589=CARTESIAN_POINT ( 'NONE',  ( 0.01170749999939314084, -0.7329999334961794233, -1.560365621481168086 ) ) ;
#54594=CARTESIAN_POINT ( 'NONE',  ( 5.870339087135666212, -1.187030499695044039, 1.445606174157453738 ) ) ;
#54595=CARTESIAN_POINT ( 'NONE',  ( 6.539320575229251808, 0.004279804010676873348, 1.996977849922920267 ) ) ;
#54596=CARTESIAN_POINT ( 'NONE',  ( 2.430607852509637290, -1.277051959022021066, 1.629327859714514659 ) ) ;
#54600=CARTESIAN_POINT ( 'NONE',  ( 0.7027501817156032171, 1.864177386631180822, 0.7691025790682110008 ) ) ;
#54606=CARTESIAN_POINT ( 'NONE',  ( 5.765228759176680207, 1.768025090248021902, -0.7378185885129113775 ) ) ;
#54614=CARTESIAN_POINT ( 'NONE',  ( 2.518638242371186386, 1.412657066830936392, -1.636333507658905173 ) ) ;
#54617=CARTESIAN_POINT ( 'NONE',  ( 0.7035762090183244055, 1.867434778015097940, -1.004864118554361863 ) ) ;
#54618=CARTESIAN_POINT ( 'NONE',  ( 6.159193757800505153, -1.567253032978152660, -0.9359774744091067245 ) ) ;
#54619=CARTESIAN_POINT ( 'NONE',  ( 2.600799297785437947, 1.585616864491301348, -1.171192495528531330 ) ) ;
#54620=CARTESIAN_POINT ( 'NONE',  ( 4.816621285000030284, -0.6497861859515661198, -1.798733151862880186 ) ) ;
#54623=CARTESIAN_POINT ( 'NONE',  ( 4.826587240018016089, -1.288162778474700287, 1.489951593160773635 ) ) ;
#54624=CARTESIAN_POINT ( 'NONE',  ( 0.2166051034824221788, -0.09641855276349860226, 1.939669501089319015 ) ) ;
#54630=CARTESIAN_POINT ( 'NONE',  ( 5.197880135092803222, 1.287283252470315720, 1.414272151883423589 ) ) ;
#54632=CARTESIAN_POINT ( 'NONE',  ( 1.343116161061377767, 0.4315099961175078991, 2.164003993775004187 ) ) ;
#54634=CARTESIAN_POINT ( 'NONE',  ( 6.533844907621704223, -1.952130696095262463, 0.4912315161729706725 ) ) ;
#54638=CARTESIAN_POINT ( 'NONE',  ( 3.402844027952243167, 0.5003511028610057032, 2.008882729757965890 ) ) ;
#54643=CARTESIAN_POINT ( 'NONE',  ( 0.1808504484964272296, -2.097240537080494516, -0.5235256853268267507 ) ) ;
#54648=CARTESIAN_POINT ( 'NONE',  ( 6.925078400183590333, 2.970608243536181359, 2.408862486266015512 ) ) ;
#54650=CARTESIAN_POINT ( 'NONE',  ( 6.451818256879360725, -1.589883334587833152, -0.6930036952102114345 ) ) ;
#54654=CARTESIAN_POINT ( 'NONE',  ( 3.256751887857904926, -0.5965066610371800859, -1.982489643792232137 ) ) ;
#54655=CARTESIAN_POINT ( 'NONE',  ( 4.077823013788191453, -0.8085361882982607939, 1.956954002425244088 ) ) ;
#54658=CARTESIAN_POINT ( 'NONE',  ( 2.430458318764291192, -1.215629356985904685, 1.549377053225237111 ) ) ;
#54659=CARTESIAN_POINT ( 'NONE',  ( 1.195406425308798148, 1.765864799226088744, -0.7346160280939582066 ) ) ;
#54660=CARTESIAN_POINT ( 'NONE',  ( 4.558679923290005043, -2.046282147472633373, -1.033175111039591698 ) ) ;
#54661=CARTESIAN_POINT ( 'NONE',  ( 2.279681363911123970, 1.122676072794186908, 1.439608767588994365 ) ) ;
#54665=CARTESIAN_POINT ( 'NONE',  ( 2.953388010686915255, -1.773442693046624496, 0.9528950618205129786 ) ) ;
#54666=CARTESIAN_POINT ( 'NONE',  ( 3.696105151714265347, 0.8860871710942277435, -1.750347149911928968 ) ) ;
#54669=CARTESIAN_POINT ( 'NONE',  ( 0.07556134207192893859, 1.990881419511018935, -2.657973000608151448 ) ) ;
#54670=CARTESIAN_POINT ( 'NONE',  ( 6.087849878328269071, -2.080457216024658607, -0.2059406971956292964 ) ) ;
#54671=CARTESIAN_POINT ( 'NONE',  ( 4.961649905909814251, 1.750258134581949232, -0.2615843724830448913 ) ) ;
#54673=CARTESIAN_POINT ( 'NONE',  ( 0.7619990552875830492, 1.083242598816274382, 1.904929396514772444 ) ) ;
#54674=CARTESIAN_POINT ( 'NONE',  ( 6.421804192028983671, 0.9955936683583621605, -1.427223192643598537 ) ) ;
#54677=CARTESIAN_POINT ( 'NONE',  ( 0.2987795159231512176, -2.099866535080958663, 0.9347484894880775386 ) ) ;
#54678=CARTESIAN_POINT ( 'NONE',  ( 0.5740950506661415265, -1.212703583203307511, 1.825263377225619266 ) ) ;
#54679=CARTESIAN_POINT ( 'NONE',  ( 1.858336453454629611, 2.200810804183956026, -0.1644699235988852648 ) ) ;
#54681=CARTESIAN_POINT ( 'NONE',  ( 6.689883316565048865, -1.412897867115006978, -1.648663827357793155 ) ) ;
#54683=CARTESIAN_POINT ( 'NONE',  ( 1.200578840252497947, 1.417437365323451104, -1.573097661806458936 ) ) ;
#54684=CARTESIAN_POINT ( 'NONE',  ( 3.875000000000003553, 2.052068128417946724, -2.337016516192933888E-13 ) ) ;
#54685=CARTESIAN_POINT ( 'NONE',  ( 6.727182134110222478, 4.688348259194305534, 2.751590707055273199 ) ) ;
#54686=CARTESIAN_POINT ( 'NONE',  ( 5.842784322950494769, 0.3761301977728331858, 1.889152344147272178 ) ) ;
#54688=CARTESIAN_POINT ( 'NONE',  ( 1.769451523944377769, 2.192225184321832554, -0.6701302238534474487 ) ) ;
#54693=CARTESIAN_POINT ( 'NONE',  ( 4.020361658589631126, -2.215315801286695585, 0.1640026922601171833 ) ) ;
#54701=CARTESIAN_POINT ( 'NONE',  ( 1.389296306420295224, -0.7283806465635984662, -1.880434191983325398 ) ) ;
#54703=CARTESIAN_POINT ( 'NONE',  ( 6.514137810226229064, 2.057410315668557921, -0.1480156956644717581 ) ) ;
#54706=CARTESIAN_POINT ( 'NONE',  ( 6.005355179794888976, -1.726165566969834586, 0.2220549178573327509 ) ) ;
#54708=CARTESIAN_POINT ( 'NONE',  ( 1.545802484126792109, 1.767419949743149532, 0.09338694931935660748 ) ) ;
#54709=CARTESIAN_POINT ( 'NONE',  ( 0.5279704824466545654, -1.728000714500482982, 1.038995864524896673 ) ) ;
#54710=CARTESIAN_POINT ( 'NONE',  ( 0.09881949811249221560, -0.4921898920670075839, 1.774194203830472993 ) ) ;
#54711=CARTESIAN_POINT ( 'NONE',  ( 4.353268756680241047, 0.5026898720560546430, -2.236438357558430123 ) ) ;
#54712=CARTESIAN_POINT ( 'NONE',  ( 3.837712106225504183, 1.832433245109680531, 0.1787696065849928018 ) ) ;
#54716=CARTESIAN_POINT ( 'NONE',  ( 4.278209411971904075, -1.050932907216840295, 1.492538610026641122 ) ) ;
#54717=CARTESIAN_POINT ( 'NONE',  ( 4.781875055470904634, 1.674888562130649960, -1.122497055794105192 ) ) ;
#54719=CARTESIAN_POINT ( 'NONE',  ( 3.520660345214459586, 1.437014610000959314, -1.747548891452437081 ) ) ;
#54721=CARTESIAN_POINT ( 'NONE',  ( 0.06524607375175436874, -1.882416456675739092, -0.9446200181052357703 ) ) ;
#54723=CARTESIAN_POINT ( 'NONE',  ( 3.455589482447298355, 1.630370400113918095, 1.275915752658786095 ) ) ;
#54726=CARTESIAN_POINT ( 'NONE',  ( 5.637388408723053246, -0.05200288984260474645, 2.120005899716829401 ) ) ;
#54728=CARTESIAN_POINT ( 'NONE',  ( 2.068856375562718508, -1.761265384887151342, -0.7809992120406393790 ) ) ;
#54730=CARTESIAN_POINT ( 'NONE',  ( 0.5374760852590576565, 1.839023226330655625, -0.7055796775109841601 ) ) ;
#54736=CARTESIAN_POINT ( 'NONE',  ( 0.5630927014088433769, 0.6521865704650819939, 2.123503569120980927 ) ) ;
#54737=CARTESIAN_POINT ( 'NONE',  ( 3.663195928028176063, -1.856456087625086182, -0.9943140874985546551 ) ) ;
#54740=CARTESIAN_POINT ( 'NONE',  ( 0.2384088454224670139, -1.803645845812065440, -0.4582378156636581767 ) ) ;
#54745=CARTESIAN_POINT ( 'NONE',  ( 1.195735321641926197, 1.957225868588155837, -0.8166992996602240318 ) ) ;
#54748=CARTESIAN_POINT ( 'NONE',  ( 3.754310534785664899, -1.959519245081872585, -0.09869234604030494018 ) ) ;
#54749=CARTESIAN_POINT ( 'NONE',  ( 1.868271315571629509, 1.111147431007172726, 1.854118885846419262 ) ) ;
#54750=CARTESIAN_POINT ( 'NONE',  ( 1.188719773494644860, 1.394467456127197025, 1.202481090285527632 ) ) ;
#54754=CARTESIAN_POINT ( 'NONE',  ( 3.327794560494615084, 1.698141246764593770, 0.3800555388253792355 ) ) ;
#54758=CARTESIAN_POINT ( 'NONE',  ( 0.5323697292517782786, 1.110078392871534314, -1.854780036684190669 ) ) ;
#54759=CARTESIAN_POINT ( 'NONE',  ( 3.831407535526813124, -1.356092489331266027, 1.492026659919619247 ) ) ;
#54762=CARTESIAN_POINT ( 'NONE',  ( 3.397303563958519401, 1.553371746707431500, 1.213851982216722636 ) ) ;
#54765=CARTESIAN_POINT ( 'NONE',  ( 2.436971693805603856, -1.440716923005976646, -1.302479457752574232 ) ) ;
#54766=CARTESIAN_POINT ( 'NONE',  ( 6.381121926128928479, -1.751337275642101510, -0.7685668267764720341 ) ) ;
#54771=CARTESIAN_POINT ( 'NONE',  ( -0.2106854629475244378, 6.948332279000682732, -2.592197477433130448 ) ) ;
#54776=CARTESIAN_POINT ( 'NONE',  ( 6.475599238194152285, 2.210894796874377288, -0.6610463658997690617 ) ) ;
#54778=CARTESIAN_POINT ( 'NONE',  ( 3.748837004188230182, -0.3782986639458625899, -1.924763881548184230 ) ) ;
#54780=CARTESIAN_POINT ( 'NONE',  ( 2.004529941291322448, -1.955172360644286789, 0.4926429297785542283 ) ) ;
#54782=CARTESIAN_POINT ( 'NONE',  ( 2.343091305525629497, -1.844686447908544746, -1.039184121536258942 ) ) ;
#54786=CARTESIAN_POINT ( 'NONE',  ( 3.099365256270599112, -1.839010575856118823, 0.09107247011905240941 ) ) ;
#54791=CARTESIAN_POINT ( 'NONE',  ( 3.972980863544761654, -1.569110274459505350, 1.426624754300914510 ) ) ;
#54792=CARTESIAN_POINT ( 'NONE',  ( 0.2164228883963260908, -0.09351453081237262599, 1.838880455306932227 ) ) ;
#54795=CARTESIAN_POINT ( 'NONE',  ( 4.622373940358720290, 1.271062617260295458, -1.621988140548079826 ) ) ;
#54797=CARTESIAN_POINT ( 'NONE',  ( 2.612652284633736777, -0.1782932461553646819, 1.832575692395449485 ) ) ;
#54804=CARTESIAN_POINT ( 'NONE',  ( 1.770444396619451632, 1.136427050704125419, 1.891651738277564831 ) ) ;
#54805=CARTESIAN_POINT ( 'NONE',  ( 4.077597889297270406, 2.132052650593726728, -0.7572755323067262845 ) ) ;
#54807=CARTESIAN_POINT ( 'NONE',  ( 3.884856352912366972, -1.692463592844297704, -0.6465920371584426007 ) ) ;
#54808=CARTESIAN_POINT ( 'NONE',  ( 4.100734417499996454, 1.753908128398029787, 0.7709784123341425488 ) ) ;
#54809=CARTESIAN_POINT ( 'NONE',  ( 5.459458695672200435, 1.690470114046587646, 1.195012289465044564 ) ) ;
#54811=CARTESIAN_POINT ( 'NONE',  ( 3.502765367584356859, 1.555092314170872347, -1.211676150289840992 ) ) ;
#54812=CARTESIAN_POINT ( 'NONE',  ( 1.623919080003157545, -1.068017489352061533, -1.603033266432315918 ) ) ;
#54813=CARTESIAN_POINT ( 'NONE',  ( 3.678450976403758066, -1.802590750232490491, -0.4997190347926713794 ) ) ;
#54814=CARTESIAN_POINT ( 'NONE',  ( 3.334905300413065543, 2.251431139208215804, 0.5058342958955232005 ) ) ;
#54815=CARTESIAN_POINT ( 'NONE',  ( 5.055058894927250357, 1.547480351173950552, -1.033501273311630886 ) ) ;
#54819=CARTESIAN_POINT ( 'NONE',  ( 1.612088513325710126, -2.090005036333367539, 0.2590644908504329824 ) ) ;
#54824=CARTESIAN_POINT ( 'NONE',  ( 3.111701630267147412, 1.674174984267240429, 1.301503359413098249 ) ) ;
#54826=CARTESIAN_POINT ( 'NONE',  ( 0.5100284451979911760, -0.7230318888242005526, 1.886137889315203875 ) ) ;
#54831=CARTESIAN_POINT ( 'NONE',  ( 2.284651837757902371, -2.119410549416993916, -0.4241055355862289877 ) ) ;
#54832=CARTESIAN_POINT ( 'NONE',  ( 6.609999999999998543, 2.109033691136730226, 2.032371550245914094 ) ) ;
#54837=CARTESIAN_POINT ( 'NONE',  ( 5.946499988598237252, -1.422611626450220434, 1.429444749906971790 ) ) ;
#54839=CARTESIAN_POINT ( 'NONE',  ( 6.392138156072928901, -0.5583118246898631787, -2.014728688386701272 ) ) ;
#54841=CARTESIAN_POINT ( 'NONE',  ( 0.4095021115802527922, 1.970281763946807541, 1.112102026807944677 ) ) ;
#54849=CARTESIAN_POINT ( 'NONE',  ( 3.070621489812708660, -1.593986286245190565, -0.6595977741803840111 ) ) ;
#54851=CARTESIAN_POINT ( 'NONE',  ( 2.354462415756667593, -1.371198970962312691, 1.118854571612490245 ) ) ;
#54852=CARTESIAN_POINT ( 'NONE',  ( 5.262800499965147871, -1.601618428465928057, 1.518362080380669221 ) ) ;
#54854=CARTESIAN_POINT ( 'NONE',  ( 4.465106368662499214, -1.619631974074808412, 1.206539259511850259 ) ) ;
#54856=CARTESIAN_POINT ( 'NONE',  ( 4.600305182625006317, -0.9987976242244798186, 1.870504488178956759 ) ) ;
#54857=CARTESIAN_POINT ( 'NONE',  ( 4.306267660493944049, 1.238306454277863677, -1.591331080693689559 ) ) ;
#54858=CARTESIAN_POINT ( 'NONE',  ( 4.693523411346745000, 1.687728755266065139, -0.6588045490927648684 ) ) ;
#54862=CARTESIAN_POINT ( 'NONE',  ( 1.393192293617943944, 1.414286473764417185, 1.224485199485196629 ) ) ;
#54863=FACE_OUTER_BOUND ( 'NONE', #95761, .T. ) ;
#54864=CARTESIAN_POINT ( 'NONE',  ( 5.637325938770506362, -0.03788160184842354061, 1.811251791611239170 ) ) ;
#54869=CARTESIAN_POINT ( 'NONE',  ( -0.07025823700084612988, -1.875094440630159065, 0.3749275819610526916 ) ) ;
#54871=CARTESIAN_POINT ( 'NONE',  ( 2.207404936347991065, -1.573848641742966459, -1.171066219227391070 ) ) ;
#54872=ADVANCED_FACE ( 'NONE', ( #209108 ), #62516, .F. ) ;
#54875=CARTESIAN_POINT ( 'NONE',  ( 4.201511661969238531, 1.892856375164463367, -0.9562558712687405649 ) ) ;
#54876=CARTESIAN_POINT ( 'NONE',  ( -0.02968770228140016343, 0.003472272166151618711, -1.826291111852257343 ) ) ;
#54877=CARTESIAN_POINT ( 'NONE',  ( 5.079350664050449105, 1.840474797211266944, -0.7068060451330003824 ) ) ;
#54879=CARTESIAN_POINT ( 'NONE',  ( 1.195565668251681535, 1.858513546554524609, -0.7743570246632487386 ) ) ;
#54881=CARTESIAN_POINT ( 'NONE',  ( -0.01776408051935850912, -2.116861762172245420, -0.04693027993646693707 ) ) ;
#54883=CARTESIAN_POINT ( 'NONE',  ( 3.016144355299533952, 2.060630728401948275, -0.2003171163396169074 ) ) ;
#54887=CARTESIAN_POINT ( 'NONE',  ( 4.593745122936496728, -2.090168268563397547, -0.05157397306862486486 ) ) ;
#54889=CARTESIAN_POINT ( 'NONE',  ( 2.608196206841297826, -0.6965810133783244540, -1.687657492251873226 ) ) ;
#54890=CARTESIAN_POINT ( 'NONE',  ( 1.330386229028382772, 1.216896677575128205, -1.342046333077246967 ) ) ;
#54892=CARTESIAN_POINT ( 'NONE',  ( 6.516270054225981490, -1.036149114087565382, -1.948532232987249424 ) ) ;
#54894=CARTESIAN_POINT ( 'NONE',  ( 3.944505925199864649, 2.195883038551619038, 0.2190369969904403802 ) ) ;
#54897=CARTESIAN_POINT ( 'NONE',  ( 2.701700744156261713, 1.353761940859641966, 1.350867010771430676 ) ) ;
#54900=CARTESIAN_POINT ( 'NONE',  ( 6.812946544903684121, -1.603000239855886466, 1.309962327488790157 ) ) ;
#54902=CARTESIAN_POINT ( 'NONE',  ( 6.339412547452306868, 0.8406370108028878851, -2.024118718474729128 ) ) ;
#54910=CARTESIAN_POINT ( 'NONE',  ( 3.374138713240721454, -1.116850685118627728, 1.500355210514233262 ) ) ;
#54911=CARTESIAN_POINT ( 'NONE',  ( -0.02319159430947542039, 0.2540490248266329965, -1.846305437520213477 ) ) ;
#54915=CARTESIAN_POINT ( 'NONE',  ( 6.684440181240522527, 1.196966437107028547, -1.688953195037292243 ) ) ;
#54916=CARTESIAN_POINT ( 'NONE',  ( 1.528922965942226986, -1.701935853630029083, 1.081086586856384590 ) ) ;
#54920=CARTESIAN_POINT ( 'NONE',  ( 1.517799938645987057, -1.219565478727736574, -1.820545776841306029 ) ) ;
#54921=CARTESIAN_POINT ( 'NONE',  ( 4.828627627824715773, 1.747987318788373656, 0.5269492854979712648 ) ) ;
#54929=CARTESIAN_POINT ( 'NONE',  ( 3.755264181858387840, 1.826884192416846631, -0.2291247506851084581 ) ) ;
#54930=CARTESIAN_POINT ( 'NONE',  ( 0.7330649400898289203, 1.860844449999502492, 0.7684416140155255759 ) ) ;
#54931=CARTESIAN_POINT ( 'NONE',  ( 1.564254705693722602, 1.878715736396416203, -1.323808166466547087 ) ) ;
#54933=CARTESIAN_POINT ( 'NONE',  ( 6.754749089495472703, -0.5201146403621333958, -1.891512521893109700 ) ) ;
#54936=CARTESIAN_POINT ( 'NONE',  ( 3.533378866418676711, -0.1359047358975660202, 1.907598245988059826 ) ) ;
#54940=CARTESIAN_POINT ( 'NONE',  ( 2.208638616728377357, 1.868957087031404285, 0.9372459875717062960 ) ) ;
#54941=CARTESIAN_POINT ( 'NONE',  ( 0.8482696660519238874, 0.5391449902514727777, 1.791282564952957124 ) ) ;
#54942=CARTESIAN_POINT ( 'NONE',  ( 1.616564310028177243, 0.5879328921069119085, -1.928455639302439462 ) ) ;
#54945=CARTESIAN_POINT ( 'NONE',  ( 3.561793593276740388, -1.166016580864630781, 1.292293876973077182 ) ) ;
#54948=CARTESIAN_POINT ( 'NONE',  ( 3.580403817701179658, -1.662759015092404535, -0.4584509792747801793 ) ) ;
#54949=CARTESIAN_POINT ( 'NONE',  ( 3.808297599986898430, 1.548825491099754315, -1.550762550882843094 ) ) ;
#54950=CARTESIAN_POINT ( 'NONE',  ( 5.865903189996044098, 2.174886565178067777, -0.3735607071253948530 ) ) ;
#54954=CARTESIAN_POINT ( 'NONE',  ( 3.749033319061449543, -0.4183670367851847205, -2.130223169982926379 ) ) ;
#54955=CARTESIAN_POINT ( 'NONE',  ( 2.191784710619415044, -0.7813054520266484726, 1.650194661559079456 ) ) ;
#54957=CARTESIAN_POINT ( 'NONE',  ( 4.751218706475199838, 0.2043725092088227169, -2.107420708596031922 ) ) ;
#54958=CARTESIAN_POINT ( 'NONE',  ( 6.609000000000036401, 7.629137130509070275, 2.600000000000000977 ) ) ;
#54961=CARTESIAN_POINT ( 'NONE',  ( 4.704755546018094314, 1.993839351151542427, 1.131020188671335136 ) ) ;
#54963=CARTESIAN_POINT ( 'NONE',  ( 6.620655732516627090, 3.711369741872071693, 2.240970959566997323 ) ) ;
#54965=CARTESIAN_POINT ( 'NONE',  ( 0.3113914200543760336, 1.760583737686383321, -1.181573663439141830 ) ) ;
#54972=CARTESIAN_POINT ( 'NONE',  ( 5.186172726741035355, 1.650080556555008293, 1.158690440749516881 ) ) ;
#54974=CARTESIAN_POINT ( 'NONE',  ( 2.940340207046471921, -1.064325496585982078, 1.766646112275678693 ) ) ;
#54976=CARTESIAN_POINT ( 'NONE',  ( 6.883263157960366918, 3.696842586722656865, 2.460469087180997327 ) ) ;
#54980=CARTESIAN_POINT ( 'NONE',  ( 5.841772037242090931, 2.188765561305112683, 0.1107676204459909497 ) ) ;
#54981=CARTESIAN_POINT ( 'NONE',  ( 5.063125043234593115, -1.117834493326537393, 1.678003986596336761 ) ) ;
#54982=CARTESIAN_POINT ( 'NONE',  ( 3.175182228840720988, 1.170341537027960843, 1.421418621496411516 ) ) ;
#54985=CARTESIAN_POINT ( 'NONE',  ( 1.061059408578250318, 0.3424711756105159877, -1.690240703899626107 ) ) ;
#54987=CARTESIAN_POINT ( 'NONE',  ( 0.7394344266866456072, 2.295659475925112769, -0.1205738325454289578 ) ) ;
#54989=CARTESIAN_POINT ( 'NONE',  ( 0.5798237426192736077, 2.110460337659907371, -0.8156065903286384700 ) ) ;
#54990=CARTESIAN_POINT ( 'NONE',  ( 3.281953686177707219, 1.336396692706752765, 1.627740544975244008 ) ) ;
#54994=CARTESIAN_POINT ( 'NONE',  ( 6.312500000001141309, 1.451031289089316667, 1.451031289060858098 ) ) ;
#54999=CARTESIAN_POINT ( 'NONE',  ( 2.338272602237463360, -1.224740070204191289, -1.730971256048131401 ) ) ;
#55000=CARTESIAN_POINT ( 'NONE',  ( 4.482826657505923684, -1.449732756002309664, 1.683255901693592849 ) ) ;
#55001=CARTESIAN_POINT ( 'NONE',  ( 2.625153213768507854, -2.044362554934661791, 0.7897752707372793779 ) ) ;
#55005=CARTESIAN_POINT ( 'NONE',  ( 5.371523934717264304, -0.2895824386080196322, 1.940264742196501802 ) ) ;
#55010=CARTESIAN_POINT ( 'NONE',  ( 4.289387122732970958, -0.003046686910593982868, -2.120778211268215419 ) ) ;
#55013=CARTESIAN_POINT ( 'NONE',  ( 6.034075718726629844, 1.069613854859407631, -1.878468107683453514 ) ) ;
#55015=CARTESIAN_POINT ( 'NONE',  ( 4.968220237687512864, -1.735557695065930606, -0.6152675618510683453 ) ) ;
#55018=CARTESIAN_POINT ( 'NONE',  ( 6.720655732516681802, 0.008434553976941013345, 1.726293928996263549 ) ) ;
#55022=CARTESIAN_POINT ( 'NONE',  ( 4.504844740329728481, 1.672958716126593082, -1.369014088531981255 ) ) ;
#55026=CARTESIAN_POINT ( 'NONE',  ( 3.362350911093567873, 0.9703303321016673033, 1.931748911306984784 ) ) ;
#55027=CARTESIAN_POINT ( 'NONE',  ( 4.516842978191152547, 1.801120551983675266, 0.8018027747202867150 ) ) ;
#55028=CARTESIAN_POINT ( 'NONE',  ( 4.130049176863603400, 0.2125952495928511154, -1.720681531008328768 ) ) ;
#55030=CARTESIAN_POINT ( 'NONE',  ( 0.6268464039562298140, 0.1668571106153530770, 2.185281662807083691 ) ) ;
#55031=CARTESIAN_POINT ( 'NONE',  ( 1.712421914926518518, -2.289955115012487052, 0.2841115493098354539 ) ) ;
#55032=CARTESIAN_POINT ( 'NONE',  ( 3.778635366994155032, -1.985013167256908240, -0.5533215937988352762 ) ) ;
#55033=CARTESIAN_POINT ( 'NONE',  ( 5.548367435846999207, -1.528527190574509032, 1.197884188273186323 ) ) ;
#55039=CARTESIAN_POINT ( 'NONE',  ( 2.907470687441279455, 1.863611109782586484, 1.181582751932461095 ) ) ;
#55042=CARTESIAN_POINT ( 'NONE',  ( 0.9888277058803507380, 0.1293858107240040412, 1.856492687334237335 ) ) ;
#55043=CARTESIAN_POINT ( 'NONE',  ( -0.1291982275798911617, 0.2270562610647832436, -2.107042122458637756 ) ) ;
#55047=CARTESIAN_POINT ( 'NONE',  ( 6.439398882927052981, 0.6998097629446423662, -1.703160347957879850 ) ) ;
#55049=CARTESIAN_POINT ( 'NONE',  ( 2.676696200465655373, -1.971695749941338560, -0.5996849476793424394 ) ) ;
#55055=CARTESIAN_POINT ( 'NONE',  ( 1.411086320874027855, 1.817183042272657145, 0.9721812696896633410 ) ) ;
#55060=CARTESIAN_POINT ( 'NONE',  ( 6.147136880733683917, -1.866598994669689926, 1.177069016086537356 ) ) ;
#55061=CARTESIAN_POINT ( 'NONE',  ( 0.8960494714182369869, -0.7788709108395329705, 2.016556642405589184 ) ) ;
#55064=CARTESIAN_POINT ( 'NONE',  ( 0.2988868148526523938, -0.2362956723594503705, -1.897694653714178781 ) ) ;
#55065=CARTESIAN_POINT ( 'NONE',  ( 1.217982839071569012, 0.9896824804975331569, -1.756856037137774162 ) ) ;
#55067=CARTESIAN_POINT ( 'NONE',  ( 1.564254705693722602, 1.878715736396416203, -1.323808166466547087 ) ) ;
#55070=CARTESIAN_POINT ( 'NONE',  ( 6.428373272941257710, -0.9058926715965059939, -1.684108486221975953 ) ) ;
#55072=CARTESIAN_POINT ( 'NONE',  ( 1.797508989346347619, -0.6330400025267440833, 1.760413054629046625 ) ) ;
#55073=CARTESIAN_POINT ( 'NONE',  ( 3.766814776335784209, -0.2024620155892907503, -2.006371719556559796 ) ) ;
#55077=CARTESIAN_POINT ( 'NONE',  ( 5.496739094006439785, -0.5105849265115348645, -2.043105244204785453 ) ) ;
#55082=CARTESIAN_POINT ( 'NONE',  ( 3.937764026144819685, -1.931520177269234306, 0.5904599756008358513 ) ) ;
#55084=CARTESIAN_POINT ( 'NONE',  ( 5.986801016505616246, 1.986937900772387078, 0.5535461689152029185 ) ) ;
#55086=CARTESIAN_POINT ( 'NONE',  ( 5.097027542433036018, 1.800287743887505343, -1.196142203056582920 ) ) ;
#55092=CARTESIAN_POINT ( 'NONE',  ( 2.541674676231266083, 1.985806779098505448, -0.8781977400831306735 ) ) ;
#55095=CARTESIAN_POINT ( 'NONE',  ( 1.628196140939692338, 0.1813696128579282696, 1.832309401408799276 ) ) ;
#55097=CARTESIAN_POINT ( 'NONE',  ( 3.368858348882136422, 0.05182064297618373117, -2.191103300807801801 ) ) ;
#55098=CARTESIAN_POINT ( 'NONE',  ( 6.883263157960371359, 1.234153227268469877, 2.265917448979277271 ) ) ;
#55099=CARTESIAN_POINT ( 'NONE',  ( 3.186655532321683637, -2.228779239134215384, -0.3884498486929898742 ) ) ;
#55105=CARTESIAN_POINT ( 'NONE',  ( 5.958207135543601041, 0.7187401461678426529, 1.617382982224302879 ) ) ;
#55107=CARTESIAN_POINT ( 'NONE',  ( 3.281892451336921201, 1.963554472591656053, -0.4431533499722385416 ) ) ;
#55109=CARTESIAN_POINT ( 'NONE',  ( 1.641775563537830829, -1.524941811188656127, -1.452692102197229884 ) ) ;
#55112=CARTESIAN_POINT ( 'NONE',  ( 0.7484202955074462649, -1.954263247020354477, -0.2444711731117015785 ) ) ;
#55115=CARTESIAN_POINT ( 'NONE',  ( 6.099861030166984222, 1.256130149795838813, 1.305615287863689078 ) ) ;
#55119=CARTESIAN_POINT ( 'NONE',  ( 4.434354141042872399, 1.834536173243521917, 0.3649259964926266364 ) ) ;
#55121=CARTESIAN_POINT ( 'NONE',  ( 5.295788417638883416, -1.460108768623759712, -1.467927865959644640 ) ) ;
#55131=CARTESIAN_POINT ( 'NONE',  ( 4.633228507203630997, 0.002057781214020309134, -1.962046631861932067 ) ) ;
#55133=CARTESIAN_POINT ( 'NONE',  ( 2.442732317853496760, 1.238130588059358717, 1.591075322344523535 ) ) ;
#55134=CARTESIAN_POINT ( 'NONE',  ( -0.1108833634137009749, 4.092508091048022933, -2.451885048449681470 ) ) ;
#55135=CARTESIAN_POINT ( 'NONE',  ( -0.05867695357848409787, -1.698172713885632401, -1.384993232510664640 ) ) ;
#55137=CARTESIAN_POINT ( 'NONE',  ( 2.372138566722302500, -1.154253592077842727, 1.471842878544210809 ) ) ;
#55139=CARTESIAN_POINT ( 'NONE',  ( 3.920185232657522167, -2.007512044478755531, 0.1524921764288286741 ) ) ;
#55142=CARTESIAN_POINT ( 'NONE',  ( 4.446934944069580453, -1.891868754433777555, -0.9506184929228760350 ) ) ;
#55144=CARTESIAN_POINT ( 'NONE',  ( 5.811005889236001032, -1.634438611397070806, 1.270752202701043609 ) ) ;
#55145=CARTESIAN_POINT ( 'NONE',  ( 1.066094891556510271, -1.323660828648763221, 1.618394379614082723 ) ) ;
#55146=CARTESIAN_POINT ( 'NONE',  ( 6.620655732516607550, 2.431211045237289703, 2.455576803978098521 ) ) ;
#55147=CARTESIAN_POINT ( 'NONE',  ( 6.510779352739587189, 1.350450193652263930, -1.228632259304612839 ) ) ;
#55155=CARTESIAN_POINT ( 'NONE',  ( 5.971340724440283410, -1.642497693792897451, -0.9790476769208908969 ) ) ;
#55166=CARTESIAN_POINT ( 'NONE',  ( 6.134388704033759687, 0.6352148712998658686, 1.913799669303432927 ) ) ;
#55167=CARTESIAN_POINT ( 'NONE',  ( 0.7156801077207708417, 1.735845614737155707, 1.217653249118654468 ) ) ;
#55169=CARTESIAN_POINT ( 'NONE',  ( -0.1394461523061196473, 5.719344608737997326, -2.874279450258274249 ) ) ;
#55172=CARTESIAN_POINT ( 'NONE',  ( 3.467590214127397541, -0.3886977184213887271, 1.930520482988388631 ) ) ;
#55173=CARTESIAN_POINT ( 'NONE',  ( 5.062125140741547291, -1.117816439015427044, 1.678017345901124058 ) ) ;
#55176=CARTESIAN_POINT ( 'NONE',  ( 5.261759291836726860, 1.077959533075742993, 1.907929976554381124 ) ) ;
#55178=CARTESIAN_POINT ( 'NONE',  ( 3.645458630373909159, -1.458056112162182893, -1.259071146193297075 ) ) ;
#55180=CARTESIAN_POINT ( 'NONE',  ( -0.1294898018152201291, 4.092224548688067287, -2.481517387982924649 ) ) ;
#55181=CARTESIAN_POINT ( 'NONE',  ( 0.1709339574563934483, -1.438030690398562239, 1.674123062825278563 ) ) ;
#55186=CARTESIAN_POINT ( 'NONE',  ( 4.680490344776488065, 1.214988973509235848, -1.549875580164503663 ) ) ;
#55187=CARTESIAN_POINT ( 'NONE',  ( -0.04160512940111232155, -1.735061556407999417, -0.8725848562033207134 ) ) ;
#55188=CARTESIAN_POINT ( 'NONE',  ( 4.406893533441514244, -0.4431801161997659944, -1.963548474556547685 ) ) ;
#55189=CARTESIAN_POINT ( 'NONE',  ( 5.905696578591778767, 0.4397782949263558949, 2.255800006528754675 ) ) ;
#55191=CARTESIAN_POINT ( 'NONE',  ( 3.696024482597393135, 0.8403398683093143973, -1.660512506883378370 ) ) ;
#55197=CARTESIAN_POINT ( 'NONE',  ( 6.005435553056907239, -2.074886976054179488, 0.2565860541952763585 ) ) ;
#55199=EDGE_LOOP ( 'NONE', ( #187167, #13871, #69767, #64564 ) ) ;
#55203=CARTESIAN_POINT ( 'NONE',  ( 1.013953575274041619, -0.8186894766500467657, -1.631917417583013341 ) ) ;
#55205=CARTESIAN_POINT ( 'NONE',  ( 2.935853622122220674, -1.419245300609776272, -0.9961633832534546595 ) ) ;
#55210=CARTESIAN_POINT ( 'NONE',  ( 6.702019227905350540, 0.8390156466466727192, -2.002601388009570549 ) ) ;
#55211=CARTESIAN_POINT ( 'NONE',  ( 5.707590141996651489, -0.4392596013848491521, 1.771934311310577659 ) ) ;
#55212=CARTESIAN_POINT ( 'NONE',  ( 3.432423435979839343, -1.172226468724973936, 1.572839002276872566 ) ) ;
#55217=CARTESIAN_POINT ( 'NONE',  ( 4.072980787186268437, -1.570383936966279981, 1.425070900414181052 ) ) ;
#55220=CARTESIAN_POINT ( 'NONE',  ( 1.252880909328604186, -0.4992908342843911940, -2.009044966204868388 ) ) ;
#55222=CARTESIAN_POINT ( 'NONE',  ( 4.864059028628820336, 0.6975124644323873468, -2.109029365712757897 ) ) ;
#55224=CARTESIAN_POINT ( 'NONE',  ( 2.286107107991880216, 1.843941258665306115, -1.372366127498450883 ) ) ;
#55226=CARTESIAN_POINT ( 'NONE',  ( 0.4616703453074429975, -0.5288386019042885522, 1.889040479230045255 ) ) ;
#55233=CARTESIAN_POINT ( 'NONE',  ( 2.988426722125224977, -1.135634098421594240, 1.538566774472991616 ) ) ;
#55235=CARTESIAN_POINT ( 'NONE',  ( 4.366008003732903653, 0.8140541678068600184, 1.520548270592293028 ) ) ;
#55236=CARTESIAN_POINT ( 'NONE',  ( 2.782435679340321322, -0.5899881929209308540, -1.928257399728677379 ) ) ;
#55237=CARTESIAN_POINT ( 'NONE',  ( 4.307493173298723832, 1.414159744579394307, -1.812179591053430627 ) ) ;
#55238=CARTESIAN_POINT ( 'NONE',  ( 3.778848203065594102, -2.179170165155080774, -0.6077416658978853636 ) ) ;
#55239=CARTESIAN_POINT ( 'NONE',  ( 6.692010077984027916, -0.9030311967607449475, 1.901034507416640373 ) ) ;
#55242=CARTESIAN_POINT ( 'NONE',  ( 4.235448325177215700, -1.219352424245947253, -1.282881785660697771 ) ) ;
#55244=CARTESIAN_POINT ( 'NONE',  ( 0.9203736287852108955, 1.361359823012283865, -1.844092865855660124 ) ) ;
#55245=CARTESIAN_POINT ( 'NONE',  ( 5.454971364017034752, 0.3553261626877933788, -1.806350769464920569 ) ) ;
#55247=CARTESIAN_POINT ( 'NONE',  ( 5.753911783233988331, 0.8852683131516884130, 2.004867968450708915 ) ) ;
#55252=CARTESIAN_POINT ( 'NONE',  ( 5.477033855465498924, 1.911541192706748715, 0.7957256658025002594 ) ) ;
#55253=CARTESIAN_POINT ( 'NONE',  ( 1.745327705122714956, 0.3399549603602426417, -1.987498286102694411 ) ) ;
#55255=CARTESIAN_POINT ( 'NONE',  ( 3.897031312914517098, 1.626875583419360005, -1.031562066982329329 ) ) ;
#55257=CARTESIAN_POINT ( 'NONE',  ( 0.7916362837351547110, -0.06200823681477837107, -2.220726283632424192 ) ) ;
#55266=CARTESIAN_POINT ( 'NONE',  ( 2.945700582358207864, 1.385421296276163838, 1.389331660621349274 ) ) ;
#55270=CARTESIAN_POINT ( 'NONE',  ( 0.2563952634283462872, -2.062181505987520147, -0.05231737696831904177 ) ) ;
#55273=CARTESIAN_POINT ( 'NONE',  ( 0.4095021115802527922, 1.970281763946807541, 1.112102026807944677 ) ) ;
#55277=CARTESIAN_POINT ( 'NONE',  ( 1.176777557245082262, -0.04011917365428705612, -1.870279424122413658 ) ) ;
#55278=CARTESIAN_POINT ( 'NONE',  ( 6.872404467231180369, -0.3655807773644218495, 1.700417682701503841 ) ) ;
#55279=EDGE_CURVE ( 'NONE', #11451, #150638, #47365, .T. ) ;
#55281=CARTESIAN_POINT ( 'NONE',  ( 4.739868811304373430, 2.185674081084403753, 0.1610935195608814985 ) ) ;
#55282=CARTESIAN_POINT ( 'NONE',  ( 5.631924041214952936, -1.458266564992457104, -1.788428398515107043 ) ) ;
#55283=CARTESIAN_POINT ( 'NONE',  ( 6.731718603199120743, -1.342629487124985532, -1.563498854789405534 ) ) ;
#55284=CARTESIAN_POINT ( 'NONE',  ( 2.009616874778739071, -0.9155987108000520625, -1.712560621339030309 ) ) ;
#55289=CARTESIAN_POINT ( 'NONE',  ( 3.252577435111691617, 1.966644794889659043, -0.4445022851852917234 ) ) ;
#55293=CARTESIAN_POINT ( 'NONE',  ( 0.8733498553583609603, 1.760202786292342170, -0.4843115980177821744 ) ) ;
#55299=CARTESIAN_POINT ( 'NONE',  ( 6.614142728931415860, -0.9689641062460941923, -1.818880834187324824 ) ) ;
#55304=CARTESIAN_POINT ( 'NONE',  ( 5.268225494782738494, 2.017278875131154336, -0.1011536798302767465 ) ) ;
#55305=CARTESIAN_POINT ( 'NONE',  ( 5.373765183877965868, 0.4349513647441177744, -2.178143251680577208 ) ) ;
#55310=CARTESIAN_POINT ( 'NONE',  ( 5.664934882792908688, -1.862169278537370465, -0.8832596265169431193 ) ) ;
#55311=CARTESIAN_POINT ( 'NONE',  ( 4.518204034511161815, -1.842447959940773705, 0.8197716922626956393 ) ) ;
#55317=CARTESIAN_POINT ( 'NONE',  ( 4.112657547701242144, 0.6818919214185631406, -1.897407125352356339 ) ) ;
#55318=CARTESIAN_POINT ( 'NONE',  ( 3.152128525617302834, -1.393660036906883226, 1.203213496783587910 ) ) ;
#55320=CARTESIAN_POINT ( 'NONE',  ( 1.946342613620454243, 0.8805590942474375016, -2.133279852835685109 ) ) ;
#55322=CARTESIAN_POINT ( 'NONE',  ( 3.884175197147401892, -1.069116497136082700, 1.878640351225938421 ) ) ;
#55326=CARTESIAN_POINT ( 'NONE',  ( 3.321888608656462072, -1.742702400767569992, 1.498638621658739511 ) ) ;
#55328=CARTESIAN_POINT ( 'NONE',  ( 2.307302758404996545, -0.4121581357655336175, 1.824517092411604979 ) ) ;
#55329=CARTESIAN_POINT ( 'NONE',  ( 6.455938704688762186, 1.966190342143339764, -0.1448359745850023028 ) ) ;
#55332=CARTESIAN_POINT ( 'NONE',  ( 1.717678464306471309, -0.2677704892378242607, 2.190511422692428045 ) ) ;
#55337=CARTESIAN_POINT ( 'NONE',  ( 5.928588038458690868, 1.899881307248694418, 0.5261610973047344819 ) ) ;
#55338=CARTESIAN_POINT ( 'NONE',  ( 5.584705890799654071, -2.250326009109602232, -0.5107660753775817852 ) ) ;
#55339=CARTESIAN_POINT ( 'NONE',  ( 6.848144937404742727, -0.7948834574948275833, 1.681425573653466676 ) ) ;
#55340=CARTESIAN_POINT ( 'NONE',  ( 4.223522562419862680, 0.2575905095270197287, -2.046390306194557418 ) ) ;
#55347=CARTESIAN_POINT ( 'NONE',  ( 6.619587810436369679, 0.3779085275587866777, -2.137903583376862038 ) ) ;
#55348=CARTESIAN_POINT ( 'NONE',  ( 6.539320575229250920, 0.004279804010676861205, 1.996977849922921155 ) ) ;
#55349=CARTESIAN_POINT ( 'NONE',  ( 5.038538826285253514, -1.576363729006284187, 0.9512496309353533075 ) ) ;
#55351=CARTESIAN_POINT ( 'NONE',  ( 6.620655732516652847, 2.468432086671234149, 2.210906647470804565 ) ) ;
#55357=CARTESIAN_POINT ( 'NONE',  ( 0.5219363917940004205, -1.903054291476031112, 0.1877445768119419822 ) ) ;
#55358=CARTESIAN_POINT ( 'NONE',  ( 2.254462534575492949, -1.370001101035130509, 1.120467526443365891 ) ) ;
#55360=CARTESIAN_POINT ( 'NONE',  ( 6.498696042004469930, -1.974701156420979542, -0.3904368389309967324 ) ) ;
#55362=CARTESIAN_POINT ( 'NONE',  ( 3.901880894453650050, -0.9877729052028583201, -1.641157072818617779 ) ) ;
#55364=CARTESIAN_POINT ( 'NONE',  ( 5.441845355777640059, 1.321472782793672085, 1.460616519443626249 ) ) ;
#55365=CARTESIAN_POINT ( 'NONE',  ( 6.433853624855537134, -1.958103210868083810, 0.4948410764434567066 ) ) ;
#55367=CARTESIAN_POINT ( 'NONE',  ( 2.992876365407059147, 1.605230647100181596, -0.9602576221170722182 ) ) ;
#55368=CARTESIAN_POINT ( 'NONE',  ( 6.586556832619708146, -1.693200007625778492, -0.3281344310326217428 ) ) ;
#55370=CARTESIAN_POINT ( 'NONE',  ( 2.051678093609669240, -1.773579625386853875, -1.313098587465796774 ) ) ;
#55373=CARTESIAN_POINT ( 'NONE',  ( 0.2388349330707796314, -2.000390574439359526, -0.5026286349697464129 ) ) ;
#55380=CARTESIAN_POINT ( 'NONE',  ( 2.752462066230080495, -2.064650614848703825, -0.1547973748374023295 ) ) ;
#55384=CARTESIAN_POINT ( 'NONE',  ( 0.5221358870723510348, -2.009748826802790322, 0.2000887155638417791 ) ) ;
#55387=CARTESIAN_POINT ( 'NONE',  ( 0.07459516483346911864, 0.7642615113957001993, -1.841455071455591064 ) ) ;
#55389=CARTESIAN_POINT ( 'NONE',  ( 6.011092252151500226, 2.013677719867816851, 0.1017325769363253418 ) ) ;
#55390=CARTESIAN_POINT ( 'NONE',  ( 5.647645028696767433, 1.886156043628923529, -0.3343808708002778407 ) ) ;
#55392=CARTESIAN_POINT ( 'NONE',  ( 3.720431430916489646, 2.081484170424623859, 0.6860852429351402826 ) ) ;
#55394=CARTESIAN_POINT ( 'NONE',  ( 2.707167837304753633, 1.638089068140319071, -0.9866689735503200165 ) ) ;
#55398=CARTESIAN_POINT ( 'NONE',  ( 1.493767781312784981, -2.000855510370867840, 0.2496291452861176263 ) ) ;
#55400=CARTESIAN_POINT ( 'NONE',  ( 6.163654587501778970, 1.125051486859941718, 1.880622087419632882 ) ) ;
#55402=CARTESIAN_POINT ( 'NONE',  ( 3.153030191819999217, -1.409141575680799230, -0.9942448187586181430 ) ) ;
#55404=CARTESIAN_POINT ( 'NONE',  ( -0.1405533004718754753, 0.003749010675345095921, -1.720146753850452681 ) ) ;
#55409=CARTESIAN_POINT ( 'NONE',  ( 0.3616705494772323726, -0.5269360983083425376, 1.889693748445469224 ) ) ;
#55411=CARTESIAN_POINT ( 'NONE',  ( 0.07536363704235479744, 6.947016338497881804, -2.739277465201896078 ) ) ;
#55415=CARTESIAN_POINT ( 'NONE',  ( 3.615680081246709143, -0.5227945197113766929, 1.734396599632443525 ) ) ;
#55419=CARTESIAN_POINT ( 'NONE',  ( 4.441949062027584993, -1.118158961774197380, -1.425077651336349227 ) ) ;
#55424=CARTESIAN_POINT ( 'NONE',  ( 5.494539847903294749, 1.833519193728103014, 0.3179774322314922741 ) ) ;
#55426=EDGE_CURVE ( 'NONE', #185672, #57833, #120784, .T. ) ;
#55427=CARTESIAN_POINT ( 'NONE',  ( 2.935058904569508353, -1.567653816607515127, -1.100626458259999385 ) ) ;
#55435=CARTESIAN_POINT ( 'NONE',  ( 1.412182186510477777, 1.403042805649477920, -1.550086674462275216 ) ) ;
#55437=CARTESIAN_POINT ( 'NONE',  ( 6.809608091213839920, -0.4246860027747687560, 1.886121680295702596 ) ) ;
#55439=CARTESIAN_POINT ( 'NONE',  ( 2.801551268311212262, -0.5745519774189576934, 1.732868645247707562 ) ) ;
#55441=CARTESIAN_POINT ( 'NONE',  ( 2.021601768330282045, -0.4154675118966509317, 1.866563793090275203 ) ) ;
#55442=CARTESIAN_POINT ( 'NONE',  ( 1.592182281804704003, 0.9734619808988297374, -1.712098776470400763 ) ) ;
#55443=CARTESIAN_POINT ( 'NONE',  ( 3.192849282005063127, 1.532776493767808113, 1.192484549457759613 ) ) ;
#55444=VERTEX_POINT ( 'NONE', #35325 ) ;
#55447=CARTESIAN_POINT ( 'NONE',  ( 6.807467476049567701, -1.494282888040651347, -1.108890849153229441 ) ) ;
#55449=CARTESIAN_POINT ( 'NONE',  ( 3.902672080109194752, -2.098000727953463151, -0.3078000538283761078 ) ) ;
#55457=CARTESIAN_POINT ( 'NONE',  ( 4.195794211080963620, -0.6966935528937777677, 1.687730213881050600 ) ) ;
#55462=CARTESIAN_POINT ( 'NONE',  ( 4.944154083221365070, 1.865701114312174225, 0.1370711555178441010 ) ) ;
#55464=CARTESIAN_POINT ( 'NONE',  ( 2.016120517293042536, -0.9081000056256024466, -1.699051532819460197 ) ) ;
#55471=CARTESIAN_POINT ( 'NONE',  ( 1.669685637109643794, 1.462710821638053105, 1.530943346549427320 ) ) ;
#55475=CARTESIAN_POINT ( 'NONE',  ( 4.944224162298806569, -0.9806570695735459253, 1.823293813017504039 ) ) ;
#55476=CARTESIAN_POINT ( 'NONE',  ( 0.9777802892061361328, -1.796362506263927017, -0.4033719513514141264 ) ) ;
#55479=CARTESIAN_POINT ( 'NONE',  ( 5.186298777384058312, 1.878100352198919465, 1.325219426413627000 ) ) ;
#55483=CARTESIAN_POINT ( 'NONE',  ( 1.588225008415785844, -2.281566021618782081, -0.2212011980115625998 ) ) ;
#55486=CARTESIAN_POINT ( 'NONE',  ( 4.945229674018920107, 0.6074099038847360355, -1.844580613826458437 ) ) ;
#55491=CARTESIAN_POINT ( 'NONE',  ( 5.871340715825057011, -1.643613990083541143, -0.9773822251149253404 ) ) ;
#55492=CARTESIAN_POINT ( 'NONE',  ( 5.137907791644652278, 2.014008302827663854, -0.1037760698975112861 ) ) ;
#55496=CARTESIAN_POINT ( 'NONE',  ( 3.292999148915674468, 1.648261854606505983, 1.285964787075925431 ) ) ;
#55497=CARTESIAN_POINT ( 'NONE',  ( 0.8656337812406755816, 0.8672032905003168590, 1.542741919674812223 ) ) ;
#55500=CARTESIAN_POINT ( 'NONE',  ( 4.752058238528302780, 0.8743775744927633209, 2.119134945200305431 ) ) ;
#55501=CARTESIAN_POINT ( 'NONE',  ( 2.185155941524752787, -0.7450687668543712894, 1.572906677108532936 ) ) ;
#55505=CARTESIAN_POINT ( 'NONE',  ( 1.827078023146003760, -1.230200505038709036, 1.222094307470813934 ) ) ;
#55506=CARTESIAN_POINT ( 'NONE',  ( 2.541674676231266083, 1.985806779098505448, -0.8781977400831306735 ) ) ;
#55508=CARTESIAN_POINT ( 'NONE',  ( 4.065638850954083061, 1.320825628876612479, 1.523796413913918846 ) ) ;
#55509=CARTESIAN_POINT ( 'NONE',  ( 3.218750000000001776, -0.7852924748298164559, 1.895863743164153847 ) ) ;
#55511=CARTESIAN_POINT ( 'NONE',  ( 0.6219390430294257088, -1.027834010343916749, -1.629101698904901863 ) ) ;
#55513=CARTESIAN_POINT ( 'NONE',  ( 4.219114570843409240, 1.715941675311336123, -1.410698622648777434 ) ) ;
#55515=CARTESIAN_POINT ( 'NONE',  ( 6.883263157960393563, 1.268976584491373183, 2.060807272249213451 ) ) ;
#55520=CARTESIAN_POINT ( 'NONE',  ( 0.4873737393681918384, -2.093643541511390538, -0.7425801828774351021 ) ) ;
#55522=CARTESIAN_POINT ( 'NONE',  ( 6.232861002365865488, -1.862453515449840724, -0.6167318247369477646 ) ) ;
#55525=CARTESIAN_POINT ( 'NONE',  ( 6.450461099754450700, 0.7004171410973459855, 2.151357330220986963 ) ) ;
#55527=CARTESIAN_POINT ( 'NONE',  ( 3.086439574430835275, 1.148074821921121647, -1.713452782031915200 ) ) ;
#55531=CARTESIAN_POINT ( 'NONE',  ( 4.745289220334846902, -1.444806058459674691, -1.188008360142885245 ) ) ;
#55532=CARTESIAN_POINT ( 'NONE',  ( 4.060950141605116137, -0.9941625748171744048, 1.420652921118512602 ) ) ;
#55533=CARTESIAN_POINT ( 'NONE',  ( 3.421201824283449877, -1.039729455425863147, -1.395559870880677789 ) ) ;
#55535=CARTESIAN_POINT ( 'NONE',  ( 0.4160993436025617886, -1.233022138464324291, -1.932370275504050827 ) ) ;
#55537=CARTESIAN_POINT ( 'NONE',  ( 4.599217410553211316, -0.5561919879800735211, 2.015351296096360656 ) ) ;
#55538=CARTESIAN_POINT ( 'NONE',  ( 6.474560584146490605, -0.09798994077552795889, -1.939597741719009338 ) ) ;
#55542=CARTESIAN_POINT ( 'NONE',  ( 0.2115648487451895210, 1.930418618556551946, 0.5826528611774861588 ) ) ;
#55543=CARTESIAN_POINT ( 'NONE',  ( 0.7387272492362946252, 1.258454933865692293, -1.706699550108881080 ) ) ;
#55545=FACE_OUTER_BOUND ( 'NONE', #85232, .T. ) ;
#55548=CARTESIAN_POINT ( 'NONE',  ( 2.666775373343560407, 0.7166976873529753433, 1.995817185486338019 ) ) ;
#55550=CARTESIAN_POINT ( 'NONE',  ( 4.266095019097836172, 0.8626762044917112293, 1.609013669381313294 ) ) ;
#55557=CARTESIAN_POINT ( 'NONE',  ( 2.619404093423041591, 1.708565301817746018, 1.076861402434741821 ) ) ;
#55558=CARTESIAN_POINT ( 'NONE',  ( 5.684669477433477169, -2.151827843693389308, -0.4886931181809702207 ) ) ;
#55560=CARTESIAN_POINT ( 'NONE',  ( 3.414761196407948063, -1.412042937968212231, 1.212274210779472394 ) ) ;
#55566=CARTESIAN_POINT ( 'NONE',  ( 4.652862234063231739, -1.464609733205827879, 1.089778014065109657 ) ) ;
#55570=CARTESIAN_POINT ( 'NONE',  ( 0.2097273702015931829, -1.334265282896981208, -1.107180986369905362 ) ) ;
#55571=CARTESIAN_POINT ( 'NONE',  ( 6.544863656343847147, -1.481929198830441274, -1.092355128777318107 ) ) ;
#55572=CARTESIAN_POINT ( 'NONE',  ( 5.813149116883928436, 2.032396105517704221, 1.093072976444838362 ) ) ;
#55574=CARTESIAN_POINT ( 'NONE',  ( 0.1751657365761209451, 0.002452341591326848407, -2.044164811867712483 ) ) ;
#55576=CARTESIAN_POINT ( 'NONE',  ( 5.835437120055854798, -1.464435618476932488, 1.771446943145409847 ) ) ;
#55579=CARTESIAN_POINT ( 'NONE',  ( 5.629731426258720361, -1.187751674602673058, -1.445209747047627946 ) ) ;
#55580=CARTESIAN_POINT ( 'NONE',  ( 3.761887187967042134, 0.6396200178584460216, -1.802413552503052463 ) ) ;
#55582=CARTESIAN_POINT ( 'NONE',  ( 5.303435803989668074, 1.802500012205746183, 1.273053691228965389 ) ) ;
#55587=CARTESIAN_POINT ( 'NONE',  ( 5.637388408723053246, -0.05200288984260474645, 2.120005899716829401 ) ) ;
#55588=CARTESIAN_POINT ( 'NONE',  ( 2.415413485888187495, 2.061215426621319402, 1.037632957015870661 ) ) ;
#55589=CARTESIAN_POINT ( 'NONE',  ( 4.053139552913617827, 1.658577106941661272, -1.047563642765911185 ) ) ;
#55590=CARTESIAN_POINT ( 'NONE',  ( 0.2682999959267086676, -0.8333247372044670920, -1.774235371720728649 ) ) ;
#55594=CARTESIAN_POINT ( 'NONE',  ( 5.981657729715996297, -0.6748525008196132324, 1.900413905137773529 ) ) ;
#55598=CARTESIAN_POINT ( 'NONE',  ( 3.502934933135398055, 0.5226102428602089622, 2.107139934106997181 ) ) ;
#55600=CARTESIAN_POINT ( 'NONE',  ( 0.7562902151678205787, 0.8540304730459827853, -1.941197329821432227 ) ) ;
#55605=CARTESIAN_POINT ( 'NONE',  ( 1.370465108300226609, -1.309671233245520483, 1.591056919209728138 ) ) ;
#55611=CARTESIAN_POINT ( 'NONE',  ( 3.650944405621194377, 0.2833616294029631111, 1.891055170903446658 ) ) ;
#55612=CARTESIAN_POINT ( 'NONE',  ( 5.735142062806906083, -1.598577407953686746, 0.7598067823499834450 ) ) ;
#55615=CARTESIAN_POINT ( 'NONE',  ( 0.3690327605676722023, -1.530577755691145958, -0.9687459989127805704 ) ) ;
#55617=CARTESIAN_POINT ( 'NONE',  ( 1.393601161502202590, -1.900819510297278025, 0.2380969459827488588 ) ) ;
#55618=CARTESIAN_POINT ( 'NONE',  ( 1.926316106172959230, 1.062450747350886848, 1.776810178100460824 ) ) ;
#55620=CARTESIAN_POINT ( 'NONE',  ( 6.473518811298506925, 1.789458955665638618, -0.5451884755478533240 ) ) ;
#55621=CARTESIAN_POINT ( 'NONE',  ( 2.736711336054332921, 0.2235625380298221498, 1.811883384933578256 ) ) ;
#55622=CARTESIAN_POINT ( 'NONE',  ( 6.656857027519620829, -1.708965229049699053, 1.396003577074665714 ) ) ;
#55625=CARTESIAN_POINT ( 'NONE',  ( 4.598127328184369311, 0.8849438138122868169, -1.863347811608778271 ) ) ;
#55631=CARTESIAN_POINT ( 'NONE',  ( 0.2741912710782665741, -2.129148944087058126, 0.4243047986705119068 ) ) ;
#55633=CARTESIAN_POINT ( 'NONE',  ( 4.218171724704827596, -1.107204882465680607, -1.856345114869990320 ) ) ;
#55634=CARTESIAN_POINT ( 'NONE',  ( 4.424476369979273294, -0.8654530498428643082, -1.825003331238822746 ) ) ;
#55635=CARTESIAN_POINT ( 'NONE',  ( 6.620655732516649294, 0.5674144795907026806, 2.226195167976598110 ) ) ;
#55640=CARTESIAN_POINT ( 'NONE',  ( 2.255092540634635156, 0.09411513195021348199, -2.014433103604281960 ) ) ;
#55645=CARTESIAN_POINT ( 'NONE',  ( 5.361546783204238942, -1.511448857895525855, -1.171587532507123441 ) ) ;
#55649=CARTESIAN_POINT ( 'NONE',  ( 3.954703970953522774, -1.882481274494081980, -0.7231244775810635739 ) ) ;
#55652=CARTESIAN_POINT ( 'NONE',  ( 6.352575194690796678, 0.5466354793271388512, 1.635951794362877187 ) ) ;
#55656=CARTESIAN_POINT ( 'NONE',  ( 5.360568611784803927, -1.355617963529401893, 1.289147430649554948 ) ) ;
#55658=CARTESIAN_POINT ( 'NONE',  ( 2.008725816923035978, 0.6454906730102347723, 1.967154155859623055 ) ) ;
#55661=CARTESIAN_POINT ( 'NONE',  ( 0.9664229901367870079, -1.967894173845801120, -0.4390061282484732930 ) ) ;
#55662=CARTESIAN_POINT ( 'NONE',  ( 1.581973821214562204, 0.9331543445117953528, 1.552620351220496353 ) ) ;
#55669=CARTESIAN_POINT ( 'NONE',  ( 5.958580499074456860, -1.820587016788511647, -0.5960958187592230173 ) ) ;
#55670=CARTESIAN_POINT ( 'NONE',  ( 0.07499057489264349119, 0.002531239327734788758, -1.955573237620360061 ) ) ;
#55676=CARTESIAN_POINT ( 'NONE',  ( 3.151412294154242844, -1.766339975446712174, -1.245920677233211649 ) ) ;
#55679=CARTESIAN_POINT ( 'NONE',  ( 1.248456593208754795, 1.040400552670465162, -1.847740296886036582 ) ) ;
#55680=CARTESIAN_POINT ( 'NONE',  ( 6.018537349360657984, 1.224031959697377658, -1.354583942311540667 ) ) ;
#55682=CARTESIAN_POINT ( 'NONE',  ( 2.389859445797080095, -0.8464594663768022498, 1.780534303499915927 ) ) ;
#55683=CARTESIAN_POINT ( 'NONE',  ( 4.113462262696740979, 1.539102623358613586, 1.134910093507961237 ) ) ;
#55686=CARTESIAN_POINT ( 'NONE',  ( 4.685976223243822680, -1.210123887884282601, -1.553869430650482997 ) ) ;
#55687=CARTESIAN_POINT ( 'NONE',  ( 6.603083112279575673, -0.4245024861969335928, 1.902271653767301007 ) ) ;
#55694=CARTESIAN_POINT ( 'NONE',  ( 5.408822929737922003, -0.4686924282312036061, -1.853821656156897646 ) ) ;
#55696=CARTESIAN_POINT ( 'NONE',  ( 0.6224627697807673110, -1.182292326766160251, -1.863150505713020211 ) ) ;
#55698=CARTESIAN_POINT ( 'NONE',  ( 5.883453010584854148, 0.1459518013421389204, -2.007843741401983184 ) ) ;
#55699=CARTESIAN_POINT ( 'NONE',  ( -0.02319159430947542386, 1.394398620246390275, -2.068318759734718792 ) ) ;
#55703=CARTESIAN_POINT ( 'NONE',  ( 2.506376218629560171, 2.069854378281150709, 0.05321039126485183068 ) ) ;
#55708=CARTESIAN_POINT ( 'NONE',  ( 0.6905621207787122628, -2.145541755201633372, -0.2633910710312590275 ) ) ;
#55714=CARTESIAN_POINT ( 'NONE',  ( 6.925078400183559246, 1.280611897634201357, 1.970548662192173284 ) ) ;
#55716=CARTESIAN_POINT ( 'NONE',  ( 5.273917847569165929, 1.525789468548454986, -0.8241785451228255122 ) ) ;
#55718=CARTESIAN_POINT ( 'NONE',  ( 2.272408084759574454, -0.9721198248324285363, -1.827787434591138238 ) ) ;
#55719=CARTESIAN_POINT ( 'NONE',  ( 4.868830934094980911, -0.2605620880507720227, -2.101091820269097354 ) ) ;
#55722=CARTESIAN_POINT ( 'NONE',  ( 1.569134323820881027, 1.734487354001874371, 0.9329377246683704383 ) ) ;
#55724=CARTESIAN_POINT ( 'NONE',  ( 0.7207899753199145110, 1.446443371814851941, -1.251069288267861346 ) ) ;
#55725=CARTESIAN_POINT ( 'NONE',  ( 4.787240309336779909, 1.696446081987776022, 1.541789747812449818 ) ) ;
#55726=CARTESIAN_POINT ( 'NONE',  ( 1.857752496991037061, 1.820901040755190214, -0.1330985588276211995 ) ) ;
#55730=( BOUNDED_CURVE ( )  B_SPLINE_CURVE ( 3, ( #66649, #82934, #67715, #131744 ),
 .UNSPECIFIED., .F., .T. ) 
 B_SPLINE_CURVE_WITH_KNOTS ( ( 4, 4 ),
 ( 0.000000000000000000, 0.4999999999999967248 ),
 .UNSPECIFIED. ) 
 CURVE ( )  GEOMETRIC_REPRESENTATION_ITEM ( )  RATIONAL_B_SPLINE_CURVE ( ( 1.000000000000000222, 0.3333333333333378112, 0.3333333333333334259, 0.9999999999999958922 ) ) 
 REPRESENTATION_ITEM ( '' )  );
#55731=CARTESIAN_POINT ( 'NONE',  ( 2.883067256526872235, -1.861736025891271407, -0.7665772676846579481 ) ) ;
#55732=CARTESIAN_POINT ( 'NONE',  ( 3.362109073961420780, -1.959717995770013932, 0.09162775335717905645 ) ) ;
#55735=CARTESIAN_POINT ( 'NONE',  ( 0.07536363704233051131, 7.629137130509080045, -2.744199452819145790 ) ) ;
#55736=CARTESIAN_POINT ( 'NONE',  ( 6.474567623737461197, -0.1010770918629246007, -2.088323083193554641 ) ) ;
#55737=CARTESIAN_POINT ( 'NONE',  ( 5.137463350450376609, -1.253266684191740810, -1.249936613051380485 ) ) ;
#55739=CARTESIAN_POINT ( 'NONE',  ( 0.2522424171345696298, 0.8426718423822797677, 2.023156535103701970 ) ) ;
#55740=CARTESIAN_POINT ( 'NONE',  ( 0.1513755341013711675, 0.6631104863988640519, 1.609371435944781936 ) ) ;
#55742=CARTESIAN_POINT ( 'NONE',  ( 0.1333692844072802142, 2.017199222642913625, -2.468757726274827036 ) ) ;
#55743=CARTESIAN_POINT ( 'NONE',  ( 6.170549959107765936, 1.581869261771509994, 1.668023173554062266 ) ) ;
#55745=CARTESIAN_POINT ( 'NONE',  ( 5.958250847983307175, 1.314789979124462382, 1.130330842948763514 ) ) ;
#55746=CARTESIAN_POINT ( 'NONE',  ( 1.664966938652842954, -1.558911317520403239, 1.562347339584921002 ) ) ;
#55747=CARTESIAN_POINT ( 'NONE',  ( 0.5675212215028536678, 1.888217155380923939, 1.071465276393630539 ) ) ;
#55749=CARTESIAN_POINT ( 'NONE',  ( 1.411481693167576434, -1.991701369327549154, 0.7188087792022596068 ) ) ;
#55750=CARTESIAN_POINT ( 'NONE',  ( 2.875000000000002220, 2.052068128417948056, -1.638482584539516883E-13 ) ) ;
#55751=CARTESIAN_POINT ( 'NONE',  ( 6.827182134110192813, 3.687242579989722824, 2.603029107617850002 ) ) ;
#55752=CARTESIAN_POINT ( 'NONE',  ( 4.418917755230268085, 1.760988537516799068, 0.7813691060932350663 ) ) ;
#55753=CARTESIAN_POINT ( 'NONE',  ( 1.137687779795238052, -0.04954009815814026940, 2.220905934856795216 ) ) ;
#55755=CARTESIAN_POINT ( 'NONE',  ( 1.664052950329899971, 1.182993008014191938, 1.963431667052175422 ) ) ;
#55759=CARTESIAN_POINT ( 'NONE',  ( 3.897323497890590627, -0.2185073706607517652, -2.210542651646169698 ) ) ;
#55765=CARTESIAN_POINT ( 'NONE',  ( 1.301407962653992501, 1.352153127569672098, -1.496052916918483522 ) ) ;
#55767=CARTESIAN_POINT ( 'NONE',  ( 6.250444628687981563, -2.052375444028589957, -0.2060817263721328174 ) ) ;
#55770=CARTESIAN_POINT ( 'NONE',  ( 0.08126746489400815676, -0.8690269180096841239, 1.623235155968821841 ) ) ;
#55773=CARTESIAN_POINT ( 'NONE',  ( 1.633702333402654361, 0.8778187100713531477, -1.536624053347920071 ) ) ;
#55774=CARTESIAN_POINT ( 'NONE',  ( 6.434187037261335007, -1.398866626055271123, -1.024706079042293938 ) ) ;
#55775=CARTESIAN_POINT ( 'NONE',  ( 6.216323138650166058, 1.627425874425829200, 0.6175015193602851893 ) ) ;
#55776=CARTESIAN_POINT ( 'NONE',  ( 3.702894494004336678, 1.966553232070525237, 1.177740060511106135 ) ) ;
#55777=CARTESIAN_POINT ( 'NONE',  ( 3.187279605439637287, -0.7454021820463945236, 1.683677988101241141 ) ) ;
#55780=CARTESIAN_POINT ( 'NONE',  ( 3.100428009929767637, -0.5284298666012043899, -1.747434388548900541 ) ) ;
#55781=CARTESIAN_POINT ( 'NONE',  ( 3.762342404062005041, 1.897698010425369786, -0.6819954029829021769 ) ) ;
#55783=CARTESIAN_POINT ( 'NONE',  ( 2.993345543732395697, 1.941157005910049138, -1.162047774482692697 ) ) ;
#55785=CARTESIAN_POINT ( 'NONE',  ( 5.930723256393157783, 2.028624516890007445, 0.5651790528119063906 ) ) ;
#55787=CARTESIAN_POINT ( 'NONE',  ( 3.859880467719906783, -0.6038372105774907350, 1.980330894321411517 ) ) ;
#55790=CARTESIAN_POINT ( 'NONE',  ( 6.024112365460934981, -2.104525519549589330, 0.2592714029671301934 ) ) ;
#55793=CARTESIAN_POINT ( 'NONE',  ( 1.330555237386946255, 1.856516968354186892, 0.5143259067744552215 ) ) ;
#55801=CARTESIAN_POINT ( 'NONE',  ( 0.7740458967449159733, 0.4260312260581029520, -2.180030009307607042 ) ) ;
#55802=CARTESIAN_POINT ( 'NONE',  ( 2.467921950875014314, 2.065534160692492627, -0.4097329821706324204 ) ) ;
#55806=CARTESIAN_POINT ( 'NONE',  ( 0.1505322013598429098, -0.3980627942141829467, -1.824191605747552014 ) ) ;
#55811=CARTESIAN_POINT ( 'NONE',  ( 0.8617730121942971389, -1.675286201960282995, -1.300076073212981242 ) ) ;
#55814=CARTESIAN_POINT ( 'NONE',  ( 3.560947883890089649, 1.548132398191165882, -1.204989647596923508 ) ) ;
#55815=CARTESIAN_POINT ( 'NONE',  ( 1.762795743007524063, -1.528684080660724920, 1.528680807790387286 ) ) ;
#55816=CARTESIAN_POINT ( 'NONE',  ( 1.786409390178132162, 1.601450680722369846, -0.9084932335857234253 ) ) ;
#55819=CARTESIAN_POINT ( 'NONE',  ( 3.855166295008194410, 1.726882014201753801, -0.2153026951989250037 ) ) ;
#55823=CARTESIAN_POINT ( 'NONE',  ( 1.059701713109785670, 0.4209238396889224965, -2.120155868012041811 ) ) ;
#55824=CARTESIAN_POINT ( 'NONE',  ( 3.040388574052850235, 1.915307028720541371, -0.6297779509270851062 ) ) ;
#55825=CARTESIAN_POINT ( 'NONE',  ( 6.825078400183582694, 6.033236438919748146, 2.839236806905225841 ) ) ;
#55826=CARTESIAN_POINT ( 'NONE',  ( 0.1632417891470130944, -1.931755829615459996, -0.9703963252955111196 ) ) ;
#55828=CARTESIAN_POINT ( 'NONE',  ( 2.518385046665332361, 1.288922565979855994, -1.491834565112426070 ) ) ;
#55829=CARTESIAN_POINT ( 'NONE',  ( 6.609000000000047947, 7.053019707385148607, 2.498153760597703332 ) ) ;
#55830=CARTESIAN_POINT ( 'NONE',  ( 2.595178948467924851, -0.6067665810922833192, 1.844924317596825070 ) ) ;
#55835=CARTESIAN_POINT ( 'NONE',  ( -0.1106856583840877956, 1.350702755748961481, -2.249207804202685956 ) ) ;
#55840=CARTESIAN_POINT ( 'NONE',  ( 6.370204010553460527, 1.178711257604664109, 1.983722394024198143 ) ) ;
#55842=CARTESIAN_POINT ( 'NONE',  ( 3.678520109711844732, 1.247982904293298168, -1.513573691770610186 ) ) ;
#55844=CARTESIAN_POINT ( 'NONE',  ( 1.037732671793228700, -1.587836052788630381, 1.242728777923551187 ) ) ;
#55846=CARTESIAN_POINT ( 'NONE',  ( 2.571616345043222118, 1.500848072127154653, 1.493768111954131284 ) ) ;
#55849=CARTESIAN_POINT ( 'NONE',  ( 3.134520880496122874, -1.623366475481220261, 0.8686021547102339424 ) ) ;
#55853=CARTESIAN_POINT ( 'NONE',  ( 4.482752736079084421, -1.382999391253452615, 1.607682512923855445 ) ) ;
#55854=CARTESIAN_POINT ( 'NONE',  ( 0.2867153840934755782, 1.362228626754984573, 1.238794746348782505 ) ) ;
#55858=CARTESIAN_POINT ( 'NONE',  ( 4.833308404897187494, -1.885807738700072678, 0.8313965460460555068 ) ) ;
#55860=CARTESIAN_POINT ( 'NONE',  ( 0.9777802892061361328, -1.796362506263927017, -0.4033719513514141264 ) ) ;
#55865=CARTESIAN_POINT ( 'NONE',  ( 1.471597369358583318, 0.1596246592955492538, -2.201166978212334424 ) ) ;
#55866=CARTESIAN_POINT ( 'NONE',  ( 3.567884397833466892, 2.208229897964437249, -0.4915367949662046154 ) ) ;
#55869=CARTESIAN_POINT ( 'NONE',  ( 4.148556159002002808, 1.777816924242316299, 0.3471830323657533746 ) ) ;
#55870=CARTESIAN_POINT ( 'NONE',  ( 3.801880972252824176, -0.9895533254376009946, -1.640229128645746215 ) ) ;
#55871=CARTESIAN_POINT ( 'NONE',  ( 5.213363469605923228, -1.747142239327776903, -1.110534646669825376 ) ) ;
#55873=CARTESIAN_POINT ( 'NONE',  ( 2.571113415349820297, 0.09854779587974149546, -1.969128565948689458 ) ) ;
#55874=CARTESIAN_POINT ( 'NONE',  ( 0.9910896068104644296, 1.700257414060426964, -0.9055851426933002601 ) ) ;
#55875=CARTESIAN_POINT ( 'NONE',  ( 4.153091690245942047, -1.555063956268587066, -1.039456662654779207 ) ) ;
#55876=CARTESIAN_POINT ( 'NONE',  ( 3.528207577792912719, -1.374008478127983546, -1.853924954965507466 ) ) ;
#55877=CARTESIAN_POINT ( 'NONE',  ( 3.666312420855986520, -0.7522870471967492145, -1.702408540065254883 ) ) ;
#55881=CARTESIAN_POINT ( 'NONE',  ( 0.7156196601619690956, -0.3068708111382661974, 2.083463767009658962 ) ) ;
#55886=CARTESIAN_POINT ( 'NONE',  ( 3.041385797112206912, 0.05609166564453024750, 2.120036961950934273 ) ) ;
#55888=CARTESIAN_POINT ( 'NONE',  ( 0.8440173190735723585, -1.284739210308597723, -1.558479848626155961 ) ) ;
#55893=CARTESIAN_POINT ( 'NONE',  ( 0.7026770610618977564, -0.7276074859871293210, -2.035605373553108777 ) ) ;
#55894=CARTESIAN_POINT ( 'NONE',  ( 6.610000000000037623, 2.481806704560181043, 2.105257736569548399 ) ) ;
#55896=CARTESIAN_POINT ( 'NONE',  ( 6.825078400183526739, -0.0002198122173602961866, 1.955566246027613531 ) ) ;
#55899=CARTESIAN_POINT ( 'NONE',  ( 5.471888747823221877, -0.9023485654677811940, 1.803414228490702209 ) ) ;
#55901=CARTESIAN_POINT ( 'NONE',  ( 0.2577194443907256383, 2.166829308800602316, -0.3276212646995610989 ) ) ;
#55903=CARTESIAN_POINT ( 'NONE',  ( 0.2864612384333536932, -1.063250325806489149, 1.997138572869002537 ) ) ;
#55907=CARTESIAN_POINT ( 'NONE',  ( 1.511203358410578179, -1.803099835331838818, 0.6471475864035965975 ) ) ;
#55911=CARTESIAN_POINT ( 'NONE',  ( 2.859633459980165160, 1.716568739768107532, -0.1690650336269062803 ) ) ;
#55913=CARTESIAN_POINT ( 'NONE',  ( 2.248939020346378381, -1.418119551073221851, -1.058484587410456701 ) ) ;
#55914=CARTESIAN_POINT ( 'NONE',  ( 2.508449741805112154, -2.007837557984166299, -0.1460343770829114485 ) ) ;
#55916=CARTESIAN_POINT ( 'NONE',  ( 5.034293675167554660, 1.138177661764948834, -1.890478833441497031 ) ) ;
#55918=CARTESIAN_POINT ( 'NONE',  ( 4.711197416960428264, 1.676919581237258372, -1.125501318796730876 ) ) ;
#55920=CARTESIAN_POINT ( 'NONE',  ( 4.828832153679845973, 1.461785933843419150, -1.536352341152541046 ) ) ;
#55921=CARTESIAN_POINT ( 'NONE',  ( 3.726185550002871327, 2.006962945745351945, 0.1948219989877792713 ) ) ;
#55922=CARTESIAN_POINT ( 'NONE',  ( 4.236430684147264536, 1.109505083903281619, -1.432011362939947574 ) ) ;
#55923=ORIENTED_EDGE ( 'NONE', *, *, #161480, .T. ) ;
#55928=CARTESIAN_POINT ( 'NONE',  ( 1.270139834521961886, -1.189467451172643964, 1.443775233441677130 ) ) ;
#55931=CARTESIAN_POINT ( 'NONE',  ( 6.094382945298186804, -0.9628849012233617888, 1.534170072110131899 ) ) ;
#55937=ORIENTED_EDGE ( 'NONE', *, *, #167677, .T. ) ;
#55938=CARTESIAN_POINT ( 'NONE',  ( 4.206267736153862735, 1.236801365491456028, -1.592660703826812352 ) ) ;
#55942=CARTESIAN_POINT ( 'NONE',  ( 4.623349522974431025, 1.846400237221163865, 1.042759738753673338 ) ) ;
#55945=CARTESIAN_POINT ( 'NONE',  ( 5.975845355540164938, 1.172130763738386650, 1.584922449839619052 ) ) ;
#55947=CARTESIAN_POINT ( 'NONE',  ( 0.4572897223803442102, -1.724499148370229218, 1.038616540587710357 ) ) ;
#55949=CARTESIAN_POINT ( 'NONE',  ( 0.4744016597374626221, -2.101792896462660210, -0.2546084012580717704 ) ) ;
#55951=CARTESIAN_POINT ( 'NONE',  ( 1.381394743813993964, -0.05274132383669553892, 2.069866178704109938 ) ) ;
#55955=CARTESIAN_POINT ( 'NONE',  ( 4.927721519287828755, 1.075078395752477878, -1.792878403059654513 ) ) ;
#55958=CARTESIAN_POINT ( 'NONE',  ( 2.801551268311212262, -0.5745519774189576934, 1.732868645247707562 ) ) ;
#55959=CARTESIAN_POINT ( 'NONE',  ( 1.242487904981701252, 1.745646600027310980, 0.4836494453460266074 ) ) ;
#55963=CIRCLE ( 'NONE', #183974, 0.04999999999999969746 ) ;
#55964=CARTESIAN_POINT ( 'NONE',  ( 3.909358855915114006, 1.891329263188616938, 1.136761501516952766 ) ) ;
#55967=CARTESIAN_POINT ( 'NONE',  ( 3.123589223026546957, -0.3706944625661895976, 1.875830702792554483 ) ) ;
#55969=CARTESIAN_POINT ( 'NONE',  ( 6.021949436824264978, 2.040384406434097464, -0.3501103912618847014 ) ) ;
#55971=CARTESIAN_POINT ( 'NONE',  ( 5.407841436338867602, -0.9846607899807978681, -1.957994596084790206 ) ) ;
#55979=CARTESIAN_POINT ( 'NONE',  ( -0.2409995289980038091, -0.004801160710915519658, -2.000252362011435636 ) ) ;
#55982=CARTESIAN_POINT ( 'NONE',  ( 5.594608825991118195, 2.038665915018455177, 0.3594684214384344378 ) ) ;
#55984=CARTESIAN_POINT ( 'NONE',  ( 1.124625310196948558, 0.3961260723950796314, 1.976952190469769111 ) ) ;
#55988=CARTESIAN_POINT ( 'NONE',  ( 1.711130781365449716, -0.2659051965858104660, 2.175189728913041964 ) ) ;
#55989=CARTESIAN_POINT ( 'NONE',  ( 5.426323838365305186, 1.084245000580752238, -1.468710674947353745 ) ) ;
#55997=CARTESIAN_POINT ( 'NONE',  ( 2.735704033801298785, 1.827604811068459956, 0.2230458208379028362 ) ) ;
#55998=CARTESIAN_POINT ( 'NONE',  ( 6.504166875733549347, -0.8557802559411722410, 1.820156917002911712 ) ) ;
#55999=CARTESIAN_POINT ( 'NONE',  ( 1.511505665106587459, 2.295766583369537095, 0.1122837871174054425 ) ) ;
#56001=CARTESIAN_POINT ( 'NONE',  ( 6.825062041929172985, -1.792332737533608666, -0.7979697884207545000 ) ) ;
#56004=CARTESIAN_POINT ( 'NONE',  ( 3.146637304467227558, 1.866760668956708447, 0.4145885930168375921 ) ) ;
#56006=CARTESIAN_POINT ( 'NONE',  ( 0.6782873735513493818, -1.106163567672680204, -1.749894625276714688 ) ) ;
#56008=CARTESIAN_POINT ( 'NONE',  ( 2.173483749353939842, 1.288726691912587041, 1.646222326975780526 ) ) ;
#56009=CARTESIAN_POINT ( 'NONE',  ( 0.6900581440293825919, -1.856003987442723657, -0.2331820809091043056 ) ) ;
#56010=CARTESIAN_POINT ( 'NONE',  ( 2.073592080879012478, 1.495823877299466087, -1.351946161731142126 ) ) ;
#56013=CARTESIAN_POINT ( 'NONE',  ( 2.682838027602444164, 1.232319236757819292, 1.229298679657732762 ) ) ;
#56017=CARTESIAN_POINT ( 'NONE',  ( 2.947548438991169473, 0.6205982292267105960, -1.609554129922322163 ) ) ;
#56018=CARTESIAN_POINT ( 'NONE',  ( 3.316156725143477146, 1.388770557483296697, -1.695381604771596606 ) ) ;
#56019=CARTESIAN_POINT ( 'NONE',  ( 5.162800556355915838, -1.600310254184673431, 1.519886962452212664 ) ) ;
#56022=CARTESIAN_POINT ( 'NONE',  ( 3.204148022151423802, 0.7856563700287253482, -2.024084340642897661 ) ) ;
#56023=CARTESIAN_POINT ( 'NONE',  ( 2.701551412915685457, -0.5726843992823158480, 1.733614832724015731 ) ) ;
#56025=CARTESIAN_POINT ( 'NONE',  ( 4.153586450535729391, 2.052860580235102095, -0.5180077198428371110 ) ) ;
#56027=CARTESIAN_POINT ( 'NONE',  ( 6.639320575229290533, 2.050619746573784763, 2.302922995531462291 ) ) ;
#56029=CARTESIAN_POINT ( 'NONE',  ( 4.441175045773351648, -1.771670475836329306, -1.454733398674179945 ) ) ;
#56033=CARTESIAN_POINT ( 'NONE',  ( -0.05774110376318035420, -1.308430771297010908, -1.669371405835825550 ) ) ;
#56039=CARTESIAN_POINT ( 'NONE',  ( 5.432267593368638181, -1.591316862017605471, -1.238322901282742805 ) ) ;
#56041=CARTESIAN_POINT ( 'NONE',  ( 3.661030488878083577, 1.629037084659604728, -1.265030972029494993 ) ) ;
#56043=CARTESIAN_POINT ( 'NONE',  ( -0.2409995289980038091, 6.947781193150415646, -2.595509233728268583 ) ) ;
#56047=CARTESIAN_POINT ( 'NONE',  ( 6.714806894218784628, -0.1628439675423892508, 2.155775914164249407 ) ) ;
#56048=CARTESIAN_POINT ( 'NONE',  ( 3.797500137148449362, 1.423962148579031917, -1.427936706820939872 ) ) ;
#56049=CARTESIAN_POINT ( 'NONE',  ( 3.755264181858387840, 1.826884192416846631, -0.2291247506851084581 ) ) ;
#56051=CARTESIAN_POINT ( 'NONE',  ( 0.3227381541650706787, -0.09231566880639123507, 1.722440863776145692 ) ) ;
#56053=CARTESIAN_POINT ( 'NONE',  ( 0.4582085974003520801, -2.167260061518965664, -0.7665384626166712456 ) ) ;
#56055=CARTESIAN_POINT ( 'NONE',  ( 0.2634263733268344398, -2.021796075192600295, -1.015562799429880814 ) ) ;
#56056=CARTESIAN_POINT ( 'NONE',  ( 2.543703448412675261, -1.561038821359970408, -1.413940773279374508 ) ) ;
#56065=CARTESIAN_POINT ( 'NONE',  ( 2.320699612028754188, -0.8158636990020677882, -1.957571985684476212 ) ) ;
#56066=CARTESIAN_POINT ( 'NONE',  ( 3.410577425615939795, -2.218986280728425076, -0.1058077642441344057 ) ) ;
#56067=CARTESIAN_POINT ( 'NONE',  ( 2.537292984272555785, -1.624655320356691801, -1.470880813658273389 ) ) ;
#56070=CARTESIAN_POINT ( 'NONE',  ( 6.883263157960366030, 3.696842586722657309, 2.460469087180996883 ) ) ;
#56072=CARTESIAN_POINT ( 'NONE',  ( 5.670351692713981429, -0.8806477319739226539, -1.753155087565357428 ) ) ;
#56077=CARTESIAN_POINT ( 'NONE',  ( 4.148766697842418694, 2.080301416381886703, 0.4105806053946169376 ) ) ;
#56079=ORIENTED_EDGE ( 'NONE', *, *, #87069, .F. ) ;
#56080=CARTESIAN_POINT ( 'NONE',  ( 5.014612968065254250, 1.493337269798940881, -1.563205770552501761 ) ) ;
#56082=CARTESIAN_POINT ( 'NONE',  ( 4.634224865634020141, 0.3196297827482602605, 1.813140464320086354 ) ) ;
#56085=CARTESIAN_POINT ( 'NONE',  ( 6.632745071352946553, -1.550850273991890127, 0.7898216520882040959 ) ) ;
#56086=CARTESIAN_POINT ( 'NONE',  ( 6.827182134110172385, 0.001020705822878456353, 1.910856149448317165 ) ) ;
#56088=DIRECTION ( 'NONE',  ( -0.9999980456341537316, 0.000000000000000000, -0.001977050295949902767 ) ) ;
#56089=CARTESIAN_POINT ( 'NONE',  ( 4.100566281481184738, -0.6756360485904688851, -2.053482476349233643 ) ) ;
#56093=CARTESIAN_POINT ( 'NONE',  ( 3.555696680978126079, 0.5271953485486252644, -2.096301903996622862 ) ) ;
#56094=CARTESIAN_POINT ( 'NONE',  ( 4.762937738300905721, -1.759534068222264436, -0.8891730789123506451 ) ) ;
#56095=CARTESIAN_POINT ( 'NONE',  ( 4.323420094722703944, -1.284794005617446278, 1.164475704859231131 ) ) ;
#56096=CARTESIAN_POINT ( 'NONE',  ( 0.3280006606478855224, 1.121390616443746602, -1.882787531365101685 ) ) ;
#56097=CARTESIAN_POINT ( 'NONE',  ( 0.8335961714901140018, 0.1734020439737720132, 2.301109984577158762 ) ) ;
#56098=CARTESIAN_POINT ( 'NONE',  ( 3.936836037902153418, 0.2985264485904081111, 2.038899620686930536 ) ) ;
#56099=CARTESIAN_POINT ( 'NONE',  ( 5.864781425808283544, 0.1387459415673809593, -1.937151248970377271 ) ) ;
#56106=CARTESIAN_POINT ( 'NONE',  ( 3.135963548190400019, -1.480894843444351849, -1.636267651353009223 ) ) ;
#56109=CARTESIAN_POINT ( 'NONE',  ( 0.3208626164478335374, -1.658663274457260473, -0.8439677346868018626 ) ) ;
#56110=CARTESIAN_POINT ( 'NONE',  ( -0.02919842301642854021, 4.085261895051949921, -2.628472738367752637 ) ) ;
#56114=CARTESIAN_POINT ( 'NONE',  ( 6.620655732516646630, 0.01042156863438315970, 1.726407961933307700 ) ) ;
#56115=CARTESIAN_POINT ( 'NONE',  ( 6.650350966976619205, -1.419654684173769166, 1.172063944840713523 ) ) ;
#56117=CARTESIAN_POINT ( 'NONE',  ( 1.956002958106726419, 2.055451868484101219, -0.1503645474096800549 ) ) ;
#56120=CARTESIAN_POINT ( 'NONE',  ( 0.07680821025391608436, 6.948789780205374633, -2.405840108717867132 ) ) ;
#56122=CARTESIAN_POINT ( 'NONE',  ( 1.059529560858112340, 0.4028119719261863962, -2.020956803572224736 ) ) ;
#56124=CARTESIAN_POINT ( 'NONE',  ( 5.319803798718575116, 1.092037692397327620, -1.482314076171886708 ) ) ;
#56128=CARTESIAN_POINT ( 'NONE',  ( 4.037865812933420173, -1.521084700717803884, -1.599171214764223636 ) ) ;
#56129=CARTESIAN_POINT ( 'NONE',  ( 0.8784639925019833706, -1.201575844224999301, 1.796657101444132154 ) ) ;
#56131=CARTESIAN_POINT ( 'NONE',  ( 6.539320575229251808, 0.01001626003939220556, 1.796977979958065852 ) ) ;
#56132=CARTESIAN_POINT ( 'NONE',  ( 1.094935803221647186, 1.780670018850015079, 0.9462964651613046119 ) ) ;
#56135=CARTESIAN_POINT ( 'NONE',  ( 6.270165159132718102, 1.906809857242173223, -0.1455798257045255450 ) ) ;
#56137=CARTESIAN_POINT ( 'NONE',  ( 1.779943879855113709, -1.003247456797161652, 1.578688272967261996 ) ) ;
#56138=CARTESIAN_POINT ( 'NONE',  ( 2.940638933469359895, -1.523795050681177710, 1.320827213682006285 ) ) ;
#56142=CARTESIAN_POINT ( 'NONE',  ( 5.584633104594088238, -2.054432100182907561, -0.4627632117069883089 ) ) ;
#56147=CARTESIAN_POINT ( 'NONE',  ( 4.201429114599513959, 1.802380596022877368, -0.9117778440167979559 ) ) ;
#56149=CARTESIAN_POINT ( 'NONE',  ( 6.689892334039674537, -1.344252178338888992, -1.564594595144116695 ) ) ;
#56151=CARTESIAN_POINT ( 'NONE',  ( 4.165412764819938829, 0.2691229397190370576, -2.144731622849817221 ) ) ;
#56156=CARTESIAN_POINT ( 'NONE',  ( 2.049520782779357120, 1.889653518395111753, -1.069053457954100006 ) ) ;
#56159=CARTESIAN_POINT ( 'NONE',  ( 1.399689850468607277, -0.6632477835330424787, -1.717811453623831808 ) ) ;
#56161=CARTESIAN_POINT ( 'NONE',  ( 2.718528139169604341, 2.064530135181973591, 0.7356957861901700646 ) ) ;
#56162=CARTESIAN_POINT ( 'NONE',  ( 3.643696890507712283, -1.711652922788420739, -1.479685619365896265 ) ) ;
#56169=CARTESIAN_POINT ( 'NONE',  ( 5.571497546025357295, 1.705283197966761310, -0.4730582879079441305 ) ) ;
#56171=CARTESIAN_POINT ( 'NONE',  ( 3.510405448560415032, -2.010878083398774052, -0.09666398930169986525 ) ) ;
#56173=CARTESIAN_POINT ( 'NONE',  ( 1.624194961551369776, -1.169474557214383870, -1.751182684644275289 ) ) ;
#56176=CARTESIAN_POINT ( 'NONE',  ( 1.170285302187854981, -0.8824026946198880728, -1.760880109839728647 ) ) ;
#56180=CARTESIAN_POINT ( 'NONE',  ( 6.029554192727712980, -0.2124046070472781211, 1.799012333733180702 ) ) ;
#56184=ADVANCED_FACE ( 'NONE', ( #93725 ), #152349, .F. ) ;
#56185=CARTESIAN_POINT ( 'NONE',  ( 4.891396039733495016, 1.386484060982313249, 1.255958711209571810 ) ) ;
#56187=CARTESIAN_POINT ( 'NONE',  ( 5.893440691016273547, -1.874049447596724427, 0.8799615681738190975 ) ) ;
#56196=CARTESIAN_POINT ( 'NONE',  ( 5.125427350195786325, 0.1941421753944693185, -1.952251141935714696 ) ) ;
#56198=CARTESIAN_POINT ( 'NONE',  ( 1.845077155533506374, -1.080901620906085547, 1.701686244941137183 ) ) ;
#56200=CARTESIAN_POINT ( 'NONE',  ( 0.1698123575781598782, 1.266975945507025081, 1.788028528876134393 ) ) ;
#56202=CARTESIAN_POINT ( 'NONE',  ( 1.792056902697708454, -1.861051795492570049, -0.1884349046137670514 ) ) ;
#56206=CARTESIAN_POINT ( 'NONE',  ( 3.075892445452293344, -0.8556518723831849638, 1.936791289764336010 ) ) ;
#56208=CARTESIAN_POINT ( 'NONE',  ( 4.545415791725802457, 1.850806902094417783, -0.9279678557222792445 ) ) ;
#56210=CARTESIAN_POINT ( 'NONE',  ( 1.575843314401915496, -1.115566239278027671, 1.768056137498266844 ) ) ;
#56211=CARTESIAN_POINT ( 'NONE',  ( 6.620655732516645742, 7.051964633898824886, 2.771890290588132189 ) ) ;
#56212=CARTESIAN_POINT ( 'NONE',  ( 6.493173258741942178, 1.586635928914212013, -0.9027890188317910791 ) ) ;
#56221=CARTESIAN_POINT ( 'NONE',  ( 6.358066468859800757, 0.7272683628555456359, -1.768788954293845528 ) ) ;
#56230=CARTESIAN_POINT ( 'NONE',  ( -0.1353477234830356701, -0.1462924468558861324, -1.883848219957585446 ) ) ;
#56237=CARTESIAN_POINT ( 'NONE',  ( 3.151173496672290852, 1.691593242058259783, -1.008282029756089493 ) ) ;
#56239=CARTESIAN_POINT ( 'NONE',  ( 4.622672832840883039, 0.3474877929729481840, 1.986098205159859909 ) ) ;
#56242=CARTESIAN_POINT ( 'NONE',  ( 4.435597005726048536, 0.9382243502508281763, -1.980580373504265301 ) ) ;
#56244=CARTESIAN_POINT ( 'NONE',  ( 3.241151106802504511, -1.699520814979482264, 0.9069582849330155572 ) ) ;
#56247=CARTESIAN_POINT ( 'NONE',  ( -0.1296875068448125057, 0.2507808023153486054, -1.861542470327881560 ) ) ;
#56255=CARTESIAN_POINT ( 'NONE',  ( 6.620655732516645742, 0.007553340620044741646, 1.826407896915737794 ) ) ;
#56256=CARTESIAN_POINT ( 'NONE',  ( 3.246742594617262334, 1.964541544574874621, 0.4388061624774098890 ) ) ;
#56257=CARTESIAN_POINT ( 'NONE',  ( 4.974093195743899187, 1.996273031041963408, 1.139003188958290780 ) ) ;
#56259=CARTESIAN_POINT ( 'NONE',  ( 3.151044791815108770, 1.598572158793242659, -0.9524303787414812872 ) ) ;
#56265=CARTESIAN_POINT ( 'NONE',  ( 6.146049400653379458, 0.6566722887273982456, 1.984991666494940743 ) ) ;
#56271=CARTESIAN_POINT ( 'NONE',  ( 0.9964003531478006215, -0.4411313887022934033, -1.771462291394958255 ) ) ;
#56273=CARTESIAN_POINT ( 'NONE',  ( 2.144752260294139568, 0.7423094788623717522, 1.567400511497107018 ) ) ;
#56277=CARTESIAN_POINT ( 'NONE',  ( 6.930535145478218695, -1.343193056793217988, 1.706537673033242664 ) ) ;
#56278=CARTESIAN_POINT ( 'NONE',  ( 5.690036971771410101, -0.8169618954828453683, 1.632782195682795257 ) ) ;
#56279=CARTESIAN_POINT ( 'NONE',  ( 3.678520109711844732, 1.247982904293298168, -1.513573691770610186 ) ) ;
#56283=CARTESIAN_POINT ( 'NONE',  ( 3.492942606646631809, -2.044086983709763050, -0.5638711869686771072 ) ) ;
#56286=CARTESIAN_POINT ( 'NONE',  ( 1.920843890195075510, -1.466934385316904565, 1.461102248941518855 ) ) ;
#56289=CARTESIAN_POINT ( 'NONE',  ( 4.899211331842913353, -0.2710981195956448375, -2.204650271698949116 ) ) ;
#56291=CARTESIAN_POINT ( 'NONE',  ( 1.881834863725037277, -0.6175646290925532744, -2.214118314682656852 ) ) ;
#56293=CARTESIAN_POINT ( 'NONE',  ( 0.3210474040165818277, -1.749687966165301312, -0.8873976775175674847 ) ) ;
#56297=CARTESIAN_POINT ( 'NONE',  ( 6.251489360189885325, 1.835807759842246423, -0.1425652098738516838 ) ) ;
#56299=CARTESIAN_POINT ( 'NONE',  ( 2.970861089138316036, -1.445268511421276214, 1.252435071843561731 ) ) ;
#56300=CARTESIAN_POINT ( 'NONE',  ( -0.2104748580754166321, -0.006608320950486632102, -2.103482951484026309 ) ) ;
#56301=CARTESIAN_POINT ( 'NONE',  ( 4.489066604428880503, 1.540008836363685241, -0.7767696631951895858 ) ) ;
#56302=CARTESIAN_POINT ( 'NONE',  ( 2.290250256651988892, -0.7762311197250795214, -1.861343989391924358 ) ) ;
#56303=CARTESIAN_POINT ( 'NONE',  ( 3.498943719384327355, -2.264459259401516267, 0.3945650996091658591 ) ) ;
#56304=CARTESIAN_POINT ( 'NONE',  ( 3.427297576727184047, 0.05164501975941707818, 2.261966552586023749 ) ) ;
#56305=CARTESIAN_POINT ( 'NONE',  ( 5.988920713192999123, -0.3073026951427524356, -2.083404400164515113 ) ) ;
#56308=CARTESIAN_POINT ( 'NONE',  ( 4.674921082483953327, 0.0007207667814621705445, -1.769921774705035755 ) ) ;
#56310=CARTESIAN_POINT ( 'NONE',  ( 0.7445458516137266614, 0.6704725750066173884, 2.192023251310899923 ) ) ;
#56311=CARTESIAN_POINT ( 'NONE',  ( 5.402248404572855378, 1.391679675130308880, -1.205515946264820615 ) ) ;
#56313=CARTESIAN_POINT ( 'NONE',  ( 5.402338782601353806, 1.661146971675907524, -1.429436781345946095 ) ) ;
#56316=CARTESIAN_POINT ( 'NONE',  ( 6.074686117427479992, 1.393331124738606652, -1.531503843499823381 ) ) ;
#56320=CARTESIAN_POINT ( 'NONE',  ( 4.266181944680371707, 0.9094715277466745018, 1.698315803094905041 ) ) ;
#56323=CARTESIAN_POINT ( 'NONE',  ( 1.143189493912871280, 2.142763695547444058, 0.5857495978145771387 ) ) ;
#56334=CARTESIAN_POINT ( 'NONE',  ( 1.557006721180295150, 1.605793932651664813, -1.126831546849601740 ) ) ;
#56337=CARTESIAN_POINT ( 'NONE',  ( 6.637165056451467038, -0.09505199798197358496, -1.959668910398344233 ) ) ;
#56340=CARTESIAN_POINT ( 'NONE',  ( 0.2161854901324336276, -2.218109922327567318, 0.4452641707137113825 ) ) ;
#56344=CARTESIAN_POINT ( 'NONE',  ( 1.071320448993583918, 1.804315561281001123, -0.4931735697189034151 ) ) ;
#56345=CARTESIAN_POINT ( 'NONE',  ( 6.802075984838630518, -1.546572159107060251, 0.7837757703139431875 ) ) ;
#56347=CARTESIAN_POINT ( 'NONE',  ( 4.195009555701286530, 1.760677850468267414, 1.304791629949946019 ) ) ;
#56348=CARTESIAN_POINT ( 'NONE',  ( 4.208297055918253093, -2.301676378859803584, 0.1658454734064350733 ) ) ;
#56349=CARTESIAN_POINT ( 'NONE',  ( 0.3036813079041804087, -0.5503025168475895734, 1.985974332091578809 ) ) ;
#56350=CARTESIAN_POINT ( 'NONE',  ( 2.624863168539525393, -1.811862388431908721, 0.6992392096202125762 ) ) ;
#56352=CARTESIAN_POINT ( 'NONE',  ( 4.992489932941452935, -1.175987964647656536, 1.764448611491518548 ) ) ;
#56354=CARTESIAN_POINT ( 'NONE',  ( 3.850232551101365086, 0.2440307281281335616, -2.001511205109906655 ) ) ;
#56358=CARTESIAN_POINT ( 'NONE',  ( 0.5569169099325711469, -1.540613122784354916, -0.9793164655157863274 ) ) ;
#56363=CARTESIAN_POINT ( 'NONE',  ( 5.770404196412942888, -1.309395467888567754, 1.591445708773833401 ) ) ;
#56369=CARTESIAN_POINT ( 'NONE',  ( 5.602215259268515268, -0.9060462314097734726, 1.805096023085197121 ) ) ;
#56370=CARTESIAN_POINT ( 'NONE',  ( 5.795613637301100241, 2.053263797698097637, -0.8479724704701059323 ) ) ;
#56374=CARTESIAN_POINT ( 'NONE',  ( 3.713790661510278923, -2.030684131657393365, 0.3505542424454102246 ) ) ;
#56375=CARTESIAN_POINT ( 'NONE',  ( 3.568982563115063122, -0.9913999084223243941, 1.755768870528085834 ) ) ;
#56382=CARTESIAN_POINT ( 'NONE',  ( 4.341172599035714619, -1.163090190446917083, 1.646587424817484324 ) ) ;
#56383=CARTESIAN_POINT ( 'NONE',  ( 3.538839456958355889, -1.395042877683351890, -1.201619466480362108 ) ) ;
#56385=CARTESIAN_POINT ( 'NONE',  ( 1.770602872417438967, 1.189155993293121716, 1.977591576486624314 ) ) ;
#56387=CARTESIAN_POINT ( 'NONE',  ( 3.268983376858981327, -1.995845357749256976, -0.8305886511386084692 ) ) ;
#56391=CARTESIAN_POINT ( 'NONE',  ( 3.286738001609066817, -2.216000729425780413, 0.6097190577039524051 ) ) ;
#56394=CARTESIAN_POINT ( 'NONE',  ( 2.834663617355744680, 0.2272019944037397543, 1.856728029318695627 ) ) ;
#56396=CARTESIAN_POINT ( 'NONE',  ( 0.3331948752925878998, -1.804169345717737238, 0.7948754592718260126 ) ) ;
#56400=CARTESIAN_POINT ( 'NONE',  ( 2.139570144280181108, -1.970530345926827742, 0.9937953903183869286 ) ) ;
#56405=CARTESIAN_POINT ( 'NONE',  ( 5.840691970153715218, 0.3840316513750040572, 1.933538979438324867 ) ) ;
#56406=CARTESIAN_POINT ( 'NONE',  ( 6.041700318104039624, -1.667111694969125368, -1.595929347687746747 ) ) ;
#56407=CARTESIAN_POINT ( 'NONE',  ( 0.3968290921660848070, 0.3316028935436679537, 1.933473477243151439 ) ) ;
#56408=CARTESIAN_POINT ( 'NONE',  ( 3.362228078103552953, -2.060403055893737623, 0.09660672959950138139 ) ) ;
#56416=CARTESIAN_POINT ( 'NONE',  ( 5.723135995274492238, -1.960344405425541670, -0.9336216343173405763 ) ) ;
#56418=CARTESIAN_POINT ( 'NONE',  ( 5.565905774130330386, -1.163279849954502287, 1.427249551226833502 ) ) ;
#56419=FACE_OUTER_BOUND ( 'NONE', #46715, .T. ) ;
#56422=CARTESIAN_POINT ( 'NONE',  ( 0.5615140978009087736, 1.851110617189118734, -0.2680550677405246773 ) ) ;
#56423=CARTESIAN_POINT ( 'NONE',  ( 0.8962371694669484246, -0.8134219682564158838, 2.111273946446708738 ) ) ;
#56424=EDGE_CURVE ( 'NONE', #33823, #200465, #143113, .T. ) ;
#56430=CARTESIAN_POINT ( 'NONE',  ( 2.061070876156974041, 0.3059375065844106012, -1.743026645166842803 ) ) ;
#56431=CARTESIAN_POINT ( 'NONE',  ( -0.07574839183086683192, -0.8175154495408327726, -1.727131953450977253 ) ) ;
#56433=CARTESIAN_POINT ( 'NONE',  ( 2.987788816292748173, -1.913300742920095221, 0.09679331860494060080 ) ) ;
#56435=CARTESIAN_POINT ( 'NONE',  ( 3.965261034597372891, 1.688065314258681893, 1.014448032605998584 ) ) ;
#56436=CARTESIAN_POINT ( 'NONE',  ( 6.486581104273712484, -1.239329707167437622, 1.595369898402546838 ) ) ;
#56438=CARTESIAN_POINT ( 'NONE',  ( 2.817106861211693847, -0.1851908181382568019, 1.861470920997858380 ) ) ;
#56439=CARTESIAN_POINT ( 'NONE',  ( 0.01192831195480706721, -0.7772932952810689411, -1.650495136788888040 ) ) ;
#56441=CARTESIAN_POINT ( 'NONE',  ( 2.227434312139275896, 0.001603268854937638837, 2.207063162490217056 ) ) ;
#56444=CARTESIAN_POINT ( 'NONE',  ( 6.496542546517183325, 1.940334402339534581, 0.2891159199209930031 ) ) ;
#56448=CARTESIAN_POINT ( 'NONE',  ( 0.1747926744264677867, 2.047238405490480861, -2.272669950590770149 ) ) ;
#56451=CARTESIAN_POINT ( 'NONE',  ( 3.156751980976373329, -0.5984545454679365273, -1.982000093670479135 ) ) ;
#56455=CARTESIAN_POINT ( 'NONE',  ( 0.8209702097039422997, 1.527776094787479444, -1.321057435245088341 ) ) ;
#56458=CARTESIAN_POINT ( 'NONE',  ( 0.07459516483345089710, 0.2549822845471191868, -1.790622017744479155 ) ) ;
#56460=CARTESIAN_POINT ( 'NONE',  ( 4.886092203009785528, -0.1017338195800701617, 2.013677658187912556 ) ) ;
#56461=CARTESIAN_POINT ( 'NONE',  ( 5.401554078093819378, -1.867474805896391032, 0.4264384668619321528 ) ) ;
#56462=CARTESIAN_POINT ( 'NONE',  ( 6.539320575229233157, 0.001224430076711413356, 2.103502572931112091 ) ) ;
#56463=CARTESIAN_POINT ( 'NONE',  ( 4.230150181147958044, 2.149441460308566754, 0.4267382380854707336 ) ) ;
#56465=CARTESIAN_POINT ( 'NONE',  ( 2.953266587970606594, -1.684550232849800544, 0.9053361341156559439 ) ) ;
#56468=CARTESIAN_POINT ( 'NONE',  ( 6.825078400183573812, 0.002648415797040087893, 1.855566311045192540 ) ) ;
#56469=CARTESIAN_POINT ( 'NONE',  ( 0.1050925082292548940, -0.09611335402343046397, 2.014234898253919326 ) ) ;
#56471=CARTESIAN_POINT ( 'NONE',  ( 6.356982542327763497, 0.3766756592470664744, -2.158781491689326426 ) ) ;
#56473=CARTESIAN_POINT ( 'NONE',  ( 2.502614896622682661, 1.386922750403916105, -1.025098202461205865 ) ) ;
#56479=CARTESIAN_POINT ( 'NONE',  ( 0.5374593765826127800, 1.831924746014142791, -0.7026076897959919743 ) ) ;
#56488=CARTESIAN_POINT ( 'NONE',  ( 2.279683508022036342, 1.776238746767303978, -0.3545518163566608871 ) ) ;
#56493=CARTESIAN_POINT ( 'NONE',  ( 3.527799351415283002, -1.784095038623861651, 0.3127521441018704107 ) ) ;
#56497=CARTESIAN_POINT ( 'NONE',  ( 5.230833165924736683, -1.752262279689630553, -0.6273003976000991466 ) ) ;
#56499=CARTESIAN_POINT ( 'NONE',  ( 3.181152667880298157, 1.511915621606011007, 1.176196041047285812 ) ) ;
#56509=CARTESIAN_POINT ( 'NONE',  ( 1.658266814308974268, -1.477475772113973740, 1.479395487768909501 ) ) ;
#56510=CARTESIAN_POINT ( 'NONE',  ( 6.405299695295086693, 1.602013123205116019, 1.069544239394400797 ) ) ;
#56513=CARTESIAN_POINT ( 'NONE',  ( 1.975362765405625609, 1.747911882041437659, -0.5268472171036930884 ) ) ;
#56514=CARTESIAN_POINT ( 'NONE',  ( 3.475398437264758389, 0.05438942809191969763, -2.206374867412825402 ) ) ;
#56516=CARTESIAN_POINT ( 'NONE',  ( 0.9668906521006037647, -1.505869814250645478, 1.178657042999963878 ) ) ;
#56517=CARTESIAN_POINT ( 'NONE',  ( 1.187880472884972560, -1.246972491003460748, -1.524547227783664249 ) ) ;
#56518=CARTESIAN_POINT ( 'NONE',  ( 3.597155123818120082, -0.5607282099057244729, 1.859368625674643782 ) ) ;
#56522=CARTESIAN_POINT ( 'NONE',  ( 6.842638030098166624, -1.824918384715786823, -0.3633994975895912805 ) ) ;
#56527=CARTESIAN_POINT ( 'NONE',  ( 3.052458795248469414, -1.657928338269051505, 1.433322580492613296 ) ) ;
#56531=CARTESIAN_POINT ( 'NONE',  ( 3.334410585898534674, 1.781380905032422746, 0.3990451814587444024 ) ) ;
#56536=CARTESIAN_POINT ( 'NONE',  ( 4.047608660086319254, 0.6306619223146043840, -1.761260876548931709 ) ) ;
#56538=CARTESIAN_POINT ( 'NONE',  ( 1.594233254470639238, -1.917152233794093164, -0.1895178900164773139 ) ) ;
#56539=CARTESIAN_POINT ( 'NONE',  ( 6.649272889308863732, 1.708415183241232205, -0.9640671636572254455 ) ) ;
#56546=CARTESIAN_POINT ( 'NONE',  ( 0.4392562211190715882, -1.791127875450468920, -1.128673114062600957 ) ) ;
#56549=CARTESIAN_POINT ( 'NONE',  ( 4.627825472248149552, 2.009385113269086087, -0.4979276649561757417 ) ) ;
#56550=CARTESIAN_POINT ( 'NONE',  ( -0.006632162239710717895, -1.840811702136424088, -0.04651623371411393176 ) ) ;
#56554=CARTESIAN_POINT ( 'NONE',  ( 5.572921396849181974, -1.036564899910274784, 2.051751470549934453 ) ) ;
#56558=CARTESIAN_POINT ( 'NONE',  ( 0.2524361811976470471, 0.8832210619409311958, 2.115471854006613750 ) ) ;
#56561=CARTESIAN_POINT ( 'NONE',  ( 4.874914055504836696, 1.811399353594527639, -0.7004420144864877962 ) ) ;
#56566=CARTESIAN_POINT ( 'NONE',  ( 0.05298979808228323346, 0.3483158054882686261, 1.982706882182909025 ) ) ;
#56568=CARTESIAN_POINT ( 'NONE',  ( 5.928922775424462444, -1.700964743930567513, 1.082835439959836776 ) ) ;
#56571=CARTESIAN_POINT ( 'NONE',  ( 3.117214558520535306, -2.014654392230078805, 0.5582205872023697779 ) ) ;
#56572=CARTESIAN_POINT ( 'NONE',  ( 1.041466456679561059, 0.7221788661597589032, -1.615996624379830493 ) ) ;
#56573=CARTESIAN_POINT ( 'NONE',  ( 6.399064592084179992, -0.9530083391863402031, -1.777013033299412292 ) ) ;
#56575=CARTESIAN_POINT ( 'NONE',  ( 4.154423454741348110, -1.699848520643287175, 1.538017723768041023 ) ) ;
#56576=CARTESIAN_POINT ( 'NONE',  ( 2.220290661370280638, -0.001068742171999540608, 1.740516466435287235 ) ) ;
#56579=CARTESIAN_POINT ( 'NONE',  ( 1.704000572024838123, -1.251590786289292101, -1.200144391261132482 ) ) ;
#56581=CARTESIAN_POINT ( 'NONE',  ( 1.574410529035878969, 1.253355123444719998, -1.375888611855519583 ) ) ;
#56582=CARTESIAN_POINT ( 'NONE',  ( 2.260437933566094681, -2.170709518246512815, 0.05174924654302060639 ) ) ;
#56584=CARTESIAN_POINT ( 'NONE',  ( 3.257046257486408969, 0.04465439498414420366, -2.016188763087948033 ) ) ;
#56585=CARTESIAN_POINT ( 'NONE',  ( 1.906250000000001332, 1.895863743164044823, -0.7852924748300882385 ) ) ;
#56587=CARTESIAN_POINT ( 'NONE',  ( 0.4813100693330485957, 1.798698175156054457, -0.6901501906162701427 ) ) ;
#56589=CARTESIAN_POINT ( 'NONE',  ( 4.746434557108095476, 1.141014917558682340, -1.905822037654863133 ) ) ;
#56594=CARTESIAN_POINT ( 'NONE',  ( 0.6807244054014843782, 1.099941690210548106, 1.929793933578232146 ) ) ;
#56595=CARTESIAN_POINT ( 'NONE',  ( 5.723093114104088386, -1.772945450647535948, -0.8403097561825513262 ) ) ;
#56598=CARTESIAN_POINT ( 'NONE',  ( 5.852851842114176861, -1.788828801601877849, 1.385077142625196434 ) ) ;
#56600=CARTESIAN_POINT ( 'NONE',  ( 3.191897189531978096, -1.383228714077057830, -1.530316362279722231 ) ) ;
#56604=CARTESIAN_POINT ( 'NONE',  ( 5.255093269098372488, -1.579555527043162488, -1.001684657140684775 ) ) ;
#56605=CARTESIAN_POINT ( 'NONE',  ( 3.340171489122942816, 0.4179119503955433523, -1.682892220811042616 ) ) ;
#56606=CARTESIAN_POINT ( 'NONE',  ( 3.122313433385078607, 0.04571620936353942150, 1.740018996352102443 ) ) ;
#56607=CARTESIAN_POINT ( 'NONE',  ( 0.2402843302407534631, 2.286812847775396840, 0.1605059593563825382 ) ) ;
#56609=CARTESIAN_POINT ( 'NONE',  ( 4.616787868375789472, -0.1008748965102136408, 2.088423895528898733 ) ) ;
#56610=CARTESIAN_POINT ( 'NONE',  ( 5.912047867262844925, 1.302452500554865722, -1.440575834569270519 ) ) ;
#56613=CARTESIAN_POINT ( 'NONE',  ( 0.4928148368598186946, -2.006445878461552645, 0.2004378712678403507 ) ) ;
#56614=CARTESIAN_POINT ( 'NONE',  ( 0.3695850531008069706, -1.794773754367712693, -1.129184308951653781 ) ) ;
#56619=CARTESIAN_POINT ( 'NONE',  ( 4.617693566336190436, -1.789886777702164089, 0.3589094947460610974 ) ) ;
#56625=CARTESIAN_POINT ( 'NONE',  ( 2.302995500392619022, -0.3493979467522835836, -1.989178256620740548 ) ) ;
#56626=CARTESIAN_POINT ( 'NONE',  ( 5.508869005905306260, 1.674340917344345536, -1.437622030140395912 ) ) ;
#56629=CARTESIAN_POINT ( 'NONE',  ( 2.940123752802700885, -0.9609217279343595930, 1.593531096896059873 ) ) ;
#56635=CARTESIAN_POINT ( 'NONE',  ( 4.688025921862073453, -0.8580590012943272171, 1.611482198803436905 ) ) ;
#56640=CARTESIAN_POINT ( 'NONE',  ( 0.2800716429562755683, -1.702078881456047688, 0.3292984779095942116 ) ) ;
#56641=CARTESIAN_POINT ( 'NONE',  ( 0.4447213192238759771, 0.5506589691408066978, -1.650998906686143464 ) ) ;
#56642=CARTESIAN_POINT ( 'NONE',  ( 5.619831112054756161, -2.252673335196005766, 0.5002786026085581650 ) ) ;
#56644=CARTESIAN_POINT ( 'NONE',  ( 0.8431279278494309137, -1.768909939683245058, 1.056965710194081920 ) ) ;
#56648=CARTESIAN_POINT ( 'NONE',  ( 6.222043071159490957, -1.966323047081437014, -1.189884408624383383 ) ) ;
#56652=CARTESIAN_POINT ( 'NONE',  ( 6.086763352761943580, -0.2763008855245497331, -1.850001521387992565 ) ) ;
#56653=CARTESIAN_POINT ( 'NONE',  ( 3.797043250571481732, -0.1924442655423033721, -1.902711443722324258 ) ) ;
#56655=CARTESIAN_POINT ( 'NONE',  ( 5.549527019956425278, -1.737703232767298545, -1.360318885177333570 ) ) ;
#56656=CARTESIAN_POINT ( 'NONE',  ( 4.452435347768154195, -1.380274204828018991, 1.605734313660161172 ) ) ;
#56658=CARTESIAN_POINT ( 'NONE',  ( 6.883263157960335832, 6.035928496661214560, 2.641088654967935323 ) ) ;
#56661=CARTESIAN_POINT ( 'NONE',  ( 5.865915527372128402, 0.6157079936559420874, -2.029145397309819021 ) ) ;
#56662=CARTESIAN_POINT ( 'NONE',  ( 2.099037836983450589, -0.6160640708386398989, -2.223778577795953115 ) ) ;
#56663=CARTESIAN_POINT ( 'NONE',  ( 3.719154087244529894, -1.729071306366702698, -0.9269775827704658244 ) ) ;
#56665=CARTESIAN_POINT ( 'NONE',  ( 6.578975509608026684, 1.922407110116808981, 0.7477742492353837145 ) ) ;
#56669=CARTESIAN_POINT ( 'NONE',  ( 5.401577436481666439, -1.966305606708594667, 0.4464985920552416720 ) ) ;
#56673=CARTESIAN_POINT ( 'NONE',  ( 2.887734989934476193, -2.027295339332426227, 0.7774125151447373039 ) ) ;
#56675=CARTESIAN_POINT ( 'NONE',  ( 0.2289750728588327566, 1.457791096766167360, -1.540313549178488284 ) ) ;
#56679=CARTESIAN_POINT ( 'NONE',  ( 1.194684731684968693, -0.4980721920408748282, -1.999570191575838818 ) ) ;
#56685=CARTESIAN_POINT ( 'NONE',  ( 3.598220562318912741, -0.9401235635465958751, 1.665135908046413871 ) ) ;
#56686=CARTESIAN_POINT ( 'NONE',  ( 5.365971031753679732, 0.8746336007162245352, 1.538519630229380875 ) ) ;
#56689=CARTESIAN_POINT ( 'NONE',  ( 0.1053163366912619470, 1.342294115999270510, 1.216805694454982767 ) ) ;
#56691=CARTESIAN_POINT ( 'NONE',  ( 6.187116780671887639, 1.595606285689795678, 1.059669358585461962 ) ) ;
#56692=CARTESIAN_POINT ( 'NONE',  ( 0.5903903138861701372, 1.065687334306382184, -1.774900233272216798 ) ) ;
#56694=CARTESIAN_POINT ( 'NONE',  ( 5.893391625361731556, 1.417579469995243091, 1.220656814419220249 ) ) ;
#56695=CARTESIAN_POINT ( 'NONE',  ( 2.842213963582499670, 1.811911227886909614, 0.2232855069103783507 ) ) ;
#56696=CARTESIAN_POINT ( 'NONE',  ( 5.777994779145079640, 1.311685685134782231, 1.774619457157788904 ) ) ;
#56699=CARTESIAN_POINT ( 'NONE',  ( 3.596185909054748553, 0.9300860933913506212, -1.841171126807969349 ) ) ;
#56703=CARTESIAN_POINT ( 'NONE',  ( 0.8257154465432202661, -2.052837714267462754, 0.6772920067378007669 ) ) ;
#56704=CARTESIAN_POINT ( 'NONE',  ( 0.2566020104313873618, -2.170709068928804886, -0.05254486697847670501 ) ) ;
#56706=CARTESIAN_POINT ( 'NONE',  ( 3.690839692606663558, -0.4176960054509891163, -2.120685484085436112 ) ) ;
#56707=CARTESIAN_POINT ( 'NONE',  ( 4.477216424163804831, -1.805109318760585779, -0.9060198856494814379 ) ) ;
#56708=CARTESIAN_POINT ( 'NONE',  ( 2.646866301197240645, -0.3325320220872363675, -1.933311746529025266 ) ) ;
#56709=CARTESIAN_POINT ( 'NONE',  ( 6.620655732516651071, 2.021119449029490589, 2.477762541108457839 ) ) ;
#56715=CARTESIAN_POINT ( 'NONE',  ( 2.501185699981960830, -0.1928336239410358699, 2.007256303757164240 ) ) ;
#56719=CARTESIAN_POINT ( 'NONE',  ( 6.258066496116281741, 0.7254575739856858885, -1.769658340881982816 ) ) ;
#56723=CARTESIAN_POINT ( 'NONE',  ( 4.710564641745673242, 1.930423983604495630, 0.5826390268678026674 ) ) ;
#56726=CARTESIAN_POINT ( 'NONE',  ( 6.668995740727024391, -1.579612310505887685, -0.6930582901118372829 ) ) ;
#56730=CARTESIAN_POINT ( 'NONE',  ( 4.921099816907485547, -0.09337705715995943401, 1.868355541605345671 ) ) ;
#56732=CARTESIAN_POINT ( 'NONE',  ( 1.780221101387355009, -1.146701191353172611, -1.723467693327894068 ) ) ;
#56736=CARTESIAN_POINT ( 'NONE',  ( 0.2984541275833849094, 1.388471424577278235, -1.462460896543740674 ) ) ;
#56737=CARTESIAN_POINT ( 'NONE',  ( 0.7381712907078247232, 1.078401568856072412, -1.455492281976622504 ) ) ;
#56743=CARTESIAN_POINT ( 'NONE',  ( 6.187116780671887639, 1.595606285689795678, 1.059669358585461962 ) ) ;
#56753=CARTESIAN_POINT ( 'NONE',  ( 2.887745953747706373, 1.527789104365802286, 1.529575784674996886 ) ) ;
#56756=CARTESIAN_POINT ( 'NONE',  ( 1.283610819548046011, 0.1505422781087061845, -2.115291873224629082 ) ) ;
#56758=CARTESIAN_POINT ( 'NONE',  ( 6.141596500199405284, -1.324292569296809052, -1.256812384211228428 ) ) ;
#56759=CARTESIAN_POINT ( 'NONE',  ( 1.018749824907847934, 1.819822117139553885, 0.7584178161138422913 ) ) ;
#56760=CARTESIAN_POINT ( 'NONE',  ( 3.322422747544371280, -0.7792853099402965444, -1.746611395919236642 ) ) ;
#56762=CARTESIAN_POINT ( 'NONE',  ( 5.019951571474082996, 1.948400538373602497, -0.2868881896359152806 ) ) ;
#56763=CARTESIAN_POINT ( 'NONE',  ( 0.2341854262303414147, 0.3310631332954366290, 1.913375037591731775 ) ) ;
#56769=CARTESIAN_POINT ( 'NONE',  ( 5.250612361737760025, 1.884661702551674534, 0.3228764834103393100 ) ) ;
#56771=CARTESIAN_POINT ( 'NONE',  ( 0.7278961316968115547, -2.094849050945537972, 0.6941159686642894844 ) ) ;
#56774=CARTESIAN_POINT ( 'NONE',  ( 0.01216826571975513152, -1.911853497171299265, -0.04704278909201110859 ) ) ;
#56776=CARTESIAN_POINT ( 'NONE',  ( 6.727182134110220701, 0.005875948494733078051, 1.810970247402940103 ) ) ;
#56777=CARTESIAN_POINT ( 'NONE',  ( 2.436061438456170958, 1.271862942251865691, 1.633573898902056731 ) ) ;
#56780=CARTESIAN_POINT ( 'NONE',  ( 0.2511322555047851290, -1.735185354305257110, 1.289038484408123963 ) ) ;
#56785=CARTESIAN_POINT ( 'NONE',  ( 6.925078400183593885, 7.629137130509070275, 2.455651831298297338 ) ) ;
#56787=CARTESIAN_POINT ( 'NONE',  ( 4.465268017702548775, -1.683484418668965921, -0.4155383358091616075 ) ) ;
#56790=CARTESIAN_POINT ( 'NONE',  ( 2.114207291064807759, 2.064986537539798661, -0.1480984254652456533 ) ) ;
#56791=CARTESIAN_POINT ( 'NONE',  ( 3.269268187362909028, 1.912946029434154038, -0.9076713616091285353 ) ) ;
#56794=CARTESIAN_POINT ( 'NONE',  ( 2.272252165359678333, -0.9238012212633615050, -1.739302338446031548 ) ) ;
#56796=CARTESIAN_POINT ( 'NONE',  ( -0.2108831679770960255, -0.001785917861228669690, -1.896958272444612792 ) ) ;
#56797=CARTESIAN_POINT ( 'NONE',  ( 4.242302733825270344, 0.6093012942862492398, 2.209731468575569124 ) ) ;
#56798=CARTESIAN_POINT ( 'NONE',  ( 2.367563199519676420, 1.790531440309536926, -0.3556685536310541518 ) ) ;
#56802=CARTESIAN_POINT ( 'NONE',  ( 2.900642264033539863, -1.984120583840060625, -0.3400495124021261084 ) ) ;
#56803=CARTESIAN_POINT ( 'NONE',  ( 3.291801117278610800, -1.314073873198824627, -1.456807609480186061 ) ) ;
#56807=CARTESIAN_POINT ( 'NONE',  ( 6.140588758375521650, -1.766823853066697536, 1.117321708369632516 ) ) ;
#56808=CARTESIAN_POINT ( 'NONE',  ( 4.610057705051894494, -0.7578761767026606089, -1.599493228202266470 ) ) ;
#56810=CARTESIAN_POINT ( 'NONE',  ( 0.9377431681640016059, 0.8850447378907433382, -2.004962588275795543 ) ) ;
#56812=CARTESIAN_POINT ( 'NONE',  ( 5.156098626313831090, -1.256936769724174674, 1.203943403725541206 ) ) ;
#56815=CARTESIAN_POINT ( 'NONE',  ( 0.1932713599902321500, -1.417659354009516148, -1.810318517150938389 ) ) ;
#56817=CARTESIAN_POINT ( 'NONE',  ( 5.923113090906284128, 0.7054357044574584013, 1.584025686543149680 ) ) ;
#56818=CARTESIAN_POINT ( 'NONE',  ( 1.541937560865791479, -1.600244427420342896, -1.519961040588948986 ) ) ;
#56820=CARTESIAN_POINT ( 'NONE',  ( 5.775877569751362017, -2.119564319632438743, 0.4699819441058172842 ) ) ;
#56822=CARTESIAN_POINT ( 'NONE',  ( 0.7435476276109568294, 0.4067398897551637305, -2.077755800567067546 ) ) ;
#56823=CARTESIAN_POINT ( 'NONE',  ( 2.656250000000001332, -1.895863743164027504, 0.7852924748301256530 ) ) ;
#56824=CARTESIAN_POINT ( 'NONE',  ( 6.727182134110196721, 7.629137130509074716, 2.689055895399253160 ) ) ;
#56825=CARTESIAN_POINT ( 'NONE',  ( 4.295867091898570855, -0.7379356464434319030, 1.779637345161827922 ) ) ;
#56826=CARTESIAN_POINT ( 'NONE',  ( 1.348599501924132804, 1.090831829848055046, -1.934932191954039427 ) ) ;
#56831=CARTESIAN_POINT ( 'NONE',  ( 3.422728177422405871, -0.9015832817733639981, -2.030284994954335787 ) ) ;
#56838=CARTESIAN_POINT ( 'NONE',  ( 1.863907939170056149, -0.1017519224979606118, -2.013985838549677609 ) ) ;
#56840=CARTESIAN_POINT ( 'NONE',  ( 6.092244811693771744, 1.020019244021443727, -1.792768071708307431 ) ) ;
#56844=CARTESIAN_POINT ( 'NONE',  ( 6.286628787680052177, 1.509496725765889114, -0.8662470760552234417 ) ) ;
#56847=CARTESIAN_POINT ( 'NONE',  ( 1.756752346989236768, -1.514669478205426190, -0.9150583790542564655 ) ) ;
#56848=CARTESIAN_POINT ( 'NONE',  ( 0.1764080092822375156, 1.496053712750060383, 1.352152247781977179 ) ) ;
#56849=CARTESIAN_POINT ( 'NONE',  ( 0.2922019606856861018, 1.531309713818730822, -1.022077305420886040 ) ) ;
#56850=CARTESIAN_POINT ( 'NONE',  ( 4.388395349243869425, -0.5016406811718626679, -2.236657869423730460 ) ) ;
#56851=CARTESIAN_POINT ( 'NONE',  ( 2.097363409947244683, -1.840767647902554982, 0.04455809990146220728 ) ) ;
#56853=CARTESIAN_POINT ( 'NONE',  ( 3.416849837094409370, 1.649954109374281996, 0.7815844185870900462 ) ) ;
#56854=CARTESIAN_POINT ( 'NONE',  ( 3.744767666119628746, 2.000857235306313875, -0.2496062519145719194 ) ) ;
#56856=CARTESIAN_POINT ( 'NONE',  ( 3.731548843211284439, -2.091483890824384684, 0.8634027215336376182 ) ) ;
#56858=CARTESIAN_POINT ( 'NONE',  ( 5.051841681570322429, 0.6635009534815727861, -1.998768678292896839 ) ) ;
#56860=CARTESIAN_POINT ( 'NONE',  ( 2.963400493335893948, 1.747644659881589568, 1.109742091278065113 ) ) ;
#56863=CARTESIAN_POINT ( 'NONE',  ( 6.305353446217972113, 1.845220813986702124, -1.044706065825385943 ) ) ;
#56865=CARTESIAN_POINT ( 'NONE',  ( 0.8735101492000696410, 1.856966920605634508, -0.5126664406217595893 ) ) ;
#56872=CARTESIAN_POINT ( 'NONE',  ( 1.055278351191447639, 0.4402236684300055991, 2.177206957374391738 ) ) ;
#56873=CARTESIAN_POINT ( 'NONE',  ( 1.905437291041052195, 1.750494195096408800, 1.170504954829422850 ) ) ;
#56876=CARTESIAN_POINT ( 'NONE',  ( 6.139480533765972581, 1.719935631569947221, -0.7110793932548589158 ) ) ;
#56881=CARTESIAN_POINT ( 'NONE',  ( 0.4398875993102538962, -2.011672884243600024, 0.6710486789910232730 ) ) ;
#56884=CARTESIAN_POINT ( 'NONE',  ( 2.963279974173158138, 1.655882904019840840, 1.051842618152734499 ) ) ;
#56885=CARTESIAN_POINT ( 'NONE',  ( 1.991316529349271836, 1.880942973025516940, -1.065213018539921563 ) ) ;
#56886=CARTESIAN_POINT ( 'NONE',  ( 1.065666191918061445, -1.167978014494171823, 1.423405568861765946 ) ) ;
#56890=CARTESIAN_POINT ( 'NONE',  ( 3.398151218454207090, 1.370964323331394397, -1.071876607410700677 ) ) ;
#56894=CARTESIAN_POINT ( 'NONE',  ( 0.7257156204387126275, -2.052300050329861847, 0.6792298617422781737 ) ) ;
#56895=CARTESIAN_POINT ( 'NONE',  ( 2.477888549845189470, 1.799646572043178683, 0.9090068759892779848 ) ) ;
#56897=CARTESIAN_POINT ( 'NONE',  ( 0.5675189469334164238, 0.2105291993744831114, -2.151437729447757796 ) ) ;
#56898=CARTESIAN_POINT ( 'NONE',  ( 2.254701366666445939, -1.525215070022269082, 1.249173565255176976 ) ) ;
#56904=CARTESIAN_POINT ( 'NONE',  ( -0.2108831679771168421, 6.948330828014878335, -2.492181822431015270 ) ) ;
#56907=CARTESIAN_POINT ( 'NONE',  ( 2.192062543670767027, 1.244387780127395482, 1.590672870423719187 ) ) ;
#56909=CARTESIAN_POINT ( 'NONE',  ( 6.071339422564090427, 0.1780416842499404351, -2.300786051158403733 ) ) ;
#56911=ADVANCED_FACE ( 'NONE', ( #76127 ), #157395, .T. ) ;
#56912=CARTESIAN_POINT ( 'NONE',  ( 3.819154011256303161, -1.728040176127441985, -0.9287006429716244682 ) ) ;
#56914=CARTESIAN_POINT ( 'NONE',  ( 1.090470458312575053, -0.4872005951904456733, 1.956561897242928172 ) ) ;
#56915=ORIENTED_EDGE ( 'NONE', *, *, #3142, .T. ) ;
#56916=CARTESIAN_POINT ( 'NONE',  ( 2.518900147204519158, 0.2643050731806431686, 2.100751150841919657 ) ) ;
#56919=CARTESIAN_POINT ( 'NONE',  ( 1.886409237429786279, 1.602333580200336671, -0.9066872629178088783 ) ) ;
#56923=CARTESIAN_POINT ( 'NONE',  ( 4.131183091185314460, 1.940096312829143299, 0.8565103500411813675 ) ) ;
#56924=CARTESIAN_POINT ( 'NONE',  ( 0.5504183687293667804, -1.553892155338543191, -0.9872222399871022347 ) ) ;
#56928=CARTESIAN_POINT ( 'NONE',  ( 3.954412886046823949, 0.7382688757093980314, 1.924196998259326996 ) ) ;
#56930=CARTESIAN_POINT ( 'NONE',  ( 1.733694375844633706, 1.821329977863223926, 0.2691589665217360983 ) ) ;
#56935=CARTESIAN_POINT ( 'NONE',  ( 0.5927436934281338221, -2.190715567557582677, -0.2661302102612560505 ) ) ;
#56936=CARTESIAN_POINT ( 'NONE',  ( 3.726065177040696952, -1.343991584994163269, -1.819822530443465425 ) ) ;
#56939=CARTESIAN_POINT ( 'NONE',  ( 4.025510356283497515, -0.3035946714039591265, 1.785781755087331391 ) ) ;
#56940=CARTESIAN_POINT ( 'NONE',  ( 3.696418550083080401, 1.350829783741511969, -1.358666786172907592 ) ) ;
#56941=CARTESIAN_POINT ( 'NONE',  ( 5.125469573878929097, 0.2063957376101481500, -2.060066405364005426 ) ) ;
#56943=CARTESIAN_POINT ( 'NONE',  ( 2.659003877371171942, -1.714407010456520108, -0.9732827283935908680 ) ) ;
#56944=CARTESIAN_POINT ( 'NONE',  ( 0.7098319175448050133, -1.917404841279496397, 0.1857973779731073583 ) ) ;
#56945=CARTESIAN_POINT ( 'NONE',  ( 4.311305935566238645, -0.3199438451688824125, 1.842931056080451935 ) ) ;
#56946=CARTESIAN_POINT ( 'NONE',  ( 1.928779914882609914, 1.326332282235458848, -1.888294200376864573 ) ) ;
#56947=CARTESIAN_POINT ( 'NONE',  ( 3.244433657958167849, -1.833057675465451730, -0.3206290368645177136 ) ) ;
#56953=CARTESIAN_POINT ( 'NONE',  ( 1.049603877184020373, -1.661282181752096410, -1.294363288650403732 ) ) ;
#56958=CARTESIAN_POINT ( 'NONE',  ( 1.687894460584405731, 2.027760172737497424, -0.6205009303206151516 ) ) ;
#56959=CARTESIAN_POINT ( 'NONE',  ( 0.7385429019767172365, 1.199765550694283478, -1.624703887242204825 ) ) ;
#56962=CARTESIAN_POINT ( 'NONE',  ( 1.440939128517594758, 0.4201678954103040819, 2.120193794684998245 ) ) ;
#56963=CARTESIAN_POINT ( 'NONE',  ( 6.610000000000042952, 1.321253023796984172, 1.840686448008920229 ) ) ;
#56966=FACE_OUTER_BOUND ( 'NONE', #57681, .T. ) ;
#56969=CARTESIAN_POINT ( 'NONE',  ( 6.139861302770143858, 2.010801613648224961, -0.1531635369260639090 ) ) ;
#56971=CARTESIAN_POINT ( 'NONE',  ( 0.1522426329377546128, 0.8445714516599597266, 2.022489037641273857 ) ) ;
#56973=CARTESIAN_POINT ( 'NONE',  ( 0.2337813496832439053, -2.066932786716439541, 0.9205801711329018033 ) ) ;
#56977=CARTESIAN_POINT ( 'NONE',  ( 0.8432031700210621539, 0.3724620109286616576, -1.878856871602401224 ) ) ;
#56981=CARTESIAN_POINT ( 'NONE',  ( 2.719059632816126282, -0.1691219839104734501, 1.716555610488319505 ) ) ;
#56983=CARTESIAN_POINT ( 'NONE',  ( 0.5261445748756715668, 1.690971295752751624, 0.5220769596525741685 ) ) ;
#56984=CARTESIAN_POINT ( 'NONE',  ( 1.647136526480545982, 0.1996500767776411833, 2.003181903140099696 ) ) ;
#56985=CARTESIAN_POINT ( 'NONE',  ( 4.577303723630254062, 0.003709267837189236805, -2.206952907291927168 ) ) ;
#56986=EDGE_LOOP ( 'NONE', ( #61819, #122721, #187159, #199682 ) ) ;
#56989=CARTESIAN_POINT ( 'NONE',  ( 4.740951199079581180, 2.029406658027664623, 0.6148427566107574904 ) ) ;
#56990=CARTESIAN_POINT ( 'NONE',  ( 3.778922869151004171, 1.701937167235707982, -1.081084515101193633 ) ) ;
#56991=ORIENTED_EDGE ( 'NONE', *, *, #161090, .F. ) ;
#56994=CARTESIAN_POINT ( 'NONE',  ( 1.041631754505952134, 0.7616270086890539748, -1.708776438048253077 ) ) ;
#57007=CARTESIAN_POINT ( 'NONE',  ( 4.324552338190708056, -0.9094542848507057853, -1.915842285305848991 ) ) ;
#57008=CARTESIAN_POINT ( 'NONE',  ( -0.1294898018152383368, 5.723764454335155349, -2.520545915250469893 ) ) ;
#57010=( BOUNDED_SURFACE ( )  B_SPLINE_SURFACE ( 3, 3, ( 
 ( #10549, #178410, #142736, #208745, #95036, #108136, #207691, #110269, #143813, #59310, #79821, #144875, #91846, #128672, #125467, #43096, #109209, #175221, #27880, #112399, #96106, #26806, #127612, #162161, #145933, #209810, #28952, #211944, #160018, #92908, #63580, #60372, #126535, #192496, #44148, #61444, #129737, #193577, #176278, #93977, #45220, #161086, #12676, #111335, #78751, #210882, #183716, #100338, #35324, #132875, #32147, #149085, #66731, #65674, #198877, #148039, #97171, #80899, #33206, #665, #113470, #117727, #49462, #150174, #164279, #197830, #179475, #81954, #67799, #163226, #131821, #2806, #47355, #15869, #84086, #151237, #115582, #214047, #146988, #134998, #68878, #14808, #101402, #181576, #199956, #99289, #165337, #16930, #83010, #31099, #1741, #213007, #64643, #130783, #196776, #50524, #133948, #167477, #48419, #116648, #51602, #19072, #182644, #34264, #85153, #166403, #114531, #180524, #98227, #17996, #37466, #20136, #170667, #123096, #6008, #189053, #156569, #154430, #55853, #39602, #40690, #168538, #4930, #106793, #105706, #172821, #72078, #185835, #88364, #138189, #71006, #204198, #87290, #36394, #86222, #186910, #122009, #52653, #56923, #203148, #89440, #103544, #137119, #118782, #21187, #7075, #102472, #54791, #8164, #201008, #169605, #23331, #90505, #120937, #153359, #152293, #74248, #184768, #3867, #24393, #38542, #139253, #104619, #22254, #187976, #171734, #69940, #136052, #155492, #73147, #205285, #202064, #53724, #119857, #174963, #95852, #92653, #160828, #128419, #46029, #9236, #44964, #206360, #173904, #161908, #78500, #13495, #110011, #77435, #209546, #107878, #41765, #12420, #75308, #190111, #108942, #176024, #25479, #192234, #140342, #29767, #194386, #60118, #43897, #27616, #191169, #210632, #26545, #158695, #127349, #57987, #91586, #142474, #93716, #157638, #112150, #177078, #124150, #28694, #178152, #10293, #76367, #208482, #159757, #141424, #61189, #126277, #207430, #59049, #125207, #42836, #11354, #143552, #193318, #111072, #94780, #144617, #62258, #167223, #130536, #81703, #32957, #147785, #213801, #166146, #67547, #145689, #115338, #116392, #179218, #14551, #80647, #148836, #83821, #99032, #79570, #65424, #131573, #164039, #17732, #211687, #197574, #15614, #146739, #162971, #149914, #117465, #31903, #196527, #49218, #100085, #34010, #180279, #199695, #181329, #212757, #182380, #63323, #64392, #1481, #129484, #30843, #96920, #113213, #195466, #165087, #48170, #133691, #408, #114283, #198626, #16678, #47097, #51340, #97980, #82763, #66480, #132619, #50273, #101135, #183458, #35064, #169349, #136863, #205029, #200754, #203952, #52403, #139007, #38284, #118530, #135794, #134745, #102217, #137931, #202888, #54534, #186658, #104361, #184513, #188800, #39351, #69690, #5744, #68622, #187723, #153102, #170406, #84895, #37213, #55600, #6823, #105447, #120680, #3612, #71821, #201818, #168285, #36134, #20934, #53463, #85967, #152042, #23074, #19883, #121755, #119600, #185584, #103287, #87030, #4677, #70751, #21995, #89190, #88105, #122839, #171483, #72902, #154176, #155241, #56675, #40437, #106538, #18809, #150983, #2547, #60657, #27088, #209021, #61733, #160299, #127901, #77976, #76902, #176554, #177630, #48691, #11902, #29238, #128948, #95330, #161379, #47642, #163505, #93196, #211161, #212226 ),
 ( #172563, #12963, #45502, #28164, #44435, #113753, #213290, #193852, #144099, #79040, #196007, #130016, #111618, #81179, #145155, #110552, #63860, #159227, #94260, #179757, #10828, #126820, #192777, #210094, #143026, #62785, #194926, #31374, #96392, #46563, #80105, #112683, #178693, #147258, #30307, #162443, #14018, #146209, #97450, #197053, #15089, #64916, #131065, #18287, #86507, #82231, #85437, #148322, #20425, #134225, #214321, #17215, #16146, #198111, #19357, #84373, #150461, #68091, #200235, #65953, #70229, #135281, #165627, #101689, #164561, #69161, #34550, #51885, #180805, #133161, #151522, #102766, #201295, #2022, #99562, #3090, #116934, #32431, #152572, #132102, #118008, #183997, #49741, #115868, #136341, #182934, #35611, #50807, #167758, #4159, #181853, #52936, #33490, #202361, #119072, #83291, #149376, #959, #67025, #185053, #36678, #168821, #114806, #98497, #199162, #100621, #166696, #104913, #40982, #103834, #8449, #188266, #139552, #120150, #72375, #173115, #42053, #140636, #172037, #38829, #107093, #170954, #137408, #87581, #204497, #22553, #121231, #187201, #58282, #71296, #157933, #156863, #108166, #88659, #56147, #138475, #89737, #75598, #123376, #154719, #9526, #153652, #186127, #5221, #6300, #122308, #39906, #106016, #169882, #55082, #23630, #141710, #155786, #7371, #73448, #205579, #57216, #206649, #174193, #37761, #189342, #90799, #203427, #24696, #74536, #124438, #190396, #25765, #54011, #91877, #21472, #77723, #145962, #207720, #61476, #143845, #208774, #76654, #79853, #31128, #160047, #110300, #45248, #13778, #162191, #94008, #113499, #209838, #142769, #96139, #80927, #126565, #211972, #59344, #158983, #10580, #26836, #125497, #111365, #60403, #63611, #128700, #27911, #78782, #176308, #177370, #129767, #195750, #11651, #179507, #127641, #192526, #47387, #191460, #44180, #97202, #43126, #193606, #28984, #92939, #109240, #95070, #161118, #163255, #194668, #12705, #112429, #144903, #175250, #14837, #210911, #62538, #46313, #178442, #30049, #168566, #149116, #166438, #83042, #50553, #118813, #114563, #117758, #180555, #52683, #18029, #32177, #49491, #48449, #15899, #51633, #116675, #182673, #100368, #84116, #98253, #102503, #167506, #197859, #133978, #196806, #101433, #66762, #150203, #213040, #165368, #183748, #135026, #19104, #34295, #131851, #199986, #115612, #81983, #164310, #697, #181607, #214077, #65703, #151266, #148071, #36427, #35358, #201040, #33235, #132903, #16961, #1775, #20166, #67831, #99317, #147017, #198908, #64670, #85182, #2838, #68907, #184798, #130816, #202099, #87323, #88398, #173941, #137154, #154465, #39636, #6043, #72114, #172860, #74282, #152323, #122045, #123132, #185867, #21219, #153391, #155532, #90543, #105745, #86253, #138223, #204236, #170699, #24431, #3900, #55888, #22285, #4962, #190148, #37502, #53758, #56959, #119890, #206394, #171771, #103578, #203179, #169636, #71040, #205321, #188009, #23368, #89477, #7112, #54826, #41802, #106830, #120976, #73185, #136082, #40724, #139291, #189090, #69971, #104652, #156607, #140376, #8197, #58021, #186944, #124185, #38577, #107915, #59084, #176056, #76399, #92683, #158728, #29801, #42869, #129516, #128451, #13533, #208516, #27651, #43929, #61224, #47132, #94813, #60151, #195496, #125244, #91622, #191204, #126308, #10325, #192268 ),
 ( #110044, #209579, #207465, #77467, #113247, #25514, #79603, #159787, #143586, #127380, #142508, #95886, #93749, #11389, #12457, #157673, #141458, #193352, #44996, #177111, #111105, #145722, #28727, #194418, #9270, #108977, #75341, #174996, #160863, #46060, #161941, #26581, #78532, #211721, #63357, #144650, #210665, #62291, #112182, #178186, #51379, #163003, #81738, #15649, #212788, #148870, #101173, #198659, #167262, #134781, #132655, #34047, #17770, #18847, #146771, #197607, #84932, #83859, #151021, #50308, #64425, #49251, #2588, #149949, #68658, #116426, #164070, #66513, #182417, #115372, #100120, #65456, #14584, #130569, #165119, #166182, #30876, #35102, #181364, #67582, #147819, #32988, #96955, #213838, #199733, #80680, #99065, #200790, #179253, #131606, #1518, #52441, #16711, #82796, #196559, #48201, #114313, #180312, #31932, #445, #117502, #133727, #183493, #98014, #120719, #152078, #40471, #105482, #104396, #87067, #106574, #172601, #36173, #153139, #74026, #70787, #139040, #24180, #90283, #201856, #23109, #184552, #3648, #140116, #56707, #206142, #88140, #55634, #187757, #86004, #19919, #205065, #53500, #168324, #4713, #154210, #69727, #170443, #118567, #7936, #156352, #38320, #22031, #5780, #169385, #188835, #136900, #202929, #171515, #102250, #135831, #186692, #71859, #121790, #54571, #119637, #137966, #72936, #185621, #37253, #103323, #20970, #203987, #122874, #39386, #89224, #155277, #6857, #128207, #93499, #193099, #95642, #109800, #207214, #144410, #41544, #174752, #108726, #91364, #27399, #194168, #77214, #45815, #13287, #11137, #127129, #110854, #111935, #26325, #175807, #78282, #12211, #158478, #177937, #142258, #141203, #160609, #145478, #190952, #62052, #57773, #9015, #75091, #157424, #123934, #159539, #124993, #210410, #44748, #92439, #176862, #59903, #189902, #29550, #25263, #60973, #143333, #58838, #42616, #79360, #126056, #209326, #208270, #28474, #161693, #10078, #94566, #76154, #107658, #173687, #192018, #43681, #112996, #80425, #116181, #181118, #32737, #164869, #16463, #30623, #167013, #17523, #47958, #198416, #46884, #165938, #131366, #82543, #63107, #15401, #182166, #199479, #83611, #115122, #196314, #50060, #114073, #146524, #96712, #147569, #180065, #64183, #130324, #1275, #14335, #100925, #99875, #51123, #31688, #213590, #81492, #98817, #18605, #66266, #97764, #84685, #162761, #129275, #212543, #163823, #65215, #197361, #49004, #179009, #148631, #197, #211473, #132414, #33797, #149692, #67333, #133477, #117246, #183246, #195248, #34850, #187509, #35926, #85751, #151833, #5526, #155024, #104144, #23932, #4462, #70532, #20724, #88969, #150772, #136650, #86818, #3406, #40210, #102003, #184301, #21777, #202675, #152884, #6608, #2334, #54323, #120464, #69475, #106320, #168072, #19672, #87886, #53252, #186436, #171261, #105221, #36992, #56455, #38074, #135582, #39138, #68410, #201604, #72689, #134537, #119383, #185369, #103075, #200543, #170191, #169130, #22855, #71607, #153960, #55384, #137718, #52189, #122615, #118315, #203738, #121539, #138784, #204804, #172344, #188578, #109546, #26072, #208020, #61787, #57523, #60708, #123681, #210143, #175550, #189643, #206956, #205890, #173424, #209071, #59646, #125804, #43422, #27139, #41294, #45554, #110605, #140942, #76953, #139859, #44488, #9825, #93245 ),
 ( #92184, #58585, #157169, #8761, #94311, #107402, #193906, #192830, #78027, #124740, #158234, #108472, #191767, #111670, #159279, #190699, #177677, #25006, #156095, #91108, #42360, #74842, #174495, #75901, #142005, #10878, #143078, #90036, #126872, #176606, #28218, #160352, #11954, #144151, #127953, #7680, #73764, #66001, #129001, #178746, #30359, #98547, #33537, #197099, #119922, #97499, #115916, #147309, #14069, #16196, #80156, #112736, #62839, #179804, #146261, #96446, #162497, #99609, #46614, #136115, #132151, #17264, #212274, #31423, #47690, #64960, #53791, #164611, #63909, #202130, #194978, #95381, #130065, #196058, #113802, #163556, #15139, #145208, #81227, #213335, #29287, #131112, #48740, #114853, #180853, #32475, #181902, #86285, #161430, #82277, #198157, #148372, #214371, #49790, #165675, #152356, #3931, #13013, #70001, #79090, #211214, #124217, #185897, #39669, #55920, #186974, #75376, #71071, #4994, #56989, #88432, #23397, #206428, #140410, #72145, #91653, #122078, #54856, #74313, #59118, #104684, #190179, #37532, #137188, #203210, #121007, #103609, #89510, #38606, #58052, #106863, #6075, #90578, #188040, #169665, #157706, #153425, #189122, #123162, #170733, #22319, #207496, #105780, #205355, #171805, #155564, #9303, #154496, #156638, #138255, #141490, #40757, #204267, #7146, #87357, #73218, #8230, #139324, #172890, #24465, #41834, #107945, #21250, #173971, #25545, #112212, #175028, #79636, #45030, #210696, #191237, #143619, #29836, #113282, #160896, #78565, #144685, #158762, #80714, #145755, #176088, #178221, #26615, #211755, #111144, #62326, #42900, #209614, #95920, #179288, #63393, #28761, #110076, #161974, #27686, #208548, #10357, #61256, #93785, #192301, #43960, #129547, #142542, #14618, #13564, #30912, #159821, #127414, #193386, #12492, #146804, #194451, #11424, #212822, #76434, #109009, #60182, #77500, #177144, #94845, #128485, #92716, #126341, #46096, #125275, #195529, #47168, #96987, #163038, #16742, #133755, #183523, #130602, #132686, #149978, #31964, #15683, #81770, #34078, #51409, #198693, #2617, #82827, #148903, #33021, #117529, #64458, #477, #165151, #213868, #196591, #147850, #164100, #100147, #181397, #50337, #35132, #101204, #99098, #84961, #66543, #65491, #199764, #48233, #49286, #167290, #114346, #131638, #197641, #115404, #180343, #166211, #116457, #18877, #151050, #182450, #98047, #17803, #1549, #83887, #67610, #46797, #129184, #193004, #11050, #65128, #45728, #63014, #194075, #161606, #15313, #77129, #14240, #143251, #163732, #195162, #209241, #160521, #159452, #127044, #162670, #13195, #111847, #196228, #29464, #12125, #95554, #177852, #60885, #179978, #30536, #79272, #78197, #31599, #97675, #175717, #144324, #213507, #210322, #64093, #81402, #147485, #44657, #80334, #109713, #110771, #131286, #47870, #43595, #145389, #112910, #178921, #176771, #28386, #130235, #94481, #93414, #61959, #211388, #128117, #96616, #27309, #146435, #212449, #113981, #100841, #18520, #33710, #53167, #165853, #17438, #184217, #70451, #98726, #199392, #84598, #134455, #83522, #36904, #2248, #151748, #48913, #164785, #115033, #148545, #117161, #3319, #119295, #82456, #68324, #201519, #185282, #150686, #118233, #20641, #34768, #132323, #69388, #181032, #99787, #149603, #16377, #166926, #102986, #200458, #169044, #152800 ),
 ( #52104, #35840, #1188, #101918, #67252, #32649, #111, #183164, #167984, #66178, #86730, #51038, #85662, #133387, #19589, #198329, #135496, #4379, #49969, #197273, #116088, #182078, #105140, #173338, #25986, #154941, #171180, #21692, #9740, #92094, #104060, #58501, #74755, #136566, #106236, #73678, #205804, #170106, #37987, #8672, #5446, #186352, #22771, #172261, #87804, #188494, #202587, #158148, #124657, #56370, #40126, #23849, #187425, #206870, #88887, #6525, #123596, #54239, #153877, #138702, #89956, #139777, #72602, #190613, #156007, #91022, #120377, #71525, #137636, #203655, #122533, #157084, #42272, #55305, #7594, #140857, #108384, #57435, #189561, #174409, #41207, #121454, #39055, #204720, #107314, #24918, #2163, #86648, #150603, #204638, #52026, #87717, #170023, #19501, #118152, #106154, #152716, #103980, #20565, #202506, #56289, #184136, #55222, #35760, #122449, #21609, #101835, #201437, #200378, #167903, #203571, #54156, #120295, #37904, #153790, #85577, #40045, #105058, #135416, #71441, #134374, #38972, #4298, #5359, #68240, #102902, #121368, #72519, #171096, #186268, #69304, #137553, #53078, #151667, #3238, #70369, #119213, #185196, #36821, #88800, #168961, #188408, #187343, #138615, #136484, #22687, #154859, #6441, #172180, #84515, #58421, #127783, #123517, #89875, #57354, #124574, #8589, #190535, #140774, #42191, #142908, #11784, #110437, #141847, #74671, #10717, #206789, #107236, #189481, #174326, #108306, #90937, #157003, #28051, #41124, #193738, #126700, #77858, #25902, #92012, #158070, #59478, #45384, #93074, #9658, #111500, #173257, #155927, #24838, #75734, #207852, #125635, #191596, #139696, #43258, #109376, #23770, #175383, #26969, #159116, #76786, #208908, #176439, #143981, #7512, #60542, #192661, #44315, #94144, #160183, #209972, #61613, #73594, #205719, #31260, #97334, #47522, #115750, #177506, #163392, #113635, #178575, #66906, #62666, #211040, #48580, #79989, #14966, #197999, #131990, #63741, #83179, #179640, #46443, #65841, #50694, #96273, #181741, #29118, #128825, #194807, #112564, #95205, #81063, #30183, #49625, #13907, #199048, #161254, #147149, #12841, #149262, #145037, #180690, #114696, #162323, #146093, #78915, #213174, #196940, #64803, #130950, #841, #212104, #148210, #129900, #133046, #32315, #195884, #98383, #164447, #16034, #82117, #214212, #33371, #99452, #165509, #17101, #75217, #140245, #167646, #106698, #166584, #74151, #39505, #205185, #182820, #18173, #200126, #24301, #89344, #155392, #73056, #139155, #150345, #141328, #206266, #19247, #172723, #84260, #57891, #105604, #56826, #34436, #138087, #90406, #107783, #124054, #23232, #101578, #156476, #85327, #51779, #1915, #55753, #151410, #183889, #35501, #190020, #134117, #9143, #8065, #173808, #5905, #121909, #204101, #6975, #207341, #188953, #71978, #116818, #67974, #100509, #117896, #187878, #171635, #122996, #40593, #41672, #25387, #91486, #157547, #109920, #61098, #12328, #127257, #193228, #145597, #47003, #125118, #94693, #95760, #158603, #208394, #60028, #128331, #63229, #78408, #146645, #44875, #110980, #143456, #211593, #58963, #176986, #209454, #126179, #162877, #10202, #92563, #144529, #175931, #28604, #79479, #13403, #159665, #179125, #160734, #142385, #161813, #191076, #192143, #129392, #42743, #76277, #43807, #27524 ),
 ( #210538, #194294, #112058, #113119, #26454, #77344, #195371, #178058, #30747, #62172, #93623, #45939, #29676, #96828, #14457, #11266, #108848, #80548, #174874, #199607, #198537, #181236, #134661, #52313, #130447, #32864, #168196, #164994, #18723, #200664, #118443, #81609, #117375, #64302, #31811, #19795, #150896, #85879, #182294, #149825, #67456, #180189, #114190, #84807, #147693, #48079, #98940, #33921, #97887, #50183, #212660, #102127, #184430, #132539, #116304, #99996, #49128, #68533, #16585, #82667, #51250, #196435, #163948, #321, #166063, #1395, #148751, #36047, #17649, #167138, #15523, #213711, #65334, #131481, #83733, #2457, #197485, #115246, #133602, #66391, #183372, #34977, #101048, #189773, #203869, #86946, #24064, #135707, #54451, #155157, #153013, #156233, #4589, #171393, #73903, #107532, #105356, #6738, #204938, #139996, #119509, #170317, #206017, #56589, #57653, #22984, #136773, #39262, #89103, #21905, #72817, #38199, #201733, #185495, #137848, #138919, #3525, #7810, #154086, #40347, #120594, #88015, #69599, #186571, #172477, #53374, #5654, #173563, #151955, #104272, #188711, #41424, #71734, #55513, #37120, #25135, #103199, #169261, #123812, #121668, #90167, #187635, #122749, #106453, #20847, #70663, #202802, #145344, #8887, #125935, #46753, #43555, #111801, #79227, #211345, #174626, #210278, #157297, #124864, #112864, #29423, #178879, #60844, #28346, #160480, #58715, #207085, #177807, #26202, #141076, #59778, #127006, #190830, #143214, #91237, #195115, #62970, #11010, #209204, #192964, #142133, #161562, #191893, #109676, #78154, #74966, #42489, #93374, #44617, #94441, #175678, #129139, #110732, #45685, #108598, #92320, #158361, #9954, #77087, #95514, #13150, #76030, #176732, #208147, #27267, #12087, #144285, #159410, #61918, #128078, #194034, #14198, #147437, #33662, #31556, #34722, #97631, #49924, #166878, #200411, #198283, #99736, #83475, #18469, #212403, #48868, #84548, #149556, #150637, #116045, #15270, #132275, #182033, #114984, #165808, #131241, #80291, #64045, #16327, #17392, #96575, #100793, #32605, #133340, #213461, #180984, #162622, #65085, #50991, #146389, #98680, #52057, #30491, #197228, #67203, #134407, #164736, #82410, #130190, #118184, #196183, #47825, #2198, #148499, #183114, #67, #66131, #1141, #199344, #113937, #68275, #117112, #179932, #163688, #81357, #106190, #186302, #122483, #170057, #86682, #21642, #37938, #3270, #172215, #171130, #87749, #152749, #23804, #89909, #101869, #4331, #139731, #136519, #204674, #155961, #7547, #53113, #88837, #35792, #69337, #205755, #188445, #57385, #153826, #121404, #39007, #151701, #85613, #56323, #119246, #19536, #70400, #5396, #135448, #71475, #184172, #73632, #167936, #104012, #137587, #203604, #20596, #40078, #202537, #54186, #22723, #201470, #185230, #55257, #187376, #105091, #120326, #36853, #154895, #138652, #102937, #168997, #6477, #72554, #43293, #144016, #193773, #8624, #142942, #127818, #45419, #159150, #44350, #161291, #175418, #58455, #210009, #107268, #25940, #126736, #124610, #111535, #190568, #208942, #177542, #78953, #76822, #192696, #176472, #29153, #90974, #141878, #95243, #28083, #12877, #60578, #108341, #10751, #110472, #207887, #94179, #9693, #173288, #157036, #109413, #160218, #189513, #145075, #125667, #11819, #92047, #59510 ),
 ( #158104, #74705, #211078, #77895, #174361, #206821, #140809, #191629, #75770, #42224, #27002, #123549, #93108, #41159, #61651, #24870, #31294, #213209, #81095, #98417, #84295, #132025, #97369, #166619, #162362, #128862, #96306, #163427, #47560, #15004, #179674, #178612, #63776, #64838, #150380, #113670, #130984, #16068, #196975, #48614, #149298, #50729, #194844, #164482, #99489, #13941, #212140, #129935, #198035, #66945, #82152, #62701, #114729, #180727, #147184, #879, #46477, #32352, #148244, #195923, #18211, #80024, #146127, #214246, #65877, #49665, #83216, #17139, #115788, #182856, #181777, #33410, #165546, #112601, #133085, #199083, #30222, #116855, #34474, #100546, #89659, #120077, #69088, #88587, #52866, #23552, #134153, #4086, #68012, #122234, #183927, #5147, #87513, #151448, #35539, #1951, #70157, #21403, #152502, #186053, #188193, #101616, #187128, #167683, #39829, #153578, #19284, #119001, #117933, #85366, #121159, #37688, #103765, #169816, #71224, #3020, #171961, #22476, #184979, #203358, #51815, #170883, #136268, #137339, #200161, #20352, #38757, #204422, #154644, #55010, #201225, #135210, #104838, #138403, #36605, #6226, #72296, #56077, #105937, #102691, #86437, #168749, #202288, #53940, #26765, #140566, #43053, #175179, #174121, #92867, #41983, #205508, #189270, #141636, #109166, #7295, #11580, #157860, #44109, #58207, #91802, #73373, #190324, #176238, #57139, #25694, #111296, #155712, #124366, #192455, #45182, #9453, #108092, #40909, #28914, #177300, #123306, #77652, #75525, #93937, #207645, #59265, #125421, #191387, #107015, #143774, #142694, #158913, #10509, #209769, #61409, #139478, #76583, #173039, #208704, #27840, #127572, #193540, #24622, #60331, #90729, #156792, #8378, #159978, #74461, #126492, #110230, #206578, #62471, #210845, #181538, #178373, #144839, #63542, #64605, #128633, #146951, #182599, #198839, #82972, #14770, #212966, #130745, #145895, #165296, #129698, #195680, #81914, #94999, #194599, #97133, #196739, #32107, #47317, #149045, #114492, #49423, #161045, #46243, #12641, #112360, #80861, #115543, #16891, #29982, #180488, #99248, #621, #48379, #15828, #132835, #98192, #96067, #33166, #78711, #211905, #164240, #162120, #66688, #116606, #148001, #113430, #50485, #13709, #79782, #179437, #31057, #163186, #214012, #65634, #131782, #197786, #36347, #121966, #85107, #102425, #202020, #168494, #20093, #120895, #22209, #100295, #69896, #70965, #133906, #183676, #35281, #103501, #38500, #53680, #34223, #86181, #152250, #118739, #186868, #166362, #3823, #184723, #101357, #138147, #199912, #67755, #119811, #151193, #136007, #54745, #203100, #134955, #154386, #185791, #117684, #137075, #17953, #167435, #104578, #84040, #51559, #19027, #2764, #150128, #37424, #68835, #170623, #200963, #55811, #1701, #169561, #52610, #5964, #21143, #87247, #153312, #4887, #88322, #72034, #204156, #207395, #124112, #91544, #159720, #155449, #158659, #7032, #93678, #59014, #73109, #90465, #89400, #56881, #92617, #157603, #9198, #141385, #125171, #139209, #143513, #208446, #24355, #174928, #23290, #142439, #107837, #191131, #39562, #206322, #10258, #175986, #60079, #75270, #172782, #26508, #156532, #123056, #205240, #190075, #8123, #40653, #106754, #192198, #189010, #77397, #76332, #27580, #74209, #41727, #57947, #42797 ) ),
 .UNSPECIFIED., .T., .F., .T. ) 
 B_SPLINE_SURFACE_WITH_KNOTS ( ( 4, 3, 4 ),
 ( 4, 1, 1, 1, 1, 1, 1, 1, 1, 1, 1, 1, 1, 1, 1, 1, 1, 1, 1, 1, 1, 1, 1, 1, 1, 1, 1, 1, 1, 1, 1, 1, 1, 1, 1, 1, 1, 1, 1, 1, 1, 1, 1, 1, 1, 1, 1, 1, 1, 1, 1, 1, 1, 1, 1, 1, 1, 1, 1, 1, 1, 1, 1, 1, 1, 1, 1, 1, 1, 1, 1, 1, 1, 1, 1, 1, 1, 1, 1, 1, 1, 1, 1, 1, 1, 1, 1, 1, 1, 1, 1, 1, 1, 1, 1, 1, 1, 1, 1, 1, 1, 1, 1, 1, 1, 1, 1, 1, 1, 1, 1, 1, 1, 1, 1, 1, 1, 1, 1, 1, 1, 1, 1, 1, 1, 1, 1, 1, 1, 1, 1, 1, 1, 1, 1, 1, 1, 1, 1, 1, 1, 1, 1, 1, 1, 1, 1, 1, 1, 1, 1, 1, 1, 1, 1, 1, 1, 1, 1, 1, 1, 1, 1, 1, 1, 1, 1, 1, 1, 1, 1, 1, 1, 1, 1, 1, 1, 1, 1, 1, 1, 1, 1, 1, 1, 1, 1, 1, 1, 1, 1, 1, 1, 1, 1, 1, 1, 1, 1, 1, 1, 1, 1, 1, 1, 1, 1, 1, 1, 1, 1, 1, 1, 1, 1, 1, 1, 1, 1, 1, 1, 1, 1, 1, 1, 1, 1, 1, 1, 1, 1, 1, 1, 1, 1, 1, 1, 1, 1, 1, 1, 1, 1, 1, 1, 1, 1, 1, 1, 1, 1, 1, 1, 1, 1, 1, 1, 1, 1, 1, 1, 1, 1, 1, 1, 1, 1, 1, 1, 1, 1, 1, 1, 1, 1, 1, 1, 1, 1, 1, 1, 1, 1, 1, 1, 1, 1, 1, 1, 1, 1, 1, 1, 1, 1, 1, 1, 1, 1, 1, 1, 1, 1, 1, 1, 1, 1, 1, 1, 1, 1, 1, 1, 1, 1, 1, 1, 1, 1, 1, 1, 1, 1, 1, 1, 1, 1, 1, 1, 1, 1, 1, 1, 1, 1, 1, 1, 1, 1, 1, 1, 1, 1, 1, 1, 1, 1, 1, 1, 1, 1, 1, 1, 1, 1, 1, 1, 1, 1, 1, 1, 1, 1, 1, 1, 1, 1, 1, 1, 1, 1, 1, 1, 1, 1, 1, 1, 1, 1, 1, 1, 1, 1, 1, 4 ),
 ( 0.000000000000000000, 0.5000000000000000000, 1.000000000000000000 ),
 ( 0.000000000000000000, 0.002599942752653872004, 0.005208763852970823248, 0.007813103504395044890, 0.01041666580238601383, 0.01302040446826325734, 0.01562503794709516405, 0.01822898659850798186, 0.02083325479626091381, 0.02343751936515397344, 0.02604147156932860516, 0.02864593660736421826, 0.03124971754428982826, 0.03385421962853985695, 0.03645805019290717514, 0.03906245553539786086, 0.04166655880408994678, 0.04427067902208449424, 0.04687506736766395427, 0.04947890482860387018, 0.05208340383233839299, 0.05468718329397467132, 0.05729165635893663372, 0.05989559287350183087, 0.06249988401580178210, 0.06510415622071820396, 0.06770810475871495704, 0.07031256650665723695, 0.07291634835701975292, 0.07552085129243907291, 0.07812468146351797538, 0.08072908640827750060, 0.08333318980393969455, 0.08593730989448074287, 0.08854169822802662737, 0.09114553558425014801, 0.09375003453682481669, 0.09635381396055957282, 0.09895828689139142542, 0.1015622234206122604, 0.1041665143989399522, 0.1067707866525781646, 0.1093747350801187734, 0.1119791968332524285, 0.1145829786367304204, 0.1171874814968899975, 0.1197913116783300008, 0.1223957164865987768, 0.1249998199429257079, 0.1276039399106482508, 0.1302083283009266290, 0.1328121656006459317, 0.1354166645410730119, 0.1380204439687620910, 0.1406249168095159707, 0.1432288533966223909, 0.1458331442541831724, 0.1484374165996726891, 0.1510413649597071029, 0.1536458267615184170, 0.1562496085608837959, 0.1588541113892728840, 0.1614579416238982879, 0.1640623463390579739, 0.1666664498991252963, 0.1692705697871219883, 0.1718749582774928841, 0.1744787955635339893, 0.1770832945353020271, 0.1796870740097127606, 0.1822915468038420750, 0.1848954834917516388, 0.1874997742717963711, 0.1901040467523684718, 0.1927079950878241021, 0.1953124569817516476, 0.1979162388197689970, 0.2005207416598733527, 0.2031245719904950509, 0.2057289766559125821, 0.2083330803627857220, 0.2109372002141371993, 0.2135415888479497148, 0.2161454261631269858, 0.2187499252097131475, 0.2213537047736018060, 0.2239581775645482220, 0.2265621143961681627, 0.2291664051419355919, 0.2317706778008114532, 0.2343746261546043874, 0.2369790881840763974, 0.2395828701034999064, 0.2421873729987945312, 0.2447912034682135918, 0.2473956081272447038, 0.2499997120239797754, 0.2526038318817556694, 0.2552082207023498306, 0.2578120580894675551, 0.2604165572543392093, 0.2630203369504529598, 0.2656248097816475973, 0.2682287467998764607, 0.2708330375545950908, 0.2734373104349877015, 0.2760412588500244513, 0.2786457210584605826, 0.2812495031020356140, 0.2838540060959860445, 0.2864578367469951536, 0.2890622414429859233, 0.2916663455726313803, 0.2942704654798921071, 0.2968748545306000852, 0.2994786920324540302, 0.3020831913590704687, 0.3046869712301484290, 0.3072914441450140810, 0.3098953813927431966, 0.3124996721996327054, 0.3151039453447485039, 0.3177078938639273376, 0.3203123562947402525, 0.3229161385052047861, 0.3255206416412691484, 0.3281244725166545528, 0.3307288772929431464, 0.3333329816985414751, 0.3359371016983396796, 0.3385414910224879836, 0.3411453286818670882, 0.3437498282136811634, 0.3463536083024566503, 0.3489580813444087548, 0.3515620188645239841, 0.3541663097667969717, 0.3567705832198370119, 0.3593745318860498972, 0.3619789945826469846, 0.3645827770027332826, 0.3671872803243637073, 0.3697911114669067967, 0.3723955163668249413, 0.3749996210914142147, 0.3776037412267966853, 0.3802081308677072724, 0.3828119687273952576, 0.3854164685078552144, 0.3880202488570567709, 0.3906247220695055478, 0.3932286599048890885, 0.3958329509457525486, 0.3984372247499146091, 0.4010411736060487398, 0.4036456366118335581, 0.4062494192842699414, 0.4088539228349143406, 0.4114577542873927851, 0.4140621593542673784, 0.4166662644408827831, 0.4192703847548917562, 0.4218747747558840855, 0.4244786128586610641, 0.4270831129312115948, 0.4296868935835649328, 0.4322913670099168826, 0.4348953052034483235, 0.4374995964261053638, 0.4401038706245853915, 0.4427078197135246862, 0.4453122830718987402, 0.4479160660394111426, 0.4505205698625146526, 0.4531244016677045128, 0.4557288069448597878, 0.4583329124365353446, 0.4609370329722101700, 0.4635414233766025904, 0.4661452617652466213, 0.4687497621733308639, 0.4713535431715604185, 0.4739580168552197104, 0.4765619554497781962, 0.4791662468974299260, 0.4817705215334236457, 0.4843744708980504132, 0.4869789346524148743, 0.4895827179577280641, 0.4921872220967347111, 0.4947910542974118808, 0.4973954598281701278, 0.4999995657679404681, 0.5026036865683194410, 0.5052080774194306345, 0.5078119161367193879, 0.5104164169237808135, 0.5130201983106112973, 0.5156246722949818784, 0.5182286113334474420, 0.5208329030492938605, 0.5234371781659985512, 0.5260411278491948783, 0.5286455920429519173, 0.5312493757287917173, 0.5338538802271461936, 0.5364577128660878991, 0.5390621186937718523, 0.5416662251246735504, 0.5442703462327953545, 0.5468747375739465566, 0.5494785766626585355, 0.5520830778721422805, 0.5546868596903002935, 0.5572913340187868325, 0.5598952735440421158, 0.5624995655712847764, 0.5651038412119004928, 0.5677077912565504647, 0.5703122559331050834, 0.5729160400421993149, 0.5755205449433484777, 0.5781243780633351648, 0.5807287842312690573, 0.5833328911963423513, 0.5859370126552478908, 0.5885414045297637786, 0.5911452440326808722, 0.5937497457080352925, 0.5963535280002507655, 0.5989580027162609843, 0.6015619427711926814, 0.6041662351530351360, 0.6067705113607667622, 0.6093744618097575172, 0.6119789270125192138, 0.6145827115875999169, 0.6171872169349945647, 0.6197910505788110092, 0.6223954571303226269, 0.6249995646726131948, 0.6276036865253464825, 0.6302080789765573954, 0.6328119189364656005, 0.6354164211211439373, 0.6380202039301521300, 0.6406246790770983024, 0.6432286197045988807, 0.6458329124842493441, 0.6484371893023079814, 0.6510411401985315427, 0.6536456059709156996, 0.6562493910547204656, 0.6588538968918166150, 0.6614577311022542538, 0.6640621380806766005, 0.6666662462432366709, 0.6692703685328477148, 0.6718747616040910975, 0.6744786020637821844, 0.6770831048012443398, 0.6796868881697873954, 0.6822913637910873463, 0.6848953050340567117, 0.6874995982547292828, 0.6901038757263339152, 0.6927078271126885234, 0.6953122934981186276, 0.6979160791333920422, 0.7005205855036529261, 0.7031244203235108570, 0.7057288277721832648, 0.7083329365980738368, 0.7109370593676189731, 0.7135414531022405971, 0.7161452941045143294, 0.7187497974382286436, 0.7213535814090563658, 0.7239580575481356917, 0.7265619994494829648, 0.7291662931543987369, 0.7317705713227778963, 0.7343745232421703406, 0.7369789902840787610, 0.7395827765135741805, 0.7421872834604720248, 0.7447911189325585601, 0.7473955268948287989, 0.7499996364271210858, 0.7526037597196653106, 0.7552081541610216053, 0.7578119957486867397, 0.7604164997221309896, 0.7630202843380037292, 0.7656247610382975743, 0.7682287036409420899, 0.7708329978733315935, 0.7734372767817252470, 0.7760412292770711984, 0.7786456970189011839, 0.7812494838853828449, 0.7838539914523996455, 0.7864578276195345330, 0.7890622361387605865, 0.7916663464205372369, 0.7942704702791556493, 0.7968748654706151457, 0.7994787076864910969, 0.8020832123431549388, 0.8046869976468442598, 0.8072914749517984268, 0.8098954182986718431, 0.8124997131017763774, 0.8151039927934364826, 0.8177079459076636025, 0.8203124143928716139, 0.8229162019391148553, 0.8255207101697450423, 0.8281245470747605752, 0.8307289561943111966, 0.8333330672686687368, 0.8359371917364484261, 0.8385415877213925340, 0.8411454306083117061, 0.8437499359916976749, 0.8463537220259882421, 0.8489581999790609679, 0.8515621441131088210, 0.8541664395301816759, 0.8567707200483754004, 0.8593746738244238959, 0.8619791430964799384, 0.8645829313652741988, 0.8671874403030259693, 0.8697912779887684298, 0.8723956877520262498, 0.8749997996620757501, 0.8776039247821166844, 0.8802083216039426894, 0.8828121652047509205, 0.8854166713583762061, 0.8880204581660676721, 0.8906249368107317377, 0.8932288817749149956, 0.8958331778492237829, 0.8984374592372342816, 0.9010414137180589034, 0.9036458838204490807, 0.9062496728545991198, 0.9088541825429954368, 0.9114580210523274273, 0.9140624315026897317, 0.9166665442915585826, 0.9192706701069754960, 0.9218750678090992245, 0.9244789121666602272, 0.9270834191340497910, 0.9296872067579531329, 0.9322916861377325004, 0.9348956319750387767, 0.9374999287497546296, 0.9401042110508202043, 0.9427081662796877870, 0.9453126372565492375, 0.9479164270979697493, 0.9505209375757615042, 0.9531247769568838013, 0.9557291881641908349, 0.9583333018366511080, 0.9609374282806871781, 0.9635418271385329803, 0.9661456726567504427, 0.9687501794391485399, 0.9713539669241311181, 0.9739584505366999378, 0.9765624007674321705, 0.9791666904763859369, 0.9817709514985233366, 0.9843749191276834898, 0.9869795472165283634, 0.9895832986789295793, 0.9921868791097946394, 0.9947912178632822844, 0.9974000636350187632, 1.000000000000000000 ),
 .UNSPECIFIED. ) 
 GEOMETRIC_REPRESENTATION_ITEM ( )  RATIONAL_B_SPLINE_SURFACE ( (
 ( 1.000000000000000222, 1.000000000000000222, 1.000000000000000444, 1.000000000000000000, 1.000000000000000444, 1.000000000000000222, 1.000000000000000444, 0.9999999999999997780, 1.000000000000000444, 1.000000000000000000, 1.000000000000000444, 1.000000000000000000, 1.000000000000000444, 1.000000000000000222, 1.000000000000000000, 1.000000000000000666, 0.9999999999999997780, 1.000000000000000444, 1.000000000000000444, 1.000000000000000444, 1.000000000000000222, 1.000000000000000222, 1.000000000000000444, 1.000000000000000444, 1.000000000000000000, 1.000000000000000222, 1.000000000000000222, 1.000000000000000444, 1.000000000000000222, 1.000000000000000444, 1.000000000000000000, 1.000000000000000222, 1.000000000000000444, 1.000000000000000000, 1.000000000000000444, 1.000000000000000222, 1.000000000000000444, 1.000000000000000444, 1.000000000000000222, 1.000000000000000000, 1.000000000000000444, 1.000000000000000222, 1.000000000000000000, 1.000000000000000222, 1.000000000000000444, 1.000000000000000444, 1.000000000000000444, 1.000000000000000444, 1.000000000000000222, 1.000000000000000444, 1.000000000000000000, 1.000000000000000444, 1.000000000000000222, 1.000000000000000222, 1.000000000000000444, 1.000000000000000000, 1.000000000000000222, 1.000000000000000444, 1.000000000000000222, 1.000000000000000000, 1.000000000000000444, 1.000000000000000222, 1.000000000000000222, 1.000000000000000000, 1.000000000000000444, 0.9999999999999997780, 1.000000000000000444, 1.000000000000000000, 1.000000000000000444, 1.000000000000000000, 1.000000000000000444, 0.9999999999999997780, 1.000000000000000222, 1.000000000000000444, 1.000000000000000444, 1.000000000000000000, 1.000000000000000444, 1.000000000000000222, 1.000000000000000000, 1.000000000000000666, 1.000000000000000000, 1.000000000000000444, 1.000000000000000222, 1.000000000000000444, 0.9999999999999997780, 1.000000000000000444, 1.000000000000000000, 1.000000000000000444, 1.000000000000000444, 1.000000000000000222, 1.000000000000000222, 1.000000000000000444, 1.000000000000000222, 1.000000000000000444, 1.000000000000000444, 1.000000000000000222, 1.000000000000000444, 1.000000000000000222, 1.000000000000000444, 1.000000000000000000, 1.000000000000000444, 1.000000000000000000, 1.000000000000000000, 1.000000000000000444, 1.000000000000000222, 1.000000000000000222, 1.000000000000000444, 1.000000000000000000, 1.000000000000000444, 1.000000000000000000, 1.000000000000000222, 1.000000000000000444, 0.9999999999999997780, 1.000000000000000444, 1.000000000000000222, 1.000000000000000444, 1.000000000000000000, 1.000000000000000444, 1.000000000000000000, 1.000000000000000222, 1.000000000000000222, 1.000000000000000444, 1.000000000000000222, 1.000000000000000000, 1.000000000000000444, 1.000000000000000222, 1.000000000000000222, 1.000000000000000222, 1.000000000000000444, 0.9999999999999997780, 1.000000000000000666, 0.9999999999999996669, 1.000000000000000444, 1.000000000000000444, 1.000000000000000222, 1.000000000000000444, 1.000000000000000444, 1.000000000000000222, 1.000000000000000000, 1.000000000000000444, 1.000000000000000000, 1.000000000000000444, 1.000000000000000222, 1.000000000000000444, 1.000000000000000000, 1.000000000000000444, 1.000000000000000222, 1.000000000000000222, 1.000000000000000444, 1.000000000000000222, 0.9999999999999997780, 1.000000000000000444, 1.000000000000000444, 1.000000000000000444, 1.000000000000000222, 1.000000000000000444, 1.000000000000000444, 1.000000000000000222, 1.000000000000000444, 1.000000000000000000, 1.000000000000000222, 1.000000000000000444, 1.000000000000000000, 1.000000000000000222, 1.000000000000000444, 1.000000000000000000, 1.000000000000000444, 0.9999999999999997780, 1.000000000000000222, 1.000000000000000444, 1.000000000000000000, 1.000000000000000222, 1.000000000000000222, 1.000000000000000444, 1.000000000000000000, 1.000000000000000666, 0.9999999999999996669, 1.000000000000000666, 1.000000000000000222, 1.000000000000000444, 1.000000000000000222, 1.000000000000000444, 1.000000000000000222, 1.000000000000000222, 1.000000000000000000, 1.000000000000000444, 0.9999999999999997780, 1.000000000000000444, 1.000000000000000222, 1.000000000000000444, 0.9999999999999997780, 1.000000000000000444, 1.000000000000000000, 1.000000000000000222, 1.000000000000000444, 1.000000000000000000, 1.000000000000000444, 1.000000000000000444, 1.000000000000000222, 1.000000000000000222, 1.000000000000000000, 1.000000000000000444, 1.000000000000000444, 1.000000000000000000, 1.000000000000000222, 1.000000000000000222, 1.000000000000000444, 1.000000000000000222, 1.000000000000000222, 1.000000000000000444, 1.000000000000000222, 1.000000000000000000, 1.000000000000000444, 1.000000000000000000, 1.000000000000000222, 1.000000000000000444, 1.000000000000000222, 1.000000000000000222, 1.000000000000000444, 1.000000000000000000, 1.000000000000000222, 1.000000000000000222, 1.000000000000000222, 1.000000000000000000, 1.000000000000000222, 1.000000000000000222, 1.000000000000000000, 1.000000000000000222, 1.000000000000000222, 1.000000000000000444, 1.000000000000000000, 1.000000000000000000, 1.000000000000000222, 1.000000000000000000, 1.000000000000000888, 1.000000000000000000, 1.000000000000000444, 1.000000000000000222, 1.000000000000000222, 1.000000000000000444, 1.000000000000000222, 1.000000000000000222, 1.000000000000000444, 1.000000000000000444, 1.000000000000000222, 1.000000000000000444, 1.000000000000000222, 1.000000000000000000, 1.000000000000000222, 1.000000000000000444, 1.000000000000000444, 1.000000000000000222, 1.000000000000000444, 1.000000000000000222, 1.000000000000000444, 1.000000000000000222, 1.000000000000000444, 1.000000000000000222, 1.000000000000000000, 1.000000000000000444, 1.000000000000000000, 1.000000000000000666, 1.000000000000000000, 1.000000000000000000, 1.000000000000000444, 1.000000000000000222, 1.000000000000000444, 0.9999999999999997780, 1.000000000000000666, 1.000000000000000222, 1.000000000000000444, 1.000000000000000222, 1.000000000000000444, 1.000000000000000222, 1.000000000000000444, 0.9999999999999997780, 1.000000000000000666, 1.000000000000000222, 1.000000000000000222, 1.000000000000000444, 1.000000000000000444, 0.9999999999999997780, 1.000000000000000444, 1.000000000000000222, 1.000000000000000222, 1.000000000000000000, 1.000000000000000000, 1.000000000000000444, 1.000000000000000444, 1.000000000000000222, 1.000000000000000000, 1.000000000000000444, 0.9999999999999997780, 1.000000000000000444, 1.000000000000000222, 1.000000000000000000, 1.000000000000000222, 1.000000000000000000, 1.000000000000000444, 1.000000000000000000, 1.000000000000000444, 1.000000000000000222, 1.000000000000000222, 1.000000000000000222, 1.000000000000000222, 1.000000000000000222, 1.000000000000000444, 1.000000000000000222, 1.000000000000000444, 1.000000000000000222, 1.000000000000000000, 1.000000000000000888, 0.9999999999999996669, 1.000000000000000444, 1.000000000000000444, 1.000000000000000222, 1.000000000000000444, 1.000000000000000000, 1.000000000000000444, 0.9999999999999997780, 1.000000000000000444, 1.000000000000000222, 1.000000000000000444, 0.9999999999999997780, 1.000000000000000222, 1.000000000000000222, 1.000000000000000444, 1.000000000000000000, 1.000000000000000444, 1.000000000000000444, 1.000000000000000222, 1.000000000000000000, 1.000000000000000444, 1.000000000000000000, 1.000000000000000222, 1.000000000000000222, 1.000000000000000444, 1.000000000000000000, 1.000000000000000666, 1.000000000000000000, 1.000000000000000444, 1.000000000000000222, 1.000000000000000444, 1.000000000000000222, 1.000000000000000444, 1.000000000000000222, 1.000000000000000222, 1.000000000000000222, 1.000000000000000444, 1.000000000000000444, 1.000000000000000222, 1.000000000000000000, 1.000000000000000444, 1.000000000000000444, 1.000000000000000000, 1.000000000000000444, 0.9999999999999997780, 1.000000000000000444, 1.000000000000000222, 1.000000000000000222, 1.000000000000000444, 1.000000000000000222, 1.000000000000000222, 1.000000000000000444, 1.000000000000000444, 1.000000000000000444, 1.000000000000000000, 1.000000000000000444, 1.000000000000000222, 1.000000000000000222, 1.000000000000000000, 1.000000000000000444, 0.9999999999999997780, 1.000000000000000444, 1.000000000000000000, 1.000000000000000444, 1.000000000000000000, 1.000000000000000444, 1.000000000000000222, 1.000000000000000000, 1.000000000000000444, 1.000000000000000222, 1.000000000000000444, 0.9999999999999997780, 1.000000000000000444, 1.000000000000000222, 1.000000000000000222),
 ( 0.3333333333333334259, 0.3333333333333334259, 0.3333333333333334814, 0.3333333333333333703, 0.3333333333333335369, 0.3333333333333334259, 0.3333333333333334814, 0.3333333333333333703, 0.3333333333333334259, 0.3333333333333333703, 0.3333333333333335369, 0.3333333333333333703, 0.3333333333333334259, 0.3333333333333334259, 0.3333333333333333703, 0.3333333333333335369, 0.3333333333333333703, 0.3333333333333334259, 0.3333333333333335369, 0.3333333333333334259, 0.3333333333333333703, 0.3333333333333334259, 0.3333333333333334814, 0.3333333333333335369, 0.3333333333333333148, 0.3333333333333334259, 0.3333333333333334259, 0.3333333333333334814, 0.3333333333333334259, 0.3333333333333334259, 0.3333333333333334259, 0.3333333333333333148, 0.3333333333333335924, 0.3333333333333333148, 0.3333333333333335369, 0.3333333333333333703, 0.3333333333333335369, 0.3333333333333334259, 0.3333333333333333703, 0.3333333333333333703, 0.3333333333333335924, 0.3333333333333333148, 0.3333333333333334259, 0.3333333333333334259, 0.3333333333333335369, 0.3333333333333334814, 0.3333333333333334259, 0.3333333333333334259, 0.3333333333333334259, 0.3333333333333334259, 0.3333333333333333703, 0.3333333333333335369, 0.3333333333333334259, 0.3333333333333334259, 0.3333333333333334814, 0.3333333333333333703, 0.3333333333333333703, 0.3333333333333334814, 0.3333333333333334259, 0.3333333333333333703, 0.3333333333333334814, 0.3333333333333333703, 0.3333333333333334814, 0.3333333333333332593, 0.3333333333333335924, 0.3333333333333333148, 0.3333333333333335924, 0.3333333333333333148, 0.3333333333333335924, 0.3333333333333334259, 0.3333333333333334814, 0.3333333333333333703, 0.3333333333333333703, 0.3333333333333334814, 0.3333333333333335369, 0.3333333333333333703, 0.3333333333333334814, 0.3333333333333334259, 0.3333333333333333703, 0.3333333333333335369, 0.3333333333333333148, 0.3333333333333335369, 0.3333333333333334259, 0.3333333333333334259, 0.3333333333333333703, 0.3333333333333334259, 0.3333333333333333703, 0.3333333333333335369, 0.3333333333333333703, 0.3333333333333334259, 0.3333333333333334259, 0.3333333333333334814, 0.3333333333333333703, 0.3333333333333335924, 0.3333333333333333703, 0.3333333333333334259, 0.3333333333333334814, 0.3333333333333334259, 0.3333333333333335369, 0.3333333333333333148, 0.3333333333333335369, 0.3333333333333333148, 0.3333333333333334259, 0.3333333333333333703, 0.3333333333333334259, 0.3333333333333334259, 0.3333333333333335924, 0.3333333333333333703, 0.3333333333333335924, 0.3333333333333333148, 0.3333333333333335369, 0.3333333333333335369, 0.3333333333333333148, 0.3333333333333334259, 0.3333333333333334259, 0.3333333333333334814, 0.3333333333333333703, 0.3333333333333335369, 0.3333333333333333703, 0.3333333333333333703, 0.3333333333333334814, 0.3333333333333334814, 0.3333333333333334259, 0.3333333333333333703, 0.3333333333333334814, 0.3333333333333334814, 0.3333333333333334259, 0.3333333333333334259, 0.3333333333333334259, 0.3333333333333333703, 0.3333333333333335369, 0.3333333333333333703, 0.3333333333333334259, 0.3333333333333334814, 0.3333333333333334259, 0.3333333333333334814, 0.3333333333333334259, 0.3333333333333333703, 0.3333333333333333703, 0.3333333333333334259, 0.3333333333333333148, 0.3333333333333334814, 0.3333333333333334814, 0.3333333333333334259, 0.3333333333333333703, 0.3333333333333334259, 0.3333333333333334259, 0.3333333333333333703, 0.3333333333333335369, 0.3333333333333334259, 0.3333333333333333148, 0.3333333333333333703, 0.3333333333333335369, 0.3333333333333335369, 0.3333333333333333148, 0.3333333333333335369, 0.3333333333333334259, 0.3333333333333334259, 0.3333333333333335369, 0.3333333333333333703, 0.3333333333333333703, 0.3333333333333334259, 0.3333333333333333703, 0.3333333333333334259, 0.3333333333333334259, 0.3333333333333333703, 0.3333333333333335369, 0.3333333333333333703, 0.3333333333333334259, 0.3333333333333335369, 0.3333333333333333703, 0.3333333333333333703, 0.3333333333333334814, 0.3333333333333334259, 0.3333333333333333703, 0.3333333333333335369, 0.3333333333333332593, 0.3333333333333335369, 0.3333333333333335369, 0.3333333333333333703, 0.3333333333333334814, 0.3333333333333334814, 0.3333333333333334259, 0.3333333333333333703, 0.3333333333333334259, 0.3333333333333334814, 0.3333333333333333148, 0.3333333333333335369, 0.3333333333333333703, 0.3333333333333334259, 0.3333333333333333703, 0.3333333333333334259, 0.3333333333333333148, 0.3333333333333334259, 0.3333333333333334814, 0.3333333333333333703, 0.3333333333333334814, 0.3333333333333334259, 0.3333333333333333703, 0.3333333333333334259, 0.3333333333333333703, 0.3333333333333334259, 0.3333333333333334814, 0.3333333333333332593, 0.3333333333333334259, 0.3333333333333333703, 0.3333333333333335369, 0.3333333333333334259, 0.3333333333333333703, 0.3333333333333334259, 0.3333333333333334259, 0.3333333333333333148, 0.3333333333333335369, 0.3333333333333333703, 0.3333333333333334259, 0.3333333333333335924, 0.3333333333333333703, 0.3333333333333334259, 0.3333333333333335369, 0.3333333333333333703, 0.3333333333333334259, 0.3333333333333334259, 0.3333333333333334259, 0.3333333333333333703, 0.3333333333333334259, 0.3333333333333334259, 0.3333333333333333703, 0.3333333333333333148, 0.3333333333333334814, 0.3333333333333334259, 0.3333333333333334259, 0.3333333333333333703, 0.3333333333333333703, 0.3333333333333334259, 0.3333333333333335369, 0.3333333333333333703, 0.3333333333333335369, 0.3333333333333333703, 0.3333333333333334259, 0.3333333333333335369, 0.3333333333333333148, 0.3333333333333334259, 0.3333333333333334814, 0.3333333333333335369, 0.3333333333333333148, 0.3333333333333335369, 0.3333333333333333703, 0.3333333333333334259, 0.3333333333333333703, 0.3333333333333335369, 0.3333333333333334259, 0.3333333333333334259, 0.3333333333333334259, 0.3333333333333333703, 0.3333333333333335924, 0.3333333333333334259, 0.3333333333333335369, 0.3333333333333333148, 0.3333333333333333703, 0.3333333333333334814, 0.3333333333333333703, 0.3333333333333335924, 0.3333333333333333148, 0.3333333333333333703, 0.3333333333333335369, 0.3333333333333333703, 0.3333333333333335924, 0.3333333333333332593, 0.3333333333333335924, 0.3333333333333334259, 0.3333333333333335369, 0.3333333333333334259, 0.3333333333333334814, 0.3333333333333333703, 0.3333333333333334814, 0.3333333333333333148, 0.3333333333333335369, 0.3333333333333333148, 0.3333333333333334814, 0.3333333333333334814, 0.3333333333333334814, 0.3333333333333333148, 0.3333333333333335369, 0.3333333333333333148, 0.3333333333333335369, 0.3333333333333333703, 0.3333333333333333703, 0.3333333333333335369, 0.3333333333333334259, 0.3333333333333334259, 0.3333333333333333703, 0.3333333333333335369, 0.3333333333333333148, 0.3333333333333335924, 0.3333333333333334259, 0.3333333333333334259, 0.3333333333333333703, 0.3333333333333333703, 0.3333333333333334259, 0.3333333333333334259, 0.3333333333333334259, 0.3333333333333334259, 0.3333333333333334259, 0.3333333333333334259, 0.3333333333333334259, 0.3333333333333333703, 0.3333333333333335369, 0.3333333333333333703, 0.3333333333333334814, 0.3333333333333333703, 0.3333333333333333148, 0.3333333333333337034, 0.3333333333333332038, 0.3333333333333334814, 0.3333333333333335369, 0.3333333333333334814, 0.3333333333333334259, 0.3333333333333334259, 0.3333333333333334814, 0.3333333333333333703, 0.3333333333333334814, 0.3333333333333334259, 0.3333333333333334814, 0.3333333333333333148, 0.3333333333333333703, 0.3333333333333335369, 0.3333333333333334259, 0.3333333333333333703, 0.3333333333333335369, 0.3333333333333334814, 0.3333333333333334259, 0.3333333333333333703, 0.3333333333333334259, 0.3333333333333333148, 0.3333333333333335369, 0.3333333333333333148, 0.3333333333333335369, 0.3333333333333333703, 0.3333333333333335369, 0.3333333333333334259, 0.3333333333333334814, 0.3333333333333334259, 0.3333333333333335369, 0.3333333333333334259, 0.3333333333333334259, 0.3333333333333333703, 0.3333333333333334259, 0.3333333333333333703, 0.3333333333333335369, 0.3333333333333334814, 0.3333333333333333703, 0.3333333333333333148, 0.3333333333333335369, 0.3333333333333333703, 0.3333333333333333703, 0.3333333333333334814, 0.3333333333333333148, 0.3333333333333334814, 0.3333333333333333703, 0.3333333333333334259, 0.3333333333333334814, 0.3333333333333334814, 0.3333333333333334259, 0.3333333333333334259, 0.3333333333333335369, 0.3333333333333334814, 0.3333333333333333148, 0.3333333333333335369, 0.3333333333333334259, 0.3333333333333333703, 0.3333333333333334259, 0.3333333333333334259, 0.3333333333333333148, 0.3333333333333334814, 0.3333333333333333703, 0.3333333333333334259, 0.3333333333333333148, 0.3333333333333334814, 0.3333333333333334259, 0.3333333333333333148, 0.3333333333333334814, 0.3333333333333334259, 0.3333333333333334814, 0.3333333333333332593, 0.3333333333333335924, 0.3333333333333334259, 0.3333333333333334259),
 ( 0.3333333333333334259, 0.3333333333333334259, 0.3333333333333334814, 0.3333333333333333703, 0.3333333333333335369, 0.3333333333333334259, 0.3333333333333334814, 0.3333333333333333703, 0.3333333333333334259, 0.3333333333333333703, 0.3333333333333335369, 0.3333333333333333703, 0.3333333333333334259, 0.3333333333333334259, 0.3333333333333333703, 0.3333333333333335369, 0.3333333333333333703, 0.3333333333333334259, 0.3333333333333335369, 0.3333333333333334259, 0.3333333333333333703, 0.3333333333333334259, 0.3333333333333334814, 0.3333333333333335369, 0.3333333333333333148, 0.3333333333333334259, 0.3333333333333334259, 0.3333333333333334814, 0.3333333333333334259, 0.3333333333333334259, 0.3333333333333334259, 0.3333333333333333148, 0.3333333333333335924, 0.3333333333333333148, 0.3333333333333335369, 0.3333333333333333703, 0.3333333333333335369, 0.3333333333333334259, 0.3333333333333333703, 0.3333333333333333703, 0.3333333333333335924, 0.3333333333333333148, 0.3333333333333334259, 0.3333333333333334259, 0.3333333333333335369, 0.3333333333333334814, 0.3333333333333334259, 0.3333333333333334259, 0.3333333333333334259, 0.3333333333333334259, 0.3333333333333333703, 0.3333333333333335369, 0.3333333333333334259, 0.3333333333333334259, 0.3333333333333334814, 0.3333333333333333703, 0.3333333333333333703, 0.3333333333333334814, 0.3333333333333334259, 0.3333333333333333703, 0.3333333333333334814, 0.3333333333333333703, 0.3333333333333334814, 0.3333333333333332593, 0.3333333333333335924, 0.3333333333333333148, 0.3333333333333335924, 0.3333333333333333148, 0.3333333333333335924, 0.3333333333333334259, 0.3333333333333334814, 0.3333333333333333703, 0.3333333333333333703, 0.3333333333333334814, 0.3333333333333335369, 0.3333333333333333703, 0.3333333333333334814, 0.3333333333333334259, 0.3333333333333333703, 0.3333333333333335369, 0.3333333333333333148, 0.3333333333333335369, 0.3333333333333334259, 0.3333333333333334259, 0.3333333333333333703, 0.3333333333333334259, 0.3333333333333333703, 0.3333333333333335369, 0.3333333333333333703, 0.3333333333333334259, 0.3333333333333334259, 0.3333333333333334814, 0.3333333333333333703, 0.3333333333333335924, 0.3333333333333333703, 0.3333333333333334259, 0.3333333333333334814, 0.3333333333333334259, 0.3333333333333335369, 0.3333333333333333148, 0.3333333333333335369, 0.3333333333333333148, 0.3333333333333334259, 0.3333333333333333703, 0.3333333333333334259, 0.3333333333333334259, 0.3333333333333335924, 0.3333333333333333703, 0.3333333333333335924, 0.3333333333333333148, 0.3333333333333335369, 0.3333333333333335369, 0.3333333333333333148, 0.3333333333333334259, 0.3333333333333334259, 0.3333333333333334814, 0.3333333333333333703, 0.3333333333333335369, 0.3333333333333333703, 0.3333333333333333703, 0.3333333333333334814, 0.3333333333333334814, 0.3333333333333334259, 0.3333333333333333703, 0.3333333333333334814, 0.3333333333333334814, 0.3333333333333334259, 0.3333333333333334259, 0.3333333333333334259, 0.3333333333333333703, 0.3333333333333335369, 0.3333333333333333703, 0.3333333333333334259, 0.3333333333333334814, 0.3333333333333334259, 0.3333333333333334814, 0.3333333333333334259, 0.3333333333333333703, 0.3333333333333333703, 0.3333333333333334259, 0.3333333333333333148, 0.3333333333333334814, 0.3333333333333334814, 0.3333333333333334259, 0.3333333333333333703, 0.3333333333333334259, 0.3333333333333334259, 0.3333333333333333703, 0.3333333333333335369, 0.3333333333333334259, 0.3333333333333333148, 0.3333333333333333703, 0.3333333333333335369, 0.3333333333333335369, 0.3333333333333333148, 0.3333333333333335369, 0.3333333333333334259, 0.3333333333333334259, 0.3333333333333335369, 0.3333333333333333703, 0.3333333333333333703, 0.3333333333333334259, 0.3333333333333333703, 0.3333333333333334259, 0.3333333333333334259, 0.3333333333333333703, 0.3333333333333335369, 0.3333333333333333703, 0.3333333333333334259, 0.3333333333333335369, 0.3333333333333333703, 0.3333333333333333703, 0.3333333333333334814, 0.3333333333333334259, 0.3333333333333333703, 0.3333333333333335369, 0.3333333333333332593, 0.3333333333333335369, 0.3333333333333335369, 0.3333333333333333703, 0.3333333333333334814, 0.3333333333333334814, 0.3333333333333334259, 0.3333333333333333703, 0.3333333333333334259, 0.3333333333333334814, 0.3333333333333333148, 0.3333333333333335369, 0.3333333333333333703, 0.3333333333333334259, 0.3333333333333333703, 0.3333333333333334259, 0.3333333333333333148, 0.3333333333333334259, 0.3333333333333334814, 0.3333333333333333703, 0.3333333333333334814, 0.3333333333333334259, 0.3333333333333333703, 0.3333333333333334259, 0.3333333333333333703, 0.3333333333333334259, 0.3333333333333334814, 0.3333333333333332593, 0.3333333333333334259, 0.3333333333333333703, 0.3333333333333335369, 0.3333333333333334259, 0.3333333333333333703, 0.3333333333333334259, 0.3333333333333334259, 0.3333333333333333148, 0.3333333333333335369, 0.3333333333333333703, 0.3333333333333334259, 0.3333333333333335924, 0.3333333333333333703, 0.3333333333333334259, 0.3333333333333335369, 0.3333333333333333703, 0.3333333333333334259, 0.3333333333333334259, 0.3333333333333334259, 0.3333333333333333703, 0.3333333333333334259, 0.3333333333333334259, 0.3333333333333333703, 0.3333333333333333148, 0.3333333333333334814, 0.3333333333333334259, 0.3333333333333334259, 0.3333333333333333703, 0.3333333333333333703, 0.3333333333333334259, 0.3333333333333335369, 0.3333333333333333703, 0.3333333333333335369, 0.3333333333333333703, 0.3333333333333334259, 0.3333333333333335369, 0.3333333333333333148, 0.3333333333333334259, 0.3333333333333334814, 0.3333333333333335369, 0.3333333333333333148, 0.3333333333333335369, 0.3333333333333333703, 0.3333333333333334259, 0.3333333333333333703, 0.3333333333333335369, 0.3333333333333334259, 0.3333333333333334259, 0.3333333333333334259, 0.3333333333333333703, 0.3333333333333335924, 0.3333333333333334259, 0.3333333333333335369, 0.3333333333333333148, 0.3333333333333333703, 0.3333333333333334814, 0.3333333333333333703, 0.3333333333333335924, 0.3333333333333333148, 0.3333333333333333703, 0.3333333333333335369, 0.3333333333333333703, 0.3333333333333335924, 0.3333333333333332593, 0.3333333333333335924, 0.3333333333333334259, 0.3333333333333335369, 0.3333333333333334259, 0.3333333333333334814, 0.3333333333333333703, 0.3333333333333334814, 0.3333333333333333148, 0.3333333333333335369, 0.3333333333333333148, 0.3333333333333334814, 0.3333333333333334814, 0.3333333333333334814, 0.3333333333333333148, 0.3333333333333335369, 0.3333333333333333148, 0.3333333333333335369, 0.3333333333333333703, 0.3333333333333333703, 0.3333333333333335369, 0.3333333333333334259, 0.3333333333333334259, 0.3333333333333333703, 0.3333333333333335369, 0.3333333333333333148, 0.3333333333333335924, 0.3333333333333334259, 0.3333333333333334259, 0.3333333333333333703, 0.3333333333333333703, 0.3333333333333334259, 0.3333333333333334259, 0.3333333333333334259, 0.3333333333333334259, 0.3333333333333334259, 0.3333333333333334259, 0.3333333333333334259, 0.3333333333333333703, 0.3333333333333335369, 0.3333333333333333703, 0.3333333333333334814, 0.3333333333333333703, 0.3333333333333333148, 0.3333333333333337034, 0.3333333333333332038, 0.3333333333333334814, 0.3333333333333335369, 0.3333333333333334814, 0.3333333333333334259, 0.3333333333333334259, 0.3333333333333334814, 0.3333333333333333703, 0.3333333333333334814, 0.3333333333333334259, 0.3333333333333334814, 0.3333333333333333148, 0.3333333333333333703, 0.3333333333333335369, 0.3333333333333334259, 0.3333333333333333703, 0.3333333333333335369, 0.3333333333333334814, 0.3333333333333334259, 0.3333333333333333703, 0.3333333333333334259, 0.3333333333333333148, 0.3333333333333335369, 0.3333333333333333148, 0.3333333333333335369, 0.3333333333333333703, 0.3333333333333335369, 0.3333333333333334259, 0.3333333333333334814, 0.3333333333333334259, 0.3333333333333335369, 0.3333333333333334259, 0.3333333333333334259, 0.3333333333333333703, 0.3333333333333334259, 0.3333333333333333703, 0.3333333333333335369, 0.3333333333333334814, 0.3333333333333333703, 0.3333333333333333148, 0.3333333333333335369, 0.3333333333333333703, 0.3333333333333333703, 0.3333333333333334814, 0.3333333333333333148, 0.3333333333333334814, 0.3333333333333333703, 0.3333333333333334259, 0.3333333333333334814, 0.3333333333333334814, 0.3333333333333334259, 0.3333333333333334259, 0.3333333333333335369, 0.3333333333333334814, 0.3333333333333333148, 0.3333333333333335369, 0.3333333333333334259, 0.3333333333333333703, 0.3333333333333334259, 0.3333333333333334259, 0.3333333333333333148, 0.3333333333333334814, 0.3333333333333333703, 0.3333333333333334259, 0.3333333333333333148, 0.3333333333333334814, 0.3333333333333334259, 0.3333333333333333148, 0.3333333333333334814, 0.3333333333333334259, 0.3333333333333334814, 0.3333333333333332593, 0.3333333333333335924, 0.3333333333333334259, 0.3333333333333334259),
 ( 1.000000000000000222, 1.000000000000000222, 1.000000000000000444, 1.000000000000000000, 1.000000000000000444, 1.000000000000000222, 1.000000000000000444, 0.9999999999999997780, 1.000000000000000444, 1.000000000000000000, 1.000000000000000444, 1.000000000000000000, 1.000000000000000444, 1.000000000000000222, 1.000000000000000000, 1.000000000000000666, 0.9999999999999997780, 1.000000000000000444, 1.000000000000000444, 1.000000000000000444, 1.000000000000000222, 1.000000000000000222, 1.000000000000000444, 1.000000000000000444, 1.000000000000000000, 1.000000000000000222, 1.000000000000000222, 1.000000000000000444, 1.000000000000000222, 1.000000000000000444, 1.000000000000000000, 1.000000000000000222, 1.000000000000000444, 1.000000000000000000, 1.000000000000000444, 1.000000000000000222, 1.000000000000000444, 1.000000000000000444, 1.000000000000000222, 1.000000000000000000, 1.000000000000000444, 1.000000000000000222, 1.000000000000000000, 1.000000000000000222, 1.000000000000000444, 1.000000000000000444, 1.000000000000000444, 1.000000000000000444, 1.000000000000000222, 1.000000000000000444, 1.000000000000000000, 1.000000000000000444, 1.000000000000000222, 1.000000000000000222, 1.000000000000000444, 1.000000000000000000, 1.000000000000000222, 1.000000000000000444, 1.000000000000000222, 1.000000000000000000, 1.000000000000000444, 1.000000000000000222, 1.000000000000000222, 1.000000000000000000, 1.000000000000000444, 0.9999999999999997780, 1.000000000000000444, 1.000000000000000000, 1.000000000000000444, 1.000000000000000000, 1.000000000000000444, 0.9999999999999997780, 1.000000000000000222, 1.000000000000000444, 1.000000000000000444, 1.000000000000000000, 1.000000000000000444, 1.000000000000000222, 1.000000000000000000, 1.000000000000000666, 1.000000000000000000, 1.000000000000000444, 1.000000000000000222, 1.000000000000000444, 0.9999999999999997780, 1.000000000000000444, 1.000000000000000000, 1.000000000000000444, 1.000000000000000444, 1.000000000000000222, 1.000000000000000222, 1.000000000000000444, 1.000000000000000222, 1.000000000000000444, 1.000000000000000444, 1.000000000000000222, 1.000000000000000444, 1.000000000000000222, 1.000000000000000444, 1.000000000000000000, 1.000000000000000444, 1.000000000000000000, 1.000000000000000000, 1.000000000000000444, 1.000000000000000222, 1.000000000000000222, 1.000000000000000444, 1.000000000000000000, 1.000000000000000444, 1.000000000000000000, 1.000000000000000222, 1.000000000000000444, 0.9999999999999997780, 1.000000000000000444, 1.000000000000000222, 1.000000000000000444, 1.000000000000000000, 1.000000000000000444, 1.000000000000000000, 1.000000000000000222, 1.000000000000000222, 1.000000000000000444, 1.000000000000000222, 1.000000000000000000, 1.000000000000000444, 1.000000000000000222, 1.000000000000000222, 1.000000000000000222, 1.000000000000000444, 0.9999999999999997780, 1.000000000000000666, 0.9999999999999996669, 1.000000000000000444, 1.000000000000000444, 1.000000000000000222, 1.000000000000000444, 1.000000000000000444, 1.000000000000000222, 1.000000000000000000, 1.000000000000000444, 1.000000000000000000, 1.000000000000000444, 1.000000000000000222, 1.000000000000000444, 1.000000000000000000, 1.000000000000000444, 1.000000000000000222, 1.000000000000000222, 1.000000000000000444, 1.000000000000000222, 0.9999999999999997780, 1.000000000000000444, 1.000000000000000444, 1.000000000000000444, 1.000000000000000222, 1.000000000000000444, 1.000000000000000444, 1.000000000000000222, 1.000000000000000444, 1.000000000000000000, 1.000000000000000222, 1.000000000000000444, 1.000000000000000000, 1.000000000000000222, 1.000000000000000444, 1.000000000000000000, 1.000000000000000444, 0.9999999999999997780, 1.000000000000000222, 1.000000000000000444, 1.000000000000000000, 1.000000000000000222, 1.000000000000000222, 1.000000000000000444, 1.000000000000000000, 1.000000000000000666, 0.9999999999999996669, 1.000000000000000666, 1.000000000000000222, 1.000000000000000444, 1.000000000000000222, 1.000000000000000444, 1.000000000000000222, 1.000000000000000222, 1.000000000000000000, 1.000000000000000444, 0.9999999999999997780, 1.000000000000000444, 1.000000000000000222, 1.000000000000000444, 0.9999999999999997780, 1.000000000000000444, 1.000000000000000000, 1.000000000000000222, 1.000000000000000444, 1.000000000000000000, 1.000000000000000444, 1.000000000000000444, 1.000000000000000222, 1.000000000000000222, 1.000000000000000000, 1.000000000000000444, 1.000000000000000444, 1.000000000000000000, 1.000000000000000222, 1.000000000000000222, 1.000000000000000444, 1.000000000000000222, 1.000000000000000222, 1.000000000000000444, 1.000000000000000222, 1.000000000000000000, 1.000000000000000444, 1.000000000000000000, 1.000000000000000222, 1.000000000000000444, 1.000000000000000222, 1.000000000000000222, 1.000000000000000444, 1.000000000000000000, 1.000000000000000222, 1.000000000000000222, 1.000000000000000222, 1.000000000000000000, 1.000000000000000222, 1.000000000000000222, 1.000000000000000000, 1.000000000000000222, 1.000000000000000222, 1.000000000000000444, 1.000000000000000000, 1.000000000000000000, 1.000000000000000222, 1.000000000000000000, 1.000000000000000888, 1.000000000000000000, 1.000000000000000444, 1.000000000000000222, 1.000000000000000222, 1.000000000000000444, 1.000000000000000222, 1.000000000000000222, 1.000000000000000444, 1.000000000000000444, 1.000000000000000222, 1.000000000000000444, 1.000000000000000222, 1.000000000000000000, 1.000000000000000222, 1.000000000000000444, 1.000000000000000444, 1.000000000000000222, 1.000000000000000444, 1.000000000000000222, 1.000000000000000444, 1.000000000000000222, 1.000000000000000444, 1.000000000000000222, 1.000000000000000000, 1.000000000000000444, 1.000000000000000000, 1.000000000000000666, 1.000000000000000000, 1.000000000000000000, 1.000000000000000444, 1.000000000000000222, 1.000000000000000444, 0.9999999999999997780, 1.000000000000000666, 1.000000000000000222, 1.000000000000000444, 1.000000000000000222, 1.000000000000000444, 1.000000000000000222, 1.000000000000000444, 0.9999999999999997780, 1.000000000000000666, 1.000000000000000222, 1.000000000000000222, 1.000000000000000444, 1.000000000000000444, 0.9999999999999997780, 1.000000000000000444, 1.000000000000000222, 1.000000000000000222, 1.000000000000000000, 1.000000000000000000, 1.000000000000000444, 1.000000000000000444, 1.000000000000000222, 1.000000000000000000, 1.000000000000000444, 0.9999999999999997780, 1.000000000000000444, 1.000000000000000222, 1.000000000000000000, 1.000000000000000222, 1.000000000000000000, 1.000000000000000444, 1.000000000000000000, 1.000000000000000444, 1.000000000000000222, 1.000000000000000222, 1.000000000000000222, 1.000000000000000222, 1.000000000000000222, 1.000000000000000444, 1.000000000000000222, 1.000000000000000444, 1.000000000000000222, 1.000000000000000000, 1.000000000000000888, 0.9999999999999996669, 1.000000000000000444, 1.000000000000000444, 1.000000000000000222, 1.000000000000000444, 1.000000000000000000, 1.000000000000000444, 0.9999999999999997780, 1.000000000000000444, 1.000000000000000222, 1.000000000000000444, 0.9999999999999997780, 1.000000000000000222, 1.000000000000000222, 1.000000000000000444, 1.000000000000000000, 1.000000000000000444, 1.000000000000000444, 1.000000000000000222, 1.000000000000000000, 1.000000000000000444, 1.000000000000000000, 1.000000000000000222, 1.000000000000000222, 1.000000000000000444, 1.000000000000000000, 1.000000000000000666, 1.000000000000000000, 1.000000000000000444, 1.000000000000000222, 1.000000000000000444, 1.000000000000000222, 1.000000000000000444, 1.000000000000000222, 1.000000000000000222, 1.000000000000000222, 1.000000000000000444, 1.000000000000000444, 1.000000000000000222, 1.000000000000000000, 1.000000000000000444, 1.000000000000000444, 1.000000000000000000, 1.000000000000000444, 0.9999999999999997780, 1.000000000000000444, 1.000000000000000222, 1.000000000000000222, 1.000000000000000444, 1.000000000000000222, 1.000000000000000222, 1.000000000000000444, 1.000000000000000444, 1.000000000000000444, 1.000000000000000000, 1.000000000000000444, 1.000000000000000222, 1.000000000000000222, 1.000000000000000000, 1.000000000000000444, 0.9999999999999997780, 1.000000000000000444, 1.000000000000000000, 1.000000000000000444, 1.000000000000000000, 1.000000000000000444, 1.000000000000000222, 1.000000000000000000, 1.000000000000000444, 1.000000000000000222, 1.000000000000000444, 0.9999999999999997780, 1.000000000000000444, 1.000000000000000222, 1.000000000000000222),
 ( 0.3333333333333334259, 0.3333333333333334259, 0.3333333333333334814, 0.3333333333333333703, 0.3333333333333335369, 0.3333333333333334259, 0.3333333333333334814, 0.3333333333333333703, 0.3333333333333334259, 0.3333333333333333703, 0.3333333333333335369, 0.3333333333333333703, 0.3333333333333334259, 0.3333333333333334259, 0.3333333333333333703, 0.3333333333333335369, 0.3333333333333333703, 0.3333333333333334259, 0.3333333333333335369, 0.3333333333333334259, 0.3333333333333333703, 0.3333333333333334259, 0.3333333333333334814, 0.3333333333333335369, 0.3333333333333333148, 0.3333333333333334259, 0.3333333333333334259, 0.3333333333333334814, 0.3333333333333334259, 0.3333333333333334259, 0.3333333333333334259, 0.3333333333333333148, 0.3333333333333335924, 0.3333333333333333148, 0.3333333333333335369, 0.3333333333333333703, 0.3333333333333335369, 0.3333333333333334259, 0.3333333333333333703, 0.3333333333333333703, 0.3333333333333335924, 0.3333333333333333148, 0.3333333333333334259, 0.3333333333333334259, 0.3333333333333335369, 0.3333333333333334814, 0.3333333333333334259, 0.3333333333333334259, 0.3333333333333334259, 0.3333333333333334259, 0.3333333333333333703, 0.3333333333333335369, 0.3333333333333334259, 0.3333333333333334259, 0.3333333333333334814, 0.3333333333333333703, 0.3333333333333333703, 0.3333333333333334814, 0.3333333333333334259, 0.3333333333333333703, 0.3333333333333334814, 0.3333333333333333703, 0.3333333333333334814, 0.3333333333333332593, 0.3333333333333335924, 0.3333333333333333148, 0.3333333333333335924, 0.3333333333333333148, 0.3333333333333335924, 0.3333333333333334259, 0.3333333333333334814, 0.3333333333333333703, 0.3333333333333333703, 0.3333333333333334814, 0.3333333333333335369, 0.3333333333333333703, 0.3333333333333334814, 0.3333333333333334259, 0.3333333333333333703, 0.3333333333333335369, 0.3333333333333333148, 0.3333333333333335369, 0.3333333333333334259, 0.3333333333333334259, 0.3333333333333333703, 0.3333333333333334259, 0.3333333333333333703, 0.3333333333333335369, 0.3333333333333333703, 0.3333333333333334259, 0.3333333333333334259, 0.3333333333333334814, 0.3333333333333333703, 0.3333333333333335924, 0.3333333333333333703, 0.3333333333333334259, 0.3333333333333334814, 0.3333333333333334259, 0.3333333333333335369, 0.3333333333333333148, 0.3333333333333335369, 0.3333333333333333148, 0.3333333333333334259, 0.3333333333333333703, 0.3333333333333334259, 0.3333333333333334259, 0.3333333333333335924, 0.3333333333333333703, 0.3333333333333335924, 0.3333333333333333148, 0.3333333333333335369, 0.3333333333333335369, 0.3333333333333333148, 0.3333333333333334259, 0.3333333333333334259, 0.3333333333333334814, 0.3333333333333333703, 0.3333333333333335369, 0.3333333333333333703, 0.3333333333333333703, 0.3333333333333334814, 0.3333333333333334814, 0.3333333333333334259, 0.3333333333333333703, 0.3333333333333334814, 0.3333333333333334814, 0.3333333333333334259, 0.3333333333333334259, 0.3333333333333334259, 0.3333333333333333703, 0.3333333333333335369, 0.3333333333333333703, 0.3333333333333334259, 0.3333333333333334814, 0.3333333333333334259, 0.3333333333333334814, 0.3333333333333334259, 0.3333333333333333703, 0.3333333333333333703, 0.3333333333333334259, 0.3333333333333333148, 0.3333333333333334814, 0.3333333333333334814, 0.3333333333333334259, 0.3333333333333333703, 0.3333333333333334259, 0.3333333333333334259, 0.3333333333333333703, 0.3333333333333335369, 0.3333333333333334259, 0.3333333333333333148, 0.3333333333333333703, 0.3333333333333335369, 0.3333333333333335369, 0.3333333333333333148, 0.3333333333333335369, 0.3333333333333334259, 0.3333333333333334259, 0.3333333333333335369, 0.3333333333333333703, 0.3333333333333333703, 0.3333333333333334259, 0.3333333333333333703, 0.3333333333333334259, 0.3333333333333334259, 0.3333333333333333703, 0.3333333333333335369, 0.3333333333333333703, 0.3333333333333334259, 0.3333333333333335369, 0.3333333333333333703, 0.3333333333333333703, 0.3333333333333334814, 0.3333333333333334259, 0.3333333333333333703, 0.3333333333333335369, 0.3333333333333332593, 0.3333333333333335369, 0.3333333333333335369, 0.3333333333333333703, 0.3333333333333334814, 0.3333333333333334814, 0.3333333333333334259, 0.3333333333333333703, 0.3333333333333334259, 0.3333333333333334814, 0.3333333333333333148, 0.3333333333333335369, 0.3333333333333333703, 0.3333333333333334259, 0.3333333333333333703, 0.3333333333333334259, 0.3333333333333333148, 0.3333333333333334259, 0.3333333333333334814, 0.3333333333333333703, 0.3333333333333334814, 0.3333333333333334259, 0.3333333333333333703, 0.3333333333333334259, 0.3333333333333333703, 0.3333333333333334259, 0.3333333333333334814, 0.3333333333333332593, 0.3333333333333334259, 0.3333333333333333703, 0.3333333333333335369, 0.3333333333333334259, 0.3333333333333333703, 0.3333333333333334259, 0.3333333333333334259, 0.3333333333333333148, 0.3333333333333335369, 0.3333333333333333703, 0.3333333333333334259, 0.3333333333333335924, 0.3333333333333333703, 0.3333333333333334259, 0.3333333333333335369, 0.3333333333333333703, 0.3333333333333334259, 0.3333333333333334259, 0.3333333333333334259, 0.3333333333333333703, 0.3333333333333334259, 0.3333333333333334259, 0.3333333333333333703, 0.3333333333333333148, 0.3333333333333334814, 0.3333333333333334259, 0.3333333333333334259, 0.3333333333333333703, 0.3333333333333333703, 0.3333333333333334259, 0.3333333333333335369, 0.3333333333333333703, 0.3333333333333335369, 0.3333333333333333703, 0.3333333333333334259, 0.3333333333333335369, 0.3333333333333333148, 0.3333333333333334259, 0.3333333333333334814, 0.3333333333333335369, 0.3333333333333333148, 0.3333333333333335369, 0.3333333333333333703, 0.3333333333333334259, 0.3333333333333333703, 0.3333333333333335369, 0.3333333333333334259, 0.3333333333333334259, 0.3333333333333334259, 0.3333333333333333703, 0.3333333333333335924, 0.3333333333333334259, 0.3333333333333335369, 0.3333333333333333148, 0.3333333333333333703, 0.3333333333333334814, 0.3333333333333333703, 0.3333333333333335924, 0.3333333333333333148, 0.3333333333333333703, 0.3333333333333335369, 0.3333333333333333703, 0.3333333333333335924, 0.3333333333333332593, 0.3333333333333335924, 0.3333333333333334259, 0.3333333333333335369, 0.3333333333333334259, 0.3333333333333334814, 0.3333333333333333703, 0.3333333333333334814, 0.3333333333333333148, 0.3333333333333335369, 0.3333333333333333148, 0.3333333333333334814, 0.3333333333333334814, 0.3333333333333334814, 0.3333333333333333148, 0.3333333333333335369, 0.3333333333333333148, 0.3333333333333335369, 0.3333333333333333703, 0.3333333333333333703, 0.3333333333333335369, 0.3333333333333334259, 0.3333333333333334259, 0.3333333333333333703, 0.3333333333333335369, 0.3333333333333333148, 0.3333333333333335924, 0.3333333333333334259, 0.3333333333333334259, 0.3333333333333333703, 0.3333333333333333703, 0.3333333333333334259, 0.3333333333333334259, 0.3333333333333334259, 0.3333333333333334259, 0.3333333333333334259, 0.3333333333333334259, 0.3333333333333334259, 0.3333333333333333703, 0.3333333333333335369, 0.3333333333333333703, 0.3333333333333334814, 0.3333333333333333703, 0.3333333333333333148, 0.3333333333333337034, 0.3333333333333332038, 0.3333333333333334814, 0.3333333333333335369, 0.3333333333333334814, 0.3333333333333334259, 0.3333333333333334259, 0.3333333333333334814, 0.3333333333333333703, 0.3333333333333334814, 0.3333333333333334259, 0.3333333333333334814, 0.3333333333333333148, 0.3333333333333333703, 0.3333333333333335369, 0.3333333333333334259, 0.3333333333333333703, 0.3333333333333335369, 0.3333333333333334814, 0.3333333333333334259, 0.3333333333333333703, 0.3333333333333334259, 0.3333333333333333148, 0.3333333333333335369, 0.3333333333333333148, 0.3333333333333335369, 0.3333333333333333703, 0.3333333333333335369, 0.3333333333333334259, 0.3333333333333334814, 0.3333333333333334259, 0.3333333333333335369, 0.3333333333333334259, 0.3333333333333334259, 0.3333333333333333703, 0.3333333333333334259, 0.3333333333333333703, 0.3333333333333335369, 0.3333333333333334814, 0.3333333333333333703, 0.3333333333333333148, 0.3333333333333335369, 0.3333333333333333703, 0.3333333333333333703, 0.3333333333333334814, 0.3333333333333333148, 0.3333333333333334814, 0.3333333333333333703, 0.3333333333333334259, 0.3333333333333334814, 0.3333333333333334814, 0.3333333333333334259, 0.3333333333333334259, 0.3333333333333335369, 0.3333333333333334814, 0.3333333333333333148, 0.3333333333333335369, 0.3333333333333334259, 0.3333333333333333703, 0.3333333333333334259, 0.3333333333333334259, 0.3333333333333333148, 0.3333333333333334814, 0.3333333333333333703, 0.3333333333333334259, 0.3333333333333333148, 0.3333333333333334814, 0.3333333333333334259, 0.3333333333333333148, 0.3333333333333334814, 0.3333333333333334259, 0.3333333333333334814, 0.3333333333333332593, 0.3333333333333335924, 0.3333333333333334259, 0.3333333333333334259),
 ( 0.3333333333333334259, 0.3333333333333334259, 0.3333333333333334814, 0.3333333333333333703, 0.3333333333333335369, 0.3333333333333334259, 0.3333333333333334814, 0.3333333333333333703, 0.3333333333333334259, 0.3333333333333333703, 0.3333333333333335369, 0.3333333333333333703, 0.3333333333333334259, 0.3333333333333334259, 0.3333333333333333703, 0.3333333333333335369, 0.3333333333333333703, 0.3333333333333334259, 0.3333333333333335369, 0.3333333333333334259, 0.3333333333333333703, 0.3333333333333334259, 0.3333333333333334814, 0.3333333333333335369, 0.3333333333333333148, 0.3333333333333334259, 0.3333333333333334259, 0.3333333333333334814, 0.3333333333333334259, 0.3333333333333334259, 0.3333333333333334259, 0.3333333333333333148, 0.3333333333333335924, 0.3333333333333333148, 0.3333333333333335369, 0.3333333333333333703, 0.3333333333333335369, 0.3333333333333334259, 0.3333333333333333703, 0.3333333333333333703, 0.3333333333333335924, 0.3333333333333333148, 0.3333333333333334259, 0.3333333333333334259, 0.3333333333333335369, 0.3333333333333334814, 0.3333333333333334259, 0.3333333333333334259, 0.3333333333333334259, 0.3333333333333334259, 0.3333333333333333703, 0.3333333333333335369, 0.3333333333333334259, 0.3333333333333334259, 0.3333333333333334814, 0.3333333333333333703, 0.3333333333333333703, 0.3333333333333334814, 0.3333333333333334259, 0.3333333333333333703, 0.3333333333333334814, 0.3333333333333333703, 0.3333333333333334814, 0.3333333333333332593, 0.3333333333333335924, 0.3333333333333333148, 0.3333333333333335924, 0.3333333333333333148, 0.3333333333333335924, 0.3333333333333334259, 0.3333333333333334814, 0.3333333333333333703, 0.3333333333333333703, 0.3333333333333334814, 0.3333333333333335369, 0.3333333333333333703, 0.3333333333333334814, 0.3333333333333334259, 0.3333333333333333703, 0.3333333333333335369, 0.3333333333333333148, 0.3333333333333335369, 0.3333333333333334259, 0.3333333333333334259, 0.3333333333333333703, 0.3333333333333334259, 0.3333333333333333703, 0.3333333333333335369, 0.3333333333333333703, 0.3333333333333334259, 0.3333333333333334259, 0.3333333333333334814, 0.3333333333333333703, 0.3333333333333335924, 0.3333333333333333703, 0.3333333333333334259, 0.3333333333333334814, 0.3333333333333334259, 0.3333333333333335369, 0.3333333333333333148, 0.3333333333333335369, 0.3333333333333333148, 0.3333333333333334259, 0.3333333333333333703, 0.3333333333333334259, 0.3333333333333334259, 0.3333333333333335924, 0.3333333333333333703, 0.3333333333333335924, 0.3333333333333333148, 0.3333333333333335369, 0.3333333333333335369, 0.3333333333333333148, 0.3333333333333334259, 0.3333333333333334259, 0.3333333333333334814, 0.3333333333333333703, 0.3333333333333335369, 0.3333333333333333703, 0.3333333333333333703, 0.3333333333333334814, 0.3333333333333334814, 0.3333333333333334259, 0.3333333333333333703, 0.3333333333333334814, 0.3333333333333334814, 0.3333333333333334259, 0.3333333333333334259, 0.3333333333333334259, 0.3333333333333333703, 0.3333333333333335369, 0.3333333333333333703, 0.3333333333333334259, 0.3333333333333334814, 0.3333333333333334259, 0.3333333333333334814, 0.3333333333333334259, 0.3333333333333333703, 0.3333333333333333703, 0.3333333333333334259, 0.3333333333333333148, 0.3333333333333334814, 0.3333333333333334814, 0.3333333333333334259, 0.3333333333333333703, 0.3333333333333334259, 0.3333333333333334259, 0.3333333333333333703, 0.3333333333333335369, 0.3333333333333334259, 0.3333333333333333148, 0.3333333333333333703, 0.3333333333333335369, 0.3333333333333335369, 0.3333333333333333148, 0.3333333333333335369, 0.3333333333333334259, 0.3333333333333334259, 0.3333333333333335369, 0.3333333333333333703, 0.3333333333333333703, 0.3333333333333334259, 0.3333333333333333703, 0.3333333333333334259, 0.3333333333333334259, 0.3333333333333333703, 0.3333333333333335369, 0.3333333333333333703, 0.3333333333333334259, 0.3333333333333335369, 0.3333333333333333703, 0.3333333333333333703, 0.3333333333333334814, 0.3333333333333334259, 0.3333333333333333703, 0.3333333333333335369, 0.3333333333333332593, 0.3333333333333335369, 0.3333333333333335369, 0.3333333333333333703, 0.3333333333333334814, 0.3333333333333334814, 0.3333333333333334259, 0.3333333333333333703, 0.3333333333333334259, 0.3333333333333334814, 0.3333333333333333148, 0.3333333333333335369, 0.3333333333333333703, 0.3333333333333334259, 0.3333333333333333703, 0.3333333333333334259, 0.3333333333333333148, 0.3333333333333334259, 0.3333333333333334814, 0.3333333333333333703, 0.3333333333333334814, 0.3333333333333334259, 0.3333333333333333703, 0.3333333333333334259, 0.3333333333333333703, 0.3333333333333334259, 0.3333333333333334814, 0.3333333333333332593, 0.3333333333333334259, 0.3333333333333333703, 0.3333333333333335369, 0.3333333333333334259, 0.3333333333333333703, 0.3333333333333334259, 0.3333333333333334259, 0.3333333333333333148, 0.3333333333333335369, 0.3333333333333333703, 0.3333333333333334259, 0.3333333333333335924, 0.3333333333333333703, 0.3333333333333334259, 0.3333333333333335369, 0.3333333333333333703, 0.3333333333333334259, 0.3333333333333334259, 0.3333333333333334259, 0.3333333333333333703, 0.3333333333333334259, 0.3333333333333334259, 0.3333333333333333703, 0.3333333333333333148, 0.3333333333333334814, 0.3333333333333334259, 0.3333333333333334259, 0.3333333333333333703, 0.3333333333333333703, 0.3333333333333334259, 0.3333333333333335369, 0.3333333333333333703, 0.3333333333333335369, 0.3333333333333333703, 0.3333333333333334259, 0.3333333333333335369, 0.3333333333333333148, 0.3333333333333334259, 0.3333333333333334814, 0.3333333333333335369, 0.3333333333333333148, 0.3333333333333335369, 0.3333333333333333703, 0.3333333333333334259, 0.3333333333333333703, 0.3333333333333335369, 0.3333333333333334259, 0.3333333333333334259, 0.3333333333333334259, 0.3333333333333333703, 0.3333333333333335924, 0.3333333333333334259, 0.3333333333333335369, 0.3333333333333333148, 0.3333333333333333703, 0.3333333333333334814, 0.3333333333333333703, 0.3333333333333335924, 0.3333333333333333148, 0.3333333333333333703, 0.3333333333333335369, 0.3333333333333333703, 0.3333333333333335924, 0.3333333333333332593, 0.3333333333333335924, 0.3333333333333334259, 0.3333333333333335369, 0.3333333333333334259, 0.3333333333333334814, 0.3333333333333333703, 0.3333333333333334814, 0.3333333333333333148, 0.3333333333333335369, 0.3333333333333333148, 0.3333333333333334814, 0.3333333333333334814, 0.3333333333333334814, 0.3333333333333333148, 0.3333333333333335369, 0.3333333333333333148, 0.3333333333333335369, 0.3333333333333333703, 0.3333333333333333703, 0.3333333333333335369, 0.3333333333333334259, 0.3333333333333334259, 0.3333333333333333703, 0.3333333333333335369, 0.3333333333333333148, 0.3333333333333335924, 0.3333333333333334259, 0.3333333333333334259, 0.3333333333333333703, 0.3333333333333333703, 0.3333333333333334259, 0.3333333333333334259, 0.3333333333333334259, 0.3333333333333334259, 0.3333333333333334259, 0.3333333333333334259, 0.3333333333333334259, 0.3333333333333333703, 0.3333333333333335369, 0.3333333333333333703, 0.3333333333333334814, 0.3333333333333333703, 0.3333333333333333148, 0.3333333333333337034, 0.3333333333333332038, 0.3333333333333334814, 0.3333333333333335369, 0.3333333333333334814, 0.3333333333333334259, 0.3333333333333334259, 0.3333333333333334814, 0.3333333333333333703, 0.3333333333333334814, 0.3333333333333334259, 0.3333333333333334814, 0.3333333333333333148, 0.3333333333333333703, 0.3333333333333335369, 0.3333333333333334259, 0.3333333333333333703, 0.3333333333333335369, 0.3333333333333334814, 0.3333333333333334259, 0.3333333333333333703, 0.3333333333333334259, 0.3333333333333333148, 0.3333333333333335369, 0.3333333333333333148, 0.3333333333333335369, 0.3333333333333333703, 0.3333333333333335369, 0.3333333333333334259, 0.3333333333333334814, 0.3333333333333334259, 0.3333333333333335369, 0.3333333333333334259, 0.3333333333333334259, 0.3333333333333333703, 0.3333333333333334259, 0.3333333333333333703, 0.3333333333333335369, 0.3333333333333334814, 0.3333333333333333703, 0.3333333333333333148, 0.3333333333333335369, 0.3333333333333333703, 0.3333333333333333703, 0.3333333333333334814, 0.3333333333333333148, 0.3333333333333334814, 0.3333333333333333703, 0.3333333333333334259, 0.3333333333333334814, 0.3333333333333334814, 0.3333333333333334259, 0.3333333333333334259, 0.3333333333333335369, 0.3333333333333334814, 0.3333333333333333148, 0.3333333333333335369, 0.3333333333333334259, 0.3333333333333333703, 0.3333333333333334259, 0.3333333333333334259, 0.3333333333333333148, 0.3333333333333334814, 0.3333333333333333703, 0.3333333333333334259, 0.3333333333333333148, 0.3333333333333334814, 0.3333333333333334259, 0.3333333333333333148, 0.3333333333333334814, 0.3333333333333334259, 0.3333333333333334814, 0.3333333333333332593, 0.3333333333333335924, 0.3333333333333334259, 0.3333333333333334259),
 ( 1.000000000000000222, 1.000000000000000222, 1.000000000000000444, 1.000000000000000000, 1.000000000000000444, 1.000000000000000222, 1.000000000000000444, 0.9999999999999997780, 1.000000000000000444, 1.000000000000000000, 1.000000000000000444, 1.000000000000000000, 1.000000000000000444, 1.000000000000000222, 1.000000000000000000, 1.000000000000000666, 0.9999999999999997780, 1.000000000000000444, 1.000000000000000444, 1.000000000000000444, 1.000000000000000222, 1.000000000000000222, 1.000000000000000444, 1.000000000000000444, 1.000000000000000000, 1.000000000000000222, 1.000000000000000222, 1.000000000000000444, 1.000000000000000222, 1.000000000000000444, 1.000000000000000000, 1.000000000000000222, 1.000000000000000444, 1.000000000000000000, 1.000000000000000444, 1.000000000000000222, 1.000000000000000444, 1.000000000000000444, 1.000000000000000222, 1.000000000000000000, 1.000000000000000444, 1.000000000000000222, 1.000000000000000000, 1.000000000000000222, 1.000000000000000444, 1.000000000000000444, 1.000000000000000444, 1.000000000000000444, 1.000000000000000222, 1.000000000000000444, 1.000000000000000000, 1.000000000000000444, 1.000000000000000222, 1.000000000000000222, 1.000000000000000444, 1.000000000000000000, 1.000000000000000222, 1.000000000000000444, 1.000000000000000222, 1.000000000000000000, 1.000000000000000444, 1.000000000000000222, 1.000000000000000222, 1.000000000000000000, 1.000000000000000444, 0.9999999999999997780, 1.000000000000000444, 1.000000000000000000, 1.000000000000000444, 1.000000000000000000, 1.000000000000000444, 0.9999999999999997780, 1.000000000000000222, 1.000000000000000444, 1.000000000000000444, 1.000000000000000000, 1.000000000000000444, 1.000000000000000222, 1.000000000000000000, 1.000000000000000666, 1.000000000000000000, 1.000000000000000444, 1.000000000000000222, 1.000000000000000444, 0.9999999999999997780, 1.000000000000000444, 1.000000000000000000, 1.000000000000000444, 1.000000000000000444, 1.000000000000000222, 1.000000000000000222, 1.000000000000000444, 1.000000000000000222, 1.000000000000000444, 1.000000000000000444, 1.000000000000000222, 1.000000000000000444, 1.000000000000000222, 1.000000000000000444, 1.000000000000000000, 1.000000000000000444, 1.000000000000000000, 1.000000000000000000, 1.000000000000000444, 1.000000000000000222, 1.000000000000000222, 1.000000000000000444, 1.000000000000000000, 1.000000000000000444, 1.000000000000000000, 1.000000000000000222, 1.000000000000000444, 0.9999999999999997780, 1.000000000000000444, 1.000000000000000222, 1.000000000000000444, 1.000000000000000000, 1.000000000000000444, 1.000000000000000000, 1.000000000000000222, 1.000000000000000222, 1.000000000000000444, 1.000000000000000222, 1.000000000000000000, 1.000000000000000444, 1.000000000000000222, 1.000000000000000222, 1.000000000000000222, 1.000000000000000444, 0.9999999999999997780, 1.000000000000000666, 0.9999999999999996669, 1.000000000000000444, 1.000000000000000444, 1.000000000000000222, 1.000000000000000444, 1.000000000000000444, 1.000000000000000222, 1.000000000000000000, 1.000000000000000444, 1.000000000000000000, 1.000000000000000444, 1.000000000000000222, 1.000000000000000444, 1.000000000000000000, 1.000000000000000444, 1.000000000000000222, 1.000000000000000222, 1.000000000000000444, 1.000000000000000222, 0.9999999999999997780, 1.000000000000000444, 1.000000000000000444, 1.000000000000000444, 1.000000000000000222, 1.000000000000000444, 1.000000000000000444, 1.000000000000000222, 1.000000000000000444, 1.000000000000000000, 1.000000000000000222, 1.000000000000000444, 1.000000000000000000, 1.000000000000000222, 1.000000000000000444, 1.000000000000000000, 1.000000000000000444, 0.9999999999999997780, 1.000000000000000222, 1.000000000000000444, 1.000000000000000000, 1.000000000000000222, 1.000000000000000222, 1.000000000000000444, 1.000000000000000000, 1.000000000000000666, 0.9999999999999996669, 1.000000000000000666, 1.000000000000000222, 1.000000000000000444, 1.000000000000000222, 1.000000000000000444, 1.000000000000000222, 1.000000000000000222, 1.000000000000000000, 1.000000000000000444, 0.9999999999999997780, 1.000000000000000444, 1.000000000000000222, 1.000000000000000444, 0.9999999999999997780, 1.000000000000000444, 1.000000000000000000, 1.000000000000000222, 1.000000000000000444, 1.000000000000000000, 1.000000000000000444, 1.000000000000000444, 1.000000000000000222, 1.000000000000000222, 1.000000000000000000, 1.000000000000000444, 1.000000000000000444, 1.000000000000000000, 1.000000000000000222, 1.000000000000000222, 1.000000000000000444, 1.000000000000000222, 1.000000000000000222, 1.000000000000000444, 1.000000000000000222, 1.000000000000000000, 1.000000000000000444, 1.000000000000000000, 1.000000000000000222, 1.000000000000000444, 1.000000000000000222, 1.000000000000000222, 1.000000000000000444, 1.000000000000000000, 1.000000000000000222, 1.000000000000000222, 1.000000000000000222, 1.000000000000000000, 1.000000000000000222, 1.000000000000000222, 1.000000000000000000, 1.000000000000000222, 1.000000000000000222, 1.000000000000000444, 1.000000000000000000, 1.000000000000000000, 1.000000000000000222, 1.000000000000000000, 1.000000000000000888, 1.000000000000000000, 1.000000000000000444, 1.000000000000000222, 1.000000000000000222, 1.000000000000000444, 1.000000000000000222, 1.000000000000000222, 1.000000000000000444, 1.000000000000000444, 1.000000000000000222, 1.000000000000000444, 1.000000000000000222, 1.000000000000000000, 1.000000000000000222, 1.000000000000000444, 1.000000000000000444, 1.000000000000000222, 1.000000000000000444, 1.000000000000000222, 1.000000000000000444, 1.000000000000000222, 1.000000000000000444, 1.000000000000000222, 1.000000000000000000, 1.000000000000000444, 1.000000000000000000, 1.000000000000000666, 1.000000000000000000, 1.000000000000000000, 1.000000000000000444, 1.000000000000000222, 1.000000000000000444, 0.9999999999999997780, 1.000000000000000666, 1.000000000000000222, 1.000000000000000444, 1.000000000000000222, 1.000000000000000444, 1.000000000000000222, 1.000000000000000444, 0.9999999999999997780, 1.000000000000000666, 1.000000000000000222, 1.000000000000000222, 1.000000000000000444, 1.000000000000000444, 0.9999999999999997780, 1.000000000000000444, 1.000000000000000222, 1.000000000000000222, 1.000000000000000000, 1.000000000000000000, 1.000000000000000444, 1.000000000000000444, 1.000000000000000222, 1.000000000000000000, 1.000000000000000444, 0.9999999999999997780, 1.000000000000000444, 1.000000000000000222, 1.000000000000000000, 1.000000000000000222, 1.000000000000000000, 1.000000000000000444, 1.000000000000000000, 1.000000000000000444, 1.000000000000000222, 1.000000000000000222, 1.000000000000000222, 1.000000000000000222, 1.000000000000000222, 1.000000000000000444, 1.000000000000000222, 1.000000000000000444, 1.000000000000000222, 1.000000000000000000, 1.000000000000000888, 0.9999999999999996669, 1.000000000000000444, 1.000000000000000444, 1.000000000000000222, 1.000000000000000444, 1.000000000000000000, 1.000000000000000444, 0.9999999999999997780, 1.000000000000000444, 1.000000000000000222, 1.000000000000000444, 0.9999999999999997780, 1.000000000000000222, 1.000000000000000222, 1.000000000000000444, 1.000000000000000000, 1.000000000000000444, 1.000000000000000444, 1.000000000000000222, 1.000000000000000000, 1.000000000000000444, 1.000000000000000000, 1.000000000000000222, 1.000000000000000222, 1.000000000000000444, 1.000000000000000000, 1.000000000000000666, 1.000000000000000000, 1.000000000000000444, 1.000000000000000222, 1.000000000000000444, 1.000000000000000222, 1.000000000000000444, 1.000000000000000222, 1.000000000000000222, 1.000000000000000222, 1.000000000000000444, 1.000000000000000444, 1.000000000000000222, 1.000000000000000000, 1.000000000000000444, 1.000000000000000444, 1.000000000000000000, 1.000000000000000444, 0.9999999999999997780, 1.000000000000000444, 1.000000000000000222, 1.000000000000000222, 1.000000000000000444, 1.000000000000000222, 1.000000000000000222, 1.000000000000000444, 1.000000000000000444, 1.000000000000000444, 1.000000000000000000, 1.000000000000000444, 1.000000000000000222, 1.000000000000000222, 1.000000000000000000, 1.000000000000000444, 0.9999999999999997780, 1.000000000000000444, 1.000000000000000000, 1.000000000000000444, 1.000000000000000000, 1.000000000000000444, 1.000000000000000222, 1.000000000000000000, 1.000000000000000444, 1.000000000000000222, 1.000000000000000444, 0.9999999999999997780, 1.000000000000000444, 1.000000000000000222, 1.000000000000000222) ) ) 
 REPRESENTATION_ITEM ( '' )  SURFACE ( )  );
#57011=CARTESIAN_POINT ( 'NONE',  ( 5.624284779170636739, 1.176309258369928390, -1.581782371169083712 ) ) ;
#57015=CARTESIAN_POINT ( 'NONE',  ( 0.3693899063928334781, -1.702925086422102163, -1.073505336752482053 ) ) ;
#57017=CARTESIAN_POINT ( 'NONE',  ( 6.157425464982741126, 2.025529447029483343, -0.6166105444416707382 ) ) ;
#57020=CARTESIAN_POINT ( 'NONE',  ( 1.979048004138800998, 1.930994533390210544, 0.7472069620131777112 ) ) ;
#57024=CARTESIAN_POINT ( 'NONE',  ( 3.363305035154311007, 2.039577031997115597, -0.4584567826917042010 ) ) ;
#57027=CARTESIAN_POINT ( 'NONE',  ( 2.151128115021032627, -1.464471472660273665, -1.089769533225225073 ) ) ;
#57028=CARTESIAN_POINT ( 'NONE',  ( 1.523755425131537278, -1.797796875034236797, 0.2216367714752715545 ) ) ;
#57029=ORIENTED_EDGE ( 'NONE', *, *, #148486, .F. ) ;
#57030=CARTESIAN_POINT ( 'NONE',  ( 4.987059637548557411, -0.2676712469649074055, -2.190530366034774801 ) ) ;
#57032=CARTESIAN_POINT ( 'NONE',  ( 3.839080194659278966, 0.3211572903306300075, 2.183152695405643051 ) ) ;
#57035=CARTESIAN_POINT ( 'NONE',  ( 3.369685512061989741, 0.4621021693036463374, -1.855490417808260961 ) ) ;
#57037=CARTESIAN_POINT ( 'NONE',  ( 5.107906530550561541, 0.6527686194882609261, -1.964817160181750788 ) ) ;
#57040=CARTESIAN_POINT ( 'NONE',  ( 6.356982542327763497, 0.3766756592470664744, -2.158781491689326426 ) ) ;
#57051=CARTESIAN_POINT ( 'NONE',  ( 6.174686067066745387, 1.394736081427111030, -1.530067588329916850 ) ) ;
#57052=CARTESIAN_POINT ( 'NONE',  ( 4.582597182753257670, -1.869065293654921023, -0.4664472792492486697 ) ) ;
#57053=CARTESIAN_POINT ( 'NONE',  ( 1.511342449054883241, -1.897691915346022329, 0.6820157586827847451 ) ) ;
#57056=CARTESIAN_POINT ( 'NONE',  ( 1.271705539736139423, 1.307743536042236920, 1.758333696453084016 ) ) ;
#57057=CARTESIAN_POINT ( 'NONE',  ( 4.986841741376339066, -0.2268417095559888130, -1.811474396668552700 ) ) ;
#57065=CARTESIAN_POINT ( 'NONE',  ( 2.542321706073047416, -1.529623444112483632, 1.024600984555257277 ) ) ;
#57066=CARTESIAN_POINT ( 'NONE',  ( 6.011982430150495382, -0.6741147929612385514, 1.897138445369117354 ) ) ;
#57067=CARTESIAN_POINT ( 'NONE',  ( 1.757567914286566335, -2.287329856776819881, -0.2253975434684113155 ) ) ;
#57068=CARTESIAN_POINT ( 'NONE',  ( 6.719590461409528537, 0.3385411321301828314, -1.932175811092277096 ) ) ;
#57074=CARTESIAN_POINT ( 'NONE',  ( 2.595357119365874432, -0.6533576199754445035, 1.986123937679643348 ) ) ;
#57075=CARTESIAN_POINT ( 'NONE',  ( 1.551402291579254022, 0.5461136009352780540, -1.789155053659279071 ) ) ;
#57076=CARTESIAN_POINT ( 'NONE',  ( 1.845077155533506374, -1.080901620906085325, 1.701686244941137183 ) ) ;
#57080=CARTESIAN_POINT ( 'NONE',  ( 2.436699184107835592, -1.290689972581187339, -1.167790367532922646 ) ) ;
#57083=CARTESIAN_POINT ( 'NONE',  ( 2.437784706471317175, 0.8137022719644730895, -1.520871857739027444 ) ) ;
#57084=CARTESIAN_POINT ( 'NONE',  ( 2.472451708263478931, -2.098117355222902436, -0.6331711661175795092 ) ) ;
#57085=CARTESIAN_POINT ( 'NONE',  ( 4.740968412965463230, 0.3751893352213676591, 2.174603215771487630 ) ) ;
#57087=CARTESIAN_POINT ( 'NONE',  ( 2.905323041198346612, -1.807408099546173208, 1.202558989554833646 ) ) ;
#57088=CARTESIAN_POINT ( 'NONE',  ( 1.400715809426569702, 1.493624456287694358, -1.049586478250638999 ) ) ;
#57089=PRESENTATION_STYLE_ASSIGNMENT (( #40858 ) ) ;
#57090=CARTESIAN_POINT ( 'NONE',  ( 4.065693644434860587, 1.385821322041587145, 1.600864752689701076 ) ) ;
#57093=CARTESIAN_POINT ( 'NONE',  ( 4.423529165095542837, -1.409716928370784661, -1.807567988613969723 ) ) ;
#57097=CARTESIAN_POINT ( 'NONE',  ( 0.6629299983115041206, 0.6194173074674096391, 2.027988828570789437 ) ) ;
#57103=CARTESIAN_POINT ( 'NONE',  ( 5.027970288326706338, -1.728003250605243180, 1.038991650911202713 ) ) ;
#57105=CARTESIAN_POINT ( 'NONE',  ( 2.905193444429104321, -1.717358790072313957, 1.142030567362181559 ) ) ;
#57107=CARTESIAN_POINT ( 'NONE',  ( -0.2409995289980246258, 2.020898751655671788, -2.415740196953279462 ) ) ;
#57111=CARTESIAN_POINT ( 'NONE',  ( 5.701184558104195332, -0.5354452791076976803, 2.124913622581547479 ) ) ;
#57112=CARTESIAN_POINT ( 'NONE',  ( 3.551407868487792552, -1.352154898762620849, 1.496051317864899088 ) ) ;
#57113=CARTESIAN_POINT ( 'NONE',  ( 2.788419073117563762, 1.577926727847511312, -0.9486480243563880643 ) ) ;
#57115=CARTESIAN_POINT ( 'NONE',  ( 6.000976577881286467, 1.490888274384492895, -1.053294804101669868 ) ) ;
#57117=CARTESIAN_POINT ( 'NONE',  ( -0.03393210605391345364, -2.232032725161440023, -0.5493522527948471179 ) ) ;
#57119=CARTESIAN_POINT ( 'NONE',  ( 0.2985908658455891929, -2.261944659375872302, -0.05357643010404227607 ) ) ;
#57120=CARTESIAN_POINT ( 'NONE',  ( 1.805437418371407254, 1.751699828856004837, 1.168899091633753384 ) ) ;
#57129=CARTESIAN_POINT ( 'NONE',  ( 4.324628213192062809, -0.9515899357304625772, -2.007430035002121471 ) ) ;
#57130=CARTESIAN_POINT ( 'NONE',  ( 2.080269975650438585, -2.149535124392497831, -0.4257020960420563882 ) ) ;
#57131=CARTESIAN_POINT ( 'NONE',  ( 0.4697016844467936103, 0.2121168557088908557, -2.196667960996725011 ) ) ;
#57133=CARTESIAN_POINT ( 'NONE',  ( 4.580490334204036174, 1.208584658811951762, -1.545285769342201965 ) ) ;
#57136=CARTESIAN_POINT ( 'NONE',  ( 6.609999999999998543, 2.109033691136730226, 2.032371550245914094 ) ) ;
#57139=CARTESIAN_POINT ( 'NONE',  ( 3.674183785563363447, 2.104178206457421485, -0.2630699042918820396 ) ) ;
#57141=CARTESIAN_POINT ( 'NONE',  ( 5.348557406608104969, 0.6236849695623291057, 2.069784783864880851 ) ) ;
#57142=CARTESIAN_POINT ( 'NONE',  ( 3.649809678215182096, 0.6660801477775115664, 1.716721118343276231 ) ) ;
#57146=CARTESIAN_POINT ( 'NONE',  ( 6.421804192028983671, 0.9955936683583621605, -1.427223192643598537 ) ) ;
#57147=CARTESIAN_POINT ( 'NONE',  ( 6.827182134110161726, 7.629137130509067610, 2.310944104600751281 ) ) ;
#57151=CARTESIAN_POINT ( 'NONE',  ( 4.329101982860062314, 0.1031891237209987822, 2.159356164053369387 ) ) ;
#57154=CARTESIAN_POINT ( 'NONE',  ( 5.905624997962407363, 0.3905408587613137805, 1.977747231101577352 ) ) ;
#57156=CARTESIAN_POINT ( 'NONE',  ( 3.801785103514757846, -0.6297183656660889639, 2.067937956787009757 ) ) ;
#57157=CARTESIAN_POINT ( 'NONE',  ( 4.938727034960622930, 0.3341968672867478007, 1.942665651468850951 ) ) ;
#57158=CARTESIAN_POINT ( 'NONE',  ( 3.708057520534962848, -1.311595775785476148, -1.134043610401070712 ) ) ;
#57160=CARTESIAN_POINT ( 'NONE',  ( 0.2928600448571066495, 1.818678932476354149, -1.222557900829209121 ) ) ;
#57161=CARTESIAN_POINT ( 'NONE',  ( 1.273011573350724568, -1.461848840328241694, 1.785463964174689000 ) ) ;
#57162=CARTESIAN_POINT ( 'NONE',  ( 3.638010413220875705, 0.9297346566990055683, -1.839232330223056433 ) ) ;
#57163=CARTESIAN_POINT ( 'NONE',  ( 5.478056170419292492, -1.895640208600479326, -0.4214399443674861079 ) ) ;
#57171=CARTESIAN_POINT ( 'NONE',  ( 2.766872162265196611, -1.522532973755141850, 1.597636210702752635 ) ) ;
#57174=CARTESIAN_POINT ( 'NONE',  ( 0.8657744530725123289, -1.852701964455932604, 0.1747518070307155780 ) ) ;
#57175=CARTESIAN_POINT ( 'NONE',  ( -0.1291982275798625457, 7.629137130509075604, -2.673995287120598086 ) ) ;
#57180=CARTESIAN_POINT ( 'NONE',  ( 6.720655732516647163, 0.005566325962592238996, 1.826293863978686982 ) ) ;
#57181=VERTEX_POINT ( 'NONE', #24707 ) ;
#57182=CARTESIAN_POINT ( 'NONE',  ( 2.237249138949083171, -1.841491494976960075, 0.9254197329602343869 ) ) ;
#57189=CARTESIAN_POINT ( 'NONE',  ( 0.6903932018771785639, -2.045263458338997253, -0.2527981509174073715 ) ) ;
#57191=CARTESIAN_POINT ( 'NONE',  ( 4.634224865634020141, 0.3196297827482602050, 1.813140464320086132 ) ) ;
#57197=CARTESIAN_POINT ( 'NONE',  ( 4.688207069967821106, -1.042061291317699423, 1.945354640606362873 ) ) ;
#57198=CARTESIAN_POINT ( 'NONE',  ( 0.2456851981432126020, -1.670693100197045977, -1.371219901248825535 ) ) ;
#57200=CARTESIAN_POINT ( 'NONE',  ( 0.2461629937395051204, 0.9812432698282257393, -1.641294572782559413 ) ) ;
#57201=CARTESIAN_POINT ( 'NONE',  ( 0.5500180045474002410, 0.9981291480291035745, 1.752136972055001518 ) ) ;
#57204=CARTESIAN_POINT ( 'NONE',  ( 6.533860241792342372, -1.853627334332415888, 0.4695604596292660138 ) ) ;
#57206=CARTESIAN_POINT ( 'NONE',  ( 0.3736316133628528879, 1.073300769168658908, 1.531925686032776124 ) ) ;
#57207=CARTESIAN_POINT ( 'NONE',  ( 1.868375392651611122, -1.978555653031977446, -0.3886301775877995524 ) ) ;
#57211=CARTESIAN_POINT ( 'NONE',  ( 3.774133669461790852, 1.169908569812891264, 1.751025317131530423 ) ) ;
#57216=CARTESIAN_POINT ( 'NONE',  ( 3.814717077619066643, -0.6377016420256261808, -1.916516432535425363 ) ) ;
#57220=CARTESIAN_POINT ( 'NONE',  ( 4.306063477043454490, -2.156128079323017754, 0.1542669963271598166 ) ) ;
#57226=CARTESIAN_POINT ( 'NONE',  ( 1.838563082212365085, -1.162459688571298111, 1.833603174184100792 ) ) ;
#57229=CARTESIAN_POINT ( 'NONE',  ( 1.434833617064284805, -1.334073193498284793, -1.269287082821937362 ) ) ;
#57231=CARTESIAN_POINT ( 'NONE',  ( 3.491892070630482348, -2.189115664112693871, -0.1057334378413293807 ) ) ;
#57233=CARTESIAN_POINT ( 'NONE',  ( 3.678848304420906601, -2.179822953419420006, -0.6058417560294343529 ) ) ;
#57240=CARTESIAN_POINT ( 'NONE',  ( 5.325387591137793919, -1.680293062798293713, 0.5557786991975487423 ) ) ;
#57242=CARTESIAN_POINT ( 'NONE',  ( 1.553890309278640025, 0.6119248022173563450, -2.015079113363055452 ) ) ;
#57245=CARTESIAN_POINT ( 'NONE',  ( 1.064831551406957511, 1.493571888342230203, -1.284017422347245807 ) ) ;
#57248=CARTESIAN_POINT ( 'NONE',  ( 5.783446960131396253, 0.1242560548703756929, -1.807377920737750499 ) ) ;
#57252=CARTESIAN_POINT ( 'NONE',  ( 4.698043743269282757, -1.870269067358639958, -0.04562963166049315705 ) ) ;
#57255=CARTESIAN_POINT ( 'NONE',  ( 4.698136132249701724, 0.8899761679339033282, -1.869364561350304488 ) ) ;
#57265=CARTESIAN_POINT ( 'NONE',  ( 4.000408739481801312, 1.952204270133122810, 0.1946113827649766925 ) ) ;
#57266=CARTESIAN_POINT ( 'NONE',  ( 1.985703663612121472, 1.880146017696176619, 0.7282698753105636413 ) ) ;
#57270=CARTESIAN_POINT ( 'NONE',  ( 1.879943753831798015, -1.004885234286160722, 1.577526331995420472 ) ) ;
#57272=CARTESIAN_POINT ( 'NONE',  ( 4.588143835816930860, 1.162566388618992308, 1.643413508355499708 ) ) ;
#57275=CARTESIAN_POINT ( 'NONE',  ( 2.882529129721671080, -0.6171794022716176054, -2.025259201532733755 ) ) ;
#57278=CARTESIAN_POINT ( 'NONE',  ( 4.527825515032589898, 2.008996319933327612, -0.4998958796476050681 ) ) ;
#57280=CARTESIAN_POINT ( 'NONE',  ( 0.1520488688747126949, 0.8040222321012976403, 1.930173718738151578 ) ) ;
#57281=CARTESIAN_POINT ( 'NONE',  ( 6.387720234973090605, 1.261301916940280154, 1.320039730931761524 ) ) ;
#57288=CARTESIAN_POINT ( 'NONE',  ( 6.041656841763191288, -1.799011877964010520, 0.6487133288125003228 ) ) ;
#57296=CARTESIAN_POINT ( 'NONE',  ( 5.413685477598253470, -1.281375732037979942, -1.556898226837098331 ) ) ;
#57300=CARTESIAN_POINT ( 'NONE',  ( -0.1405533004718494683, 4.096626656942652822, -2.275097870671268563 ) ) ;
#57304=CARTESIAN_POINT ( 'NONE',  ( 2.799605281554286229, -1.456005023894543893, -1.326338995474019011 ) ) ;
#57305=CARTESIAN_POINT ( 'NONE',  ( 3.972279928656559100, -1.994873972748755442, -0.2930500606010341125 ) ) ;
#57307=CARTESIAN_POINT ( 'NONE',  ( 6.727182134110178069, 2.947419669445831669, 2.641212418657997496 ) ) ;
#57308=CARTESIAN_POINT ( 'NONE',  ( 5.208995777154565410, -0.3238732214236837992, 2.167259527466679270 ) ) ;
#57309=CARTESIAN_POINT ( 'NONE',  ( 3.135679483595578798, -1.292546426170533058, -1.428565414989799054 ) ) ;
#57313=CARTESIAN_POINT ( 'NONE',  ( 0.07556134207193675179, -0.004209888911949481380, -2.244269416743961187 ) ) ;
#57318=CARTESIAN_POINT ( 'NONE',  ( 6.269096963164666469, 1.759884223096353173, -0.5412972069449849544 ) ) ;
#57319=CARTESIAN_POINT ( 'NONE',  ( 2.965492324039080252, -1.647071928310759326, -1.157207142784054010 ) ) ;
#57320=CARTESIAN_POINT ( 'NONE',  ( 5.624470717464387093, 0.4563550445067353079, -2.252502686463413006 ) ) ;
#57322=CARTESIAN_POINT ( 'NONE',  ( 3.274093294390582276, -0.9130387472845059582, -1.621452132119176159 ) ) ;
#57328=CARTESIAN_POINT ( 'NONE',  ( 5.917543283689063571, -1.162172991910553010, -1.737764066907695915 ) ) ;
#57334=CARTESIAN_POINT ( 'NONE',  ( 6.252575197229738535, 0.5485693247098271108, 1.635415954441843844 ) ) ;
#57336=CARTESIAN_POINT ( 'NONE',  ( 1.599856272741075447, -0.2119130288822292651, 1.721036989116639493 ) ) ;
#57341=CARTESIAN_POINT ( 'NONE',  ( 6.772352023501587936, -1.015705593385501482, -1.918810339808636023 ) ) ;
#57342=CARTESIAN_POINT ( 'NONE',  ( 5.303274670167754223, 1.494737065598227943, 1.048009559513597866 ) ) ;
#57343=CARTESIAN_POINT ( 'NONE',  ( 2.096468001391890823, 1.939661435718213811, 0.2929505381348077031 ) ) ;
#57346=CARTESIAN_POINT ( 'NONE',  ( 3.686284471605893120, 1.179319764668992576, 1.762089746328721507 ) ) ;
#57351=CARTESIAN_POINT ( 'NONE',  ( 2.325130699016836555, -1.891071737562114219, -0.8429460452448679364 ) ) ;
#57354=CARTESIAN_POINT ( 'NONE',  ( 3.950012332353939559, -1.532167235135332373, -1.608510083909537869 ) ) ;
#57356=CARTESIAN_POINT ( 'NONE',  ( 1.477568294945711180, -2.288151160537778672, -0.2198310841375460678 ) ) ;
#57358=CARTESIAN_POINT ( 'NONE',  ( 0.3737810522974581717, -1.925036204310347943, 0.3769080146646397456 ) ) ;
#57365=CARTESIAN_POINT ( 'NONE',  ( -0.2102771530458277249, 4.081134801423261571, -2.758393064927369576 ) ) ;
#57366=CARTESIAN_POINT ( 'NONE',  ( 2.942113945249478668, 1.711507881387188013, 0.2129122850730424121 ) ) ;
#57367=CARTESIAN_POINT ( 'NONE',  ( 1.850796360583713884, -1.845628094615419768, -0.8128149310912060610 ) ) ;
#57368=CARTESIAN_POINT ( 'NONE',  ( 3.567884397833466892, 2.208229897964437249, -0.4915367949662046154 ) ) ;
#57369=CARTESIAN_POINT ( 'NONE',  ( 5.285806214103678791, 1.413684203821091945, 1.561263235811745309 ) ) ;
#57371=CARTESIAN_POINT ( 'NONE',  ( 3.532247091833766284, 1.725908789131404220, 0.3905704408769093416 ) ) ;
#57373=CARTESIAN_POINT ( 'NONE',  ( 6.321853416579415352, 1.323700039822506280, -1.871417125626378075 ) ) ;
#57374=CARTESIAN_POINT ( 'NONE',  ( 5.507694354943953208, -0.8313836724207699369, -1.642813217252625524 ) ) ;
#57376=CARTESIAN_POINT ( 'NONE',  ( 5.630878078874809844, -1.982435003639994031, 0.9343296635366815650 ) ) ;
#57379=CARTESIAN_POINT ( 'NONE',  ( 5.740704066448026666, -2.019076491677873619, -0.4572469816465085657 ) ) ;
#57380=CARTESIAN_POINT ( 'NONE',  ( 0.02267320670834571672, 0.3494893071277604402, 1.985867805234131644 ) ) ;
#57382=CARTESIAN_POINT ( 'NONE',  ( 4.529859951405730278, -1.186268397688082343, -1.517871513682719886 ) ) ;
#57385=CARTESIAN_POINT ( 'NONE',  ( 1.248599636731639428, 1.089134306475655789, -1.936006665247846481 ) ) ;
#57391=DIRECTION ( 'NONE',  ( 2.949029909160572061E-17, 1.000000000000000000, -8.673600428462616880E-15 ) ) ;
#57394=CARTESIAN_POINT ( 'NONE',  ( 1.504273306027693602, 1.959471947749168663, 0.09963418240711149898 ) ) ;
#57398=CARTESIAN_POINT ( 'NONE',  ( 0.4146024514614836676, 0.7878568475925759040, 1.906473239439598677 ) ) ;
#57401=CARTESIAN_POINT ( 'NONE',  ( 0.6028508490328026159, -0.7652319425662640340, -2.129318446015377120 ) ) ;
#57405=CARTESIAN_POINT ( 'NONE',  ( 1.915107840602244593, -0.2339084544023955492, 1.855816807740391150 ) ) ;
#57406=CARTESIAN_POINT ( 'NONE',  ( 0.2637851986186890429, 1.619078963417280859, -0.6216347861247341067 ) ) ;
#57408=CARTESIAN_POINT ( 'NONE',  ( 3.896163805485418852, -0.6886730243073329039, -2.080591098665984795 ) ) ;
#57409=CARTESIAN_POINT ( 'NONE',  ( 4.823409937486792032, -0.1187154998047341425, 2.304658580708033533 ) ) ;
#57411=CARTESIAN_POINT ( 'NONE',  ( 0.08096513915848214948, -0.1534363407719694927, -2.027498111301667905 ) ) ;
#57412=CARTESIAN_POINT ( 'NONE',  ( 2.660020691486902233, -1.338829530657672073, 1.406886975181226296 ) ) ;
#57417=CARTESIAN_POINT ( 'NONE',  ( 5.273731010124149243, 0.4114677744767555878, -2.080124947408354963 ) ) ;
#57419=CARTESIAN_POINT ( 'NONE',  ( 3.867814693791224112, -0.2004342644464084944, -2.006446243107910199 ) ) ;
#57423=CARTESIAN_POINT ( 'NONE',  ( 0.5217476098421744979, -0.9739702522407606144, -1.544006022310390192 ) ) ;
#57428=CARTESIAN_POINT ( 'NONE',  ( 5.840714686760185792, 0.3996242267790580116, 2.021590886677153254 ) ) ;
#57434=CARTESIAN_POINT ( 'NONE',  ( 4.020179312760450152, -2.014129041962478883, 0.1506293649766801690 ) ) ;
#57435=CARTESIAN_POINT ( 'NONE',  ( 5.303485788544977098, 1.959706058537356910, -1.045853978123905570 ) ) ;
#57440=CARTESIAN_POINT ( 'NONE',  ( 4.698151523293167209, -2.060395484190484794, -0.05257267949314303745 ) ) ;
#57441=CARTESIAN_POINT ( 'NONE',  ( 3.990861413484114273, -2.010826503599131065, 0.1511389102963680842 ) ) ;
#57449=CARTESIAN_POINT ( 'NONE',  ( 3.585314394424500062, 1.281165535658060017, -1.556669873624405120 ) ) ;
#57450=CARTESIAN_POINT ( 'NONE',  ( 2.677489186553200007, -0.9463553590365643142, 1.579155189138586435 ) ) ;
#57453=CARTESIAN_POINT ( 'NONE',  ( 0.9971819109757291688, -0.5654680449962052879, -2.237236815885994989 ) ) ;
#57455=CARTESIAN_POINT ( 'NONE',  ( 3.831458500214664387, -1.998831773244442056, 0.8233788064144487162 ) ) ;
#57457=CARTESIAN_POINT ( 'NONE',  ( 3.339543098909302898, -1.371423271284638590, 1.844254897846734131 ) ) ;
#57460=CARTESIAN_POINT ( 'NONE',  ( 2.588565208901713266, -0.3177388942022137397, -1.843305967786903032 ) ) ;
#57461=CARTESIAN_POINT ( 'NONE',  ( 6.280149219824591178, -1.055055557545642175, 1.665224566959803143 ) ) ;
#57467=CARTESIAN_POINT ( 'NONE',  ( 0.7685542157043163680, 1.090964843879228097, 1.918292034055509632 ) ) ;
#57472=CARTESIAN_POINT ( 'NONE',  ( 6.473508845062264427, 1.886732274579514756, -0.5718055884485659934 ) ) ;
#57474=CARTESIAN_POINT ( 'NONE',  ( 5.988978958577418688, -0.3324729122747641097, -2.283524998171110543 ) ) ;
#57475=CARTESIAN_POINT ( 'NONE',  ( 6.619592957969418379, 0.3166511089685022928, -1.833750044983559535 ) ) ;
#57476=CARTESIAN_POINT ( 'NONE',  ( 3.098538415137185531, 2.046439989356943823, 0.2571918767454490773 ) ) ;
#57483=CARTESIAN_POINT ( 'NONE',  ( 5.248546085168739772, -2.154154806625402596, -0.2710006578958406576 ) ) ;
#57484=CARTESIAN_POINT ( 'NONE',  ( 4.722110844128335039, 1.763445737372179689, 0.5296355584529164329 ) ) ;
#57486=CARTESIAN_POINT ( 'NONE',  ( 6.620655732516649294, 0.5971256128398574337, 1.879834161342401666 ) ) ;
#57487=CARTESIAN_POINT ( 'NONE',  ( 6.515165533258342023, -2.126321577054360201, 0.5302794918828001025 ) ) ;
#57488=CARTESIAN_POINT ( 'NONE',  ( 0.5439545674776785633, 1.865077268347898665, 0.1441030193207945287 ) ) ;
#57489=CARTESIAN_POINT ( 'NONE',  ( 6.737213295527981316, -2.024711933681651477, 1.009942563148768846 ) ) ;
#57495=CARTESIAN_POINT ( 'NONE',  ( 0.2582720099171369466, 1.907150531373353664, 0.1405958444523764117 ) ) ;
#57496=CARTESIAN_POINT ( 'NONE',  ( 1.428175943150990390, 1.704372189200783705, 0.4766478552604267449 ) ) ;
#57498=CARTESIAN_POINT ( 'NONE',  ( 5.988937038716908745, -1.912324646158647168, -0.6291777902352905238 ) ) ;
#57500=CARTESIAN_POINT ( 'NONE',  ( 3.673361179623610084, 1.389826993061950899, 1.318567953439080620 ) ) ;
#57502=CARTESIAN_POINT ( 'NONE',  ( 4.598083368088573764, 0.8440023354334601491, -1.779705283501178181 ) ) ;
#57503=CARTESIAN_POINT ( 'NONE',  ( 6.240491321897984278, 1.159586379754873331, -1.653562141909877603 ) ) ;
#57505=CARTESIAN_POINT ( 'NONE',  ( 2.746779440450992649, -1.556306552617524597, 1.037596984913228937 ) ) ;
#57506=CARTESIAN_POINT ( 'NONE',  ( 5.830603237517035353, 1.664100180626144398, 0.4535787370015566533 ) ) ;
#57508=CARTESIAN_POINT ( 'NONE',  ( 2.754729969050898841, 0.7443088323898851000, 2.077706851784946185 ) ) ;
#57512=CARTESIAN_POINT ( 'NONE',  ( 6.426224708462171087, 1.007414738832881351, 1.683299376423300853 ) ) ;
#57519=CARTESIAN_POINT ( 'NONE',  ( 1.856005582152659317, -0.6995316168164237292, 1.948720873434762080 ) ) ;
#57523=CARTESIAN_POINT ( 'NONE',  ( 0.2584707923105635796, 2.014430608512500775, 0.1461574478831758339 ) ) ;
#57530=CARTESIAN_POINT ( 'NONE',  ( 5.220077296912079667, -1.701688162634030999, -1.080898591909580597 ) ) ;
#57531=CARTESIAN_POINT ( 'NONE',  ( 5.049963001771692106, 0.9498492218114750196, 1.663612537209507858 ) ) ;
#57532=CARTESIAN_POINT ( 'NONE',  ( 6.539320575229274013, 2.055156488754609878, 2.310649141506931681 ) ) ;
#57533=CARTESIAN_POINT ( 'NONE',  ( 2.226364491882920404, 2.126620374013419301, 0.5291077681483095096 ) ) ;
#57535=CARTESIAN_POINT ( 'NONE',  ( 2.742330423940505302, 1.058908597569432120, -1.592262909973440888 ) ) ;
#57538=CARTESIAN_POINT ( 'NONE',  ( 0.08751785467620704084, -0.5350655163729299835, 1.944078888069140865 ) ) ;
#57541=CARTESIAN_POINT ( 'NONE',  ( 5.618738332679400038, -0.05485954975367920983, 2.191026952110195491 ) ) ;
#57543=CARTESIAN_POINT ( 'NONE',  ( 3.592533753846867128, -0.3360022577178176650, -1.691527450499834995 ) ) ;
#57545=CARTESIAN_POINT ( 'NONE',  ( 5.888958097455844864, -2.014202512972632420, -0.6635655960139998921 ) ) ;
#57547=CARTESIAN_POINT ( 'NONE',  ( 0.2034672893990868703, -1.513989045467616146, -1.247398002513319781 ) ) ;
#57550=CARTESIAN_POINT ( 'NONE',  ( 0.1399997263885795762, 1.361443548867202757, -2.255028951473649901 ) ) ;
#57554=CARTESIAN_POINT ( 'NONE',  ( 2.930093016812723050, -0.8946826049299866357, -1.575034454935933859 ) ) ;
#57558=CARTESIAN_POINT ( 'NONE',  ( 3.492628052329676880, -1.746589362535276191, -0.4802254367691183856 ) ) ;
#57562=CARTESIAN_POINT ( 'NONE',  ( 4.756226040108163744, -1.860656195911802646, -0.04637829637440040592 ) ) ;
#57564=CARTESIAN_POINT ( 'NONE',  ( 2.987788816292748173, -1.913300742920095221, 0.09679331860494060080 ) ) ;
#57565=CARTESIAN_POINT ( 'NONE',  ( 1.026062881544724137, 1.091098483296793820, -1.463488004260153907 ) ) ;
#57573=CARTESIAN_POINT ( 'NONE',  ( 5.576995328841173105, 1.818227641914264225, 0.7572995901278417596 ) ) ;
#57575=CARTESIAN_POINT ( 'NONE',  ( 1.078203232848734094, -2.040033308301641757, -0.4564361842656887713 ) ) ;
#57576=CARTESIAN_POINT ( 'NONE',  ( 6.756866522006341746, -1.488468187722398417, 1.222521302487014072 ) ) ;
#57579=CARTESIAN_POINT ( 'NONE',  ( 1.992912282819898850, 1.589903476415389871, -0.8970392876451321884 ) ) ;
#57580=CARTESIAN_POINT ( 'NONE',  ( 3.580891165198408110, -2.126768340858419926, -0.5889919780145411732 ) ) ;
#57582=CARTESIAN_POINT ( 'NONE',  ( 0.9492982845318720386, -1.727743609841876360, 0.8201845251225792222 ) ) ;
#57583=CARTESIAN_POINT ( 'NONE',  ( 2.014047288863869412, 1.964499257916036079, -0.1416769614510370867 ) ) ;
#57584=CARTESIAN_POINT ( 'NONE',  ( 2.349080241353004528, 0.5156090978439072936, -1.872316843566106614 ) ) ;
#57589=CARTESIAN_POINT ( 'NONE',  ( 6.983263157960402090, -0.0002233252893329463486, 1.845923184817334084 ) ) ;
#57594=CARTESIAN_POINT ( 'NONE',  ( 2.525153347276567484, -2.043736813514348771, 0.7916865192442237298 ) ) ;
#57597=CARTESIAN_POINT ( 'NONE',  ( 2.965264444195826243, 0.2674972279559268973, -1.805858685475017378 ) ) ;
#57603=CARTESIAN_POINT ( 'NONE',  ( 2.314956460678399885, 1.720770591318865339, 0.8663633404912238767 ) ) ;
#57614=CARTESIAN_POINT ( 'NONE',  ( 5.243061650278370678, -0.2479348644398685908, -2.055265572831247667 ) ) ;
#57615=CARTESIAN_POINT ( 'NONE',  ( 0.2043192855987647494, 1.601443664334546213, 0.9084302959305108338 ) ) ;
#57618=CARTESIAN_POINT ( 'NONE',  ( 5.291695567192507887, 1.742433043099327561, -1.499359156687163575 ) ) ;
#57622=CARTESIAN_POINT ( 'NONE',  ( 6.585440809757122871, -0.9837151097084917417, 2.068200907652519405 ) ) ;
#57625=CARTESIAN_POINT ( 'NONE',  ( 4.435450497376713486, 0.8291751068889623433, -1.756158939159500276 ) ) ;
#57629=CARTESIAN_POINT ( 'NONE',  ( -0.1052096654315381741, -1.953846233167291002, -0.4849948655165080558 ) ) ;
#57630=CARTESIAN_POINT ( 'NONE',  ( 0.09967489844521590370, -1.724374414367945141, -0.04833993824084405894 ) ) ;
#57631=CARTESIAN_POINT ( 'NONE',  ( 6.051970301643104122, 1.040788372175960541, 1.727066800951609027 ) ) ;
#57635=CARTESIAN_POINT ( 'NONE',  ( 2.273483640244071680, 1.287084957891961423, 1.647379119656503965 ) ) ;
#57636=CARTESIAN_POINT ( 'NONE',  ( 1.094210320218844679, -0.4249228298987791086, -1.717946482988210510 ) ) ;
#57638=CARTESIAN_POINT ( 'NONE',  ( 4.066585926679040064, -2.138228679320841152, -0.8265488639036464580 ) ) ;
#57639=CARTESIAN_POINT ( 'NONE',  ( 2.589492015636893907, -1.735658606974595619, -0.1281804514613407997 ) ) ;
#57642=CARTESIAN_POINT ( 'NONE',  ( 1.756802591741468245, -1.724947740463366852, -0.1754148046573481556 ) ) ;
#57644=CARTESIAN_POINT ( 'NONE',  ( 2.084208510888691190, 1.074786400414856624, -1.519112143004421434 ) ) ;
#57645=CARTESIAN_POINT ( 'NONE',  ( 2.277988012537075502, -2.106425727361205702, 0.5258826003073436839 ) ) ;
#57647=CARTESIAN_POINT ( 'NONE',  ( 3.766814776335784209, -0.2024620155892907503, -2.006371719556559796 ) ) ;
#57648=CARTESIAN_POINT ( 'NONE',  ( 2.875000000000002220, 2.052068128417948056, -1.638482584539516883E-13 ) ) ;
#57651=CARTESIAN_POINT ( 'NONE',  ( 1.184454412485607344, -1.878822398200689525, -0.4247803175085519412 ) ) ;
#57653=CARTESIAN_POINT ( 'NONE',  ( 4.728890529236228879, 1.530954898644999451, -1.609847601234422276 ) ) ;
#57660=CARTESIAN_POINT ( 'NONE',  ( 5.976846119194893170, -1.571437351877506439, 1.570356403719268101 ) ) ;
#57662=CARTESIAN_POINT ( 'NONE',  ( 4.773855682050706761, -1.924389145058275963, 0.3807478752155256663 ) ) ;
#57664=CARTESIAN_POINT ( 'NONE',  ( 5.501357770389488699, 1.845074063491736860, 1.309031944507930589 ) ) ;
#57666=CARTESIAN_POINT ( 'NONE',  ( 2.805193546069509214, -1.716336894061726737, 1.143758443631032407 ) ) ;
#57671=CARTESIAN_POINT ( 'NONE',  ( 5.096879011283717453, 1.555924861325823416, -1.037969726935553005 ) ) ;
#57672=CARTESIAN_POINT ( 'NONE',  ( 3.322662972295143291, 0.7760272377477626105, -1.550874960589002871 ) ) ;
#57673=CARTESIAN_POINT ( 'NONE',  ( 2.788295088316892656, 1.491546084125561888, -0.8966509355741271170 ) ) ;
#57674=CARTESIAN_POINT ( 'NONE',  ( 0.6973257247198815234, 1.878305535369644064, 1.313909787900492843 ) ) ;
#57675=CARTESIAN_POINT ( 'NONE',  ( 0.5873203293235219613, -0.2722241568871349160, -2.189838084831654541 ) ) ;
#57676=CARTESIAN_POINT ( 'NONE',  ( 4.810148555269133652, 1.440736570533694527, -1.515338330687252988 ) ) ;
#57677=CARTESIAN_POINT ( 'NONE',  ( 5.138593782488270811, -1.664572445771801634, 0.9999684565626990596 ) ) ;
#57681=EDGE_LOOP ( 'NONE', ( #145116, #116094, #143253, #159848 ) ) ;
#57682=CARTESIAN_POINT ( 'NONE',  ( 0.2467204944939948574, 1.994070950632735428, -0.2986300710981006357 ) ) ;
#57683=CARTESIAN_POINT ( 'NONE',  ( -0.1753031400193918732, -0.9122597987226389593, -1.912455998546586544 ) ) ;
#57687=CARTESIAN_POINT ( 'NONE',  ( 3.914527900857078357, 1.289819402409349669, -1.292354223553587644 ) ) ;
#57688=CARTESIAN_POINT ( 'NONE',  ( 2.063769564651289912, 0.3772465526380370804, -2.174136642525636098 ) ) ;
#57694=CARTESIAN_POINT ( 'NONE',  ( 1.424088383587719386, -2.004042310577313302, 0.2513328237187910652 ) ) ;
#57696=CARTESIAN_POINT ( 'NONE',  ( 3.485049009367678252, 0.04119252264746588871, 1.860649646085434039 ) ) ;
#57702=CARTESIAN_POINT ( 'NONE',  ( 5.356004772612798170, 1.823420152956479523, -0.09349780940721279243 ) ) ;
#57706=CARTESIAN_POINT ( 'NONE',  ( 0.3152591496230552348, -1.397726865852641387, 1.025726801146044531 ) ) ;
#57707=CARTESIAN_POINT ( 'NONE',  ( 6.597600327481837112, -1.840612352326329804, 0.05063316525460298534 ) ) ;
#57708=CARTESIAN_POINT ( 'NONE',  ( 4.301628547034565209, 1.852045629758605649, 1.376555262909467947 ) ) ;
#57710=CARTESIAN_POINT ( 'NONE',  ( 0.5794586325245559832, 1.923780613697351427, -0.7393501692522960189 ) ) ;
#57712=CARTESIAN_POINT ( 'NONE',  ( 6.046309306592402955, 2.127046199546629435, -0.8712367593181246095 ) ) ;
#57715=CARTESIAN_POINT ( 'NONE',  ( 5.664887262500884368, -1.691755685069219695, -0.7986314380193232365 ) ) ;
#57716=EDGE_LOOP ( 'NONE', ( #98343, #125560, #42423, #32241 ) ) ;
#57717=CARTESIAN_POINT ( 'NONE',  ( 2.443496805918866865, -1.782974011999260977, 0.6919810379762069141 ) ) ;
#57720=CARTESIAN_POINT ( 'NONE',  ( 5.127635347277352373, -2.096377701570474539, 0.6897739467496829535 ) ) ;
#57721=CARTESIAN_POINT ( 'NONE',  ( 4.259064461820570635, -0.003692207519963904699, -2.117513409117043999 ) ) ;
#57727=CARTESIAN_POINT ( 'NONE',  ( 1.835461723582560767, 0.2275736305563350881, 2.296322244814374081 ) ) ;
#57728=CARTESIAN_POINT ( 'NONE',  ( 3.262109210011232108, -1.959739898415867154, 0.09363895518171151677 ) ) ;
#57730=CARTESIAN_POINT ( 'NONE',  ( 6.227400143195995774, 0.1575970216860186346, -2.056636196940288652 ) ) ;
#57734=CARTESIAN_POINT ( 'NONE',  ( 5.770720322323381168, -0.3006437417610394736, -1.993894057904864514 ) ) ;
#57737=CARTESIAN_POINT ( 'NONE',  ( 1.551893958816989993, 1.642325835523240629, 1.420010234424383455 ) ) ;
#57743=CARTESIAN_POINT ( 'NONE',  ( 0.7376602057446514094, -1.455437688833590926, -1.459210590049898171 ) ) ;
#57745=CARTESIAN_POINT ( 'NONE',  ( 6.727182134110209155, 1.290711256955964448, 1.927001067762003972 ) ) ;
#57749=CARTESIAN_POINT ( 'NONE',  ( 3.404848115249804685, -0.3755933644018424888, -1.874856250562627391 ) ) ;
#57750=CARTESIAN_POINT ( 'NONE',  ( 5.576936095668227900, -0.04655786065462656775, -1.769397458738901197 ) ) ;
#57754=CARTESIAN_POINT ( 'NONE',  ( 6.603150280507321668, -0.1401627607961895561, 1.883980500587930429 ) ) ;
#57756=CARTESIAN_POINT ( 'NONE',  ( 0.6607010325807397555, -0.6960017893198193750, -1.950014918625786020 ) ) ;
#57758=CARTESIAN_POINT ( 'NONE',  ( 5.858239598252557911, 0.7595784280203803362, 1.709674162104061645 ) ) ;
#57759=CARTESIAN_POINT ( 'NONE',  ( 2.648829494986388422, -1.517897411861212076, 1.014145048410304284 ) ) ;
#57760=CARTESIAN_POINT ( 'NONE',  ( 5.988949835885216011, -0.3198878037087344306, -2.183464699167809275 ) ) ;
#57763=CARTESIAN_POINT ( 'NONE',  ( 2.822777196768213592, -1.424206252425799679, 1.492280444834346520 ) ) ;
#57767=CARTESIAN_POINT ( 'NONE',  ( 0.6148119136215323133, 1.491057340773978446, -1.565211586912764963 ) ) ;
#57769=CARTESIAN_POINT ( 'NONE',  ( 5.723117673755029777, -1.870111591731966616, -0.8886290660751752224 ) ) ;
#57771=CARTESIAN_POINT ( 'NONE',  ( 3.655696586050953378, 0.5291108212043382775, -2.095698868369605616 ) ) ;
#57773=CARTESIAN_POINT ( 'NONE',  ( 3.141275609595588492, 0.05172059693002092201, 2.019191109193402056 ) ) ;
#57774=CARTESIAN_POINT ( 'NONE',  ( 2.224987305166142626, -1.792472147789250236, -0.7979012372742313453 ) ) ;
#57779=CARTESIAN_POINT ( 'NONE',  ( 2.940638933469359895, -1.523795050681177710, 1.320827213682006285 ) ) ;
#57783=CARTESIAN_POINT ( 'NONE',  ( 6.275647926998928483, 0.3200337115364470519, -1.885262484646981873 ) ) ;
#57787=CARTESIAN_POINT ( 'NONE',  ( 3.726185550002871771, 2.006962945745351945, 0.1948219989877792990 ) ) ;
#57790=CARTESIAN_POINT ( 'NONE',  ( 5.877914075457827181, 1.031193140389017548, 1.382412309478407542 ) ) ;
#57794=CARTESIAN_POINT ( 'NONE',  ( 4.868341698904518289, -1.223052743625025141, 1.415352931214426846 ) ) ;
#57797=CARTESIAN_POINT ( 'NONE',  ( 2.659107809384615884, 1.665393510391148801, -1.229642267604726058 ) ) ;
#57802=CARTESIAN_POINT ( 'NONE',  ( 0.3163054335677130680, -0.6107064426322272865, -1.705642966030767260 ) ) ;
#57808=CARTESIAN_POINT ( 'NONE',  ( 5.571877068885287443, -0.8567909204831600789, 1.713377365699362054 ) ) ;
#57811=VERTEX_POINT ( 'NONE', #85193 ) ;
#57814=CARTESIAN_POINT ( 'NONE',  ( 3.028364643526501698, 1.202066397148596977, -1.796461956351296019 ) ) ;
#57817=CARTESIAN_POINT ( 'NONE',  ( -0.05226516427493665962, -1.936187138999283297, 0.8653993394739032397 ) ) ;
#57818=CARTESIAN_POINT ( 'NONE',  ( 5.315394819225006451, -0.2661953434012730435, 1.805952802178517613 ) ) ;
#57820=CARTESIAN_POINT ( 'NONE',  ( 1.159376733683295191, 0.3886980088604417016, -1.932498344103703136 ) ) ;
#57821=CARTESIAN_POINT ( 'NONE',  ( 3.498220628606643956, -0.9384276995785534314, 1.666209768436441419 ) ) ;
#57824=CARTESIAN_POINT ( 'NONE',  ( 4.949637397294944563, 1.457986120030363431, 1.324331637980098675 ) ) ;
#57826=CARTESIAN_POINT ( 'NONE',  ( 6.128462272945822242, 0.1949450651400796986, 1.932269955005933904 ) ) ;
#57832=CARTESIAN_POINT ( 'NONE',  ( 4.143145976665215002, 0.09703654569752531711, 1.909951782607082427 ) ) ;
#57833=VERTEX_POINT ( 'NONE', #131861 ) ;
#57834=CARTESIAN_POINT ( 'NONE',  ( 0.6400319944965120467, -1.562016764346199960, -1.559085968200937478 ) ) ;
#57836=CARTESIAN_POINT ( 'NONE',  ( 6.445953599032193004, -1.316566896158730238, -1.522954124987923930 ) ) ;
#57839=CARTESIAN_POINT ( 'NONE',  ( 1.662640112210824306, -0.7432673875312335587, -1.932532381715674097 ) ) ;
#57850=CARTESIAN_POINT ( 'NONE',  ( 6.825078400183592464, 1.263193418084729958, 2.069194724180785538 ) ) ;
#57853=CARTESIAN_POINT ( 'NONE',  ( 5.238767818816652877, 1.731821575490007703, -0.09270464131736801117 ) ) ;
#57855=CARTESIAN_POINT ( 'NONE',  ( 1.903268718874175480, -1.751121435885591548, 1.104011288380807532 ) ) ;
#57856=CARTESIAN_POINT ( 'NONE',  ( 3.198929712650464996, 1.915108447241938627, 0.9030302060772307238 ) ) ;
#57859=CARTESIAN_POINT ( 'NONE',  ( 1.498812192398508270, 0.3789717401675870567, 1.932455098789982895 ) ) ;
#57863=CARTESIAN_POINT ( 'NONE',  ( 3.644716121489647076, -1.874467426877159504, 1.319156965210349197 ) ) ;
#57864=CARTESIAN_POINT ( 'NONE',  ( 2.174178736149934732, -1.123764393468742906, 1.438770255985911684 ) ) ;
#57868=CARTESIAN_POINT ( 'NONE',  ( 2.408449855729302591, -2.008082631278225616, -0.1440398445633188362 ) ) ;
#57869=CARTESIAN_POINT ( 'NONE',  ( 3.379693149055284174, -1.891888713350448947, 0.5187481205842571219 ) ) ;
#57873=CARTESIAN_POINT ( 'NONE',  ( 0.07516593201273635838, 0.2333279341363985182, -2.077802470623245856 ) ) ;
#57874=CARTESIAN_POINT ( 'NONE',  ( 6.632766914392992597, -1.868179159523954302, 0.9385789683672930428 ) ) ;
#57875=CARTESIAN_POINT ( 'NONE',  ( 4.680378828550276538, -1.717002404052007325, -0.4286406472287905278 ) ) ;
#57877=CARTESIAN_POINT ( 'NONE',  ( 1.271705539736139423, 1.307743536042236920, 1.758333696453084016 ) ) ;
#57878=CARTESIAN_POINT ( 'NONE',  ( 5.964775352603689740, 0.1210227373375266924, -1.736196924002187947 ) ) ;
#57881=CARTESIAN_POINT ( 'NONE',  ( 0.1757712021154093640, -0.9832847084251387093, -2.074436467499872094 ) ) ;
#57882=CARTESIAN_POINT ( 'NONE',  ( 0.1333692844072559280, 0.001398348041498076455, -2.053671342968105051 ) ) ;
#57883=CARTESIAN_POINT ( 'NONE',  ( 5.114428339645875177, 0.5428861372157275378, -1.646692512460482982 ) ) ;
#57884=CARTESIAN_POINT ( 'NONE',  ( 5.793482113768906316, -1.965262051535413335, 0.9231745368859373135 ) ) ;
#57886=CARTESIAN_POINT ( 'NONE',  ( 0.4447203898077173312, -1.529029696559053741, 1.464872618488068490 ) ) ;
#57887=CARTESIAN_POINT ( 'NONE',  ( 3.062500000000001776, -1.451031289061242013, -1.451031289060994656 ) ) ;
#57888=CARTESIAN_POINT ( 'NONE',  ( 6.827182134110196365, 7.629137130509086262, 2.689055895399253160 ) ) ;
#57889=CARTESIAN_POINT ( 'NONE',  ( 4.383760159432283032, 1.257691660000469058, 1.459273733648867699 ) ) ;
#57891=CARTESIAN_POINT ( 'NONE',  ( 1.383751715516433833, 0.1588885597470449385, -2.215665637441687430 ) ) ;
#57896=CARTESIAN_POINT ( 'NONE',  ( 2.895431823567701457, -0.1657752626464791268, -2.215182847160178881 ) ) ;
#57902=CARTESIAN_POINT ( 'NONE',  ( 1.090470458312575053, -0.4872005951904456733, 1.956561897242928172 ) ) ;
#57904=CARTESIAN_POINT ( 'NONE',  ( 0.4794367124230074495, -0.1050040150484717050, 2.060039547518006664 ) ) ;
#57909=CARTESIAN_POINT ( 'NONE',  ( 1.071160155259534674, 1.707552549077664183, -0.4648152392626672680 ) ) ;
#57910=CARTESIAN_POINT ( 'NONE',  ( 0.6861729220449981348, 1.650083401500940239, 1.158686392676591570 ) ) ;
#57911=CARTESIAN_POINT ( 'NONE',  ( 0.2043192855987647494, 1.601443664334546213, 0.9084302959305108338 ) ) ;
#57912=CARTESIAN_POINT ( 'NONE',  ( 3.843561273245421628, 0.7716866907857397040, -2.158722107141448188 ) ) ;
#57914=CARTESIAN_POINT ( 'NONE',  ( 1.991909005812149358, -0.4902695928585449892, -1.774584731258487036 ) ) ;
#57918=CARTESIAN_POINT ( 'NONE',  ( 3.030095697178539549, 1.015519584536026976, -1.516846343748608605 ) ) ;
#57919=CARTESIAN_POINT ( 'NONE',  ( 4.166638809851969327, 1.319227567334404494, 1.525044649537968589 ) ) ;
#57921=CARTESIAN_POINT ( 'NONE',  ( 3.151526295007577527, -1.848778841746369972, -1.303968314058404854 ) ) ;
#57923=CARTESIAN_POINT ( 'NONE',  ( 5.086996280900090817, -0.2547426189827053378, -2.090417274992136587 ) ) ;
#57925=CARTESIAN_POINT ( 'NONE',  ( 2.857943571468853250, -0.6518772230660694333, 1.965110387975615991 ) ) ;
#57928=CARTESIAN_POINT ( 'NONE',  ( 5.057343377742961721, -1.818460011135439869, 1.090507627184752693 ) ) ;
#57931=CARTESIAN_POINT ( 'NONE',  ( 0.7153026426200872478, -0.2839029868492106701, 1.905349893463634814 ) ) ;
#57938=CARTESIAN_POINT ( 'NONE',  ( 0.4752230700786713169, -1.603524673181003779, 1.537559121520514660 ) ) ;
#57939=CARTESIAN_POINT ( 'NONE',  ( 2.555815334374893943, 0.5629295958425766244, -2.029244372067032565 ) ) ;
#57942=CARTESIAN_POINT ( 'NONE',  ( 6.367989434593707365, -1.846973275860162467, 0.2267098040239327594 ) ) ;
#57947=CARTESIAN_POINT ( 'NONE',  ( -0.2046613956954954905, -0.1581703332043625232, -2.086340352340488646 ) ) ;
#57950=CARTESIAN_POINT ( 'NONE',  ( 3.578520225191741844, 1.246510459297203610, -1.514941731618473009 ) ) ;
#57951=CARTESIAN_POINT ( 'NONE',  ( 1.833122199354455972, 0.2117775504973731793, 2.151289291301178075 ) ) ;
#57955=CARTESIAN_POINT ( 'NONE',  ( 3.064111502348449978, -1.608305157344312564, -0.6653965878143754953 ) ) ;
#57958=AXIS2_PLACEMENT_3D ( 'NONE', #40432, #191976, #108683 ) ;
#57960=CARTESIAN_POINT ( 'NONE',  ( 2.143907462275076892, -0.09611812122205246056, -2.013924455302518624 ) ) ;
#57961=CARTESIAN_POINT ( 'NONE',  ( 6.825078400183572036, 7.629137130509069387, 2.744348168701661095 ) ) ;
#57963=CARTESIAN_POINT ( 'NONE',  ( 2.026188796938654946, 1.136581424768828397, -1.610674104117129302 ) ) ;
#57971=CARTESIAN_POINT ( 'NONE',  ( 2.631515421131935817, -0.1955963300145530936, 2.010161875231412765 ) ) ;
#57973=ADVANCED_FACE ( 'NONE', ( #199996 ), #32157, .T. ) ;
#57974=CARTESIAN_POINT ( 'NONE',  ( 5.385860071389879877, 1.544758419828775153, 1.714431625121175751 ) ) ;
#57975=CARTESIAN_POINT ( 'NONE',  ( 6.883263157960391787, -0.001104538646235289417, 1.946037152736757925 ) ) ;
#57976=CARTESIAN_POINT ( 'NONE',  ( 2.500770564479499303, 0.4249116886347775179, 1.915039037836663738 ) ) ;
#57978=CARTESIAN_POINT ( 'NONE',  ( 0.9146856577476671912, -1.281363086869342194, -1.556907195799726917 ) ) ;
#57980=CARTESIAN_POINT ( 'NONE',  ( 2.061849949441786123, 1.306762352624482038, 1.665877332585569803 ) ) ;
#57983=CARTESIAN_POINT ( 'NONE',  ( 2.114959233223293822, -1.785989328681826027, 0.4467204754193611627 ) ) ;
#57987=CARTESIAN_POINT ( 'NONE',  ( 2.865608904542978674, -1.736054085904148669, -1.217558864107195715 ) ) ;
#57988=CARTESIAN_POINT ( 'NONE',  ( 0.4273693582952375891, 0.9489586001507933632, -1.577591209259328275 ) ) ;
#57992=CARTESIAN_POINT ( 'NONE',  ( 4.270816029187285423, -1.921422972303673093, -0.7454010919232464394 ) ) ;
#57994=CARTESIAN_POINT ( 'NONE',  ( 1.364538772237647413, 0.1349417713633893900, -1.836341338755695940 ) ) ;
#57998=CARTESIAN_POINT ( 'NONE',  ( 1.260703874955213744, 0.8971468365699288849, 2.016480257658866737 ) ) ;
#57999=CARTESIAN_POINT ( 'NONE',  ( 3.497619258099498030, 1.781045823846095111, 1.394991416339389501 ) ) ;
#58001=CARTESIAN_POINT ( 'NONE',  ( 3.691515636560299463, 1.703854809669336001, -0.6157217382992925536 ) ) ;
#58002=CARTESIAN_POINT ( 'NONE',  ( 3.028439059693835311, 0.4704065786719989761, 1.856910451861475631 ) ) ;
#58003=CARTESIAN_POINT ( 'NONE',  ( 3.947765587739564097, 1.497496809916948779, 1.429883829622953462 ) ) ;
#58005=CARTESIAN_POINT ( 'NONE',  ( 2.518385046665332361, 1.288922565979855994, -1.491834565112426070 ) ) ;
#58006=CARTESIAN_POINT ( 'NONE',  ( 0.8680396935916842027, 0.9469273490957976769, 1.677514697326354387 ) ) ;
#58007=CARTESIAN_POINT ( 'NONE',  ( 3.467518583331068438, 1.825290416974333807, -0.4087457676540603990 ) ) ;
#58008=CARTESIAN_POINT ( 'NONE',  ( 2.227567673948157800, 0.002208658356158287820, 2.307868969919598889 ) ) ;
#58009=CARTESIAN_POINT ( 'NONE',  ( 3.578407426278474190, 1.182412371022481645, -1.437126236693661241 ) ) ;
#58015=CARTESIAN_POINT ( 'NONE',  ( 0.2937649352797070401, 1.562083697590540998, 1.412785709394439815 ) ) ;
#58019=CARTESIAN_POINT ( 'NONE',  ( 6.784453917077649443, -2.118420112955111456, -0.4290502581522498415 ) ) ;
#58020=CARTESIAN_POINT ( 'NONE',  ( 1.600013431492643745, 1.466117565985028515, 1.532352819790145482 ) ) ;
#58021=CARTESIAN_POINT ( 'NONE',  ( 0.2639333133152200750, 0.6296502125625064172, -1.919233096100453118 ) ) ;
#58025=CARTESIAN_POINT ( 'NONE',  ( 1.388190569347878212, -0.9732202972718406730, 1.930209198840258100 ) ) ;
#58027=CARTESIAN_POINT ( 'NONE',  ( 6.925078400183553029, 0.5781763343528348864, 2.007479843201316783 ) ) ;
#58030=CARTESIAN_POINT ( 'NONE',  ( 5.331267653506235327, -1.592659417495114083, -1.236803018183525449 ) ) ;
#58034=CARTESIAN_POINT ( 'NONE',  ( 0.4798239446817476606, 2.109833986122396254, -0.8175194613929820386 ) ) ;
#58038=CARTESIAN_POINT ( 'NONE',  ( 0.01699859406821546334, -1.751214827781864436, 0.7768474416505846136 ) ) ;
#58042=CARTESIAN_POINT ( 'NONE',  ( 3.422183312176851455, 1.093272757541150719, -1.334144266598129791 ) ) ;
#58045=CARTESIAN_POINT ( 'NONE',  ( 1.405125766016354305, -0.4367768486257683769, 1.714848201936822525 ) ) ;
#58046=CARTESIAN_POINT ( 'NONE',  ( 1.576815760046655912, -1.422047136828644476, 1.425140908648862448 ) ) ;
#58048=CARTESIAN_POINT ( 'NONE',  ( 4.243358471946375943, -1.921622210924242458, 1.084848892642875429 ) ) ;
#58052=CARTESIAN_POINT ( 'NONE',  ( 4.389387035479824561, -0.001039498178659337352, -2.120667954306009406 ) ) ;
#58053=CARTESIAN_POINT ( 'NONE',  ( 2.987907820627898392, -2.013986125068282007, 0.1017690403029153784 ) ) ;
#58054=CARTESIAN_POINT ( 'NONE',  ( 3.181707836761258790, 1.766318828868058910, -0.4016052188219875752 ) ) ;
#58058=CARTESIAN_POINT ( 'NONE',  ( 1.727212824277712944, -1.762453432929488528, 0.6273722324065673650 ) ) ;
#58060=CARTESIAN_POINT ( 'NONE',  ( 6.340460056601358474, 1.806591233369018834, 0.2625940548972791611 ) ) ;
#58062=CARTESIAN_POINT ( 'NONE',  ( 2.360426208626884570, -1.834515764125169257, -0.5519355525325749801 ) ) ;
#58072=CARTESIAN_POINT ( 'NONE',  ( 4.588201236890728119, 1.223260742344203900, 1.732012071221388450 ) ) ;
#58074=CARTESIAN_POINT ( 'NONE',  ( -0.1296875068448159474, 0.7431874094961619104, -1.910093690679348200 ) ) ;
#58076=CARTESIAN_POINT ( 'NONE',  ( 3.901606001822624403, -0.5752225463674947026, 1.885544661340606165 ) ) ;
#58077=CARTESIAN_POINT ( 'NONE',  ( 0.2639318008525155523, 0.6274397771241714272, -1.913028341257965170 ) ) ;
#58079=CARTESIAN_POINT ( 'NONE',  ( 0.3865160979802947927, -0.7177084582802439883, -1.991989965223327275 ) ) ;
#58081=CARTESIAN_POINT ( 'NONE',  ( 1.311079954825690619, -1.633285661836245906, 1.272233187909928454 ) ) ;
#58086=CARTESIAN_POINT ( 'NONE',  ( 3.943374907373353278, 0.7044166278388838132, -1.968527102906494575 ) ) ;
#58089=CARTESIAN_POINT ( 'NONE',  ( 2.379681254797087586, 1.121034037677430595, 1.440765146680768272 ) ) ;
#58090=CARTESIAN_POINT ( 'NONE',  ( 0.7678511737040129015, 1.809490520450097284, -0.08760732307166485544 ) ) ;
#58092=CARTESIAN_POINT ( 'NONE',  ( 5.883472226557854512, 2.040502603023553796, -0.8411249186189363458 ) ) ;
#58094=CARTESIAN_POINT ( 'NONE',  ( 3.803933094734159415, -0.6430795383850876901, 2.110982628114480786 ) ) ;
#58097=CARTESIAN_POINT ( 'NONE',  ( 2.666550042863625958, 0.6461651886627232111, 1.799920402468312197 ) ) ;
#58101=CARTESIAN_POINT ( 'NONE',  ( 5.301260566756325510, -1.777534899005998481, 1.061244097098137829 ) ) ;
#58103=CARTESIAN_POINT ( 'NONE',  ( 2.501032641837992454, 1.736685530831501456, -1.287010829427559289 ) ) ;
#58104=CARTESIAN_POINT ( 'NONE',  ( 5.847271748948593029, 0.6375361197438635941, -2.096799129279611762 ) ) ;
#58115=CARTESIAN_POINT ( 'NONE',  ( 6.086797785588474063, 1.993605056338519699, 0.5577928598018768724 ) ) ;
#58116=CARTESIAN_POINT ( 'NONE',  ( 4.512281715141372551, -0.8252044610495885557, -1.740951444232276657 ) ) ;
#58117=CARTESIAN_POINT ( 'NONE',  ( 6.450787963126683344, -1.935726721829626351, -0.8580517621625349811 ) ) ;
#58121=CARTESIAN_POINT ( 'NONE',  ( 0.2874129202556953144, 1.626693421326959710, 1.468627725614686463 ) ) ;
#58122=CARTESIAN_POINT ( 'NONE',  ( 5.039593146249601752, -1.293522693445445793, -1.288650932716684627 ) ) ;
#58129=CARTESIAN_POINT ( 'NONE',  ( 2.190726087351921425, 1.424366561657765207, 1.166803476217087576 ) ) ;
#58130=CARTESIAN_POINT ( 'NONE',  ( 6.381113974719265336, -1.842344568942927419, -0.8120077521172417434 ) ) ;
#58131=CARTESIAN_POINT ( 'NONE',  ( 0.7030180566853957425, -1.627119059678893587, -1.623510667393740725 ) ) ;
#58132=CARTESIAN_POINT ( 'NONE',  ( 6.315287901512626867, -1.680818388338392699, -1.011408691396285420 ) ) ;
#58136=CARTESIAN_POINT ( 'NONE',  ( 0.5903903138861701372, 1.065687334306382184, -1.774900233272216798 ) ) ;
#58138=CARTESIAN_POINT ( 'NONE',  ( 2.331682703721962291, 0.9828498176551370147, -1.845303212725694975 ) ) ;
#58139=CARTESIAN_POINT ( 'NONE',  ( 1.410794581852807150, 1.648159533202856686, 0.8848386531258023435 ) ) ;
#58140=CARTESIAN_POINT ( 'NONE',  ( 1.546249734355091388, 1.863884247081739609, -0.7690006294575402190 ) ) ;
#58144=CARTESIAN_POINT ( 'NONE',  ( 2.454330514505886018, -1.515118085899306521, -0.8562798468515414596 ) ) ;
#58149=CARTESIAN_POINT ( 'NONE',  ( 2.842114037233371082, 1.711851238368550909, 0.2109339381748502329 ) ) ;
#58150=CARTESIAN_POINT ( 'NONE',  ( 3.228257827484398490, 2.138632370135685523, 0.4780590757816546854 ) ) ;
#58151=CARTESIAN_POINT ( 'NONE',  ( 4.987059637548557411, -0.2676712469649074055, -2.190530366034774801 ) ) ;
#58153=CARTESIAN_POINT ( 'NONE',  ( 2.290094988384860919, -1.415387839477784571, -1.646397135256922661 ) ) ;
#58154=CARTESIAN_POINT ( 'NONE',  ( 1.224926655537651676, -0.04696546880481740349, 1.825250005322680780 ) ) ;
#58155=CARTESIAN_POINT ( 'NONE',  ( 3.714152660773429648, 1.129254856714853261, -1.790882643308453703 ) ) ;
#58156=CARTESIAN_POINT ( 'NONE',  ( 6.539320575229292665, 7.052829955583200139, 2.594893642179775028 ) ) ;
#58159=CARTESIAN_POINT ( 'NONE',  ( 4.054423531099146771, -1.698574802010197837, 1.539571537138052948 ) ) ;
#58163=CARTESIAN_POINT ( 'NONE',  ( 6.568989397875739655, -1.719265429537725431, 1.406094356362475706 ) ) ;
#58169=CARTESIAN_POINT ( 'NONE',  ( 4.658827374183164949, 1.163267680695536876, 1.646840100852072997 ) ) ;
#58171=CARTESIAN_POINT ( 'NONE',  ( 3.274340622259350742, -1.012630945124261661, -1.796778529651460898 ) ) ;
#58175=CARTESIAN_POINT ( 'NONE',  ( 6.298795234281088895, 1.819837665574381091, 1.220625243075368127 ) ) ;
#58176=CARTESIAN_POINT ( 'NONE',  ( 3.322888845334175389, 0.9041102021897020613, -1.802417075407992897 ) ) ;
#58177=CARTESIAN_POINT ( 'NONE',  ( 3.667381569930192597, 1.025862638139760419, 1.528780434079744843 ) ) ;
#58181=CARTESIAN_POINT ( 'NONE',  ( 6.686557121163758666, -1.791048715316777562, -0.3524728914669760793 ) ) ;
#58182=CARTESIAN_POINT ( 'NONE',  ( -0.06910031042392690559, -1.782763753708914267, -1.450585907311294775 ) ) ;
#58184=CARTESIAN_POINT ( 'NONE',  ( 6.631690487938540102, -1.471565961622269381, -1.718669407966398666 ) ) ;
#58185=CARTESIAN_POINT ( 'NONE',  ( 2.016375119164611984, -0.9936656701176631579, -1.856918979450744578 ) ) ;
#58194=CARTESIAN_POINT ( 'NONE',  ( 2.391022662813433453, -2.030629854096975606, -0.6112283555373964061 ) ) ;
#58195=CARTESIAN_POINT ( 'NONE',  ( 3.832468605949594043, -1.144296635937601669, -1.903904886208422909 ) ) ;
#58196=CARTESIAN_POINT ( 'NONE',  ( 1.588088344156918907, -2.181139600106785092, -0.2122876309011075546 ) ) ;
#58197=CARTESIAN_POINT ( 'NONE',  ( 0.4170028235400899397, 1.518763190251697370, -1.601383572969114599 ) ) ;
#58199=CARTESIAN_POINT ( 'NONE',  ( 4.141029529442549872, -0.1900441490861082827, -1.952618137025011746 ) ) ;
#58203=CARTESIAN_POINT ( 'NONE',  ( 6.610000000000037623, 2.481806704560181043, 2.105257736569548399 ) ) ;
#58207=CARTESIAN_POINT ( 'NONE',  ( 3.762070191281779774, 0.7111978290502696254, -1.997938288694045550 ) ) ;
#58209=CARTESIAN_POINT ( 'NONE',  ( 5.823154874416164084, -0.05760400987671504547, 2.161107263091876618 ) ) ;
#58210=CARTESIAN_POINT ( 'NONE',  ( 3.983814121021773680, -1.821778379405362136, -0.2661574599523569007 ) ) ;
#58214=CARTESIAN_POINT ( 'NONE',  ( 0.5029371931441508625, -1.732330776274123796, 0.1679752909130062255 ) ) ;
#58215=CARTESIAN_POINT ( 'NONE',  ( 6.827182134110203471, 1.269052739965634391, 2.024653661457261222 ) ) ;
#58218=CARTESIAN_POINT ( 'NONE',  ( 4.083022661009271914, -0.2092679848491978134, -2.151539631373246220 ) ) ;
#58219=CARTESIAN_POINT ( 'NONE',  ( 5.782577320554741718, -1.967585831723076772, 0.4389650999883643046 ) ) ;
#58222=CARTESIAN_POINT ( 'NONE',  ( 3.678741886385179072, -2.082744454470350615, -0.5786317199799119182 ) ) ;
#58223=CARTESIAN_POINT ( 'NONE',  ( 3.848864690211077466, -1.613568265775822130, 1.132301161112803545 ) ) ;
#58225=CARTESIAN_POINT ( 'NONE',  ( 1.114821240386947965, -1.040235440384199794, -2.059874970276051265 ) ) ;
#58226=CARTESIAN_POINT ( 'NONE',  ( 3.304032624679804631, -2.058584765098357749, 0.09746896435120806779 ) ) ;
#58227=CARTESIAN_POINT ( 'NONE',  ( 6.040568865451770186, -1.638250791085652303, 1.042688759833640066 ) ) ;
#58236=CARTESIAN_POINT ( 'NONE',  ( 1.975870009618452050, 2.111717515986545113, -0.6407313945460398896 ) ) ;
#58239=CARTESIAN_POINT ( 'NONE',  ( 6.614115624646348834, 1.956711779489667125, -0.1410536379464824575 ) ) ;
#58240=CARTESIAN_POINT ( 'NONE',  ( -0.02880301295729841352, 5.718910385480866054, -2.867850616339829628 ) ) ;
#58244=CARTESIAN_POINT ( 'NONE',  ( 5.103375755629981469, -1.831930319445294719, 0.1838923505294575433 ) ) ;
#58246=CARTESIAN_POINT ( 'NONE',  ( 2.623961231070126132, -1.185536401616044566, -1.685555923420704039 ) ) ;
#58254=CARTESIAN_POINT ( 'NONE',  ( 0.9189065912094130928, 1.903898908998642447, 0.7894373168981814182 ) ) ;
#58256=CARTESIAN_POINT ( 'NONE',  ( 4.599059095968327071, -0.4863373063577690059, 1.775805238918099382 ) ) ;
#58262=CARTESIAN_POINT ( 'NONE',  ( 3.914836437932368796, 1.561248537261412883, -1.560010120355350471 ) ) ;
#58263=CARTESIAN_POINT ( 'NONE',  ( 6.925078400183534377, -0.01048729610059369148, 2.244148362790527429 ) ) ;
#58265=CARTESIAN_POINT ( 'NONE',  ( 6.486573133654839118, -1.106559166176981579, 1.434805384617921842 ) ) ;
#58266=CARTESIAN_POINT ( 'NONE',  ( 6.069544675611900253, 1.326465198304109583, 1.382431045765440514 ) ) ;
#58269=CARTESIAN_POINT ( 'NONE',  ( 1.704906730629534684, -1.665072001576539007, -1.584524786048894240 ) ) ;
#58271=CARTESIAN_POINT ( 'NONE',  ( 5.250612361737760025, 1.884661702551674534, 0.3228764834103393100 ) ) ;
#58274=CARTESIAN_POINT ( 'NONE',  ( 0.7603692911175019553, -1.357789551990191246, 1.287012767582619510 ) ) ;
#58275=CARTESIAN_POINT ( 'NONE',  ( 2.659388954101277847, 1.913261587491304150, -0.6371546050257800298 ) ) ;
#58277=CARTESIAN_POINT ( 'NONE',  ( 4.231157339275457119, 0.1028475037690677746, 2.103686673710772670 ) ) ;
#58282=CARTESIAN_POINT ( 'NONE',  ( 4.306902303582704761, -0.4466378413249347257, -1.969604032634456825 ) ) ;
#58285=CARTESIAN_POINT ( 'NONE',  ( 4.393933622532245842, -0.8317529007547798114, 1.995363109761492337 ) ) ;
#58291=CARTESIAN_POINT ( 'NONE',  ( 2.383468162319524630, -0.001743713053406481962, 2.171350059665664300 ) ) ;
#58294=CARTESIAN_POINT ( 'NONE',  ( 0.3800845246329161431, -0.2246070939678334044, -1.827447590993152682 ) ) ;
#58296=CARTESIAN_POINT ( 'NONE',  ( 3.193114300108112147, 1.729001323093733111, 1.346577201094656395 ) ) ;
#58297=CARTESIAN_POINT ( 'NONE',  ( 6.983263157960355016, 2.444413620957446742, 2.336241774956763884 ) ) ;
#58298=CARTESIAN_POINT ( 'NONE',  ( 3.309705378935084763, -0.4432241279512488807, 2.218521802316391511 ) ) ;
#58305=CARTESIAN_POINT ( 'NONE',  ( 4.797990518455403475, -1.769373726167685623, -0.04385371103611360177 ) ) ;
#58307=CARTESIAN_POINT ( 'NONE',  ( 0.2707219772894990384, -1.375384669632748524, 1.594866825539154043 ) ) ;
#58310=CARTESIAN_POINT ( 'NONE',  ( 1.135132829348266092, -0.04487231981731241992, -1.969206670302141804 ) ) ;
#58313=CARTESIAN_POINT ( 'NONE',  ( 0.2737812321212430566, -1.924752420120953822, 0.3788971555385572954 ) ) ;
#58316=CARTESIAN_POINT ( 'NONE',  ( 4.522238337509359773, 1.150754656758418593, -1.474723989322044737 ) ) ;
#58318=CARTESIAN_POINT ( 'NONE',  ( 4.223533608758993196, 0.2584441732129874603, -2.054024224480345939 ) ) ;
#58328=CARTESIAN_POINT ( 'NONE',  ( 4.281663391851794565, -1.878042059144067633, 0.5673916069991248312 ) ) ;
#58329=CARTESIAN_POINT ( 'NONE',  ( 2.477888549845189470, 1.799646572043178683, 0.9090068759892779848 ) ) ;
#58333=CARTESIAN_POINT ( 'NONE',  ( 0.4736314445139556684, 1.071599637473351629, 1.532994764490814177 ) ) ;
#58335=CARTESIAN_POINT ( 'NONE',  ( 2.549090200060105893, 0.2507624435445845457, 1.997490752340509879 ) ) ;
#58337=CARTESIAN_POINT ( 'NONE',  ( 3.357133807288110727, 0.04956003552011908203, -2.116800119666595315 ) ) ;
#58339=CARTESIAN_POINT ( 'NONE',  ( 5.248515149483167441, -2.054309126314420642, -0.2569322651706855143 ) ) ;
#58341=CARTESIAN_POINT ( 'NONE',  ( 0.6090670738765286973, -0.3027767823605455599, 2.068569423397928819 ) ) ;
#58343=CARTESIAN_POINT ( 'NONE',  ( 5.895480738319402114, 1.384055093596334274, 1.190509915477963698 ) ) ;
#58350=CARTESIAN_POINT ( 'NONE',  ( 5.707647354773449422, 1.450964518888698596, 1.245719642194928811 ) ) ;
#58362=CARTESIAN_POINT ( 'NONE',  ( 5.466422796518627614, -1.967893101392578448, -0.4390109167287381542 ) ) ;
#58369=CARTESIAN_POINT ( 'NONE',  ( 2.043745906638486431, 1.354474275242853798, 1.429983431767953617 ) ) ;
#58370=CARTESIAN_POINT ( 'NONE',  ( 2.970327539257538341, -1.987051465770898417, -0.3419137282784574516 ) ) ;
#58372=CARTESIAN_POINT ( 'NONE',  ( 6.727182134110196721, 7.629137130509074716, 2.889055895399252005 ) ) ;
#58373=CARTESIAN_POINT ( 'NONE',  ( 3.609492757825348175, -2.159078094573213757, 0.3743817768235499499 ) ) ;
#58374=CARTESIAN_POINT ( 'NONE',  ( 2.327063250521405724, -0.002089543651138252821, 1.926566264030280307 ) ) ;
#58376=CARTESIAN_POINT ( 'NONE',  ( 0.2331563151865730654, 0.7315591717663977311, -2.029986209603263259 ) ) ;
#58384=CARTESIAN_POINT ( 'NONE',  ( 5.618664544990171095, -0.03892770779775727580, 1.841008343696965310 ) ) ;
#58385=CARTESIAN_POINT ( 'NONE',  ( 2.895184040856535468, -0.1504547458161388240, -2.007539188286605825 ) ) ;
#58386=CARTESIAN_POINT ( 'NONE',  ( 4.235939456923387247, -2.142719978266393710, -0.8318502446633867509 ) ) ;
#58387=CARTESIAN_POINT ( 'NONE',  ( -0.02880301295722555166, 0.6711181056864559125, -2.353869138803561079 ) ) ;
#58388=CARTESIAN_POINT ( 'NONE',  ( 2.764321045800025800, -0.7073474514263197177, -1.721481455096545377 ) ) ;
#58394=CARTESIAN_POINT ( 'NONE',  ( 6.058164993413670096, -1.477959563288837375, 1.479067623735799586 ) ) ;
#58401=CARTESIAN_POINT ( 'NONE',  ( 6.375633740537438143, 1.648238817998586958, -0.5085109915310691564 ) ) ;
#58403=CARTESIAN_POINT ( 'NONE',  ( 1.265804362365889668, 1.602598504008081237, -0.6630416328189077113 ) ) ;
#58407=CARTESIAN_POINT ( 'NONE',  ( 6.139545750997863927, 2.009069680886385267, -0.8233997750264672177 ) ) ;
#58408=CARTESIAN_POINT ( 'NONE',  ( 4.600122369450095228, -1.825375079466069694, -0.04201004182294298950 ) ) ;
#58409=CARTESIAN_POINT ( 'NONE',  ( 2.008577182894935476, 0.6104510041588115943, 1.864461945915835583 ) ) ;
#58413=CARTESIAN_POINT ( 'NONE',  ( 3.176547234745368264, 0.9552152173708803318, 1.893241096743401464 ) ) ;
#58418=CARTESIAN_POINT ( 'NONE',  ( 2.307561340129569150, -1.660171796135110567, -1.236610361758017973 ) ) ;
#58421=CARTESIAN_POINT ( 'NONE',  ( 4.020361658589631126, -2.215315801286695585, 0.1640026922601171833 ) ) ;
#58423=CARTESIAN_POINT ( 'NONE',  ( 2.198211363809216667, 2.055062875077425577, 1.030007645627160517 ) ) ;
#58425=CARTESIAN_POINT ( 'NONE',  ( 6.455934469078565385, -0.7002696157344409089, 1.940163012464599879 ) ) ;
#58429=CARTESIAN_POINT ( 'NONE',  ( 6.603072989126265391, -0.3962418105841297722, 1.804722624154910360 ) ) ;
#58431=CARTESIAN_POINT ( 'NONE',  ( -0.2104748580754409182, 6.947232144882289795, -2.698723162346649662 ) ) ;
#58432=CARTESIAN_POINT ( 'NONE',  ( 2.783889825318270450, -0.8885198777363271239, 1.478144978849999847 ) ) ;
#58433=CARTESIAN_POINT ( 'NONE',  ( 2.852750215419812108, -1.865046845876184189, -0.7672916333427428626 ) ) ;
#58434=CARTESIAN_POINT ( 'NONE',  ( 2.971610153692927803, -2.265147269936502727, -0.3905154627303064618 ) ) ;
#58435=CARTESIAN_POINT ( 'NONE',  ( 3.251526197659323270, -1.847530484110882387, -1.305540666510462078 ) ) ;
#58436=CARTESIAN_POINT ( 'NONE',  ( 5.250649905694958264, 0.6104557620976447385, 2.015647016877469166 ) ) ;
#58438=CARTESIAN_POINT ( 'NONE',  ( 3.461912321176093599, 0.7928900474763724837, 1.582224000876080172 ) ) ;
#58440=CARTESIAN_POINT ( 'NONE',  ( 6.110887424941569002, -0.2848874328069994633, 2.274520343394012212 ) ) ;
#58441=CARTESIAN_POINT ( 'NONE',  ( 5.982333729491328356, -0.2747192703472668418, -1.820405398140816589 ) ) ;
#58445=CARTESIAN_POINT ( 'NONE',  ( 5.296902861200166512, 1.790115547914197247, 1.263834295783084150 ) ) ;
#58448=CARTESIAN_POINT ( 'NONE',  ( 5.494608840674215955, 2.039112051642687717, 0.3575134270455831986 ) ) ;
#58452=CARTESIAN_POINT ( 'NONE',  ( 4.213445252184796708, -0.3281303603181011108, 1.898201707710310826 ) ) ;
#58455=CARTESIAN_POINT ( 'NONE',  ( 0.4049022847291971483, -2.205595429402911201, -0.2640273158710532142 ) ) ;
#58465=CARTESIAN_POINT ( 'NONE',  ( 1.064813361795993618, 1.487921858168140377, -1.278797858372302088 ) ) ;
#58468=CARTESIAN_POINT ( 'NONE',  ( 5.670351692713981429, -0.8806477319739226539, -1.753155087565357428 ) ) ;
#58471=CARTESIAN_POINT ( 'NONE',  ( 6.596550757224428629, -0.5713381284546023009, -2.084776384472402100 ) ) ;
#58475=CARTESIAN_POINT ( 'NONE',  ( 0.5791066246769066561, 1.747692025923882841, -0.6672336632058751826 ) ) ;
#58476=CARTESIAN_POINT ( 'NONE',  ( 5.729790939124476346, -1.568816369837353619, -0.7386035493782086014 ) ) ;
#58478=CARTESIAN_POINT ( 'NONE',  ( 3.439196427729715566, -1.660734982795486481, -1.430121640581414111 ) ) ;
#58479=CARTESIAN_POINT ( 'NONE',  ( 3.927071981709300719, 2.190135382617847792, 0.7269923479944776501 ) ) ;
#58480=CARTESIAN_POINT ( 'NONE',  ( 6.696563014664697278, -0.5452183415704283664, -1.987298092995327226 ) ) ;
#58481=CARTESIAN_POINT ( 'NONE',  ( 2.238135065718354078, 0.4255327557451081266, 1.894600943326588238 ) ) ;
#58484=CARTESIAN_POINT ( 'NONE',  ( 4.869442314738527067, -1.792836814666173062, -1.132239877606910472 ) ) ;
#58486=CARTESIAN_POINT ( 'NONE',  ( 3.322888845334175389, 0.9041102021897020613, -1.802417075407992897 ) ) ;
#58490=CARTESIAN_POINT ( 'NONE',  ( 0.9085097582094739943, 1.384192474337717194, -1.190531929384466281 ) ) ;
#58495=CARTESIAN_POINT ( 'NONE',  ( 6.069226122992825267, 0.1539936439061925788, -2.055202734049704105 ) ) ;
#58500=CARTESIAN_POINT ( 'NONE',  ( 5.039715841750210146, -1.917062458738912012, 0.6357382205050918778 ) ) ;
#58501=CARTESIAN_POINT ( 'NONE',  ( 6.112022827852052309, -0.7509524718064889415, 2.090657394127520163 ) ) ;
#58506=CARTESIAN_POINT ( 'NONE',  ( 3.801680928091007772, -0.6000553829732765410, 1.971583879547859963 ) ) ;
#58507=CARTESIAN_POINT ( 'NONE',  ( 3.815077410725796980, 1.076317812134291119, -1.704938119663282903 ) ) ;
#58512=ORIENTED_EDGE ( 'NONE', *, *, #97813, .F. ) ;
#58514=CARTESIAN_POINT ( 'NONE',  ( 3.848982377512807140, -0.9961485462514390044, 1.752762419822328832 ) ) ;
#58515=CARTESIAN_POINT ( 'NONE',  ( 2.202840038917678545, -0.4038221959529255112, 1.796142596185656526 ) ) ;
#58516=CARTESIAN_POINT ( 'NONE',  ( 0.7510979139944070626, 0.6750874020578813139, 2.206752807669599470 ) ) ;
#58518=CARTESIAN_POINT ( 'NONE',  ( 4.270900206319126369, -2.015198044118733822, -0.7823990653590962019 ) ) ;
#58520=ORIENTED_EDGE ( 'NONE', *, *, #207763, .T. ) ;
#58522=CARTESIAN_POINT ( 'NONE',  ( 2.395189659270926086, 1.444574673180216706, 1.188490415850687265 ) ) ;
#58524=CARTESIAN_POINT ( 'NONE',  ( 5.471542181860619358, 1.900225975651721244, -0.5249898485142224791 ) ) ;
#58528=CARTESIAN_POINT ( 'NONE',  ( 0.3466626200071438180, 2.201290530325435757, 0.1579762268871589825 ) ) ;
#58532=CARTESIAN_POINT ( 'NONE',  ( 6.539320575229256249, 7.052319431262985105, 2.701414634427783845 ) ) ;
#58533=CARTESIAN_POINT ( 'NONE',  ( 6.455938704688762186, 1.966190342143339764, -0.1448359745850023028 ) ) ;
#58534=CARTESIAN_POINT ( 'NONE',  ( 5.321043329010971767, 2.130378997510178785, 0.8875623774946446165 ) ) ;
#58535=CARTESIAN_POINT ( 'NONE',  ( 5.740631066870683696, -1.815735608131360479, -0.4073663091734185948 ) ) ;
#58536=CARTESIAN_POINT ( 'NONE',  ( 2.799736005369108049, -1.525370932871713547, -1.388464765246626875 ) ) ;
#58543=CARTESIAN_POINT ( 'NONE',  ( 5.441899255841128102, 1.454089660041712140, 1.612519925251713060 ) ) ;
#58546=CARTESIAN_POINT ( 'NONE',  ( 3.526749072549471453, -1.699942963128863838, 0.7078653300200200560 ) ) ;
#58551=CARTESIAN_POINT ( 'NONE',  ( 0.5446534387809185418, 2.256470935699141034, 0.1650129453365980214 ) ) ;
#58557=CARTESIAN_POINT ( 'NONE',  ( -0.1049974700286886165, -0.1398519552151776535, -1.881156918050665094 ) ) ;
#58558=CARTESIAN_POINT ( 'NONE',  ( 0.3734444151584931926, 1.013553851667288841, 1.450680648178425125 ) ) ;
#58559=CARTESIAN_POINT ( 'NONE',  ( 4.934244218189309805, -1.078892596291732398, -1.699401429059212765 ) ) ;
#58561=CARTESIAN_POINT ( 'NONE',  ( 3.856552995061765632, 0.7561154531541111057, 1.965730562608114740 ) ) ;
#58563=CARTESIAN_POINT ( 'NONE',  ( 3.005391328865916645, -1.845313015785840172, 0.5138285116655214591 ) ) ;
#58565=CARTESIAN_POINT ( 'NONE',  ( 3.894935592111925526, 0.2864876570476772022, 1.948460325470881660 ) ) ;
#58566=CARTESIAN_POINT ( 'NONE',  ( 5.449475261934634496, -1.824267568868439771, 0.8672911397697125047 ) ) ;
#58567=CARTESIAN_POINT ( 'NONE',  ( 2.324885834233282544, -0.002380789299309681549, 1.870836310375329381 ) ) ;
#58568=CARTESIAN_POINT ( 'NONE',  ( 5.162619097868246243, -1.245661315326980212, 1.193383824415847450 ) ) ;
#58570=CARTESIAN_POINT ( 'NONE',  ( 2.350463684150871035, 2.206416367115513477, 0.05273732197710182673 ) ) ;
#58573=CARTESIAN_POINT ( 'NONE',  ( 6.057081135787192316, 1.604708697955498087, -1.128374156723031430 ) ) ;
#58581=CARTESIAN_POINT ( 'NONE',  ( 2.014207461368537455, 2.064961549741591185, -0.1501100615294431728 ) ) ;
#58585=CARTESIAN_POINT ( 'NONE',  ( 6.633471380297788045, -0.1541069161683609745, 2.086224335282916620 ) ) ;
#58590=CARTESIAN_POINT ( 'NONE',  ( 4.991564454312596766, 1.928456700051227379, 0.5879293935868237231 ) ) ;
#58591=CARTESIAN_POINT ( 'NONE',  ( 4.768704397049558175, -0.2406929234074564883, -1.900496090682921579 ) ) ;
#58592=CARTESIAN_POINT ( 'NONE',  ( 6.539320575229236709, 3.694699318329996540, 2.517509839998680832 ) ) ;
#58593=CARTESIAN_POINT ( 'NONE',  ( 2.156058135970494227, 0.9403143569667195001, 1.979733194660021622 ) ) ;
#58596=CARTESIAN_POINT ( 'NONE',  ( 0.1529896150729666005, 0.3463191217260193633, 1.982936507005612414 ) ) ;
#58597=CARTESIAN_POINT ( 'NONE',  ( 2.373185085050379506, -1.665764800640230803, -0.9392108107411781814 ) ) ;
#58600=CARTESIAN_POINT ( 'NONE',  ( 6.573823534745116604, -0.9041686956474543901, 1.912245183953432237 ) ) ;
#58603=CARTESIAN_POINT ( 'NONE',  ( 3.667594231577479658, 1.163246697351211223, 1.737046641446901463 ) ) ;
#58605=CARTESIAN_POINT ( 'NONE',  ( 2.326796526899118422, -0.003300274434325441240, 1.724958192180660044 ) ) ;
#58614=CARTESIAN_POINT ( 'NONE',  ( 2.473076435208894530, -1.576862618776267100, -0.8914009245391883995 ) ) ;
#58618=CARTESIAN_POINT ( 'NONE',  ( 3.756361958294622383, 1.803085962505234008, 0.1738922897399265421 ) ) ;
#58619=CARTESIAN_POINT ( 'NONE',  ( 6.539320575229274901, 7.053161517996441532, 2.494893549996656912 ) ) ;
#58625=CARTESIAN_POINT ( 'NONE',  ( 3.859670702416746924, -0.5421201558965526024, 1.780318336934373802 ) ) ;
#58627=CARTESIAN_POINT ( 'NONE',  ( 1.581495747622517323, -0.6437907056052544208, 1.804334155150161267 ) ) ;
#58628=CARTESIAN_POINT ( 'NONE',  ( 0.6744773098602949712, -1.717252091951677384, -0.6198786263262797691 ) ) ;
#58634=CARTESIAN_POINT ( 'NONE',  ( 6.925078400183593885, 7.051837472187183486, 2.742497896504832333 ) ) ;
#58636=CARTESIAN_POINT ( 'NONE',  ( 5.858249334120006147, -1.969629310164786373, -0.003746551262697600092 ) ) ;
#58639=CARTESIAN_POINT ( 'NONE',  ( 1.834041477103361739, 2.068079971995392619, 0.3053845110000241170 ) ) ;
#58640=CARTESIAN_POINT ( 'NONE',  ( 6.264670948233396430, -1.361836867979081545, 1.362739274238314868 ) ) ;
#58642=CARTESIAN_POINT ( 'NONE',  ( 1.447985623159939284, 1.823312892812560593, 0.09356915273009414058 ) ) ;
#58643=CARTESIAN_POINT ( 'NONE',  ( 3.686314334879085663, -1.088174899301070253, 1.919869060924610293 ) ) ;
#58645=CARTESIAN_POINT ( 'NONE',  ( 1.353610510645312237, -1.387278792934818705, -1.316581319992945920 ) ) ;
#58647=CARTESIAN_POINT ( 'NONE',  ( 1.029674291210751269, 1.899031994249468225, -0.5220998716058099509 ) ) ;
#58648=CARTESIAN_POINT ( 'NONE',  ( 2.401813893259804100, -0.7453968187615340746, -1.793506507769267788 ) ) ;
#58652=CARTESIAN_POINT ( 'NONE',  ( 6.367989434593707365, -1.846973275860162467, 0.2267098040239327594 ) ) ;
#58657=CARTESIAN_POINT ( 'NONE',  ( 3.070069520051089906, -1.303570237086741024, 1.761582097007891923 ) ) ;
#58660=CARTESIAN_POINT ( 'NONE',  ( 3.158640206316553289, -1.382037546686708973, 1.193037399656725395 ) ) ;
#58665=CARTESIAN_POINT ( 'NONE',  ( 6.925078400183546812, 2.074047572655359328, 2.163550030515603684 ) ) ;
#58667=CARTESIAN_POINT ( 'NONE',  ( 0.6098321186917586845, -1.917330571200571265, 0.1878080533235688687 ) ) ;
#58669=CARTESIAN_POINT ( 'NONE',  ( 5.436364959771895045, -1.092926877770916017, 1.628904810760459121 ) ) ;
#58673=CARTESIAN_POINT ( 'NONE',  ( 5.144143540903125533, 0.6357783856077160456, 2.097287126430439130 ) ) ;
#58676=EDGE_CURVE ( 'NONE', #190223, #11451, #95777, .T. ) ;
#58677=CARTESIAN_POINT ( 'NONE',  ( 5.524307029080702591, 1.015476208609331188, 1.803995072556117574 ) ) ;
#58681=CARTESIAN_POINT ( 'NONE',  ( 4.799617249347348569, 1.585997580420713593, -1.664126067976256840 ) ) ;
#58684=CARTESIAN_POINT ( 'NONE',  ( 0.07670252363861564115, -2.225146658028719582, -0.5502862128906602646 ) ) ;
#58687=CARTESIAN_POINT ( 'NONE',  ( 5.437426780092255996, 0.7852709207246920675, -1.776270868113111856 ) ) ;
#58691=CARTESIAN_POINT ( 'NONE',  ( 0.0002439367322616680669, -0.9454701154091667004, 1.777349279628215095 ) ) ;
#58692=CARTESIAN_POINT ( 'NONE',  ( 6.510786919798099426, 1.273903079158642981, -1.162983891536113479 ) ) ;
#58693=CARTESIAN_POINT ( 'NONE',  ( 5.577361344084559747, 1.530155114678043660, 1.313547687611632764 ) ) ;
#58697=CARTESIAN_POINT ( 'NONE',  ( 2.009825619773229377, -0.9864030779522957593, -1.843301731911746399 ) ) ;
#58698=CARTESIAN_POINT ( 'NONE',  ( 6.555894367415777246, 1.764769525206461687, -0.1329060007094622631 ) ) ;
#58699=CARTESIAN_POINT ( 'NONE',  ( 5.555314621531947772, -1.277044735018734833, 1.560499014526220307 ) ) ;
#58701=CARTESIAN_POINT ( 'NONE',  ( 3.064699953192471682, -2.118106589925540906, -0.8768602481810504612 ) ) ;
#58703=CARTESIAN_POINT ( 'NONE',  ( 2.413636602577839518, 1.137377966863511780, -1.317326450295707607 ) ) ;
#58705=CARTESIAN_POINT ( 'NONE',  ( 1.862203476926355794, -0.5897614712949137417, 1.630587920151181924 ) ) ;
#58707=CARTESIAN_POINT ( 'NONE',  ( 1.820531350174507512, -1.319122485308525716, 1.313071031887176998 ) ) ;
#58709=CARTESIAN_POINT ( 'NONE',  ( 2.770184829093131462, -2.147865496273542174, 0.3164581508635355145 ) ) ;
#58710=CARTESIAN_POINT ( 'NONE',  ( 3.274625289317079524, -0.3981104328964027994, -1.976669913042613747 ) ) ;
#58711=CARTESIAN_POINT ( 'NONE',  ( 3.843750000000002220, 1.895863743164162063, 0.7852924748297951396 ) ) ;
#58713=CARTESIAN_POINT ( 'NONE',  ( 0.9207747878037384481, 1.778742719161881203, 0.7400954639872597829 ) ) ;
#58715=CARTESIAN_POINT ( 'NONE',  ( 3.656649667753679278, 2.210956852819144114, 0.2149545701610345305 ) ) ;
#58720=CARTESIAN_POINT ( 'NONE',  ( 0.04794026018281431767, -2.028123841075918588, 0.9064578031776747702 ) ) ;
#58721=CARTESIAN_POINT ( 'NONE',  ( 4.633228507203630997, 0.002057781214020309134, -1.962046631861932067 ) ) ;
#58726=CARTESIAN_POINT ( 'NONE',  ( 5.220128827380259295, -1.204132088723122385, -1.915181361845545105 ) ) ;
#58728=CARTESIAN_POINT ( 'NONE',  ( 2.453648911872767346, 1.593012163857405961, 1.310297011819524293 ) ) ;
#58733=CARTESIAN_POINT ( 'NONE',  ( 3.303821147848403861, -1.868562489643767144, 0.08839296284299941187 ) ) ;
#58734=CARTESIAN_POINT ( 'NONE',  ( 3.076526641549358398, -0.6997103666757237272, 1.586905598789583482 ) ) ;
#58735=CARTESIAN_POINT ( 'NONE',  ( 0.5040057298127769148, -2.280580521882575429, 0.2324455964911649464 ) ) ;
#58736=CARTESIAN_POINT ( 'NONE',  ( 0.6576010401811819284, -1.865379905010958517, -1.178792301215730642 ) ) ;
#58737=CARTESIAN_POINT ( 'NONE',  ( 4.107036007299074143, -0.3554739980045698022, 2.060130632118581051 ) ) ;
#58738=CARTESIAN_POINT ( 'NONE',  ( 5.753840666697315420, 0.7890659797671593090, 1.774590222461839506 ) ) ;
#58741=CARTESIAN_POINT ( 'NONE',  ( 0.2499999969303341174, 7.552774431159578439E-08, 2.052068128417954274 ) ) ;
#58742=CARTESIAN_POINT ( 'NONE',  ( 0.5103889644224939293, -1.913802852362625151, 0.6352017490645140985 ) ) ;
#58748=CARTESIAN_POINT ( 'NONE',  ( 4.547361323050268744, -1.413013347330991598, -1.156083184146582177 ) ) ;
#58749=CARTESIAN_POINT ( 'NONE',  ( 2.081372155488591780, -0.1082299263688718260, -2.204229314041641352 ) ) ;
#58755=CARTESIAN_POINT ( 'NONE',  ( 1.441672106306312484, -1.900340447277752087, 0.6846001189487918026 ) ) ;
#58758=CARTESIAN_POINT ( 'NONE',  ( 3.238934005158759621, -0.1320712000743811398, -1.856290971584534377 ) ) ;
#58761=ORIENTED_EDGE ( 'NONE', *, *, #205304, .T. ) ;
#58764=CARTESIAN_POINT ( 'NONE',  ( 3.703562413045482060, -0.5285312144065814621, 1.747510042522756990 ) ) ;
#58768=CARTESIAN_POINT ( 'NONE',  ( 0.9129801003131752246, 0.4962884120854795245, 1.661303041287894411 ) ) ;
#58769=CARTESIAN_POINT ( 'NONE',  ( 6.351489326974223637, 1.835832825663574752, -0.1405570519043483624 ) ) ;
#58770=CARTESIAN_POINT ( 'NONE',  ( 4.811288673970230967, 2.006026520401600788, 1.140621419682581239 ) ) ;
#58772=CARTESIAN_POINT ( 'NONE',  ( 6.714160596891073141, -1.012370167489636819, -1.909856561116265450 ) ) ;
#58776=CARTESIAN_POINT ( 'NONE',  ( 5.536544918007444416, 2.217299919257350371, -0.6050018498083614693 ) ) ;
#58779=CARTESIAN_POINT ( 'NONE',  ( 5.524238439434661530, 1.113281918156138639, -1.503147240406087271 ) ) ;
#58780=CARTESIAN_POINT ( 'NONE',  ( 2.689602200614676697, 1.814610489020528350, -0.6038049036062518304 ) ) ;
#58782=CARTESIAN_POINT ( 'NONE',  ( 3.932405576212230525, 1.181341412803040614, -1.863887651898883613 ) ) ;
#58783=CARTESIAN_POINT ( 'NONE',  ( 4.241493788847498614, 0.4602237217972443561, -2.066584722733503909 ) ) ;
#58785=CARTESIAN_POINT ( 'NONE',  ( 6.983263157960366563, 2.432509251381759441, 2.428019605373044509 ) ) ;
#58789=CARTESIAN_POINT ( 'NONE',  ( 2.433052891977859566, 2.238319448195260186, 0.5606502339033142546 ) ) ;
#58790=CARTESIAN_POINT ( 'NONE',  ( 2.998438581075290710, 1.946722116546204306, 0.2428724957088539971 ) ) ;
#58792=CARTESIAN_POINT ( 'NONE',  ( 6.965701137139799215, -0.4614044149895025204, 2.017943399502773349 ) ) ;
#58796=CARTESIAN_POINT ( 'NONE',  ( 4.856657812281613751, -1.900414607462055816, -0.6748505307947461063 ) ) ;
#58801=CARTESIAN_POINT ( 'NONE',  ( 2.413135165516873126, -1.680682958684741823, 1.374403011902309402 ) ) ;
#58802=CARTESIAN_POINT ( 'NONE',  ( 6.933263157960367629, 7.629137130509066722, 2.653810918356712900 ) ) ;
#58807=CARTESIAN_POINT ( 'NONE',  ( 1.300152579660202923, -2.060967562519558705, -0.002860995899278336550 ) ) ;
#58808=CARTESIAN_POINT ( 'NONE',  ( -0.02244404828160087226, 4.081832076214893412, -2.743766916979750281 ) ) ;
#58809=CARTESIAN_POINT ( 'NONE',  ( 6.727182134110237577, 2.455520393281558356, 2.294684051055717600 ) ) ;
#58813=CARTESIAN_POINT ( 'NONE',  ( 3.018110381800835018, -1.909997030407738938, 0.09613604992317337228 ) ) ;
#58815=CARTESIAN_POINT ( 'NONE',  ( 4.750734298983296355, -1.420434005603900429, 1.055588576545069657 ) ) ;
#58816=CARTESIAN_POINT ( 'NONE',  ( 2.191926089937683564, 1.177725938178806997, 1.506473034612793915 ) ) ;
#58819=CARTESIAN_POINT ( 'NONE',  ( 0.2158530320381162604, 0.9822752966809102926, -1.644539037099991718 ) ) ;
#58821=CARTESIAN_POINT ( 'NONE',  ( 0.7661813929631040576, -2.060537521029872643, 0.2012509062776293156 ) ) ;
#58823=CARTESIAN_POINT ( 'NONE',  ( 6.157094445334826638, -1.605393284960114242, -0.9600186418455139981 ) ) ;
#58824=CARTESIAN_POINT ( 'NONE',  ( 2.191784710619415044, -0.7813054520266484726, 1.650194661559079456 ) ) ;
#58825=CARTESIAN_POINT ( 'NONE',  ( 5.848300530743933301, 2.204158087718602221, 0.1119919437090263481 ) ) ;
#58828=CARTESIAN_POINT ( 'NONE',  ( 3.121586329596927722, 0.3053734461533639255, -2.039847365138738766 ) ) ;
#58832=CARTESIAN_POINT ( 'NONE',  ( 0.8608787451157869919, -1.566265403972837866, 1.489986575276234460 ) ) ;
#58834=CARTESIAN_POINT ( 'NONE',  ( 5.547352688424546763, 1.827615396715172258, -0.9727077141251788683 ) ) ;
#58836=CARTESIAN_POINT ( 'NONE',  ( 2.477987356985793088, 1.327747062846416526, 1.705691702009938915 ) ) ;
#58838=CARTESIAN_POINT ( 'NONE',  ( 2.842449411481930532, 1.120122121419616423, -1.680381219987029606 ) ) ;
#58839=CARTESIAN_POINT ( 'NONE',  ( 2.453501617077270769, 1.514643136537169310, 1.246875331876770243 ) ) ;
#58840=CARTESIAN_POINT ( 'NONE',  ( 6.620655732516649294, 2.950034989283246478, 2.626075342966327497 ) ) ;
#58844=CARTESIAN_POINT ( 'NONE',  ( 1.042204282965590201, 0.8216761606248854655, 1.841732292558920570 ) ) ;
#58847=CARTESIAN_POINT ( 'NONE',  ( 6.392125918040960642, -0.5824770489515176397, -2.112646119873210271 ) ) ;
#58849=CARTESIAN_POINT ( 'NONE',  ( 5.994389040191066442, -1.017321598621454548, 1.619163160827830517 ) ) ;
#58853=CARTESIAN_POINT ( 'NONE',  ( 2.741814726283864800, 2.006445297011373974, -0.2004551355171620974 ) ) ;
#58856=CARTESIAN_POINT ( 'NONE',  ( 6.545920775329808983, 0.6544052999908689383, -1.596017746584824426 ) ) ;
#58860=CARTESIAN_POINT ( 'NONE',  ( 4.340975799156801429, -1.628549031532234403, 0.9200136957008757665 ) ) ;
#58861=CARTESIAN_POINT ( 'NONE',  ( 1.604436975501881468, 2.067711310959176707, 0.1055696395834623824 ) ) ;
#58867=CARTESIAN_POINT ( 'NONE',  ( 0.5447927104418804900, 0.1337802856970966847, 1.806726864048732173 ) ) ;
#58874=CARTESIAN_POINT ( 'NONE',  ( 1.029656018189710309, 1.891699080040713410, -0.5197978237033785698 ) ) ;
#58876=CARTESIAN_POINT ( 'NONE',  ( 4.587445725801254426, -0.5070264450876013074, 1.847228357985892577 ) ) ;
#58881=CARTESIAN_POINT ( 'NONE',  ( 6.825078400183573812, 0.002648415797040087893, 1.855566311045192540 ) ) ;
#58885=CARTESIAN_POINT ( 'NONE',  ( 2.571340117545738657, 0.1069729528509130723, -2.159185227005658181 ) ) ;
#58889=CARTESIAN_POINT ( 'NONE',  ( -0.1225938595818750754, -1.897163925677572305, -0.9476133185889324961 ) ) ;
#58890=CARTESIAN_POINT ( 'NONE',  ( 4.453998568579462969, 1.825179399820752169, -0.04523609120457571658 ) ) ;
#58893=CARTESIAN_POINT ( 'NONE',  ( 1.317580156568556538, -1.924246910545416522, 0.4277698889081028577 ) ) ;
#58894=CARTESIAN_POINT ( 'NONE',  ( 3.761887187967042134, 0.6396200178584460216, -1.802413552503052463 ) ) ;
#58898=CARTESIAN_POINT ( 'NONE',  ( 4.738697576358215535, -1.909850223682897807, -0.4806687167441258679 ) ) ;
#58900=CARTESIAN_POINT ( 'NONE',  ( 6.075724011240296818, -1.035248994944122369, 1.642949693582099302 ) ) ;
#58904=CARTESIAN_POINT ( 'NONE',  ( 6.187751663909415001, 2.028806014889028120, -0.6170373231123224000 ) ) ;
#58906=CARTESIAN_POINT ( 'NONE',  ( 4.336511155197938727, 1.173803677898217712, -1.509565991254034678 ) ) ;
#58909=CARTESIAN_POINT ( 'NONE',  ( 4.969394074578011633, -1.701821450762316612, -1.075051190359946895 ) ) ;
#58911=CARTESIAN_POINT ( 'NONE',  ( 5.900976575431972293, 1.489821718068456979, -1.054992404821846863 ) ) ;
#58912=CARTESIAN_POINT ( 'NONE',  ( 1.539598694730393680, 1.913698299121506352, -0.7905179490511196061 ) ) ;
#58915=CARTESIAN_POINT ( 'NONE',  ( 6.455916552660014851, 1.865467424361374249, -0.1398750677365916961 ) ) ;
#58920=CARTESIAN_POINT ( 'NONE',  ( 6.825078400183548055, 2.461594334264828987, 2.239602747093616841 ) ) ;
#58922=CARTESIAN_POINT ( 'NONE',  ( 4.852092609920839905, 0.1625460678297725725, -1.726498261149024271 ) ) ;
#58924=CARTESIAN_POINT ( 'NONE',  ( 2.588806720547200513, 2.007000696110202043, 0.5072723548179418618 ) ) ;
#58925=CARTESIAN_POINT ( 'NONE',  ( 3.480171074976373013, -2.114893226951024108, -0.1016293738061168905 ) ) ;
#58929=CARTESIAN_POINT ( 'NONE',  ( 1.199983893365302201, 0.8030756602186311932, -1.798478550607261583 ) ) ;
#58932=CARTESIAN_POINT ( 'NONE',  ( 0.2461629937395051204, 0.9812432698282257393, -1.641294572782559413 ) ) ;
#58933=CARTESIAN_POINT ( 'NONE',  ( 3.679849949768813744, -1.130634651955428671, 1.993948080406320766 ) ) ;
#58934=CARTESIAN_POINT ( 'NONE',  ( 1.488595654847741923, -0.2661386877833260556, -1.806066791206423217 ) ) ;
#58939=CARTESIAN_POINT ( 'NONE',  ( 3.217044422572811424, 1.584514289383936347, -1.241758421991135064 ) ) ;
#58940=CARTESIAN_POINT ( 'NONE',  ( 2.166782468979636000, 1.457124453068344039, -1.313723524322525815 ) ) ;
#58943=CARTESIAN_POINT ( 'NONE',  ( 0.07516593201273635838, 6.947014887512039216, -2.639261810199782232 ) ) ;
#58944=CARTESIAN_POINT ( 'NONE',  ( 4.523432754507224374, -1.286067535266706807, -1.648171318802932106 ) ) ;
#58945=CARTESIAN_POINT ( 'NONE',  ( 3.484973364136711549, 1.600408865665205571, -0.7559459569618111052 ) ) ;
#58947=CARTESIAN_POINT ( 'NONE',  ( 6.140627040082555332, -1.939752761746313059, 1.221158637518650503 ) ) ;
#58948=CARTESIAN_POINT ( 'NONE',  ( 5.384588317801639157, 1.532214865288351158, -0.8252546180599307224 ) ) ;
#58950=CARTESIAN_POINT ( 'NONE',  ( 5.906922434318937931, -1.273882657197453305, -1.913274281643152941 ) ) ;
#58951=CARTESIAN_POINT ( 'NONE',  ( 0.1333692844072559280, 6.947498546895843674, -2.648624074793118233 ) ) ;
#58952=CARTESIAN_POINT ( 'NONE',  ( 5.905553417332951582, 0.3413034225961882884, 1.699694455674398919 ) ) ;
#58953=CARTESIAN_POINT ( 'NONE',  ( 6.438686429976131720, -1.555646628146038157, 1.282773817382940384 ) ) ;
#58956=CARTESIAN_POINT ( 'NONE',  ( 5.969212972359552616, 1.911920703953375655, 1.028910892658722265 ) ) ;
#58958=CARTESIAN_POINT ( 'NONE',  ( 0.1810649180928698143, 1.756560269771380911, -1.181951075121101979 ) ) ;
#58959=CARTESIAN_POINT ( 'NONE',  ( 4.875000000000002665, 2.052068128417942727, -2.776269294175867294E-13 ) ) ;
#58961=CARTESIAN_POINT ( 'NONE',  ( 4.225552302291880835, -1.843726210754624173, 0.5582998813679838079 ) ) ;
#58963=CARTESIAN_POINT ( 'NONE',  ( 0.2764465059262249391, 2.196205179236205396, -0.3323138113263158222 ) ) ;
#58968=CARTESIAN_POINT ( 'NONE',  ( 2.403257875557132994, -0.3827610287685556112, -2.187935401104672994 ) ) ;
#58969=CARTESIAN_POINT ( 'NONE',  ( -0.02900071798685524560, 2.860900941590225344, -2.661937258840251008 ) ) ;
#58973=CARTESIAN_POINT ( 'NONE',  ( 1.125625214514534900, 0.3961039030971893471, 1.976955501819408711 ) ) ;
#58975=CARTESIAN_POINT ( 'NONE',  ( 6.566849514013569866, 1.531126396248701171, -1.382332999690039754 ) ) ;
#58980=CARTESIAN_POINT ( 'NONE',  ( 1.457869587114325460, 0.7109265171535653627, 1.620852848218183873 ) ) ;
#58981=CARTESIAN_POINT ( 'NONE',  ( 0.07093568767341934533, -0.9480374005119349690, 1.779628194860154222 ) ) ;
#58982=CARTESIAN_POINT ( 'NONE',  ( 6.146048976554097543, 0.5551056870855082259, 1.649627438850902017 ) ) ;
#58983=CARTESIAN_POINT ( 'NONE',  ( 4.616876278103482001, -0.1136277499396514262, 2.289655339347085317 ) ) ;
#58985=CARTESIAN_POINT ( 'NONE',  ( 2.343484645521694887, 1.840739972059933560, 0.04548452486473342216 ) ) ;
#58988=CARTESIAN_POINT ( 'NONE',  ( 2.713660727937649231, -1.805999004224107418, 0.2657717501357085843 ) ) ;
#58989=CARTESIAN_POINT ( 'NONE',  ( 3.955704058034177351, -1.882473782773282700, -0.7231407674024927790 ) ) ;
#58991=CARTESIAN_POINT ( 'NONE',  ( 1.938691616020698172, 2.238021082172815479, 0.3313278802117639033 ) ) ;
#58993=CARTESIAN_POINT ( 'NONE',  ( 5.860410395878546730, 0.8502751990519905601, 1.926866089339970056 ) ) ;
#58995=CARTESIAN_POINT ( 'NONE',  ( 2.875506610227479332, -0.2054619808779626633, 2.060159609288146232 ) ) ;
#58998=CARTESIAN_POINT ( 'NONE',  ( 4.213620120093874988, 1.703795446819071691, 1.262174061880352305 ) ) ;
#59000=CARTESIAN_POINT ( 'NONE',  ( 0.5746741651161955122, -1.813631458699631160, -0.6500969746191431753 ) ) ;
#59006=CARTESIAN_POINT ( 'NONE',  ( 5.853796514643677007, -1.537196951383312804, -1.461068456062891041 ) ) ;
#59007=CARTESIAN_POINT ( 'NONE',  ( 2.362460971492767570, 0.8994288142968703825, 1.904360703123770149 ) ) ;
#59010=CARTESIAN_POINT ( 'NONE',  ( 6.385601346537729484, -1.752585461374029929, 0.6262014864842447848 ) ) ;
#59014=CARTESIAN_POINT ( 'NONE',  ( 0.5102161431939798986, -0.7575819503438313562, 1.980855387931411915 ) ) ;
#59017=CARTESIAN_POINT ( 'NONE',  ( 3.859774877264535053, -0.5717695562157121270, 1.876676618968641019 ) ) ;
#59018=CARTESIAN_POINT ( 'NONE',  ( 0.9894095316701527754, 1.906041449620498929, -1.019753361306941386 ) ) ;
#59022=CARTESIAN_POINT ( 'NONE',  ( 2.360927591450364904, 1.706848764895356085, -0.3387292939842252437 ) ) ;
#59025=CARTESIAN_POINT ( 'NONE',  ( 2.618517346670693247, 0.5404096030681636575, -1.942243668081746311 ) ) ;
#59028=CARTESIAN_POINT ( 'NONE',  ( 2.834795904189919558, 0.2398841137210059038, 1.956746676604983248 ) ) ;
#59029=CARTESIAN_POINT ( 'NONE',  ( 6.240485052285455581, 1.095381943021833449, -1.567431287326017664 ) ) ;
#59034=CARTESIAN_POINT ( 'NONE',  ( 2.508468462390922138, -2.014426205243079693, -0.1462163075645859234 ) ) ;
#59036=CARTESIAN_POINT ( 'NONE',  ( 5.175001447075725736, -2.170742607874641461, -0.7831926130325519431 ) ) ;
#59037=CARTESIAN_POINT ( 'NONE',  ( 6.549272904993657995, 1.707534169505098953, -0.9658701945045378157 ) ) ;
#59038=CARTESIAN_POINT ( 'NONE',  ( 3.256644689873238629, -0.5649923015349536115, -1.878667693404307171 ) ) ;
#59040=CARTESIAN_POINT ( 'NONE',  ( 0.9322677863709986079, -1.591319861332978425, -1.238319039483272599 ) ) ;
#59042=CARTESIAN_POINT ( 'NONE',  ( 0.8489989883206483512, -1.916807839401615476, -0.8996751459469201073 ) ) ;
#59045=CARTESIAN_POINT ( 'NONE',  ( 1.851249556194194179, 1.836288347861175785, -0.1344999175661651392 ) ) ;
#59047=CARTESIAN_POINT ( 'NONE',  ( 3.081267818761534549, 1.592661989535900657, 1.236799713577160231 ) ) ;
#59049=CARTESIAN_POINT ( 'NONE',  ( 2.549219474610735947, 0.2639673528169217964, 2.104066465523121376 ) ) ;
#59053=CARTESIAN_POINT ( 'NONE',  ( 4.552062217129227761, 2.060418430787996691, -0.04653940209857834048 ) ) ;
#59056=CARTESIAN_POINT ( 'NONE',  ( 1.751249726499287673, 1.836263021919124050, -0.1365115386888632321 ) ) ;
#59058=CARTESIAN_POINT ( 'NONE',  ( -0.02244404828160087226, 1.995160441984781041, -2.602654351998904492 ) ) ;
#59061=CARTESIAN_POINT ( 'NONE',  ( 1.612255294781844706, -2.189918024983358080, 0.2725913246661854084 ) ) ;
#59062=CARTESIAN_POINT ( 'NONE',  ( 2.671453201960610091, 0.1136055399131811194, -2.259690131287622084 ) ) ;
#59064=CARTESIAN_POINT ( 'NONE',  ( 3.216879062660949362, 1.425012358211204422, -1.118398921490076026 ) ) ;
#59065=CARTESIAN_POINT ( 'NONE',  ( 2.975699994382564828, -0.7717752754876210375, 1.753554302899827277 ) ) ;
#59066=CARTESIAN_POINT ( 'NONE',  ( 3.965334771736851671, 1.774175476309115984, 1.066894043611272824 ) ) ;
#59068=CARTESIAN_POINT ( 'NONE',  ( 2.535955197907293179, 0.9309914139831111379, -1.737806310995954728 ) ) ;
#59069=CARTESIAN_POINT ( 'NONE',  ( 6.445928676245076261, 0.7346846062235148356, -1.781103304711729729 ) ) ;
#59070=CARTESIAN_POINT ( 'NONE',  ( 3.766346201128992988, -1.256895078192099335, 1.385637336983977397 ) ) ;
#59072=CARTESIAN_POINT ( 'NONE',  ( 2.016686958704193344, -1.090287029490369930, -2.033897785187769536 ) ) ;
#59074=CARTESIAN_POINT ( 'NONE',  ( 3.806960202730264253, -1.522499362102507359, 1.069998817686746984 ) ) ;
#59079=CARTESIAN_POINT ( 'NONE',  ( 0.7683615598204245334, 1.039662503867449184, 1.831484773650635223 ) ) ;
#59082=CARTESIAN_POINT ( 'NONE',  ( 6.889893180375397996, -0.9309023296741396614, 1.948985471107896439 ) ) ;
#59083=CARTESIAN_POINT ( 'NONE',  ( 2.127334043950947606, 1.896359100603739911, 0.9491756072362851349 ) ) ;
#59084=CARTESIAN_POINT ( 'NONE',  ( 0.1760434994887878080, 1.997199259934297366, -0.3004917578056826022 ) ) ;
#59088=CARTESIAN_POINT ( 'NONE',  ( 0.8784639925019833706, -1.201575844224999301, 1.796657101444132154 ) ) ;
#59093=CARTESIAN_POINT ( 'NONE',  ( 4.821500071095637274, -1.429446227384461032, -1.422610148874188463 ) ) ;
#59097=CARTESIAN_POINT ( 'NONE',  ( 0.4446536212460248105, 2.256715800172736763, 0.1630166291790128841 ) ) ;
#59101=CARTESIAN_POINT ( 'NONE',  ( 6.257435441360899908, 1.928747933193178721, -0.5880367767025842518 ) ) ;
#59103=CARTESIAN_POINT ( 'NONE',  ( 6.883263157960358924, 4.692138088316172073, 2.616388454592593504 ) ) ;
#59105=CARTESIAN_POINT ( 'NONE',  ( 3.281609485064349130, 1.095178418435642120, 1.332575575002497681 ) ) ;
#59108=CARTESIAN_POINT ( 'NONE',  ( 1.229378055282577042, -1.117200307070218779, -1.372552531265440523 ) ) ;
#59110=CARTESIAN_POINT ( 'NONE',  ( 2.227199469478642335, 1.799111979166287512, 0.9032904990664193390 ) ) ;
#59111=CARTESIAN_POINT ( 'NONE',  ( 6.883263157960401557, -0.003972766660575013931, 2.046037087719231096 ) ) ;
#59112=CARTESIAN_POINT ( 'NONE',  ( 4.753059971535213535, -1.774748228059085164, 1.311344899593884561 ) ) ;
#59118=CARTESIAN_POINT ( 'NONE',  ( 4.565154201998150363, -1.702539431995837349, 1.263830167178958463 ) ) ;
#59119=CARTESIAN_POINT ( 'NONE',  ( 2.460564738353550496, -1.930424690641812768, -0.5826366834433827080 ) ) ;
#59120=CARTESIAN_POINT ( 'NONE',  ( 2.882852291059742278, -1.675512013591500482, -0.6893320933419128105 ) ) ;
#59124=CARTESIAN_POINT ( 'NONE',  ( 0.1802491246630563149, -1.813337052076903877, -0.4591185353455888296 ) ) ;
#59126=CARTESIAN_POINT ( 'NONE',  ( 5.830640656690653678, 1.760721658632548037, 0.4824517239352192344 ) ) ;
#59128=CARTESIAN_POINT ( 'NONE',  ( 2.729585477426241802, 0.6851132086851609015, -1.789222977413899462 ) ) ;
#59136=CARTESIAN_POINT ( 'NONE',  ( 2.777707764728345907, 0.3069055913166895966, -2.098134212408508059 ) ) ;
#59137=CARTESIAN_POINT ( 'NONE',  ( -0.1296875068448125057, 0.2507808023153486054, -1.861542470327881560 ) ) ;
#59139=CARTESIAN_POINT ( 'NONE',  ( 4.762937738300905721, -1.759534068222264436, -0.8891730789123506451 ) ) ;
#59140=CARTESIAN_POINT ( 'NONE',  ( 6.345967646908174054, -1.254484226688237447, -1.443505786478386899 ) ) ;
#59142=CARTESIAN_POINT ( 'NONE',  ( -0.03531552556956805977, -2.054970391365168680, -0.5093743926467135807 ) ) ;
#59144=CARTESIAN_POINT ( 'NONE',  ( 1.908725956546155178, 0.6474277305483535638, 1.966616875269424192 ) ) ;
#59145=CARTESIAN_POINT ( 'NONE',  ( 2.255715180780485607, 0.8305992003537970847, 1.755491392210324353 ) ) ;
#59149=CARTESIAN_POINT ( 'NONE',  ( 4.066417572287989834, -1.950679019168543471, -0.7525511210752598990 ) ) ;
#59152=CARTESIAN_POINT ( 'NONE',  ( 0.8909134567714148689, -0.04341352697850982267, -1.811128585712480366 ) ) ;
#59154=CARTESIAN_POINT ( 'NONE',  ( 5.321004863918796346, 2.037934703285459115, 0.8473243778325880715 ) ) ;
#59156=CARTESIAN_POINT ( 'NONE',  ( 3.680891063843365174, -2.126115503207156809, -0.5908918699835326027 ) ) ;
#59159=CARTESIAN_POINT ( 'NONE',  ( 2.754443878939544454, 1.898071056134968959, 0.2320119769325945103 ) ) ;
#59161=CARTESIAN_POINT ( 'NONE',  ( 4.826661161267837841, -1.354893614093263254, 1.565527137264411728 ) ) ;
#59163=CARTESIAN_POINT ( 'NONE',  ( 2.395597313961893349, 1.670541196947441520, 1.371929806955954012 ) ) ;
#59164=CARTESIAN_POINT ( 'NONE',  ( 5.355090213057959403, 0.4282289882464126451, -2.149144931432686256 ) ) ;
#59172=CARTESIAN_POINT ( 'NONE',  ( 5.946161111532238586, -0.9360204806616537754, 1.846680006623670156 ) ) ;
#59173=CARTESIAN_POINT ( 'NONE',  ( 4.863854859025781074, 1.905264070129700782, -0.2845116402651908794 ) ) ;
#59174=CARTESIAN_POINT ( 'NONE',  ( 0.2457205463545810431, 1.994068899247893434, -0.2986513045247774500 ) ) ;
#59178=CARTESIAN_POINT ( 'NONE',  ( 5.629738194587773137, 1.899041559284548208, -0.5217042529989719402 ) ) ;
#59180=CARTESIAN_POINT ( 'NONE',  ( 6.714806895146447907, -0.1657305019511661481, 2.255884130952827249 ) ) ;
#59181=CARTESIAN_POINT ( 'NONE',  ( 5.180226163740526246, -1.011166736308216629, 1.519887457628710248 ) ) ;
#59189=CARTESIAN_POINT ( 'NONE',  ( 2.278628554356322500, 1.682734121078124812, -0.7478279864501293783 ) ) ;
#59190=CARTESIAN_POINT ( 'NONE',  ( 0.06508986333318785011, -1.615617207129100397, 1.200762793324720690 ) ) ;
#59191=CARTESIAN_POINT ( 'NONE',  ( 0.5624050986996537160, 1.909334820886617656, -1.279222687617764809 ) ) ;
#59192=CARTESIAN_POINT ( 'NONE',  ( 5.629730433169950921, 1.891637868780412068, -0.5196590155819302836 ) ) ;
#59197=CARTESIAN_POINT ( 'NONE',  ( 1.066094891556510271, -1.323660828648763221, 1.618394379614082723 ) ) ;
#59198=CARTESIAN_POINT ( 'NONE',  ( 1.147088892781012781, -1.472398045354219365, -1.153743250124287689 ) ) ;
#59199=CARTESIAN_POINT ( 'NONE',  ( 1.757185253014027282, -2.006138798620077157, -0.2004061740628823030 ) ) ;
#59201=CARTESIAN_POINT ( 'NONE',  ( 2.348798421458723862, 0.4629176777091792983, -1.677682632058958845 ) ) ;
#59205=CARTESIAN_POINT ( 'NONE',  ( 3.263966975432155415, 0.7763617936313322865, 1.540355606630551710 ) ) ;
#59206=CARTESIAN_POINT ( 'NONE',  ( 2.577880719133851084, -1.123996537731044354, 1.881222605751430521 ) ) ;
#59207=CARTESIAN_POINT ( 'NONE',  ( 5.145248760827346501, -1.894204247122273088, 1.132176536499051700 ) ) ;
#59209=CARTESIAN_POINT ( 'NONE',  ( 2.624086282063769815, 2.129961278301984784, -0.4196836606994054364 ) ) ;
#59210=CARTESIAN_POINT ( 'NONE',  ( 1.242498012622397674, 0.3540479964400863877, 1.790853789395550955 ) ) ;
#59211=CARTESIAN_POINT ( 'NONE',  ( 3.239577248433673784, 0.5100137816880914166, -2.054909399002705861 ) ) ;
#59212=CARTESIAN_POINT ( 'NONE',  ( 6.539320575229287336, 0.5820952121784334077, 2.049435377300548033 ) ) ;
#59214=CARTESIAN_POINT ( 'NONE',  ( 3.491970780479057179, -2.289775125716007054, -0.1112369151145074092 ) ) ;
#59218=CARTESIAN_POINT ( 'NONE',  ( 5.584718243131947091, -1.410645330893144589, 1.715908544892131626 ) ) ;
#59224=CARTESIAN_POINT ( 'NONE',  ( 4.623672751230786027, 0.3474658942751900903, 1.986100912583692812 ) ) ;
#59226=CARTESIAN_POINT ( 'NONE',  ( 3.854389151762872778, -2.059979072249884080, -0.1062074158154867054 ) ) ;
#59231=CARTESIAN_POINT ( 'NONE',  ( 6.052700813158569559, -1.877759139263988297, -1.129571069393126459 ) ) ;
#59232=CARTESIAN_POINT ( 'NONE',  ( 3.094375128876575065, -0.3905979561782264575, 1.978050703236901686 ) ) ;
#59233=CARTESIAN_POINT ( 'NONE',  ( 2.718100415690410721, 1.734538518968967935, 0.6181264464550640936 ) ) ;
#59235=CARTESIAN_POINT ( 'NONE',  ( 6.458013382736495167, 1.820430347099718293, -0.1376817787434730933 ) ) ;
#59236=CARTESIAN_POINT ( 'NONE',  ( -0.08672817704761734414, -1.422268874607252043, -1.807091132531572608 ) ) ;
#59238=CARTESIAN_POINT ( 'NONE',  ( 5.911039803662155201, 1.992093809783651803, 1.072660102914186897 ) ) ;
#59240=CARTESIAN_POINT ( 'NONE',  ( 1.946058636591390334, 0.8049280153260234272, -1.946384432229040673 ) ) ;
#59250=CARTESIAN_POINT ( 'NONE',  ( 2.039458538997685366, 0.004855507148140979744, 2.120778211687989856 ) ) ;
#59251=CARTESIAN_POINT ( 'NONE',  ( 2.672393786618231015, 2.210292516208379521, -0.2222851140616446397 ) ) ;
#59252=CARTESIAN_POINT ( 'NONE',  ( 0.08304785351339466493, -2.141800023564765620, -0.5316218738360134477 ) ) ;
#59255=CARTESIAN_POINT ( 'NONE',  ( 4.475024536774164119, 1.792854848340214025, 0.7970393728587571447 ) ) ;
#59265=CARTESIAN_POINT ( 'NONE',  ( 3.375340920106313813, -1.871962376360849056, -0.9962781187466958066 ) ) ;
#59267=CARTESIAN_POINT ( 'NONE',  ( 5.278265135069068137, -1.204163492603943064, 1.795060720813673738 ) ) ;
#59268=CARTESIAN_POINT ( 'NONE',  ( 4.089279031174639201, -0.7008038172400687937, 1.702867937621636463 ) ) ;
#59269=CARTESIAN_POINT ( 'NONE',  ( 4.909388789075159742, -1.913262893431907141, 0.6371506334161003426 ) ) ;
#59273=CARTESIAN_POINT ( 'NONE',  ( 6.544851825567233661, -1.402524398529688021, -1.030163739638074727 ) ) ;
#59274=CARTESIAN_POINT ( 'NONE',  ( 6.827182134110200806, 1.308106637204756728, 1.828351192278207638 ) ) ;
#59277=CARTESIAN_POINT ( 'NONE',  ( 4.557600102482579629, 0.4766696971462945909, -2.108333899287537339 ) ) ;
#59278=CARTESIAN_POINT ( 'NONE',  ( 5.202499893966790800, -1.423744420606623429, -1.427717849564233532 ) ) ;
#59280=CARTESIAN_POINT ( 'NONE',  ( 3.186554565756247737, -2.129457467500107004, -0.3711038070777841202 ) ) ;
#59282=CARTESIAN_POINT ( 'NONE',  ( 3.673081450605990117, 0.05180205286909286139, -1.970847691630872811 ) ) ;
#59283=CARTESIAN_POINT ( 'NONE',  ( 0.2401087780563165297, 2.186128513634697512, 0.1550312349237955856 ) ) ;
#59284=CARTESIAN_POINT ( 'NONE',  ( 0.9214421848816763960, 2.133375822355741303, 0.8800392910873405805 ) ) ;
#59285=CARTESIAN_POINT ( 'NONE',  ( 2.952472966291960876, 0.6911811108033919515, 1.941568756818631725 ) ) ;
#59286=CARTESIAN_POINT ( 'NONE',  ( 5.108904621496645149, -0.2812511558281989288, 1.921465535368711786 ) ) ;
#59295=CARTESIAN_POINT ( 'NONE',  ( 2.028631293930313717, 1.270571802522667992, -1.804104215285810886 ) ) ;
#59297=CARTESIAN_POINT ( 'NONE',  ( 6.543807102324334934, 1.350441955444921849, 1.423202910149905298 ) ) ;
#59302=CARTESIAN_POINT ( 'NONE',  ( 0.1749903794560410675, 1.362372954287846882, -2.209288650253756536 ) ) ;
#59304=CARTESIAN_POINT ( 'NONE',  ( 5.718664505737725001, -0.04093049815006092468, 1.840854889930729543 ) ) ;
#59306=CARTESIAN_POINT ( 'NONE',  ( 2.764585236803930979, -1.422233405468891210, 1.491712647946776826 ) ) ;
#59310=CARTESIAN_POINT ( 'NONE',  ( 6.398696098476772676, -2.079943653215409416, -0.4123558718646391785 ) ) ;
#59314=CARTESIAN_POINT ( 'NONE',  ( 0.6025036485793239249, -0.6938342907959176298, -1.940726168717278322 ) ) ;
#59317=CARTESIAN_POINT ( 'NONE',  ( 2.347915429038241353, -0.7989592750466242288, 1.680985684562475990 ) ) ;
#59318=CARTESIAN_POINT ( 'NONE',  ( 4.686955257832659427, 1.367739038236553517, 1.232883728221023212 ) ) ;
#59324=CARTESIAN_POINT ( 'NONE',  ( 4.371826309796801979, 2.140994599346605742, -0.5347268394074317088 ) ) ;
#59325=CARTESIAN_POINT ( 'NONE',  ( 6.397788901632932124, -0.7711469528366134973, 2.127058432633963658 ) ) ;
#59327=CARTESIAN_POINT ( 'NONE',  ( 0.5625819312903357350, 0.5574351770905332515, 1.829310545699929458 ) ) ;
#59328=CARTESIAN_POINT ( 'NONE',  ( 0.1632964843477149597, 1.879801964727344732, -0.7303121171872913875 ) ) ;
#59333=CARTESIAN_POINT ( 'NONE',  ( 5.901015568784107046, -0.2851453878830525479, -1.890788771128081969 ) ) ;
#59336=CARTESIAN_POINT ( 'NONE',  ( 0.7076149179639171782, -1.862046558926268913, 0.1791945732521060819 ) ) ;
#59337=CARTESIAN_POINT ( 'NONE',  ( 2.958220528980558761, -1.197304571117228100, 1.622486353517027968 ) ) ;
#59339=CARTESIAN_POINT ( 'NONE',  ( 4.160836958300685673, -1.560740793797481318, 1.414261741400888006 ) ) ;
#59344=CARTESIAN_POINT ( 'NONE',  ( 3.164323975240455944, 2.019972749466778073, -0.004219792236043878007 ) ) ;
#59347=CARTESIAN_POINT ( 'NONE',  ( 4.059979352932830743, 2.145800628424157974, -0.2601280725000321148 ) ) ;
#59351=CARTESIAN_POINT ( 'NONE',  ( 2.295604378506800103, -1.940070289243904567, 0.9748468494522060102 ) ) ;
#59354=CARTESIAN_POINT ( 'NONE',  ( 0.8547319020580852467, 0.3593373433725781108, -1.805665335529122784 ) ) ;
#59356=CARTESIAN_POINT ( 'NONE',  ( 1.663894474538109236, 1.130263417742288112, 1.877492182091732076 ) ) ;
#59357=CARTESIAN_POINT ( 'NONE',  ( 6.983263157960331036, 2.967600560354208383, 2.406739638166929041 ) ) ;
#59358=CARTESIAN_POINT ( 'NONE',  ( 3.256942907105137230, -1.714491093362701335, 1.476422526664717072 ) ) ;
#59360=CARTESIAN_POINT ( 'NONE',  ( 4.487517715496184501, -0.5331711073110931842, 1.944729879240604253 ) ) ;
#59366=CARTESIAN_POINT ( 'NONE',  ( 4.815556489234497306, -1.735627832820924477, 0.3447801454335273630 ) ) ;
#59369=CARTESIAN_POINT ( 'NONE',  ( 0.2179827029432715169, -2.065224962065722369, 0.4112614876821736321 ) ) ;
#59373=CARTESIAN_POINT ( 'NONE',  ( 6.503528962204017994, -1.955192063461574259, 0.4926555484118036454 ) ) ;
#59374=CARTESIAN_POINT ( 'NONE',  ( 5.273626195773981173, 0.3454419319289269708, -1.778163250140889717 ) ) ;
#59379=CARTESIAN_POINT ( 'NONE',  ( 4.153091690245942047, -1.555063956268587066, -1.039456662654779207 ) ) ;
#59380=CARTESIAN_POINT ( 'NONE',  ( 4.082924941702062327, 1.964217522864346810, 0.6541895251909736198 ) ) ;
#59388=CARTESIAN_POINT ( 'NONE',  ( 3.859774877264535053, -0.5717695562157121270, 1.876676618968641019 ) ) ;
#59389=CARTESIAN_POINT ( 'NONE',  ( 1.511092056569414366, 2.013677475703846476, 0.1017375232199163593 ) ) ;
#59393=CARTESIAN_POINT ( 'NONE',  ( 0.8076147168173102298, -1.862120749842037570, 0.1771838942275505424 ) ) ;
#59395=CARTESIAN_POINT ( 'NONE',  ( 3.287361135653954491, 0.04523670859641867187, -2.012844072734306433 ) ) ;
#59397=CARTESIAN_POINT ( 'NONE',  ( 3.831750911750389399, 0.7112487137725398423, -1.994330698664834589 ) ) ;
#59399=CARTESIAN_POINT ( 'NONE',  ( 5.406714943436663035, 0.5975561702324573288, 1.982271326387271770 ) ) ;
#59401=CARTESIAN_POINT ( 'NONE',  ( 0.1344724916707736029, 0.3614680779570299540, 2.059103226732065028 ) ) ;
#59403=CARTESIAN_POINT ( 'NONE',  ( 5.157177646623883227, -1.542991646335686973, -0.9753701268572569916 ) ) ;
#59410=CARTESIAN_POINT ( 'NONE',  ( 6.445967652843097362, -1.252902786447611883, -1.444740716957277904 ) ) ;
#59423=CARTESIAN_POINT ( 'NONE',  ( -0.1405533004718495238, 2.888985375434447889, -2.209311699518405447 ) ) ;
#59426=CARTESIAN_POINT ( 'NONE',  ( 2.026157484158600752, 1.007934145216189625, 1.691802187876802810 ) ) ;
#59427=CARTESIAN_POINT ( 'NONE',  ( 3.234000073275579812, 2.016598147164900823, -0.002828922958116042007 ) ) ;
#59429=CARTESIAN_POINT ( 'NONE',  ( 6.727182134110222478, 4.688348259194305534, 2.751590707055273199 ) ) ;
#59431=CARTESIAN_POINT ( 'NONE',  ( 3.627062487484993714, -2.024900418628313936, 0.8384617360315260726 ) ) ;
#59433=CARTESIAN_POINT ( 'NONE',  ( 1.922754896507544720, 1.796626380246616028, 0.6955005520668521291 ) ) ;
#59436=CARTESIAN_POINT ( 'NONE',  ( 0.2331563151865486683, 0.2490001740663889407, -1.980811336351681273 ) ) ;
#59443=CARTESIAN_POINT ( 'NONE',  ( 5.530750200611445067, -1.661959182355336795, 0.7928504710919548337 ) ) ;
#59444=CARTESIAN_POINT ( 'NONE',  ( 2.666654630192913267, 0.6802043231916419241, 1.894807776549158218 ) ) ;
#59445=CARTESIAN_POINT ( 'NONE',  ( 4.253462032731039066, -2.272626950162641268, -0.3425954598320450906 ) ) ;
#59446=CARTESIAN_POINT ( 'NONE',  ( -0.1291982275798807533, 5.720674304969967316, -2.668085245563474484 ) ) ;
#59447=CARTESIAN_POINT ( 'NONE',  ( 3.555356577358064207, 1.464247429212956808, 1.148356018212342233 ) ) ;
#59450=EDGE_CURVE ( 'NONE', #185927, #82118, #83532, .T. ) ;
#59451=CARTESIAN_POINT ( 'NONE',  ( 6.398695753475230674, -1.876852914212179035, -0.3660984893600614520 ) ) ;
#59454=CARTESIAN_POINT ( 'NONE',  ( 5.882390464068013358, -0.3075192527470702042, -2.067890480286633803 ) ) ;
#59458=CARTESIAN_POINT ( 'NONE',  ( 5.918504666124354330, 1.153338095414379261, -1.282764499605532738 ) ) ;
#59460=CARTESIAN_POINT ( 'NONE',  ( 1.687715598229572844, 1.441817134274174794, 0.9631580532376384784 ) ) ;
#59464=CARTESIAN_POINT ( 'NONE',  ( 5.998927374810688384, 0.4157333352466702769, 2.130747042934706403 ) ) ;
#59465=CARTESIAN_POINT ( 'NONE',  ( 4.019992336727182369, -0.9402185374879183932, -1.564826772493657536 ) ) ;
#59466=CARTESIAN_POINT ( 'NONE',  ( 2.412880707699780025, -1.519673801815585312, 1.240645658979570909 ) ) ;
#59470=CARTESIAN_POINT ( 'NONE',  ( 2.192179715818479036, 1.306768369893403170, 1.669877806752372740 ) ) ;
#59475=CARTESIAN_POINT ( 'NONE',  ( 0.5673436759025469733, 1.799520464221905369, 1.023488823764052480 ) ) ;
#59478=CARTESIAN_POINT ( 'NONE',  ( 3.475417139410865275, -1.959577385150832907, -1.046020024706290297 ) ) ;
#59480=CARTESIAN_POINT ( 'NONE',  ( 0.4582085974003520801, -2.167260061518965664, -0.7665384626166712456 ) ) ;
#59482=CARTESIAN_POINT ( 'NONE',  ( 6.877782380132525297, -2.002170498271789167, 0.4952429967341723804 ) ) ;
#59487=CARTESIAN_POINT ( 'NONE',  ( -0.2102771530458094895, 2.860119660625429550, -2.691685224125789588 ) ) ;
#59488=CARTESIAN_POINT ( 'NONE',  ( 2.520142033498268486, 1.128878695625197492, -1.304093658461308980 ) ) ;
#59489=CARTESIAN_POINT ( 'NONE',  ( 0.7785302072789467287, -0.4946362931835950327, -1.954778448132548752 ) ) ;
#59490=CARTESIAN_POINT ( 'NONE',  ( 3.235276958591898566, 2.298851035330526038, -0.002058992973525546142 ) ) ;
#59491=CARTESIAN_POINT ( 'NONE',  ( 2.987861924072153563, 1.597690390425403173, 1.602079265715735223 ) ) ;
#59492=CARTESIAN_POINT ( 'NONE',  ( 5.303390785913836503, 1.721067984382893545, 1.213575365270858075 ) ) ;
#59494=CARTESIAN_POINT ( 'NONE',  ( 4.112378888775404917, 1.252788995219549895, -1.250258383314418520 ) ) ;
#59496=CARTESIAN_POINT ( 'NONE',  ( 6.480031627576305020, -2.247188937338239434, -0.4521185302251101157 ) ) ;
#59497=CARTESIAN_POINT ( 'NONE',  ( 5.120983416928425846, -1.747193932927636029, 0.5808180576658967809 ) ) ;
#59501=CARTESIAN_POINT ( 'NONE',  ( 4.804715953495782621, 1.905792977913090214, 1.081705336968781239 ) ) ;
#59504=CARTESIAN_POINT ( 'NONE',  ( 5.758279222819879806, -2.070544812512797428, -0.003756845764937844813 ) ) ;
#59505=CARTESIAN_POINT ( 'NONE',  ( -0.08279552664090458758, -1.841734517378278424, 0.8216794407479923734 ) ) ;
#59507=CARTESIAN_POINT ( 'NONE',  ( 3.457566480858861091, 0.4672022665876771619, -1.868877010067309330 ) ) ;
#59510=CARTESIAN_POINT ( 'NONE',  ( -0.2102771530458277249, -0.008943344768331040057, -2.203482896658352175 ) ) ;
#59519=CARTESIAN_POINT ( 'NONE',  ( 0.7484013653801385724, -1.946605496936428370, -0.2438083268051088881 ) ) ;
#59522=CARTESIAN_POINT ( 'NONE',  ( 5.125427350195786325, 0.1941421753944693185, -1.952251141935714696 ) ) ;
#59525=CARTESIAN_POINT ( 'NONE',  ( 6.403215362905616992, 1.794359850238020693, 1.205212418099836480 ) ) ;
#59529=CARTESIAN_POINT ( 'NONE',  ( 6.731714608790520415, -1.285842040959904287, -1.494388255172361513 ) ) ;
#59530=CARTESIAN_POINT ( 'NONE',  ( 6.011065113327825671, 1.732079373560748481, 0.08140909068810914251 ) ) ;
#59532=CARTESIAN_POINT ( 'NONE',  ( 2.771223791512751333, 2.080116120148074010, -0.6901165687889164735 ) ) ;
#59533=CARTESIAN_POINT ( 'NONE',  ( 4.173124822893734986, -2.151704308474690741, -0.8341741560445140591 ) ) ;
#59534=CARTESIAN_POINT ( 'NONE',  ( 5.712203248095857333, -0.9225367590200548307, -1.842806303608224949 ) ) ;
#59535=CARTESIAN_POINT ( 'NONE',  ( 1.868985280173897756, 1.858391233338702042, -0.5634987755925959796 ) ) ;
#59538=CARTESIAN_POINT ( 'NONE',  ( 5.133110336712339183, 1.960249873928998410, 0.8093987030339530042 ) ) ;
#59540=CARTESIAN_POINT ( 'NONE',  ( 3.358046224211252095, 0.04667712216412447934, -2.016033814150198999 ) ) ;
#59546=CARTESIAN_POINT ( 'NONE',  ( 0.4162703231485806454, 1.261427835099769634, -1.320066674804179385 ) ) ;
#59551=CARTESIAN_POINT ( 'NONE',  ( 5.454002199308585652, 2.058645617578058751, -0.09870700237277732492 ) ) ;
#59556=CARTESIAN_POINT ( 'NONE',  ( 4.969401683643670076, -1.707372507963246022, -1.078548144515010909 ) ) ;
#59558=ORIENTED_EDGE ( 'NONE', *, *, #176737, .T. ) ;
#59562=CARTESIAN_POINT ( 'NONE',  ( 4.539950165727339559, 0.8829098278404916567, -1.862335138179547211 ) ) ;
#59563=CARTESIAN_POINT ( 'NONE',  ( 3.076796235938106694, -0.8146265060355702969, 1.844709937164575875 ) ) ;
#59567=CARTESIAN_POINT ( 'NONE',  ( 3.257046257486408969, 0.04465439498414420366, -2.016188763087948033 ) ) ;
#59571=CARTESIAN_POINT ( 'NONE',  ( 3.339220083777879378, -1.203169880011810022, 1.617570133648409847 ) ) ;
#59572=CARTESIAN_POINT ( 'NONE',  ( 2.132514540308296791, -1.644867172388216003, 0.8273176719292076875 ) ) ;
#59574=CARTESIAN_POINT ( 'NONE',  ( 1.419075709855713630, 1.546787523640520856, -1.712735560227249820 ) ) ;
#59576=CARTESIAN_POINT ( 'NONE',  ( 3.356853517036356038, -1.639235867460669072, 1.409173823127254366 ) ) ;
#59580=CARTESIAN_POINT ( 'NONE',  ( 3.093437905492165907, 1.279035344561373355, -1.909460003155829311 ) ) ;
#59583=CARTESIAN_POINT ( 'NONE',  ( 1.217418975555501826, -1.825842229346545498, 0.4062821374252246764 ) ) ;
#59584=CARTESIAN_POINT ( 'NONE',  ( 5.559438140644474835, 0.3852295531507047843, -1.933300702130675397 ) ) ;
#59588=CARTESIAN_POINT ( 'NONE',  ( 0.8564375766340023288, 2.204168734417511821, -0.1118928034387969561 ) ) ;
#59592=CARTESIAN_POINT ( 'NONE',  ( 6.539320575229292665, 2.014857154840712372, 2.506613887083661840 ) ) ;
#59593=CARTESIAN_POINT ( 'NONE',  ( 5.330923369760363961, 0.1444485787395009269, 1.966219458991929514 ) ) ;
#59594=CARTESIAN_POINT ( 'NONE',  ( 5.127664261384059508, -2.192653808335935928, 0.7197182627937804833 ) ) ;
#59595=CARTESIAN_POINT ( 'NONE',  ( 6.092234697878679661, 0.9164522128973868753, -1.619700000576968391 ) ) ;
#59596=CARTESIAN_POINT ( 'NONE',  ( 3.502832280938583676, 0.4964207669093263497, 2.001847840641638232 ) ) ;
#59604=CARTESIAN_POINT ( 'NONE',  ( 5.600102540861260358, 0.8850759393619503923, -1.982774263332246489 ) ) ;
#59605=CARTESIAN_POINT ( 'NONE',  ( 3.046111529846948329, 0.9110102549910354952, 1.799122713138465279 ) ) ;
#59608=CARTESIAN_POINT ( 'NONE',  ( 4.124425300631988200, 0.09459923933386081563, 1.838956108544815171 ) ) ;
#59610=CARTESIAN_POINT ( 'NONE',  ( 6.620655732516613767, 2.976578140159558128, 2.379908536877679559 ) ) ;
#59611=CARTESIAN_POINT ( 'NONE',  ( 6.146043800834426918, 0.6857851511376764631, 2.081541312870714311 ) ) ;
#59612=CARTESIAN_POINT ( 'NONE',  ( 0.1247927721447598948, 7.629137130509083597, -2.455404827119290978 ) ) ;
#59613=CARTESIAN_POINT ( 'NONE',  ( 0.5622849326936694148, 2.237558834470813274, -0.3334926475991057959 ) ) ;
#59620=CARTESIAN_POINT ( 'NONE',  ( 0.7074158718562081338, -1.761916611671160204, 0.1673130110368889201 ) ) ;
#59621=CARTESIAN_POINT ( 'NONE',  ( 5.443998933236983362, -1.278728028966215957, -1.554778559382914871 ) ) ;
#59623=CARTESIAN_POINT ( 'NONE',  ( 4.172956468465331525, -1.964154803760146617, -0.7601757144085323770 ) ) ;
#59624=CARTESIAN_POINT ( 'NONE',  ( 3.690956203553748427, 1.644769065816154008, 0.9816995294186120491 ) ) ;
#59625=CARTESIAN_POINT ( 'NONE',  ( 4.545333244533083850, 1.760332640988309993, -0.8834868730601146414 ) ) ;
#59626=CARTESIAN_POINT ( 'NONE',  ( 5.572523036771587890, 0.8223149429010238043, 1.845017218462653208 ) ) ;
#59627=CARTESIAN_POINT ( 'NONE',  ( 1.955717210371358483, 1.865846021326333926, -0.1348392221205765851 ) ) ;
#59628=CARTESIAN_POINT ( 'NONE',  ( 4.705503516419368815, -0.4560151319670002756, 1.663429522189649790 ) ) ;
#59629=CARTESIAN_POINT ( 'NONE',  ( 1.494246876672610025, -1.020364814108923213, 1.617233793950809906 ) ) ;
#59630=CARTESIAN_POINT ( 'NONE',  ( 2.262606014870732096, 0.9450075053254001212, 1.994452002680577429 ) ) ;
#59633=CARTESIAN_POINT ( 'NONE',  ( 6.619590441841329387, 0.3365870006281460047, -1.932621868259084330 ) ) ;
#59641=CARTESIAN_POINT ( 'NONE',  ( 2.225130849662222410, -1.891980959128433781, -0.8411517639917851508 ) ) ;
#59646=CARTESIAN_POINT ( 'NONE',  ( 0.08268334464456467137, -1.317614589208983444, 1.530782303595918714 ) ) ;
#59651=CARTESIAN_POINT ( 'NONE',  ( 5.114611164699836010, 0.6351010243071940620, -1.913510948406547563 ) ) ;
#59653=CARTESIAN_POINT ( 'NONE',  ( 4.487445792895001340, -0.5051273088985311910, 1.847880739403139572 ) ) ;
#59655=CARTESIAN_POINT ( 'NONE',  ( 2.788834510562918645, 1.878274557074947948, -1.128960604485473862 ) ) ;
#59658=CARTESIAN_POINT ( 'NONE',  ( 5.484640381798278952, -1.273743769317101648, 1.559065439997550762 ) ) ;
#59659=CARTESIAN_POINT ( 'NONE',  ( 1.494246876672610025, -1.020364814108923213, 1.617233793950809906 ) ) ;
#59661=CARTESIAN_POINT ( 'NONE',  ( 0.2808753465170962249, 1.674874268995883320, -1.122520385770640061 ) ) ;
#59663=CARTESIAN_POINT ( 'NONE',  ( 3.491813360781896858, -2.088456202509383797, -0.1002299605681444133 ) ) ;
#59665=CARTESIAN_POINT ( 'NONE',  ( 1.746655555778130253, -1.459509165399446529, 0.9187280511932097715 ) ) ;
#59675=CARTESIAN_POINT ( 'NONE',  ( 3.176200218816268350, 0.8167180202140277290, 1.616994655555709981 ) ) ;
#59679=CARTESIAN_POINT ( 'NONE',  ( 4.160681542540445754, 0.4872625442002316287, 1.744618836514327587 ) ) ;
#59683=CARTESIAN_POINT ( 'NONE',  ( 4.193699477585779434, -1.282400645549033547, -1.348940618851623974 ) ) ;
#59684=CARTESIAN_POINT ( 'NONE',  ( 1.546349530022947727, -1.353405651413071453, 1.355934989043396044 ) ) ;
#59685=CARTESIAN_POINT ( 'NONE',  ( 0.4811275135914867551, 1.705355465787803393, -0.6520327999673739550 ) ) ;
#59692=CARTESIAN_POINT ( 'NONE',  ( 5.998876245820001785, 0.3805640578184403822, 1.932138370648580628 ) ) ;
#59696=CARTESIAN_POINT ( 'NONE',  ( 0.7793769126323678575, 1.405529721366456597, 1.547827308177295746 ) ) ;
#59698=CARTESIAN_POINT ( 'NONE',  ( 5.122061974917812677, -1.030465543002171858, -1.627433240741954723 ) ) ;
#59700=CARTESIAN_POINT ( 'NONE',  ( 1.694096453153286497, -1.816434584207878622, -0.1825648128309723117 ) ) ;
#59701=CARTESIAN_POINT ( 'NONE',  ( 1.717678464306471087, -0.2677704892378242607, 2.190511422692428045 ) ) ;
#59703=CARTESIAN_POINT ( 'NONE',  ( 0.6680393924826667496, 1.910109291395128972, -0.09634788558426229943 ) ) ;
#59706=CARTESIAN_POINT ( 'NONE',  ( 6.877801621836153068, -1.911143888484008846, 0.4753377615324301253 ) ) ;
#59707=CARTESIAN_POINT ( 'NONE',  ( 2.929168808825276749, -1.306124965484034117, -1.437377093338227496 ) ) ;
#59709=CARTESIAN_POINT ( 'NONE',  ( 0.9310172746952742884, 0.9912447863934905623, 1.755501862388042067 ) ) ;
#59711=CARTESIAN_POINT ( 'NONE',  ( 6.104338052012460381, 1.858797879379699536, 0.09248701691148655812 ) ) ;
#59718=CARTESIAN_POINT ( 'NONE',  ( 2.964592600559623037, -2.025863808726846127, -0.8364240203130177687 ) ) ;
#59722=CARTESIAN_POINT ( 'NONE',  ( 2.437895498511342574, 0.8609710149188254391, -1.609920059450341778 ) ) ;
#59727=CARTESIAN_POINT ( 'NONE',  ( -0.02968770228140016343, 0.003472272166151618711, -1.826291111852257343 ) ) ;
#59730=CARTESIAN_POINT ( 'NONE',  ( 0.5043604530000692643, -0.6477430859608296343, -1.814464506502324159 ) ) ;
#59731=CARTESIAN_POINT ( 'NONE',  ( 5.735196368693616265, -0.04450293679344322767, -1.961403813732150780 ) ) ;
#59735=CARTESIAN_POINT ( 'NONE',  ( 4.739868811304373430, 2.185674081084403753, 0.1610935195608814985 ) ) ;
#59738=CARTESIAN_POINT ( 'NONE',  ( 3.959880360806608213, -0.6057208360459276353, 1.979630382156400303 ) ) ;
#59742=CARTESIAN_POINT ( 'NONE',  ( 4.500793239850611194, -2.254531372669385636, 0.4477389049844481272 ) ) ;
#59745=CARTESIAN_POINT ( 'NONE',  ( 0.2348727637096776621, 0.3982709639365061838, 2.257261336973298338 ) ) ;
#59746=CARTESIAN_POINT ( 'NONE',  ( 6.620655732516645742, 3.706282450693794139, 2.340867613974298767 ) ) ;
#59748=CARTESIAN_POINT ( 'NONE',  ( 5.050698599679353862, -1.641444558978710555, -1.037428038565652466 ) ) ;
#59752=CARTESIAN_POINT ( 'NONE',  ( 5.361546783204238942, -1.511448857895525855, -1.171587532507123441 ) ) ;
#59753=CARTESIAN_POINT ( 'NONE',  ( 6.036138234293757954, 0.8456279901550376454, -1.503183349252550371 ) ) ;
#59754=CARTESIAN_POINT ( 'NONE',  ( 5.208220363674559650, 1.197307938467083055, -1.622483861274232719 ) ) ;
#59758=CARTESIAN_POINT ( 'NONE',  ( 1.869195317527425404, 2.000202809997845499, -0.6082070056973082339 ) ) ;
#59759=CARTESIAN_POINT ( 'NONE',  ( 6.678955280633751102, -0.08981333502068940267, -1.767555964166868998 ) ) ;
#59760=CARTESIAN_POINT ( 'NONE',  ( 5.326796142270829648, 0.8146286751641409474, -1.844708973168760924 ) ) ;
#59762=CARTESIAN_POINT ( 'NONE',  ( 3.222906779550426926, 0.05642716604136116532, 2.291727194984194860 ) ) ;
#59763=CARTESIAN_POINT ( 'NONE',  ( 1.728031430807571267, 0.1683455491279534644, 1.732166925338991303 ) ) ;
#59765=CARTESIAN_POINT ( 'NONE',  ( 3.023802379225454473, -0.4096935937694180518, 2.080477853870852378 ) ) ;
#59767=CARTESIAN_POINT ( 'NONE',  ( 2.688496201417677867, -0.9952141288376895600, -1.419535560660119655 ) ) ;
#59769=CARTESIAN_POINT ( 'NONE',  ( 1.486513762117396498, 1.792272468715813138, 0.5009694556475997596 ) ) ;
#59770=CARTESIAN_POINT ( 'NONE',  ( 2.313135284333038832, -1.679484837851461965, 1.376015783590480934 ) ) ;
#59771=CARTESIAN_POINT ( 'NONE',  ( 3.837125247982266174, -1.679222704393277921, -1.116210984008485507 ) ) ;
#59772=CARTESIAN_POINT ( 'NONE',  ( 5.000000000000003553, -2.717005030479747438E-13, -2.052068128417942727 ) ) ;
#59774=CARTESIAN_POINT ( 'NONE',  ( 6.586557377926046897, -1.889895688126231876, -0.3729288831034789364 ) ) ;
#59778=CARTESIAN_POINT ( 'NONE',  ( 3.568779976319371272, 0.8023129380761647722, 2.071619486725768677 ) ) ;
#59784=CARTESIAN_POINT ( 'NONE',  ( 6.099871961099720963, 1.531114646448136218, 1.609653004599376658 ) ) ;
#59785=CARTESIAN_POINT ( 'NONE',  ( 4.738696794244872557, -1.902450960283699422, -0.4786090228221794307 ) ) ;
#59789=CARTESIAN_POINT ( 'NONE',  ( 6.046200420459929781, 2.259369630126391471, 0.1200006983746708389 ) ) ;
#59792=CARTESIAN_POINT ( 'NONE',  ( 2.629405133799759486, 0.1038056934173016560, -2.060197576267445818 ) ) ;
#59796=CARTESIAN_POINT ( 'NONE',  ( 4.130043426961079511, 1.002751595458702738, -1.578879078160302818 ) ) ;
#59797=CARTESIAN_POINT ( 'NONE',  ( 2.566726881135486416, -0.8894074178381355944, 1.488501414198806883 ) ) ;
#59798=CARTESIAN_POINT ( 'NONE',  ( 0.04695162158900589161, -1.836028162657590501, 1.372410674757597704 ) ) ;
#59799=CARTESIAN_POINT ( 'NONE',  ( 1.097021799178355739, -0.5375665728563282508, -2.140183485690804410 ) ) ;
#59800=CARTESIAN_POINT ( 'NONE',  ( 6.246037776718591061, 0.6113502166280659900, 1.843275756764614082 ) ) ;
#59803=CARTESIAN_POINT ( 'NONE',  ( 0.1874999572450692098, -1.451030237095527475, 1.451031289061128993 ) ) ;
#59804=CARTESIAN_POINT ( 'NONE',  ( 0.1764080092822375156, 1.496053712750060383, 1.352152247781977179 ) ) ;
#59808=CARTESIAN_POINT ( 'NONE',  ( 6.399064592084179992, -0.9530083391863402031, -1.777013033299412292 ) ) ;
#59812=CARTESIAN_POINT ( 'NONE',  ( 4.934128534657983067, 0.9357288403324083292, -1.567518238613223813 ) ) ;
#59813=CARTESIAN_POINT ( 'NONE',  ( 1.958336283151569157, 2.200835622443702011, -0.1624582802550941507 ) ) ;
#59819=CARTESIAN_POINT ( 'NONE',  ( 0.8264327134144221487, -0.9118592345104499231, -1.802339519251413780 ) ) ;
#59823=CARTESIAN_POINT ( 'NONE',  ( 2.957670719111748614, -0.5886736602933821949, 1.765425544305933014 ) ) ;
#59825=CARTESIAN_POINT ( 'NONE',  ( 5.836564609439236939, 0.5826586670559866787, -1.930416874340326938 ) ) ;
#59829=CARTESIAN_POINT ( 'NONE',  ( 4.195794211080963620, -0.6966935528937777677, 1.687730213881050600 ) ) ;
#59833=CARTESIAN_POINT ( 'NONE',  ( 6.608749954595573683, 0.7741944705832277673, -1.861732896133998727 ) ) ;
#59834=CARTESIAN_POINT ( 'NONE',  ( 5.613187951484799321, -1.795345830453990654, 0.4073638586896133340 ) ) ;
#59835=CARTESIAN_POINT ( 'NONE',  ( 4.670747285963097184, -1.509779504925019999, 1.745381082733918676 ) ) ;
#59837=CARTESIAN_POINT ( 'NONE',  ( 6.802040682177005415, -2.161276877365316818, 0.04550429416337595928 ) ) ;
#59838=CARTESIAN_POINT ( 'NONE',  ( 1.944774020950320592, -1.561091384877069554, -1.155077030050962295 ) ) ;
#59839=ADVANCED_FACE ( 'NONE', ( #90351 ), #164986, .T. ) ;
#59840=CARTESIAN_POINT ( 'NONE',  ( 5.975955848901470802, 2.022625890308630048, 1.091648031176053468 ) ) ;
#59843=CARTESIAN_POINT ( 'NONE',  ( 4.153091690245942047, -1.555063956268587066, -1.039456662654779207 ) ) ;
#59845=CARTESIAN_POINT ( 'NONE',  ( 2.795058504854182946, -0.1448928079688660830, -1.906987441340234568 ) ) ;
#59848=CARTESIAN_POINT ( 'NONE',  ( 4.354274438496381627, 2.206422198305586058, -0.05263853172451230661 ) ) ;
#59850=FACE_OUTER_BOUND ( 'NONE', #20221, .T. ) ;
#59853=CARTESIAN_POINT ( 'NONE',  ( 1.985558396190547858, 1.356547016436062014, 1.430631702862941168 ) ) ;
#59854=CARTESIAN_POINT ( 'NONE',  ( 2.292384291596425427, -0.9864983578860975211, 2.086231237977907327 ) ) ;
#59855=CARTESIAN_POINT ( 'NONE',  ( 3.051168888765115828, 1.684027830550902882, -1.006202029777767848 ) ) ;
#59857=CARTESIAN_POINT ( 'NONE',  ( 6.104357437187505120, 2.059938769829409377, 0.1070097549743902060 ) ) ;
#59859=CARTESIAN_POINT ( 'NONE',  ( 4.048064755690682581, 0.9548552675892291175, 1.776167154503265566 ) ) ;
#59862=CARTESIAN_POINT ( 'NONE',  ( 4.663296154398564042, 1.879804967172087782, -0.7303043177912388328 ) ) ;
#59867=CARTESIAN_POINT ( 'NONE',  ( 2.044024736616629312, 1.494777392302085062, 1.574780046323517313 ) ) ;
#59870=CARTESIAN_POINT ( 'NONE',  ( 2.794054307841778773, -1.865266697571519972, -0.1415833504254116748 ) ) ;
#59871=CARTESIAN_POINT ( 'NONE',  ( 6.468072252983536607, 1.105043713804385153, 1.857642994352682653 ) ) ;
#59872=CARTESIAN_POINT ( 'NONE',  ( -0.02244404828160087226, 6.946777552644228138, -2.784171975256703124 ) ) ;
#59873=CARTESIAN_POINT ( 'NONE',  ( 6.827182134110172385, 0.001020705822878456353, 1.910856149448317165 ) ) ;
#59875=CARTESIAN_POINT ( 'NONE',  ( -0.1409997244346088141, 7.629137130509076492, -2.600278764091648487 ) ) ;
#59876=CARTESIAN_POINT ( 'NONE',  ( 3.914637684252043393, -0.6027250981219151038, -1.814865640613130493 ) ) ;
#59878=CARTESIAN_POINT ( 'NONE',  ( 4.012378993168019825, 1.251447367628313767, -1.251755930634059100 ) ) ;
#59879=CARTESIAN_POINT ( 'NONE',  ( 1.928230879603441750, -0.9027140558476205445, -1.685813393195116694 ) ) ;
#59883=CARTESIAN_POINT ( 'NONE',  ( 6.450803866275835574, -1.753708343991422502, -0.7711757456045026382 ) ) ;
#59885=CARTESIAN_POINT ( 'NONE',  ( 1.293514844328220281, -1.872496763586928514, 0.8835221827151735763 ) ) ;
#59887=CARTESIAN_POINT ( 'NONE',  ( 6.578970801323708706, -0.09418725797194843485, -1.868394071727994543 ) ) ;
#59888=CARTESIAN_POINT ( 'NONE',  ( 1.541335573940459058, -1.321205422867760548, -1.260230113935792318 ) ) ;
#59889=CARTESIAN_POINT ( 'NONE',  ( 6.129534211984397629, -2.079372889712034489, 0.7396383780838566846 ) ) ;
#59892=CARTESIAN_POINT ( 'NONE',  ( 3.104023224481029519, 0.7448178976848550681, -1.923671348419103921 ) ) ;
#59896=CARTESIAN_POINT ( 'NONE',  ( 0.4917760118960182170, 1.601382895956671826, 1.452064325093614716 ) ) ;
#59898=ORIENTED_EDGE ( 'NONE', *, *, #130874, .T. ) ;
#59899=CARTESIAN_POINT ( 'NONE',  ( 4.844224204019831781, -0.9789346907586125024, 1.824324395707350943 ) ) ;
#59901=CARTESIAN_POINT ( 'NONE',  ( 2.741676502816026595, -1.599691942034554337, -1.453933697666408120 ) ) ;
#59903=CARTESIAN_POINT ( 'NONE',  ( 2.947920495102425154, -1.358134161044775245, -1.495000266999703564 ) ) ;
#59904=CARTESIAN_POINT ( 'NONE',  ( 6.620655732516651071, 2.021119449029490589, 2.477762541108457839 ) ) ;
#59908=CARTESIAN_POINT ( 'NONE',  ( 1.059780186608853203, 1.205045252304644210, 1.616690996016925563 ) ) ;
#59910=CARTESIAN_POINT ( 'NONE',  ( 5.671465802443460547, 1.304529079428708549, 1.760837017921567771 ) ) ;
#59911=CARTESIAN_POINT ( 'NONE',  ( 5.115449499555525747, 1.566912803841558732, 1.096118974231160781 ) ) ;
#59915=CARTESIAN_POINT ( 'NONE',  ( 3.427361390312729572, -1.528753972193249933, -1.314983687342549556 ) ) ;
#59918=CARTESIAN_POINT ( 'NONE',  ( 5.825168945638790063, -0.03770542841243298970, 1.724543776939557960 ) ) ;
#59923=CARTESIAN_POINT ( 'NONE',  ( 4.077312411328878561, 1.762187477035919603, -0.6278270876356045749 ) ) ;
#59925=CARTESIAN_POINT ( 'NONE',  ( 1.129834432590616000, 1.996231214973245516, -0.5485114149718293142 ) ) ;
#59928=CARTESIAN_POINT ( 'NONE',  ( 6.252603509501785339, 1.792834410666717337, 0.2582872775454737591 ) ) ;
#59930=CARTESIAN_POINT ( 'NONE',  ( -0.08826282632121498772, -1.242921985031696153, -1.588411632956095110 ) ) ;
#59931=CARTESIAN_POINT ( 'NONE',  ( 0.1756362645438137582, 1.791864648875134636, -0.2657654445481233418 ) ) ;
#59934=VERTEX_POINT ( 'NONE', #94214 ) ;
#59936=CARTESIAN_POINT ( 'NONE',  ( 1.047228354049560828, 1.731870006261830630, -0.9216698261682305660 ) ) ;
#59938=CARTESIAN_POINT ( 'NONE',  ( 4.851152330137978197, 0.1832884931825354280, -1.906798003172151867 ) ) ;
#59940=CARTESIAN_POINT ( 'NONE',  ( 6.827182134110195477, 0.006757161851597697118, 1.710856279483467857 ) ) ;
#59946=CARTESIAN_POINT ( 'NONE',  ( 1.745224485312408813, -1.826185749030174499, 1.156423465944363294 ) ) ;
#59949=CARTESIAN_POINT ( 'NONE',  ( 0.05319811239242258627, 0.3688592364489845510, 2.088132107045739705 ) ) ;
#59950=CARTESIAN_POINT ( 'NONE',  ( 4.348545414961950684, 0.4871326187540457875, 1.759326811173238303 ) ) ;
#59953=CARTESIAN_POINT ( 'NONE',  ( 1.581257511629934775, 1.823016439315219062, -0.7507060404894276839 ) ) ;
#59954=CARTESIAN_POINT ( 'NONE',  ( 3.287273477832891366, 0.04233216220104508987, -1.912079899511004433 ) ) ;
#59957=CARTESIAN_POINT ( 'NONE',  ( 4.123468233510577896, 0.2432657155154849538, -1.954413393957514788 ) ) ;
#59959=CARTESIAN_POINT ( 'NONE',  ( 5.812047917624927784, 1.301047364602755829, -1.442011890679588904 ) ) ;
#59966=CARTESIAN_POINT ( 'NONE',  ( 4.459560945705238311, -1.480416612418914424, -1.210464771850598975 ) ) ;
#59967=CARTESIAN_POINT ( 'NONE',  ( 6.983263157960366563, -0.003091553303710344557, 1.945923119799706669 ) ) ;
#59970=CARTESIAN_POINT ( 'NONE',  ( 5.426436493548534301, -0.9073095142285032555, -1.797119830347380542 ) ) ;
#59973=CARTESIAN_POINT ( 'NONE',  ( 6.445924739416000193, 0.6936395621829589686, -1.688995215704327313 ) ) ;
#59974=CARTESIAN_POINT ( 'NONE',  ( 2.049362625460974030, 1.802418521853879962, -1.018503948505583789 ) ) ;
#59978=CARTESIAN_POINT ( 'NONE',  ( 6.332864056472936376, 0.1854757364097951722, 1.861418627818342664 ) ) ;
#59987=CARTESIAN_POINT ( 'NONE',  ( 3.973097536218972436, -1.716008982208137468, -0.2490561736530460535 ) ) ;
#59989=CARTESIAN_POINT ( 'NONE',  ( 2.202089267374872872, 0.7962392033929905910, -1.911209141678638090 ) ) ;
#59991=CARTESIAN_POINT ( 'NONE',  ( 3.620818518838536004, 0.3129716219542731936, 2.093870907184330221 ) ) ;
#59994=CARTESIAN_POINT ( 'NONE',  ( 1.323035253951538426, -1.778235669024318177, -0.8468731209588018505 ) ) ;
#59998=CARTESIAN_POINT ( 'NONE',  ( -0.1933232215488022709, -0.4202133615931051835, -1.872389726556406897 ) ) ;
#59999=CARTESIAN_POINT ( 'NONE',  ( 3.521668038933927658, -1.364967583988693889, -1.841414078927001041 ) ) ;
#60000=CARTESIAN_POINT ( 'NONE',  ( 0.2580658466875830337, 0.6954254843183352852, 1.688255465954719536 ) ) ;
#60001=CARTESIAN_POINT ( 'NONE',  ( 2.847809051801777791, -1.287500320553297994, -1.414207669007704116 ) ) ;
#60005=CARTESIAN_POINT ( 'NONE',  ( 1.318609283782465003, -0.7284450440303428254, -1.876953636963938354 ) ) ;
#60006=CARTESIAN_POINT ( 'NONE',  ( 2.114041031776827673, 1.956853317873577414, -0.1391692324632237410 ) ) ;
#60010=CARTESIAN_POINT ( 'NONE',  ( 4.646477879911859787, -1.679251869332079483, 1.245118527403435094 ) ) ;
#60011=CARTESIAN_POINT ( 'NONE',  ( 3.608038473134207891, -0.7167157551234564217, -1.618410677222481553 ) ) ;
#60013=CARTESIAN_POINT ( 'NONE',  ( 0.1995291103054769866, -0.5802879427523646161, 2.113158525371459096 ) ) ;
#60014=CARTESIAN_POINT ( 'NONE',  ( 5.208843366089195293, -0.2500283176610699210, 1.722145524253251514 ) ) ;
#60016=CARTESIAN_POINT ( 'NONE',  ( 6.293571109369822558, 1.706569967861866877, -1.540138442258129459 ) ) ;
#60018=CARTESIAN_POINT ( 'NONE',  ( 5.343005094570719038, -0.9615459055183853687, 1.442522970604209531 ) ) ;
#60020=CARTESIAN_POINT ( 'NONE',  ( 6.320782530974223157, -1.539933897815339403, 1.530818809132200142 ) ) ;
#60022=CARTESIAN_POINT ( 'NONE',  ( 0.1459223332197969736, 2.093306735845179567, -0.3175718533311999714 ) ) ;
#60023=CARTESIAN_POINT ( 'NONE',  ( 4.625000000000002665, -2.052068128417944504, 2.503915141160646116E-13 ) ) ;
#60026=CARTESIAN_POINT ( 'NONE',  ( 3.047785661706010174, 0.6947733606382737737, -1.796906316042534923 ) ) ;
#60028=CARTESIAN_POINT ( 'NONE',  ( 0.4346306299643958315, -1.193539479193185038, -1.873246666896864143 ) ) ;
#60033=CARTESIAN_POINT ( 'NONE',  ( 2.086886708931742884, -1.363721155840109889, 1.753348597404544185 ) ) ;
#60038=CARTESIAN_POINT ( 'NONE',  ( 1.231092510272915552, 2.014232830173094513, 0.09613330637052441840 ) ) ;
#60040=CARTESIAN_POINT ( 'NONE',  ( 5.371554553765571782, -0.3061699256626281840, 2.039728424269163121 ) ) ;
#60045=CARTESIAN_POINT ( 'NONE',  ( 0.3327835722091445070, -1.621720136574826610, 0.7089735832957798634 ) ) ;
#60046=CARTESIAN_POINT ( 'NONE',  ( 6.152912852923398290, 0.8997199139058277284, 1.482343192998013537 ) ) ;
#60047=CARTESIAN_POINT ( 'NONE',  ( 5.688919983501732780, 1.323409507385058914, 1.130498143038612513 ) ) ;
#60048=CARTESIAN_POINT ( 'NONE',  ( 2.665910428807946708, 1.228978066529669899, 1.934933738419620575 ) ) ;
#60050=CARTESIAN_POINT ( 'NONE',  ( 2.167674216824653222, -1.133089441918342599, 1.451089449600144521 ) ) ;
#60053=CARTESIAN_POINT ( 'NONE',  ( 2.573050890253928635, 0.09191801231544714790, -1.823395950357763695 ) ) ;
#60054=CARTESIAN_POINT ( 'NONE',  ( 3.815077410725797424, 1.076317812134291119, -1.704938119663282903 ) ) ;
#60057=CARTESIAN_POINT ( 'NONE',  ( 4.946364073002400552, 2.100128792357182750, 0.1576013620808654481 ) ) ;
#60060=CARTESIAN_POINT ( 'NONE',  ( 2.049362625460974030, 1.802418521853879962, -1.018503948505583789 ) ) ;
#60063=CARTESIAN_POINT ( 'NONE',  ( 4.459710115430675081, -1.639780234044617035, -1.344486126324248465 ) ) ;
#60064=CARTESIAN_POINT ( 'NONE',  ( 1.365712245162364225, 1.898099017218597195, -0.3287360691993664874 ) ) ;
#60071=CARTESIAN_POINT ( 'NONE',  ( 6.047156637250688860, 0.2094617991648151656, 2.110256208591613003 ) ) ;
#60072=CARTESIAN_POINT ( 'NONE',  ( 2.766744854014174138, -1.453255750356880371, 1.524405782528108766 ) ) ;
#60075=CARTESIAN_POINT ( 'NONE',  ( 5.998848716047340268, 0.3616406339099677014, 1.825274704766747913 ) ) ;
#60079=CARTESIAN_POINT ( 'NONE',  ( 0.1059362375676886209, 1.575662574916199210, 1.419458935296296520 ) ) ;
#60082=CARTESIAN_POINT ( 'NONE',  ( 2.541395235131336694, 1.794889867694851260, -0.7924082849640816661 ) ) ;
#60083=CARTESIAN_POINT ( 'NONE',  ( 1.182749364907993206, -2.109161078630458430, -0.4729781282231394490 ) ) ;
#60087=CARTESIAN_POINT ( 'NONE',  ( 2.519154997858559231, -1.001672848371559787, -1.422942596517995817 ) ) ;
#60092=CARTESIAN_POINT ( 'NONE',  ( 2.284529629648517801, -1.956262009633228605, 0.4871271731112236658 ) ) ;
#60093=CARTESIAN_POINT ( 'NONE',  ( -0.02968770228139669398, 7.629137130509076492, -2.426318643530885222 ) ) ;
#60096=CARTESIAN_POINT ( 'NONE',  ( 1.832829291326312005, 0.1914625595707402927, 1.962137882790424559 ) ) ;
#60098=CARTESIAN_POINT ( 'NONE',  ( 5.554919272666569263, 0.3793472168572444292, 1.874222000232607765 ) ) ;
#60102=EDGE_CURVE ( 'NONE', #124676, #39684, #118243, .T. ) ;
#60104=CARTESIAN_POINT ( 'NONE',  ( 1.154951149459724880, 0.3962062163746901677, 1.980246309512444070 ) ) ;
#60106=CARTESIAN_POINT ( 'NONE',  ( 6.194374175331438082, -2.295634644278636394, -0.2347168956345067892 ) ) ;
#60107=CARTESIAN_POINT ( 'NONE',  ( 5.793401095800717826, -1.774274828963496198, 0.8374297333502839225 ) ) ;
#60108=CARTESIAN_POINT ( 'NONE',  ( 3.080854412065773928, 1.845568107317007822, 0.6654098317215583203 ) ) ;
#60110=CARTESIAN_POINT ( 'NONE',  ( 0.6861729220449981348, 1.650083401500940239, 1.158686392676591570 ) ) ;
#60112=CARTESIAN_POINT ( 'NONE',  ( 1.218125882790439762, 1.038422275552937757, -1.845119264165562711 ) ) ;
#60115=CARTESIAN_POINT ( 'NONE',  ( 1.552429278155377679, -1.578373273985161473, -0.9476568548090894550 ) ) ;
#60118=CARTESIAN_POINT ( 'NONE',  ( 3.006218798242997980, -0.8556837461295877523, 1.940463308995137526 ) ) ;
#60122=CARTESIAN_POINT ( 'NONE',  ( 3.778635366994155032, -1.985013167256908240, -0.5533215937988352762 ) ) ;
#60124=CARTESIAN_POINT ( 'NONE',  ( 0.6789530235665336422, 1.236279375446739603, 1.364625092910062953 ) ) ;
#60128=CARTESIAN_POINT ( 'NONE',  ( 0.8388348947251201837, 2.174866457552121268, 0.3736606161612308630 ) ) ;
#60129=CARTESIAN_POINT ( 'NONE',  ( 2.108995328314038353, 1.677457623459570168, -1.518302342262042304 ) ) ;
#60131=CARTESIAN_POINT ( 'NONE',  ( 2.724650786558381999, 1.309284593816659736, -1.252271045645783065 ) ) ;
#60133=CARTESIAN_POINT ( 'NONE',  ( 3.169047557264609072, 1.729775434385946831, -0.8236773211035466336 ) ) ;
#60134=CARTESIAN_POINT ( 'NONE',  ( 4.510256325466165173, 2.069976601481211542, -0.04757507122059301263 ) ) ;
#60136=CARTESIAN_POINT ( 'NONE',  ( 2.746899856880557600, -1.639987585725300123, 1.093844759732710781 ) ) ;
#60137=CARTESIAN_POINT ( 'NONE',  ( 6.481085492957645577, -0.09751705652460275486, -1.924153034975156995 ) ) ;
#60138=CARTESIAN_POINT ( 'NONE',  ( 2.992876365407059147, 1.605230647100181596, -0.9602576221170722182 ) ) ;
#60139=CARTESIAN_POINT ( 'NONE',  ( 1.770602872417438967, 1.189155993293121716, 1.977591576486624314 ) ) ;
#60141=CARTESIAN_POINT ( 'NONE',  ( 4.070637595011177723, 1.317219721392929310, -1.314973792616628945 ) ) ;
#60143=CARTESIAN_POINT ( 'NONE',  ( 6.848098694195379643, -0.8844518680410964340, 1.861345814548149624 ) ) ;
#60147=CARTESIAN_POINT ( 'NONE',  ( 0.6628876427188118425, -1.523960678047535877, 1.453889595790233802 ) ) ;
#60150=CARTESIAN_POINT ( 'NONE',  ( 6.257120919624137301, -1.850417449585840313, -1.117149918570578437 ) ) ;
#60151=CARTESIAN_POINT ( 'NONE',  ( -0.1052055632086721232, -1.960199907271743314, -0.4866737942672630379 ) ) ;
#60156=CARTESIAN_POINT ( 'NONE',  ( 6.825078400183553384, 0.5907600490881077526, 1.908621492364571903 ) ) ;
#60160=CARTESIAN_POINT ( 'NONE',  ( 5.050017674172561755, 0.9981218692422781924, 1.752141108012375437 ) ) ;
#60163=APPLICATION_CONTEXT ( 'automotive_design' ) ;
#60164=CARTESIAN_POINT ( 'NONE',  ( 6.455963997168007396, 2.156291961557708525, -0.1537611777119098910 ) ) ;
#60168=CARTESIAN_POINT ( 'NONE',  ( 0.2103571609669597775, 1.833310535235525673, 0.5554914372104239328 ) ) ;
#60172=CARTESIAN_POINT ( 'NONE',  ( 1.646655695949898135, -1.458533453692168358, 0.9204839396419748354 ) ) ;
#60176=CARTESIAN_POINT ( 'NONE',  ( 0.6492013947936903229, 0.5632195774387914744, -1.677790250104938874 ) ) ;
#60177=CARTESIAN_POINT ( 'NONE',  ( 1.735022414761304921, 1.879166562360615966, 0.7224556781355166990 ) ) ;
#60178=CARTESIAN_POINT ( 'NONE',  ( 3.891806949550260519, 1.596497936513015192, 1.523729906679156754 ) ) ;
#60179=CARTESIAN_POINT ( 'NONE',  ( 4.856392247755495717, -2.170420479375735123, -0.05992511257937349622 ) ) ;
#60182=CARTESIAN_POINT ( 'NONE',  ( 2.860144583491229131, 0.7611018733697445526, -1.979373954265637892 ) ) ;
#60183=CARTESIAN_POINT ( 'NONE',  ( 2.583611426500436625, -0.6298568260672476882, 1.915607262459443572 ) ) ;
#60184=CARTESIAN_POINT ( 'NONE',  ( 3.550846374533889183, 0.2710319999918932021, 1.791078082347187683 ) ) ;
#60188=CARTESIAN_POINT ( 'NONE',  ( 0.7955152940811484052, -0.6771210053572243037, 1.743984199989514927 ) ) ;
#60190=CARTESIAN_POINT ( 'NONE',  ( 6.393173274427864428, 1.585754722747900969, -0.9045919592586546543 ) ) ;
#60192=CARTESIAN_POINT ( 'NONE',  ( 1.024461926017742996, 0.3770999164835596162, 1.878046770817816791 ) ) ;
#60197=CARTESIAN_POINT ( 'NONE',  ( 5.278265135069068137, -1.204163492603943064, 1.795060720813673738 ) ) ;
#60200=CARTESIAN_POINT ( 'NONE',  ( 2.601940685209406467, 1.502730264585940168, 1.496503045097858697 ) ) ;
#60201=CARTESIAN_POINT ( 'NONE',  ( -0.02988540731101250320, 5.726092063503692486, -2.320384613474982594 ) ) ;
#60203=CARTESIAN_POINT ( 'NONE',  ( 4.587161778375014265, 1.762195453814468182, -0.8837856115832108950 ) ) ;
#60204=CARTESIAN_POINT ( 'NONE',  ( -0.2106854629475244378, -0.004120941679102134263, -1.996958217618934661 ) ) ;
#60206=CARTESIAN_POINT ( 'NONE',  ( 5.454358448847595575, -1.341013495729547644, 1.638584853213326031 ) ) ;
#60208=CARTESIAN_POINT ( 'NONE',  ( 0.8540665308606997241, -0.7467690478978536994, 1.931163149162813619 ) ) ;
#60209=CARTESIAN_POINT ( 'NONE',  ( 3.117060223387691398, -1.871409496450952226, 0.5184039432134399661 ) ) ;
#60213=CARTESIAN_POINT ( 'NONE',  ( 3.855486427358902013, 2.074851370404519280, -0.2558628111340756628 ) ) ;
#60218=CARTESIAN_POINT ( 'NONE',  ( 0.5217373455332212639, -1.802923944912222520, 0.1758665181858156124 ) ) ;
#60220=CARTESIAN_POINT ( 'NONE',  ( 5.637410271038987730, -1.996576301129053377, 0.9405272304151902629 ) ) ;
#60222=CARTESIAN_POINT ( 'NONE',  ( 3.100804818134130780, -0.6391501652806098610, -2.112195066926086273 ) ) ;
#60224=CARTESIAN_POINT ( 'NONE',  ( 2.139182944796279351, 0.001596215867826628054, 1.912461472203148771 ) ) ;
#60226=CARTESIAN_POINT ( 'NONE',  ( 5.723117673755029777, -1.870111591731966616, -0.8886290660751752224 ) ) ;
#60228=CARTESIAN_POINT ( 'NONE',  ( 2.817419395390472037, -0.2130390993498078311, 2.151187356804876050 ) ) ;
#60229=CARTESIAN_POINT ( 'NONE',  ( 5.232042516939362287, 2.159042084939459816, 0.3751777721049884273 ) ) ;
#60240=CARTESIAN_POINT ( 'NONE',  ( 6.280147189154119403, -1.145143509460907039, -1.724508502191648862 ) ) ;
#60241=CARTESIAN_POINT ( 'NONE',  ( 3.861874329138580197, 1.911805356762337205, -0.2370204922254297297 ) ) ;
#60242=CARTESIAN_POINT ( 'NONE',  ( 6.362923164919582319, -0.1041218986313949546, -2.114803170081226646 ) ) ;
#60247=CARTESIAN_POINT ( 'NONE',  ( 4.926587155384105188, -1.289601243782242834, 1.488548236191704177 ) ) ;
#60248=CARTESIAN_POINT ( 'NONE',  ( 0.2170718473699268514, -0.1031819972749977166, 2.189145592210713698 ) ) ;
#60249=CARTESIAN_POINT ( 'NONE',  ( 4.336427269025699971, 1.790907886515300085, 0.3537760332646966432 ) ) ;
#60256=CARTESIAN_POINT ( 'NONE',  ( 2.665370095338463585, 0.9869154847663293983, 1.554228294351194473 ) ) ;
#60257=CARTESIAN_POINT ( 'NONE',  ( 5.238544184099147571, 1.195677241517135281, -1.619561112405358827 ) ) ;
#60258=CARTESIAN_POINT ( 'NONE',  ( 1.107258645251009144, 0.9300933289658299685, -2.101954592823534362 ) ) ;
#60259=CARTESIAN_POINT ( 'NONE',  ( 5.823093080589802462, -1.771997608643091304, -0.8420800316405114838 ) ) ;
#60263=CARTESIAN_POINT ( 'NONE',  ( 0.4497787391488928810, 1.533077660697563793, 1.391591089521776681 ) ) ;
#60265=CARTESIAN_POINT ( 'NONE',  ( 1.681308932615958041, 1.444198878393717411, 1.512019500502481018 ) ) ;
#60266=CARTESIAN_POINT ( 'NONE',  ( 0.1626889888870358680, -1.668787113083155305, -0.8454427722031019332 ) ) ;
#60268=VERTEX_POINT ( 'NONE', #69124 ) ;
#60269=CARTESIAN_POINT ( 'NONE',  ( -0.1102773484823963285, 5.719690680991945442, -2.797532285072940272 ) ) ;
#60270=CARTESIAN_POINT ( 'NONE',  ( 1.803882474592255258, 1.289405681850508190, -1.169162514946599174 ) ) ;
#60274=CARTESIAN_POINT ( 'NONE',  ( 2.648709078547459850, -1.434216206362935564, 0.9578970732360950757 ) ) ;
#60275=CARTESIAN_POINT ( 'NONE',  ( 2.911879292414458309, -1.082406496695037301, -1.905547650945007776 ) ) ;
#60276=CARTESIAN_POINT ( 'NONE',  ( 5.690102719724574598, -0.9953569382129350274, 1.969734210959340093 ) ) ;
#60278=CARTESIAN_POINT ( 'NONE',  ( 2.940461416894753377, -1.119856305176626821, 1.859859765203975890 ) ) ;
#60279=CARTESIAN_POINT ( 'NONE',  ( 0.6623940301842005107, -1.324425631624454036, 1.256838194884236204 ) ) ;
#60280=CARTESIAN_POINT ( 'NONE',  ( 3.626253288856711610, 2.107507776945900524, 0.2035006255925037866 ) ) ;
#60281=CARTESIAN_POINT ( 'NONE',  ( 6.639320575229278099, 1.279659970127836388, 2.012538313910294807 ) ) ;
#60283=CARTESIAN_POINT ( 'NONE',  ( 3.861076399890978283, 0.2801353988391065419, -2.275111823818583456 ) ) ;
#60286=CARTESIAN_POINT ( 'NONE',  ( 6.252596820807392319, 2.196675488376065744, 0.3289990992049235397 ) ) ;
#60294=CARTESIAN_POINT ( 'NONE',  ( 4.360000113718985659, -0.002809843368253156070, -2.016597020062675050 ) ) ;
#60296=CARTESIAN_POINT ( 'NONE',  ( 2.448158969691970555, -0.8859891528392377369, 1.862743816677481679 ) ) ;
#60301=CARTESIAN_POINT ( 'NONE',  ( 5.279302027902110339, 1.469929824498400039, 1.625505876179579534 ) ) ;
#60302=CARTESIAN_POINT ( 'NONE',  ( 3.692029868468839737, 1.730865839653324079, 1.034166058993556181 ) ) ;
#60303=CARTESIAN_POINT ( 'NONE',  ( 1.997363575765517485, -1.840834563946552649, 0.04656924640939614363 ) ) ;
#60305=CARTESIAN_POINT ( 'NONE',  ( 6.774438514930277933, -1.120217847261167243, 1.442041797927499980 ) ) ;
#60307=CARTESIAN_POINT ( 'NONE',  ( 5.594667793837476033, -0.5436135106791986082, -2.196135934016548052 ) ) ;
#60309=CARTESIAN_POINT ( 'NONE',  ( 1.453890484719716492, 0.6100395758942640523, -2.015780296659912985 ) ) ;
#60319=CARTESIAN_POINT ( 'NONE',  ( 2.461440635673370014, -1.844245817859784031, 1.238046099332066108 ) ) ;
#60320=CARTESIAN_POINT ( 'NONE',  ( 0.7157882511714327434, -0.3199875008889854766, 2.183444778895065941 ) ) ;
#60323=CARTESIAN_POINT ( 'NONE',  ( 3.965250677406896962, 1.681448970545707855, 1.010551734412237446 ) ) ;
#60331=CARTESIAN_POINT ( 'NONE',  ( 3.058948843759463188, 0.5191580478346514704, 2.055925682384197373 ) ) ;
#60333=CARTESIAN_POINT ( 'NONE',  ( 3.942369626403975147, 2.151062187213080623, 0.2142938780915065733 ) ) ;
#60334=CARTESIAN_POINT ( 'NONE',  ( 4.247483403459266782, 1.840758003770435414, -0.04960325993209198370 ) ) ;
#60338=CARTESIAN_POINT ( 'NONE',  ( 5.718645868333249283, -0.03627580822302550745, 1.740135244698801431 ) ) ;
#60339=CARTESIAN_POINT ( 'NONE',  ( 6.727182134110196721, 2.084960209934753284, 2.120171393779949565 ) ) ;
#60342=CARTESIAN_POINT ( 'NONE',  ( 3.292016909520224743, -0.8776455207864016783, 1.975710135277891633 ) ) ;
#60343=CARTESIAN_POINT ( 'NONE',  ( 5.817732461567613811, -1.591073081590412830, 1.238133459405404757 ) ) ;
#60345=CARTESIAN_POINT ( 'NONE',  ( 2.676834871759771417, -2.068302492614528365, -0.6285112194897370941 ) ) ;
#60346=CARTESIAN_POINT ( 'NONE',  ( 4.182859841474963147, -0.1902271694152017079, -1.962134583082324024 ) ) ;
#60347=CARTESIAN_POINT ( 'NONE',  ( 0.08191350661116909848, -1.027414926483052326, 1.935800647029708443 ) ) ;
#60348=CARTESIAN_POINT ( 'NONE',  ( 0.8687466845767909396, 1.140460243972157395, 2.005982166855703852 ) ) ;
#60349=CARTESIAN_POINT ( 'NONE',  ( 4.722180519508206054, 1.859554500701779745, 0.5601121866093302648 ) ) ;
#60359=CARTESIAN_POINT ( 'NONE',  ( 1.817678338065799704, -0.2697497798337232244, 2.190168480848574628 ) ) ;
#60361=CARTESIAN_POINT ( 'NONE',  ( 6.789906393989944888, -1.279003670332454989, -1.487618534420580119 ) ) ;
#60367=CARTESIAN_POINT ( 'NONE',  ( 5.578019757025042047, -1.797138167560994759, -0.3993771437491022702 ) ) ;
#60372=CARTESIAN_POINT ( 'NONE',  ( 6.011998765391792787, -0.7129019540204998284, 1.997330473063135381 ) ) ;
#60375=CARTESIAN_POINT ( 'NONE',  ( 0.2685257609614790097, -1.346659848514593305, 1.560126313484144545 ) ) ;
#60377=CARTESIAN_POINT ( 'NONE',  ( 2.400643840759258740, 0.4042734059873221986, 1.816444493264858906 ) ) ;
#60378=CARTESIAN_POINT ( 'NONE',  ( 4.862772069579198941, 0.1752732939881325724, -1.832877676746891726 ) ) ;
#60384=CARTESIAN_POINT ( 'NONE',  ( 4.213639274598267370, -0.3785452818781535611, 2.174016619501429215 ) ) ;
#60385=CARTESIAN_POINT ( 'NONE',  ( 6.573497657123517079, 2.167905964706399846, -0.6471699410235329797 ) ) ;
#60387=CARTESIAN_POINT ( 'NONE',  ( 5.607607993782223410, 1.377354484090735243, 1.176896650239395603 ) ) ;
#60388=CARTESIAN_POINT ( 'NONE',  ( 5.981633625760849782, -0.6386546108097415075, 1.806296054365429393 ) ) ;
#60390=CARTESIAN_POINT ( 'NONE',  ( 6.819227946136852125, -0.1326586024288610444, 1.840611662119538749 ) ) ;
#60391=CARTESIAN_POINT ( 'NONE',  ( 5.180287844241702189, 0.9460499258955605839, 1.661804969971327983 ) ) ;
#60394=CARTESIAN_POINT ( 'NONE',  ( 0.1978467685152424937, -1.870139902624564865, -0.05068021481659244765 ) ) ;
#60395=CARTESIAN_POINT ( 'NONE',  ( 2.712125330650519750, 1.116209241849321465, -1.679223868463100011 ) ) ;
#60397=CARTESIAN_POINT ( 'NONE',  ( 3.844438321715905715, 2.095922912919225389, 0.2063985846082766473 ) ) ;
#60403=CARTESIAN_POINT ( 'NONE',  ( 3.058857861556500968, 0.4949273143410140574, 1.958058250343613693 ) ) ;
#60408=CARTESIAN_POINT ( 'NONE',  ( 3.919328646192806520, -0.1633067429045453600, 2.155504054270485970 ) ) ;
#60414=CARTESIAN_POINT ( 'NONE',  ( 1.610090671168771470, 0.6309225058772853778, -2.077463247357013820 ) ) ;
#60418=CARTESIAN_POINT ( 'NONE',  ( 0.7668492355173107677, 1.774547462407764842, -0.4907661837717376407 ) ) ;
#60420=CARTESIAN_POINT ( 'NONE',  ( 2.033021410476544943, -1.955939774129427988, 0.9887309579383956049 ) ) ;
#60421=CARTESIAN_POINT ( 'NONE',  ( 6.883263157960358924, 4.692138088316172073, 2.616388454592593504 ) ) ;
#60422=CARTESIAN_POINT ( 'NONE',  ( 2.782378429719241986, -1.163933448739282062, 1.940043740367594305 ) ) ;
#60428=CARTESIAN_POINT ( 'NONE',  ( 4.727684277059563733, -1.088367244632810094, -1.395429379651995649 ) ) ;
#60430=CARTESIAN_POINT ( 'NONE',  ( 0.7101633350218137242, -2.095805943121428427, 0.2063731196077517871 ) ) ;
#60434=CARTESIAN_POINT ( 'NONE',  ( 6.204703874486805049, 1.882480396761162744, 0.7231267579426368108 ) ) ;
#60435=CARTESIAN_POINT ( 'NONE',  ( 5.080233222017616512, 0.8995743074830947483, 1.572398339973365422 ) ) ;
#60438=CARTESIAN_POINT ( 'NONE',  ( 3.731198135974967300, -1.728734619261709682, 0.7151963084984153118 ) ) ;
#60439=CARTESIAN_POINT ( 'NONE',  ( 4.504778988403771223, 0.5471568804141565545, 1.996604337080605474 ) ) ;
#60449=CARTESIAN_POINT ( 'NONE',  ( 3.683996026499200660, -1.166640140252427793, -1.577160851978461009 ) ) ;
#60450=CARTESIAN_POINT ( 'NONE',  ( 0.5442957877539145173, 1.882187304385819493, -0.7230256762977352869 ) ) ;
#60454=CARTESIAN_POINT ( 'NONE',  ( 1.282252794574537447, -1.823689378192733912, -0.4153219600965887826 ) ) ;
#60456=CARTESIAN_POINT ( 'NONE',  ( 3.551042609437846220, 0.2996916850201857829, 1.990680017358969600 ) ) ;
#60458=CARTESIAN_POINT ( 'NONE',  ( 3.884452219389774363, -0.6659801820031689967, -2.009805269316313314 ) ) ;
#60460=CARTESIAN_POINT ( 'NONE',  ( 4.721179655770254335, -1.847879960204744432, -0.9338546512941485744 ) ) ;
#60462=CARTESIAN_POINT ( 'NONE',  ( 6.667919252303131650, -1.287369299672879830, 1.647753151290908047 ) ) ;
#60464=CARTESIAN_POINT ( 'NONE',  ( 4.823181420811452291, -0.08861582515604787824, 1.823562061424352621 ) ) ;
#60469=CARTESIAN_POINT ( 'NONE',  ( 6.686557766011572923, -2.162873314485185272, -0.4371622687903350957 ) ) ;
#60471=CARTESIAN_POINT ( 'NONE',  ( 5.109976026518994630, -0.6845719981980763480, 1.785733525123212928 ) ) ;
#60479=CARTESIAN_POINT ( 'NONE',  ( -0.02299388927988389730, 6.948790505698306141, -2.506045543530223352 ) ) ;
#60483=CARTESIAN_POINT ( 'NONE',  ( 0.1394461523057136665, 2.058909413595513715, -2.136561586061051621 ) ) ;
#60486=CARTESIAN_POINT ( 'NONE',  ( 2.764455286864405004, -0.7492524419267130309, -1.821560881719074709 ) ) ;
#60487=CARTESIAN_POINT ( 'NONE',  ( 3.515250061227533696, -1.862011288300661871, 0.7743320027404425598 ) ) ;
#60490=CARTESIAN_POINT ( 'NONE',  ( 6.727182134110234024, 7.051482179251418181, 2.887205776801844426 ) ) ;
#60491=CARTESIAN_POINT ( 'NONE',  ( 3.275498427308475069, 1.390425696708731396, 1.693851754907250928 ) ) ;
#60492=CARTESIAN_POINT ( 'NONE',  ( 1.817283056450700318, -0.2383884500203499179, 1.911531453543861225 ) ) ;
#60495=CARTESIAN_POINT ( 'NONE',  ( 0.1329588055935760349, 6.948069629093068578, -2.440977959956799115 ) ) ;
#60502=CARTESIAN_POINT ( 'NONE',  ( 6.110883706712432861, -0.2185277653131960651, 1.828168259763853776 ) ) ;
#60503=CARTESIAN_POINT ( 'NONE',  ( 3.053387886640859694, -1.774279702891886190, 0.9510675200815300601 ) ) ;
#60504=CARTESIAN_POINT ( 'NONE',  ( 4.552342272275657464, 2.055464322635578878, -1.028527531867760914 ) ) ;
#60505=CARTESIAN_POINT ( 'NONE',  ( -0.1288028175206725467, 0.2223783146117243037, -2.307352578052775272 ) ) ;
#60506=CARTESIAN_POINT ( 'NONE',  ( 1.832617572280154539, -1.765004919984759058, -0.5899526775028116621 ) ) ;
#60509=CARTESIAN_POINT ( 'NONE',  ( 6.469012471580376733, -1.473683540339595810, 1.218514635347216046 ) ) ;
#60512=CARTESIAN_POINT ( 'NONE',  ( 4.985920054561153059, -2.075123007882358817, -0.2543892858761549469 ) ) ;
#60513=CARTESIAN_POINT ( 'NONE',  ( 3.186256133050053840, -1.842714570631575510, -0.3211874441736498054 ) ) ;
#60519=CARTESIAN_POINT ( 'NONE',  ( 6.199779612253428773, -0.5740575353240050527, 1.626695425327763678 ) ) ;
#60521=CARTESIAN_POINT ( 'NONE',  ( 1.810757103121255707, 0.9981641815470091439, -1.417837687506792621 ) ) ;
#60525=CARTESIAN_POINT ( 'NONE',  ( 6.262575984712966282, -0.7736541179628317888, -2.028742479192620518 ) ) ;
#60526=CARTESIAN_POINT ( 'NONE',  ( 4.652862234063231739, -1.464609733205827879, 1.089778014065109657 ) ) ;
#60527=CARTESIAN_POINT ( 'NONE',  ( 2.782025223480470544, -1.125517505138178942, -1.606590762409945583 ) ) ;
#60528=CARTESIAN_POINT ( 'NONE',  ( 6.350787976822619640, -1.936633936377421206, -0.8562603515115329023 ) ) ;
#60533=CARTESIAN_POINT ( 'NONE',  ( 3.000754678503589012, -2.089479603458433754, -0.3603616953608209661 ) ) ;
#60538=CARTESIAN_POINT ( 'NONE',  ( 0.2509399751232620490, -0.4509356589572112162, -2.027996233343106081 ) ) ;
#60542=CARTESIAN_POINT ( 'NONE',  ( 3.053626115265011709, -1.958026000861570415, 1.048987487942198094 ) ) ;
#60544=CARTESIAN_POINT ( 'NONE',  ( 0.8799778958844242105, -0.5652253508772618895, -2.228020342328890901 ) ) ;
#60546=CARTESIAN_POINT ( 'NONE',  ( 5.418824339757763120, -1.497735668165665723, 1.418348116948890736 ) ) ;
#60550=CARTESIAN_POINT ( 'NONE',  ( 5.618664544990171095, -0.03892770779775727580, 1.841008343696965310 ) ) ;
#60552=CARTESIAN_POINT ( 'NONE',  ( -0.1102773484824301209, 0.2280386113255315761, -2.237141580442712829 ) ) ;
#60553=CARTESIAN_POINT ( 'NONE',  ( 3.153030191819999217, -1.409141575680799230, -0.9942448187586181430 ) ) ;
#60554=CARTESIAN_POINT ( 'NONE',  ( 1.745327705122714956, 0.3399549603602426417, -1.987498286102694411 ) ) ;
#60555=CARTESIAN_POINT ( 'NONE',  ( 3.375889859521400194, -0.4501408176796182770, -2.254053602989118499 ) ) ;
#60557=CARTESIAN_POINT ( 'NONE',  ( 2.653932422735814978, 0.6056841677779849498, -2.179737047031413244 ) ) ;
#60558=CARTESIAN_POINT ( 'NONE',  ( 5.619784395276031574, -2.055015178219528948, 0.4601488667864346849 ) ) ;
#60560=CARTESIAN_POINT ( 'NONE',  ( 4.077242326343363032, 1.667005924876462597, -0.5946135600440533020 ) ) ;
#60562=CARTESIAN_POINT ( 'NONE',  ( 6.356980026238091774, 0.3966049396831958229, -2.257653707126358267 ) ) ;
#60563=CARTESIAN_POINT ( 'NONE',  ( 4.171694865975253741, -1.058263924308279424, 1.506412014522513720 ) ) ;
#60567=CARTESIAN_POINT ( 'NONE',  ( 4.910206770677443266, 1.512653250323254817, -1.585896273577400484 ) ) ;
#60571=CARTESIAN_POINT ( 'NONE',  ( 5.266107318980479235, -2.060723932065291031, 0.1993833602659672022 ) ) ;
#60572=CARTESIAN_POINT ( 'NONE',  ( 0.2863426850727782136, -0.6839425765656822476, -1.897108587135355684 ) ) ;
#60574=CARTESIAN_POINT ( 'NONE',  ( 3.246621724073412096, 0.4685524532376301177, 1.868535087029847386 ) ) ;
#60578=CARTESIAN_POINT ( 'NONE',  ( 0.05339833992625257070, 0.3882609103176749010, 2.187096328411592516 ) ) ;
#60587=CARTESIAN_POINT ( 'NONE',  ( 1.803102349535959714, -1.659081995624330563, 1.046767247423967095 ) ) ;
#60589=CARTESIAN_POINT ( 'NONE',  ( 6.420800710400103917, 2.015122584031241004, 0.7829223626853940576 ) ) ;
#60590=CARTESIAN_POINT ( 'NONE',  ( 5.494571831323358246, 1.932540981948445147, 0.3370517209014682325 ) ) ;
#60593=CARTESIAN_POINT ( 'NONE',  ( 5.752838164830007983, -1.706859214253673152, 1.326403591387192771 ) ) ;
#60597=CARTESIAN_POINT ( 'NONE',  ( 6.802032592820894230, -1.970958832386409565, 0.04617810802716794394 ) ) ;
#60598=CARTESIAN_POINT ( 'NONE',  ( 6.626334403847231158, 0.2915952204957816263, -1.708955668912811587 ) ) ;
#60600=CARTESIAN_POINT ( 'NONE',  ( 3.614928802375876771, -0.1595779646587774658, 2.185787688459623901 ) ) ;
#60601=CARTESIAN_POINT ( 'NONE',  ( 4.770747201329826659, -1.511217855519477293, 1.743977600800976857 ) ) ;
#60602=CARTESIAN_POINT ( 'NONE',  ( 5.852824474907069252, -1.627199953678662991, 1.264450640605979892 ) ) ;
#60603=CARTESIAN_POINT ( 'NONE',  ( 1.077954490650166575, -1.894526023430597617, -0.4258829084243920260 ) ) ;
#60608=CARTESIAN_POINT ( 'NONE',  ( 4.605793411009856619, 1.573235607984494688, 1.422142093439874522 ) ) ;
#60610=CARTESIAN_POINT ( 'NONE',  ( 2.215470409936692420, 1.956561601830292485, 0.4872017847364697452 ) ) ;
#60612=CARTESIAN_POINT ( 'NONE',  ( 5.614374367772542840, -0.9875226594672004143, -1.973556357105679115 ) ) ;
#60615=CARTESIAN_POINT ( 'NONE',  ( 0.3108172448005979138, 1.586703044182024458, 0.9029097728878652251 ) ) ;
#60620=CARTESIAN_POINT ( 'NONE',  ( 5.418845456765190249, 1.903306360667684993, 0.7908678518537788360 ) ) ;
#60625=CARTESIAN_POINT ( 'NONE',  ( 4.529947673531667718, -1.980263497020241292, 0.3961197999026391248 ) ) ;
#60630=CARTESIAN_POINT ( 'NONE',  ( 4.223548136977580469, -1.972658117897459151, 0.5965803236557595257 ) ) ;
#60631=CARTESIAN_POINT ( 'NONE',  ( 2.971327447312217540, -1.987046587055636859, -0.3419355124290661685 ) ) ;
#60638=CARTESIAN_POINT ( 'NONE',  ( 3.075545897833771747, 1.462222457232667416, -1.388272539953112839 ) ) ;
#60639=CARTESIAN_POINT ( 'NONE',  ( 2.941158370608713213, 0.6622022323767087215, -1.718108305994885177 ) ) ;
#60640=CARTESIAN_POINT ( 'NONE',  ( 0.8390048429645606820, 2.274487955075610301, 0.3892829850337137243 ) ) ;
#60642=CARTESIAN_POINT ( 'NONE',  ( 2.759224924868249662, -1.879262701025650850, -1.068020781904190253 ) ) ;
#60644=CARTESIAN_POINT ( 'NONE',  ( 2.390373184264094952, -0.001117755346285650552, 2.298542322714514530 ) ) ;
#60646=CARTESIAN_POINT ( 'NONE',  ( 1.252583056964752029, -1.476889893665521925, 1.148006582770304096 ) ) ;
#60647=CARTESIAN_POINT ( 'NONE',  ( 5.383651750111712708, 1.323420565077202182, 1.461416689776244615 ) ) ;
#60651=CARTESIAN_POINT ( 'NONE',  ( 0.9794701899953797142, -0.05759512415488829418, -2.206297691287119722 ) ) ;
#60655=CARTESIAN_POINT ( 'NONE',  ( 6.639320575229286092, 4.689090874229541406, 2.765823994384248419 ) ) ;
#60656=CARTESIAN_POINT ( 'NONE',  ( 4.504732016840462983, 1.524723275766314279, -1.249774587014943483 ) ) ;
#60657=CARTESIAN_POINT ( 'NONE',  ( 0.1234922912959918878, 1.848187084301698757, 1.039613981531524400 ) ) ;
#60658=CARTESIAN_POINT ( 'NONE',  ( 4.828937647557053126, 2.207305988086407655, 0.6732806465959675357 ) ) ;
#60660=CARTESIAN_POINT ( 'NONE',  ( 3.221586243988622034, 0.3073416805365276061, -2.039453084318449072 ) ) ;
#60667=CARTESIAN_POINT ( 'NONE',  ( 5.494640824104591204, 2.138133990741352353, 0.3765844856341519775 ) ) ;
#60669=CARTESIAN_POINT ( 'NONE',  ( 4.159580895514263688, 0.8717668643758098579, 1.621812032879976329 ) ) ;
#60672=CARTESIAN_POINT ( 'NONE',  ( 6.720655732516671144, 1.288224904612661925, 1.942155157606942240 ) ) ;
#60673=CARTESIAN_POINT ( 'NONE',  ( 5.689076433642084041, 1.658752129386225516, 1.432425853890168188 ) ) ;
#60675=CARTESIAN_POINT ( 'NONE',  ( 6.614178507701674370, -1.059427008983104601, -1.999161347636166930 ) ) ;
#60681=CARTESIAN_POINT ( 'NONE',  ( 0.7425837709835466649, -1.521049679623546425, 0.9045992453171716186 ) ) ;
#60682=CARTESIAN_POINT ( 'NONE',  ( 5.039702193125279450, -1.910865547410881549, 0.6335069822010936935 ) ) ;
#60684=CARTESIAN_POINT ( 'NONE',  ( 3.628042789974804450, -1.253006538321174146, -1.692492853607285630 ) ) ;
#60685=CARTESIAN_POINT ( 'NONE',  ( 2.706530202829552145, 1.804627309565815185, 0.6429686382581675241 ) ) ;
#60687=CARTESIAN_POINT ( 'NONE',  ( 4.053143702687862060, 1.665121224333296235, -1.051576502219366605 ) ) ;
#60688=CARTESIAN_POINT ( 'NONE',  ( 5.976820969762068003, -1.425406409037911937, 1.431266451708369303 ) ) ;
#60689=CARTESIAN_POINT ( 'NONE',  ( 1.340467186903429253, 0.3614942610149494695, 1.835218787103513050 ) ) ;
#60690=CARTESIAN_POINT ( 'NONE',  ( 4.635198054048816019, -1.575417825122129134, 0.7027606912313691945 ) ) ;
#60691=CARTESIAN_POINT ( 'NONE',  ( 1.722773492080275748, 1.414811824084385661, -1.286832238068566392 ) ) ;
#60693=CARTESIAN_POINT ( 'NONE',  ( 1.014635385311330795, -0.9952708415592588231, -1.969785480804244315 ) ) ;
#60698=CARTESIAN_POINT ( 'NONE',  ( 6.684453402082995765, -1.835023323784425342, -0.3624468955198830167 ) ) ;
#60702=CARTESIAN_POINT ( 'NONE',  ( 1.592325325408463055, 1.022198633559557646, -1.800363622228560168 ) ) ;
#60708=CARTESIAN_POINT ( 'NONE',  ( 0.2408861781304712513, 1.933338575160881367, 0.5842326518414300285 ) ) ;
#60711=ORIENTED_EDGE ( 'NONE', *, *, #159948, .F. ) ;
#60714=CARTESIAN_POINT ( 'NONE',  ( 4.165388622617651748, -0.6297791189726584804, -1.915306643112117291 ) ) ;
#60715=CARTESIAN_POINT ( 'NONE',  ( 4.821452977306352139, -1.359283356373307328, -1.350213215339219897 ) ) ;
#60717=CARTESIAN_POINT ( 'NONE',  ( 2.525153347276567484, -2.043736813514348771, 0.7916865192442237298 ) ) ;
#60720=CARTESIAN_POINT ( 'NONE',  ( 5.660407656431548418, 2.011079132963066840, 0.09461074985974733675 ) ) ;
#60723=CARTESIAN_POINT ( 'NONE',  ( 6.433232048832024930, -1.700592621796994441, -1.261046147972416875 ) ) ;
#60725=CARTESIAN_POINT ( 'NONE',  ( 3.456657222422593545, -1.844998171120499020, -0.9834188347317989187 ) ) ;
#60727=CARTESIAN_POINT ( 'NONE',  ( 1.834533585138716782, 0.1645414454686990324, 1.716894335133994698 ) ) ;
#60738=CARTESIAN_POINT ( 'NONE',  ( 2.596125760314275777, -0.9296622322433767405, 1.554548433350180225 ) ) ;
#60745=CARTESIAN_POINT ( 'NONE',  ( 3.896947601784990223, -0.1811674076915045506, -1.802394175579679958 ) ) ;
#60746=CARTESIAN_POINT ( 'NONE',  ( 6.539320575229287336, 0.5820952121784334077, 2.049435377300548033 ) ) ;
#60750=CARTESIAN_POINT ( 'NONE',  ( 4.070637595011177723, 1.317219721392929310, -1.314973792616628945 ) ) ;
#60751=CARTESIAN_POINT ( 'NONE',  ( 1.933070621186453897, -1.539717990624125621, -1.139454883405303098 ) ) ;
#60752=CARTESIAN_POINT ( 'NONE',  ( 0.4283665542385572955, 1.745377284433462295, 0.5351633580037706839 ) ) ;
#60762=CARTESIAN_POINT ( 'NONE',  ( 5.436368237181718577, -1.097297496841664444, 1.635214795183062675 ) ) ;
#60766=CARTESIAN_POINT ( 'NONE',  ( 0.6387612955554131666, -1.792149412372344042, 1.076304641864724410 ) ) ;
#60768=CARTESIAN_POINT ( 'NONE',  ( 5.420897863522853299, 1.779935589243306859, 0.7372156234431108679 ) ) ;
#60770=CARTESIAN_POINT ( 'NONE',  ( 0.9733497034139363402, 1.760643049788807257, -0.4823509818385819936 ) ) ;
#60771=CARTESIAN_POINT ( 'NONE',  ( 2.192262590105994668, -0.9421081357594159877, 1.995820444975453745 ) ) ;
#60774=CARTESIAN_POINT ( 'NONE',  ( 0.5977379272000953314, 1.286164058678052946, 1.415416067018962165 ) ) ;
#60776=CARTESIAN_POINT ( 'NONE',  ( 0.8363043462186695587, -1.097040784323728424, 1.635518954194992824 ) ) ;
#60777=CARTESIAN_POINT ( 'NONE',  ( 3.087376005906359744, -0.7846555324184587565, 1.776656735299622980 ) ) ;
#60779=CARTESIAN_POINT ( 'NONE',  ( 1.335314297916901927, -1.281167425915705316, 1.556668322744148014 ) ) ;
#60781=CARTESIAN_POINT ( 'NONE',  ( 5.032013264887808646, 1.069401199365666688, 1.522792188549914272 ) ) ;
#60783=DIRECTION ( 'NONE',  ( -0.9999980456341538426, 0.000000000000000000, -0.001977050295941262543 ) ) ;
#60787=CARTESIAN_POINT ( 'NONE',  ( 1.277182604683280598, 2.023070758711601691, -0.8431670391453591762 ) ) ;
#60791=CARTESIAN_POINT ( 'NONE',  ( 2.947667120405720986, 0.6567698719579934119, -1.703645827024417914 ) ) ;
#60795=CARTESIAN_POINT ( 'NONE',  ( -0.02968770228137587730, 6.948707269782667062, -2.421356871654921417 ) ) ;
#60797=CARTESIAN_POINT ( 'NONE',  ( 0.6625679566808447829, -1.396226752684716521, 1.327616383781888176 ) ) ;
#60798=CARTESIAN_POINT ( 'NONE',  ( 5.612146373276853950, 1.959670608579218376, -0.09257137562097839112 ) ) ;
#60803=CARTESIAN_POINT ( 'NONE',  ( 5.038714576072483631, -1.879839391954684746, 1.126354835186346603 ) ) ;
#60804=CARTESIAN_POINT ( 'NONE',  ( 4.241125740018336643, -0.1978421677554068614, -2.060750949040678570 ) ) ;
#60808=CARTESIAN_POINT ( 'NONE',  ( 4.430533913404213209, -1.776825693393409455, -1.458421372522151538 ) ) ;
#60815=CARTESIAN_POINT ( 'NONE',  ( 4.101460596356475641, -1.936652220471976937, 0.1442349196467233863 ) ) ;
#60816=EDGE_LOOP ( 'NONE', ( #185921, #209169, #32202, #9675 ) ) ;
#60820=CARTESIAN_POINT ( 'NONE',  ( 5.027564050633359649, -0.2746679736120913318, 1.892429487827557599 ) ) ;
#60821=CARTESIAN_POINT ( 'NONE',  ( 6.387718858896353602, 1.193691027695796825, 1.245227284122518485 ) ) ;
#60822=CARTESIAN_POINT ( 'NONE',  ( 4.786342355033275986, -0.6839347017603313317, -1.897111394664739104 ) ) ;
#60824=CARTESIAN_POINT ( 'NONE',  ( 1.366164030173490973, 2.173753390890633685, -0.3800739277931909355 ) ) ;
#60827=CARTESIAN_POINT ( 'NONE',  ( 1.658266814308974268, -1.477475772113973740, 1.479395487768909501 ) ) ;
#60828=CARTESIAN_POINT ( 'NONE',  ( 6.520749347316099787, 1.652272609716086249, 0.6344386834381664508 ) ) ;
#60829=CARTESIAN_POINT ( 'NONE',  ( 6.170546107226446253, 1.392543322632183722, 1.458558933167881211 ) ) ;
#60831=CARTESIAN_POINT ( 'NONE',  ( 3.187719515414323190, -0.9288583595017800842, 2.095805606604860039 ) ) ;
#60832=CARTESIAN_POINT ( 'NONE',  ( 0.6732859938517594678, -0.9703907760119870884, 1.444448127723398478 ) ) ;
#60833=CARTESIAN_POINT ( 'NONE',  ( 2.637105894733019262, 1.998242115483703341, 0.7103459930332192140 ) ) ;
#60835=CARTESIAN_POINT ( 'NONE',  ( 0.5261554912905551662, 1.716204961384654171, -0.2456527019241669663 ) ) ;
#60837=CARTESIAN_POINT ( 'NONE',  ( 2.172091045797384989, -0.8737597001905510474, -1.643165899227620796 ) ) ;
#60838=CARTESIAN_POINT ( 'NONE',  ( 1.047617182619766885, 1.914800503461089543, -1.023450759211230521 ) ) ;
#60839=CARTESIAN_POINT ( 'NONE',  ( 2.940638933469359895, -1.523795050681177710, 1.320827213682006285 ) ) ;
#60840=CARTESIAN_POINT ( 'NONE',  ( 4.937500000000003553, 1.451031289060916496, -1.451031289061313512 ) ) ;
#60842=CARTESIAN_POINT ( 'NONE',  ( 6.463506663115213158, 0.3265968279197262181, -1.898468693527188389 ) ) ;
#60844=CARTESIAN_POINT ( 'NONE',  ( 3.709420277874009297, 1.875127481890274561, -1.190789481685197604 ) ) ;
#60846=CARTESIAN_POINT ( 'NONE',  ( -0.2110808730067326444, 6.948329377029001996, -2.392166167428900536 ) ) ;
#60849=CARTESIAN_POINT ( 'NONE',  ( 6.110887277445514520, -0.2035749799894230883, 1.728432721540203998 ) ) ;
#60850=CARTESIAN_POINT ( 'NONE',  ( 4.580490334204036174, 1.208584658811951762, -1.545285769342201965 ) ) ;
#60854=CARTESIAN_POINT ( 'NONE',  ( 6.098944901167723032, 1.854799121126067485, -1.295245758874500996 ) ) ;
#60856=CARTESIAN_POINT ( 'NONE',  ( 2.523947517756039982, 2.023366295090854194, -0.3999800566471324315 ) ) ;
#60861=CARTESIAN_POINT ( 'NONE',  ( 4.217926093758464390, -0.9595593063399066036, -1.605508702137818045 ) ) ;
#60862=CARTESIAN_POINT ( 'NONE',  ( 2.390900936787855091, -0.6653014413638760338, -1.601662460290956380 ) ) ;
#60863=CARTESIAN_POINT ( 'NONE',  ( 5.952700804540857149, -1.878875186057769486, -1.127905468421293689 ) ) ;
#60864=CARTESIAN_POINT ( 'NONE',  ( 0.7630613749609324037, -1.597064910551798667, 1.523150255686569254 ) ) ;
#60865=CARTESIAN_POINT ( 'NONE',  ( 3.608425205800522839, -0.8741791752944136906, -1.977237025433141504 ) ) ;
#60866=CARTESIAN_POINT ( 'NONE',  ( 5.191327941051770978, -0.6971716684453888035, 1.812662890818200756 ) ) ;
#60874=CARTESIAN_POINT ( 'NONE',  ( 5.502577337681268332, -1.966645332631598908, 0.4444998760482973821 ) ) ;
#60878=CARTESIAN_POINT ( 'NONE',  ( 3.351995281737112364, 1.825872481133209879, -0.0009662468829912954560 ) ) ;
#60879=CARTESIAN_POINT ( 'NONE',  ( 1.712255133470397261, -2.190042126362458319, 0.2705847154940849153 ) ) ;
#60884=CARTESIAN_POINT ( 'NONE',  ( 0.6858141477139628739, 1.945346236745447488, -0.5429362378739016615 ) ) ;
#60885=CARTESIAN_POINT ( 'NONE',  ( 1.243013918421622455, 2.044566944090483229, 0.5621290157047582614 ) ) ;
#60888=CARTESIAN_POINT ( 'NONE',  ( 1.797469275952040979, -1.343413903288761313, -1.288013994602929646 ) ) ;
#60890=CARTESIAN_POINT ( 'NONE',  ( 1.077287230265553397, -0.05381693868444264311, -2.161191418701657430 ) ) ;
#60891=CARTESIAN_POINT ( 'NONE',  ( 5.783827325522512552, 1.646840809264274119, -1.163266671679111353 ) ) ;
#60895=CARTESIAN_POINT ( 'NONE',  ( 3.791466046568803705, 1.323482414808102137, 1.257835202898072380 ) ) ;
#60901=CARTESIAN_POINT ( 'NONE',  ( 6.222029796014385106, -1.727739227931901489, -1.038831587593692873 ) ) ;
#60902=CARTESIAN_POINT ( 'NONE',  ( 6.035073252477260120, -1.336788798515762489, -1.266260169258619284 ) ) ;
#60904=CARTESIAN_POINT ( 'NONE',  ( 4.160959874251066282, -1.711463231979272859, 1.548185629304731581 ) ) ;
#60906=CARTESIAN_POINT ( 'NONE',  ( 6.134075720976177593, 1.071308383804179476, -1.877395391766012445 ) ) ;
#60908=CARTESIAN_POINT ( 'NONE',  ( 1.927192517792934101, -1.269957001497720395, -1.469349730274618571 ) ) ;
#60909=CARTESIAN_POINT ( 'NONE',  ( 4.745672437882476835, -2.227950070917711134, -0.5642311211754289513 ) ) ;
#60913=CARTESIAN_POINT ( 'NONE',  ( 4.469519713540137218, 1.814478506493342191, -0.4545110902946307152 ) ) ;
#60915=CARTESIAN_POINT ( 'NONE',  ( 2.830216799141628492, -0.9462872844297947061, -1.661813493071498726 ) ) ;
#60918=CARTESIAN_POINT ( 'NONE',  ( 3.598431038176507002, -2.204323482753521635, -0.1086902067785888437 ) ) ;
#60919=EDGE_CURVE ( 'NONE', #41604, #21324, #170115, .T. ) ;
#60920=CARTESIAN_POINT ( 'NONE',  ( 6.983263157960370116, 1.266851337794393961, 2.060309365732877485 ) ) ;
#60924=CARTESIAN_POINT ( 'NONE',  ( 1.651575284419577461, 0.5759676520707255332, -1.885319811257283096 ) ) ;
#60925=CARTESIAN_POINT ( 'NONE',  ( 1.589377644589501148, -0.3404682245478432567, -2.282209529656929803 ) ) ;
#60926=CARTESIAN_POINT ( 'NONE',  ( 2.857805160684105950, -0.6180756922911297968, 1.862011555624979886 ) ) ;
#60928=CARTESIAN_POINT ( 'NONE',  ( 6.842638575262629530, -2.021612500624434539, -0.4081942145969327251 ) ) ;
#60930=CARTESIAN_POINT ( 'NONE',  ( 3.766814776335784209, -0.2024620155892907503, -2.006371719556559796 ) ) ;
#60936=CARTESIAN_POINT ( 'NONE',  ( 1.991327249661909882, 0.2097703728867078010, 2.160876515670279385 ) ) ;
#60941=CARTESIAN_POINT ( 'NONE',  ( 2.741296213614560440, -1.383352855433259698, -1.259238407996167153 ) ) ;
#60942=CARTESIAN_POINT ( 'NONE',  ( 6.819591527820957566, -2.098570527662356522, 0.5178885164088961046 ) ) ;
#60944=CARTESIAN_POINT ( 'NONE',  ( 6.727182134110186063, 1.310238205575515957, 1.828849833172506489 ) ) ;
#60947=CARTESIAN_POINT ( 'NONE',  ( 2.490748672031910083, -1.830495558572857728, -0.5533032672612181457 ) ) ;
#60948=CARTESIAN_POINT ( 'NONE',  ( 4.715556530927702106, -1.735345248271908947, 0.3467660769565800161 ) ) ;
#60949=CARTESIAN_POINT ( 'NONE',  ( 1.312987857083922627, 1.562780923097413677, -1.101767902142808175 ) ) ;
#60952=CARTESIAN_POINT ( 'NONE',  ( 6.362892188913578551, -0.09940890854263698118, -1.913169475778592865 ) ) ;
#60954=CARTESIAN_POINT ( 'NONE',  ( 0.8013346216862862192, -1.776568573310655985, 1.062853015585236482 ) ) ;
#60957=CARTESIAN_POINT ( 'NONE',  ( 5.576977133510579776, -0.04717937999037385977, -1.870219006134994588 ) ) ;
#60958=CARTESIAN_POINT ( 'NONE',  ( 1.734698295210383767, 0.1775668987445792879, 1.817036636966688823 ) ) ;
#60959=CARTESIAN_POINT ( 'NONE',  ( 5.373716497573798101, 2.127666891504222058, -0.5857064233696291922 ) ) ;
#60962=CARTESIAN_POINT ( 'NONE',  ( 2.523947517756039982, 2.023366295090854194, -0.3999800566471324315 ) ) ;
#60964=CARTESIAN_POINT ( 'NONE',  ( 6.610000000000028741, 4.695285100415147461, 2.562642482393460597 ) ) ;
#60969=CARTESIAN_POINT ( 'NONE',  ( 5.494608840674215955, 2.039112051642687717, 0.3575134270455831986 ) ) ;
#60971=CARTESIAN_POINT ( 'NONE',  ( 2.390102426918311540, -0.9266024157483061519, 1.953076554623616401 ) ) ;
#60973=CARTESIAN_POINT ( 'NONE',  ( 2.877608074518396286, 0.2940240112025078179, -1.998017427383149913 ) ) ;
#60981=CARTESIAN_POINT ( 'NONE',  ( 1.534389036647098692, 0.6371565916030231813, 1.913260934284975345 ) ) ;
#60983=CARTESIAN_POINT ( 'NONE',  ( 6.128506746050899068, 0.2130254606748181456, 2.181202035047181020 ) ) ;
#60986=CARTESIAN_POINT ( 'NONE',  ( 5.027564050633359649, -0.2746679736120913318, 1.892429487827557599 ) ) ;
#60990=CARTESIAN_POINT ( 'NONE',  ( 2.987907820627898836, -2.013986125068282007, 0.1017690403029153645 ) ) ;
#60993=CARTESIAN_POINT ( 'NONE',  ( 5.772382705887088683, -1.090832958316660273, 1.335977363661453809 ) ) ;
#60997=CARTESIAN_POINT ( 'NONE',  ( 4.464026755505964950, 0.8799173153972823513, 1.650629236088823282 ) ) ;
#60999=CARTESIAN_POINT ( 'NONE',  ( 1.147426569842596722, 1.827566109494669577, -0.9725325914680116313 ) ) ;
#61001=CARTESIAN_POINT ( 'NONE',  ( 5.883446949022190786, 0.1262479900229801499, -1.807133042791621458 ) ) ;
#61003=CARTESIAN_POINT ( 'NONE',  ( -0.1407840215364779823, -1.400018645128609629, -1.149511601580233577 ) ) ;
#61006=CARTESIAN_POINT ( 'NONE',  ( 2.976726284633357533, -0.1618151936485581754, -2.185533650236513914 ) ) ;
#61009=CARTESIAN_POINT ( 'NONE',  ( 0.4671467121175364445, 1.705069321186868159, 0.9702857188121425391 ) ) ;
#61011=CARTESIAN_POINT ( 'NONE',  ( 4.903869178324737454, -1.028422014321051403, -1.615943446245589943 ) ) ;
#61019=CARTESIAN_POINT ( 'NONE',  ( 1.358524781292804517, 0.8764843271744371389, 1.976213614152767750 ) ) ;
#61023=CARTESIAN_POINT ( 'NONE',  ( 4.577060434696750946, -0.0006114206978560799951, -1.825762228460731551 ) ) ;
#61025=CARTESIAN_POINT ( 'NONE',  ( 1.563680990848853591, 1.942865793614118930, -0.3330471066002506642 ) ) ;
#61026=CARTESIAN_POINT ( 'NONE',  ( 3.709155072767254868, 1.612916391665040416, -1.027221078234448859 ) ) ;
#61027=ORIENTED_EDGE ( 'NONE', *, *, #166608, .F. ) ;
#61028=CARTESIAN_POINT ( 'NONE',  ( 4.070725410728625704, 1.394476139410082638, -1.391156265790331581 ) ) ;
#61030=CARTESIAN_POINT ( 'NONE',  ( 5.724156413028869572, 1.872829174467111946, 0.5137480774947185136 ) ) ;
#61034=CARTESIAN_POINT ( 'NONE',  ( 5.853796514643677007, -1.537196951383312804, -1.461068456062891041 ) ) ;
#61036=CARTESIAN_POINT ( 'NONE',  ( 4.266199323752727146, 1.911794059647478949, -0.05023246155653331158 ) ) ;
#61041=CARTESIAN_POINT ( 'NONE',  ( 5.514319586171100518, -2.013265972089046230, 0.002284521408187425995 ) ) ;
#61043=CARTESIAN_POINT ( 'NONE',  ( 5.830640656690653678, 1.760721658632548037, 0.4824517239352192344 ) ) ;
#61044=CARTESIAN_POINT ( 'NONE',  ( 2.189971326302230903, -1.350648006375281929, -1.569233719104834890 ) ) ;
#61058=CARTESIAN_POINT ( 'NONE',  ( 3.850049338483009009, 0.2070581644968480517, -1.721641829124469059 ) ) ;
#61060=CARTESIAN_POINT ( 'NONE',  ( 0.9540663221972445207, -0.7486024665571254788, 1.930331157511067097 ) ) ;
#61061=CARTESIAN_POINT ( 'NONE',  ( 3.655961130333235776, 1.178038043211126817, 1.759042251235248600 ) ) ;
#61065=CARTESIAN_POINT ( 'NONE',  ( 0.3034763168169403169, -1.518637222489120919, -1.253724199518479354 ) ) ;
#61070=CARTESIAN_POINT ( 'NONE',  ( 3.697495799125404492, -0.6661743112182354487, 2.193330854740268343 ) ) ;
#61071=CARTESIAN_POINT ( 'NONE',  ( 0.2932112110246976044, 1.350478442433366677, 1.228755397233910696 ) ) ;
#61072=CARTESIAN_POINT ( 'NONE',  ( 3.621269620730773298, 1.642686141288721480, 0.9789267784374030557 ) ) ;
#61076=CARTESIAN_POINT ( 'NONE',  ( 1.617441171277278711, 1.676116182522195519, 1.114898189108826543 ) ) ;
#61077=CARTESIAN_POINT ( 'NONE',  ( 1.762477828903946442, -0.7011357286515782494, -1.832381215946830011 ) ) ;
#61081=CARTESIAN_POINT ( 'NONE',  ( 5.103505634659632584, -2.080644823048905412, 0.2041521072984452956 ) ) ;
#61082=CARTESIAN_POINT ( 'NONE',  ( 3.502600007508451352, 1.395586194379776712, -1.088321832170894288 ) ) ;
#61086=CARTESIAN_POINT ( 'NONE',  ( 5.964811824374402605, 0.1744345966951440507, -2.285673535861055594 ) ) ;
#61087=CARTESIAN_POINT ( 'NONE',  ( 5.367066450689647716, 1.675684007255513475, -0.4696764748959629809 ) ) ;
#61089=CARTESIAN_POINT ( 'NONE',  ( -0.1104750535120043037, 1.338503269012698116, -2.356272470560859755 ) ) ;
#61090=CARTESIAN_POINT ( 'NONE',  ( 4.305767739847966347, -1.508829150093475180, 0.8539562774845139703 ) ) ;
#61091=CARTESIAN_POINT ( 'NONE',  ( 5.916515574059204141, 0.8745146271147998807, 1.987442084954823773 ) ) ;
#61093=CARTESIAN_POINT ( 'NONE',  ( 0.4974488191052604535, -0.3042024069639309158, 2.095249342460514086 ) ) ;
#61094=CARTESIAN_POINT ( 'NONE',  ( 5.843750000000004441, 1.895863743164205140, 0.7852924748296741253 ) ) ;
#61096=CARTESIAN_POINT ( 'NONE',  ( 3.416937173653651794, 1.740928992956072952, 0.8250102540389223638 ) ) ;
#61098=CARTESIAN_POINT ( 'NONE',  ( 0.6279475770487872310, -0.3202071342675495425, 2.197987568497254074 ) ) ;
#61100=CARTESIAN_POINT ( 'NONE',  ( -0.2408018239684330541, 4.084923768815020395, -2.655285172934387372 ) ) ;
#61103=CARTESIAN_POINT ( 'NONE',  ( 2.983289111093189394, -2.053184633062016484, -0.8481636011889515103 ) ) ;
#61104=CARTESIAN_POINT ( 'NONE',  ( -0.02900071798683095947, 1.997299723774683455, -2.587491137808914488 ) ) ;
#61108=CARTESIAN_POINT ( 'NONE',  ( 0.4576579978108759050, -1.899619568183811058, -0.6767110947205197125 ) ) ;
#61110=CARTESIAN_POINT ( 'NONE',  ( 5.248506731170051509, -2.046683549694120252, -0.2560125357965719606 ) ) ;
#61114=CARTESIAN_POINT ( 'NONE',  ( 0.5261445748756715668, 1.690971295752751624, 0.5220769596525741685 ) ) ;
#61115=CARTESIAN_POINT ( 'NONE',  ( 6.188101721744481587, 1.447254432076927166, 0.9550205611794166938 ) ) ;
#61116=CARTESIAN_POINT ( 'NONE',  ( 5.214300491592821274, 1.611006010870178251, 0.6591642633846701571 ) ) ;
#61117=CARTESIAN_POINT ( 'NONE',  ( 2.560454162224240271, -1.578354536769586591, 1.662689614829175211 ) ) ;
#61119=CARTESIAN_POINT ( 'NONE',  ( 2.448939195788137013, 0.4911642875529352303, -1.774347143093172097 ) ) ;
#61122=CARTESIAN_POINT ( 'NONE',  ( 1.746812667857342349, -1.544096848276183209, 0.9736100143667850704 ) ) ;
#61123=CARTESIAN_POINT ( 'NONE',  ( 2.602185585689294367, -0.1948409242511044692, 2.006959980107574371 ) ) ;
#61126=CARTESIAN_POINT ( 'NONE',  ( 4.401466734191799901, 1.689890445582131084, 1.256493114684479329 ) ) ;
#61129=CARTESIAN_POINT ( 'NONE',  ( 2.629418614236479712, 0.1040367438073786233, -2.067886086930009970 ) ) ;
#61132=CARTESIAN_POINT ( 'NONE',  ( 4.442108405842562391, -1.305342523080333272, -1.670987904322115636 ) ) ;
#61133=CARTESIAN_POINT ( 'NONE',  ( 6.533835636172961259, -1.196796279342365210, -1.378804128639096849 ) ) ;
#61140=CARTESIAN_POINT ( 'NONE',  ( 6.275647701495586261, 0.3610785225884837746, -2.089460823871174266 ) ) ;
#61141=CARTESIAN_POINT ( 'NONE',  ( 1.044129769988952683, 0.8535497088724073311, -1.925424821390888663 ) ) ;
#61144=CARTESIAN_POINT ( 'NONE',  ( 6.069184012654499583, 1.640672622335254793, 0.8782983229575453965 ) ) ;
#61153=CARTESIAN_POINT ( 'NONE',  ( 2.664445928352857429, -0.7481792696971515388, -1.813797970468238985 ) ) ;
#61154=CARTESIAN_POINT ( 'NONE',  ( 1.253037233087474611, -1.703760181015579134, 1.330383891403746688 ) ) ;
#61158=CARTESIAN_POINT ( 'NONE',  ( 2.706025971585944490, -1.282006620817040643, -1.167505586895122072 ) ) ;
#61159=CARTESIAN_POINT ( 'NONE',  ( 2.694910210795556260, -0.5461130550479543766, 1.652493440627414323 ) ) ;
#61162=CIRCLE ( 'NONE', #71489, 0.04999999999999883010 ) ;
#61163=CARTESIAN_POINT ( 'NONE',  ( 2.372422516638694745, -0.4444355326964634090, 1.966343308868031103 ) ) ;
#61164=CARTESIAN_POINT ( 'NONE',  ( 6.825078400183510752, 2.433016701115862102, 2.426111979085682879 ) ) ;
#61166=CARTESIAN_POINT ( 'NONE',  ( 1.076956826339631856, -0.04624765943369788662, -1.971079714834519159 ) ) ;
#61169=CARTESIAN_POINT ( 'NONE',  ( 6.293217207623316156, -0.1008467329366956045, -1.909883259500498198 ) ) ;
#61174=CARTESIAN_POINT ( 'NONE',  ( 0.9440171659906453350, -1.283125807103436600, -1.559678575094858077 ) ) ;
#61176=CARTESIAN_POINT ( 'NONE',  ( 5.526528793889518454, 1.380124021263717804, -1.849252619965065847 ) ) ;
#61177=CARTESIAN_POINT ( 'NONE',  ( 6.021922112293466967, 1.933069186966931863, -0.3339256516061983038 ) ) ;
#61178=CARTESIAN_POINT ( 'NONE',  ( 3.098438489093110704, 1.946378968836332213, 0.2448508753878294586 ) ) ;
#61182=CARTESIAN_POINT ( 'NONE',  ( 0.6732554233833996093, 1.864234297354839143, -1.003953180072956419 ) ) ;
#61185=CARTESIAN_POINT ( 'NONE',  ( 1.974305314296275649, -0.08955604370030831318, -1.839086841257123073 ) ) ;
#61187=CARTESIAN_POINT ( 'NONE',  ( 3.151577601795185757, 1.966304690962265234, -0.4465026806126579095 ) ) ;
#61189=CARTESIAN_POINT ( 'NONE',  ( 2.601940685209406467, 1.502730264585940168, 1.496503045097858919 ) ) ;
#61194=CARTESIAN_POINT ( 'NONE',  ( 3.427077464676528074, 0.04692547926744317088, 2.060408731095995094 ) ) ;
#61196=CARTESIAN_POINT ( 'NONE',  ( 0.6965153189463432204, 1.505040478001760107, 1.060415605250275339 ) ) ;
#61198=CARTESIAN_POINT ( 'NONE',  ( -0.02224634325202062834, 1.297472808610355521, -2.537530276547406149 ) ) ;
#61202=CARTESIAN_POINT ( 'NONE',  ( 2.917521460708580872, -0.2248114924257374192, 2.251233801775154308 ) ) ;
#61204=CARTESIAN_POINT ( 'NONE',  ( 2.232397805642115873, 1.180933449141470026, -1.373882015996011452 ) ) ;
#61205=CARTESIAN_POINT ( 'NONE',  ( 2.958105166426743704, -1.137214127935105790, 1.541527475959689308 ) ) ;
#61206=CARTESIAN_POINT ( 'NONE',  ( 4.088381982606685838, 1.110138344689771239, -1.747393465062855533 ) ) ;
#61209=CARTESIAN_POINT ( 'NONE',  ( 1.885558555406470660, 1.358073900086468333, 1.429321910850362753 ) ) ;
#61210=CARTESIAN_POINT ( 'NONE',  ( 6.428350398238483088, 1.106843121268024976, -1.576624894639609309 ) ) ;
#61211=CARTESIAN_POINT ( 'NONE',  ( 3.256579335763456040, -1.417408692332474462, 1.220890361658559575 ) ) ;
#61212=CARTESIAN_POINT ( 'NONE',  ( 2.456097291302907770, 0.6137686719557032822, -2.224517260854632639 ) ) ;
#61214=CARTESIAN_POINT ( 'NONE',  ( 2.365471783816187834, -0.4113058309756181807, 1.814853103561973935 ) ) ;
#61216=CARTESIAN_POINT ( 'NONE',  ( 6.725054104113727504, -1.884248279909329638, -0.8396177084525523471 ) ) ;
#61221=CARTESIAN_POINT ( 'NONE',  ( 6.809622064836790223, -0.4623527835773094119, 2.061910140347056331 ) ) ;
#61223=CARTESIAN_POINT ( 'NONE',  ( 5.536455037250767930, 2.128579029500421438, 0.3755436860354774420 ) ) ;
#61224=CARTESIAN_POINT ( 'NONE',  ( -0.05247081622378191312, -1.844958069526716926, 0.8224554107575526851 ) ) ;
#61229=CARTESIAN_POINT ( 'NONE',  ( 6.825078400183544503, 2.075476428726834577, 2.163873318353096931 ) ) ;
#61232=CARTESIAN_POINT ( 'NONE',  ( 5.085172837459294826, 1.651341431264556014, 1.157102043685846793 ) ) ;
#61237=CARTESIAN_POINT ( 'NONE',  ( 5.823154874416164084, -0.05760400987671504547, 2.161107263091876618 ) ) ;
#61241=CARTESIAN_POINT ( 'NONE',  ( 0.1049102937123137097, -0.09321989032292328503, 1.913444960606479395 ) ) ;
#61243=DIRECTION ( 'NONE',  ( 1.016547956922408957E-15, 1.000000000000000000, -4.622230424712075819E-32 ) ) ;
#61244=CARTESIAN_POINT ( 'NONE',  ( 1.804884324593715839, 1.432779585713826576, 0.9600471282974596399 ) ) ;
#61248=CARTESIAN_POINT ( 'NONE',  ( 1.000807349803897628, 1.442299932730039869, 1.025250199436118503 ) ) ;
#61250=CARTESIAN_POINT ( 'NONE',  ( 2.455728839946738518, -1.493258543598206201, -1.350275873876593868 ) ) ;
#61251=CARTESIAN_POINT ( 'NONE',  ( 4.506973327934083784, 1.708129512224244806, -1.397202154207459524 ) ) ;
#61252=CARTESIAN_POINT ( 'NONE',  ( 5.102462520977921301, 2.164757797245045357, 0.1666947352320021780 ) ) ;
#61253=ORIENTED_EDGE ( 'NONE', *, *, #183399, .F. ) ;
#61256=CARTESIAN_POINT ( 'NONE',  ( 3.194099758881031814, 1.346771490053525033, 1.637864368873870990 ) ) ;
#61257=CARTESIAN_POINT ( 'NONE',  ( 3.427361390312729572, -1.528753972193249933, -1.314983687342549556 ) ) ;
#61258=CARTESIAN_POINT ( 'NONE',  ( 2.970771795020191064, -1.368765343908146415, 1.186782720094860855 ) ) ;
#61264=CARTESIAN_POINT ( 'NONE',  ( 5.918537399722813674, 1.222626809077583587, -1.356019982345892050 ) ) ;
#61266=CARTESIAN_POINT ( 'NONE',  ( 1.499098398830187362, -0.2305585200724231121, 1.901688874922660588 ) ) ;
#61272=CARTESIAN_POINT ( 'NONE',  ( 5.014612968065254250, 1.493337269798940881, -1.563205770552501761 ) ) ;
#61275=CARTESIAN_POINT ( 'NONE',  ( 3.305043459179863419, -0.4174351347619070784, -2.078937965663613774 ) ) ;
#61278=CARTESIAN_POINT ( 'NONE',  ( 4.024654096683129900, 1.870930367033913688, 0.6213144229534044438 ) ) ;
#61279=CARTESIAN_POINT ( 'NONE',  ( 6.029550621839829816, -0.2273517531893587407, 1.898748578088353733 ) ) ;
#61282=CARTESIAN_POINT ( 'NONE',  ( 5.805892041792804825, -1.178307743425134335, -1.758994673012766574 ) ) ;
#61284=CARTESIAN_POINT ( 'NONE',  ( 0.8013346216862862192, -1.776568573310655985, 1.062853015585236482 ) ) ;
#61285=CARTESIAN_POINT ( 'NONE',  ( 2.220557385006210804, 0.0001418518128949025625, 1.942124712491780869 ) ) ;
#61289=CARTESIAN_POINT ( 'NONE',  ( 3.099644000116580589, -2.088226275799191622, 0.1030096337034935861 ) ) ;
#61292=CARTESIAN_POINT ( 'NONE',  ( 0.2053161149570548183, 1.340855080820763545, 1.218213988936674763 ) ) ;
#61294=CARTESIAN_POINT ( 'NONE',  ( 5.197975494389605267, -0.7968864405506062010, 2.058166701804148957 ) ) ;
#61296=CARTESIAN_POINT ( 'NONE',  ( 3.505080564089088746, 1.740947047783932611, -1.355986173033681075 ) ) ;
#61299=CARTESIAN_POINT ( 'NONE',  ( 2.016128127738999076, -1.911839501640894001, 0.04842977492004740814 ) ) ;
#61301=CARTESIAN_POINT ( 'NONE',  ( 5.020015195830264787, 2.048331326439792210, -0.3003445753073652469 ) ) ;
#61303=CARTESIAN_POINT ( 'NONE',  ( 3.168983506954273999, -1.996715753333128118, -0.8287754370841573515 ) ) ;
#61304=CARTESIAN_POINT ( 'NONE',  ( 4.476244563333130699, -2.125884358948509689, -0.5320566845071761364 ) ) ;
#61313=CARTESIAN_POINT ( 'NONE',  ( -0.1102773484824129541, -0.006951161900758274365, -2.203378182130751206 ) ) ;
#61314=CARTESIAN_POINT ( 'NONE',  ( -0.03452862918938356951, -1.956592590566148093, -0.4871966601913205186 ) ) ;
#61318=CARTESIAN_POINT ( 'NONE',  ( 5.067269747081383890, 1.798595138155817841, 1.025117745595036878 ) ) ;
#61319=CARTESIAN_POINT ( 'NONE',  ( 4.951747152513418904, 0.6024649636334912239, -1.829943702413504791 ) ) ;
#61320=CARTESIAN_POINT ( 'NONE',  ( 0.4215001937674204280, -1.427952733550428288, -1.423947716221201976 ) ) ;
#61324=CARTESIAN_POINT ( 'NONE',  ( 4.434397634191796556, -1.137439385922611290, 1.607554744723362017 ) ) ;
#61325=CARTESIAN_POINT ( 'NONE',  ( 0.05887529153619439071, -1.959562692596405364, -0.9812908054248059564 ) ) ;
#61326=CARTESIAN_POINT ( 'NONE',  ( 3.879382553896340013, 1.718498013671100777, -0.6167319420108534622 ) ) ;
#61333=CARTESIAN_POINT ( 'NONE',  ( 1.259045258496578557, 1.813921241667546758, -0.3151448728593714277 ) ) ;
#61334=CARTESIAN_POINT ( 'NONE',  ( 4.640889591357927557, 1.927823495868080439, 0.5801764560204000221 ) ) ;
#61335=CARTESIAN_POINT ( 'NONE',  ( 0.8964060800229460835, 0.1715710081350088068, 2.292006659179766537 ) ) ;
#61336=CARTESIAN_POINT ( 'NONE',  ( 5.260583753728677259, -0.6573284944802314511, -1.848511375219172415 ) ) ;
#61342=CARTESIAN_POINT ( 'NONE',  ( 0.9606207175340542026, -1.891748053602306578, -0.8905051939756128965 ) ) ;
#61343=CARTESIAN_POINT ( 'NONE',  ( 6.508682224664005922, 1.308065493886721775, -1.192407281889706905 ) ) ;
#61345=CARTESIAN_POINT ( 'NONE',  ( -0.1104750535120025690, -0.004616138082884356161, -2.103378236956428893 ) ) ;
#61346=CARTESIAN_POINT ( 'NONE',  ( 2.542201289624079319, -1.445942355291447434, 0.9683529963873671598 ) ) ;
#61350=CARTESIAN_POINT ( 'NONE',  ( 1.558790235068749030, -1.477961618093760032, -0.8890178537931183733 ) ) ;
#61351=CARTESIAN_POINT ( 'NONE',  ( 2.068174269828721101, -1.345378145056834063, 1.729934933326432445 ) ) ;
#61352=CARTESIAN_POINT ( 'NONE',  ( 3.686314334879085663, -1.088174899301070253, 1.919869060924610293 ) ) ;
#61355=CARTESIAN_POINT ( 'NONE',  ( 2.167058194802372828, 1.611091607626200961, -1.455523108145313937 ) ) ;
#61356=CARTESIAN_POINT ( 'NONE',  ( 1.207329354700342305, -0.4456725867950651621, 1.770335049871730071 ) ) ;
#61357=CARTESIAN_POINT ( 'NONE',  ( 3.485668972010677269, -0.6104075878305641467, 2.027481811383638810 ) ) ;
#61358=CARTESIAN_POINT ( 'NONE',  ( 6.539320575229250920, 2.072231551265828475, 2.205269387046896679 ) ) ;
#61361=CARTESIAN_POINT ( 'NONE',  ( 3.175583430956610886, 1.455732557240730696, 1.770799584264992399 ) ) ;
#61363=CARTESIAN_POINT ( 'NONE',  ( 0.07755575628181492209, 4.082361791518872352, -2.743585103993382734 ) ) ;
#61366=CARTESIAN_POINT ( 'NONE',  ( 5.795613637301100241, 2.053263797698097637, -0.8479724704701059323 ) ) ;
#61372=CARTESIAN_POINT ( 'NONE',  ( 3.779922787921150995, 1.701948043757589124, -1.081065327119046016 ) ) ;
#61374=CARTESIAN_POINT ( 'NONE',  ( 2.588800687925230992, 1.999571085336487641, 0.5053362289856622169 ) ) ;
#61380=CARTESIAN_POINT ( 'NONE',  ( 4.646525747415945595, -1.761044916313101671, 1.304081410864160739 ) ) ;
#61381=CARTESIAN_POINT ( 'NONE',  ( 2.338517726396415863, 0.5350873343827439177, -1.944071628254496087 ) ) ;
#61382=CARTESIAN_POINT ( 'NONE',  ( 2.085277916773973228, -0.7859315772556186852, 1.665205719185464561 ) ) ;
#61384=CARTESIAN_POINT ( 'NONE',  ( 6.756878055424797580, -1.408711550780303634, 1.160885376127060775 ) ) ;
#61386=CARTESIAN_POINT ( 'NONE',  ( 5.243177039506740300, -1.943355607328334678, 1.158386780943015504 ) ) ;
#61388=CARTESIAN_POINT ( 'NONE',  ( 0.2937649352797070401, 1.562083697590540998, 1.412785709394439815 ) ) ;
#61397=CARTESIAN_POINT ( 'NONE',  ( 3.094184762719538906, 1.412074837861827303, 1.714815191315356868 ) ) ;
#61401=CARTESIAN_POINT ( 'NONE',  ( 4.527759979645433752, 1.903474890065796732, -0.4746247275292309609 ) ) ;
#61409=CARTESIAN_POINT ( 'NONE',  ( 3.217144136595586179, 1.669276650691432495, -1.307696563879121365 ) ) ;
#61411=CARTESIAN_POINT ( 'NONE',  ( 4.469695567000064429, 2.097540297429688838, -0.5223010940857697459 ) ) ;
#61412=CARTESIAN_POINT ( 'NONE',  ( 4.159580895514263688, 0.8717668643758098579, 1.621812032879976329 ) ) ;
#61415=CARTESIAN_POINT ( 'NONE',  ( 5.595574051893665413, -1.740516469239574704, 0.006108698158355239591 ) ) ;
#61418=CARTESIAN_POINT ( 'NONE',  ( 3.239309987758617115, -1.907233169736745060, 1.017530501952010447 ) ) ;
#61419=CARTESIAN_POINT ( 'NONE',  ( 5.940779784064256219, 1.198679029392090589, 1.620932600025201786 ) ) ;
#61421=CARTESIAN_POINT ( 'NONE',  ( 2.149508875876861236, -1.735919364271593768, -1.288018159417112729 ) ) ;
#61422=CARTESIAN_POINT ( 'NONE',  ( 3.391827608253958015, -0.8021585586163967330, 1.800962559972321575 ) ) ;
#61423=CARTESIAN_POINT ( 'NONE',  ( 4.229980187955574067, 1.905242447948073403, 0.3755566216582290617 ) ) ;
#61432=CARTESIAN_POINT ( 'NONE',  ( 2.503190323335769740, 1.772782541628318720, -1.313999973512294472 ) ) ;
#61434=CARTESIAN_POINT ( 'NONE',  ( 6.174655700867183405, 1.320063289540554408, -1.451312704123429498 ) ) ;
#61439=CARTESIAN_POINT ( 'NONE',  ( 6.287735281038357549, 1.518688880046001444, 1.601449620450722700 ) ) ;
#61440=CARTESIAN_POINT ( 'NONE',  ( 5.507694354943953208, -0.8313836724207699369, -1.642813217252625524 ) ) ;
#61444=CARTESIAN_POINT ( 'NONE',  ( 5.941668366282724101, -1.996146358238064522, 0.7160658055916299114 ) ) ;
#61448=CARTESIAN_POINT ( 'NONE',  ( 6.116494506269664733, 1.387434351230539598, -1.523912472565646770 ) ) ;
#61450=CARTESIAN_POINT ( 'NONE',  ( 1.925991809680915878, 0.9530580284189617002, 1.598336604343030931 ) ) ;
#61451=CARTESIAN_POINT ( 'NONE',  ( 3.491602800004707241, -1.839307750763185645, -0.08696504193297231733 ) ) ;
#61458=CARTESIAN_POINT ( 'NONE',  ( 3.317197348578094562, 1.995112415077514356, 0.9436014139095407760 ) ) ;
#61459=CARTESIAN_POINT ( 'NONE',  ( 6.309908665641647652, -2.246456703917932618, 0.2676860584361096529 ) ) ;
#61461=CARTESIAN_POINT ( 'NONE',  ( 5.519718948577209794, -0.4320008574366646648, 1.759211659423996155 ) ) ;
#61462=CARTESIAN_POINT ( 'NONE',  ( 0.04025042243083893495, 0.7762349914572730381, 1.861342399428978389 ) ) ;
#61464=CARTESIAN_POINT ( 'NONE',  ( 6.332864056472936376, 0.1854757364097951722, 1.861418627818342664 ) ) ;
#61465=CARTESIAN_POINT ( 'NONE',  ( 5.567032834676129305, -1.504811603839781631, 1.179860560037985895 ) ) ;
#61467=CARTESIAN_POINT ( 'NONE',  ( 0.6548940681232479077, -1.578012236938080015, -1.004313744925364071 ) ) ;
#61469=CARTESIAN_POINT ( 'NONE',  ( 1.798064920797682653, -0.9548589541341389042, -1.776165177175797583 ) ) ;
#61471=CARTESIAN_POINT ( 'NONE',  ( 3.651088154774425387, -1.721711045478736102, 1.212656735320973400 ) ) ;
#61476=CARTESIAN_POINT ( 'NONE',  ( 3.498311158119755682, -0.9917195014866404534, 1.759444004082431068 ) ) ;
#61480=CARTESIAN_POINT ( 'NONE',  ( 2.724079341238437646, -1.242159841233332562, -1.768869243570107885 ) ) ;
#61486=CARTESIAN_POINT ( 'NONE',  ( 0.3972422249299937258, 0.3718246657071262451, 2.138946393809169511 ) ) ;
#61490=CARTESIAN_POINT ( 'NONE',  ( 2.472451708263478931, -2.098117355222902436, -0.6331711661175795092 ) ) ;
#61491=CARTESIAN_POINT ( 'NONE',  ( 6.883263157960365142, -0.001323150302089473379, 1.953658984494692330 ) ) ;
#61492=CARTESIAN_POINT ( 'NONE',  ( 2.096875702627752691, -0.6037365238656807742, -2.180425337281781673 ) ) ;
#61498=CARTESIAN_POINT ( 'NONE',  ( 4.481574309046215454, 1.155277477370730832, 1.340746495013745543 ) ) ;
#61501=CARTESIAN_POINT ( 'NONE',  ( 0.8507726699197988296, 0.6114878368043925594, 2.015236747771311343 ) ) ;
#61505=CARTESIAN_POINT ( 'NONE',  ( 6.603150281434943203, -0.1430492952050037847, 1.984088717376513822 ) ) ;
#61510=CARTESIAN_POINT ( 'NONE',  ( 4.223419137798128276, -1.790188510885984297, 0.5427707113358354318 ) ) ;
#61511=CARTESIAN_POINT ( 'NONE',  ( 4.592674910654532816, 2.029287475768901228, 0.4089837765668055680 ) ) ;
#61516=FILL_AREA_STYLE_COLOUR ( '', #169905 ) ;
#61517=CARTESIAN_POINT ( 'NONE',  ( 6.315313271410192719, -0.2696487299426887363, 2.144762774094311375 ) ) ;
#61519=CARTESIAN_POINT ( 'NONE',  ( 3.508209890309890167, 1.962046631884439174, 0.002529298861464468473 ) ) ;
#61520=CARTESIAN_POINT ( 'NONE',  ( 0.5970295589228531430, 1.038836743281198238, -1.727736137786803461 ) ) ;
#61524=CARTESIAN_POINT ( 'NONE',  ( 0.8779421195594695471, -1.044212112285093585, 1.551753832453220294 ) ) ;
#61526=CARTESIAN_POINT ( 'NONE',  ( 3.181892525975566155, 1.963218260121324166, -0.4451317699624996460 ) ) ;
#61528=CARTESIAN_POINT ( 'NONE',  ( 2.091562808734966250, -0.4604446976123123814, 2.066416142659666111 ) ) ;
#61530=CARTESIAN_POINT ( 'NONE',  ( 3.912603064140641074, 0.7423916865902054907, 1.932869565047180549 ) ) ;
#61532=CARTESIAN_POINT ( 'NONE',  ( 0.5914941650546343688, -0.7489122546765265565, 1.952206342558031160 ) ) ;
#61534=CARTESIAN_POINT ( 'NONE',  ( 5.491160184941096922, 1.609068807629027820, -0.8623064814072267659 ) ) ;
#61539=CARTESIAN_POINT ( 'NONE',  ( 6.264705869774118696, -1.564926740429407603, 1.556175991035801287 ) ) ;
#61541=CARTESIAN_POINT ( 'NONE',  ( 4.600206319907148789, -0.8982956317880007591, 1.688143452400918454 ) ) ;
#61555=FILL_AREA_STYLE ('',( #77801 ) ) ;
#61559=CARTESIAN_POINT ( 'NONE',  ( 2.500782807205007341, 0.4266943614082556180, 1.922505800989605218 ) ) ;
#61561=CARTESIAN_POINT ( 'NONE',  ( 2.952750085323506024, -1.864176452196796507, -0.7691048347045483791 ) ) ;
#61564=CARTESIAN_POINT ( 'NONE',  ( 6.827182134110199030, 6.034458849223407029, 2.683941674059683979 ) ) ;
#61565=CARTESIAN_POINT ( 'NONE',  ( 3.644632398932126094, -1.791719913761843364, 1.261548167004488130 ) ) ;
#61567=CARTESIAN_POINT ( 'NONE',  ( 2.538006180297863068, 0.9099634639774205613, -1.697936525022441190 ) ) ;
#61569=CARTESIAN_POINT ( 'NONE',  ( 0.1331565106231571705, 2.881392620029461504, -2.434650611646618223 ) ) ;
#61576=CARTESIAN_POINT ( 'NONE',  ( 5.126429434416579056, 0.1410513515392505246, 1.835921608166577013 ) ) ;
#61577=CARTESIAN_POINT ( 'NONE',  ( 1.805339258485965992, 1.750370858315702272, -0.9942575048343755828 ) ) ;
#61578=CARTESIAN_POINT ( 'NONE',  ( 3.884340333706528092, -0.1737987063687232436, 2.291882653078499477 ) ) ;
#61579=CARTESIAN_POINT ( 'NONE',  ( -0.1290005225502675879, 2.860092606084875033, -2.662085506130333457 ) ) ;
#61580=CARTESIAN_POINT ( 'NONE',  ( 2.096333906143353243, 1.839810448830980105, 0.2789567515945317600 ) ) ;
#61583=CARTESIAN_POINT ( 'NONE',  ( 6.011958326525193463, -0.6379227081053112647, 1.803018720113582773 ) ) ;
#61586=CARTESIAN_POINT ( 'NONE',  ( 4.792568760853118448, 1.737405308921141645, -1.162709912544395152 ) ) ;
#61587=CARTESIAN_POINT ( 'NONE',  ( 3.168673215318769110, -1.727878594304608217, -0.7172629358194044791 ) ) ;
#61591=CARTESIAN_POINT ( 'NONE',  ( 6.586556832619708146, -1.693200007625778492, -0.3281344310326217428 ) ) ;
#61593=CARTESIAN_POINT ( 'NONE',  ( 1.072469862579095379, -0.7803941858975007584, 1.548669665330544953 ) ) ;
#61597=FILL_AREA_STYLE_COLOUR ( '', #138096 ) ;
#61598=CARTESIAN_POINT ( 'NONE',  ( 5.524361701572801486, 1.063745579927848794, 1.892525341434271091 ) ) ;
#61599=CARTESIAN_POINT ( 'NONE',  ( 5.004447790439923160, -0.6182884515001166870, -1.717943145347331502 ) ) ;
#61600=CARTESIAN_POINT ( 'NONE',  ( 1.903102209365503894, -1.660057620245494636, 1.045011325395063251 ) ) ;
#61601=CARTESIAN_POINT ( 'NONE',  ( 0.2986504545328653726, 1.456477371935499088, -1.536899124724122601 ) ) ;
#61605=CARTESIAN_POINT ( 'NONE',  ( 2.631617588254760776, -0.2053842346896698201, 2.110501108333342035 ) ) ;
#61610=CARTESIAN_POINT ( 'NONE',  ( 6.930535145478218695, -1.343193056793217988, 1.706537673033242664 ) ) ;
#61613=CARTESIAN_POINT ( 'NONE',  ( 2.948112417477159575, -1.493347798232132373, -1.644555409524293577 ) ) ;
#61615=CARTESIAN_POINT ( 'NONE',  ( 0.3703313985920617668, -0.2899475993979240274, -2.280306813078219363 ) ) ;
#61617=CARTESIAN_POINT ( 'NONE',  ( 6.051645708474242547, 1.558200330177769377, 1.351431136778310726 ) ) ;
#61621=CARTESIAN_POINT ( 'NONE',  ( 0.1329588055935213564, 1.397696041676167678, -2.105440929937075989 ) ) ;
#61622=CARTESIAN_POINT ( 'NONE',  ( 5.601068772352080671, -0.4412860211496574814, 1.787476196608045464 ) ) ;
#61627=CARTESIAN_POINT ( 'NONE',  ( 3.434305118180380756, 1.682496158873967529, 0.3786907865064632062 ) ) ;
#61628=CARTESIAN_POINT ( 'NONE',  ( 0.8488426437929346147, -1.825078332268307513, -0.8578388575243289793 ) ) ;
#61629=CARTESIAN_POINT ( 'NONE',  ( 2.655266180633470086, 1.232652804806773528, 1.940110688254999438 ) ) ;
#61631=CARTESIAN_POINT ( 'NONE',  ( 2.812116484403729633, -2.238188867732244791, 0.3292703641907517298 ) ) ;
#61632=CARTESIAN_POINT ( 'NONE',  ( 4.881522348829672175, 1.965384978258335247, -0.7572991678025364770 ) ) ;
#61634=CARTESIAN_POINT ( 'NONE',  ( 4.059615542810626643, 1.756569389245852042, -0.2146349482602862846 ) ) ;
#61637=CARTESIAN_POINT ( 'NONE',  ( 6.198803536200695241, 1.903451089567553822, 1.277169966706873883 ) ) ;
#61638=CARTESIAN_POINT ( 'NONE',  ( 4.804558796598876746, 1.603369264058150279, 0.9048477820690554729 ) ) ;
#61642=CARTESIAN_POINT ( 'NONE',  ( 4.259861650310483583, 1.032037387010206198, 1.933225914978464299 ) ) ;
#61648=CARTESIAN_POINT ( 'NONE',  ( 3.738824155997504395, 0.2837420414000761393, 1.905379044178076686 ) ) ;
#61651=CARTESIAN_POINT ( 'NONE',  ( 6.310795917644286490, -0.5669512758468171487, -2.043305014803979525 ) ) ;
#61659=CARTESIAN_POINT ( 'NONE',  ( 2.665247472508886606, 0.9327722559238416089, 1.469172323213832065 ) ) ;
#61664=CARTESIAN_POINT ( 'NONE',  ( 6.280167721515548251, -1.160692707240444710, 1.823489969145650313 ) ) ;
#61667=CARTESIAN_POINT ( 'NONE',  ( 6.280167721515548251, -1.160692707240444710, 1.823489969145650313 ) ) ;
#61671=CARTESIAN_POINT ( 'NONE',  ( 0.2275331484566482099, -1.145445245298154946, -1.479381579510357980 ) ) ;
#61672=CARTESIAN_POINT ( 'NONE',  ( 5.905553417332951582, 0.3413034225961882884, 1.699694455674398919 ) ) ;
#61674=CARTESIAN_POINT ( 'NONE',  ( 3.632539538618652752, 0.3231117836275976818, 2.167502126216628522 ) ) ;
#61675=CARTESIAN_POINT ( 'NONE',  ( 3.856711057068095805, 0.8274802039119494301, 2.154294293310366371 ) ) ;
#61676=CARTESIAN_POINT ( 'NONE',  ( 5.659468487958158711, 0.4062720387869744876, -2.020156115232510707 ) ) ;
#61677=CARTESIAN_POINT ( 'NONE',  ( 1.429522090333503304, 0.9575595492820774268, -1.689375863068052430 ) ) ;
#61681=CARTESIAN_POINT ( 'NONE',  ( 4.447591161967184625, -1.937652164471121763, 0.8620916771790232414 ) ) ;
#61683=CARTESIAN_POINT ( 'NONE',  ( 1.881482635453747720, -0.5404922439061732309, -1.942541187959702764 ) ) ;
#61685=CARTESIAN_POINT ( 'NONE',  ( 5.227635310461984375, -2.096914331502324647, 0.6878394029543041244 ) ) ;
#61694=CARTESIAN_POINT ( 'NONE',  ( 4.733308493599470701, -1.885100903509504544, 0.8332785242166717010 ) ) ;
#61699=CARTESIAN_POINT ( 'NONE',  ( 5.057288377774205479, -1.731171949422895651, 1.040023186547271328 ) ) ;
#61705=CARTESIAN_POINT ( 'NONE',  ( 2.887629844759795450, 1.456389637235107948, 1.458414562493230759 ) ) ;
#61706=CARTESIAN_POINT ( 'NONE',  ( 2.883435573726996548, -0.5880205015329244000, -1.928751729079546173 ) ) ;
#61712=CARTESIAN_POINT ( 'NONE',  ( 2.706407486732204770, -1.492025830231600070, -1.356093404896424826 ) ) ;
#61713=CARTESIAN_POINT ( 'NONE',  ( 2.343484645521694887, 1.840739972059933560, 0.04548452486473342216 ) ) ;
#61714=CARTESIAN_POINT ( 'NONE',  ( 0.5402173299829955422, -1.636151841282366126, -1.627667753820499330 ) ) ;
#61716=CARTESIAN_POINT ( 'NONE',  ( 3.005316911853897821, 1.824354345256746557, 1.159134172154026032 ) ) ;
#61719=CARTESIAN_POINT ( 'NONE',  ( 2.794613785990595733, -2.145299970026095071, 0.8252070097543462435 ) ) ;
#61722=CARTESIAN_POINT ( 'NONE',  ( 1.463515404423965105, 1.843522461416190250, -0.3164952454337774390 ) ) ;
#61723=CARTESIAN_POINT ( 'NONE',  ( 5.963742398600946792, 1.942370021616221409, -0.3365726279523760800 ) ) ;
#61727=CARTESIAN_POINT ( 'NONE',  ( 1.014635385311330795, -0.9952708415592588231, -1.969785480804244315 ) ) ;
#61728=CARTESIAN_POINT ( 'NONE',  ( 6.232888004217203459, -1.964670499678453197, -0.6532144590316590893 ) ) ;
#61731=CARTESIAN_POINT ( 'NONE',  ( 6.639320575229281651, 0.5623622132289189945, 2.255000583061476771 ) ) ;
#61732=CARTESIAN_POINT ( 'NONE',  ( 4.539890248181537302, 0.8439850759212139675, -1.781816264247655157 ) ) ;
#61733=CARTESIAN_POINT ( 'NONE',  ( 0.07077104593807002908, 0.8175350930016941353, 1.956879683024402183 ) ) ;
#61735=CARTESIAN_POINT ( 'NONE',  ( 4.530063604893081575, -1.417328398590127714, -1.821081770091488083 ) ) ;
#61737=CARTESIAN_POINT ( 'NONE',  ( 2.008709601793839283, 0.6428708581102732245, 1.959923294053036669 ) ) ;
#61744=CARTESIAN_POINT ( 'NONE',  ( 4.229095133649480864, -2.024433085375398900, -0.7850780064641171840 ) ) ;
#61746=CARTESIAN_POINT ( 'NONE',  ( 3.860763913883006992, 0.2215400755124704024, -1.827792592973469743 ) ) ;
#61748=CARTESIAN_POINT ( 'NONE',  ( 6.720655732516666703, 0.5845450044974825898, 1.978693153076715783 ) ) ;
#61749=CARTESIAN_POINT ( 'NONE',  ( 5.021103811603734535, -2.081066139062941023, 0.6872292908843835590 ) ) ;
#61751=CARTESIAN_POINT ( 'NONE',  ( 5.911039803662155201, 1.992093809783651803, 1.072660102914186897 ) ) ;
#61758=CARTESIAN_POINT ( 'NONE',  ( 1.287592460671227457, -0.8000790430911768336, 1.578758917787604021 ) ) ;
#61760=CARTESIAN_POINT ( 'NONE',  ( 5.197907085625908863, 1.353584514550598472, 1.490229472901122065 ) ) ;
#61762=CARTESIAN_POINT ( 'NONE',  ( 4.401466734191799901, 1.689890445582131084, 1.256493114684479329 ) ) ;
#61763=CARTESIAN_POINT ( 'NONE',  ( 2.337376834759529398, 0.5087095155123841916, -1.846764813590465515 ) ) ;
#61765=CARTESIAN_POINT ( 'NONE',  ( 3.367590298639517421, -0.3867537717311599343, 1.931019599036578160 ) ) ;
#61766=CARTESIAN_POINT ( 'NONE',  ( 5.801037524829370184, -0.3003419868748377630, -1.997221587554024458 ) ) ;
#61768=CARTESIAN_POINT ( 'NONE',  ( 1.744777856283234785, -1.581906188472384400, 0.9981555316627908070 ) ) ;
#61769=CARTESIAN_POINT ( 'NONE',  ( 5.004412211769132313, -0.5859011197271257743, -1.622467267129880097 ) ) ;
#61770=CARTESIAN_POINT ( 'NONE',  ( 1.002048865836258518, -0.8573748960705518396, 1.709468765625526521 ) ) ;
#61772=CARTESIAN_POINT ( 'NONE',  ( 0.9970219447392356660, -0.5395372827587068265, -2.139793933917451874 ) ) ;
#61782=CARTESIAN_POINT ( 'NONE',  ( 1.469279758060073160, 1.824989553406907383, 0.9776941847434923449 ) ) ;
#61787=CARTESIAN_POINT ( 'NONE',  ( 0.2760433103432077262, 1.997375541027920587, -0.2984889601853820129 ) ) ;
#61790=CARTESIAN_POINT ( 'NONE',  ( 6.865691018405424728, -0.4312029709039078007, 1.920920986087648163 ) ) ;
#61792=CARTESIAN_POINT ( 'NONE',  ( 4.516953773913958692, 2.015725170860783066, -0.04666989112152990227 ) ) ;
#61793=CARTESIAN_POINT ( 'NONE',  ( 4.223789564141206654, 0.8136391335250325874, -1.734469729061314913 ) ) ;
#61794=CARTESIAN_POINT ( 'NONE',  ( 3.122796855005858241, 0.05607861761174406934, 2.191015320347329709 ) ) ;
#61797=CARTESIAN_POINT ( 'NONE',  ( 4.992444313356595664, -1.114831962662912845, 1.676160436541684229 ) ) ;
#61800=CARTESIAN_POINT ( 'NONE',  ( 5.782842150838196638, 1.730585719646136056, -1.219460781990765463 ) ) ;
#61802=CARTESIAN_POINT ( 'NONE',  ( 3.526972370393847811, -1.930915134098612373, 0.8022322841883463562 ) ) ;
#61804=CARTESIAN_POINT ( 'NONE',  ( 1.641173577361688896, -1.245895879902914727, -1.192971367628747448 ) ) ;
#61806=CARTESIAN_POINT ( 'NONE',  ( 4.851869265964163347, -1.501451181749386743, -1.497782127133556296 ) ) ;
#61815=CARTESIAN_POINT ( 'NONE',  ( 1.453448513857479973, -1.311971142947904401, -1.249319819763055950 ) ) ;
#61819=ORIENTED_EDGE ( 'NONE', *, *, #66399, .F. ) ;
#61821=CARTESIAN_POINT ( 'NONE',  ( 3.105918186854994989, -0.7317858000257486673, 1.657260211903899938 ) ) ;
#61822=CARTESIAN_POINT ( 'NONE',  ( 6.539320575229279342, 6.038407674219216759, 2.491644695858772796 ) ) ;
#61825=CARTESIAN_POINT ( 'NONE',  ( 3.842128478764065047, -0.9187925100661897826, 1.618370328034287597 ) ) ;
#61826=CARTESIAN_POINT ( 'NONE',  ( 1.792461972651203439, 1.418048008323580911, -1.288064678409290398 ) ) ;
#61827=CARTESIAN_POINT ( 'NONE',  ( 6.317406038308035043, -0.2352959436980571473, 1.911917130847824886 ) ) ;
#61834=CARTESIAN_POINT ( 'NONE',  ( 6.192246204073627247, 0.9737480728593052026, -1.711826031884769339 ) ) ;
#61837=CARTESIAN_POINT ( 'NONE',  ( -0.01160896700787457207, -0.4585933848370716270, -2.046879979534850236 ) ) ;
#61839=CARTESIAN_POINT ( 'NONE',  ( 5.807627864512785898, -0.4676060548664852101, 1.868651349408587681 ) ) ;
#61841=CARTESIAN_POINT ( 'NONE',  ( 0.7799652524137988818, -1.018268764971082430, 1.515009401286564694 ) ) ;
#61842=CARTESIAN_POINT ( 'NONE',  ( 2.227434312139275896, 0.001603268854937638837, 2.207063162490217056 ) ) ;
#61845=CARTESIAN_POINT ( 'NONE',  ( 0.1055216070770526038, 1.418477292093557329, 1.282857148695019989 ) ) ;
#61846=CARTESIAN_POINT ( 'NONE',  ( 0.4320049508096295288, 1.131045402950446199, 1.612214446364314213 ) ) ;
#61847=CARTESIAN_POINT ( 'NONE',  ( 2.683070245604711523, 1.375115853580029635, 1.371619177916082011 ) ) ;
#61848=CARTESIAN_POINT ( 'NONE',  ( 1.264999722075825561, -2.016288307338756525, -0.002813990012486000669 ) ) ;
#61850=CARTESIAN_POINT ( 'NONE',  ( 5.365987026107917224, -1.852166562183876986, 0.1801111341232768115 ) ) ;
#61856=CARTESIAN_POINT ( 'NONE',  ( 1.224469250947546328, 2.113408192816915943, 0.5798510048089372537 ) ) ;
#61862=CARTESIAN_POINT ( 'NONE',  ( 2.209345402013741300, -0.4006574107652469130, 1.781019818369505847 ) ) ;
#61866=CARTESIAN_POINT ( 'NONE',  ( 6.608999999999983999, 4.692729314731947099, 2.662616042240486536 ) ) ;
#61868=CARTESIAN_POINT ( 'NONE',  ( 0.8207749864527034145, 1.779613767027238502, 0.7382806748287008558 ) ) ;
#61869=CARTESIAN_POINT ( 'NONE',  ( 5.418788444413384475, -1.423528547644649755, 1.350099487149841071 ) ) ;
#61872=CARTESIAN_POINT ( 'NONE',  ( 4.722331747100577459, 2.097238624054961864, 0.6360808509995665716 ) ) ;
#61874=CARTESIAN_POINT ( 'NONE',  ( 4.469627305733424372, -0.3590069766891256231, 2.038746214588673666 ) ) ;
#61878=CARTESIAN_POINT ( 'NONE',  ( 4.448018067569548428, -2.052855444095956550, -1.034378808386252624 ) ) ;
#61883=CARTESIAN_POINT ( 'NONE',  ( 6.620655732516649294, 0.5971256128398574337, 1.879834161342401666 ) ) ;
#61887=CARTESIAN_POINT ( 'NONE',  ( 3.837779778221518168, 1.932683437559437500, 0.1894486881511766863 ) ) ;
#61891=ORIENTED_EDGE ( 'NONE', *, *, #173375, .T. ) ;
#61892=CARTESIAN_POINT ( 'NONE',  ( 5.695548698317931091, 1.764485844685494742, -0.7379451211212140205 ) ) ;
#61894=CARTESIAN_POINT ( 'NONE',  ( 6.370102249521607973, 0.8915232854993185851, 1.476320845237573787 ) ) ;
#61895=CARTESIAN_POINT ( 'NONE',  ( 4.382046175016578005, -2.016188710442788246, -0.04465648322755921829 ) ) ;
#61897=CARTESIAN_POINT ( 'NONE',  ( 1.875870136999336246, 2.111227540014638304, -0.6426800678154330759 ) ) ;
#61900=CARTESIAN_POINT ( 'NONE',  ( 2.044979492446592939, -1.679722130475280961, -1.244493991799436650 ) ) ;
#61901=CARTESIAN_POINT ( 'NONE',  ( 0.5843626980001519478, -0.2102794380555508547, -1.757238120818458649 ) ) ;
#61902=CARTESIAN_POINT ( 'NONE',  ( 6.152970239395502361, 1.038990588714868490, 1.728003889287746286 ) ) ;
#61904=CARTESIAN_POINT ( 'NONE',  ( 2.642860430951101680, -1.905069302404806875, 1.274549645703947132 ) ) ;
#61905=CARTESIAN_POINT ( 'NONE',  ( 1.024908375165583863, -1.101351337790077212, -1.347483777630980040 ) ) ;
#61907=CARTESIAN_POINT ( 'NONE',  ( 1.598581759805017155, 0.8596790983186454183, -1.505624278722474951 ) ) ;
#61910=CARTESIAN_POINT ( 'NONE',  ( 1.399139394074319753, 0.4229888639164773867, 2.129416274499373429 ) ) ;
#61911=CARTESIAN_POINT ( 'NONE',  ( 2.395720570290179374, -1.993893129684479293, 0.3006499569925198956 ) ) ;
#61912=CARTESIAN_POINT ( 'NONE',  ( 3.625000000000002665, -2.052068128417946280, 2.068584262981140017E-13 ) ) ;
#61916=CARTESIAN_POINT ( 'NONE',  ( 6.182248986134903035, -1.028413017182037370, 1.628868941788450764 ) ) ;
#61918=CARTESIAN_POINT ( 'NONE',  ( 2.900855728284880808, -2.189247779298031826, -0.3757519495388698672 ) ) ;
#61924=CARTESIAN_POINT ( 'NONE',  ( 4.968161617874263136, -1.641142972212021656, -0.5799033918824270106 ) ) ;
#61925=CARTESIAN_POINT ( 'NONE',  ( 4.088298575758734898, 1.051444423028622399, -1.656135347060924135 ) ) ;
#61929=CARTESIAN_POINT ( 'NONE',  ( 4.991644252507740021, 1.671830779756987573, 1.524457814443666903 ) ) ;
#61931=CARTESIAN_POINT ( 'NONE',  ( 1.908709741418318062, 0.6448079515158434694, 1.959386160279535494 ) ) ;
#61935=CARTESIAN_POINT ( 'NONE',  ( 3.128041797164154758, 1.042111378005972311, -1.553157497896196393 ) ) ;
#61936=CARTESIAN_POINT ( 'NONE',  ( 2.637049607583162203, 0.5866705090989009497, 1.632017879250416525 ) ) ;
#61937=CARTESIAN_POINT ( 'NONE',  ( 0.06458782335966220534, -1.490751515076127465, 1.741559778653593238 ) ) ;
#61938=CARTESIAN_POINT ( 'NONE',  ( 0.1654306582001447423, -1.972458130798220077, -0.9897840116655574061 ) ) ;
#61939=CARTESIAN_POINT ( 'NONE',  ( 3.467792127863758456, 2.109446376165153847, -0.4717452660116944196 ) ) ;
#61940=CARTESIAN_POINT ( 'NONE',  ( 4.681548850490841573, -0.9142078566968904196, 1.713296222823880166 ) ) ;
#61942=CARTESIAN_POINT ( 'NONE',  ( 6.731728662460410462, -1.222180481402233898, -1.416172877279207931 ) ) ;
#61945=CARTESIAN_POINT ( 'NONE',  ( 0.03560581989598374242, -0.09759080014098624190, 2.118463022953632091 ) ) ;
#61947=CARTESIAN_POINT ( 'NONE',  ( 5.449842333688053486, -1.824117940560719298, -0.8596331684956670660 ) ) ;
#61951=CARTESIAN_POINT ( 'NONE',  ( 3.017977635683791071, -0.9002817137206723386, -1.588204215665294461 ) ) ;
#61952=CARTESIAN_POINT ( 'NONE',  ( 2.520803682403276902, 1.441976459853638204, -1.670562425240495363 ) ) ;
#61958=CARTESIAN_POINT ( 'NONE',  ( 0.5100284451979911760, -0.7230318888242005526, 1.886137889315203875 ) ) ;
#61959=CARTESIAN_POINT ( 'NONE',  ( 0.7332529803791461021, 1.960763319057107879, 0.8078710241638600298 ) ) ;
#61962=CARTESIAN_POINT ( 'NONE',  ( 1.516205985490867381, 0.7479433349990645130, 1.704208623783896259 ) ) ;
#61965=CARTESIAN_POINT ( 'NONE',  ( 5.946181061342999286, 2.058424064105804696, 0.1035008386942332104 ) ) ;
#61966=CARTESIAN_POINT ( 'NONE',  ( 6.258435431136967431, 1.928752767684217106, -0.5880170417187426946 ) ) ;
#61971=CARTESIAN_POINT ( 'NONE',  ( 3.457459740917231628, 0.4424662778084071935, -1.771134634090239190 ) ) ;
#61976=CARTESIAN_POINT ( 'NONE',  ( 5.940779784064256219, 1.198679029392090589, 1.620932600025201786 ) ) ;
#61977=CARTESIAN_POINT ( 'NONE',  ( 5.683513393433289096, -0.8240744568873883402, 1.646495476055845231 ) ) ;
#61978=CARTESIAN_POINT ( 'NONE',  ( 0.07680821025391608436, 0.2560392329899116026, -1.846278364303982178 ) ) ;
#61979=CARTESIAN_POINT ( 'NONE',  ( 4.073124928733475869, -2.152535440544633971, -0.8323431910086924734 ) ) ;
#61981=CARTESIAN_POINT ( 'NONE',  ( 6.362596528949501895, -1.533591692085239266, 1.523617273982772247 ) ) ;
#61983=CARTESIAN_POINT ( 'NONE',  ( 1.505311199525250831, -1.927169978453403321, 0.2396651170105366657 ) ) ;
#61986=CARTESIAN_POINT ( 'NONE',  ( 5.079617024973425821, 1.589842341716392493, -1.660015637060639371 ) ) ;
#61989=CARTESIAN_POINT ( 'NONE',  ( 4.451927283622527654, 1.870250842541102410, -0.04591718433973044494 ) ) ;
#61991=CARTESIAN_POINT ( 'NONE',  ( 2.935702856749936362, -1.841876368404654629, 0.5141854427313449216 ) ) ;
#61994=CARTESIAN_POINT ( 'NONE',  ( 3.563272299071856164, -1.946135509614330239, -1.040604674307284316 ) ) ;
#61995=CARTESIAN_POINT ( 'NONE',  ( 6.883263157960393563, 1.268976584491373183, 2.060807272249213451 ) ) ;
#62000=CARTESIAN_POINT ( 'NONE',  ( 1.686731049638652502, -0.2853660037422758866, -1.950466449893713428 ) ) ;
#62001=CARTESIAN_POINT ( 'NONE',  ( 1.483892314354786857, 2.131289638308156320, -0.8850757863276045301 ) ) ;
#62002=CARTESIAN_POINT ( 'NONE',  ( 2.383191274269541360, -0.003000794896521400724, 1.962046632024143866 ) ) ;
#62004=CARTESIAN_POINT ( 'NONE',  ( 4.821169966264648998, -1.840000718094082943, -0.9321929973984711681 ) ) ;
#62011=CARTESIAN_POINT ( 'NONE',  ( 0.8312205373445592516, -2.043673001365586384, -0.7330250775806450569 ) ) ;
#62015=CARTESIAN_POINT ( 'NONE',  ( 2.600682448077856090, 1.504852936121018558, -1.110837741034584436 ) ) ;
#62017=CARTESIAN_POINT ( 'NONE',  ( 6.731704548537910782, -1.406307105171537009, -1.641701734229366716 ) ) ;
#62019=CARTESIAN_POINT ( 'NONE',  ( 0.07755575628181145265, 0.2276780653837663093, -2.222404768597834757 ) ) ;
#62020=SURFACE_SIDE_STYLE ('',( #194136 ) ) ;
#62022=CARTESIAN_POINT ( 'NONE',  ( 2.051281676579026492, -1.707476168062868060, 0.8611843332394365502 ) ) ;
#62023=CARTESIAN_POINT ( 'NONE',  ( 4.311239457809501907, -0.3017279273445966914, 1.743759454612598070 ) ) ;
#62024=CARTESIAN_POINT ( 'NONE',  ( 2.297387027313551044, 1.747684631587187454, -0.7765785915121098393 ) ) ;
#62027=CARTESIAN_POINT ( 'NONE',  ( 6.046487378053778450, -1.350936885689631772, 1.358403761460762471 ) ) ;
#62028=AXIS2_PLACEMENT_3D ( 'NONE', #84477, #53038, #151630 ) ;
#62030=CARTESIAN_POINT ( 'NONE',  ( 6.584429662329396749, 1.135205087083859476, -1.609268749140836618 ) ) ;
#62034=CARTESIAN_POINT ( 'NONE',  ( 5.313307075269409374, -0.2735208697075517947, 1.850433306854900817 ) ) ;
#62035=CARTESIAN_POINT ( 'NONE',  ( 2.086296903703276140, -1.790263230197926436, -0.3570169370194844483 ) ) ;
#62037=CARTESIAN_POINT ( 'NONE',  ( 4.987059637548557411, -0.2676712469649074055, -2.190530366034774801 ) ) ;
#62041=CARTESIAN_POINT ( 'NONE',  ( 2.805193546069509214, -1.716336894061726737, 1.143758443631032407 ) ) ;
#62048=CARTESIAN_POINT ( 'NONE',  ( 5.564915762860970894, 1.570151797963925455, -1.349580972669261580 ) ) ;
#62050=CARTESIAN_POINT ( 'NONE',  ( 3.181113218772323226, -0.1555236193923059951, -2.156033859764289407 ) ) ;
#62052=CARTESIAN_POINT ( 'NONE',  ( 3.158857784513937617, 0.4929582698031101939, 1.958447305144744410 ) ) ;
#62053=CARTESIAN_POINT ( 'NONE',  ( 6.620655732516652847, 0.5779860733656561056, 2.127054332187257923 ) ) ;
#62059=CARTESIAN_POINT ( 'NONE',  ( 1.516814941429758701, 0.2024661778830244008, 2.006371303556075958 ) ) ;
#62060=CARTESIAN_POINT ( 'NONE',  ( 6.532779862045914321, -1.958661757936002612, 0.9833580883553474372 ) ) ;
#62062=CARTESIAN_POINT ( 'NONE',  ( 5.168181644781757456, 1.909928461159452251, -0.09994665148223277895 ) ) ;
#62066=CARTESIAN_POINT ( 'NONE',  ( 2.847279977023515318, 0.2930488483154705670, -1.994874153863256172 ) ) ;
#62069=CARTESIAN_POINT ( 'NONE',  ( 5.614166379062860202, -0.7790257685919326214, -1.538869111107727505 ) ) ;
#62073=CARTESIAN_POINT ( 'NONE',  ( 1.006788857090525013, 0.5974033793386055446, 1.982218910981221827 ) ) ;
#62076=CARTESIAN_POINT ( 'NONE',  ( 5.162699569786796339, 0.5314807639728249544, 1.731738579618222973 ) ) ;
#62079=CARTESIAN_POINT ( 'NONE',  ( 6.006502151196043471, -1.803439199047681907, -0.1703578026433834602 ) ) ;
#62081=CARTESIAN_POINT ( 'NONE',  ( 3.556733441538503016, -1.932615445784117369, -1.033156731641969195 ) ) ;
#62083=CARTESIAN_POINT ( 'NONE',  ( 0.2737812321212430566, -1.924752420120953822, 0.3788971555385572954 ) ) ;
#62085=CARTESIAN_POINT ( 'NONE',  ( 4.921452907191903314, -1.357786409588169096, -1.351554235494869749 ) ) ;
#62093=CARTESIAN_POINT ( 'NONE',  ( 1.639762333045853726, -1.565812861550972324, -1.490595759849027813 ) ) ;
#62096=CARTESIAN_POINT ( 'NONE',  ( 1.535882326342351334, 0.9031702520058831896, -1.586444745400449108 ) ) ;
#62098=CARTESIAN_POINT ( 'NONE',  ( 4.963791182761823961, 1.805510465697376610, -0.2690417022049585438 ) ) ;
#62101=CARTESIAN_POINT ( 'NONE',  ( 2.847809051801777791, -1.287500320553297994, -1.414207669007704116 ) ) ;
#62103=CARTESIAN_POINT ( 'NONE',  ( 3.508217419976053630, 1.969739563948954331, 0.002549893942540777322 ) ) ;
#62105=CARTESIAN_POINT ( 'NONE',  ( 6.146037779257278011, 0.6132840560482490933, 1.842739892034722882 ) ) ;
#62109=CARTESIAN_POINT ( 'NONE',  ( 5.625269520628737752, 1.871107552910089122, 0.9978724776121964402 ) ) ;
#62111=CARTESIAN_POINT ( 'NONE',  ( 4.195896582043898704, 1.251535281948525036, 1.445917311372606262 ) ) ;
#62115=CARTESIAN_POINT ( 'NONE',  ( 0.2357703454196959370, -2.016519153289020760, 0.8967723332334791575 ) ) ;
#62116=CARTESIAN_POINT ( 'NONE',  ( 4.916656812733911863, -0.6802563888389367985, -1.894789199515679146 ) ) ;
#62118=CARTESIAN_POINT ( 'NONE',  ( 6.041596546049881944, -1.325759876995153075, -1.255439798616593716 ) ) ;
#62119=CARTESIAN_POINT ( 'NONE',  ( 0.3267351109269464593, -1.353470794461093751, 1.566751113397255590 ) ) ;
#62123=CARTESIAN_POINT ( 'NONE',  ( 6.561405567229332547, 0.3174558530528898692, -1.843364171016811603 ) ) ;
#62131=CARTESIAN_POINT ( 'NONE',  ( 4.183993884235046146, 1.395953275470160682, 1.028640563475995640 ) ) ;
#62133=CARTESIAN_POINT ( 'NONE',  ( 1.868117093089691760, -2.055091939184821026, 0.2493290443424806546 ) ) ;
#62134=CARTESIAN_POINT ( 'NONE',  ( 2.038805038046047624, -1.634495437704911458, 1.345740563223641217 ) ) ;
#62138=CARTESIAN_POINT ( 'NONE',  ( 0.6374758831957715310, 1.839649526063956042, -0.7036667969960698210 ) ) ;
#62143=CARTESIAN_POINT ( 'NONE',  ( 2.045279198001882737, -1.842668879747776156, -1.363283251902024817 ) ) ;
#62144=CARTESIAN_POINT ( 'NONE',  ( 1.154616158753757338, -1.440623569337009968, 1.121372061650728558 ) ) ;
#62146=CARTESIAN_POINT ( 'NONE',  ( 3.304848191199673213, -0.3775801424153284458, -1.874573493127674961 ) ) ;
#62150=CARTESIAN_POINT ( 'NONE',  ( 1.547136693356679249, 0.2016598947911317496, 2.003107868921078616 ) ) ;
#62151=CARTESIAN_POINT ( 'NONE',  ( 2.430452978529148655, -1.210835280720125917, 1.543375930141199115 ) ) ;
#62156=CARTESIAN_POINT ( 'NONE',  ( 5.367163668781920194, 2.014996964747676422, -0.5569773519958736152 ) ) ;
#62157=CARTESIAN_POINT ( 'NONE',  ( 3.748697311245871688, -1.446992627045262214, 1.018796548582428185 ) ) ;
#62160=CARTESIAN_POINT ( 'NONE',  ( 6.720655732516684466, -0.007268404184076341853, 2.273772995263834140 ) ) ;
#62161=CARTESIAN_POINT ( 'NONE',  ( 4.593551391122507432, -1.740074876368927104, -0.03866795590094784102 ) ) ;
#62164=CARTESIAN_POINT ( 'NONE',  ( 4.077271355118361029, 1.226738060269889408, -1.225556752838660168 ) ) ;
#62165=CARTESIAN_POINT ( 'NONE',  ( 5.072805357664615045, 1.500764584350265718, -1.569201701505947844 ) ) ;
#62167=CARTESIAN_POINT ( 'NONE',  ( -0.1529269513586241080, -1.894431756695889923, -0.9458152384202949126 ) ) ;
#62168=CARTESIAN_POINT ( 'NONE',  ( 5.250000000000002665, 2.988487650205320908E-13, 2.052068128417942283 ) ) ;
#62170=CARTESIAN_POINT ( 'NONE',  ( 3.504829168241951898, 1.519505285488613744, -1.184012928881588822 ) ) ;
#62172=CARTESIAN_POINT ( 'NONE',  ( 6.398696371038459674, -2.178289998122169280, -0.4347530419120289036 ) ) ;
#62174=CARTESIAN_POINT ( 'NONE',  ( 6.983263157960371004, 2.969675876345272858, 2.399270433241917466 ) ) ;
#62177=CARTESIAN_POINT ( 'NONE',  ( 2.174768466102798836, 0.9529365794415098900, 2.006655600372597714 ) ) ;
#62184=CARTESIAN_POINT ( 'NONE',  ( 0.3521856818783953846, 0.1948384997633167970, -2.006960225185448810 ) ) ;
#62186=CARTESIAN_POINT ( 'NONE',  ( 5.740703853076708718, -2.011634581743710903, -0.4553567745326501104 ) ) ;
#62191=CARTESIAN_POINT ( 'NONE',  ( 6.802024559211160337, -1.870114703409443857, 0.04643648283486622591 ) ) ;
#62192=CARTESIAN_POINT ( 'NONE',  ( 6.293613488329289574, 1.277945636399902440, -1.172455961997687535 ) ) ;
#62193=CARTESIAN_POINT ( 'NONE',  ( 5.144012499716256848, 0.5123920008897012712, 1.663301317158589754 ) ) ;
#62194=CARTESIAN_POINT ( 'NONE',  ( 2.876852093609012950, -0.1713799144957695864, -2.286037302510893099 ) ) ;
#62196=CARTESIAN_POINT ( 'NONE',  ( 1.499689682683522207, -0.6613356838569836027, -1.718437284301529422 ) ) ;
#62198=CARTESIAN_POINT ( 'NONE',  ( 1.922601709848625440, 1.702220721529534853, 0.6601445126475160574 ) ) ;
#62199=CARTESIAN_POINT ( 'NONE',  ( 2.848279904836711118, 0.2930702634792031747, -1.994869876753922799 ) ) ;
#62200=CARTESIAN_POINT ( 'NONE',  ( 1.218978173989828884, -0.05078841826402365894, 2.191026318449231791 ) ) ;
#62202=CARTESIAN_POINT ( 'NONE',  ( 4.436618261691759102, 2.064837277596673903, 0.4132364508900014943 ) ) ;
#62205=CARTESIAN_POINT ( 'NONE',  ( 1.680221237283368696, -1.148429780529091948, -1.722445320287042447 ) ) ;
#62208=CARTESIAN_POINT ( 'NONE',  ( 4.248766647586673884, 2.079802475202694900, 0.4125236972643344102 ) ) ;
#62209=CARTESIAN_POINT ( 'NONE',  ( 6.217409598193539999, -0.2183660865492654257, 1.812524795094340835 ) ) ;
#62216=CARTESIAN_POINT ( 'NONE',  ( -0.1927127643980519056, -0.4999767001874329542, -2.172835435166208473 ) ) ;
#62217=CARTESIAN_POINT ( 'NONE',  ( 0.7628874492277806230, -1.525271245827728661, 1.452362197770618923 ) ) ;
#62220=CARTESIAN_POINT ( 'NONE',  ( 5.084723738625635647, 1.780007044882421008, 0.5427147737909858716 ) ) ;
#62227=CARTESIAN_POINT ( 'NONE',  ( 2.137090596337941406, -0.09316805448006218460, -1.959763546484971197 ) ) ;
#62228=CARTESIAN_POINT ( 'NONE',  ( 0.7081719773709761467, -2.151164098719647200, 0.2130325561137471624 ) ) ;
#62232=CARTESIAN_POINT ( 'NONE',  ( 2.917049273830461864, 0.5812832248327322038, 1.633648419047509792 ) ) ;
#62233=CARTESIAN_POINT ( 'NONE',  ( 1.851089384485626210, 1.735827849189163663, -0.1260499613615853887 ) ) ;
#62236=CARTESIAN_POINT ( 'NONE',  ( 1.458361007166041334, 1.524808354686446821, 1.319028796778199730 ) ) ;
#62237=CARTESIAN_POINT ( 'NONE',  ( 6.925078400183582339, 6.034855204486058611, 2.639235227498262670 ) ) ;
#62239=CARTESIAN_POINT ( 'NONE',  ( 1.164844247922683707, -1.781316891034259164, -0.8450378345598685836 ) ) ;
#62240=CARTESIAN_POINT ( 'NONE',  ( 5.607647405131535479, 1.452367144367059826, 1.244281684088064166 ) ) ;
#62245=CARTESIAN_POINT ( 'NONE',  ( 1.594405160661801490, -1.078473704070359140, 1.707419690039575499 ) ) ;
#62246=CARTESIAN_POINT ( 'NONE',  ( 4.594930786881223916, -0.5007672277346334466, -2.252456893713528530 ) ) ;
#62247=CARTESIAN_POINT ( 'NONE',  ( 5.969191311310417802, 1.729517061547349632, 0.9261464158661563140 ) ) ;
#62248=CARTESIAN_POINT ( 'NONE',  ( 2.131626046773547500, 1.878804184644796926, -0.5645400877590660560 ) ) ;
#62252=CARTESIAN_POINT ( 'NONE',  ( 1.604857428818485587, 1.977717902320776266, 0.7566523057890365278 ) ) ;
#62255=CARTESIAN_POINT ( 'NONE',  ( 0.9723034553027897209, -0.04304006056080752346, -1.840805954149108636 ) ) ;
#62258=CARTESIAN_POINT ( 'NONE',  ( 2.391022662813433453, -2.030629854096975606, -0.6112283555373964061 ) ) ;
#62262=CARTESIAN_POINT ( 'NONE',  ( 3.550122082181893290, 2.060967561582152108, 0.003633429623469893420 ) ) ;
#62265=CARTESIAN_POINT ( 'NONE',  ( -0.02423404108400224743, -1.785672699080865788, -0.4486397487279417118 ) ) ;
#62267=CARTESIAN_POINT ( 'NONE',  ( -0.02244404828160087226, 4.081832076214893412, -2.743766916979750281 ) ) ;
#62270=CARTESIAN_POINT ( 'NONE',  ( 2.724197551734920175, -1.300482880258296836, -1.851114353284079472 ) ) ;
#62272=CARTESIAN_POINT ( 'NONE',  ( 2.109342631017618874, 1.402271653390272377, 1.146968571259598058 ) ) ;
#62273=CARTESIAN_POINT ( 'NONE',  ( 3.151485257178482158, 1.867856130240726387, -0.4247363484005464151 ) ) ;
#62274=CARTESIAN_POINT ( 'NONE',  ( 4.439934286204096914, 1.349936692791346093, 1.569845735447549906 ) ) ;
#62277=CARTESIAN_POINT ( 'NONE',  ( 1.604304721248978494, -0.7076282383621353977, -1.840268529672415498 ) ) ;
#62278=CARTESIAN_POINT ( 'NONE',  ( 6.217406027492617504, -0.2333201818524588411, 1.912260165615098595 ) ) ;
#62279=CARTESIAN_POINT ( 'NONE',  ( 2.606148294764852213, -0.7140300644919925777, -1.729217693616967644 ) ) ;
#62281=CARTESIAN_POINT ( 'NONE',  ( 1.067484182866541564, -2.088262569869667740, -0.9824423588734966239 ) ) ;
#62283=CARTESIAN_POINT ( 'NONE',  ( 2.523689441098162511, 1.825779920793478839, -0.3596660026494375995 ) ) ;
#62285=CARTESIAN_POINT ( 'NONE',  ( 6.162562474744170515, -0.7388518307863629619, -1.925989236560563977 ) ) ;
#62288=CARTESIAN_POINT ( 'NONE',  ( 5.983450976520548359, 1.947180606154915727, -0.8027177699698545554 ) ) ;
#62290=CARTESIAN_POINT ( 'NONE',  ( 6.239563118392394969, -1.560868990211834895, -1.495623836407403484 ) ) ;
#62291=CARTESIAN_POINT ( 'NONE',  ( 6.006511931541290927, -2.010153113457528118, -0.1956843118748711474 ) ) ;
#62297=CARTESIAN_POINT ( 'NONE',  ( 6.825078400183556049, 7.053092130845653784, 2.453807127456457238 ) ) ;
#62300=CARTESIAN_POINT ( 'NONE',  ( 4.680875185974167074, 1.673856063443099895, -1.124242729735332347 ) ) ;
#62305=CARTESIAN_POINT ( 'NONE',  ( 5.893488898593548520, 1.633865717575968324, 1.415524914074948404 ) ) ;
#62310=CARTESIAN_POINT ( 'NONE',  ( 6.362907676916636390, -0.1017654035869921675, -2.013986322929907757 ) ) ;
#62312=CARTESIAN_POINT ( 'NONE',  ( 6.639320575229232801, 7.629137130509035636, 2.803262396134009737 ) ) ;
#62313=CARTESIAN_POINT ( 'NONE',  ( 2.244387868473923575, 0.3767020243423558901, 1.683057829810198136 ) ) ;
#62317=CARTESIAN_POINT ( 'NONE',  ( 6.116445839754358182, 1.256427234498383561, -1.385894902050835542 ) ) ;
#62318=CARTESIAN_POINT ( 'NONE',  ( 1.260403266252381416, 2.010875322206317151, 0.09671919503399273310 ) ) ;
#62320=CARTESIAN_POINT ( 'NONE',  ( 2.960231987352707428, 2.196266598062237563, -0.2149427413448631863 ) ) ;
#62321=CARTESIAN_POINT ( 'NONE',  ( 5.049771808528761952, 1.604214368398539925, 1.463040072455735974 ) ) ;
#62326=CARTESIAN_POINT ( 'NONE',  ( 3.405043383231837417, -0.4154483767263848493, -2.079220720149973278 ) ) ;
#62327=CARTESIAN_POINT ( 'NONE',  ( 2.952750085323506468, -1.864176452196796507, -0.7691048347045483791 ) ) ;
#62328=CARTESIAN_POINT ( 'NONE',  ( 3.603588835282888869, 1.315886683649561295, 1.245372468285299128 ) ) ;
#62332=CARTESIAN_POINT ( 'NONE',  ( 0.8131078318618142342, -0.2785150557334699073, 1.849687307983488571 ) ) ;
#62335=CARTESIAN_POINT ( 'NONE',  ( 1.288148359701014600, -0.6930021182445024186, -1.786147582385696486 ) ) ;
#62341=CARTESIAN_POINT ( 'NONE',  ( 5.471600609837615536, 2.084441204114939161, -0.5725544205837928002 ) ) ;
#62344=CARTESIAN_POINT ( 'NONE',  ( 3.199588043238619672, 1.915454767000431602, -0.9102714984489733707 ) ) ;
#62345=DIRECTION ( 'NONE',  ( -3.451266460341926649E-31, -5.200010849845536803E-32, 1.000000000000000000 ) ) ;
#62347=CARTESIAN_POINT ( 'NONE',  ( 4.358636338273668365, -1.462950666040288006, 1.321578431016472654 ) ) ;
#62348=CARTESIAN_POINT ( 'NONE',  ( 6.135011676971934058, 1.786887936952135991, 0.6819008164158719687 ) ) ;
#62350=CARTESIAN_POINT ( 'NONE',  ( 0.3267351109269465148, -1.353470794461093973, 1.566751113397255812 ) ) ;
#62351=CARTESIAN_POINT ( 'NONE',  ( 2.923698373526161465, 1.078347508963822587, -1.614843327186490374 ) ) ;
#62355=CARTESIAN_POINT ( 'NONE',  ( 2.730511870197129820, 0.2565026084431647480, 2.074771742164283950 ) ) ;
#62358=CARTESIAN_POINT ( 'NONE',  ( 0.5920784091685951100, -1.007499442088593211, 1.505216462368397234 ) ) ;
#62360=CARTESIAN_POINT ( 'NONE',  ( 4.406973378220558679, 1.706932345810768359, -1.398813476408675260 ) ) ;
#62361=CARTESIAN_POINT ( 'NONE',  ( 2.977765718515756888, 2.095881712254169305, -0.6909776239150815513 ) ) ;
#62362=CARTESIAN_POINT ( 'NONE',  ( 1.189939518123926510, 1.139724415472416652, 1.535358521287055300 ) ) ;
#62365=CARTESIAN_POINT ( 'NONE',  ( 4.510256325466165173, 2.069976601481211542, -0.04757507122059301263 ) ) ;
#62367=CARTESIAN_POINT ( 'NONE',  ( 3.151412294154242844, -1.766339975446712174, -1.245920677233211871 ) ) ;
#62368=CARTESIAN_POINT ( 'NONE',  ( 4.810206850810132551, 1.511280187219691928, -1.587364365194674498 ) ) ;
#62375=CARTESIAN_POINT ( 'NONE',  ( 0.4049229342097167006, -1.081068455937021611, -1.701946057285643743 ) ) ;
#62377=CARTESIAN_POINT ( 'NONE',  ( 4.188381925097388603, 1.111774711627441681, -1.746232563387891679 ) ) ;
#62378=CARTESIAN_POINT ( 'NONE',  ( 3.791558849520747287, 1.396117892292214613, 1.327735796816224223 ) ) ;
#62379=CARTESIAN_POINT ( 'NONE',  ( -0.03552856956758054796, -1.956598898622825766, -0.4871759670460884539 ) ) ;
#62382=CARTESIAN_POINT ( 'NONE',  ( 3.502752968683011225, 0.4741538486671539876, 1.911403532405174133 ) ) ;
#62383=CARTESIAN_POINT ( 'NONE',  ( 0.8147124124333324779, 2.026155960571228043, 0.8354305900151803854 ) ) ;
#62384=CARTESIAN_POINT ( 'NONE',  ( 4.266095019097836172, 0.8626762044917112293, 1.609013669381313294 ) ) ;
#62390=CARTESIAN_POINT ( 'NONE',  ( 1.628196140939692338, 0.1813696128579282696, 1.832309401408799276 ) ) ;
#62391=CARTESIAN_POINT ( 'NONE',  ( 5.273694575261410833, 0.3885250917745143862, -1.975199337908732256 ) ) ;
#62392=CARTESIAN_POINT ( 'NONE',  ( 0.3691051123158794467, -0.6094954538576388137, 2.216020297015007134 ) ) ;
#62393=CARTESIAN_POINT ( 'NONE',  ( 5.225427317040848507, 0.1961275920050585819, -1.951957996302315257 ) ) ;
#62401=CARTESIAN_POINT ( 'NONE',  ( 1.734041596967655252, 2.068474147835582144, 0.3034153833333247396 ) ) ;
#62402=CARTESIAN_POINT ( 'NONE',  ( 0.4263524580605422276, 1.788790299270696993, 0.5473224044415525569 ) ) ;
#62404=CARTESIAN_POINT ( 'NONE',  ( -0.1106727585415836906, 0.7252806920327293794, -2.087287528096515299 ) ) ;
#62405=CARTESIAN_POINT ( 'NONE',  ( 0.3975144409600079309, -0.5839149016878465437, -1.639678601710597983 ) ) ;
#62409=CARTESIAN_POINT ( 'NONE',  ( 1.980655567072008072, -0.08268669962357808045, -1.723028944404185303 ) ) ;
#62410=CARTESIAN_POINT ( 'NONE',  ( 1.294752383181968503, 1.788903229852260246, -1.265732775075766092 ) ) ;
#62411=CARTESIAN_POINT ( 'NONE',  ( 4.635508124736155366, -2.018492079602551392, 0.8926152185086615454 ) ) ;
#62413=CARTESIAN_POINT ( 'NONE',  ( 0.8839112305873472186, -2.062193702853211352, 0.6791930824729536242 ) ) ;
#62414=CARTESIAN_POINT ( 'NONE',  ( 0.1701549220758866166, -1.195335944658926230, 1.380069390326914336 ) ) ;
#62415=CARTESIAN_POINT ( 'NONE',  ( 2.852857698155007782, -1.958159313504294730, -0.8059144277542380497 ) ) ;
#62416=CARTESIAN_POINT ( 'NONE',  ( 6.539320575229268684, 7.629137130509104026, 2.396737603865983779 ) ) ;
#62418=CARTESIAN_POINT ( 'NONE',  ( 3.386539700769741312, -0.4487184517108309123, -2.247870937536749381 ) ) ;
#62420=CARTESIAN_POINT ( 'NONE',  ( 0.07755575628183573877, 1.996246338214379801, -2.602582295553407032 ) ) ;
#62422=CARTESIAN_POINT ( 'NONE',  ( 5.813180279319686505, 1.817354232980341378, -1.277000798603223464 ) ) ;
#62430=CARTESIAN_POINT ( 'NONE',  ( 3.656875104409584853, 1.122498086849915921, 1.674887873639265390 ) ) ;
#62432=CARTESIAN_POINT ( 'NONE',  ( 2.254800304804779110, -0.5458148477457210879, -1.989007103235032048 ) ) ;
#62437=CARTESIAN_POINT ( 'NONE',  ( 5.314472526525434226, 2.023830839259177949, 0.8410439265160507549 ) ) ;
#62438=CARTESIAN_POINT ( 'NONE',  ( 2.268204128460939550, 1.842446992372799963, -0.8197738674571022344 ) ) ;
#62439=CARTESIAN_POINT ( 'NONE',  ( 1.891909123491273492, -0.4922293657834125313, -1.774144672653771293 ) ) ;
#62442=CARTESIAN_POINT ( 'NONE',  ( 5.209893869493905427, -1.816617279468687229, 0.1804919988709560719 ) ) ;
#62443=CARTESIAN_POINT ( 'NONE',  ( 6.557263107265463020, -1.238491779027944162, 1.591905563659588907 ) ) ;
#62445=CARTESIAN_POINT ( 'NONE',  ( 5.418922386936855240, 2.088194672119690676, 0.8713435986696310698 ) ) ;
#62447=CARTESIAN_POINT ( 'NONE',  ( 1.225372267635124635, -0.04993704651819717150, 2.105648344105083947 ) ) ;
#62458=CARTESIAN_POINT ( 'NONE',  ( 1.986737319265439394, -1.300789755646198476, 1.674730562594067829 ) ) ;
#62459=CARTESIAN_POINT ( 'NONE',  ( 2.830584216690882116, -1.098655552678593716, -1.930667878645520474 ) ) ;
#62464=CARTESIAN_POINT ( 'NONE',  ( 2.980854556682940526, 1.846358069237159949, 0.6635599008937702603 ) ) ;
#62471=CARTESIAN_POINT ( 'NONE',  ( 2.900754761704402274, -2.089926006748676457, -0.3584049868644647585 ) ) ;
#62473=CARTESIAN_POINT ( 'NONE',  ( 4.416967121957662279, 1.975198431823081302, 0.8787980929093119897 ) ) ;
#62474=CARTESIAN_POINT ( 'NONE',  ( 3.210337823311388394, 1.665856106666419034, 0.7845605768846477535 ) ) ;
#62477=CARTESIAN_POINT ( 'NONE',  ( 5.630708778567339756, -1.570753007681056079, 0.7496256940079452091 ) ) ;
#62481=CARTESIAN_POINT ( 'NONE',  ( 3.028364643526501698, 1.202066397148596977, -1.796461956351296019 ) ) ;
#62482=CARTESIAN_POINT ( 'NONE',  ( 4.481795959180916888, 1.842165523724150544, 0.8196470798618460396 ) ) ;
#62484=CARTESIAN_POINT ( 'NONE',  ( 2.905317003618158367, 1.825515667692039878, 1.157497049167732550 ) ) ;
#62485=CARTESIAN_POINT ( 'NONE',  ( 2.899638734157696796, -0.6216841358992927224, 1.870808799549168233 ) ) ;
#62487=CARTESIAN_POINT ( 'NONE',  ( 4.563973399113295137, -1.265747467430546225, 1.473022616845516053 ) ) ;
#62495=CARTESIAN_POINT ( 'NONE',  ( 0.6048602812970468312, -0.7454967350204610987, -2.077179305122120123 ) ) ;
#62497=CARTESIAN_POINT ( 'NONE',  ( 5.910985094894211755, -1.548708053515185812, 1.204094020389692155 ) ) ;
#62501=CARTESIAN_POINT ( 'NONE',  ( 0.07499057489264347731, 2.883324855518037300, -2.444194386608829372 ) ) ;
#62502=CARTESIAN_POINT ( 'NONE',  ( 4.927609005033061429, 0.9437523325564222132, -1.580719041474540010 ) ) ;
#62510=CARTESIAN_POINT ( 'NONE',  ( 6.696563014664697278, -0.5452183415704283664, -1.987298092995327226 ) ) ;
#62512=CARTESIAN_POINT ( 'NONE',  ( 1.715070751487054013, -1.593955780799067412, -0.9604075334226671590 ) ) ;
#62513=CARTESIAN_POINT ( 'NONE',  ( 3.720104550828434942, 1.749555917645674530, 0.5740644926693627692 ) ) ;
#62516=( BOUNDED_SURFACE ( )  B_SPLINE_SURFACE ( 3, 3, ( 
 ( #78065, #58619, #61822, #195019, #76990, #145245, #43460, #210182, #161470, #192867, #46651 ),
 ( #109581, #91143, #157199, #27175, #8796, #74875, #190734, #42397, #108507, #60746, #126908 ),
 ( #176642, #11989, #45590, #175585, #193943, #95418, #93279, #159317, #111706, #44523, #28254 ),
 ( #144190, #177715, #29324, #47727, #67107, #214408, #64993, #183017, #97537, #196094, #179839 ),
 ( #31460, #30399, #15177, #146298, #181942, #96485, #66039, #32511, #163594, #130100, #162532 ),
 ( #180889, #81264, #132186, #113843, #147343, #213371, #212310, #112774, #50895, #117021, #99644 ),
 ( #198192, #33572, #178785, #131147, #197136, #14104, #148409, #165711, #17300, #48775, #80194 ) ),
 .UNSPECIFIED., .T., .F., .T. ) 
 B_SPLINE_SURFACE_WITH_KNOTS ( ( 4, 3, 4 ),
 ( 4, 1, 1, 1, 1, 1, 1, 1, 4 ),
 ( 0.000000000000000000, 0.5000000000000000000, 1.000000000000000000 ),
 ( 0.000000000000000000, 0.2255234228546724728, 0.3973271701647976828, 0.5245128843546777997, 0.6161923999872991331, 0.6815320185768301009, 0.7298552812456317040, 0.7704940248801678271, 1.000000000000000000 ),
 .UNSPECIFIED. ) 
 GEOMETRIC_REPRESENTATION_ITEM ( )  RATIONAL_B_SPLINE_SURFACE ( (
 ( 1.000000000000000222, 1.000000000000000222, 1.000000000000000666, 0.9999999999999996669, 1.000000000000000222, 0.9999999999999997780, 1.000000000000000000, 1.000000000000000222, 1.000000000000000000, 1.000000000000000000, 1.000000000000000000),
 ( 0.3333333333333334259, 0.3333333333333334259, 0.3333333333333335369, 0.3333333333333333148, 0.3333333333333333148, 0.3333333333333333703, 0.3333333333333333703, 0.3333333333333334814, 0.3333333333333333148, 0.3333333333333334259, 0.3333333333333333703),
 ( 0.3333333333333334259, 0.3333333333333334259, 0.3333333333333335369, 0.3333333333333333148, 0.3333333333333333148, 0.3333333333333333703, 0.3333333333333333703, 0.3333333333333334814, 0.3333333333333333148, 0.3333333333333334259, 0.3333333333333333703),
 ( 1.000000000000000222, 1.000000000000000222, 1.000000000000000666, 0.9999999999999996669, 1.000000000000000222, 0.9999999999999997780, 1.000000000000000000, 1.000000000000000222, 1.000000000000000000, 1.000000000000000000, 1.000000000000000000),
 ( 0.3333333333333334259, 0.3333333333333334259, 0.3333333333333335369, 0.3333333333333333148, 0.3333333333333333148, 0.3333333333333333703, 0.3333333333333333703, 0.3333333333333334814, 0.3333333333333333148, 0.3333333333333334259, 0.3333333333333333703),
 ( 0.3333333333333334259, 0.3333333333333334259, 0.3333333333333335369, 0.3333333333333333148, 0.3333333333333333148, 0.3333333333333333703, 0.3333333333333333703, 0.3333333333333334814, 0.3333333333333333148, 0.3333333333333334259, 0.3333333333333333703),
 ( 1.000000000000000222, 1.000000000000000222, 1.000000000000000666, 0.9999999999999996669, 1.000000000000000222, 0.9999999999999997780, 1.000000000000000000, 1.000000000000000222, 1.000000000000000000, 1.000000000000000000, 1.000000000000000000) ) ) 
 REPRESENTATION_ITEM ( '' )  SURFACE ( )  );
#62520=ORIENTED_EDGE ( 'NONE', *, *, #132876, .F. ) ;
#62521=CARTESIAN_POINT ( 'NONE',  ( 3.369938178094655346, 2.153121441420174698, -0.4834393813165636100 ) ) ;
#62522=CARTESIAN_POINT ( 'NONE',  ( 6.221994747346401233, -1.249160343739505352, -1.886125069868335613 ) ) ;
#62524=CARTESIAN_POINT ( 'NONE',  ( 5.871335974614770414, -1.558408318232169298, -0.9234296637983196998 ) ) ;
#62525=CARTESIAN_POINT ( 'NONE',  ( 5.999236059146234368, -0.2270968913323672123, 1.902120139356741069 ) ) ;
#62528=CARTESIAN_POINT ( 'NONE',  ( 6.016445890116215445, 1.255022122864515310, -1.387330985440645037 ) ) ;
#62530=CARTESIAN_POINT ( 'NONE',  ( 6.473528777534793832, 1.692185636751794897, -0.5185713626470798143 ) ) ;
#62531=CARTESIAN_POINT ( 'NONE',  ( 1.182827746461931229, 1.645757370610765102, -1.164989914844760444 ) ) ;
#62533=CARTESIAN_POINT ( 'NONE',  ( 3.334694542603059642, 2.054772597177223936, 0.4612437286577449891 ) ) ;
#62538=CARTESIAN_POINT ( 'NONE',  ( 2.496358458697241378, -1.034576831241553307, 1.734530517449877740 ) ) ;
#62541=CARTESIAN_POINT ( 'NONE',  ( 3.497504216883956296, 1.701635573755799324, 1.332874705691905248 ) ) ;
#62545=CARTESIAN_POINT ( 'NONE',  ( 0.7663804396884700276, -2.160669279729439562, 0.2131170157090022665 ) ) ;
#62549=CARTESIAN_POINT ( 'NONE',  ( 2.560326853991791829, -1.509077608345666066, 1.589458984681046516 ) ) ;
#62550=CARTESIAN_POINT ( 'NONE',  ( 6.983263157960368339, 1.271300847835453940, 2.069154070428773196 ) ) ;
#62551=CARTESIAN_POINT ( 'NONE',  ( 3.046068780686244981, 0.8155736813739141722, -2.110571434806473690 ) ) ;
#62558=CARTESIAN_POINT ( 'NONE',  ( 3.848697245170757508, -1.448060206101034808, 1.017097547381773159 ) ) ;
#62560=CARTESIAN_POINT ( 'NONE',  ( 6.704147062870869256, -2.206433763861126884, 0.04732420095975712476 ) ) ;
#62566=CARTESIAN_POINT ( 'NONE',  ( 4.012460596634464416, 1.323225596166040186, -1.322536486416128199 ) ) ;
#62567=CARTESIAN_POINT ( 'NONE',  ( 3.731357587288411715, 0.05568397596692270524, -2.069689236595618542 ) ) ;
#62573=CARTESIAN_POINT ( 'NONE',  ( 6.139563164240942506, -1.562336469324271837, -1.494251390645913835 ) ) ;
#62575=CARTESIAN_POINT ( 'NONE',  ( 3.262109210011232108, -1.959739898415867154, 0.09363895518171151677 ) ) ;
#62576=CARTESIAN_POINT ( 'NONE',  ( 1.106795812180675798, 0.8196504822069600182, -1.842164015508622521 ) ) ;
#62580=CARTESIAN_POINT ( 'NONE',  ( 0.5615140978009087736, 1.851110617189118734, -0.2680550677405246773 ) ) ;
#62582=CARTESIAN_POINT ( 'NONE',  ( 2.672137747239998529, 2.003105221038860684, -0.2016864653290161569 ) ) ;
#62584=CARTESIAN_POINT ( 'NONE',  ( 1.792722901331974761, 1.566437577840825712, -1.424566180320179010 ) ) ;
#62586=CARTESIAN_POINT ( 'NONE',  ( 4.246580143467587831, -2.047389768388275577, -0.3068500204662719666 ) ) ;
#62588=CARTESIAN_POINT ( 'NONE',  ( 5.419903170966573924, 1.246048553727102659, -1.678571210107776324 ) ) ;
#62590=CARTESIAN_POINT ( 'NONE',  ( 5.332948099851452461, 0.1360325894329272867, 1.820554394434070744 ) ) ;
#62596=CARTESIAN_POINT ( 'NONE',  ( 6.458075443588827014, 2.201329523236052577, -0.1558686762383256486 ) ) ;
#62598=CARTESIAN_POINT ( 'NONE',  ( 5.180287844241702189, 0.9460499258955605839, 1.661804969971327761 ) ) ;
#62606=CARTESIAN_POINT ( 'NONE',  ( 5.096879011283717453, 1.555924861325823416, -1.037969726935553005 ) ) ;
#62607=CARTESIAN_POINT ( 'NONE',  ( -0.02319159430949970999, 0.003959926571647092407, -1.810968101872318714 ) ) ;
#62614=CARTESIAN_POINT ( 'NONE',  ( 0.8835773814684219074, -1.871821877138898582, 0.6126781507047509567 ) ) ;
#62615=CARTESIAN_POINT ( 'NONE',  ( 3.304314702139679039, 1.277028363417181289, -1.560513873864778578 ) ) ;
#62619=CARTESIAN_POINT ( 'NONE',  ( 3.152458698460915532, -1.659165413833121550, 1.431739491984926671 ) ) ;
#62621=CARTESIAN_POINT ( 'NONE',  ( 6.825078400183572036, 4.699117039843025090, 2.418333817060664526 ) ) ;
#62628=CARTESIAN_POINT ( 'NONE',  ( 5.003375819710620398, -1.831856422778654681, 0.1858995714831001289 ) ) ;
#62629=CARTESIAN_POINT ( 'NONE',  ( 1.436190773529995468, -1.120142249841639348, -1.672479584328613988 ) ) ;
#62630=CARTESIAN_POINT ( 'NONE',  ( 3.814061661026487915, -1.881531058455442329, 1.319806432912509209 ) ) ;
#62631=CARTESIAN_POINT ( 'NONE',  ( -0.02880301295724378360, 1.300294777490899056, -2.522425657339548266 ) ) ;
#62632=CARTESIAN_POINT ( 'NONE',  ( 2.131498006616658891, 1.782543213153169548, -0.5345681993311669489 ) ) ;
#62635=CARTESIAN_POINT ( 'NONE',  ( 5.431871263539022721, -1.864374737420209760, 0.4251265778823994368 ) ) ;
#62639=CARTESIAN_POINT ( 'NONE',  ( 4.335544241866786663, 0.8922555979511301860, -1.890918108395107211 ) ) ;
#62640=CARTESIAN_POINT ( 'NONE',  ( 2.887410755087606695, 1.321643875934110479, 1.324118206929347563 ) ) ;
#62642=CARTESIAN_POINT ( 'NONE',  ( 6.216338285296751920, 1.720575329815833943, 0.6561210673821931127 ) ) ;
#62645=CARTESIAN_POINT ( 'NONE',  ( 5.373588365490253871, 1.660756567380991866, -0.4657003604296525157 ) ) ;
#62651=CARTESIAN_POINT ( 'NONE',  ( 5.014598762909163732, 0.8246402433861481640, 2.008555861535677778 ) ) ;
#62652=CARTESIAN_POINT ( 'NONE',  ( 4.564971734551386717, -1.632036996880025903, -0.8184370388232551363 ) ) ;
#62653=CARTESIAN_POINT ( 'NONE',  ( 1.586688997538304058, 1.889165970957426444, 0.5283831072378853966 ) ) ;
#62654=CARTESIAN_POINT ( 'NONE',  ( -0.1056256405159265443, -0.9088113327815927622, -1.910082645617340757 ) ) ;
#62659=CARTESIAN_POINT ( 'NONE',  ( 3.071057173463411338, -1.604308532545582366, 1.386676294644908713 ) ) ;
#62663=CARTESIAN_POINT ( 'NONE',  ( 0.4794554595633391814, -0.1051018081165492196, 2.067734805981166435 ) ) ;
#62664=CARTESIAN_POINT ( 'NONE',  ( 6.883263157960371359, 1.234153227268469877, 2.265917448979277271 ) ) ;
#62666=CARTESIAN_POINT ( 'NONE',  ( 2.737233380259511684, 2.092449130469396401, 0.7459289674271016857 ) ) ;
#62668=CARTESIAN_POINT ( 'NONE',  ( 0.2296305240335142495, 2.293118238291039113, 0.1608910274224564507 ) ) ;
#62670=CARTESIAN_POINT ( 'NONE',  ( 5.278211761479340680, -1.098870959053561469, -1.745292714083917174 ) ) ;
#62674=CARTESIAN_POINT ( 'NONE',  ( 0.2333540202161792088, 6.948072531064760859, -2.640811564931430766 ) ) ;
#62675=CARTESIAN_POINT ( 'NONE',  ( 5.319803798718575116, 1.092037692397327620, -1.482314076171886708 ) ) ;
#62677=CARTESIAN_POINT ( 'NONE',  ( 1.482971688208828187, 1.595641881047437538, -0.6553127101004208033 ) ) ;
#62678=CARTESIAN_POINT ( 'NONE',  ( 0.6906390985809904848, 1.523792322931913468, -1.320830384837400118 ) ) ;
#62680=CARTESIAN_POINT ( 'NONE',  ( 2.303761666418477461, 1.498124540730429333, -1.743551778261544838 ) ) ;
#62682=CARTESIAN_POINT ( 'NONE',  ( 2.161739655719534081, 0.3883039046224411317, -2.228698702525088393 ) ) ;
#62683=CARTESIAN_POINT ( 'NONE',  ( 3.633512520595981066, -1.945918672469678867, 0.8060524589711003385 ) ) ;
#62685=CARTESIAN_POINT ( 'NONE',  ( 2.952157954411178675, 0.5926004979403748374, 1.667723606733088060 ) ) ;
#62688=CARTESIAN_POINT ( 'NONE',  ( 5.706620831843001618, 2.020032061211772589, 1.083668233456626551 ) ) ;
#62689=CARTESIAN_POINT ( 'NONE',  ( 4.945164379994194448, 0.5744887182440976403, -1.749284230371531024 ) ) ;
#62693=CARTESIAN_POINT ( 'NONE',  ( 4.119203469048302146, -2.097337170177868693, 0.6352863671069891582 ) ) ;
#62698=CARTESIAN_POINT ( 'NONE',  ( 3.264201069286599477, 0.8669165009558920110, 1.720499056138290683 ) ) ;
#62701=CARTESIAN_POINT ( 'NONE',  ( 5.660427296577901224, 2.118236611397010805, 0.1021076702828054988 ) ) ;
#62711=CARTESIAN_POINT ( 'NONE',  ( 2.208218529973245303, 1.555207145793806811, 0.7814158636046761863 ) ) ;
#62713=CARTESIAN_POINT ( 'NONE',  ( 0.3968290921660848625, 0.3316028935436679537, 1.933473477243151439 ) ) ;
#62716=CARTESIAN_POINT ( 'NONE',  ( 6.139563164240942506, -1.562336469324271837, -1.494251390645913613 ) ) ;
#62720=CARTESIAN_POINT ( 'NONE',  ( 5.454052192070485638, 2.159419290912270029, -0.1019294599445344784 ) ) ;
#62724=CARTESIAN_POINT ( 'NONE',  ( 6.555938671473301227, 1.966215360770405818, -0.1428278144062731236 ) ) ;
#62725=CARTESIAN_POINT ( 'NONE',  ( 6.397740202767369766, 0.1737558121157663782, 1.725068634017632885 ) ) ;
#62727=CARTESIAN_POINT ( 'NONE',  ( 2.788834510562918645, 1.878274557074947948, -1.128960604485473862 ) ) ;
#62728=CARTESIAN_POINT ( 'NONE',  ( 3.821538862543779391, -0.1730032229720068482, 2.301163704417693356 ) ) ;
#62729=CARTESIAN_POINT ( 'NONE',  ( 5.940714679333914283, 0.3976391751681263576, 2.021873298595587176 ) ) ;
#62730=CARTESIAN_POINT ( 'NONE',  ( 1.060374178334378303, -1.755330386401842802, -0.8309217204432550741 ) ) ;
#62735=CARTESIAN_POINT ( 'NONE',  ( 3.990573222356631256, -1.218298518170106925, 1.735533685479621502 ) ) ;
#62736=CARTESIAN_POINT ( 'NONE',  ( 2.408827471728996361, -1.163269702728772392, -1.646838680093346996 ) ) ;
#62738=CARTESIAN_POINT ( 'NONE',  ( 4.120313900606538127, -1.131812998600056241, -1.894281110011143632 ) ) ;
#62741=CARTESIAN_POINT ( 'NONE',  ( 0.3986991128735201673, 1.519733473351183362, -1.011397189243423700 ) ) ;
#62744=CARTESIAN_POINT ( 'NONE',  ( 6.825078400183572036, 2.942104585519232263, 2.696255528691358982 ) ) ;
#62747=CARTESIAN_POINT ( 'NONE',  ( 4.416905344109374632, 1.883477791879540231, 0.8369615876049685266 ) ) ;
#62752=CARTESIAN_POINT ( 'NONE',  ( 2.930336769707508893, -0.9972767022783147750, -1.756213584645490267 ) ) ;
#62757=CARTESIAN_POINT ( 'NONE',  ( 2.536071046656536598, 0.9725223524452746293, -1.817000187329747884 ) ) ;
#62758=CARTESIAN_POINT ( 'NONE',  ( 2.901017702322743919, -0.9963018188003970321, -1.753030416019534021 ) ) ;
#62763=CARTESIAN_POINT ( 'NONE',  ( 3.181017370561005198, -0.9912469002804729090, -1.755500664876320727 ) ) ;
#62764=CARTESIAN_POINT ( 'NONE',  ( 1.868857239601273923, 1.762127240619456803, -0.5335365013287919345 ) ) ;
#62765=CARTESIAN_POINT ( 'NONE',  ( 6.656857027519620829, -1.708965229049699053, 1.396003577074665714 ) ) ;
#62767=CARTESIAN_POINT ( 'NONE',  ( 2.214359598146302677, -1.016813397907929239, -1.907474440234189217 ) ) ;
#62769=CARTESIAN_POINT ( 'NONE',  ( 5.102788515576859751, 1.957488760995762300, 0.8075332785216599030 ) ) ;
#62773=CARTESIAN_POINT ( 'NONE',  ( 0.8834254411415434216, 1.253375741028007084, 1.388844808110502038 ) ) ;
#62775=CARTESIAN_POINT ( 'NONE',  ( 5.489129097700779170, 1.738912991666073715, -0.9288780838571459864 ) ) ;
#62779=CARTESIAN_POINT ( 'NONE',  ( 6.498663405296385420, -0.5599463640075187376, -2.030188946737851108 ) ) ;
#62780=CARTESIAN_POINT ( 'NONE',  ( 5.934052368846653991, 1.230181698326970885, 1.665117723180092213 ) ) ;
#62783=CARTESIAN_POINT ( 'NONE',  ( 6.639320575229281651, -0.0007625845807879281287, 2.103388539994067497 ) ) ;
#62784=CARTESIAN_POINT ( 'NONE',  ( 4.821144081919094049, -0.09777198692111942202, 1.969167557456591666 ) ) ;
#62785=CARTESIAN_POINT ( 'NONE',  ( 6.117445925308827803, 1.681535965833020230, 1.118592408852390641 ) ) ;
#62787=CARTESIAN_POINT ( 'NONE',  ( 4.688248866636615553, -1.090845489383242883, 2.033590232148785759 ) ) ;
#62789=CARTESIAN_POINT ( 'NONE',  ( 1.938405323705337135, -1.106995438288145950, 1.740174596247965555 ) ) ;
#62796=CARTESIAN_POINT ( 'NONE',  ( 4.176368576274028577, -1.112882343535037677, -1.864130199707826785 ) ) ;
#62799=CARTESIAN_POINT ( 'NONE',  ( 3.597050949361340511, -0.5310884314010614338, 1.763007376093472800 ) ) ;
#62802=CARTESIAN_POINT ( 'NONE',  ( 6.620655732516647518, 7.053381450551401421, 2.424417106520880161 ) ) ;
#62803=CARTESIAN_POINT ( 'NONE',  ( 5.513277522340928272, -2.138352208816508782, 0.4792397250529822905 ) ) ;
#62805=CARTESIAN_POINT ( 'NONE',  ( 5.647450836711301214, -1.779752484188871886, -1.396855495411459147 ) ) ;
#62811=CARTESIAN_POINT ( 'NONE',  ( 0.6722625022101048620, -1.664400848580146919, -0.6021564899992714048 ) ) ;
#62813=CARTESIAN_POINT ( 'NONE',  ( 4.811194018343159406, 1.672433887399711994, -1.120210643937557871 ) ) ;
#62815=CARTESIAN_POINT ( 'NONE',  ( 4.489357033980984291, 1.882333632172785487, -0.9445240646021864084 ) ) ;
#62816=CARTESIAN_POINT ( 'NONE',  ( 2.495587842290597713, -1.894396863028270594, 0.2834604161582406356 ) ) ;
#62819=CARTESIAN_POINT ( 'NONE',  ( 2.910559396907284047, 0.6610699718948702674, 1.855445417178583911 ) ) ;
#62820=CARTESIAN_POINT ( 'NONE',  ( 5.273696820376614802, 0.3899264243738297941, -1.981607871481812833 ) ) ;
#62821=CARTESIAN_POINT ( 'NONE',  ( 1.463515404423965105, 1.843522461416190250, -0.3164952454337774390 ) ) ;
#62822=CARTESIAN_POINT ( 'NONE',  ( 2.049198471137442912, 1.708465938063120637, -0.9642302061752603404 ) ) ;
#62823=CARTESIAN_POINT ( 'NONE',  ( 3.457353000975535551, 0.4177302890290990889, -1.673392258113172382 ) ) ;
#62824=CARTESIAN_POINT ( 'NONE',  ( 1.037202349414727109, -0.04413313863061394532, 1.912034500058952036 ) ) ;
#62826=CARTESIAN_POINT ( 'NONE',  ( 1.278255639411193245, 1.316999024263129092, 1.770685722221450709 ) ) ;
#62833=CARTESIAN_POINT ( 'NONE',  ( 6.965700764728601335, -0.4599482372066622249, 2.025938098699997525 ) ) ;
#62834=CARTESIAN_POINT ( 'NONE',  ( 1.258353326579707776, -2.070544811992577561, -0.001879966208345739808 ) ) ;
#62839=CARTESIAN_POINT ( 'NONE',  ( 5.742871283745087041, 2.043606947765171267, 0.5656136300068030920 ) ) ;
#62845=CARTESIAN_POINT ( 'NONE',  ( 6.144970055084349347, -0.2864424343173576082, -1.940704187532462210 ) ) ;
#62847=CARTESIAN_POINT ( 'NONE',  ( 4.569685373303983944, 1.560260980002409870, -1.276848140101802365 ) ) ;
#62848=CARTESIAN_POINT ( 'NONE',  ( 3.344859342474030939, -1.692025585574646662, -0.8982749641134063490 ) ) ;
#62849=CARTESIAN_POINT ( 'NONE',  ( 1.611130907606239004, -0.2639259086049255965, 2.175532687872412829 ) ) ;
#62852=CARTESIAN_POINT ( 'NONE',  ( 4.799092303436800933, -0.2508153390233992530, -1.997484173059483892 ) ) ;
#62854=CARTESIAN_POINT ( 'NONE',  ( 5.958642064211575828, -2.010625215935774257, -0.6636248059145292144 ) ) ;
#62855=CARTESIAN_POINT ( 'NONE',  ( 3.263305109790759939, 2.039240668410980284, -0.4604351538632973639 ) ) ;
#62857=CARTESIAN_POINT ( 'NONE',  ( 1.693959787788183347, -1.716010565565774915, -0.1736237626131422462 ) ) ;
#62859=CARTESIAN_POINT ( 'NONE',  ( 4.939744792934912532, -2.012803497507459127, 0.6676120485993168874 ) ) ;
#62863=FILL_AREA_STYLE ('',( #212300 ) ) ;
#62868=CARTESIAN_POINT ( 'NONE',  ( 1.312835156398382885, 1.481033882128342194, -1.042734985588577468 ) ) ;
#62874=CARTESIAN_POINT ( 'NONE',  ( 2.332397652471474903, 1.182373381703984094, -1.372477691862858729 ) ) ;
#62879=CARTESIAN_POINT ( 'NONE',  ( 3.455356687279837136, 1.465577529964179115, 1.146850193174092203 ) ) ;
#62880=CARTESIAN_POINT ( 'NONE',  ( 1.036581048048822673, -1.509151586612084373, 1.179680973199858318 ) ) ;
#62881=CARTESIAN_POINT ( 'NONE',  ( 0.2174332111963481196, -1.791455004416471430, 0.3504355335035569396 ) ) ;
#62888=CARTESIAN_POINT ( 'NONE',  ( 4.293777937636614972, -1.355062202172536034, -1.429424366026492033 ) ) ;
#62892=CARTESIAN_POINT ( 'NONE',  ( 0.6211766780156646739, -1.984520161701831986, 0.6578015034230285663 ) ) ;
#62894=CARTESIAN_POINT ( 'NONE',  ( 5.491212607897098863, 1.698784202212012762, -0.9083314536618128932 ) ) ;
#62896=CARTESIAN_POINT ( 'NONE',  ( 1.500715674837904468, 1.494693011815557693, -1.047886037138339166 ) ) ;
#62897=CARTESIAN_POINT ( 'NONE',  ( 2.438337523484556790, 1.039148161723329578, -1.946916322307743252 ) ) ;
#62899=CARTESIAN_POINT ( 'NONE',  ( 0.4043728756845180183, -1.898191424145349471, -0.2318213773434482650 ) ) ;
#62902=CARTESIAN_POINT ( 'NONE',  ( 0.1683113222354900018, -0.8393015767643360325, -1.780324559216818425 ) ) ;
#62903=CARTESIAN_POINT ( 'NONE',  ( 1.399837892970667630, -0.7005499098489911258, -1.811468074468420841 ) ) ;
#62904=CARTESIAN_POINT ( 'NONE',  ( 1.194685229111978497, -1.276845315561925931, -1.560263297373874813 ) ) ;
#62906=CARTESIAN_POINT ( 'NONE',  ( 5.664867498354182018, 1.410286671683948168, -1.214315750818369510 ) ) ;
#62913=CARTESIAN_POINT ( 'NONE',  ( 1.382659466718983543, -0.3261178763579902218, -2.167053615394160637 ) ) ;
#62918=CARTESIAN_POINT ( 'NONE',  ( 1.400715809426569702, 1.493624456287694358, -1.049586478250638999 ) ) ;
#62922=CARTESIAN_POINT ( 'NONE',  ( 6.609000000000038177, 0.002801690667396730672, 2.000160786441218530 ) ) ;
#62924=CARTESIAN_POINT ( 'NONE',  ( 1.049297559255836010, -1.518254527582623359, -1.185787014772927916 ) ) ;
#62925=CARTESIAN_POINT ( 'NONE',  ( 6.034033239799157400, 1.165729394902741189, 1.577711426528668692 ) ) ;
#62929=CARTESIAN_POINT ( 'NONE',  ( 4.827760788416924242, 1.126602223531171898, -1.879657820484957664 ) ) ;
#62932=CARTESIAN_POINT ( 'NONE',  ( 3.748938768049938197, -0.3990674421511587466, -2.031259957477090428 ) ) ;
#62936=CARTESIAN_POINT ( 'NONE',  ( 3.955939753277417648, -2.145046849925678956, -0.8267234532119535073 ) ) ;
#62941=CARTESIAN_POINT ( 'NONE',  ( 6.620655732516668834, 7.629137130509086262, 2.526260288887293814 ) ) ;
#62942=CARTESIAN_POINT ( 'NONE',  ( 3.872937777176552299, 1.828215432968218535, -0.6551730591081408317 ) ) ;
#62945=CARTESIAN_POINT ( 'NONE',  ( 5.326388512780113160, -0.8654452107222168067, -1.705464787417856787 ) ) ;
#62947=CARTESIAN_POINT ( 'NONE',  ( 6.809587843971872445, -0.3681478646948634914, 1.690922663601742038 ) ) ;
#62948=CARTESIAN_POINT ( 'NONE',  ( 4.171111447311355747, 1.799123655847803205, -0.9110083886025857058 ) ) ;
#62950=CARTESIAN_POINT ( 'NONE',  ( 0.6630615684519860498, -1.595754342771567025, 1.524677653706180802 ) ) ;
#62953=CARTESIAN_POINT ( 'NONE',  ( 0.07627643479381736313, -2.028408900457449704, -0.5058713263092640133 ) ) ;
#62954=CARTESIAN_POINT ( 'NONE',  ( 6.591055360535956531, 1.538344802651976373, -0.8746889052434738687 ) ) ;
#62955=CARTESIAN_POINT ( 'NONE',  ( 5.432267593368638181, -1.591316862017605471, -1.238322901282742805 ) ) ;
#62957=CARTESIAN_POINT ( 'NONE',  ( 3.574455624386526420, -2.209025962754256334, -0.6118928016028857275 ) ) ;
#62958=CARTESIAN_POINT ( 'NONE',  ( 0.9193797689642355664, 1.039780534333001771, -1.395406566618085709 ) ) ;
#62959=DIRECTION ( 'NONE',  ( 1.039099362110107450E-15, 1.000000000000000000, -4.583713267641621330E-32 ) ) ;
#62960=CARTESIAN_POINT ( 'NONE',  ( 1.369977976685434751, -0.4280273037657927881, 1.680018549819038531 ) ) ;
#62963=CARTESIAN_POINT ( 'NONE',  ( 1.733130889747940495, -2.061367544037566280, -0.6818780404978814769 ) ) ;
#62964=CARTESIAN_POINT ( 'NONE',  ( 2.044158018538293042, 0.8666093899718421145, 1.820985203412978093 ) ) ;
#62965=CARTESIAN_POINT ( 'NONE',  ( 4.406250000000002665, 1.895863743163984649, -0.7852924748302168023 ) ) ;
#62968=CARTESIAN_POINT ( 'NONE',  ( 6.076777883369302913, -1.830186849185039044, -0.6017253874085000120 ) ) ;
#62970=CARTESIAN_POINT ( 'NONE',  ( 3.463320643641348173, -1.814240386431978713, 1.281607931980492054 ) ) ;
#62977=CARTESIAN_POINT ( 'NONE',  ( 5.267066465580821699, 1.675244640197434798, -0.4716337365339871579 ) ) ;
#62978=CARTESIAN_POINT ( 'NONE',  ( 3.719154087244529894, -1.729071306366702476, -0.9269775827704658244 ) ) ;
#62983=CARTESIAN_POINT ( 'NONE',  ( 4.077597889297270406, 2.132052650593726728, -0.7572755323067262845 ) ) ;
#62984=CARTESIAN_POINT ( 'NONE',  ( 1.662626038903247228, -0.7403543059694576156, -1.925410787417888958 ) ) ;
#62986=CARTESIAN_POINT ( 'NONE',  ( 2.870297354751516039, 1.209492683862042339, 1.911920897162355582 ) ) ;
#62989=CARTESIAN_POINT ( 'NONE',  ( 3.725732288501612199, -1.111853074318921664, -1.504101509696729400 ) ) ;
#62990=CARTESIAN_POINT ( 'NONE',  ( 2.232704217388951751, 1.733830997258398066, 0.04099941454244887540 ) ) ;
#62991=CARTESIAN_POINT ( 'NONE',  ( 6.075747529084263299, -1.173811750163206158, 1.850510016281024850 ) ) ;
#62992=CARTESIAN_POINT ( 'NONE',  ( 6.791963826450252206, -0.9943653912195188349, 2.080009744879149913 ) ) ;
#62993=CARTESIAN_POINT ( 'NONE',  ( 4.399409362686744096, 1.734418756986338295, 1.290045131933370781 ) ) ;
#62994=CARTESIAN_POINT ( 'NONE',  ( 4.751864635371732426, 0.7446896046985322926, 1.793680106537680174 ) ) ;
#62996=CARTESIAN_POINT ( 'NONE',  ( 6.919227945209173392, -0.1346273106918663420, 1.840389347376285345 ) ) ;
#63002=CARTESIAN_POINT ( 'NONE',  ( 6.082657761774013849, -0.6767167302549759178, 1.899617564980569995 ) ) ;
#63007=CARTESIAN_POINT ( 'NONE',  ( 3.492628380820805400, -0.3572889717703279788, -1.790209119249221548 ) ) ;
#63008=CARTESIAN_POINT ( 'NONE',  ( -0.1296875068447916890, 6.948706544289747988, -2.421546651465163347 ) ) ;
#63013=CARTESIAN_POINT ( 'NONE',  ( 0.2815179179852530522, 0.1935487615560542163, -2.010460980806235920 ) ) ;
#63014=CARTESIAN_POINT ( 'NONE',  ( 1.612141420133822223, -0.7113448269009944314, 1.997755531611951962 ) ) ;
#63018=CARTESIAN_POINT ( 'NONE',  ( 1.692022144237431469, 0.9228297918665344657, -1.615966242530289199 ) ) ;
#63021=CARTESIAN_POINT ( 'NONE',  ( 0.07536363704235826688, -0.001874865094115066300, -2.144269471569634877 ) ) ;
#63022=CARTESIAN_POINT ( 'NONE',  ( 5.977185442992979603, -2.006959616289708315, -0.1948445219252663840 ) ) ;
#63028=CARTESIAN_POINT ( 'NONE',  ( 4.389149243953620605, 1.629682310347341456, -0.8231139397327084106 ) ) ;
#63033=CARTESIAN_POINT ( 'NONE',  ( 6.204453847213379447, -1.458334814074750740, -1.392330997281837623 ) ) ;
#63034=CARTESIAN_POINT ( 'NONE',  ( 5.982333729491328356, -0.2747192703472668418, -1.820405398140816589 ) ) ;
#63036=CARTESIAN_POINT ( 'NONE',  ( 3.211855371912860413, -0.4501829054360923510, 2.263203710529379187 ) ) ;
#63038=CARTESIAN_POINT ( 'NONE',  ( 5.641917277892137150, 0.8817427965214555963, -1.973778517010720490 ) ) ;
#63040=CARTESIAN_POINT ( 'NONE',  ( 1.628360684195095054, 0.1923838640373880249, 1.932526033267305765 ) ) ;
#63042=CARTESIAN_POINT ( 'NONE',  ( 5.044420649243852139, 2.147057653193120252, -0.8206418397275447862 ) ) ;
#63046=CARTESIAN_POINT ( 'NONE',  ( 4.188257260935820625, -1.850246793840780279, -0.2747695030091561463 ) ) ;
#63048=B_SPLINE_CURVE_WITH_KNOTS ( 'NONE', 3,
 ( #126796, #192751, #76878, #127876, #208997, #44408, #110528, #163479, #176528, #31351, #28140 ),
 .UNSPECIFIED., .F., .F.,
 ( 4, 1, 1, 1, 1, 1, 1, 1, 4 ),
 ( 0.000000000000000000, 0.2256926809922864541, 0.3979886288388991278, 0.5260859906349554249, 0.6192013483571605637, 0.6864504996671639825, 0.7364865548622955282, 0.7772638159577213157, 1.000000000000000000 ),
 .UNSPECIFIED. ) ;
#63049=CARTESIAN_POINT ( 'NONE',  ( 1.037202349414727109, -0.04413313863061394532, 1.912034500058952036 ) ) ;
#63052=CARTESIAN_POINT ( 'NONE',  ( 4.442132104469964204, 0.9450947508268662256, -1.994404356956205326 ) ) ;
#63053=CARTESIAN_POINT ( 'NONE',  ( 6.983263157960327483, 4.697935251208478213, 2.408834092705824936 ) ) ;
#63057=CARTESIAN_POINT ( 'NONE',  ( 1.493369529629706705, 1.490176471889271603, 1.290657618255620864 ) ) ;
#63058=CARTESIAN_POINT ( 'NONE',  ( 1.519075522400476830, 1.548194965108589782, -1.711296875134951545 ) ) ;
#63059=CARTESIAN_POINT ( 'NONE',  ( 2.682025323810240280, -1.127217178123595565, -1.605522638798158264 ) ) ;
#63061=CARTESIAN_POINT ( 'NONE',  ( 5.717653809678179044, 0.4078037869292486239, -2.021697613586806774 ) ) ;
#63068=CARTESIAN_POINT ( 'NONE',  ( 1.182764167570474534, 1.294921473658101840, -1.742447618606123960 ) ) ;
#63073=CARTESIAN_POINT ( 'NONE',  ( 2.143623209005097507, 0.7202431893391960660, -1.726524797105493336 ) ) ;
#63074=CARTESIAN_POINT ( 'NONE',  ( 6.450466699499744827, 0.6713059571747861387, 2.054807225473152865 ) ) ;
#63076=CARTESIAN_POINT ( 'NONE',  ( 6.827182134110207024, 2.985003573113382824, 2.264833014350222662 ) ) ;
#63079=CARTESIAN_POINT ( 'NONE',  ( 2.525908831824146716, -1.891188341833285103, 0.2824699455093656053 ) ) ;
#63080=CARTESIAN_POINT ( 'NONE',  ( 4.223360090310752213, -1.693420319160190646, 0.5144795390387302270 ) ) ;
#63081=CARTESIAN_POINT ( 'NONE',  ( 1.752457306817490457, 1.891635876823925200, 0.2793096714826873161 ) ) ;
#63084=CARTESIAN_POINT ( 'NONE',  ( 5.800374965758359203, 1.282846238547242557, -1.422814914302351852 ) ) ;
#63085=CARTESIAN_POINT ( 'NONE',  ( 0.1685321339487330372, -0.8835925182541467526, -1.870455940253319183 ) ) ;
#63087=CARTESIAN_POINT ( 'NONE',  ( 2.267978396857213585, 0.5610993688725562922, -2.044979925899123252 ) ) ;
#63089=CARTESIAN_POINT ( 'NONE',  ( 5.278141497218024725, -1.038406966791558528, 1.555765341417144842 ) ) ;
#63090=CARTESIAN_POINT ( 'NONE',  ( 1.857752496991037061, 1.820901040755190214, -0.1330985588276211995 ) ) ;
#63091=VERTEX_POINT ( 'NONE', #3316 ) ;
#63092=CARTESIAN_POINT ( 'NONE',  ( 4.108205984530819421, -2.201057848371779535, 0.1611738814469021175 ) ) ;
#63095=CARTESIAN_POINT ( 'NONE',  ( 1.943872066224684669, 1.420748078972498440, 1.495595626624636409 ) ) ;
#63103=CARTESIAN_POINT ( 'NONE',  ( 4.246580143467587831, -2.047389768388275577, -0.3068500204662719666 ) ) ;
#63105=CARTESIAN_POINT ( 'NONE',  ( 2.091316376603330252, 1.881825464268515269, -1.063406855978922039 ) ) ;
#63107=CARTESIAN_POINT ( 'NONE',  ( 2.297526485177129540, 1.845687725436034432, -0.8205148536439119678 ) ) ;
#63109=CARTESIAN_POINT ( 'NONE',  ( 6.620655732516611103, 6.035157181942712334, 2.668628960472289702 ) ) ;
#63116=CARTESIAN_POINT ( 'NONE',  ( 1.499232818411553536, -0.2420282084563407654, 2.001858358113464575 ) ) ;
#63117=CARTESIAN_POINT ( 'NONE',  ( 5.653911837654605144, 0.8871495062587383407, 2.004161502255866090 ) ) ;
#63119=CARTESIAN_POINT ( 'NONE',  ( 5.220932206144772714, 1.444093599275039885, -1.253800916539760113 ) ) ;
#63121=CARTESIAN_POINT ( 'NONE',  ( 4.259000112335223243, -0.004834882008357410665, -2.016708403958865414 ) ) ;
#63124=CARTESIAN_POINT ( 'NONE',  ( 1.845327587665198443, 0.3419125196015109225, -1.987051676161588620 ) ) ;
#63127=CARTESIAN_POINT ( 'NONE',  ( 5.473588350598873831, 1.661195908839340873, -0.4637430927098630806 ) ) ;
#63128=CARTESIAN_POINT ( 'NONE',  ( -0.1394461523061326647, 2.860155921427895542, -2.768185420354400073 ) ) ;
#63131=( BOUNDED_SURFACE ( )  B_SPLINE_SURFACE ( 3, 3, ( 
 ( #93254, #31434, #114864, #28227, #97512, #96457, #163569, #15152, #213347, #81238 ),
 ( #30370, #94320, #146274, #27150, #159288, #10887, #44498, #209081, #126881, #192839 ),
 ( #110615, #160361, #18352, #165686, #49801, #20480, #119129, #33547, #151582, #1018 ),
 ( #100678, #135338, #136401, #70285, #17275, #201352, #150519, #67083, #84430, #83351 ),
 ( #2080, #185109, #36735, #180865, #202417, #52993, #102821, #132162, #34609, #16206 ),
 ( #68153, #182992, #166756, #69219, #134287, #4216, #167817, #149436, #164621, #99620 ),
 ( #101750, #50870, #35672, #184053, #168876, #116992, #200292, #19417, #133217, #54072 ) ),
 .UNSPECIFIED., .T., .F., .F. ) 
 B_SPLINE_SURFACE_WITH_KNOTS ( ( 4, 3, 4 ),
 ( 4, 1, 1, 1, 1, 1, 1, 4 ),
 ( 0.000000000000000000, 0.5000000000000000000, 1.000000000000000000 ),
 ( 0.000000000000000000, 0.09373397616858752945, 0.1863105892815605236, 0.2574079725677296260, 0.3612190813870841954, 0.5208938042821120717, 0.7336009914826546741, 1.000000000000000000 ),
 .UNSPECIFIED. ) 
 GEOMETRIC_REPRESENTATION_ITEM ( )  RATIONAL_B_SPLINE_SURFACE ( (
 ( 1.000000000000000000, 1.000000000000000000, 0.9999999999999997780, 1.000000000000000000, 1.000000000000000000, 1.000000000000000222, 1.000000000000000444, 1.000000000000000222, 1.000000000000000000, 1.000000000000000000),
 ( 0.3333333333333333703, 0.3333333333333333703, 0.3333333333333332593, 0.3333333333333333703, 0.3333333333333333703, 0.3333333333333334259, 0.3333333333333334814, 0.3333333333333334259, 0.3333333333333333703, 0.3333333333333333703),
 ( 0.3333333333333333703, 0.3333333333333333703, 0.3333333333333332593, 0.3333333333333333703, 0.3333333333333333703, 0.3333333333333334259, 0.3333333333333334814, 0.3333333333333334259, 0.3333333333333333703, 0.3333333333333333703),
 ( 1.000000000000000000, 1.000000000000000000, 0.9999999999999997780, 1.000000000000000000, 1.000000000000000000, 1.000000000000000222, 1.000000000000000444, 1.000000000000000222, 1.000000000000000000, 1.000000000000000000),
 ( 0.3333333333333333703, 0.3333333333333333703, 0.3333333333333332593, 0.3333333333333333703, 0.3333333333333333703, 0.3333333333333334259, 0.3333333333333334814, 0.3333333333333334259, 0.3333333333333333703, 0.3333333333333333703),
 ( 0.3333333333333333703, 0.3333333333333333703, 0.3333333333333332593, 0.3333333333333333703, 0.3333333333333333703, 0.3333333333333334259, 0.3333333333333334814, 0.3333333333333334259, 0.3333333333333333703, 0.3333333333333333703),
 ( 1.000000000000000000, 1.000000000000000000, 0.9999999999999997780, 1.000000000000000000, 1.000000000000000000, 1.000000000000000222, 1.000000000000000444, 1.000000000000000222, 1.000000000000000000, 1.000000000000000000) ) ) 
 REPRESENTATION_ITEM ( '' )  SURFACE ( )  );
#63134=CARTESIAN_POINT ( 'NONE',  ( 0.9364849611055334755, -1.153160888946737961, 1.719151461320179042 ) ) ;
#63137=CARTESIAN_POINT ( 'NONE',  ( 4.600164522386200439, -0.8494929878282222457, 1.599918020626096782 ) ) ;
#63140=CARTESIAN_POINT ( 'NONE',  ( 6.610000000000006537, 0.002781820520842553934, 2.000159646111852929 ) ) ;
#63141=CARTESIAN_POINT ( 'NONE',  ( 6.076794983551159213, -1.275939312151072258, 1.286130553019491307 ) ) ;
#63144=CARTESIAN_POINT ( 'NONE',  ( 3.082162360440068749, -2.159116730143955998, -0.3741398933536920768 ) ) ;
#63146=CARTESIAN_POINT ( 'NONE',  ( 0.1390251588108057101, -0.1389306544097475005, -1.930426113910483688 ) ) ;
#63148=CARTESIAN_POINT ( 'NONE',  ( 5.132410944242819184, 0.5605724621733051416, 1.831730044279370029 ) ) ;
#63154=CARTESIAN_POINT ( 'NONE',  ( 1.411231610350563992, 1.906656261001705488, 1.018656936289302539 ) ) ;
#63157=CARTESIAN_POINT ( 'NONE',  ( 1.711645973048509850, -1.812212506298327197, 0.2199163931802459171 ) ) ;
#63159=CARTESIAN_POINT ( 'NONE',  ( 4.190329584092522097, -1.805708503706305423, -0.2678305112727846771 ) ) ;
#63162=CARTESIAN_POINT ( 'NONE',  ( 4.088306882321583124, 1.055547913133596749, -1.662622193200061771 ) ) ;
#63164=CARTESIAN_POINT ( 'NONE',  ( 5.179219622276672652, 1.307079648806110050, 1.436513822289321674 ) ) ;
#63168=CARTESIAN_POINT ( 'NONE',  ( 5.150683391976684788, 2.089615912265533559, 0.3601871064465370087 ) ) ;
#63170=CARTESIAN_POINT ( 'NONE',  ( 2.701700744156261713, 1.353761940859641966, 1.350867010771430676 ) ) ;
#63172=CARTESIAN_POINT ( 'NONE',  ( 6.983263157960393208, 0.5798717822590447879, 1.998431770337566027 ) ) ;
#63175=CARTESIAN_POINT ( 'NONE',  ( 5.039702193125279450, -1.910865547410881549, 0.6335069822010936935 ) ) ;
#63177=CARTESIAN_POINT ( 'NONE',  ( 6.129513044595952032, -1.717388127611047421, 0.6198453807191862674 ) ) ;
#63178=CARTESIAN_POINT ( 'NONE',  ( 1.293514844328220281, -1.872496763586928514, 0.8835221827151735763 ) ) ;
#63180=( BOUNDED_SURFACE ( )  B_SPLINE_SURFACE ( 3, 3, ( 
 ( #24239, #90341, #107720, #109857, #191012, #144467, #175871, #173747, #208332, #10137, #125057, #156410, #25324, #207273, #27459, #141265, #76212, #94629, #108787, #26389, #7997, #58904, #189959, #92501, #193162, #126118, #174813, #188890, #158540, #140180, #192078, #74089, #93557, #160672, #122933, #110916, #159601, #78344, #11199, #77280, #61034, #49063, #181178, #83667, #128268, #146586, #45874, #163887, #197421, #31749, #30684, #132475, #165999, #62109, #97822, #96767, #80486, #145535, #65275, #210471, #114132, #95697, #15462, #14395, #81548, #180124, #177998, #129334, #17584, #131421, #147631, #111996, #213649, #182232, #179065, #32803, #82605, #194230, #115183, #29612, #63168, #98877, #48015, #33856, #164930, #195310, #99937, #211533, #16522, #148690, #259, #198477, #161752, #13343, #50122, #46941, #116243, #113059, #79418, #212603, #162818, #64241, #130385, #196375, #85814, #201667, #86883, #149758, #100984, #3468, #186507, #69537, #150833, #168133, #185434, #37054, #151893, #103137, #135644, #137784, #184365, #2395, #202739, #154024, #200603, #5591, #68474, #18665, #183305, #52250, #167073, #84745, #53314, #187573, #134602, #4525, #203803, #118377, #19735, #35987, #1335, #133537, #119446, #102068, #169195, #199544, #171326, #20788, #152950, #70600, #136714, #55449, #87950, #54390, #67396, #120528, #38138, #104210, #121601, #170257, #21842, #71670, #39198, #105290, #51186, #117309, #34912, #84114, #150202, #135024, #6041, #170697, #100366, #87321, #68905, #36425, #35356, #117756, #199984, #71039, #19102, #201038, #51631, #22283, #21217, #119888, #166436, #153389, #154463, #4960, #137152, #18027, #1773, #102501, #67829, #53755, #54824, #136080, #52681, #88396, #55886, #133976, #202097, #20164, #86251, #167504, #169634, #85180, #151264, #138221, #2836, #183746, #152321, #3898, #185865, #120973, #103576, #37500, #186942, #38575, #72112, #204234, #191203, #25513, #212520, #162739, #91621, #95622, #42868, #174995, #108976, #80406, #106828, #13266, #79339, #8196, #157672, #172858, #145456, #9269, #206393, #75340, #211453, #26580, #63087, #129257, #173940, #146503, #64162, #141457, #207464, #205319, #59083, #90541, #24429, #195227, #107914, #46864, #125243, #161673, #130304, #112977, #39634, #178989, #89475, #105743, #171769, #123130, #30604, #96692, #74281, #14311, #23366, #155530, #7110, #73183, #139289, #56958, #156606, #189089, #40722, #140375, #58020, #124184, #190147, #41801, #50037, #81473, #164851, #132394, #183225, #32715, #149673, #101982, #182147, #165918, #163803, #181099, #197342, #17503, #118295, #51102, #131347, #114052, #115102, #65194, #199460, #15379, #82523, #168051, #47938, #35907, #117227, #19653, #69456, #67312, #1254, #116161, #147550, #16443, #198396, #34831, #98797, #133455, #85727, #33777, #83591, #213572, #148609, #48984, #100905, #184281, #166994, #178, #180045, #66246, #99856, #18585, #84663, #150752, #151813, #31667, #3386, #2313, #196292, #97744, #68390, #134519, #200523, #52169, #8742, #53232, #71588, #185350, #88949, #122595, #171239, #170171, #205869, #91089, #201585, #22835, #21759, #5508, #70513, #204782, #136628, #202655, #173405, #120442, #157149, #186416, #87867, #39119, #188558, #138765, #6588, #152865, #7660, #54304, #153939, #72667, #121518, #135561, #41273, #187489, #40189 ),
 ( #105202, #137697, #155003, #106301, #56436, #172323, #156074, #55365, #24986, #119362, #23913, #90017, #86799, #73744, #38053, #104125, #139840, #203717, #57503, #123662, #189625, #36972, #107382, #103055, #169108, #20705, #4443, #30340, #158215, #94292, #209052, #43400, #78008, #60688, #112713, #190680, #46595, #124720, #42339, #125783, #127935, #126852, #162476, #61766, #191745, #79070, #109522, #145188, #141986, #9804, #108454, #175530, #92163, #75879, #192809, #178725, #59626, #144132, #128980, #27119, #93225, #208000, #74823, #58566, #143057, #159257, #10858, #174474, #96425, #76931, #44468, #160332, #110584, #62820, #12995, #176586, #206937, #28198, #11936, #210125, #194959, #193887, #45535, #177661, #111649, #26049, #211194, #29269, #95361, #161411, #140923, #48722, #51917, #118040, #147289, #213321, #32461, #164591, #16177, #82261, #148354, #214353, #65983, #83322, #151295, #55918, #121005, #4992, #73216, #200013, #103607, #2866, #21248, #69999, #137186, #87355, #167534, #118845, #51664, #54854, #203208, #19132, #38604, #171803, #168595, #22317, #138253, #68936, #153423, #117787, #52712, #104682, #37530, #23395, #170731, #184827, #89508, #201070, #88430, #154494, #188038, #39667, #135058, #36457, #105778, #102533, #155562, #20195, #86283, #136113, #152354, #202128, #53789, #119920, #185895, #16630, #116345, #179170, #130494, #32906, #1437, #98984, #180233, #197527, #361, #66433, #181280, #132576, #165037, #167177, #213755, #31856, #17690, #198579, #97932, #18766, #117419, #82714, #96873, #148791, #163990, #196481, #84850, #81652, #50226, #67502, #15565, #48123, #183416, #147739, #131524, #162923, #14503, #65378, #150940, #35019, #30794, #166104, #49171, #115289, #114235, #182336, #64348, #149869, #33964, #100041, #83776, #101090, #133648, #199647, #52358, #80595, #51294, #2503, #68575, #134702, #200707, #146691, #212707, #37165, #140034, #187674, #137891, #168238, #55557, #90207, #86984, #155196, #204980, #102171, #88056, #184470, #185537, #23027, #170361, #156271, #105399, #103243, #7853, #119551, #21946, #72852, #56625, #171437, #36087, #19837, #138959, #169303, #122790, #20887, #6777, #54491, #188749, #136815, #53414, #89142, #120635, #154128, #121712, #118486, #69642, #186613, #40388, #38239, #153054, #202842, #5698, #71775, #104312, #203910, #39304, #106492, #4630, #70702, #172518, #24103, #73940, #206059, #85923, #201774, #151996, #3568, #135750, #207129, #175716, #95553, #42534, #127043, #111846, #108638, #76070, #58755, #57694, #41464, #125973, #124907, #190870, #107573, #79271, #142170, #75009, #161605, #173607, #29463, #25179, #91281, #174666, #110770, #191930, #145388, #44656, #26240, #143250, #11049, #43594, #157340, #92357, #208186, #176770, #158395, #77128, #177851, #109712, #27308, #8928, #9993, #59819, #93413, #194074, #193003, #159451, #189814, #209240, #141118, #60884, #28385, #94480, #13194, #123851, #160520, #12124, #78196, #144323, #210321, #61958, #128116, #45727, #84597, #129183, #147484, #46796, #164784, #198328, #32648, #31598, #67251, #166925, #63013, #98725, #97674, #81401, #146434, #66177, #212448, #64092, #34767, #196227, #18519, #47869, #163731, #115032, #49968, #110, #82455, #14239, #83521, #130234, #15312, #148544, #197272, #211387, #117160, #48912, #116087, #132322, #182077, #33709 ),
 ( #99786, #165852, #17437, #149602, #131285, #100840, #195161, #181031, #16376, #162669, #1187, #113980, #179977, #133386, #65127, #199391, #51037, #183163, #112909, #178920, #30535, #96615, #80333, #213506, #106235, #19588, #170105, #70450, #119294, #153876, #136565, #134454, #4378, #3318, #69387, #200457, #172260, #20640, #167983, #21691, #151747, #138701, #88886, #202586, #68323, #54238, #135495, #85661, #204719, #53166, #152799, #39054, #201518, #101917, #154940, #185281, #102985, #52103, #118232, #36903, #56369, #6524, #150685, #137635, #169043, #86729, #120376, #186351, #35839, #121453, #37986, #104059, #87803, #72601, #71524, #5445, #23848, #2247, #203654, #55304, #187424, #105139, #171179, #22770, #184216, #122532, #188493, #40125, #109458, #139776, #27049, #61699, #58500, #126787, #176519, #73677, #59556, #156006, #157083, #208989, #141922, #127868, #76869, #8671, #193818, #91021, #207934, #44398, #28131, #142989, #7593, #205803, #110519, #74754, #94227, #140856, #192743, #25985, #160265, #108383, #24917, #60625, #92093, #125715, #93157, #89955, #41206, #158147, #11867, #9739, #206869, #174408, #191676, #43338, #75814, #175464, #159195, #77944, #124656, #190612, #144065, #210060, #42271, #45466, #10795, #173337, #123595, #111583, #107313, #177593, #57434, #189560, #13990, #98467, #83262, #80074, #47609, #30273, #29205, #66995, #116905, #164532, #149348, #82201, #214292, #95295, #161344, #179727, #79005, #197024, #16118, #64888, #63830, #99535, #199132, #12925, #131034, #129988, #113723, #178661, #148294, #96358, #162413, #133133, #146177, #50777, #212192, #195976, #147233, #65926, #32401, #114777, #46531, #115840, #31346, #97420, #180775, #15056, #145122, #928, #81148, #132073, #198084, #49711, #181826, #211128, #163474, #33459, #165596, #213261, #48661, #17187, #62752, #128912, #194893, #112652, #156554, #189037, #8149, #206344, #102737, #75292, #141407, #168792, #70200, #134196, #139235, #19331, #35583, #57971, #36651, #124135, #20398, #24378, #207415, #86481, #59034, #40675, #18259, #9220, #182904, #51858, #205266, #152545, #151494, #106778, #4131, #34521, #84342, #157623, #150430, #1995, #85409, #90491, #56907, #100593, #172806, #3063, #123080, #74233, #140326, #68060, #69133, #119042, #190096, #135255, #41750, #91571, #107862, #173888, #200205, #167730, #183971, #25463, #166668, #117980, #101662, #201269, #52909, #185026, #128404, #158680, #11340, #96905, #191155, #179204, #194371, #177064, #62245, #125192, #76353, #193304, #161893, #44949, #126263, #143538, #160815, #12406, #127335, #78486, #111057, #113198, #159742, #192220, #178137, #129468, #176009, #195452, #43883, #208468, #10278, #27601, #142460, #60104, #28680, #162956, #109997, #46014, #30828, #93701, #209532, #77421, #42822, #108928, #94767, #61174, #144603, #174949, #146723, #210618, #112134, #29752, #95837, #14534, #63307, #13480, #26531, #79556, #145674, #211671, #80631, #47080, #212741, #92639, #131557, #15598, #2533, #49202, #16663, #48155, #114268, #99014, #184501, #134732, #64376, #51324, #32941, #148821, #213786, #81684, #164023, #35050, #197558, #165071, #147770, #68609, #199681, #83808, #152030, #130522, #182366, #65409, #100070, #82748, #149900, #33996, #31888, #115323, #85955, #133676, #1468, #180264, #67534, #36120, #394, #101121, #150969 ),
 ( #196512, #166132, #66465, #132606, #181313, #117452, #198612, #50259, #102204, #116378, #19870, #17719, #183446, #167209, #18797, #84882, #200739, #52389, #118517, #168270, #97965, #185569, #70735, #103273, #20920, #154163, #24135, #4663, #39337, #40421, #136849, #186644, #87015, #3599, #201805, #21980, #202873, #54521, #53447, #7886, #104347, #169336, #121742, #153087, #106524, #56661, #88090, #119586, #5729, #120666, #38270, #172550, #170391, #71808, #72887, #137919, #203939, #122824, #55587, #187709, #37199, #105434, #171470, #90237, #188785, #69676, #23059, #89176, #155228, #6809, #138994, #205015, #156303, #135782, #165770, #82372, #201431, #118145, #2157, #70363, #197190, #100754, #148462, #18432, #1103, #68234, #166836, #164699, #116008, #4292, #52020, #134367, #32563, #200372, #168955, #17353, #19495, #69297, #180943, #84506, #48828, #49883, #101827, #34685, #20559, #184130, #181994, #86642, #198245, #150595, #151660, #135409, #35753, #114943, #98640, #3231, #33627, #53071, #99700, #85570, #133298, #119204, #67162, #132237, #167895, #199304, #185190, #36814, #16286, #30, #50949, #102896, #117074, #83435, #183073, #152709, #66094, #149517, #23764, #138609, #124567, #171087, #203564, #189475, #38966, #204632, #24830, #55217, #87711, #74663, #121362, #88794, #120287, #186262, #22682, #42183, #206780, #136477, #123511, #105051, #6436, #71434, #153782, #21604, #107227, #187337, #154852, #5352, #140767, #57346, #155920, #9649, #202499, #40037, #137546, #172172, #72512, #7504, #106148, #103974, #56283, #158063, #205712, #73588, #37897, #139690, #108298, #122442, #173250, #8583, #170016, #89869, #54150, #188400, #41117, #90930, #174319, #156996, #58413, #25893, #190527, #92003, #30174, #162315, #62659, #207845, #191588, #96263, #60533, #13901, #142900, #112554, #11776, #79982, #94137, #10710, #128817, #77849, #127775, #12833, #75726, #26959, #143972, #178567, #209965, #76778, #160176, #111492, #177499, #61605, #29112, #193731, #63734, #110429, #208901, #194800, #146085, #126693, #212097, #192655, #159109, #109368, #44307, #93066, #176433, #45376, #113627, #28044, #145029, #129892, #95195, #161247, #78907, #141840, #59470, #211033, #46436, #195877, #125629, #97328, #47515, #179631, #31253, #163384, #43249, #175376, #149256, #147141, #83173, #214203, #32308, #2977, #213167, #130940, #183882, #65834, #35494, #82110, #51770, #165501, #101572, #33364, #164438, #67966, #17094, #66899, #166577, #14958, #180682, #829, #117890, #133039, #16026, #99446, #50686, #116811, #199038, #182812, #34428, #69045, #49618, #148203, #134109, #19241, #131982, #85321, #197990, #98375, #48572, #115743, #181732, #100502, #18164, #52819, #84252, #150338, #135164, #1906, #200118, #167639, #81056, #64796, #151404, #201181, #118957, #196933, #36560, #184936, #102648, #114690, #169770, #156745, #106972, #88542, #86393, #22432, #153534, #186006, #8335, #71179, #170842, #57097, #21360, #120031, #172996, #5103, #121117, #152462, #4042, #203315, #74420, #24577, #168704, #155667, #137298, #38715, #103719, #37641, #53895, #139429, #87467, #54965, #187082, #90684, #89616, #188152, #41938, #20308, #72251, #104795, #204377, #154604, #39784, #138359, #136223, #6183, #190280, #23511, #105889, #70110, #171915, #140519, #56033, #205464, #40867, #202244, #122186 ),
 ( #206533, #7251, #73327, #123263, #189228, #58163, #124321, #143727, #142647, #178329, #63495, #174075, #209720, #208656, #192408, #43005, #177252, #109118, #175132, #145851, #92821, #129650, #158866, #60286, #11534, #94951, #111249, #193495, #125376, #194553, #26720, #126445, #45137, #93892, #195635, #13663, #159931, #160999, #28864, #12591, #78665, #211858, #10462, #144792, #210799, #76536, #77604, #44064, #62422, #61366, #110182, #127524, #128587, #46196, #112314, #29937, #27794, #108050, #25647, #96021, #162073, #59218, #79735, #176193, #91758, #157811, #9410, #75481, #141592, #207598, #191339, #33119, #134906, #116554, #97086, #85059, #2713, #130701, #66638, #181490, #15781, #50435, #99197, #151145, #163139, #18975, #14722, #80813, #98145, #100244, #165248, #47268, #34172, #164194, #132783, #572, #115495, #146904, #81866, #197738, #166312, #147952, #198786, #167385, #16841, #82923, #212923, #32058, #48331, #148996, #183622, #182548, #196692, #179391, #180442, #114441, #17902, #64557, #213965, #68786, #113383, #101305, #83987, #31011, #65585, #150075, #131732, #1647, #67705, #49377, #133853, #199863, #51506, #117631, #35230, #186818, #171641, #204107, #23238, #6980, #120844, #90411, #156481, #38446, #88268, #152203, #154336, #37374, #53629, #73061, #54693, #139160, #104526, #39512, #8070, #170572, #74156, #55759, #36298, #24306, #200912, #69845, #5911, #22153, #169509, #121915, #71985, #52560, #102374, #172728, #168444, #20043, #103449, #105610, #138094, #118692, #187884, #21091, #89350, #155398, #205190, #86130, #87195, #137024, #56831, #153259, #123002, #106704, #188958, #40598, #3771, #185740, #201971, #184676, #135956, #119761, #4834, #70914, #203051, #9148, #143461, #173813, #26459, #112063, #206272, #194300, #209459, #178063, #13408, #61103, #45944, #193233, #110986, #140250, #57896, #76282, #190025, #93627, #127262, #175936, #174879, #210543, #95765, #124060, #27530, #92568, #10207, #75223, #44880, #141334, #207347, #29681, #125123, #161819, #191081, #158610, #43812, #176991, #28609, #11271, #157552, #12333, #58968, #142390, #77349, #126184, #41677, #107788, #192148, #94698, #160739, #78413, #144534, #25392, #42748, #62177, #128336, #108853, #91491, #208399, #60033, #109925, #159669, #65339, #212665, #33928, #131486, #31816, #197491, #50189, #82673, #100003, #17657, #213716, #34985, #145603, #49133, #181241, #30752, #32869, #130452, #146651, #83740, #147698, #149832, #164999, #132545, #211598, #16591, #129397, #327, #195376, #117382, #47008, #162883, #66397, #198543, #48084, #1402, #67463, #113124, #96833, #51258, #14462, #80553, #196440, #114195, #180195, #97892, #15529, #81614, #104280, #186578, #86953, #118450, #201740, #169268, #5661, #69607, #38206, #138926, #4596, #202809, #200671, #3533, #19802, #54457, #155162, #88021, #168203, #150903, #151962, #102134, #21912, #52321, #119516, #204943, #84814, #72822, #154093, #56594, #106459, #71741, #122756, #137855, #203876, #18730, #2464, #20854, #68540, #170325, #55520, #120601, #53381, #89108, #188717, #134669, #121676, #185502, #103206, #85886, #187641, #135714, #37127, #40354, #153021, #184437, #70670, #136780, #39269, #105363, #171400, #22990, #36054, #6744, #107538, #58720, #109681, #158367, #130976, #81087, #9960, #11017, #175684, #93380, #27273, #146118 ),
 ( #25141, #195914, #26208, #113662, #92325, #80015, #196967, #76037, #48604, #159416, #7816, #213201, #172483, #41430, #191899, #142139, #141082, #212131, #208154, #64830, #73909, #147175, #140002, #206023, #8893, #63767, #59784, #24070, #129926, #74972, #43561, #125941, #47551, #57660, #207092, #108604, #179666, #124870, #31285, #90173, #97361, #163419, #123819, #157303, #173570, #14994, #156239, #189779, #91243, #190836, #42496, #174632, #117925, #148236, #871, #86429, #180719, #168740, #183919, #152494, #202279, #35531, #20343, #167674, #85357, #114722, #32343, #50722, #164473, #68005, #101607, #150373, #149290, #184970, #70148, #98409, #1943, #66936, #199076, #49656, #19275, #115779, #181768, #4077, #99480, #136259, #165538, #133078, #18203, #151439, #3010, #200153, #132017, #201217, #33401, #116847, #51807, #100538, #16060, #82144, #166613, #69080, #135200, #52858, #118991, #214238, #17131, #36595, #102682, #83207, #84287, #182848, #65868, #134145, #34467, #198027, #203347, #123296, #55000, #121151, #91790, #38748, #9441, #104830, #6217, #171950, #40898, #57129, #139466, #71214, #140554, #187116, #154636, #205496, #39818, #75512, #174109, #105926, #107003, #189259, #173028, #24610, #157846, #170875, #90718, #156781, #22467, #23539, #88578, #8367, #89648, #72286, #155702, #74450, #206568, #58195, #124353, #188183, #141623, #53932, #7283, #73360, #5138, #190311, #138394, #204412, #41969, #122223, #108080, #25681, #120068, #186044, #37679, #103756, #169805, #21394, #87505, #153569, #137331, #56066, #127560, #176225, #210833, #193528, #31047, #109154, #179426, #43041, #175166, #44098, #46233, #45171, #80850, #194588, #110218, #78700, #161034, #61397, #92854, #27827, #143762, #112350, #93924, #12629, #113420, #111283, #177288, #26753, #192443, #208692, #28903, #129687, #62459, #142681, #125408, #126479, #76570, #128622, #158900, #159964, #97122, #59251, #47306, #178363, #163175, #207632, #29971, #14759, #96056, #162109, #191375, #10497, #209756, #60319, #144826, #13698, #94988, #11570, #63532, #77640, #79771, #145884, #211894, #195670, #1691, #81903, #64595, #65622, #15818, #150118, #180478, #33156, #118729, #212956, #200952, #67745, #184714, #20083, #133895, #52601, #199902, #117672, #146941, #130735, #82961, #196728, #100285, #51548, #182589, #181528, #2755, #102416, #48368, #34212, #99237, #16880, #147991, #183665, #214001, #131771, #36338, #197775, #168484, #49412, #165286, #50474, #35269, #101346, #17942, #164230, #19018, #115533, #149034, #84028, #132825, #114481, #32096, #198829, #167426, #85098, #151183, #68824, #98182, #610, #134946, #66677, #116595, #166351, #4877, #123048, #72025, #38490, #138137, #56872, #89391, #188999, #106745, #5954, #190066, #41718, #204146, #187922, #37415, #39553, #137066, #153301, #172772, #154377, #24346, #55801, #139201, #107828, #121956, #173853, #155439, #135997, #124103, #86171, #169552, #105654, #171682, #54736, #7024, #23279, #152241, #202011, #57938, #53670, #119802, #203091, #205231, #73100, #3813, #40642, #120886, #90456, #156522, #8113, #185781, #186860, #22200, #74201, #104568, #140295, #206314, #69885, #103491, #21133, #70956, #87237, #170613, #88313, #211639, #26499, #77387, #194340, #112103, #12374, #157594, #141374, #45982, #10247, #178106, #92606, #62216, #175977, #29722 ),
 ( #145644, #11309, #78454, #28648, #160781, #177031, #63275, #158649, #210586, #128373, #208437, #143503, #76323, #95804, #209500, #192188, #61140, #161860, #94735, #13450, #79526, #159710, #129437, #195420, #127302, #193273, #191121, #44918, #142428, #60071, #47050, #93668, #113166, #111026, #144572, #25429, #91535, #9189, #75260, #207385, #59006, #125162, #108896, #42787, #174919, #126227, #43852, #109966, #27570, #172245, #28113, #106219, #23832, #107297, #109441, #190597, #144046, #43322, #173320, #141906, #9724, #124640, #155990, #24899, #206852, #175447, #91005, #75799, #176502, #42254, #25969, #89938, #41190, #57417, #92075, #192725, #125698, #205787, #188478, #189542, #139761, #59538, #7577, #157067, #94207, #122515, #110502, #191658, #160247, #56352, #27031, #11848, #93140, #159177, #40108, #73662, #58484, #123580, #207918, #10778, #158132, #8656, #76852, #77926, #108368, #142971, #74735, #140840, #174392, #208973, #44379, #60608, #126767, #127850, #128894, #78988, #213242, #29186, #96340, #181811, #61681, #49695, #64872, #33443, #83246, #131017, #115823, #48645, #180759, #210042, #193801, #146159, #45449, #163459, #197009, #31327, #30255, #65910, #165578, #111565, #97403, #162396, #80058, #145105, #114763, #211110, #62735, #99519, #194876, #17172, #46511, #13972, #113705, #32387, #98452, #81130, #12908, #82185, #112634, #212175, #147216, #195956, #177573, #95276, #47591, #164516, #16101, #148278, #214277, #161324, #178644, #132057, #198067, #63809, #179710, #129969, #15038, #50759, #199115, #116888, #34504, #182887, #100577, #166650, #18241, #149331, #911, #66979, #133117, #90155, #92306, #189759, #41412, #159399, #190817, #77075, #42478, #43543, #94430, #108587, #12076, #59765, #40335, #176721, #160469, #139984, #158350, #174615, #173549, #125925, #26191, #28333, #106441, #110721, #172464, #24052, #25123, #27255, #10998, #204926, #143203, #8876, #209193, #60833, #126994, #74955, #192953, #44605, #180718, #128853, #177532, #53931, #120067, #186043, #37678, #103755, #76569, #58194, #22466, #10496, #54999, #56065, #206567, #123295, #155701, #190310, #24609, #187115, #154635, #6216, #105925, #139465, #205495, #41968, #91789, #157845, #75511, #59250, #109153, #79770, #62458, #27826, #111282, #78699, #129686, #45170, #211893, #48367, #128621, #29970, #110217, #127559, #143761, #47305, #130734, #113419, #77639, #126478, #177287, #11569, #31046, #176224, #28902, #114480, #208691, #196727, #163174, #32095, #15817, #98181, #164229, #142680, #192442, #44097, #94987, #194587, #161033, #12628, #71761, #117671, #116594, #155184, #40377, #147990, #183664, #182588, #166350, #16879, #154114, #82960, #149033, #122778, #66676, #106479, #132824, #34211, #199901, #137877, #88043, #170348, #99236, #171425, #609, #100284, #21933, #67744, #172506, #204967, #133894, #203898, #5684, #55543, #121697, #188738, #198828, #187662, #39290, #50473, #51547, #17941, #105385, #35268, #84027, #101345, #23012, #89129, #6767, #72842, #1690, #81902, #214000, #138946, #56614, #33155, #65621, #150117, #131770, #197774, #49411, #115532, #181527, #165285, #92345, #176757, #158385, #77114, #194062, #9980, #111833, #93401, #73929, #61945, #45715, #107560, #43583, #76058, #207117, #27294, #142157, #128104, #140021, #210309, #206047, #57683, #74997, #143238, #208173 ) ),
 .UNSPECIFIED., .T., .F., .T. ) 
 B_SPLINE_SURFACE_WITH_KNOTS ( ( 4, 3, 4 ),
 ( 4, 1, 1, 1, 1, 1, 1, 1, 1, 1, 1, 1, 1, 1, 1, 1, 1, 1, 1, 1, 1, 1, 1, 1, 1, 1, 1, 1, 1, 1, 1, 1, 1, 1, 1, 1, 1, 1, 1, 1, 1, 1, 1, 1, 1, 1, 1, 1, 1, 1, 1, 1, 1, 1, 1, 1, 1, 1, 1, 1, 1, 1, 1, 1, 1, 1, 1, 1, 1, 1, 1, 1, 1, 1, 1, 1, 1, 1, 1, 1, 1, 1, 1, 1, 1, 1, 1, 1, 1, 1, 1, 1, 1, 1, 1, 1, 1, 1, 1, 1, 1, 1, 1, 1, 1, 1, 1, 1, 1, 1, 1, 1, 1, 1, 1, 1, 1, 1, 1, 1, 1, 1, 1, 1, 1, 1, 1, 1, 1, 1, 1, 1, 1, 1, 1, 1, 1, 1, 1, 1, 1, 1, 1, 1, 1, 1, 1, 1, 1, 1, 1, 1, 1, 1, 1, 1, 1, 1, 1, 1, 1, 1, 1, 1, 1, 1, 1, 1, 1, 1, 1, 1, 1, 1, 1, 1, 1, 1, 1, 1, 1, 1, 1, 1, 1, 1, 1, 1, 1, 1, 1, 1, 1, 1, 1, 1, 1, 1, 1, 1, 1, 1, 1, 1, 1, 1, 1, 1, 1, 1, 1, 1, 1, 1, 1, 1, 1, 1, 1, 1, 1, 1, 1, 1, 1, 1, 1, 1, 1, 1, 1, 1, 1, 1, 1, 1, 1, 1, 1, 1, 1, 1, 1, 1, 1, 1, 1, 1, 1, 1, 1, 1, 1, 1, 1, 1, 1, 1, 1, 1, 1, 1, 1, 1, 1, 1, 1, 1, 1, 1, 1, 1, 1, 1, 1, 1, 1, 1, 1, 1, 1, 1, 1, 1, 1, 1, 1, 1, 1, 1, 1, 1, 1, 1, 1, 1, 1, 1, 1, 1, 1, 1, 1, 1, 1, 1, 1, 1, 1, 1, 1, 1, 1, 1, 1, 1, 1, 1, 1, 1, 1, 1, 1, 1, 1, 1, 1, 1, 1, 1, 1, 1, 1, 1, 1, 1, 1, 1, 1, 1, 1, 1, 1, 1, 1, 1, 1, 1, 1, 1, 1, 1, 1, 1, 1, 1, 1, 1, 1, 1, 1, 1, 1, 1, 1, 1, 1, 1, 1, 1, 1, 1, 1, 1, 1, 1, 1, 1, 1, 1, 1, 1, 1, 1, 4 ),
 ( 0.000000000000000000, 0.5000000000000000000, 1.000000000000000000 ),
 ( 0.000000000000000000, 0.002599942752653872004, 0.005208763852970823248, 0.007813103504395044890, 0.01041666580238601383, 0.01302040446826325734, 0.01562503794709516405, 0.01822898659850798186, 0.02083325479626091381, 0.02343751936515397344, 0.02604147156932860516, 0.02864593660736421826, 0.03124971754428982826, 0.03385421962853985695, 0.03645805019290717514, 0.03906245553539786086, 0.04166655880408994678, 0.04427067902208449424, 0.04687506736766395427, 0.04947890482860387018, 0.05208340383233839299, 0.05468718329397467132, 0.05729165635893663372, 0.05989559287350183087, 0.06249988401580178210, 0.06510415622071820396, 0.06770810475871495704, 0.07031256650665723695, 0.07291634835701975292, 0.07552085129243907291, 0.07812468146351797538, 0.08072908640827750060, 0.08333318980393969455, 0.08593730989448074287, 0.08854169822802662737, 0.09114553558425014801, 0.09375003453682481669, 0.09635381396055957282, 0.09895828689139142542, 0.1015622234206122604, 0.1041665143989399522, 0.1067707866525781646, 0.1093747350801187734, 0.1119791968332524285, 0.1145829786367304204, 0.1171874814968899975, 0.1197913116783300008, 0.1223957164865987768, 0.1249998199429257079, 0.1276039399106482508, 0.1302083283009266290, 0.1328121656006459317, 0.1354166645410730119, 0.1380204439687620910, 0.1406249168095159707, 0.1432288533966223909, 0.1458331442541831724, 0.1484374165996726891, 0.1510413649597071029, 0.1536458267615184170, 0.1562496085608837959, 0.1588541113892728840, 0.1614579416238982879, 0.1640623463390579739, 0.1666664498991252963, 0.1692705697871219883, 0.1718749582774928841, 0.1744787955635339893, 0.1770832945353020271, 0.1796870740097127606, 0.1822915468038420750, 0.1848954834917516388, 0.1874997742717963711, 0.1901040467523684718, 0.1927079950878241021, 0.1953124569817516476, 0.1979162388197689970, 0.2005207416598733527, 0.2031245719904950509, 0.2057289766559125821, 0.2083330803627857220, 0.2109372002141371993, 0.2135415888479497148, 0.2161454261631269858, 0.2187499252097131475, 0.2213537047736018060, 0.2239581775645482220, 0.2265621143961681627, 0.2291664051419355919, 0.2317706778008114532, 0.2343746261546043874, 0.2369790881840763974, 0.2395828701034999064, 0.2421873729987945312, 0.2447912034682135918, 0.2473956081272447038, 0.2499997120239797754, 0.2526038318817556694, 0.2552082207023498306, 0.2578120580894675551, 0.2604165572543392093, 0.2630203369504529598, 0.2656248097816475973, 0.2682287467998764607, 0.2708330375545950908, 0.2734373104349877015, 0.2760412588500244513, 0.2786457210584605826, 0.2812495031020356140, 0.2838540060959860445, 0.2864578367469951536, 0.2890622414429859233, 0.2916663455726313803, 0.2942704654798921071, 0.2968748545306000852, 0.2994786920324540302, 0.3020831913590704687, 0.3046869712301484290, 0.3072914441450140810, 0.3098953813927431966, 0.3124996721996327054, 0.3151039453447485039, 0.3177078938639273376, 0.3203123562947402525, 0.3229161385052047861, 0.3255206416412691484, 0.3281244725166545528, 0.3307288772929431464, 0.3333329816985414751, 0.3359371016983396796, 0.3385414910224879836, 0.3411453286818670882, 0.3437498282136811634, 0.3463536083024566503, 0.3489580813444087548, 0.3515620188645239841, 0.3541663097667969717, 0.3567705832198370119, 0.3593745318860498972, 0.3619789945826469846, 0.3645827770027332826, 0.3671872803243637073, 0.3697911114669067967, 0.3723955163668249413, 0.3749996210914142147, 0.3776037412267966853, 0.3802081308677072724, 0.3828119687273952576, 0.3854164685078552144, 0.3880202488570567709, 0.3906247220695055478, 0.3932286599048890885, 0.3958329509457525486, 0.3984372247499146091, 0.4010411736060487398, 0.4036456366118335581, 0.4062494192842699414, 0.4088539228349143406, 0.4114577542873927851, 0.4140621593542673784, 0.4166662644408827831, 0.4192703847548917562, 0.4218747747558840855, 0.4244786128586610641, 0.4270831129312115948, 0.4296868935835649328, 0.4322913670099168826, 0.4348953052034483235, 0.4374995964261053638, 0.4401038706245853915, 0.4427078197135246862, 0.4453122830718987402, 0.4479160660394111426, 0.4505205698625146526, 0.4531244016677045128, 0.4557288069448597878, 0.4583329124365353446, 0.4609370329722101700, 0.4635414233766025904, 0.4661452617652466213, 0.4687497621733308639, 0.4713535431715604185, 0.4739580168552197104, 0.4765619554497781962, 0.4791662468974299260, 0.4817705215334236457, 0.4843744708980504132, 0.4869789346524148743, 0.4895827179577280641, 0.4921872220967347111, 0.4947910542974118808, 0.4973954598281701278, 0.4999995657679404681, 0.5026036865683194410, 0.5052080774194306345, 0.5078119161367193879, 0.5104164169237808135, 0.5130201983106112973, 0.5156246722949818784, 0.5182286113334474420, 0.5208329030492938605, 0.5234371781659985512, 0.5260411278491948783, 0.5286455920429519173, 0.5312493757287917173, 0.5338538802271461936, 0.5364577128660878991, 0.5390621186937718523, 0.5416662251246735504, 0.5442703462327953545, 0.5468747375739465566, 0.5494785766626585355, 0.5520830778721422805, 0.5546868596903002935, 0.5572913340187868325, 0.5598952735440421158, 0.5624995655712847764, 0.5651038412119004928, 0.5677077912565504647, 0.5703122559331050834, 0.5729160400421993149, 0.5755205449433484777, 0.5781243780633351648, 0.5807287842312690573, 0.5833328911963423513, 0.5859370126552478908, 0.5885414045297637786, 0.5911452440326808722, 0.5937497457080352925, 0.5963535280002507655, 0.5989580027162609843, 0.6015619427711926814, 0.6041662351530351360, 0.6067705113607667622, 0.6093744618097575172, 0.6119789270125192138, 0.6145827115875999169, 0.6171872169349945647, 0.6197910505788110092, 0.6223954571303226269, 0.6249995646726131948, 0.6276036865253464825, 0.6302080789765573954, 0.6328119189364656005, 0.6354164211211439373, 0.6380202039301521300, 0.6406246790770983024, 0.6432286197045988807, 0.6458329124842493441, 0.6484371893023079814, 0.6510411401985315427, 0.6536456059709156996, 0.6562493910547204656, 0.6588538968918166150, 0.6614577311022542538, 0.6640621380806766005, 0.6666662462432366709, 0.6692703685328477148, 0.6718747616040910975, 0.6744786020637821844, 0.6770831048012443398, 0.6796868881697873954, 0.6822913637910873463, 0.6848953050340567117, 0.6874995982547292828, 0.6901038757263339152, 0.6927078271126885234, 0.6953122934981186276, 0.6979160791333920422, 0.7005205855036529261, 0.7031244203235108570, 0.7057288277721832648, 0.7083329365980738368, 0.7109370593676189731, 0.7135414531022405971, 0.7161452941045143294, 0.7187497974382286436, 0.7213535814090563658, 0.7239580575481356917, 0.7265619994494829648, 0.7291662931543987369, 0.7317705713227778963, 0.7343745232421703406, 0.7369789902840787610, 0.7395827765135741805, 0.7421872834604720248, 0.7447911189325585601, 0.7473955268948287989, 0.7499996364271210858, 0.7526037597196653106, 0.7552081541610216053, 0.7578119957486867397, 0.7604164997221309896, 0.7630202843380037292, 0.7656247610382975743, 0.7682287036409420899, 0.7708329978733315935, 0.7734372767817252470, 0.7760412292770711984, 0.7786456970189011839, 0.7812494838853828449, 0.7838539914523996455, 0.7864578276195345330, 0.7890622361387605865, 0.7916663464205372369, 0.7942704702791556493, 0.7968748654706151457, 0.7994787076864910969, 0.8020832123431549388, 0.8046869976468442598, 0.8072914749517984268, 0.8098954182986718431, 0.8124997131017763774, 0.8151039927934364826, 0.8177079459076636025, 0.8203124143928716139, 0.8229162019391148553, 0.8255207101697450423, 0.8281245470747605752, 0.8307289561943111966, 0.8333330672686687368, 0.8359371917364484261, 0.8385415877213925340, 0.8411454306083117061, 0.8437499359916976749, 0.8463537220259882421, 0.8489581999790609679, 0.8515621441131088210, 0.8541664395301816759, 0.8567707200483754004, 0.8593746738244238959, 0.8619791430964799384, 0.8645829313652741988, 0.8671874403030259693, 0.8697912779887684298, 0.8723956877520262498, 0.8749997996620757501, 0.8776039247821166844, 0.8802083216039426894, 0.8828121652047509205, 0.8854166713583762061, 0.8880204581660676721, 0.8906249368107317377, 0.8932288817749149956, 0.8958331778492237829, 0.8984374592372342816, 0.9010414137180589034, 0.9036458838204490807, 0.9062496728545991198, 0.9088541825429954368, 0.9114580210523274273, 0.9140624315026897317, 0.9166665442915585826, 0.9192706701069754960, 0.9218750678090992245, 0.9244789121666602272, 0.9270834191340497910, 0.9296872067579531329, 0.9322916861377325004, 0.9348956319750387767, 0.9374999287497546296, 0.9401042110508202043, 0.9427081662796877870, 0.9453126372565492375, 0.9479164270979697493, 0.9505209375757615042, 0.9531247769568838013, 0.9557291881641908349, 0.9583333018366511080, 0.9609374282806871781, 0.9635418271385329803, 0.9661456726567504427, 0.9687501794391485399, 0.9713539669241311181, 0.9739584505366999378, 0.9765624007674321705, 0.9791666904763859369, 0.9817709514985233366, 0.9843749191276834898, 0.9869795472165283634, 0.9895832986789295793, 0.9921868791097946394, 0.9947912178632822844, 0.9974000636350187632, 1.000000000000000000 ),
 .UNSPECIFIED. ) 
 GEOMETRIC_REPRESENTATION_ITEM ( )  RATIONAL_B_SPLINE_SURFACE ( (
 ( 1.000000000000000222, 1.000000000000000222, 1.000000000000000444, 1.000000000000000000, 1.000000000000000444, 1.000000000000000222, 1.000000000000000444, 0.9999999999999997780, 1.000000000000000444, 1.000000000000000000, 1.000000000000000444, 1.000000000000000000, 1.000000000000000444, 1.000000000000000222, 1.000000000000000000, 1.000000000000000666, 0.9999999999999997780, 1.000000000000000444, 1.000000000000000444, 1.000000000000000444, 1.000000000000000222, 1.000000000000000222, 1.000000000000000444, 1.000000000000000444, 1.000000000000000000, 1.000000000000000222, 1.000000000000000222, 1.000000000000000444, 1.000000000000000222, 1.000000000000000444, 1.000000000000000000, 1.000000000000000222, 1.000000000000000444, 1.000000000000000000, 1.000000000000000444, 1.000000000000000222, 1.000000000000000444, 1.000000000000000444, 1.000000000000000222, 1.000000000000000000, 1.000000000000000444, 1.000000000000000222, 1.000000000000000000, 1.000000000000000222, 1.000000000000000444, 1.000000000000000444, 1.000000000000000444, 1.000000000000000444, 1.000000000000000222, 1.000000000000000444, 1.000000000000000000, 1.000000000000000444, 1.000000000000000222, 1.000000000000000222, 1.000000000000000444, 1.000000000000000000, 1.000000000000000222, 1.000000000000000444, 1.000000000000000222, 1.000000000000000000, 1.000000000000000444, 1.000000000000000222, 1.000000000000000222, 1.000000000000000000, 1.000000000000000444, 0.9999999999999997780, 1.000000000000000444, 1.000000000000000000, 1.000000000000000444, 1.000000000000000000, 1.000000000000000444, 0.9999999999999997780, 1.000000000000000222, 1.000000000000000444, 1.000000000000000444, 1.000000000000000000, 1.000000000000000444, 1.000000000000000222, 1.000000000000000000, 1.000000000000000666, 1.000000000000000000, 1.000000000000000444, 1.000000000000000222, 1.000000000000000444, 0.9999999999999997780, 1.000000000000000444, 1.000000000000000000, 1.000000000000000444, 1.000000000000000444, 1.000000000000000222, 1.000000000000000222, 1.000000000000000444, 1.000000000000000222, 1.000000000000000444, 1.000000000000000444, 1.000000000000000222, 1.000000000000000444, 1.000000000000000222, 1.000000000000000444, 1.000000000000000000, 1.000000000000000444, 1.000000000000000000, 1.000000000000000000, 1.000000000000000444, 1.000000000000000222, 1.000000000000000222, 1.000000000000000444, 1.000000000000000000, 1.000000000000000444, 1.000000000000000000, 1.000000000000000222, 1.000000000000000444, 0.9999999999999997780, 1.000000000000000444, 1.000000000000000222, 1.000000000000000444, 1.000000000000000000, 1.000000000000000444, 1.000000000000000000, 1.000000000000000222, 1.000000000000000222, 1.000000000000000444, 1.000000000000000222, 1.000000000000000000, 1.000000000000000444, 1.000000000000000222, 1.000000000000000222, 1.000000000000000222, 1.000000000000000444, 0.9999999999999997780, 1.000000000000000666, 0.9999999999999996669, 1.000000000000000444, 1.000000000000000444, 1.000000000000000222, 1.000000000000000444, 1.000000000000000444, 1.000000000000000222, 1.000000000000000000, 1.000000000000000444, 1.000000000000000000, 1.000000000000000444, 1.000000000000000222, 1.000000000000000444, 1.000000000000000000, 1.000000000000000444, 1.000000000000000222, 1.000000000000000222, 1.000000000000000444, 1.000000000000000222, 0.9999999999999997780, 1.000000000000000444, 1.000000000000000444, 1.000000000000000444, 1.000000000000000222, 1.000000000000000444, 1.000000000000000444, 1.000000000000000222, 1.000000000000000444, 1.000000000000000000, 1.000000000000000222, 1.000000000000000444, 1.000000000000000000, 1.000000000000000222, 1.000000000000000444, 1.000000000000000000, 1.000000000000000444, 0.9999999999999997780, 1.000000000000000222, 1.000000000000000444, 1.000000000000000000, 1.000000000000000222, 1.000000000000000222, 1.000000000000000444, 1.000000000000000000, 1.000000000000000666, 0.9999999999999996669, 1.000000000000000666, 1.000000000000000222, 1.000000000000000444, 1.000000000000000222, 1.000000000000000444, 1.000000000000000222, 1.000000000000000222, 1.000000000000000000, 1.000000000000000444, 0.9999999999999997780, 1.000000000000000444, 1.000000000000000222, 1.000000000000000444, 0.9999999999999997780, 1.000000000000000444, 1.000000000000000000, 1.000000000000000222, 1.000000000000000444, 1.000000000000000000, 1.000000000000000444, 1.000000000000000444, 1.000000000000000222, 1.000000000000000222, 1.000000000000000000, 1.000000000000000444, 1.000000000000000444, 1.000000000000000000, 1.000000000000000222, 1.000000000000000222, 1.000000000000000444, 1.000000000000000222, 1.000000000000000222, 1.000000000000000444, 1.000000000000000222, 1.000000000000000000, 1.000000000000000444, 1.000000000000000000, 1.000000000000000222, 1.000000000000000444, 1.000000000000000222, 1.000000000000000222, 1.000000000000000444, 1.000000000000000000, 1.000000000000000222, 1.000000000000000222, 1.000000000000000222, 1.000000000000000000, 1.000000000000000222, 1.000000000000000222, 1.000000000000000000, 1.000000000000000222, 1.000000000000000222, 1.000000000000000444, 1.000000000000000000, 1.000000000000000000, 1.000000000000000222, 1.000000000000000000, 1.000000000000000888, 1.000000000000000000, 1.000000000000000444, 1.000000000000000222, 1.000000000000000222, 1.000000000000000444, 1.000000000000000222, 1.000000000000000222, 1.000000000000000444, 1.000000000000000444, 1.000000000000000222, 1.000000000000000444, 1.000000000000000222, 1.000000000000000000, 1.000000000000000222, 1.000000000000000444, 1.000000000000000444, 1.000000000000000222, 1.000000000000000444, 1.000000000000000222, 1.000000000000000444, 1.000000000000000222, 1.000000000000000444, 1.000000000000000222, 1.000000000000000000, 1.000000000000000444, 1.000000000000000000, 1.000000000000000666, 1.000000000000000000, 1.000000000000000000, 1.000000000000000444, 1.000000000000000222, 1.000000000000000444, 0.9999999999999997780, 1.000000000000000666, 1.000000000000000222, 1.000000000000000444, 1.000000000000000222, 1.000000000000000444, 1.000000000000000222, 1.000000000000000444, 0.9999999999999997780, 1.000000000000000666, 1.000000000000000222, 1.000000000000000222, 1.000000000000000444, 1.000000000000000444, 0.9999999999999997780, 1.000000000000000444, 1.000000000000000222, 1.000000000000000222, 1.000000000000000000, 1.000000000000000000, 1.000000000000000444, 1.000000000000000444, 1.000000000000000222, 1.000000000000000000, 1.000000000000000444, 0.9999999999999997780, 1.000000000000000444, 1.000000000000000222, 1.000000000000000000, 1.000000000000000222, 1.000000000000000000, 1.000000000000000444, 1.000000000000000000, 1.000000000000000444, 1.000000000000000222, 1.000000000000000222, 1.000000000000000222, 1.000000000000000222, 1.000000000000000222, 1.000000000000000444, 1.000000000000000222, 1.000000000000000444, 1.000000000000000222, 1.000000000000000000, 1.000000000000000888, 0.9999999999999996669, 1.000000000000000444, 1.000000000000000444, 1.000000000000000222, 1.000000000000000444, 1.000000000000000000, 1.000000000000000444, 0.9999999999999997780, 1.000000000000000444, 1.000000000000000222, 1.000000000000000444, 0.9999999999999997780, 1.000000000000000222, 1.000000000000000222, 1.000000000000000444, 1.000000000000000000, 1.000000000000000444, 1.000000000000000444, 1.000000000000000222, 1.000000000000000000, 1.000000000000000444, 1.000000000000000000, 1.000000000000000222, 1.000000000000000222, 1.000000000000000444, 1.000000000000000000, 1.000000000000000666, 1.000000000000000000, 1.000000000000000444, 1.000000000000000222, 1.000000000000000444, 1.000000000000000222, 1.000000000000000444, 1.000000000000000222, 1.000000000000000222, 1.000000000000000222, 1.000000000000000444, 1.000000000000000444, 1.000000000000000222, 1.000000000000000000, 1.000000000000000444, 1.000000000000000444, 1.000000000000000000, 1.000000000000000444, 0.9999999999999997780, 1.000000000000000444, 1.000000000000000222, 1.000000000000000222, 1.000000000000000444, 1.000000000000000222, 1.000000000000000222, 1.000000000000000444, 1.000000000000000444, 1.000000000000000444, 1.000000000000000000, 1.000000000000000444, 1.000000000000000222, 1.000000000000000222, 1.000000000000000000, 1.000000000000000444, 0.9999999999999997780, 1.000000000000000444, 1.000000000000000000, 1.000000000000000444, 1.000000000000000000, 1.000000000000000444, 1.000000000000000222, 1.000000000000000000, 1.000000000000000444, 1.000000000000000222, 1.000000000000000444, 0.9999999999999997780, 1.000000000000000444, 1.000000000000000222, 1.000000000000000222),
 ( 0.3333333333333334259, 0.3333333333333334259, 0.3333333333333334814, 0.3333333333333333703, 0.3333333333333335369, 0.3333333333333334259, 0.3333333333333334814, 0.3333333333333333703, 0.3333333333333334259, 0.3333333333333333703, 0.3333333333333335369, 0.3333333333333333703, 0.3333333333333334259, 0.3333333333333334259, 0.3333333333333333703, 0.3333333333333335369, 0.3333333333333333703, 0.3333333333333334259, 0.3333333333333335369, 0.3333333333333334259, 0.3333333333333333703, 0.3333333333333334259, 0.3333333333333334814, 0.3333333333333335369, 0.3333333333333333148, 0.3333333333333334259, 0.3333333333333334259, 0.3333333333333334814, 0.3333333333333334259, 0.3333333333333334259, 0.3333333333333334259, 0.3333333333333333148, 0.3333333333333335924, 0.3333333333333333148, 0.3333333333333335369, 0.3333333333333333703, 0.3333333333333335369, 0.3333333333333334259, 0.3333333333333333703, 0.3333333333333333703, 0.3333333333333335924, 0.3333333333333333148, 0.3333333333333334259, 0.3333333333333334259, 0.3333333333333335369, 0.3333333333333334814, 0.3333333333333334259, 0.3333333333333334259, 0.3333333333333334259, 0.3333333333333334259, 0.3333333333333333703, 0.3333333333333335369, 0.3333333333333334259, 0.3333333333333334259, 0.3333333333333334814, 0.3333333333333333703, 0.3333333333333333703, 0.3333333333333334814, 0.3333333333333334259, 0.3333333333333333703, 0.3333333333333334814, 0.3333333333333333703, 0.3333333333333334814, 0.3333333333333332593, 0.3333333333333335924, 0.3333333333333333148, 0.3333333333333335924, 0.3333333333333333148, 0.3333333333333335924, 0.3333333333333334259, 0.3333333333333334814, 0.3333333333333333703, 0.3333333333333333703, 0.3333333333333334814, 0.3333333333333335369, 0.3333333333333333703, 0.3333333333333334814, 0.3333333333333334259, 0.3333333333333333703, 0.3333333333333335369, 0.3333333333333333148, 0.3333333333333335369, 0.3333333333333334259, 0.3333333333333334259, 0.3333333333333333703, 0.3333333333333334259, 0.3333333333333333703, 0.3333333333333335369, 0.3333333333333333703, 0.3333333333333334259, 0.3333333333333334259, 0.3333333333333334814, 0.3333333333333333703, 0.3333333333333335924, 0.3333333333333333703, 0.3333333333333334259, 0.3333333333333334814, 0.3333333333333334259, 0.3333333333333335369, 0.3333333333333333148, 0.3333333333333335369, 0.3333333333333333148, 0.3333333333333334259, 0.3333333333333333703, 0.3333333333333334259, 0.3333333333333334259, 0.3333333333333335924, 0.3333333333333333703, 0.3333333333333335924, 0.3333333333333333148, 0.3333333333333335369, 0.3333333333333335369, 0.3333333333333333148, 0.3333333333333334259, 0.3333333333333334259, 0.3333333333333334814, 0.3333333333333333703, 0.3333333333333335369, 0.3333333333333333703, 0.3333333333333333703, 0.3333333333333334814, 0.3333333333333334814, 0.3333333333333334259, 0.3333333333333333703, 0.3333333333333334814, 0.3333333333333334814, 0.3333333333333334259, 0.3333333333333334259, 0.3333333333333334259, 0.3333333333333333703, 0.3333333333333335369, 0.3333333333333333703, 0.3333333333333334259, 0.3333333333333334814, 0.3333333333333334259, 0.3333333333333334814, 0.3333333333333334259, 0.3333333333333333703, 0.3333333333333333703, 0.3333333333333334259, 0.3333333333333333148, 0.3333333333333334814, 0.3333333333333334814, 0.3333333333333334259, 0.3333333333333333703, 0.3333333333333334259, 0.3333333333333334259, 0.3333333333333333703, 0.3333333333333335369, 0.3333333333333334259, 0.3333333333333333148, 0.3333333333333333703, 0.3333333333333335369, 0.3333333333333335369, 0.3333333333333333148, 0.3333333333333335369, 0.3333333333333334259, 0.3333333333333334259, 0.3333333333333335369, 0.3333333333333333703, 0.3333333333333333703, 0.3333333333333334259, 0.3333333333333333703, 0.3333333333333334259, 0.3333333333333334259, 0.3333333333333333703, 0.3333333333333335369, 0.3333333333333333703, 0.3333333333333334259, 0.3333333333333335369, 0.3333333333333333703, 0.3333333333333333703, 0.3333333333333334814, 0.3333333333333334259, 0.3333333333333333703, 0.3333333333333335369, 0.3333333333333332593, 0.3333333333333335369, 0.3333333333333335369, 0.3333333333333333703, 0.3333333333333334814, 0.3333333333333334814, 0.3333333333333334259, 0.3333333333333333703, 0.3333333333333334259, 0.3333333333333334814, 0.3333333333333333148, 0.3333333333333335369, 0.3333333333333333703, 0.3333333333333334259, 0.3333333333333333703, 0.3333333333333334259, 0.3333333333333333148, 0.3333333333333334259, 0.3333333333333334814, 0.3333333333333333703, 0.3333333333333334814, 0.3333333333333334259, 0.3333333333333333703, 0.3333333333333334259, 0.3333333333333333703, 0.3333333333333334259, 0.3333333333333334814, 0.3333333333333332593, 0.3333333333333334259, 0.3333333333333333703, 0.3333333333333335369, 0.3333333333333334259, 0.3333333333333333703, 0.3333333333333334259, 0.3333333333333334259, 0.3333333333333333148, 0.3333333333333335369, 0.3333333333333333703, 0.3333333333333334259, 0.3333333333333335924, 0.3333333333333333703, 0.3333333333333334259, 0.3333333333333335369, 0.3333333333333333703, 0.3333333333333334259, 0.3333333333333334259, 0.3333333333333334259, 0.3333333333333333703, 0.3333333333333334259, 0.3333333333333334259, 0.3333333333333333703, 0.3333333333333333148, 0.3333333333333334814, 0.3333333333333334259, 0.3333333333333334259, 0.3333333333333333703, 0.3333333333333333703, 0.3333333333333334259, 0.3333333333333335369, 0.3333333333333333703, 0.3333333333333335369, 0.3333333333333333703, 0.3333333333333334259, 0.3333333333333335369, 0.3333333333333333148, 0.3333333333333334259, 0.3333333333333334814, 0.3333333333333335369, 0.3333333333333333148, 0.3333333333333335369, 0.3333333333333333703, 0.3333333333333334259, 0.3333333333333333703, 0.3333333333333335369, 0.3333333333333334259, 0.3333333333333334259, 0.3333333333333334259, 0.3333333333333333703, 0.3333333333333335924, 0.3333333333333334259, 0.3333333333333335369, 0.3333333333333333148, 0.3333333333333333703, 0.3333333333333334814, 0.3333333333333333703, 0.3333333333333335924, 0.3333333333333333148, 0.3333333333333333703, 0.3333333333333335369, 0.3333333333333333703, 0.3333333333333335924, 0.3333333333333332593, 0.3333333333333335924, 0.3333333333333334259, 0.3333333333333335369, 0.3333333333333334259, 0.3333333333333334814, 0.3333333333333333703, 0.3333333333333334814, 0.3333333333333333148, 0.3333333333333335369, 0.3333333333333333148, 0.3333333333333334814, 0.3333333333333334814, 0.3333333333333334814, 0.3333333333333333148, 0.3333333333333335369, 0.3333333333333333148, 0.3333333333333335369, 0.3333333333333333703, 0.3333333333333333703, 0.3333333333333335369, 0.3333333333333334259, 0.3333333333333334259, 0.3333333333333333703, 0.3333333333333335369, 0.3333333333333333148, 0.3333333333333335924, 0.3333333333333334259, 0.3333333333333334259, 0.3333333333333333703, 0.3333333333333333703, 0.3333333333333334259, 0.3333333333333334259, 0.3333333333333334259, 0.3333333333333334259, 0.3333333333333334259, 0.3333333333333334259, 0.3333333333333334259, 0.3333333333333333703, 0.3333333333333335369, 0.3333333333333333703, 0.3333333333333334814, 0.3333333333333333703, 0.3333333333333333148, 0.3333333333333337034, 0.3333333333333332038, 0.3333333333333334814, 0.3333333333333335369, 0.3333333333333334814, 0.3333333333333334259, 0.3333333333333334259, 0.3333333333333334814, 0.3333333333333333703, 0.3333333333333334814, 0.3333333333333334259, 0.3333333333333334814, 0.3333333333333333148, 0.3333333333333333703, 0.3333333333333335369, 0.3333333333333334259, 0.3333333333333333703, 0.3333333333333335369, 0.3333333333333334814, 0.3333333333333334259, 0.3333333333333333703, 0.3333333333333334259, 0.3333333333333333148, 0.3333333333333335369, 0.3333333333333333148, 0.3333333333333335369, 0.3333333333333333703, 0.3333333333333335369, 0.3333333333333334259, 0.3333333333333334814, 0.3333333333333334259, 0.3333333333333335369, 0.3333333333333334259, 0.3333333333333334259, 0.3333333333333333703, 0.3333333333333334259, 0.3333333333333333703, 0.3333333333333335369, 0.3333333333333334814, 0.3333333333333333703, 0.3333333333333333148, 0.3333333333333335369, 0.3333333333333333703, 0.3333333333333333703, 0.3333333333333334814, 0.3333333333333333148, 0.3333333333333334814, 0.3333333333333333703, 0.3333333333333334259, 0.3333333333333334814, 0.3333333333333334814, 0.3333333333333334259, 0.3333333333333334259, 0.3333333333333335369, 0.3333333333333334814, 0.3333333333333333148, 0.3333333333333335369, 0.3333333333333334259, 0.3333333333333333703, 0.3333333333333334259, 0.3333333333333334259, 0.3333333333333333148, 0.3333333333333334814, 0.3333333333333333703, 0.3333333333333334259, 0.3333333333333333148, 0.3333333333333334814, 0.3333333333333334259, 0.3333333333333333148, 0.3333333333333334814, 0.3333333333333334259, 0.3333333333333334814, 0.3333333333333332593, 0.3333333333333335924, 0.3333333333333334259, 0.3333333333333334259),
 ( 0.3333333333333334259, 0.3333333333333334259, 0.3333333333333334814, 0.3333333333333333703, 0.3333333333333335369, 0.3333333333333334259, 0.3333333333333334814, 0.3333333333333333703, 0.3333333333333334259, 0.3333333333333333703, 0.3333333333333335369, 0.3333333333333333703, 0.3333333333333334259, 0.3333333333333334259, 0.3333333333333333703, 0.3333333333333335369, 0.3333333333333333703, 0.3333333333333334259, 0.3333333333333335369, 0.3333333333333334259, 0.3333333333333333703, 0.3333333333333334259, 0.3333333333333334814, 0.3333333333333335369, 0.3333333333333333148, 0.3333333333333334259, 0.3333333333333334259, 0.3333333333333334814, 0.3333333333333334259, 0.3333333333333334259, 0.3333333333333334259, 0.3333333333333333148, 0.3333333333333335924, 0.3333333333333333148, 0.3333333333333335369, 0.3333333333333333703, 0.3333333333333335369, 0.3333333333333334259, 0.3333333333333333703, 0.3333333333333333703, 0.3333333333333335924, 0.3333333333333333148, 0.3333333333333334259, 0.3333333333333334259, 0.3333333333333335369, 0.3333333333333334814, 0.3333333333333334259, 0.3333333333333334259, 0.3333333333333334259, 0.3333333333333334259, 0.3333333333333333703, 0.3333333333333335369, 0.3333333333333334259, 0.3333333333333334259, 0.3333333333333334814, 0.3333333333333333703, 0.3333333333333333703, 0.3333333333333334814, 0.3333333333333334259, 0.3333333333333333703, 0.3333333333333334814, 0.3333333333333333703, 0.3333333333333334814, 0.3333333333333332593, 0.3333333333333335924, 0.3333333333333333148, 0.3333333333333335924, 0.3333333333333333148, 0.3333333333333335924, 0.3333333333333334259, 0.3333333333333334814, 0.3333333333333333703, 0.3333333333333333703, 0.3333333333333334814, 0.3333333333333335369, 0.3333333333333333703, 0.3333333333333334814, 0.3333333333333334259, 0.3333333333333333703, 0.3333333333333335369, 0.3333333333333333148, 0.3333333333333335369, 0.3333333333333334259, 0.3333333333333334259, 0.3333333333333333703, 0.3333333333333334259, 0.3333333333333333703, 0.3333333333333335369, 0.3333333333333333703, 0.3333333333333334259, 0.3333333333333334259, 0.3333333333333334814, 0.3333333333333333703, 0.3333333333333335924, 0.3333333333333333703, 0.3333333333333334259, 0.3333333333333334814, 0.3333333333333334259, 0.3333333333333335369, 0.3333333333333333148, 0.3333333333333335369, 0.3333333333333333148, 0.3333333333333334259, 0.3333333333333333703, 0.3333333333333334259, 0.3333333333333334259, 0.3333333333333335924, 0.3333333333333333703, 0.3333333333333335924, 0.3333333333333333148, 0.3333333333333335369, 0.3333333333333335369, 0.3333333333333333148, 0.3333333333333334259, 0.3333333333333334259, 0.3333333333333334814, 0.3333333333333333703, 0.3333333333333335369, 0.3333333333333333703, 0.3333333333333333703, 0.3333333333333334814, 0.3333333333333334814, 0.3333333333333334259, 0.3333333333333333703, 0.3333333333333334814, 0.3333333333333334814, 0.3333333333333334259, 0.3333333333333334259, 0.3333333333333334259, 0.3333333333333333703, 0.3333333333333335369, 0.3333333333333333703, 0.3333333333333334259, 0.3333333333333334814, 0.3333333333333334259, 0.3333333333333334814, 0.3333333333333334259, 0.3333333333333333703, 0.3333333333333333703, 0.3333333333333334259, 0.3333333333333333148, 0.3333333333333334814, 0.3333333333333334814, 0.3333333333333334259, 0.3333333333333333703, 0.3333333333333334259, 0.3333333333333334259, 0.3333333333333333703, 0.3333333333333335369, 0.3333333333333334259, 0.3333333333333333148, 0.3333333333333333703, 0.3333333333333335369, 0.3333333333333335369, 0.3333333333333333148, 0.3333333333333335369, 0.3333333333333334259, 0.3333333333333334259, 0.3333333333333335369, 0.3333333333333333703, 0.3333333333333333703, 0.3333333333333334259, 0.3333333333333333703, 0.3333333333333334259, 0.3333333333333334259, 0.3333333333333333703, 0.3333333333333335369, 0.3333333333333333703, 0.3333333333333334259, 0.3333333333333335369, 0.3333333333333333703, 0.3333333333333333703, 0.3333333333333334814, 0.3333333333333334259, 0.3333333333333333703, 0.3333333333333335369, 0.3333333333333332593, 0.3333333333333335369, 0.3333333333333335369, 0.3333333333333333703, 0.3333333333333334814, 0.3333333333333334814, 0.3333333333333334259, 0.3333333333333333703, 0.3333333333333334259, 0.3333333333333334814, 0.3333333333333333148, 0.3333333333333335369, 0.3333333333333333703, 0.3333333333333334259, 0.3333333333333333703, 0.3333333333333334259, 0.3333333333333333148, 0.3333333333333334259, 0.3333333333333334814, 0.3333333333333333703, 0.3333333333333334814, 0.3333333333333334259, 0.3333333333333333703, 0.3333333333333334259, 0.3333333333333333703, 0.3333333333333334259, 0.3333333333333334814, 0.3333333333333332593, 0.3333333333333334259, 0.3333333333333333703, 0.3333333333333335369, 0.3333333333333334259, 0.3333333333333333703, 0.3333333333333334259, 0.3333333333333334259, 0.3333333333333333148, 0.3333333333333335369, 0.3333333333333333703, 0.3333333333333334259, 0.3333333333333335924, 0.3333333333333333703, 0.3333333333333334259, 0.3333333333333335369, 0.3333333333333333703, 0.3333333333333334259, 0.3333333333333334259, 0.3333333333333334259, 0.3333333333333333703, 0.3333333333333334259, 0.3333333333333334259, 0.3333333333333333703, 0.3333333333333333148, 0.3333333333333334814, 0.3333333333333334259, 0.3333333333333334259, 0.3333333333333333703, 0.3333333333333333703, 0.3333333333333334259, 0.3333333333333335369, 0.3333333333333333703, 0.3333333333333335369, 0.3333333333333333703, 0.3333333333333334259, 0.3333333333333335369, 0.3333333333333333148, 0.3333333333333334259, 0.3333333333333334814, 0.3333333333333335369, 0.3333333333333333148, 0.3333333333333335369, 0.3333333333333333703, 0.3333333333333334259, 0.3333333333333333703, 0.3333333333333335369, 0.3333333333333334259, 0.3333333333333334259, 0.3333333333333334259, 0.3333333333333333703, 0.3333333333333335924, 0.3333333333333334259, 0.3333333333333335369, 0.3333333333333333148, 0.3333333333333333703, 0.3333333333333334814, 0.3333333333333333703, 0.3333333333333335924, 0.3333333333333333148, 0.3333333333333333703, 0.3333333333333335369, 0.3333333333333333703, 0.3333333333333335924, 0.3333333333333332593, 0.3333333333333335924, 0.3333333333333334259, 0.3333333333333335369, 0.3333333333333334259, 0.3333333333333334814, 0.3333333333333333703, 0.3333333333333334814, 0.3333333333333333148, 0.3333333333333335369, 0.3333333333333333148, 0.3333333333333334814, 0.3333333333333334814, 0.3333333333333334814, 0.3333333333333333148, 0.3333333333333335369, 0.3333333333333333148, 0.3333333333333335369, 0.3333333333333333703, 0.3333333333333333703, 0.3333333333333335369, 0.3333333333333334259, 0.3333333333333334259, 0.3333333333333333703, 0.3333333333333335369, 0.3333333333333333148, 0.3333333333333335924, 0.3333333333333334259, 0.3333333333333334259, 0.3333333333333333703, 0.3333333333333333703, 0.3333333333333334259, 0.3333333333333334259, 0.3333333333333334259, 0.3333333333333334259, 0.3333333333333334259, 0.3333333333333334259, 0.3333333333333334259, 0.3333333333333333703, 0.3333333333333335369, 0.3333333333333333703, 0.3333333333333334814, 0.3333333333333333703, 0.3333333333333333148, 0.3333333333333337034, 0.3333333333333332038, 0.3333333333333334814, 0.3333333333333335369, 0.3333333333333334814, 0.3333333333333334259, 0.3333333333333334259, 0.3333333333333334814, 0.3333333333333333703, 0.3333333333333334814, 0.3333333333333334259, 0.3333333333333334814, 0.3333333333333333148, 0.3333333333333333703, 0.3333333333333335369, 0.3333333333333334259, 0.3333333333333333703, 0.3333333333333335369, 0.3333333333333334814, 0.3333333333333334259, 0.3333333333333333703, 0.3333333333333334259, 0.3333333333333333148, 0.3333333333333335369, 0.3333333333333333148, 0.3333333333333335369, 0.3333333333333333703, 0.3333333333333335369, 0.3333333333333334259, 0.3333333333333334814, 0.3333333333333334259, 0.3333333333333335369, 0.3333333333333334259, 0.3333333333333334259, 0.3333333333333333703, 0.3333333333333334259, 0.3333333333333333703, 0.3333333333333335369, 0.3333333333333334814, 0.3333333333333333703, 0.3333333333333333148, 0.3333333333333335369, 0.3333333333333333703, 0.3333333333333333703, 0.3333333333333334814, 0.3333333333333333148, 0.3333333333333334814, 0.3333333333333333703, 0.3333333333333334259, 0.3333333333333334814, 0.3333333333333334814, 0.3333333333333334259, 0.3333333333333334259, 0.3333333333333335369, 0.3333333333333334814, 0.3333333333333333148, 0.3333333333333335369, 0.3333333333333334259, 0.3333333333333333703, 0.3333333333333334259, 0.3333333333333334259, 0.3333333333333333148, 0.3333333333333334814, 0.3333333333333333703, 0.3333333333333334259, 0.3333333333333333148, 0.3333333333333334814, 0.3333333333333334259, 0.3333333333333333148, 0.3333333333333334814, 0.3333333333333334259, 0.3333333333333334814, 0.3333333333333332593, 0.3333333333333335924, 0.3333333333333334259, 0.3333333333333334259),
 ( 1.000000000000000222, 1.000000000000000222, 1.000000000000000444, 1.000000000000000000, 1.000000000000000444, 1.000000000000000222, 1.000000000000000444, 0.9999999999999997780, 1.000000000000000444, 1.000000000000000000, 1.000000000000000444, 1.000000000000000000, 1.000000000000000444, 1.000000000000000222, 1.000000000000000000, 1.000000000000000666, 0.9999999999999997780, 1.000000000000000444, 1.000000000000000444, 1.000000000000000444, 1.000000000000000222, 1.000000000000000222, 1.000000000000000444, 1.000000000000000444, 1.000000000000000000, 1.000000000000000222, 1.000000000000000222, 1.000000000000000444, 1.000000000000000222, 1.000000000000000444, 1.000000000000000000, 1.000000000000000222, 1.000000000000000444, 1.000000000000000000, 1.000000000000000444, 1.000000000000000222, 1.000000000000000444, 1.000000000000000444, 1.000000000000000222, 1.000000000000000000, 1.000000000000000444, 1.000000000000000222, 1.000000000000000000, 1.000000000000000222, 1.000000000000000444, 1.000000000000000444, 1.000000000000000444, 1.000000000000000444, 1.000000000000000222, 1.000000000000000444, 1.000000000000000000, 1.000000000000000444, 1.000000000000000222, 1.000000000000000222, 1.000000000000000444, 1.000000000000000000, 1.000000000000000222, 1.000000000000000444, 1.000000000000000222, 1.000000000000000000, 1.000000000000000444, 1.000000000000000222, 1.000000000000000222, 1.000000000000000000, 1.000000000000000444, 0.9999999999999997780, 1.000000000000000444, 1.000000000000000000, 1.000000000000000444, 1.000000000000000000, 1.000000000000000444, 0.9999999999999997780, 1.000000000000000222, 1.000000000000000444, 1.000000000000000444, 1.000000000000000000, 1.000000000000000444, 1.000000000000000222, 1.000000000000000000, 1.000000000000000666, 1.000000000000000000, 1.000000000000000444, 1.000000000000000222, 1.000000000000000444, 0.9999999999999997780, 1.000000000000000444, 1.000000000000000000, 1.000000000000000444, 1.000000000000000444, 1.000000000000000222, 1.000000000000000222, 1.000000000000000444, 1.000000000000000222, 1.000000000000000444, 1.000000000000000444, 1.000000000000000222, 1.000000000000000444, 1.000000000000000222, 1.000000000000000444, 1.000000000000000000, 1.000000000000000444, 1.000000000000000000, 1.000000000000000000, 1.000000000000000444, 1.000000000000000222, 1.000000000000000222, 1.000000000000000444, 1.000000000000000000, 1.000000000000000444, 1.000000000000000000, 1.000000000000000222, 1.000000000000000444, 0.9999999999999997780, 1.000000000000000444, 1.000000000000000222, 1.000000000000000444, 1.000000000000000000, 1.000000000000000444, 1.000000000000000000, 1.000000000000000222, 1.000000000000000222, 1.000000000000000444, 1.000000000000000222, 1.000000000000000000, 1.000000000000000444, 1.000000000000000222, 1.000000000000000222, 1.000000000000000222, 1.000000000000000444, 0.9999999999999997780, 1.000000000000000666, 0.9999999999999996669, 1.000000000000000444, 1.000000000000000444, 1.000000000000000222, 1.000000000000000444, 1.000000000000000444, 1.000000000000000222, 1.000000000000000000, 1.000000000000000444, 1.000000000000000000, 1.000000000000000444, 1.000000000000000222, 1.000000000000000444, 1.000000000000000000, 1.000000000000000444, 1.000000000000000222, 1.000000000000000222, 1.000000000000000444, 1.000000000000000222, 0.9999999999999997780, 1.000000000000000444, 1.000000000000000444, 1.000000000000000444, 1.000000000000000222, 1.000000000000000444, 1.000000000000000444, 1.000000000000000222, 1.000000000000000444, 1.000000000000000000, 1.000000000000000222, 1.000000000000000444, 1.000000000000000000, 1.000000000000000222, 1.000000000000000444, 1.000000000000000000, 1.000000000000000444, 0.9999999999999997780, 1.000000000000000222, 1.000000000000000444, 1.000000000000000000, 1.000000000000000222, 1.000000000000000222, 1.000000000000000444, 1.000000000000000000, 1.000000000000000666, 0.9999999999999996669, 1.000000000000000666, 1.000000000000000222, 1.000000000000000444, 1.000000000000000222, 1.000000000000000444, 1.000000000000000222, 1.000000000000000222, 1.000000000000000000, 1.000000000000000444, 0.9999999999999997780, 1.000000000000000444, 1.000000000000000222, 1.000000000000000444, 0.9999999999999997780, 1.000000000000000444, 1.000000000000000000, 1.000000000000000222, 1.000000000000000444, 1.000000000000000000, 1.000000000000000444, 1.000000000000000444, 1.000000000000000222, 1.000000000000000222, 1.000000000000000000, 1.000000000000000444, 1.000000000000000444, 1.000000000000000000, 1.000000000000000222, 1.000000000000000222, 1.000000000000000444, 1.000000000000000222, 1.000000000000000222, 1.000000000000000444, 1.000000000000000222, 1.000000000000000000, 1.000000000000000444, 1.000000000000000000, 1.000000000000000222, 1.000000000000000444, 1.000000000000000222, 1.000000000000000222, 1.000000000000000444, 1.000000000000000000, 1.000000000000000222, 1.000000000000000222, 1.000000000000000222, 1.000000000000000000, 1.000000000000000222, 1.000000000000000222, 1.000000000000000000, 1.000000000000000222, 1.000000000000000222, 1.000000000000000444, 1.000000000000000000, 1.000000000000000000, 1.000000000000000222, 1.000000000000000000, 1.000000000000000888, 1.000000000000000000, 1.000000000000000444, 1.000000000000000222, 1.000000000000000222, 1.000000000000000444, 1.000000000000000222, 1.000000000000000222, 1.000000000000000444, 1.000000000000000444, 1.000000000000000222, 1.000000000000000444, 1.000000000000000222, 1.000000000000000000, 1.000000000000000222, 1.000000000000000444, 1.000000000000000444, 1.000000000000000222, 1.000000000000000444, 1.000000000000000222, 1.000000000000000444, 1.000000000000000222, 1.000000000000000444, 1.000000000000000222, 1.000000000000000000, 1.000000000000000444, 1.000000000000000000, 1.000000000000000666, 1.000000000000000000, 1.000000000000000000, 1.000000000000000444, 1.000000000000000222, 1.000000000000000444, 0.9999999999999997780, 1.000000000000000666, 1.000000000000000222, 1.000000000000000444, 1.000000000000000222, 1.000000000000000444, 1.000000000000000222, 1.000000000000000444, 0.9999999999999997780, 1.000000000000000666, 1.000000000000000222, 1.000000000000000222, 1.000000000000000444, 1.000000000000000444, 0.9999999999999997780, 1.000000000000000444, 1.000000000000000222, 1.000000000000000222, 1.000000000000000000, 1.000000000000000000, 1.000000000000000444, 1.000000000000000444, 1.000000000000000222, 1.000000000000000000, 1.000000000000000444, 0.9999999999999997780, 1.000000000000000444, 1.000000000000000222, 1.000000000000000000, 1.000000000000000222, 1.000000000000000000, 1.000000000000000444, 1.000000000000000000, 1.000000000000000444, 1.000000000000000222, 1.000000000000000222, 1.000000000000000222, 1.000000000000000222, 1.000000000000000222, 1.000000000000000444, 1.000000000000000222, 1.000000000000000444, 1.000000000000000222, 1.000000000000000000, 1.000000000000000888, 0.9999999999999996669, 1.000000000000000444, 1.000000000000000444, 1.000000000000000222, 1.000000000000000444, 1.000000000000000000, 1.000000000000000444, 0.9999999999999997780, 1.000000000000000444, 1.000000000000000222, 1.000000000000000444, 0.9999999999999997780, 1.000000000000000222, 1.000000000000000222, 1.000000000000000444, 1.000000000000000000, 1.000000000000000444, 1.000000000000000444, 1.000000000000000222, 1.000000000000000000, 1.000000000000000444, 1.000000000000000000, 1.000000000000000222, 1.000000000000000222, 1.000000000000000444, 1.000000000000000000, 1.000000000000000666, 1.000000000000000000, 1.000000000000000444, 1.000000000000000222, 1.000000000000000444, 1.000000000000000222, 1.000000000000000444, 1.000000000000000222, 1.000000000000000222, 1.000000000000000222, 1.000000000000000444, 1.000000000000000444, 1.000000000000000222, 1.000000000000000000, 1.000000000000000444, 1.000000000000000444, 1.000000000000000000, 1.000000000000000444, 0.9999999999999997780, 1.000000000000000444, 1.000000000000000222, 1.000000000000000222, 1.000000000000000444, 1.000000000000000222, 1.000000000000000222, 1.000000000000000444, 1.000000000000000444, 1.000000000000000444, 1.000000000000000000, 1.000000000000000444, 1.000000000000000222, 1.000000000000000222, 1.000000000000000000, 1.000000000000000444, 0.9999999999999997780, 1.000000000000000444, 1.000000000000000000, 1.000000000000000444, 1.000000000000000000, 1.000000000000000444, 1.000000000000000222, 1.000000000000000000, 1.000000000000000444, 1.000000000000000222, 1.000000000000000444, 0.9999999999999997780, 1.000000000000000444, 1.000000000000000222, 1.000000000000000222),
 ( 0.3333333333333334259, 0.3333333333333334259, 0.3333333333333334814, 0.3333333333333333703, 0.3333333333333335369, 0.3333333333333334259, 0.3333333333333334814, 0.3333333333333333703, 0.3333333333333334259, 0.3333333333333333703, 0.3333333333333335369, 0.3333333333333333703, 0.3333333333333334259, 0.3333333333333334259, 0.3333333333333333703, 0.3333333333333335369, 0.3333333333333333703, 0.3333333333333334259, 0.3333333333333335369, 0.3333333333333334259, 0.3333333333333333703, 0.3333333333333334259, 0.3333333333333334814, 0.3333333333333335369, 0.3333333333333333148, 0.3333333333333334259, 0.3333333333333334259, 0.3333333333333334814, 0.3333333333333334259, 0.3333333333333334259, 0.3333333333333334259, 0.3333333333333333148, 0.3333333333333335924, 0.3333333333333333148, 0.3333333333333335369, 0.3333333333333333703, 0.3333333333333335369, 0.3333333333333334259, 0.3333333333333333703, 0.3333333333333333703, 0.3333333333333335924, 0.3333333333333333148, 0.3333333333333334259, 0.3333333333333334259, 0.3333333333333335369, 0.3333333333333334814, 0.3333333333333334259, 0.3333333333333334259, 0.3333333333333334259, 0.3333333333333334259, 0.3333333333333333703, 0.3333333333333335369, 0.3333333333333334259, 0.3333333333333334259, 0.3333333333333334814, 0.3333333333333333703, 0.3333333333333333703, 0.3333333333333334814, 0.3333333333333334259, 0.3333333333333333703, 0.3333333333333334814, 0.3333333333333333703, 0.3333333333333334814, 0.3333333333333332593, 0.3333333333333335924, 0.3333333333333333148, 0.3333333333333335924, 0.3333333333333333148, 0.3333333333333335924, 0.3333333333333334259, 0.3333333333333334814, 0.3333333333333333703, 0.3333333333333333703, 0.3333333333333334814, 0.3333333333333335369, 0.3333333333333333703, 0.3333333333333334814, 0.3333333333333334259, 0.3333333333333333703, 0.3333333333333335369, 0.3333333333333333148, 0.3333333333333335369, 0.3333333333333334259, 0.3333333333333334259, 0.3333333333333333703, 0.3333333333333334259, 0.3333333333333333703, 0.3333333333333335369, 0.3333333333333333703, 0.3333333333333334259, 0.3333333333333334259, 0.3333333333333334814, 0.3333333333333333703, 0.3333333333333335924, 0.3333333333333333703, 0.3333333333333334259, 0.3333333333333334814, 0.3333333333333334259, 0.3333333333333335369, 0.3333333333333333148, 0.3333333333333335369, 0.3333333333333333148, 0.3333333333333334259, 0.3333333333333333703, 0.3333333333333334259, 0.3333333333333334259, 0.3333333333333335924, 0.3333333333333333703, 0.3333333333333335924, 0.3333333333333333148, 0.3333333333333335369, 0.3333333333333335369, 0.3333333333333333148, 0.3333333333333334259, 0.3333333333333334259, 0.3333333333333334814, 0.3333333333333333703, 0.3333333333333335369, 0.3333333333333333703, 0.3333333333333333703, 0.3333333333333334814, 0.3333333333333334814, 0.3333333333333334259, 0.3333333333333333703, 0.3333333333333334814, 0.3333333333333334814, 0.3333333333333334259, 0.3333333333333334259, 0.3333333333333334259, 0.3333333333333333703, 0.3333333333333335369, 0.3333333333333333703, 0.3333333333333334259, 0.3333333333333334814, 0.3333333333333334259, 0.3333333333333334814, 0.3333333333333334259, 0.3333333333333333703, 0.3333333333333333703, 0.3333333333333334259, 0.3333333333333333148, 0.3333333333333334814, 0.3333333333333334814, 0.3333333333333334259, 0.3333333333333333703, 0.3333333333333334259, 0.3333333333333334259, 0.3333333333333333703, 0.3333333333333335369, 0.3333333333333334259, 0.3333333333333333148, 0.3333333333333333703, 0.3333333333333335369, 0.3333333333333335369, 0.3333333333333333148, 0.3333333333333335369, 0.3333333333333334259, 0.3333333333333334259, 0.3333333333333335369, 0.3333333333333333703, 0.3333333333333333703, 0.3333333333333334259, 0.3333333333333333703, 0.3333333333333334259, 0.3333333333333334259, 0.3333333333333333703, 0.3333333333333335369, 0.3333333333333333703, 0.3333333333333334259, 0.3333333333333335369, 0.3333333333333333703, 0.3333333333333333703, 0.3333333333333334814, 0.3333333333333334259, 0.3333333333333333703, 0.3333333333333335369, 0.3333333333333332593, 0.3333333333333335369, 0.3333333333333335369, 0.3333333333333333703, 0.3333333333333334814, 0.3333333333333334814, 0.3333333333333334259, 0.3333333333333333703, 0.3333333333333334259, 0.3333333333333334814, 0.3333333333333333148, 0.3333333333333335369, 0.3333333333333333703, 0.3333333333333334259, 0.3333333333333333703, 0.3333333333333334259, 0.3333333333333333148, 0.3333333333333334259, 0.3333333333333334814, 0.3333333333333333703, 0.3333333333333334814, 0.3333333333333334259, 0.3333333333333333703, 0.3333333333333334259, 0.3333333333333333703, 0.3333333333333334259, 0.3333333333333334814, 0.3333333333333332593, 0.3333333333333334259, 0.3333333333333333703, 0.3333333333333335369, 0.3333333333333334259, 0.3333333333333333703, 0.3333333333333334259, 0.3333333333333334259, 0.3333333333333333148, 0.3333333333333335369, 0.3333333333333333703, 0.3333333333333334259, 0.3333333333333335924, 0.3333333333333333703, 0.3333333333333334259, 0.3333333333333335369, 0.3333333333333333703, 0.3333333333333334259, 0.3333333333333334259, 0.3333333333333334259, 0.3333333333333333703, 0.3333333333333334259, 0.3333333333333334259, 0.3333333333333333703, 0.3333333333333333148, 0.3333333333333334814, 0.3333333333333334259, 0.3333333333333334259, 0.3333333333333333703, 0.3333333333333333703, 0.3333333333333334259, 0.3333333333333335369, 0.3333333333333333703, 0.3333333333333335369, 0.3333333333333333703, 0.3333333333333334259, 0.3333333333333335369, 0.3333333333333333148, 0.3333333333333334259, 0.3333333333333334814, 0.3333333333333335369, 0.3333333333333333148, 0.3333333333333335369, 0.3333333333333333703, 0.3333333333333334259, 0.3333333333333333703, 0.3333333333333335369, 0.3333333333333334259, 0.3333333333333334259, 0.3333333333333334259, 0.3333333333333333703, 0.3333333333333335924, 0.3333333333333334259, 0.3333333333333335369, 0.3333333333333333148, 0.3333333333333333703, 0.3333333333333334814, 0.3333333333333333703, 0.3333333333333335924, 0.3333333333333333148, 0.3333333333333333703, 0.3333333333333335369, 0.3333333333333333703, 0.3333333333333335924, 0.3333333333333332593, 0.3333333333333335924, 0.3333333333333334259, 0.3333333333333335369, 0.3333333333333334259, 0.3333333333333334814, 0.3333333333333333703, 0.3333333333333334814, 0.3333333333333333148, 0.3333333333333335369, 0.3333333333333333148, 0.3333333333333334814, 0.3333333333333334814, 0.3333333333333334814, 0.3333333333333333148, 0.3333333333333335369, 0.3333333333333333148, 0.3333333333333335369, 0.3333333333333333703, 0.3333333333333333703, 0.3333333333333335369, 0.3333333333333334259, 0.3333333333333334259, 0.3333333333333333703, 0.3333333333333335369, 0.3333333333333333148, 0.3333333333333335924, 0.3333333333333334259, 0.3333333333333334259, 0.3333333333333333703, 0.3333333333333333703, 0.3333333333333334259, 0.3333333333333334259, 0.3333333333333334259, 0.3333333333333334259, 0.3333333333333334259, 0.3333333333333334259, 0.3333333333333334259, 0.3333333333333333703, 0.3333333333333335369, 0.3333333333333333703, 0.3333333333333334814, 0.3333333333333333703, 0.3333333333333333148, 0.3333333333333337034, 0.3333333333333332038, 0.3333333333333334814, 0.3333333333333335369, 0.3333333333333334814, 0.3333333333333334259, 0.3333333333333334259, 0.3333333333333334814, 0.3333333333333333703, 0.3333333333333334814, 0.3333333333333334259, 0.3333333333333334814, 0.3333333333333333148, 0.3333333333333333703, 0.3333333333333335369, 0.3333333333333334259, 0.3333333333333333703, 0.3333333333333335369, 0.3333333333333334814, 0.3333333333333334259, 0.3333333333333333703, 0.3333333333333334259, 0.3333333333333333148, 0.3333333333333335369, 0.3333333333333333148, 0.3333333333333335369, 0.3333333333333333703, 0.3333333333333335369, 0.3333333333333334259, 0.3333333333333334814, 0.3333333333333334259, 0.3333333333333335369, 0.3333333333333334259, 0.3333333333333334259, 0.3333333333333333703, 0.3333333333333334259, 0.3333333333333333703, 0.3333333333333335369, 0.3333333333333334814, 0.3333333333333333703, 0.3333333333333333148, 0.3333333333333335369, 0.3333333333333333703, 0.3333333333333333703, 0.3333333333333334814, 0.3333333333333333148, 0.3333333333333334814, 0.3333333333333333703, 0.3333333333333334259, 0.3333333333333334814, 0.3333333333333334814, 0.3333333333333334259, 0.3333333333333334259, 0.3333333333333335369, 0.3333333333333334814, 0.3333333333333333148, 0.3333333333333335369, 0.3333333333333334259, 0.3333333333333333703, 0.3333333333333334259, 0.3333333333333334259, 0.3333333333333333148, 0.3333333333333334814, 0.3333333333333333703, 0.3333333333333334259, 0.3333333333333333148, 0.3333333333333334814, 0.3333333333333334259, 0.3333333333333333148, 0.3333333333333334814, 0.3333333333333334259, 0.3333333333333334814, 0.3333333333333332593, 0.3333333333333335924, 0.3333333333333334259, 0.3333333333333334259),
 ( 0.3333333333333334259, 0.3333333333333334259, 0.3333333333333334814, 0.3333333333333333703, 0.3333333333333335369, 0.3333333333333334259, 0.3333333333333334814, 0.3333333333333333703, 0.3333333333333334259, 0.3333333333333333703, 0.3333333333333335369, 0.3333333333333333703, 0.3333333333333334259, 0.3333333333333334259, 0.3333333333333333703, 0.3333333333333335369, 0.3333333333333333703, 0.3333333333333334259, 0.3333333333333335369, 0.3333333333333334259, 0.3333333333333333703, 0.3333333333333334259, 0.3333333333333334814, 0.3333333333333335369, 0.3333333333333333148, 0.3333333333333334259, 0.3333333333333334259, 0.3333333333333334814, 0.3333333333333334259, 0.3333333333333334259, 0.3333333333333334259, 0.3333333333333333148, 0.3333333333333335924, 0.3333333333333333148, 0.3333333333333335369, 0.3333333333333333703, 0.3333333333333335369, 0.3333333333333334259, 0.3333333333333333703, 0.3333333333333333703, 0.3333333333333335924, 0.3333333333333333148, 0.3333333333333334259, 0.3333333333333334259, 0.3333333333333335369, 0.3333333333333334814, 0.3333333333333334259, 0.3333333333333334259, 0.3333333333333334259, 0.3333333333333334259, 0.3333333333333333703, 0.3333333333333335369, 0.3333333333333334259, 0.3333333333333334259, 0.3333333333333334814, 0.3333333333333333703, 0.3333333333333333703, 0.3333333333333334814, 0.3333333333333334259, 0.3333333333333333703, 0.3333333333333334814, 0.3333333333333333703, 0.3333333333333334814, 0.3333333333333332593, 0.3333333333333335924, 0.3333333333333333148, 0.3333333333333335924, 0.3333333333333333148, 0.3333333333333335924, 0.3333333333333334259, 0.3333333333333334814, 0.3333333333333333703, 0.3333333333333333703, 0.3333333333333334814, 0.3333333333333335369, 0.3333333333333333703, 0.3333333333333334814, 0.3333333333333334259, 0.3333333333333333703, 0.3333333333333335369, 0.3333333333333333148, 0.3333333333333335369, 0.3333333333333334259, 0.3333333333333334259, 0.3333333333333333703, 0.3333333333333334259, 0.3333333333333333703, 0.3333333333333335369, 0.3333333333333333703, 0.3333333333333334259, 0.3333333333333334259, 0.3333333333333334814, 0.3333333333333333703, 0.3333333333333335924, 0.3333333333333333703, 0.3333333333333334259, 0.3333333333333334814, 0.3333333333333334259, 0.3333333333333335369, 0.3333333333333333148, 0.3333333333333335369, 0.3333333333333333148, 0.3333333333333334259, 0.3333333333333333703, 0.3333333333333334259, 0.3333333333333334259, 0.3333333333333335924, 0.3333333333333333703, 0.3333333333333335924, 0.3333333333333333148, 0.3333333333333335369, 0.3333333333333335369, 0.3333333333333333148, 0.3333333333333334259, 0.3333333333333334259, 0.3333333333333334814, 0.3333333333333333703, 0.3333333333333335369, 0.3333333333333333703, 0.3333333333333333703, 0.3333333333333334814, 0.3333333333333334814, 0.3333333333333334259, 0.3333333333333333703, 0.3333333333333334814, 0.3333333333333334814, 0.3333333333333334259, 0.3333333333333334259, 0.3333333333333334259, 0.3333333333333333703, 0.3333333333333335369, 0.3333333333333333703, 0.3333333333333334259, 0.3333333333333334814, 0.3333333333333334259, 0.3333333333333334814, 0.3333333333333334259, 0.3333333333333333703, 0.3333333333333333703, 0.3333333333333334259, 0.3333333333333333148, 0.3333333333333334814, 0.3333333333333334814, 0.3333333333333334259, 0.3333333333333333703, 0.3333333333333334259, 0.3333333333333334259, 0.3333333333333333703, 0.3333333333333335369, 0.3333333333333334259, 0.3333333333333333148, 0.3333333333333333703, 0.3333333333333335369, 0.3333333333333335369, 0.3333333333333333148, 0.3333333333333335369, 0.3333333333333334259, 0.3333333333333334259, 0.3333333333333335369, 0.3333333333333333703, 0.3333333333333333703, 0.3333333333333334259, 0.3333333333333333703, 0.3333333333333334259, 0.3333333333333334259, 0.3333333333333333703, 0.3333333333333335369, 0.3333333333333333703, 0.3333333333333334259, 0.3333333333333335369, 0.3333333333333333703, 0.3333333333333333703, 0.3333333333333334814, 0.3333333333333334259, 0.3333333333333333703, 0.3333333333333335369, 0.3333333333333332593, 0.3333333333333335369, 0.3333333333333335369, 0.3333333333333333703, 0.3333333333333334814, 0.3333333333333334814, 0.3333333333333334259, 0.3333333333333333703, 0.3333333333333334259, 0.3333333333333334814, 0.3333333333333333148, 0.3333333333333335369, 0.3333333333333333703, 0.3333333333333334259, 0.3333333333333333703, 0.3333333333333334259, 0.3333333333333333148, 0.3333333333333334259, 0.3333333333333334814, 0.3333333333333333703, 0.3333333333333334814, 0.3333333333333334259, 0.3333333333333333703, 0.3333333333333334259, 0.3333333333333333703, 0.3333333333333334259, 0.3333333333333334814, 0.3333333333333332593, 0.3333333333333334259, 0.3333333333333333703, 0.3333333333333335369, 0.3333333333333334259, 0.3333333333333333703, 0.3333333333333334259, 0.3333333333333334259, 0.3333333333333333148, 0.3333333333333335369, 0.3333333333333333703, 0.3333333333333334259, 0.3333333333333335924, 0.3333333333333333703, 0.3333333333333334259, 0.3333333333333335369, 0.3333333333333333703, 0.3333333333333334259, 0.3333333333333334259, 0.3333333333333334259, 0.3333333333333333703, 0.3333333333333334259, 0.3333333333333334259, 0.3333333333333333703, 0.3333333333333333148, 0.3333333333333334814, 0.3333333333333334259, 0.3333333333333334259, 0.3333333333333333703, 0.3333333333333333703, 0.3333333333333334259, 0.3333333333333335369, 0.3333333333333333703, 0.3333333333333335369, 0.3333333333333333703, 0.3333333333333334259, 0.3333333333333335369, 0.3333333333333333148, 0.3333333333333334259, 0.3333333333333334814, 0.3333333333333335369, 0.3333333333333333148, 0.3333333333333335369, 0.3333333333333333703, 0.3333333333333334259, 0.3333333333333333703, 0.3333333333333335369, 0.3333333333333334259, 0.3333333333333334259, 0.3333333333333334259, 0.3333333333333333703, 0.3333333333333335924, 0.3333333333333334259, 0.3333333333333335369, 0.3333333333333333148, 0.3333333333333333703, 0.3333333333333334814, 0.3333333333333333703, 0.3333333333333335924, 0.3333333333333333148, 0.3333333333333333703, 0.3333333333333335369, 0.3333333333333333703, 0.3333333333333335924, 0.3333333333333332593, 0.3333333333333335924, 0.3333333333333334259, 0.3333333333333335369, 0.3333333333333334259, 0.3333333333333334814, 0.3333333333333333703, 0.3333333333333334814, 0.3333333333333333148, 0.3333333333333335369, 0.3333333333333333148, 0.3333333333333334814, 0.3333333333333334814, 0.3333333333333334814, 0.3333333333333333148, 0.3333333333333335369, 0.3333333333333333148, 0.3333333333333335369, 0.3333333333333333703, 0.3333333333333333703, 0.3333333333333335369, 0.3333333333333334259, 0.3333333333333334259, 0.3333333333333333703, 0.3333333333333335369, 0.3333333333333333148, 0.3333333333333335924, 0.3333333333333334259, 0.3333333333333334259, 0.3333333333333333703, 0.3333333333333333703, 0.3333333333333334259, 0.3333333333333334259, 0.3333333333333334259, 0.3333333333333334259, 0.3333333333333334259, 0.3333333333333334259, 0.3333333333333334259, 0.3333333333333333703, 0.3333333333333335369, 0.3333333333333333703, 0.3333333333333334814, 0.3333333333333333703, 0.3333333333333333148, 0.3333333333333337034, 0.3333333333333332038, 0.3333333333333334814, 0.3333333333333335369, 0.3333333333333334814, 0.3333333333333334259, 0.3333333333333334259, 0.3333333333333334814, 0.3333333333333333703, 0.3333333333333334814, 0.3333333333333334259, 0.3333333333333334814, 0.3333333333333333148, 0.3333333333333333703, 0.3333333333333335369, 0.3333333333333334259, 0.3333333333333333703, 0.3333333333333335369, 0.3333333333333334814, 0.3333333333333334259, 0.3333333333333333703, 0.3333333333333334259, 0.3333333333333333148, 0.3333333333333335369, 0.3333333333333333148, 0.3333333333333335369, 0.3333333333333333703, 0.3333333333333335369, 0.3333333333333334259, 0.3333333333333334814, 0.3333333333333334259, 0.3333333333333335369, 0.3333333333333334259, 0.3333333333333334259, 0.3333333333333333703, 0.3333333333333334259, 0.3333333333333333703, 0.3333333333333335369, 0.3333333333333334814, 0.3333333333333333703, 0.3333333333333333148, 0.3333333333333335369, 0.3333333333333333703, 0.3333333333333333703, 0.3333333333333334814, 0.3333333333333333148, 0.3333333333333334814, 0.3333333333333333703, 0.3333333333333334259, 0.3333333333333334814, 0.3333333333333334814, 0.3333333333333334259, 0.3333333333333334259, 0.3333333333333335369, 0.3333333333333334814, 0.3333333333333333148, 0.3333333333333335369, 0.3333333333333334259, 0.3333333333333333703, 0.3333333333333334259, 0.3333333333333334259, 0.3333333333333333148, 0.3333333333333334814, 0.3333333333333333703, 0.3333333333333334259, 0.3333333333333333148, 0.3333333333333334814, 0.3333333333333334259, 0.3333333333333333148, 0.3333333333333334814, 0.3333333333333334259, 0.3333333333333334814, 0.3333333333333332593, 0.3333333333333335924, 0.3333333333333334259, 0.3333333333333334259),
 ( 1.000000000000000222, 1.000000000000000222, 1.000000000000000444, 1.000000000000000000, 1.000000000000000444, 1.000000000000000222, 1.000000000000000444, 0.9999999999999997780, 1.000000000000000444, 1.000000000000000000, 1.000000000000000444, 1.000000000000000000, 1.000000000000000444, 1.000000000000000222, 1.000000000000000000, 1.000000000000000666, 0.9999999999999997780, 1.000000000000000444, 1.000000000000000444, 1.000000000000000444, 1.000000000000000222, 1.000000000000000222, 1.000000000000000444, 1.000000000000000444, 1.000000000000000000, 1.000000000000000222, 1.000000000000000222, 1.000000000000000444, 1.000000000000000222, 1.000000000000000444, 1.000000000000000000, 1.000000000000000222, 1.000000000000000444, 1.000000000000000000, 1.000000000000000444, 1.000000000000000222, 1.000000000000000444, 1.000000000000000444, 1.000000000000000222, 1.000000000000000000, 1.000000000000000444, 1.000000000000000222, 1.000000000000000000, 1.000000000000000222, 1.000000000000000444, 1.000000000000000444, 1.000000000000000444, 1.000000000000000444, 1.000000000000000222, 1.000000000000000444, 1.000000000000000000, 1.000000000000000444, 1.000000000000000222, 1.000000000000000222, 1.000000000000000444, 1.000000000000000000, 1.000000000000000222, 1.000000000000000444, 1.000000000000000222, 1.000000000000000000, 1.000000000000000444, 1.000000000000000222, 1.000000000000000222, 1.000000000000000000, 1.000000000000000444, 0.9999999999999997780, 1.000000000000000444, 1.000000000000000000, 1.000000000000000444, 1.000000000000000000, 1.000000000000000444, 0.9999999999999997780, 1.000000000000000222, 1.000000000000000444, 1.000000000000000444, 1.000000000000000000, 1.000000000000000444, 1.000000000000000222, 1.000000000000000000, 1.000000000000000666, 1.000000000000000000, 1.000000000000000444, 1.000000000000000222, 1.000000000000000444, 0.9999999999999997780, 1.000000000000000444, 1.000000000000000000, 1.000000000000000444, 1.000000000000000444, 1.000000000000000222, 1.000000000000000222, 1.000000000000000444, 1.000000000000000222, 1.000000000000000444, 1.000000000000000444, 1.000000000000000222, 1.000000000000000444, 1.000000000000000222, 1.000000000000000444, 1.000000000000000000, 1.000000000000000444, 1.000000000000000000, 1.000000000000000000, 1.000000000000000444, 1.000000000000000222, 1.000000000000000222, 1.000000000000000444, 1.000000000000000000, 1.000000000000000444, 1.000000000000000000, 1.000000000000000222, 1.000000000000000444, 0.9999999999999997780, 1.000000000000000444, 1.000000000000000222, 1.000000000000000444, 1.000000000000000000, 1.000000000000000444, 1.000000000000000000, 1.000000000000000222, 1.000000000000000222, 1.000000000000000444, 1.000000000000000222, 1.000000000000000000, 1.000000000000000444, 1.000000000000000222, 1.000000000000000222, 1.000000000000000222, 1.000000000000000444, 0.9999999999999997780, 1.000000000000000666, 0.9999999999999996669, 1.000000000000000444, 1.000000000000000444, 1.000000000000000222, 1.000000000000000444, 1.000000000000000444, 1.000000000000000222, 1.000000000000000000, 1.000000000000000444, 1.000000000000000000, 1.000000000000000444, 1.000000000000000222, 1.000000000000000444, 1.000000000000000000, 1.000000000000000444, 1.000000000000000222, 1.000000000000000222, 1.000000000000000444, 1.000000000000000222, 0.9999999999999997780, 1.000000000000000444, 1.000000000000000444, 1.000000000000000444, 1.000000000000000222, 1.000000000000000444, 1.000000000000000444, 1.000000000000000222, 1.000000000000000444, 1.000000000000000000, 1.000000000000000222, 1.000000000000000444, 1.000000000000000000, 1.000000000000000222, 1.000000000000000444, 1.000000000000000000, 1.000000000000000444, 0.9999999999999997780, 1.000000000000000222, 1.000000000000000444, 1.000000000000000000, 1.000000000000000222, 1.000000000000000222, 1.000000000000000444, 1.000000000000000000, 1.000000000000000666, 0.9999999999999996669, 1.000000000000000666, 1.000000000000000222, 1.000000000000000444, 1.000000000000000222, 1.000000000000000444, 1.000000000000000222, 1.000000000000000222, 1.000000000000000000, 1.000000000000000444, 0.9999999999999997780, 1.000000000000000444, 1.000000000000000222, 1.000000000000000444, 0.9999999999999997780, 1.000000000000000444, 1.000000000000000000, 1.000000000000000222, 1.000000000000000444, 1.000000000000000000, 1.000000000000000444, 1.000000000000000444, 1.000000000000000222, 1.000000000000000222, 1.000000000000000000, 1.000000000000000444, 1.000000000000000444, 1.000000000000000000, 1.000000000000000222, 1.000000000000000222, 1.000000000000000444, 1.000000000000000222, 1.000000000000000222, 1.000000000000000444, 1.000000000000000222, 1.000000000000000000, 1.000000000000000444, 1.000000000000000000, 1.000000000000000222, 1.000000000000000444, 1.000000000000000222, 1.000000000000000222, 1.000000000000000444, 1.000000000000000000, 1.000000000000000222, 1.000000000000000222, 1.000000000000000222, 1.000000000000000000, 1.000000000000000222, 1.000000000000000222, 1.000000000000000000, 1.000000000000000222, 1.000000000000000222, 1.000000000000000444, 1.000000000000000000, 1.000000000000000000, 1.000000000000000222, 1.000000000000000000, 1.000000000000000888, 1.000000000000000000, 1.000000000000000444, 1.000000000000000222, 1.000000000000000222, 1.000000000000000444, 1.000000000000000222, 1.000000000000000222, 1.000000000000000444, 1.000000000000000444, 1.000000000000000222, 1.000000000000000444, 1.000000000000000222, 1.000000000000000000, 1.000000000000000222, 1.000000000000000444, 1.000000000000000444, 1.000000000000000222, 1.000000000000000444, 1.000000000000000222, 1.000000000000000444, 1.000000000000000222, 1.000000000000000444, 1.000000000000000222, 1.000000000000000000, 1.000000000000000444, 1.000000000000000000, 1.000000000000000666, 1.000000000000000000, 1.000000000000000000, 1.000000000000000444, 1.000000000000000222, 1.000000000000000444, 0.9999999999999997780, 1.000000000000000666, 1.000000000000000222, 1.000000000000000444, 1.000000000000000222, 1.000000000000000444, 1.000000000000000222, 1.000000000000000444, 0.9999999999999997780, 1.000000000000000666, 1.000000000000000222, 1.000000000000000222, 1.000000000000000444, 1.000000000000000444, 0.9999999999999997780, 1.000000000000000444, 1.000000000000000222, 1.000000000000000222, 1.000000000000000000, 1.000000000000000000, 1.000000000000000444, 1.000000000000000444, 1.000000000000000222, 1.000000000000000000, 1.000000000000000444, 0.9999999999999997780, 1.000000000000000444, 1.000000000000000222, 1.000000000000000000, 1.000000000000000222, 1.000000000000000000, 1.000000000000000444, 1.000000000000000000, 1.000000000000000444, 1.000000000000000222, 1.000000000000000222, 1.000000000000000222, 1.000000000000000222, 1.000000000000000222, 1.000000000000000444, 1.000000000000000222, 1.000000000000000444, 1.000000000000000222, 1.000000000000000000, 1.000000000000000888, 0.9999999999999996669, 1.000000000000000444, 1.000000000000000444, 1.000000000000000222, 1.000000000000000444, 1.000000000000000000, 1.000000000000000444, 0.9999999999999997780, 1.000000000000000444, 1.000000000000000222, 1.000000000000000444, 0.9999999999999997780, 1.000000000000000222, 1.000000000000000222, 1.000000000000000444, 1.000000000000000000, 1.000000000000000444, 1.000000000000000444, 1.000000000000000222, 1.000000000000000000, 1.000000000000000444, 1.000000000000000000, 1.000000000000000222, 1.000000000000000222, 1.000000000000000444, 1.000000000000000000, 1.000000000000000666, 1.000000000000000000, 1.000000000000000444, 1.000000000000000222, 1.000000000000000444, 1.000000000000000222, 1.000000000000000444, 1.000000000000000222, 1.000000000000000222, 1.000000000000000222, 1.000000000000000444, 1.000000000000000444, 1.000000000000000222, 1.000000000000000000, 1.000000000000000444, 1.000000000000000444, 1.000000000000000000, 1.000000000000000444, 0.9999999999999997780, 1.000000000000000444, 1.000000000000000222, 1.000000000000000222, 1.000000000000000444, 1.000000000000000222, 1.000000000000000222, 1.000000000000000444, 1.000000000000000444, 1.000000000000000444, 1.000000000000000000, 1.000000000000000444, 1.000000000000000222, 1.000000000000000222, 1.000000000000000000, 1.000000000000000444, 0.9999999999999997780, 1.000000000000000444, 1.000000000000000000, 1.000000000000000444, 1.000000000000000000, 1.000000000000000444, 1.000000000000000222, 1.000000000000000000, 1.000000000000000444, 1.000000000000000222, 1.000000000000000444, 0.9999999999999997780, 1.000000000000000444, 1.000000000000000222, 1.000000000000000222) ) ) 
 REPRESENTATION_ITEM ( '' )  SURFACE ( )  );
#63187=( LENGTH_UNIT ( ) NAMED_UNIT ( * ) SI_UNIT ( .MILLI., .METRE. ) );
#63192=CARTESIAN_POINT ( 'NONE',  ( 1.112269271232646739, 2.068042923180101411, -0.09779880236997220977 ) ) ;
#63193=CARTESIAN_POINT ( 'NONE',  ( 2.460703409257146923, -2.027034307268358315, -0.6114533316685047959 ) ) ;
#63196=CARTESIAN_POINT ( 'NONE',  ( 1.006626315519317139, 0.5665869296403948097, 1.886213005043664515 ) ) ;
#63200=CARTESIAN_POINT ( 'NONE',  ( 0.1831564129048668388, 7.629137130509052511, -2.545826866328745997 ) ) ;
#63201=CARTESIAN_POINT ( 'NONE',  ( 2.730776445121200435, 0.2818232878892740212, 2.274813446668845884 ) ) ;
#63202=CARTESIAN_POINT ( 'NONE',  ( 0.2229205655521030172, -0.09321834626660817358, 1.823428419517532983 ) ) ;
#63203=CARTESIAN_POINT ( 'NONE',  ( 2.021601768330282045, -0.4154675118966509317, 1.866563793090275203 ) ) ;
#63206=CARTESIAN_POINT ( 'NONE',  ( 1.705339411233731672, 1.749488060808137790, -0.9960635233151514667 ) ) ;
#63207=CARTESIAN_POINT ( 'NONE',  ( 2.237090426018002454, -0.09115598566783281176, -1.959741687340323946 ) ) ;
#63211=CARTESIAN_POINT ( 'NONE',  ( 4.593745122936496728, -2.090168268563397547, -0.05157397306862486486 ) ) ;
#63212=CARTESIAN_POINT ( 'NONE',  ( 3.291635156611854462, -0.7182737719314927771, 1.617730789815795545 ) ) ;
#63215=CARTESIAN_POINT ( 'NONE',  ( 6.246038198481189241, 0.7129642902690846995, 2.178627299872720524 ) ) ;
#63216=CARTESIAN_POINT ( 'NONE',  ( 4.646296158022299672, -1.395249218123927104, 1.039982334504330197 ) ) ;
#63221=CARTESIAN_POINT ( 'NONE',  ( 3.971823236585111161, 1.486633142371917238, 0.8919779901093974894 ) ) ;
#63222=CARTESIAN_POINT ( 'NONE',  ( 4.773980394326226673, -2.130202496963151670, 0.4190362392007019876 ) ) ;
#63224=CARTESIAN_POINT ( 'NONE',  ( 5.858611323429600226, -1.916351766245901977, -0.6279953093112633500 ) ) ;
#63225=CARTESIAN_POINT ( 'NONE',  ( 5.093750000000003553, -1.895863743164187376, -0.7852924748297283042 ) ) ;
#63227=CARTESIAN_POINT ( 'NONE',  ( 3.715773558573881363, -1.898061356504710639, 0.3282749975898023309 ) ) ;
#63229=CARTESIAN_POINT ( 'NONE',  ( 0.3994919479695389075, -0.2781545790336605317, -2.203771652037065376 ) ) ;
#63231=CARTESIAN_POINT ( 'NONE',  ( 6.983263157960365675, 7.629137130509070275, 2.446189081643288521 ) ) ;
#63240=CARTESIAN_POINT ( 'NONE',  ( 0.05336153386781630759, -1.314994204386025434, 1.528742563917218078 ) ) ;
#63242=CARTESIAN_POINT ( 'NONE',  ( 6.021949879679938000, 2.032782779420911456, -0.3490252056354887222 ) ) ;
#63247=CARTESIAN_POINT ( 'NONE',  ( 0.7195362622018970367, -0.9397137143956849625, -1.499438161327722341 ) ) ;
#63248=CARTESIAN_POINT ( 'NONE',  ( 5.766190679352209969, 1.598854145598350929, -0.6720813200297001133 ) ) ;
#63249=CARTESIAN_POINT ( 'NONE',  ( 5.091228679354776965, -0.6197342532976670704, 1.626566373401008070 ) ) ;
#63251=CARTESIAN_POINT ( 'NONE',  ( 3.228363206396630769, 2.236961789864226002, 0.5003539455325100027 ) ) ;
#63253=CARTESIAN_POINT ( 'NONE',  ( 1.042614295247261680, -1.450156864641814369, -1.134287774663629733 ) ) ;
#63256=CARTESIAN_POINT ( 'NONE',  ( 2.186296784933777992, -1.789763940591000191, -0.3589617604915079085 ) ) ;
#63257=CARTESIAN_POINT ( 'NONE',  ( 2.619767714365705658, 0.2496074646863334634, 2.000857082853441327 ) ) ;
#63258=CARTESIAN_POINT ( 'NONE',  ( 1.517799938645987057, -1.219565478727736574, -1.820545776841306029 ) ) ;
#63260=CARTESIAN_POINT ( 'NONE',  ( 4.682709062318923365, -2.042047207266047604, -0.5143438382350475901 ) ) ;
#63263=CARTESIAN_POINT ( 'NONE',  ( 1.275928261265106833, -2.020323679977220621, 0.4517519998969782291 ) ) ;
#63266=CARTESIAN_POINT ( 'NONE',  ( 3.440189854244297241, -1.264556376030629981, -1.702001827410426049 ) ) ;
#63268=CARTESIAN_POINT ( 'NONE',  ( 6.721331454403435934, -0.1262074967819451221, 1.796610827203233063 ) ) ;
#63275=CARTESIAN_POINT ( 'NONE',  ( 6.451439665316073935, -1.893653415279672902, 0.9546920624979161607 ) ) ;
#63276=CARTESIAN_POINT ( 'NONE',  ( 1.167171324275569466, -1.903845421566036311, -0.9005605707013781824 ) ) ;
#63279=CARTESIAN_POINT ( 'NONE',  ( 5.313276548598107496, -1.570925495967404828, -0.9973500568975323111 ) ) ;
#63287=CARTESIAN_POINT ( 'NONE',  ( 2.049198471137442912, 1.708465938063120637, -0.9642302061752603404 ) ) ;
#63288=CARTESIAN_POINT ( 'NONE',  ( 0.6554165194554737450, -1.826866057147133349, -1.155366728873077342 ) ) ;
#63293=CARTESIAN_POINT ( 'NONE',  ( 3.268574299048069953, -1.732005324549376279, 0.08218708453346619536 ) ) ;
#63294=CARTESIAN_POINT ( 'NONE',  ( 2.009305037403839922, -0.8189296680943327633, -1.535607775426613086 ) ) ;
#63297=CARTESIAN_POINT ( 'NONE',  ( 3.040362567271452487, 2.044824973086068809, 0.2555446107466197714 ) ) ;
#63298=CARTESIAN_POINT ( 'NONE',  ( 0.6673420201736457447, -0.6766069248959759586, -1.899328980164962877 ) ) ;
#63299=CARTESIAN_POINT ( 'NONE',  ( 6.825078400183579141, 1.241995729952071637, 2.258014901253778461 ) ) ;
#63301=CARTESIAN_POINT ( 'NONE',  ( 0.9714808946714141857, 1.900638238906343425, -0.5234924991099793035 ) ) ;
#63302=CARTESIAN_POINT ( 'NONE',  ( 5.642805672956042962, 1.844803604357934779, 0.5037821151940986564 ) ) ;
#63307=CARTESIAN_POINT ( 'NONE',  ( 0.7858139957730024827, 1.945786914974199089, -0.5409757216557200543 ) ) ;
#63309=CARTESIAN_POINT ( 'NONE',  ( 5.051972272063284031, 0.7293918257267332228, -2.189345848185173082 ) ) ;
#63310=CARTESIAN_POINT ( 'NONE',  ( 5.529730448059603454, 1.891198321494348633, -0.5216162335564683561 ) ) ;
#63312=CARTESIAN_POINT ( 'NONE',  ( 2.307404798597446849, -1.572557994556064154, -1.172606125687980061 ) ) ;
#63316=CARTESIAN_POINT ( 'NONE',  ( 1.270887751945870336, -0.3167050496251391234, -2.093436144997854687 ) ) ;
#63319=CARTESIAN_POINT ( 'NONE',  ( 1.376629057770164311, 1.701771572936720212, -0.7031625657484343872 ) ) ;
#63321=CARTESIAN_POINT ( 'NONE',  ( 4.223599041728074432, 0.2716450895321539383, -2.153977947863388476 ) ) ;
#63323=CARTESIAN_POINT ( 'NONE',  ( 1.687894460584405731, 2.027760172737497424, -0.6205009303206151516 ) ) ;
#63327=CARTESIAN_POINT ( 'NONE',  ( 3.251298195952691206, -1.682652751511631850, -1.189445392860078110 ) ) ;
#63330=CARTESIAN_POINT ( 'NONE',  ( 0.7140992756325339474, 1.701125707204936166, 0.7050099338341904165 ) ) ;
#63332=CARTESIAN_POINT ( 'NONE',  ( 0.07735805125222076917, 2.865712030211249761, -2.577262785371988496 ) ) ;
#63333=EDGE_CURVE ( 'NONE', #92893, #5628, #100314, .T. ) ;
#63335=CARTESIAN_POINT ( 'NONE',  ( 0.1884680354247054990, -1.036234488384666586, 1.948478269905975946 ) ) ;
#63336=CARTESIAN_POINT ( 'NONE',  ( 2.407839351892237634, -0.4975810599385386834, 2.206854368276117917 ) ) ;
#63338=CARTESIAN_POINT ( 'NONE',  ( 2.759786284469767814, 0.6482482438519759915, -1.691825979898635035 ) ) ;
#63339=CARTESIAN_POINT ( 'NONE',  ( 2.149496333622540334, 1.877876629180765589, -0.3779552698702989266 ) ) ;
#63340=CARTESIAN_POINT ( 'NONE',  ( 3.350112325975619587, -0.8415805752714689003, 1.891790567983504312 ) ) ;
#63342=CARTESIAN_POINT ( 'NONE',  ( 1.797671122125501952, -0.6659361598389621495, 1.855707729256075522 ) ) ;
#63343=CARTESIAN_POINT ( 'NONE',  ( 0.2352082051719720512, -1.762675558584745783, 0.7775455664775063891 ) ) ;
#63344=CARTESIAN_POINT ( 'NONE',  ( 2.817106861211693847, -0.1851908181382568019, 1.861470920997858380 ) ) ;
#63345=CARTESIAN_POINT ( 'NONE',  ( 1.190513350481865240, -1.033627929232444620, 2.063343651489284003 ) ) ;
#63347=CARTESIAN_POINT ( 'NONE',  ( 3.051044903872371261, 1.597643715361036998, -0.9542115197753370248 ) ) ;
#63349=CARTESIAN_POINT ( 'NONE',  ( 5.635237469726069648, -0.04712981909091130961, -2.062292871413499373 ) ) ;
#63354=CARTESIAN_POINT ( 'NONE',  ( 6.370163019944321547, 1.079249059096079044, 1.808242165975785909 ) ) ;
#63356=CARTESIAN_POINT ( 'NONE',  ( 5.483715611629243369, 1.447241891022777560, 1.605803905980404123 ) ) ;
#63357=CARTESIAN_POINT ( 'NONE',  ( 6.059241617823571957, -1.705078594313869988, 1.082191098076368929 ) ) ;
#63367=CARTESIAN_POINT ( 'NONE',  ( 5.067592334412735156, 1.357865985192594271, 1.490972259599515848 ) ) ;
#63372=CARTESIAN_POINT ( 'NONE',  ( 6.016527291255574283, 1.455332790597754000, -1.598591904487467463 ) ) ;
#63377=CARTESIAN_POINT ( 'NONE',  ( 5.448842280278080707, -1.824126957265741256, -0.8596167168879662590 ) ) ;
#63380=CARTESIAN_POINT ( 'NONE',  ( 1.347838067242516313, 1.722766431120416941, 0.08778956860019770936 ) ) ;
#63385=CARTESIAN_POINT ( 'NONE',  ( 6.784453417974287248, -1.834524189944960693, -0.3643881242741816573 ) ) ;
#63386=CARTESIAN_POINT ( 'NONE',  ( 0.5221354380547962304, -2.003184638039813503, 0.1996226354380666868 ) ) ;
#63388=CARTESIAN_POINT ( 'NONE',  ( 2.977765718515757332, 2.095881712254169305, -0.6909776239150815513 ) ) ;
#63389=CARTESIAN_POINT ( 'NONE',  ( 5.823135961761455981, -1.959396665126054815, -0.9353919727212963720 ) ) ;
#63393=CARTESIAN_POINT ( 'NONE',  ( 3.317144061745095129, 1.670432841370917298, -1.306055464808851818 ) ) ;
#63394=CARTESIAN_POINT ( 'NONE',  ( 2.003530013310977242, -1.955168117277843898, 0.4926643476272293820 ) ) ;
#63395=CARTESIAN_POINT ( 'NONE',  ( 2.654344044762357413, 1.798353594787518217, 0.2176890031466270636 ) ) ;
#63401=CARTESIAN_POINT ( 'NONE',  ( 1.657307721912592458, 1.831997054396968361, -0.5600143317019135036 ) ) ;
#63409=CARTESIAN_POINT ( 'NONE',  ( 4.803692121107413726, -0.5798474923815257753, 2.082409481564663434 ) ) ;
#63412=CARTESIAN_POINT ( 'NONE',  ( 1.512141599020993432, -0.7094941370262075608, 1.998545949238240027 ) ) ;
#63415=CARTESIAN_POINT ( 'NONE',  ( 3.550034410471062163, 1.971530340838826278, 0.003394978380427334484 ) ) ;
#63416=CARTESIAN_POINT ( 'NONE',  ( 5.924064563541377559, -1.897137492723115049, 0.2407653536913647030 ) ) ;
#63419=CARTESIAN_POINT ( 'NONE',  ( 0.2036857628631080219, -1.599406074100502506, -1.314310892166506095 ) ) ;
#63420=CARTESIAN_POINT ( 'NONE',  ( 2.449080105735270685, 0.5175099976203160201, -1.871664248846743872 ) ) ;
#63425=CARTESIAN_POINT ( 'NONE',  ( 2.554727279587006183, -1.819456544085126026, -1.029573916123826427 ) ) ;
#63428=CARTESIAN_POINT ( 'NONE',  ( 6.182274467271688501, 0.9872068455926674702, 1.637624497839342608 ) ) ;
#63430=CARTESIAN_POINT ( 'NONE',  ( 4.442132104469964204, 0.9450947508268662256, -1.994404356956205548 ) ) ;
#63431=CARTESIAN_POINT ( 'NONE',  ( 3.628125149645112568, -1.312672481567092708, -1.773765351669121415 ) ) ;
#63433=CARTESIAN_POINT ( 'NONE',  ( 1.822773347178743286, 1.416086463930026573, -1.285276961632122683 ) ) ;
#63437=CARTESIAN_POINT ( 'NONE',  ( 4.738769824615551407, -2.007376682328159134, -0.5062664373569197851 ) ) ;
#63440=CARTESIAN_POINT ( 'NONE',  ( 1.991316529349271836, 1.880942973025516940, -1.065213018539921563 ) ) ;
#63441=CARTESIAN_POINT ( 'NONE',  ( 5.319949580897746166, 1.306013235697962571, -1.759773446019400778 ) ) ;
#63447=CARTESIAN_POINT ( 'NONE',  ( 0.03578008775950020093, -1.617816776142148250, 1.203357013023528932 ) ) ;
#63450=CARTESIAN_POINT ( 'NONE',  ( 4.838769763947080804, -2.006773940031422399, -0.5081810985937407210 ) ) ;
#63451=CARTESIAN_POINT ( 'NONE',  ( 3.686086919817387564, -0.9488725894866935073, 1.676545010912360745 ) ) ;
#63452=CARTESIAN_POINT ( 'NONE',  ( 6.064083512088704886, -1.132370213454384045, 1.788784107109566701 ) ) ;
#63455=CARTESIAN_POINT ( 'NONE',  ( 4.381674357853755808, -1.885861198437089437, 0.5677522405800348171 ) ) ;
#63456=CARTESIAN_POINT ( 'NONE',  ( 5.894527261468666346, 1.877221869688485700, -1.315242172555250555 ) ) ;
#63457=CARTESIAN_POINT ( 'NONE',  ( 4.072732355924274295, -1.704239406772959153, -0.6552279023967975125 ) ) ;
#63463=CARTESIAN_POINT ( 'NONE',  ( 1.716098596715152746, 1.718394358364897068, 0.6617865747741287219 ) ) ;
#63464=CARTESIAN_POINT ( 'NONE',  ( 5.484640381798278952, -1.273743769317101648, 1.559065439997550762 ) ) ;
#63465=CARTESIAN_POINT ( 'NONE',  ( 5.766309430914762224, 2.125181855325126712, -0.8765443895848085143 ) ) ;
#63466=CARTESIAN_POINT ( 'NONE',  ( 5.418788444413384475, -1.423528547644649755, 1.350099487149841071 ) ) ;
#63471=CARTESIAN_POINT ( 'NONE',  ( 1.751626234865871767, 2.084932195785852649, -0.1569159079413025293 ) ) ;
#63472=CARTESIAN_POINT ( 'NONE',  ( 0.4615142869485132637, 1.850934062480696252, -0.2700578556205368574 ) ) ;
#63474=CARTESIAN_POINT ( 'NONE',  ( 6.351511478899689145, 1.936555568076937295, -0.1455203235936879114 ) ) ;
#63475=CARTESIAN_POINT ( 'NONE',  ( -0.1106727585415837045, 2.871245121144291090, -2.491938459964110120 ) ) ;
#63476=CARTESIAN_POINT ( 'NONE',  ( 0.9776059304600862587, -1.697647217183468449, -0.3827929467696991050 ) ) ;
#63480=CARTESIAN_POINT ( 'NONE',  ( 1.840065157383737438, 1.705764225012149859, 0.2551292777918309773 ) ) ;
#63481=CARTESIAN_POINT ( 'NONE',  ( 1.242012060539962492, 2.189267750446591609, 0.1026977899005257211 ) ) ;
#63482=CARTESIAN_POINT ( 'NONE',  ( -0.1405533004718754753, 0.003749010675345095921, -1.720146753850458010 ) ) ;
#63483=CARTESIAN_POINT ( 'NONE',  ( 4.143358556170802842, -1.920740624720223666, 1.086653567583625746 ) ) ;
#63485=CARTESIAN_POINT ( 'NONE',  ( 1.710090495726908966, 0.6328077935687204114, -2.076762233347277053 ) ) ;
#63487=CARTESIAN_POINT ( 'NONE',  ( 2.132168502032088409, 2.116975549207784635, 0.04667972686168975205 ) ) ;
#63490=CARTESIAN_POINT ( 'NONE',  ( 2.507732108623667688, -2.266951094411073786, 0.3397945559272512739 ) ) ;
#63492=CARTESIAN_POINT ( 'NONE',  ( 0.07755575628183571102, 2.860544851022389867, -2.677061994759164065 ) ) ;
#63495=CARTESIAN_POINT ( 'NONE',  ( 6.481102860290734569, -2.029466250747449685, -0.9033904549611364576 ) ) ;
#63503=CARTESIAN_POINT ( 'NONE',  ( 3.498672800139957406, -1.986100699840901651, 0.3474671148789992836 ) ) ;
#63505=CARTESIAN_POINT ( 'NONE',  ( 2.202078444200939789, 0.7933530804136761372, -1.904077301569401914 ) ) ;
#63511=CARTESIAN_POINT ( 'NONE',  ( 4.787173061057010237, 1.622617466453496471, 1.473133629693436975 ) ) ;
#63512=CARTESIAN_POINT ( 'NONE',  ( 2.022111496571117772, -1.799922141918413487, 0.9091460122201827643 ) ) ;
#63513=CARTESIAN_POINT ( 'NONE',  ( 1.944624168438695566, -1.479605912621816621, -1.095697124569312564 ) ) ;
#63517=CARTESIAN_POINT ( 'NONE',  ( 5.790036952090301448, -0.8187086143041850672, 1.631793460665122986 ) ) ;
#63519=CARTESIAN_POINT ( 'NONE',  ( 6.311172677262812059, 1.158691452862798954, -1.650079838712660063 ) ) ;
#63521=CARTESIAN_POINT ( 'NONE',  ( 5.805634902324096736, -0.5560928936223124008, 2.193004490925544392 ) ) ;
#63523=CARTESIAN_POINT ( 'NONE',  ( 1.172648168047723649, -1.334858166028422222, 1.629009436104215558 ) ) ;
#63532=CARTESIAN_POINT ( 'NONE',  ( 2.373529451608622054, -1.935128245189758012, -1.090680762624636868 ) ) ;
#63536=CARTESIAN_POINT ( 'NONE',  ( 3.051168888765115828, 1.684027830550902882, -1.006202029777767848 ) ) ;
#63542=CARTESIAN_POINT ( 'NONE',  ( 2.812858766682566181, -0.6196351552101020399, -2.028021595557969015 ) ) ;
#63544=CARTESIAN_POINT ( 'NONE',  ( 4.047864428982482110, 0.7307185629543844207, -2.034579650689218866 ) ) ;
#63545=CARTESIAN_POINT ( 'NONE',  ( 3.368544699895597461, 0.04196216268675251326, -1.840931771443871101 ) ) ;
#63548=CARTESIAN_POINT ( 'NONE',  ( 5.613164593121685364, -1.696513092703657799, 0.3873091720919922265 ) ) ;
#63549=CARTESIAN_POINT ( 'NONE',  ( 6.727182134110237577, 2.483225874290733159, 2.096421262816303255 ) ) ;
#63552=CARTESIAN_POINT ( 'NONE',  ( 2.694378501574711926, -2.155843008138720762, -0.1600555415394027403 ) ) ;
#63553=CARTESIAN_POINT ( 'NONE',  ( 4.095077249698628741, 1.080899603560569799, -1.701687522498253946 ) ) ;
#63555=CARTESIAN_POINT ( 'NONE',  ( 2.835029207381420502, 0.2633842809251253358, 2.145520918749081574 ) ) ;
#63556=CARTESIAN_POINT ( 'NONE',  ( 2.425019040235734558, -0.003784258722050458899, 1.971530340264670889 ) ) ;
#63558=CARTESIAN_POINT ( 'NONE',  ( 5.056170473960743372, -1.404048225252243265, 1.341958350743667205 ) ) ;
#63565=ORIENTED_EDGE ( 'NONE', *, *, #14173, .F. ) ;
#63567=CARTESIAN_POINT ( 'NONE',  ( 1.571597221169357628, 0.1616201177277211132, -2.200922231076734459 ) ) ;
#63570=CARTESIAN_POINT ( 'NONE',  ( 5.119951393648711324, 1.940949770148656661, -0.2839766199017114690 ) ) ;
#63575=CARTESIAN_POINT ( 'NONE',  ( 3.784953330938052751, 1.334695924059103644, 1.268461399425282909 ) ) ;
#63580=CARTESIAN_POINT ( 'NONE',  ( 6.029554895997981667, -0.2579198037528374066, 2.104758538420265168 ) ) ;
#63583=CARTESIAN_POINT ( 'NONE',  ( 6.889916301919797981, -0.8861221739737500380, 1.859037482098152338 ) ) ;
#63585=CARTESIAN_POINT ( 'NONE',  ( 1.381066672459789979, -0.05041352683890670816, 1.860554536023711458 ) ) ;
#63586=CARTESIAN_POINT ( 'NONE',  ( 4.036529152626888717, -1.599951230533543267, 0.9111318136766360931 ) ) ;
#63593=CARTESIAN_POINT ( 'NONE',  ( 2.789901687333019797, 1.561178712900921584, 1.560079944692857046 ) ) ;
#63594=CARTESIAN_POINT ( 'NONE',  ( 6.327429347084096101, -2.133486974870369313, 0.7532543551938327697 ) ) ;
#63596=CARTESIAN_POINT ( 'NONE',  ( 6.099861030166984222, 1.256130149795838813, 1.305615287863689078 ) ) ;
#63598=CARTESIAN_POINT ( 'NONE',  ( 5.788286065124909285, -0.6962570634414954052, -1.784894364769493924 ) ) ;
#63600=CARTESIAN_POINT ( 'NONE',  ( 5.910993886665249164, 1.650546521282238110, 0.8803886038859505270 ) ) ;
#63601=CARTESIAN_POINT ( 'NONE',  ( 6.057066403244290242, 1.520950583283819935, -1.072200347198979831 ) ) ;
#63603=CARTESIAN_POINT ( 'NONE',  ( 0.08069323953814251660, -0.1329233695197447052, -1.840450602299897431 ) ) ;
#63604=CARTESIAN_POINT ( 'NONE',  ( 1.499232818411553536, -0.2420282084563407654, 2.001858358113464575 ) ) ;
#63606=CARTESIAN_POINT ( 'NONE',  ( 3.035867697866540205, -1.414839191968674470, -1.560218430392734446 ) ) ;
#63611=CARTESIAN_POINT ( 'NONE',  ( 3.041275741140234246, 0.05373089442234183638, 2.019258232931480546 ) ) ;
#63615=CARTESIAN_POINT ( 'NONE',  ( 3.602937629199114866, 1.706465849011790104, -1.326752773236601346 ) ) ;
#63621=CARTESIAN_POINT ( 'NONE',  ( 0.7487581336349375949, -2.154818914559033072, -0.2656684361399003214 ) ) ;
#63626=CARTESIAN_POINT ( 'NONE',  ( 2.437293137456029157, -1.626093413141915134, -1.469474007205706645 ) ) ;
#63628=CARTESIAN_POINT ( 'NONE',  ( 2.747247497433321861, -1.881545503785379436, 1.256212651835092231 ) ) ;
#63635=CARTESIAN_POINT ( 'NONE',  ( 3.110363945789674123, 1.284354398739546266, -1.217803596734900573 ) ) ;
#63637=CARTESIAN_POINT ( 'NONE',  ( 5.948300505803370442, 2.203960110721484789, 0.1139900122707343255 ) ) ;
#63642=CARTESIAN_POINT ( 'NONE',  ( 3.572993900519233712, 0.04689164532409998559, -1.870237235490713079 ) ) ;
#63643=CARTESIAN_POINT ( 'NONE',  ( 3.432542862244458259, -1.236986750340131724, 1.659893174209552846 ) ) ;
#63652=CARTESIAN_POINT ( 'NONE',  ( 1.283307755816986528, 0.1377011610334301639, -1.907463248872851347 ) ) ;
#63653=CARTESIAN_POINT ( 'NONE',  ( 2.646866301197240645, -0.3325320220872363675, -1.933311746529025266 ) ) ;
#63654=CARTESIAN_POINT ( 'NONE',  ( 1.264999722075825561, -2.016288307338756525, -0.002813990012486000669 ) ) ;
#63658=CARTESIAN_POINT ( 'NONE',  ( 6.889933812677610625, -0.8438472966565238043, 1.779621742589713618 ) ) ;
#63660=CARTESIAN_POINT ( 'NONE',  ( 1.406495263175694399, -2.003875642784687994, -0.1933051647188162026 ) ) ;
#63662=CARTESIAN_POINT ( 'NONE',  ( 2.741944773236061117, 2.106750310803459758, -0.2105854985169057503 ) ) ;
#63664=CARTESIAN_POINT ( 'NONE',  ( 3.385274849524767316, 0.04804411014160993310, 2.069964801482151895 ) ) ;
#63666=CARTESIAN_POINT ( 'NONE',  ( 6.246049398119083662, 0.6547385654485110562, 1.985528007121174943 ) ) ;
#63668=CARTESIAN_POINT ( 'NONE',  ( 4.084828617465196210, -0.1788469021064206521, -1.816781805555576668 ) ) ;
#63673=CARTESIAN_POINT ( 'NONE',  ( 6.352570083819033542, 0.6862697483850827007, 2.097430819677794656 ) ) ;
#63675=CARTESIAN_POINT ( 'NONE',  ( 5.338497774373327509, 1.135723818413657549, -1.538349510941657838 ) ) ;
#63681=CARTESIAN_POINT ( 'NONE',  ( 0.4152503475762689411, -0.9843521281015167324, -1.555853522519357712 ) ) ;
#63683=CARTESIAN_POINT ( 'NONE',  ( 4.182764291190976813, -0.1809548918480126112, -1.861743760598027597 ) ) ;
#63684=CARTESIAN_POINT ( 'NONE',  ( -0.02319159430947368913, 6.948789054712430691, -2.406029888528108618 ) ) ;
#63692=CARTESIAN_POINT ( 'NONE',  ( 0.9538786243144499188, -0.7140540310214549269, 1.835613268467409576 ) ) ;
#63693=CARTESIAN_POINT ( 'NONE',  ( 2.794546173781168541, 1.458544728081469177, -1.392559875802508396 ) ) ;
#63697=CARTESIAN_POINT ( 'NONE',  ( 2.080269975650438585, -2.149535124392497831, -0.4257020960420563882 ) ) ;
#63699=CARTESIAN_POINT ( 'NONE',  ( 6.825078400183570260, 4.696493799637426747, 2.518305144748238966 ) ) ;
#63705=CARTESIAN_POINT ( 'NONE',  ( 5.337399561049260832, 0.7408347518493042516, -1.685818907712175019 ) ) ;
#63706=CARTESIAN_POINT ( 'NONE',  ( 1.664698924820615433, 0.6334283372178346472, 1.910891431425953302 ) ) ;
#63707=CARTESIAN_POINT ( 'NONE',  ( 3.128558558221442354, 0.3401759809690939051, -2.272988164180503201 ) ) ;
#63709=CARTESIAN_POINT ( 'NONE',  ( 2.324856365976185391, -1.699136111967664453, -0.7594513203179918959 ) ) ;
#63712=CARTESIAN_POINT ( 'NONE',  ( 5.994389040191065554, -1.017321598621454548, 1.619163160827830517 ) ) ;
#63715=CARTESIAN_POINT ( 'NONE',  ( 4.968349523292523884, -1.969100025901071360, -0.7031758509000278767 ) ) ;
#63716=CARTESIAN_POINT ( 'NONE',  ( 3.660894226558962128, -1.649352935060313552, -0.8826137995501317501 ) ) ;
#63718=CARTESIAN_POINT ( 'NONE',  ( 6.392148736875968851, -0.4980823202534767624, -1.772533436741857260 ) ) ;
#63721=CARTESIAN_POINT ( 'NONE',  ( 5.057137062068671973, -1.459852279745242010, -0.9183987515692086934 ) ) ;
#63725=CARTESIAN_POINT ( 'NONE',  ( 4.364261492936694076, -2.165649721281979190, 0.1538544128360258556 ) ) ;
#63726=CARTESIAN_POINT ( 'NONE',  ( 3.510199737632841543, -0.7410081052188906003, -1.668730646197075673 ) ) ;
#63727=CARTESIAN_POINT ( 'NONE',  ( 1.604273143990111672, 1.959273547513197711, 0.1016356785708133759 ) ) ;
#63728=CARTESIAN_POINT ( 'NONE',  ( 0.2810647479330531939, 1.757583132164267647, -1.180221762011339326 ) ) ;
#63729=CARTESIAN_POINT ( 'NONE',  ( 6.480031627576305020, -2.247188937338239434, -0.4521185302251101157 ) ) ;
#63734=CARTESIAN_POINT ( 'NONE',  ( 2.578903501431661915, -1.460476376761214556, 1.537597662120089081 ) ) ;
#63736=CLOSED_SHELL ( 'NONE', ( #172437, #78294, #160656, #34764, #101479, #64064, #45767, #34888 ) ) ;
#63738=CARTESIAN_POINT ( 'NONE',  ( 0.2392000317489213768, -0.1454578200970526591, -2.037356452166842580 ) ) ;
#63739=CARTESIAN_POINT ( 'NONE',  ( 6.883263157960330503, 7.629137130509037412, 2.553810918356711479 ) ) ;
#63741=CARTESIAN_POINT ( 'NONE',  ( 2.614199364429617756, -0.6941352821057051870, 2.110140411616817868 ) ) ;
#63743=CARTESIAN_POINT ( 'NONE',  ( 0.1593517250534680629, 1.330572521919655360, 1.874314102060254505 ) ) ;
#63745=CARTESIAN_POINT ( 'NONE',  ( 5.717653809678179044, 0.4078037869292486239, -2.021697613586806774 ) ) ;
#63750=CARTESIAN_POINT ( 'NONE',  ( 0.1331565106231328566, 1.371277436080810208, -2.201942895618694607 ) ) ;
#63751=CARTESIAN_POINT ( 'NONE',  ( 5.495603940606402560, -1.841430844871448258, 0.006098274996368944698 ) ) ;
#63754=CARTESIAN_POINT ( 'NONE',  ( 1.904884197260014567, 1.431573929998239958, 0.9616530215695131556 ) ) ;
#63755=CARTESIAN_POINT ( 'NONE',  ( 1.622280145275534435, 1.995268681201247452, 0.2910785328335343536 ) ) ;
#63756=CARTESIAN_POINT ( 'NONE',  ( 2.268584743917153368, 2.099868620093465754, -0.9355518099330699666 ) ) ;
#63758=CARTESIAN_POINT ( 'NONE',  ( 1.968429645022830465, 1.162096202078844120, 1.940986467279571359 ) ) ;
#63759=CARTESIAN_POINT ( 'NONE',  ( 4.301466803424673913, 1.691180239654224815, 1.254954771472403641 ) ) ;
#63761=CARTESIAN_POINT ( 'NONE',  ( 2.846658922380195911, -1.473647421164023141, 0.9796213258056789552 ) ) ;
#63764=CARTESIAN_POINT ( 'NONE',  ( 5.636350782834250062, 0.4440221345313396517, 2.248805093627189500 ) ) ;
#63767=CARTESIAN_POINT ( 'NONE',  ( 6.117462548578989967, 1.846355941783444976, 1.234888080409371369 ) ) ;
#63768=CARTESIAN_POINT ( 'NONE',  ( 4.365290731249091394, 2.125951747006165959, -0.5312598475561494116 ) ) ;
#63771=CARTESIAN_POINT ( 'NONE',  ( 6.604144390287855160, -0.9070803646254663732, 1.914764756563241965 ) ) ;
#63772=( BOUNDED_SURFACE ( )  B_SPLINE_SURFACE ( 3, 3, ( 
 ( #57961, #124126, #190088, #92631, #41741, #107852, #173878, #5979, #157615, #72050, #25452 ),
 ( #141397, #207407, #55825, #125184, #108918, #174940, #26522, #158672, #10269, #121981, #95827 ),
 ( #94757, #194363, #143527, #213777, #49192, #131547, #197548, #160806, #15587, #130514, #178128 ),
 ( #144595, #78476, #96897, #195442, #176001, #12397, #128396, #79547, #209523, #46005, #161884 ),
 ( #48145, #111048, #62237, #113189, #179195, #210609, #147760, #145665, #14526, #30818, #162946 ),
 ( #177055, #212730, #77411, #97956, #27593, #28672, #61164, #81674, #13471, #112124, #211663 ),
 ( #93691, #127326, #80623, #29744, #164012, #47072, #159734, #146713, #63299, #11332, #193296 ) ),
 .UNSPECIFIED., .T., .F., .F. ) 
 B_SPLINE_SURFACE_WITH_KNOTS ( ( 4, 3, 4 ),
 ( 4, 1, 1, 1, 1, 1, 1, 1, 4 ),
 ( 0.000000000000000000, 0.5000000000000000000, 1.000000000000000000 ),
 ( 0.000000000000000000, 0.2256337125576066971, 0.3978389261578171299, 0.5257960283851228489, 0.6187025735204009225, 0.6856790771877526725, 0.7354782194756434022, 0.7762620033627533056, 0.9999999999999998890 ),
 .UNSPECIFIED. ) 
 GEOMETRIC_REPRESENTATION_ITEM ( )  RATIONAL_B_SPLINE_SURFACE ( (
 ( 1.000000000000000000, 1.000000000000000000, 1.000000000000000222, 1.000000000000000000, 0.9999999999999997780, 1.000000000000000222, 0.9999999999999997780, 1.000000000000000222, 0.9999999999999992228, 1.000000000000000000, 1.000000000000000000),
 ( 0.3333333333333333703, 0.3333333333333334259, 0.3333333333333334259, 0.3333333333333333703, 0.3333333333333333148, 0.3333333333333334259, 0.3333333333333333703, 0.3333333333333334259, 0.3333333333333330928, 0.3333333333333333703, 0.3333333333333333703),
 ( 0.3333333333333333703, 0.3333333333333334259, 0.3333333333333334259, 0.3333333333333333703, 0.3333333333333333148, 0.3333333333333334259, 0.3333333333333333703, 0.3333333333333334259, 0.3333333333333330928, 0.3333333333333333703, 0.3333333333333333703),
 ( 1.000000000000000000, 1.000000000000000000, 1.000000000000000222, 1.000000000000000000, 0.9999999999999997780, 1.000000000000000222, 0.9999999999999997780, 1.000000000000000222, 0.9999999999999992228, 1.000000000000000000, 1.000000000000000000),
 ( 0.3333333333333333703, 0.3333333333333334259, 0.3333333333333334259, 0.3333333333333333703, 0.3333333333333333148, 0.3333333333333334259, 0.3333333333333333703, 0.3333333333333334259, 0.3333333333333330928, 0.3333333333333333703, 0.3333333333333333703),
 ( 0.3333333333333333703, 0.3333333333333334259, 0.3333333333333334259, 0.3333333333333333703, 0.3333333333333333148, 0.3333333333333334259, 0.3333333333333333703, 0.3333333333333334259, 0.3333333333333330928, 0.3333333333333333703, 0.3333333333333333703),
 ( 1.000000000000000000, 1.000000000000000000, 1.000000000000000222, 1.000000000000000000, 0.9999999999999997780, 1.000000000000000222, 0.9999999999999997780, 1.000000000000000222, 0.9999999999999992228, 1.000000000000000000, 1.000000000000000000) ) ) 
 REPRESENTATION_ITEM ( '' )  SURFACE ( )  );
#63776=CARTESIAN_POINT ( 'NONE',  ( 5.994406619193555663, -1.133004004027007294, 1.792352430775605798 ) ) ;
#63782=CARTESIAN_POINT ( 'NONE',  ( 5.671403949121008203, 1.101820082107987098, 1.475039313902235305 ) ) ;
#63786=CARTESIAN_POINT ( 'NONE',  ( 1.733560280482333571, 1.721479560191770730, 0.2551580012965410371 ) ) ;
#63788=CARTESIAN_POINT ( 'NONE',  ( 0.1390251588108057101, -0.1389306544097475005, -1.930426113910483688 ) ) ;
#63791=CARTESIAN_POINT ( 'NONE',  ( 6.315313271410192719, -0.2696487299426887363, 2.144762774094311375 ) ) ;
#63795=CARTESIAN_POINT ( 'NONE',  ( 5.770447993230207295, -1.374857387916775364, 1.668144713590607120 ) ) ;
#63799=CARTESIAN_POINT ( 'NONE',  ( 5.800065155369113157, -1.971530342684927772, -0.002616305567698303924 ) ) ;
#63800=CARTESIAN_POINT ( 'NONE',  ( 5.360564742968721319, -0.6223997329263281086, 1.618453672356393147 ) ) ;
#63802=CARTESIAN_POINT ( 'NONE',  ( 1.400213348495438437, -0.7931047570679079506, -2.043190674350242819 ) ) ;
#63803=CARTESIAN_POINT ( 'NONE',  ( 3.839178312322106823, 0.3354718084071331430, 2.282954970297036201 ) ) ;
#63804=CARTESIAN_POINT ( 'NONE',  ( 5.466112512051848782, 1.011855222795062348, 1.795159749414678929 ) ) ;
#63805=CARTESIAN_POINT ( 'NONE',  ( 1.130689739129210336, -1.755767597885007136, 0.8300169520328912753 ) ) ;
#63809=CARTESIAN_POINT ( 'NONE',  ( 3.515986968957810266, -0.6120941298391362473, 2.030368431519948391 ) ) ;
#63811=CARTESIAN_POINT ( 'NONE',  ( 2.057267738415057057, -1.238319999287675888, 1.591319116112683618 ) ) ;
#63813=CARTESIAN_POINT ( 'NONE',  ( 4.436686946050734548, 2.163524548302516060, 0.4339203326570104102 ) ) ;
#63824=CARTESIAN_POINT ( 'NONE',  ( 3.942301955389547974, 2.050809467686238285, 0.2036389587714466376 ) ) ;
#63830=CARTESIAN_POINT ( 'NONE',  ( 3.633467297704314980, -0.1462457305761339643, 2.014424004083538833 ) ) ;
#63834=CARTESIAN_POINT ( 'NONE',  ( 3.274343757225039120, -1.228935477529419451, 1.654214949985348904 ) ) ;
#63838=CARTESIAN_POINT ( 'NONE',  ( 1.675478281319711549, -0.9859397310463119402, 1.554705294492392254 ) ) ;
#63840=CARTESIAN_POINT ( 'NONE',  ( 0.03047818801908425135, -1.425887938121385590, -1.815451699675968644 ) ) ;
#63842=CARTESIAN_POINT ( 'NONE',  ( 2.601032539102793084, 1.737798908178284307, -1.285340053188685383 ) ) ;
#63844=CARTESIAN_POINT ( 'NONE',  ( 4.048151681910251654, 1.001636719310808887, 1.865476516996619649 ) ) ;
#63845=CARTESIAN_POINT ( 'NONE',  ( 2.935265884076414977, 1.227738246725296634, 1.942841054583419602 ) ) ;
#63847=CARTESIAN_POINT ( 'NONE',  ( 0.9009904985227291663, 1.526999960511504772, 1.080287613699250304 ) ) ;
#63848=CARTESIAN_POINT ( 'NONE',  ( 4.328955620115590541, 0.09577655398496780215, 1.969249263103334702 ) ) ;
#63850=CARTESIAN_POINT ( 'NONE',  ( 4.803922858132807505, -1.082837210388952309, -1.700963621564715700 ) ) ;
#63854=CARTESIAN_POINT ( 'NONE',  ( 5.742829910930518977, 0.4094298153964996967, 2.065706902019475599 ) ) ;
#63855=CARTESIAN_POINT ( 'NONE',  ( 6.549288556030710140, 1.803345607721940524, -1.016871928424132099 ) ) ;
#63858=CARTESIAN_POINT ( 'NONE',  ( 6.639320575229288757, 4.694344378759712555, 2.565881548192010975 ) ) ;
#63859=CARTESIAN_POINT ( 'NONE',  ( 4.961777154302105863, 1.950117994852887282, -0.2885197095366370257 ) ) ;
#63860=CARTESIAN_POINT ( 'NONE',  ( 6.275650217586050239, 0.3411474428106214263, -1.990588700022011714 ) ) ;
#63862=CARTESIAN_POINT ( 'NONE',  ( 4.881611394917170443, 2.154576904714616603, -0.8270325966449257882 ) ) ;
#63864=CARTESIAN_POINT ( 'NONE',  ( 2.307554651200398599, -1.654038752482372088, -1.231991790176652612 ) ) ;
#63871=CARTESIAN_POINT ( 'NONE',  ( 3.895131827238162536, 0.3151296210822142063, 2.148063795774640461 ) ) ;
#63874=CARTESIAN_POINT ( 'NONE',  ( 2.964219115174483665, -1.702287218311925310, -0.7022057971969236645 ) ) ;
#63877=CARTESIAN_POINT ( 'NONE',  ( 5.372676843235411503, -0.05303982195071360595, -2.191091664329389399 ) ) ;
#63879=CARTESIAN_POINT ( 'NONE',  ( 6.455986150183742112, 2.257016316038124693, -0.1587017259171065731 ) ) ;
#63884=CARTESIAN_POINT ( 'NONE',  ( 6.362547694819080668, -1.249765848162401438, 1.253281529121505589 ) ) ;
#63885=CARTESIAN_POINT ( 'NONE',  ( 4.459639246686514902, -1.557681092447872784, -1.275236256583739403 ) ) ;
#63887=CARTESIAN_POINT ( 'NONE',  ( 2.749164281075014760, -1.751614713500139198, 1.168827980950073009 ) ) ;
#63888=CARTESIAN_POINT ( 'NONE',  ( 2.601083430876732105, -0.1850255667073404386, 1.906624535778883578 ) ) ;
#63890=CARTESIAN_POINT ( 'NONE',  ( 3.684007040126308752, -1.171275171843730867, -1.583282632743492790 ) ) ;
#63891=CARTESIAN_POINT ( 'NONE',  ( 1.604156678829884886, -0.6703249191640224813, -1.746612230856612769 ) ) ;
#63892=CARTESIAN_POINT ( 'NONE',  ( 2.418345249890076154, 0.8361516037145629854, 1.774881043358336630 ) ) ;
#63893=CARTESIAN_POINT ( 'NONE',  ( 3.598037535421601429, -1.723020282968828809, -0.08274337828741322454 ) ) ;
#63894=CARTESIAN_POINT ( 'NONE',  ( 0.3340484552533556362, -1.024938778295768849, -1.614363347046356756 ) ) ;
#63896=CARTESIAN_POINT ( 'NONE',  ( 1.717678464306471309, -0.2677704892378242607, 2.190511422692428045 ) ) ;
#63902=CARTESIAN_POINT ( 'NONE',  ( 6.877786287229037399, -2.009644702432196617, 0.4970176993947388322 ) ) ;
#63904=CARTESIAN_POINT ( 'NONE',  ( 1.416557266959647787, 0.8372786474034592530, 1.893679232998768391 ) ) ;
#63909=CARTESIAN_POINT ( 'NONE',  ( 5.461630201184114242, -1.671734486004393450, -1.304435072541964447 ) ) ;
#63913=CARTESIAN_POINT ( 'NONE',  ( 6.443807124430430910, 1.351966286592180211, 1.421895456074427688 ) ) ;
#63915=CARTESIAN_POINT ( 'NONE',  ( 3.813827237909522605, -1.649828814528127907, 1.158511658058670957 ) ) ;
#63916=CARTESIAN_POINT ( 'NONE',  ( 4.047977829471119726, 0.9080738158676031624, 1.686857792009839097 ) ) ;
#63918=CARTESIAN_POINT ( 'NONE',  ( 1.716621854089026344, 2.046377219401524616, 0.7848826361863748824 ) ) ;
#63921=CARTESIAN_POINT ( 'NONE',  ( 4.974862723197266412, -1.455255168294814272, 1.391337642457886270 ) ) ;
#63924=CARTESIAN_POINT ( 'NONE',  ( 5.800440434243619769, 1.421441630026821112, -1.569310636533404635 ) ) ;
#63926=CARTESIAN_POINT ( 'NONE',  ( 2.560199545759346496, -1.439800679921798165, 1.516228354532923372 ) ) ;
#63928=CARTESIAN_POINT ( 'NONE',  ( 0.3578718668165404293, 0.6529773653428347924, 1.596609206317510132 ) ) ;
#63933=SURFACE_STYLE_FILL_AREA ( #62863 ) ;
#63941=CARTESIAN_POINT ( 'NONE',  ( 1.875370188833940244, 0.3090493442242334132, -1.784726349569294213 ) ) ;
#63950=CARTESIAN_POINT ( 'NONE',  ( 3.191705266286504639, -1.248028223939607884, -1.380750640708436006 ) ) ;
#63951=CARTESIAN_POINT ( 'NONE',  ( 0.7904806358284102163, 1.449672126929082872, -1.252262404471200075 ) ) ;
#63952=CARTESIAN_POINT ( 'NONE',  ( 6.633821588623410648, -1.258873362295178655, -1.458256629947017879 ) ) ;
#63961=CARTESIAN_POINT ( 'NONE',  ( 4.785976182654667177, -1.208483435658064487, -1.555025035033012148 ) ) ;
#63962=CARTESIAN_POINT ( 'NONE',  ( 1.383610671357866639, 0.1525377206293351273, -2.115047022047947589 ) ) ;
#63966=CARTESIAN_POINT ( 'NONE',  ( 5.578137875217415775, -2.137416510240647494, -0.4829537091169676666 ) ) ;
#63968=CARTESIAN_POINT ( 'NONE',  ( 5.350583055395741638, 0.5590458624239265095, 1.843501136262601037 ) ) ;
#63970=CARTESIAN_POINT ( 'NONE',  ( 0.09436191691250192526, -0.3928898508825870439, -1.789253991261535726 ) ) ;
#63971=CARTESIAN_POINT ( 'NONE',  ( 1.120068590173186163, -2.152398693614396397, 0.4866647226241942459 ) ) ;
#63973=CARTESIAN_POINT ( 'NONE',  ( -0.2108831679770960255, -0.001785917861228669690, -1.896958272444612792 ) ) ;
#63978=CARTESIAN_POINT ( 'NONE',  ( 6.086760365903021608, 1.896989206666617633, 0.5289026096024685986 ) ) ;
#63979=CARTESIAN_POINT ( 'NONE',  ( 1.927192517792934101, -1.269957001497720395, -1.469349730274618571 ) ) ;
#63981=CARTESIAN_POINT ( 'NONE',  ( 0.9837497097957871306, 1.861730512597782550, 0.7742002051285418185 ) ) ;
#63983=CARTESIAN_POINT ( 'NONE',  ( 5.963677626732073023, -0.4536248188283693583, 1.804646041804882195 ) ) ;
#63989=CARTESIAN_POINT ( 'NONE',  ( 1.997856853652695497, -2.190977152517746163, 0.05759783203293508680 ) ) ;
#63993=CARTESIAN_POINT ( 'NONE',  ( 1.224926655537651676, -0.04696546880481740349, 1.825250005322680780 ) ) ;
#63996=CARTESIAN_POINT ( 'NONE',  ( 6.609000000000047947, 7.052356515605485932, 2.698153947863399793 ) ) ;
#63999=CARTESIAN_POINT ( 'NONE',  ( 6.674438497507635404, -1.118711561685633349, 1.443368817030561635 ) ) ;
#64000=CARTESIAN_POINT ( 'NONE',  ( 5.014483083204026137, 0.7471541359172823027, 1.814103259000845680 ) ) ;
#64004=CARTESIAN_POINT ( 'NONE',  ( 3.404031855413204966, -0.8899279105200922357, -2.002928011436304612 ) ) ;
#64007=CARTESIAN_POINT ( 'NONE',  ( 3.696198088285786998, 0.9351842759567146057, -1.847102243037239910 ) ) ;
#64011=CARTESIAN_POINT ( 'NONE',  ( 3.727375017909192234, 2.287664543646179105, 0.2247039424928508056 ) ) ;
#64015=CARTESIAN_POINT ( 'NONE',  ( 6.620655732516649294, 2.985444497229528427, 2.280274006979409407 ) ) ;
#64017=CARTESIAN_POINT ( 'NONE',  ( 4.136618238866495822, -1.688923885309162376, 0.9583718017313649362 ) ) ;
#64018=ORIENTED_EDGE ( 'NONE', *, *, #47626, .F. ) ;
#64022=CARTESIAN_POINT ( 'NONE',  ( 3.797043250571481732, -0.1924442655423033721, -1.902711443722324258 ) ) ;
#64024=CARTESIAN_POINT ( 'NONE',  ( 5.227475398614537916, -1.636741361296644603, 0.5442337529403593610 ) ) ;
#64025=CARTESIAN_POINT ( 'NONE',  ( 4.259000112335223243, -0.004834882008357410665, -2.016708403958865414 ) ) ;
#64026=CARTESIAN_POINT ( 'NONE',  ( 5.133504205653830255, 0.6649215086056580182, 2.200401518963719383 ) ) ;
#64028=CARTESIAN_POINT ( 'NONE',  ( 1.190363680384380229, -0.9894552095768920363, 1.972713631218452557 ) ) ;
#64031=CARTESIAN_POINT ( 'NONE',  ( 6.344957943996793581, -1.493715166628902580, 0.9487403735100213842 ) ) ;
#64033=CARTESIAN_POINT ( 'NONE',  ( 2.502247188656173016, -0.8787990176886916194, -2.117303525603573267 ) ) ;
#64034=CARTESIAN_POINT ( 'NONE',  ( 1.306181984371343585, 1.533458449073618057, 0.8229166363448844335 ) ) ;
#64037=CARTESIAN_POINT ( 'NONE',  ( 1.334805274328724867, -1.105471761691357191, 1.335692278477951689 ) ) ;
#64040=CARTESIAN_POINT ( 'NONE',  ( 1.469425047783163407, 1.914459939344328010, 1.024175319008380658 ) ) ;
#64041=CARTESIAN_POINT ( 'NONE',  ( 2.483611571103708116, -0.6279893487078171965, 1.916353726171161620 ) ) ;
#64043=CARTESIAN_POINT ( 'NONE',  ( 0.09454951164026764721, -0.4206464163897213893, -1.887090839307656864 ) ) ;
#64045=CARTESIAN_POINT ( 'NONE',  ( 2.391161334010579509, -2.127237363102509882, -0.6400520371602820280 ) ) ;
#64053=CARTESIAN_POINT ( 'NONE',  ( 5.056098682708163317, -1.255628792201430644, 1.205468413292756669 ) ) ;
#64054=CARTESIAN_POINT ( 'NONE',  ( 3.121486724888074882, 0.2905151309811822569, -1.940125473959073421 ) ) ;
#64058=CARTESIAN_POINT ( 'NONE',  ( 5.132209903004834928, 1.169260703421838743, -1.936728657785217411 ) ) ;
#64059=CARTESIAN_POINT ( 'NONE',  ( 1.363816705371086568, -0.5030291501087379435, 2.000271598109978566 ) ) ;
#64061=CARTESIAN_POINT ( 'NONE',  ( 2.044175283654376951, 0.8654258166664110519, -2.090645895884978955 ) ) ;
#64064=ADVANCED_FACE ( 'NONE', ( #176936 ), #125216, .T. ) ;
#64065=CARTESIAN_POINT ( 'NONE',  ( 2.969827553264007047, 0.9974664638083343693, 1.582205488144486250 ) ) ;
#64066=CARTESIAN_POINT ( 'NONE',  ( 1.933800834616914877, -1.393042465158848886, -1.032573028607612464 ) ) ;
#64067=CARTESIAN_POINT ( 'NONE',  ( 5.794512526436308875, 1.792401445336734733, -1.260760892635464980 ) ) ;
#64068=CARTESIAN_POINT ( 'NONE',  ( 6.809642309899604840, -0.5188996100353564511, 2.257106211077652969 ) ) ;
#64069=CARTESIAN_POINT ( 'NONE',  ( 4.311504812833309330, -0.3723461477018601973, 2.129241309423899775 ) ) ;
#64070=CARTESIAN_POINT ( 'NONE',  ( 4.558499613049934673, -1.735246752265024561, -0.8719658702049468690 ) ) ;
#64074=CARTESIAN_POINT ( 'NONE',  ( 1.031250000000000888, -0.7852924748300426083, -1.895863743164066584 ) ) ;
#64079=CARTESIAN_POINT ( 'NONE',  ( 5.713517581197447015, 1.944070655204039433, 0.5350908816983344085 ) ) ;
#64083=CARTESIAN_POINT ( 'NONE',  ( 3.756323439517950558, 0.6585720284536450420, 1.702948436616057881 ) ) ;
#64092=CARTESIAN_POINT ( 'NONE',  ( 0.1584709747761771925, 2.014675524564497167, 0.1441611394625528231 ) ) ;
#64093=CARTESIAN_POINT ( 'NONE',  ( 1.049659257133638945, -1.915429643647760249, 0.9100379840868355608 ) ) ;
#64098=CARTESIAN_POINT ( 'NONE',  ( 6.561407802241105536, 0.3549014609278942078, -2.029936712941163623 ) ) ;
#64099=CARTESIAN_POINT ( 'NONE',  ( 6.434220164165640021, -1.621181005584397372, -1.198863592720422977 ) ) ;
#64108=CARTESIAN_POINT ( 'NONE',  ( 6.274767501101933043, -2.001204493855372579, 0.2439949869823473949 ) ) ;
#64109=CARTESIAN_POINT ( 'NONE',  ( 4.892441406782115365, 1.528958278715689234, -1.025397978904031060 ) ) ;
#64110=CARTESIAN_POINT ( 'NONE',  ( -0.02299388927988129522, 0.2517100516001030686, -1.946460665317284011 ) ) ;
#64111=CARTESIAN_POINT ( 'NONE',  ( 3.246982502279437188, 0.5605648102574630753, 2.238460633888791573 ) ) ;
#64113=CARTESIAN_POINT ( 'NONE',  ( 6.151685507011436904, 0.6340151041426717038, -2.066508600247290328 ) ) ;
#64115=CARTESIAN_POINT ( 'NONE',  ( 1.206472709818911637, 1.713414686832109179, 0.9141866466196489904 ) ) ;
#64118=CARTESIAN_POINT ( 'NONE',  ( 4.921405902946369260, 0.8734970824106644827, 2.126109943308290617 ) ) ;
#64122=CARTESIAN_POINT ( 'NONE',  ( 4.399188623838041323, 1.502396186649012311, 1.114296746780506497 ) ) ;
#64123=CARTESIAN_POINT ( 'NONE',  ( 1.265713261412576562, 0.5522810963098608861, -1.830935845731461953 ) ) ;
#64126=CARTESIAN_POINT ( 'NONE',  ( 3.229339687698820072, 0.05429069646168545316, 2.206380697113208722 ) ) ;
#64127=CARTESIAN_POINT ( 'NONE',  ( 6.883263157960371359, 6.037760411968411844, 2.441088155713948549 ) ) ;
#64132=CARTESIAN_POINT ( 'NONE',  ( 2.178924785135676334, -0.09298872875643586500, -1.969266502737290425 ) ) ;
#64133=CARTESIAN_POINT ( 'NONE',  ( 0.7105614292102403473, -2.296071549169254489, 0.2300874200455073904 ) ) ;
#64134=CARTESIAN_POINT ( 'NONE',  ( 1.715213470010600538, -1.680963409367957295, -1.011360081469035999 ) ) ;
#64135=CARTESIAN_POINT ( 'NONE',  ( 5.524308913217452321, 1.011932313297726038, 1.797175476313887188 ) ) ;
#64142=CARTESIAN_POINT ( 'NONE',  ( 1.358521007292138538, -2.171239805896512554, -0.002410242577662382712 ) ) ;
#64144=CARTESIAN_POINT ( 'NONE',  ( 5.812015183962491172, 1.231757822100377320, -1.368757117762291253 ) ) ;
#64148=CARTESIAN_POINT ( 'NONE',  ( 1.827212670807505379, -1.763035892288829620, 0.6254473451912796467 ) ) ;
#64149=CARTESIAN_POINT ( 'NONE',  ( 6.257120919624137301, -1.850417449585840313, -1.117149918570578437 ) ) ;
#64151=CARTESIAN_POINT ( 'NONE',  ( -0.02264175331116376200, 2.864903628641465971, -2.577409799940860946 ) ) ;
#64153=CARTESIAN_POINT ( 'NONE',  ( 2.156764536687346467, 0.4205103164258168769, 1.865301821287323136 ) ) ;
#64154=CARTESIAN_POINT ( 'NONE',  ( 4.240886712856615226, -1.539575280908970223, 0.8727758839858139606 ) ) ;
#64155=STYLED_ITEM ( 'NONE', ( #100694 ), #94059 ) ;
#64156=CARTESIAN_POINT ( 'NONE',  ( 0.3637282827039616251, 0.5997036651611362679, -1.815894722023647656 ) ) ;
#64159=CARTESIAN_POINT ( 'NONE',  ( 5.044510182127093678, -1.384340171167136369, 1.324308159167127075 ) ) ;
#64160=CARTESIAN_POINT ( 'NONE',  ( 6.496546994228061145, 1.947915994809066076, 0.2903317952503216559 ) ) ;
#64162=CARTESIAN_POINT ( 'NONE',  ( 2.197662576721173266, 1.936918166296027977, -0.8637449004969055544 ) ) ;
#64163=CARTESIAN_POINT ( 'NONE',  ( 5.119927267529915227, -1.001353885182048931, -1.579878405157906673 ) ) ;
#64164=CARTESIAN_POINT ( 'NONE',  ( 0.2229205655521030172, -0.09321834626660817358, 1.823428419517532983 ) ) ;
#64166=CARTESIAN_POINT ( 'NONE',  ( 4.793709216081707858, 1.633822259641436903, 1.483752339651790653 ) ) ;
#64169=CARTESIAN_POINT ( 'NONE',  ( 1.680209433476518521, -1.144093268944153641, -1.716113171863597797 ) ) ;
#64177=CARTESIAN_POINT ( 'NONE',  ( 6.398695753475230674, -1.876852914212179035, -0.3660984893600614520 ) ) ;
#64179=CARTESIAN_POINT ( 'NONE',  ( 4.176279081494421952, -1.061646348645030713, -1.777293304589353085 ) ) ;
#64181=CARTESIAN_POINT ( 'NONE',  ( 1.581558009922879204, 1.997867266642009643, -0.8257073301623578665 ) ) ;
#64183=CARTESIAN_POINT ( 'NONE',  ( 2.069016002695713397, -1.559697248980717266, 1.283103002569847106 ) ) ;
#64191=CARTESIAN_POINT ( 'NONE',  ( 0.5148617154710420918, 0.1531739628206352510, 2.010800830040265996 ) ) ;
#64192=CARTESIAN_POINT ( 'NONE',  ( 4.634432875810733599, 0.3748786239917040186, 2.159109584303263940 ) ) ;
#64194=CARTESIAN_POINT ( 'NONE',  ( 4.447458312869024155, -1.746245811230531908, 0.7801085911468000900 ) ) ;
#64198=CARTESIAN_POINT ( 'NONE',  ( 2.530875249677287719, -1.674875632724934338, 1.122518345125958383 ) ) ;
#64200=CARTESIAN_POINT ( 'NONE',  ( 0.06458782335966220534, -1.490751515076127465, 1.741559778653593238 ) ) ;
#64202=CARTESIAN_POINT ( 'NONE',  ( 4.963727558602625933, 1.705580761961351444, -0.2555711148431466517 ) ) ;
#64203=CARTESIAN_POINT ( 'NONE',  ( -0.1394461523061195918, 0.2309855492786689335, -2.314897844796594661 ) ) ;
#64207=CARTESIAN_POINT ( 'NONE',  ( 0.2685318824256071601, -0.8817220219094963340, -1.871193708407721035 ) ) ;
#64209=CARTESIAN_POINT ( 'NONE',  ( 5.268131585227527225, 1.809134041791292002, -0.09470131462574123138 ) ) ;
#64214=CARTESIAN_POINT ( 'NONE',  ( 6.199861008060345569, 1.254605797456327831, 1.306922710324806225 ) ) ;
#64217=CARTESIAN_POINT ( 'NONE',  ( 2.783357461837578484, 1.550338952211056220, 1.549093164327268068 ) ) ;
#64220=CARTESIAN_POINT ( 'NONE',  ( 6.812964112091245639, -1.437450002374938585, 1.181853997439401116 ) ) ;
#64222=CARTESIAN_POINT ( 'NONE',  ( 3.901880894453650050, -0.9877729052028583201, -1.641157072818617779 ) ) ;
#64227=CARTESIAN_POINT ( 'NONE',  ( 1.692469166403000491, -2.151312531270420436, -0.2117842694067117448 ) ) ;
#64230=CARTESIAN_POINT ( 'NONE',  ( 1.500715674837904468, 1.494693011815557471, -1.047886037138339166 ) ) ;
#64232=CARTESIAN_POINT ( 'NONE',  ( 3.557459645987316232, 0.4443818804308434789, -1.770531947851671006 ) ) ;
#64235=CARTESIAN_POINT ( 'NONE',  ( 4.387129405986627262, 0.09430581837475923712, 1.967405897498993195 ) ) ;
#64237=CARTESIAN_POINT ( 'NONE',  ( 5.144061591681034606, 0.5672955765679200679, 1.857344180792292354 ) ) ;
#64241=CARTESIAN_POINT ( 'NONE',  ( 4.781546299372162245, 0.2051969522943071500, -2.110614603223801122 ) ) ;
#64243=CARTESIAN_POINT ( 'NONE',  ( 3.141163725242692273, 0.04933110545866059571, 1.911816780882446221 ) ) ;
#64249=CARTESIAN_POINT ( 'NONE',  ( 3.668611300974702782, 0.7265845916090816203, 1.877559629772174166 ) ) ;
#64251=CARTESIAN_POINT ( 'NONE',  ( 5.022008369909983116, -0.9795521577263366364, -1.540466923627185292 ) ) ;
#64252=CARTESIAN_POINT ( 'NONE',  ( 0.6958625912084139831, -1.462932864358768459, -1.465259690088885014 ) ) ;
#64256=CARTESIAN_POINT ( 'NONE',  ( 5.489076674590072535, 1.649195787720953987, -0.8828566466120502110 ) ) ;
#64266=CARTESIAN_POINT ( 'NONE',  ( 0.9364849611055334755, -1.153160888946737961, 1.719151461320179042 ) ) ;
#64267=CARTESIAN_POINT ( 'NONE',  ( 2.003655485592752861, -2.052825532818176590, 0.5177380972332337183 ) ) ;
#64270=CARTESIAN_POINT ( 'NONE',  ( 0.4792732452305690782, -0.1022114018467655538, 1.966944630885968603 ) ) ;
#64275=CARTESIAN_POINT ( 'NONE',  ( 2.888958383575964017, 1.965592292480751402, -1.179159595035377261 ) ) ;
#64276=CARTESIAN_POINT ( 'NONE',  ( 0.6975366375942676500, -0.6598540886826111951, 1.702458561391326342 ) ) ;
#64277=CARTESIAN_POINT ( 'NONE',  ( 2.338023529656753752, -1.104205016203146705, -1.561194055274425452 ) ) ;
#64278=VERTEX_POINT ( 'NONE', #136374 ) ;
#64281=CARTESIAN_POINT ( 'NONE',  ( 1.828386956846822509, -0.9528715280972717139, -1.773455306963005462 ) ) ;
#64282=CARTESIAN_POINT ( 'NONE',  ( 0.4968289091572677396, 0.3296062100675010154, 1.933703066120408209 ) ) ;
#64286=CARTESIAN_POINT ( 'NONE',  ( 4.330081446525359645, 2.050255175485806269, 0.4079974934644239326 ) ) ;
#64287=CARTESIAN_POINT ( 'NONE',  ( 2.307162891426073337, -0.3907249415124186553, 1.725993255813297989 ) ) ;
#64289=CARTESIAN_POINT ( 'NONE',  ( 4.822401350889861327, 2.192639013963990635, 0.6684651760814497301 ) ) ;
#64290=CARTESIAN_POINT ( 'NONE',  ( 4.523245630038312370, -1.073764689188366317, -1.369494959904279829 ) ) ;
#64293=CARTESIAN_POINT ( 'NONE',  ( 4.428821037005469030, 0.8169072895964669678, 1.529287752448208471 ) ) ;
#64294=CARTESIAN_POINT ( 'NONE',  ( 4.510331875626576448, 2.170777084992558059, -0.04906379945510477847 ) ) ;
#64296=CARTESIAN_POINT ( 'NONE',  ( 6.262907710099243630, -0.1037740067610822270, -2.014008436551452785 ) ) ;
#64297=CARTESIAN_POINT ( 'NONE',  ( 0.1874999572450692098, -1.451030237095527475, 1.451031289061128993 ) ) ;
#64300=CARTESIAN_POINT ( 'NONE',  ( 3.610301043878104021, -0.7796817500047310556, -1.761725471645478436 ) ) ;
#64302=CARTESIAN_POINT ( 'NONE',  ( 5.976846119194893170, -1.571437351877506439, 1.570356403719268101 ) ) ;
#64304=CARTESIAN_POINT ( 'NONE',  ( 6.983263157960402090, 0.5904152146812295943, 1.899285251901380089 ) ) ;
#64314=CARTESIAN_POINT ( 'NONE',  ( 4.580570881008502404, 1.271380961112581032, -1.624167499240388057 ) ) ;
#64319=CARTESIAN_POINT ( 'NONE',  ( 6.538356921592370696, 1.850225872366149105, 0.2742375073267953045 ) ) ;
#64320=CARTESIAN_POINT ( 'NONE',  ( 5.801316117833412278, 1.158123311926442911, -1.290955512118051818 ) ) ;
#64321=CARTESIAN_POINT ( 'NONE',  ( 4.581465296696157097, -0.8148697087324536792, 1.537882137665383064 ) ) ;
#64323=CARTESIAN_POINT ( 'NONE',  ( 3.579850016053500728, -1.128938594042153021, 1.995021623459404703 ) ) ;
#64325=CARTESIAN_POINT ( 'NONE',  ( 1.464538624043790316, 0.1369371521719800755, -1.836096087760468398 ) ) ;
#64330=CARTESIAN_POINT ( 'NONE',  ( 1.641335390984842491, -1.319735721761399638, -1.261605215524951085 ) ) ;
#64331=CARTESIAN_POINT ( 'NONE',  ( 3.094375128876575065, -0.3905979561782264575, 1.978050703236901686 ) ) ;
#64332=CARTESIAN_POINT ( 'NONE',  ( 0.9729166594223404019, -0.05710519180573449260, -2.190871861337650994 ) ) ;
#64334=CARTESIAN_POINT ( 'NONE',  ( 4.331157237497373025, 0.1008371559532254685, 2.103664472247131378 ) ) ;
#64337=CARTESIAN_POINT ( 'NONE',  ( 1.803268859043684058, -1.750145871244257467, 1.105767233283899920 ) ) ;
#64340=CARTESIAN_POINT ( 'NONE',  ( 3.211701520346501582, 1.672844727185973657, 1.303009041611735030 ) ) ;
#64341=CARTESIAN_POINT ( 'NONE',  ( 0.1703666795057276195, -1.259402025324443564, 1.457936571737717735 ) ) ;
#64348=CARTESIAN_POINT ( 'NONE',  ( 3.006122514718052585, -0.8146449015280079475, 1.848388696978587875 ) ) ;
#64349=CARTESIAN_POINT ( 'NONE',  ( 1.132014994273435216, -1.335988328115779167, -1.627952913800976731 ) ) ;
#64352=CARTESIAN_POINT ( 'NONE',  ( 5.242936282186112962, -0.2253732266207208457, -1.847139840844784775 ) ) ;
#64357=CARTESIAN_POINT ( 'NONE',  ( 6.596562995212404523, -0.5471746534140635720, -1.986858483302299083 ) ) ;
#64361=CARTESIAN_POINT ( 'NONE',  ( 2.495074604456462009, 1.680611355344446389, 0.4256512511701947554 ) ) ;
#64362=CARTESIAN_POINT ( 'NONE',  ( 1.112787002727889885, -1.698604791339110465, 0.3779700589620417217 ) ) ;
#64363=CARTESIAN_POINT ( 'NONE',  ( 0.1832606990049808204, -2.239562280805599492, -0.5557475372391910140 ) ) ;
#64366=CARTESIAN_POINT ( 'NONE',  ( 2.847006562934909280, -1.715207642559450685, 1.141990792043580338 ) ) ;
#64367=CARTESIAN_POINT ( 'NONE',  ( 1.229842044428463010, -1.821462008879136896, -0.8645945014377558469 ) ) ;
#64370=CARTESIAN_POINT ( 'NONE',  ( 1.569145635881466605, 0.1472162271188414695, -1.966034296795520664 ) ) ;
#64371=CARTESIAN_POINT ( 'NONE',  ( 4.799029005866479736, -0.2398712174674077491, -1.897248949554980024 ) ) ;
#64376=CARTESIAN_POINT ( 'NONE',  ( 0.4342474147537092044, -1.082315208530496786, -1.704999936850047249 ) ) ;
#64378=CARTESIAN_POINT ( 'NONE',  ( 4.981611329956401768, 2.155202031093924830, -0.8251229701327715826 ) ) ;
#64379=CARTESIAN_POINT ( 'NONE',  ( 6.426224708462171087, 1.007414738832881351, 1.683299376423300853 ) ) ;
#64380=CARTESIAN_POINT ( 'NONE',  ( 2.201936455694650796, 0.7555380192853027310, -1.810630540845730385 ) ) ;
#64384=CARTESIAN_POINT ( 'NONE',  ( 0.3744018202470792978, -2.102136181054746089, -0.2526282858289953248 ) ) ;
#64387=CARTESIAN_POINT ( 'NONE',  ( 0.8668490835730925381, 1.774987751554598869, -0.4888055736953432207 ) ) ;
#64389=CARTESIAN_POINT ( 'NONE',  ( 3.836941170392699885, -2.090934008593826832, -0.5840943183372940828 ) ) ;
#64392=CARTESIAN_POINT ( 'NONE',  ( 1.670341986359990205, 2.114562342887704283, -0.1611296783964668855 ) ) ;
#64396=CARTESIAN_POINT ( 'NONE',  ( 3.655589845848466801, 0.5043569952981543647, -1.997962123967106374 ) ) ;
#64398=CARTESIAN_POINT ( 'NONE',  ( -0.09456490281532430042, -0.7861721075429689565, -1.663503389917226460 ) ) ;
#64403=CARTESIAN_POINT ( 'NONE',  ( 0.01274299142895937362, -0.9473294304004549193, -1.991142614049784099 ) ) ;
#64404=CARTESIAN_POINT ( 'NONE',  ( 1.652057636490380732, 0.6571787646297929664, -2.164825341390004709 ) ) ;
#64406=CARTESIAN_POINT ( 'NONE',  ( 1.687489445765244289, 1.732788098368071461, -0.5283295289823899399 ) ) ;
#64407=CARTESIAN_POINT ( 'NONE',  ( 1.463933648137748733, -1.021544554152100437, 1.620407321708102533 ) ) ;
#64408=CARTESIAN_POINT ( 'NONE',  ( 3.227070907399377298, -1.911900318415656441, -0.7948586591664741352 ) ) ;
#64410=CARTESIAN_POINT ( 'NONE',  ( 1.481257693138532616, 1.822349276556498143, -0.7526048170787935643 ) ) ;
#64411=CARTESIAN_POINT ( 'NONE',  ( 5.250583079984638246, 0.5609921762826737268, 1.843012466491249723 ) ) ;
#64412=CARTESIAN_POINT ( 'NONE',  ( 0.7862591250819307431, 1.553807182831347777, 1.706378029075397151 ) ) ;
#64414=CARTESIAN_POINT ( 'NONE',  ( 2.769781630715903997, -1.841240947949342788, 0.2698520108674675733 ) ) ;
#64417=CARTESIAN_POINT ( 'NONE',  ( 5.389153705970353592, 0.1484172631736270231, 2.057380146747369576 ) ) ;
#64420=CARTESIAN_POINT ( 'NONE',  ( 6.792010069470917344, -0.9048057162561828903, 1.900113248071538585 ) ) ;
#64423=CARTESIAN_POINT ( 'NONE',  ( 6.046190728430958394, 2.158797838069245412, 0.1127497994189360364 ) ) ;
#64424=CARTESIAN_POINT ( 'NONE',  ( 0.4855842612344652975, -1.827229208960782447, -0.2260576252584786672 ) ) ;
#64425=CARTESIAN_POINT ( 'NONE',  ( 5.602215259268515268, -0.9060462314097734726, 1.805096023085197121 ) ) ;
#64426=CARTESIAN_POINT ( 'NONE',  ( -0.1399997263889819765, 0.7174702203470960660, -2.082715917450683740 ) ) ;
#64433=CARTESIAN_POINT ( 'NONE',  ( 4.135954056172497673, 2.015980767636461835, -0.05432360925018697717 ) ) ;
#64438=CARTESIAN_POINT ( 'NONE',  ( 6.491117449447131982, 1.883434485765375310, -1.060826435891427666 ) ) ;
#64443=CARTESIAN_POINT ( 'NONE',  ( 5.167592292328679449, 1.356312711205298172, 1.492245250866150785 ) ) ;
#64445=CARTESIAN_POINT ( 'NONE',  ( 2.209205535023693212, -0.3792257637574465434, 1.682495413129220907 ) ) ;
#64450=CARTESIAN_POINT ( 'NONE',  ( 6.696569769017397533, -0.4992639023812006638, -1.802638941973549569 ) ) ;
#64451=CARTESIAN_POINT ( 'NONE',  ( 1.277990700441207661, 1.982931799766519676, -0.3463461644656241623 ) ) ;
#64453=CARTESIAN_POINT ( 'NONE',  ( 2.749284697512776710, -1.835294401387000285, 1.225074929180599792 ) ) ;
#64455=CARTESIAN_POINT ( 'NONE',  ( 5.348546061712845301, -2.153812021095147688, -0.2729773376510102323 ) ) ;
#64458=CARTESIAN_POINT ( 'NONE',  ( 2.332823983099761911, 1.383068002389773454, -1.607457772141835717 ) ) ;
#64459=CARTESIAN_POINT ( 'NONE',  ( 2.232046197884657968, 2.016035414700023676, 0.04665772616015140262 ) ) ;
#64460=CARTESIAN_POINT ( 'NONE',  ( 1.828075118979434865, -0.8562131971674535880, -1.596496639089627578 ) ) ;
#64468=CARTESIAN_POINT ( 'NONE',  ( 1.727608309356289729, 0.7294743340424666433, -1.771600730223451547 ) ) ;
#64476=CARTESIAN_POINT ( 'NONE',  ( 5.700121470611750674, -2.161883445634639411, -0.004416275431240455560 ) ) ;
#64479=CARTESIAN_POINT ( 'NONE',  ( 1.740644586495963209, 1.216819214799185866, -1.736574482785017137 ) ) ;
#64481=CARTESIAN_POINT ( 'NONE',  ( 2.829319923597766628, -1.840754522440336327, 0.7060794426061881568 ) ) ;
#64482=CARTESIAN_POINT ( 'NONE',  ( 5.537344615273096515, -0.04053095765194079242, 1.912125305397804009 ) ) ;
#64484=CARTESIAN_POINT ( 'NONE',  ( 0.7837444799244470683, -1.966470238067185905, 0.6478734989143407619 ) ) ;
#64485=CARTESIAN_POINT ( 'NONE',  ( 1.324054681829215818, 1.871493247920783753, 0.5181311518769672331 ) ) ;
#64490=CARTESIAN_POINT ( 'NONE',  ( 2.519574111291386309, -1.204466598365286023, -1.708601439550963663 ) ) ;
#64493=CARTESIAN_POINT ( 'NONE',  ( 5.936178161767468708, -1.066166440211462563, -1.587280745415058814 ) ) ;
#64495=CARTESIAN_POINT ( 'NONE',  ( 4.319099500008596770, 2.017107695584336557, 0.8957252843501888329 ) ) ;
#64496=CARTESIAN_POINT ( 'NONE',  ( 3.452368941479638131, 2.206952907609287973, 0.002057427529567057434 ) ) ;
#64498=CARTESIAN_POINT ( 'NONE',  ( 2.104032245951466429, -0.8162354410432022256, 1.729450509904674416 ) ) ;
#64501=CARTESIAN_POINT ( 'NONE',  ( 4.053231837324381637, 1.750648263899981849, -1.104974720517466480 ) ) ;
#64503=CARTESIAN_POINT ( 'NONE',  ( 1.270647086845246188, -1.370953960119488668, 1.671340013135722558 ) ) ;
#64504=CARTESIAN_POINT ( 'NONE',  ( 3.843468145482428877, 0.7371271433744167600, -2.064019554291535830 ) ) ;
#64511=CARTESIAN_POINT ( 'NONE',  ( 6.609999999999995879, 0.01081285896096205283, 1.720159828161060833 ) ) ;
#64513=CARTESIAN_POINT ( 'NONE',  ( 4.610256228194366201, 2.069909489248497714, -0.04556564433023241323 ) ) ;
#64514=CARTESIAN_POINT ( 'NONE',  ( 3.229043484313653511, 0.04796440165338172745, 1.926065231962639679 ) ) ;
#64515=CARTESIAN_POINT ( 'NONE',  ( 5.642236307234618664, 0.8587400236706268508, 1.935442681345787452 ) ) ;
#64518=CARTESIAN_POINT ( 'NONE',  ( 3.854321288642187149, -1.967005588004781202, -0.1009957709416451771 ) ) ;
#64519=CARTESIAN_POINT ( 'NONE',  ( 5.964811824374402605, 0.1744345966951440507, -2.285673535861055594 ) ) ;
#64520=CARTESIAN_POINT ( 'NONE',  ( 3.967279163243800255, 0.2216459979678051528, -1.812115712870238537 ) ) ;
#64528=CARTESIAN_POINT ( 'NONE',  ( 5.449481901252090310, -1.818156339564154012, 0.8647962134734816786 ) ) ;
#64529=CARTESIAN_POINT ( 'NONE',  ( 0.1405533004714097089, -0.003749010675423158478, -2.279853246149381452 ) ) ;
#64530=CARTESIAN_POINT ( 'NONE',  ( 4.592600981049492326, 1.923087700504518605, 0.3867253955378775476 ) ) ;
#64536=CARTESIAN_POINT ( 'NONE',  ( 0.5211768519108473940, -1.983982463993728906, 0.6597393503331959730 ) ) ;
#64537=CARTESIAN_POINT ( 'NONE',  ( 0.09234973940512071489, -0.4041859633337717694, -1.833079292876439670 ) ) ;
#64539=CARTESIAN_POINT ( 'NONE',  ( 6.474560584146490605, -0.09798994077552795889, -1.939597741719009338 ) ) ;
#64540=CARTESIAN_POINT ( 'NONE',  ( -0.2102771530458094895, 2.860119660625429550, -2.691685224125789588 ) ) ;
#64541=CARTESIAN_POINT ( 'NONE',  ( 0.6611568445531558202, 0.8558493542428649015, 1.515405575314775044 ) ) ;
#64544=CARTESIAN_POINT ( 'NONE',  ( 1.523609404914439969, -0.9557964113278711871, -1.435619824176268100 ) ) ;
#64545=CARTESIAN_POINT ( 'NONE',  ( 1.980270094416748394, -2.150034404144373301, -0.4237573071887782983 ) ) ;
#64547=CARTESIAN_POINT ( 'NONE',  ( 4.389439674793148782, 1.972019932058775016, -0.9908447712502415072 ) ) ;
#64548=CARTESIAN_POINT ( 'NONE',  ( 1.129994725911891207, 2.092989821048664822, -0.5768834896340956364 ) ) ;
#64550=CARTESIAN_POINT ( 'NONE',  ( 2.571616345043222118, 1.500848072127154653, 1.493768111954131284 ) ) ;
#64553=CARTESIAN_POINT ( 'NONE',  ( 2.384684040179287479, -0.3955501765894597344, -2.257852644028814915 ) ) ;
#64557=CARTESIAN_POINT ( 'NONE',  ( 4.600346979525781421, -1.047586700562872286, 1.958737397810013325 ) ) ;
#64564=ORIENTED_EDGE ( 'NONE', *, *, #59450, .F. ) ;
#64565=CARTESIAN_POINT ( 'NONE',  ( 3.445935549842124690, -1.779626424299302956, -0.9480406757386842242 ) ) ;
#64567=CARTESIAN_POINT ( 'NONE',  ( 2.272402725641348820, -0.9685827254542198617, -1.820965734949228310 ) ) ;
#64573=CARTESIAN_POINT ( 'NONE',  ( 5.542994302928621053, -1.725804593724251657, -1.350479894307685447 ) ) ;
#64574=CARTESIAN_POINT ( 'NONE',  ( 2.110000207431836472, 0.002812218110825881467, 2.016597019944998959 ) ) ;
#64575=CARTESIAN_POINT ( 'NONE',  ( 0.5734669319550633748, -1.023298125840161887, 1.530493987491374330 ) ) ;
#64576=ADVANCED_FACE ( 'NONE', ( #148392 ), #141631, .F. ) ;
#64578=CARTESIAN_POINT ( 'NONE',  ( 5.579063851370913873, -0.04688903583028104782, -1.825137680102270288 ) ) ;
#64579=CARTESIAN_POINT ( 'NONE',  ( 6.416638760586134360, -1.319225726833603840, -1.525046029381103452 ) ) ;
#64581=CARTESIAN_POINT ( 'NONE',  ( 5.049841537476964959, 0.7145653451936549994, -2.146778123354900814 ) ) ;
#64583=CARTESIAN_POINT ( 'NONE',  ( 0.3992258182855871196, 1.749727718737997373, -1.171850562161039777 ) ) ;
#64585=CARTESIAN_POINT ( 'NONE',  ( 4.404779037558821386, 0.5491149005726041477, 1.996164414091922135 ) ) ;
#64595=CARTESIAN_POINT ( 'NONE',  ( 2.232967058637932656, 1.447036570497368446, -1.685575845266892747 ) ) ;
#64598=CARTESIAN_POINT ( 'NONE',  ( 3.719154087244529894, -1.729071306366702698, -0.9269775827704658244 ) ) ;
#64605=CARTESIAN_POINT ( 'NONE',  ( 2.795306286867365486, -0.1602278063087131110, -2.114629986603839829 ) ) ;
#64607=CARTESIAN_POINT ( 'NONE',  ( 5.793401095800717826, -1.774274828963496198, 0.8374297333502839225 ) ) ;
#64608=CARTESIAN_POINT ( 'NONE',  ( 4.030267251519312310, 1.158562084521784108, -1.824840551714689507 ) ) ;
#64609=CARTESIAN_POINT ( 'NONE',  ( 3.227900028218867234, 1.797025815167479390, 0.4004103908350764573 ) ) ;
#64613=CARTESIAN_POINT ( 'NONE',  ( 5.771390581163715616, 1.041905927170128754, 1.393825671036960534 ) ) ;
#64614=CARTESIAN_POINT ( 'NONE',  ( 6.727182134110200273, 2.469373133786161745, 2.195552656936059055 ) ) ;
#64617=CARTESIAN_POINT ( 'NONE',  ( 3.186554565756247737, -2.129457467500107004, -0.3711038070777841202 ) ) ;
#64618=CARTESIAN_POINT ( 'NONE',  ( 4.886092203009785528, -0.1017338195800701617, 2.013677658187912556 ) ) ;
#64620=CARTESIAN_POINT ( 'NONE',  ( 2.377987466095924152, 1.329388817951412394, 1.704534938537699995 ) ) ;
#64621=CARTESIAN_POINT ( 'NONE',  ( 2.548066081221173729, 1.970837879163300332, 0.05219120132928834616 ) ) ;
#64622=CARTESIAN_POINT ( 'NONE',  ( 6.509000000000032315, 0.5738235599486035676, 2.152438501345500743 ) ) ;
#64623=CARTESIAN_POINT ( 'NONE',  ( 4.001460698126992455, -1.936627024540507946, 0.1462448094460607750 ) ) ;
#64632=CARTESIAN_POINT ( 'NONE',  ( 0.9036964725192305758, 1.805054822729842190, 1.269220749904229839 ) ) ;
#64634=CARTESIAN_POINT ( 'NONE',  ( 5.348475771816908697, -1.946495798708135938, -0.2439133590248846462 ) ) ;
#64637=CARTESIAN_POINT ( 'NONE',  ( 0.07479286986305369589, 1.387406912293275729, -2.112587013352088317 ) ) ;
#64638=CARTESIAN_POINT ( 'NONE',  ( 3.890429890068654917, 1.554390554365025379, -0.9864425779082321988 ) ) ;
#64643=CARTESIAN_POINT ( 'NONE',  ( 4.939744792934912532, -2.012803497507458683, 0.6676120485993168874 ) ) ;
#64646=CARTESIAN_POINT ( 'NONE',  ( 0.1630570004950296636, -1.840724325608022127, -0.9269800520197747362 ) ) ;
#64648=CARTESIAN_POINT ( 'NONE',  ( 0.2735837943700462627, -1.826300444241350851, 0.3570272679806109073 ) ) ;
#64649=CARTESIAN_POINT ( 'NONE',  ( 3.808014051635350672, 1.299385917162833692, -1.304790556973287163 ) ) ;
#64654=CARTESIAN_POINT ( 'NONE',  ( 3.422699507934781060, 1.400174360247144589, -1.705827624971032686 ) ) ;
#64655=CARTESIAN_POINT ( 'NONE',  ( 4.517028817706403743, 2.066010597640522750, 0.9224273224419097250 ) ) ;
#64657=CARTESIAN_POINT ( 'NONE',  ( 6.011934222899888880, -0.6017306232493442320, 1.708898994858050191 ) ) ;
#64658=CARTESIAN_POINT ( 'NONE',  ( 5.120295473698084798, 1.888475294726537079, 0.3208887515022250669 ) ) ;
#64659=CARTESIAN_POINT ( 'NONE',  ( 6.227412191919261986, -1.760757567598171480, 0.6321290105378990498 ) ) ;
#64660=CARTESIAN_POINT ( 'NONE',  ( 5.529708137783917898, 1.793509118821761561, -0.4966223845426844252 ) ) ;
#64662=CARTESIAN_POINT ( 'NONE',  ( 6.403183007056281184, 1.474056081383187555, 0.9792082336040304202 ) ) ;
#64663=CARTESIAN_POINT ( 'NONE',  ( 1.428923106112218067, -1.700960256238340573, 1.082842518468102089 ) ) ;
#64665=CARTESIAN_POINT ( 'NONE',  ( 2.930406704442231725, 1.169546373139153328, -1.751267329298618280 ) ) ;
#64670=CARTESIAN_POINT ( 'NONE',  ( 1.406516720256438369, -2.010457973371252205, -0.1935789593500591155 ) ) ;
#64673=CARTESIAN_POINT ( 'NONE',  ( 2.917419293707240069, -0.2150262876145451196, 2.150894318904146729 ) ) ;
#64674=CARTESIAN_POINT ( 'NONE',  ( 6.620655732516643965, 2.083750514537034970, 2.135603474206409835 ) ) ;
#64681=CARTESIAN_POINT ( 'NONE',  ( 0.4334776158547505864, -1.553986563932317377, -1.545601477622601472 ) ) ;
#64683=CARTESIAN_POINT ( 'NONE',  ( 3.116390431409152395, -1.113901014592171723, -1.969235179105185640 ) ) ;
#64685=CARTESIAN_POINT ( 'NONE',  ( 4.364470425680367249, -1.957169923074707274, -0.4852690807995581057 ) ) ;
#64691=CARTESIAN_POINT ( 'NONE',  ( 3.145496161269778046, 0.6404232447230692182, -1.649968755877039506 ) ) ;
#64693=CARTESIAN_POINT ( 'NONE',  ( 6.633804142636003931, -1.436369002829580133, -1.675418478561958802 ) ) ;
#64696=CARTESIAN_POINT ( 'NONE',  ( 4.903922820734956112, -1.081083478763317007, -1.701937824264573518 ) ) ;
#64699=CARTESIAN_POINT ( 'NONE',  ( 2.729206520949432946, -1.746158693253213379, 0.6715030345267187784 ) ) ;
#64701=CARTESIAN_POINT ( 'NONE',  ( 3.151297481648129395, 1.777980080355131109, -1.060267355625019281 ) ) ;
#64706=CARTESIAN_POINT ( 'NONE',  ( 1.054777118923880597, 0.3758132965740559883, 1.874924941132802836 ) ) ;
#64707=CARTESIAN_POINT ( 'NONE',  ( 2.312880826517309085, -1.518475810973318074, 1.242258525517292433 ) ) ;
#64708=CARTESIAN_POINT ( 'NONE',  ( 0.9134352171796226161, 0.5825640498151598567, 1.930122961472901633 ) ) ;
#64713=CARTESIAN_POINT ( 'NONE',  ( 0.3505827959322353471, -1.506356567903786470, 1.108807183729618062 ) ) ;
#64715=CARTESIAN_POINT ( 'NONE',  ( 1.582290772395946066, 1.038639357175192401, 1.724485448976780688 ) ) ;
#64717=CARTESIAN_POINT ( 'NONE',  ( 1.950926998395795753, -1.937146449801559367, -0.8548520037577662656 ) ) ;
#64719=CARTESIAN_POINT ( 'NONE',  ( 3.666520218671379450, -0.8364210039109070127, -1.894060025281426807 ) ) ;
#64721=CARTESIAN_POINT ( 'NONE',  ( 5.613254157830992241, -2.039858995719573631, 0.4571984828403846124 ) ) ;
#64723=CARTESIAN_POINT ( 'NONE',  ( 4.067279105520240634, 0.2236234833344897255, -1.811772463268163547 ) ) ;
#64728=CARTESIAN_POINT ( 'NONE',  ( 6.106501571484221458, -0.7887142981495840477, -2.061199855587454444 ) ) ;
#64731=CARTESIAN_POINT ( 'NONE',  ( 4.934190575774549892, -1.026228162776990027, -1.613408319405706504 ) ) ;
#64740=CARTESIAN_POINT ( 'NONE',  ( 0.5734669319550633748, -1.023298125840161887, 1.530493987491374330 ) ) ;
#64744=CARTESIAN_POINT ( 'NONE',  ( 4.411305886619627081, -0.3218996851035611506, 1.842484647571709822 ) ) ;
#64745=CARTESIAN_POINT ( 'NONE',  ( -0.02299388927987088688, 7.629137130509112907, -2.510989390717012881 ) ) ;
#64750=CARTESIAN_POINT ( 'NONE',  ( 1.657020797538899748, 1.613050045282127032, -1.129676354644502556 ) ) ;
#64751=CARTESIAN_POINT ( 'NONE',  ( 2.513296185832504470, -1.880429104915388727, 0.7283969491318904588 ) ) ;
#64756=CARTESIAN_POINT ( 'NONE',  ( 2.871223686158608679, 2.080653275041044026, -0.6881803712485771163 ) ) ;
#64767=CARTESIAN_POINT ( 'NONE',  ( 4.722110844128335039, 1.763445737372179689, 0.5296355584529164329 ) ) ;
#64768=CARTESIAN_POINT ( 'NONE',  ( 2.051433223282957297, -1.797157160989469427, 0.9072355583341712437 ) ) ;
#64769=CARTESIAN_POINT ( 'NONE',  ( 3.040662745855776006, 2.183360198754655812, -0.7182390863737651010 ) ) ;
#64771=CARTESIAN_POINT ( 'NONE',  ( 1.551354284286353247, 1.404667267363783667, 1.220738542487237677 ) ) ;
#64774=CARTESIAN_POINT ( 'NONE',  ( 5.519756697582541172, -0.4584384640409416289, 1.856529252577573619 ) ) ;
#64777=CARTESIAN_POINT ( 'NONE',  ( 4.634370609685579900, 0.3589238887658425248, 2.059545865661859931 ) ) ;
#64778=CARTESIAN_POINT ( 'NONE',  ( 3.274138816734498025, -1.115311402298941656, 1.501645261301733481 ) ) ;
#64780=CARTESIAN_POINT ( 'NONE',  ( 5.495603940606402560, -1.841430844871448258, 0.006098274996368944698 ) ) ;
#64783=CARTESIAN_POINT ( 'NONE',  ( 4.670341630432963242, -1.123608009272176078, 1.308792564452855522 ) ) ;
#64788=CARTESIAN_POINT ( 'NONE',  ( 4.452125263715247527, -0.8365346480432279686, 2.003629037444945471 ) ) ;
#64789=CARTESIAN_POINT ( 'NONE',  ( 3.439906511156048285, 0.8199118703316324863, -1.631291955839441865 ) ) ;
#64790=CARTESIAN_POINT ( 'NONE',  ( 1.094497266827038962, 1.931770780797737341, 0.3408682529649207926 ) ) ;
#64791=CARTESIAN_POINT ( 'NONE',  ( 5.436746213213202061, -1.667492067756784158, 1.304688015722222039 ) ) ;
#64792=CARTESIAN_POINT ( 'NONE',  ( 6.023008118121612853, -2.159854764417634687, 0.7684156934805678185 ) ) ;
#64796=CARTESIAN_POINT ( 'NONE',  ( 1.014494059972574691, -2.120667955011676487, 0.003750198165439199392 ) ) ;
#64800=CARTESIAN_POINT ( 'NONE',  ( 6.157114316693172995, 1.779627781583184909, -1.243356570269833483 ) ) ;
#64801=CARTESIAN_POINT ( 'NONE',  ( 6.983263157960363010, -0.003310164959547181717, 1.953544951557646403 ) ) ;
#64803=CARTESIAN_POINT ( 'NONE',  ( 2.086886708931742884, -1.363721155840109889, 1.753348597404544185 ) ) ;
#64805=CARTESIAN_POINT ( 'NONE',  ( 5.836564609439236939, 0.5826586670559866787, -1.930416874340326938 ) ) ;
#64807=CARTESIAN_POINT ( 'NONE',  ( 5.102416002207363022, 2.056666295747246576, 0.1571963825151497518 ) ) ;
#64813=CARTESIAN_POINT ( 'NONE',  ( 0.2333540202161220045, 5.723122673495201873, -2.639760918834464398 ) ) ;
#64814=CARTESIAN_POINT ( 'NONE',  ( 5.284640796330934087, 1.621094592300664328, -0.8731043043393662550 ) ) ;
#64816=CARTESIAN_POINT ( 'NONE',  ( 1.799380453634431998, -0.5854278125525367305, 1.622511832645438190 ) ) ;
#64817=CARTESIAN_POINT ( 'NONE',  ( 0.5500180045474002410, 0.9981291480291036855, 1.752136972055001296 ) ) ;
#64818=CARTESIAN_POINT ( 'NONE',  ( 2.127932615311285414, 0.5078372532463393263, 2.241765503411979221 ) ) ;
#64820=CARTESIAN_POINT ( 'NONE',  ( 2.372703478119597698, -1.393307465234068898, 1.782356930206913770 ) ) ;
#64821=CARTESIAN_POINT ( 'NONE',  ( 4.055375990838584244, -1.750834834141304697, -1.170193647660602965 ) ) ;
#64823=CARTESIAN_POINT ( 'NONE',  ( 3.004884002558502853, 1.492965937746863148, 0.9499605963744962578 ) ) ;
#64830=CARTESIAN_POINT ( 'NONE',  ( 6.222901868277154414, 1.646860780578407013, -1.490944794436506626 ) ) ;
#64831=CARTESIAN_POINT ( 'NONE',  ( 2.923975034273151419, 1.216836049711809586, -1.822369523680394066 ) ) ;
#64838=CARTESIAN_POINT ( 'NONE',  ( 5.976833544478475702, -1.498421880457675215, 1.500811427713820478 ) ) ;
#64848=CARTESIAN_POINT ( 'NONE',  ( 2.717972786412402364, 1.639536828598524121, 0.5844088115515410076 ) ) ;
#64853=CARTESIAN_POINT ( 'NONE',  ( 6.297764839082774735, -0.7330946318361495351, 2.033732118066629457 ) ) ;
#64858=CARTESIAN_POINT ( 'NONE',  ( 5.840740251263128791, 0.4172088472891195554, 2.120894824392767664 ) ) ;
#64862=CARTESIAN_POINT ( 'NONE',  ( 5.641858350889248364, 0.8014469270729590589, -1.801278572543635326 ) ) ;
#64863=CARTESIAN_POINT ( 'NONE',  ( 5.378194026956880869, -0.2521426391564468572, 1.715267145961799411 ) ) ;
#64865=CARTESIAN_POINT ( 'NONE',  ( 1.857222401600963302, 0.3706860215506869172, -2.159823580554325329 ) ) ;
#64866=CARTESIAN_POINT ( 'NONE',  ( 2.977863636430440941, 2.191611430486348766, -0.7225824955255434334 ) ) ;
#64867=CARTESIAN_POINT ( 'NONE',  ( 4.341127749375134570, -1.794969056106166860, 1.012190969697931209 ) ) ;
#64868=CARTESIAN_POINT ( 'NONE',  ( 0.7791178172221034925, 1.303614328124411692, 1.439515497156283796 ) ) ;
#64872=CARTESIAN_POINT ( 'NONE',  ( 4.412424163657523657, -2.120181911468725033, -0.04909571644767100895 ) ) ;
#64873=CARTESIAN_POINT ( 'NONE',  ( 2.848279904836711118, 0.2930702634792031747, -1.994869876753922799 ) ) ;
#64875=CARTESIAN_POINT ( 'NONE',  ( 4.893709131440695081, 1.632385321431808256, 1.485157849447714451 ) ) ;
#64881=CARTESIAN_POINT ( 'NONE',  ( -0.02919842301645384983, -0.002306431287177927551, -2.073770398395402115 ) ) ;
#64884=CARTESIAN_POINT ( 'NONE',  ( 4.276283029400809177, -1.188189442049456535, 1.683678490072185285 ) ) ;
#64888=CARTESIAN_POINT ( 'NONE',  ( 3.651039828637154372, 0.2984016815541118417, 1.997388552288078545 ) ) ;
#64892=CARTESIAN_POINT ( 'NONE',  ( 3.502855024581267518, 1.625569291660882598, -1.266701038991333572 ) ) ;
#64896=CARTESIAN_POINT ( 'NONE',  ( -0.1411974294642332484, 2.879603353482541817, -2.388950311486548461 ) ) ;
#64897=CARTESIAN_POINT ( 'NONE',  ( 1.816098422328410900, 1.717562825535594140, 0.6636192267199735317 ) ) ;
#64898=CARTESIAN_POINT ( 'NONE',  ( 0.2941754776928190429, 1.714430973684363257, 1.544913290951188012 ) ) ;
#64900=CARTESIAN_POINT ( 'NONE',  ( 2.056162960589353883, 2.155939639820044107, -0.1567802445739118478 ) ) ;
#64902=CARTESIAN_POINT ( 'NONE',  ( 2.255092540634635156, 0.09411513195021348199, -2.014433103604281960 ) ) ;
#64905=CARTESIAN_POINT ( 'NONE',  ( 0.07479286986305370977, 0.004866263145587856019, -1.855573292446038414 ) ) ;
#64906=CARTESIAN_POINT ( 'NONE',  ( 4.645367602377043603, -1.523440194387800650, -1.251305281888495102 ) ) ;
#64907=CARTESIAN_POINT ( 'NONE',  ( 4.628138809701114020, 2.011451458044950069, 0.1435230606586651581 ) ) ;
#64911=CARTESIAN_POINT ( 'NONE',  ( 5.830723289215218763, 2.029276893092274658, 0.5632808350878695247 ) ) ;
#64912=CARTESIAN_POINT ( 'NONE',  ( 6.074686117427479992, 1.393331124738606652, -1.531503843499823381 ) ) ;
#64915=CARTESIAN_POINT ( 'NONE',  ( 6.539320575229274901, 4.692178491785949923, 2.665866134390063813 ) ) ;
#64916=CARTESIAN_POINT ( 'NONE',  ( 5.836196223694859242, -1.125476168604349514, -1.676936384952235404 ) ) ;
#64918=CARTESIAN_POINT ( 'NONE',  ( 4.090657727307928759, -2.282307194306469444, -0.3406017358680757390 ) ) ;
#64919=CARTESIAN_POINT ( 'NONE',  ( 1.569262014403381755, 1.817060349070098724, 0.9760215062899217919 ) ) ;
#64927=CARTESIAN_POINT ( 'NONE',  ( 4.193918837840154623, -1.494357529231920889, -1.575321265833210305 ) ) ;
#64929=CARTESIAN_POINT ( 'NONE',  ( 3.473999211503727036, -1.775402473473717935, -0.4878004006634574230 ) ) ;
#64931=CARTESIAN_POINT ( 'NONE',  ( 5.355090213057959403, 0.4282289882464126451, -2.149144931432686256 ) ) ;
#64933=CARTESIAN_POINT ( 'NONE',  ( 5.752851848433533810, -1.787673638215280913, 1.386716842396797489 ) ) ;
#64938=CARTESIAN_POINT ( 'NONE',  ( 6.239478240350173621, -1.283343308616216705, -1.218829697195593642 ) ) ;
#64939=CARTESIAN_POINT ( 'NONE',  ( 4.125643262898153196, -0.3419791877451948681, 1.983678759314363438 ) ) ;
#64941=CARTESIAN_POINT ( 'NONE',  ( 3.206187942969561000, -2.103625563118251218, 0.1016139793386036383 ) ) ;
#64942=CARTESIAN_POINT ( 'NONE',  ( 1.880356884260485195, -0.5129869988758984922, -1.845544782535366801 ) ) ;
#64943=CARTESIAN_POINT ( 'NONE',  ( 3.596117507753269660, 0.8876951776618343670, -1.758253228584506944 ) ) ;
#64944=CARTESIAN_POINT ( 'NONE',  ( 0.2857447052702493662, -0.8859512962964136706, 1.647562673099879138 ) ) ;
#64945=CARTESIAN_POINT ( 'NONE',  ( 0.9593383959572501229, 1.601786533887459507, 1.132500672181527168 ) ) ;
#64946=CARTESIAN_POINT ( 'NONE',  ( 0.3516297456669579269, -1.353986107606550471, -1.350798769753497552 ) ) ;
#64953=CARTESIAN_POINT ( 'NONE',  ( 6.860220180191213046, -2.069926439015772335, 0.04462916171246724545 ) ) ;
#64955=CARTESIAN_POINT ( 'NONE',  ( 0.6431357727456864515, -0.2518013131528433757, -2.054909676291870380 ) ) ;
#64960=CARTESIAN_POINT ( 'NONE',  ( 5.514351353798126354, -2.120667953778174741, 0.0001357579994532010219 ) ) ;
#64964=CARTESIAN_POINT ( 'NONE',  ( 6.215287892896892430, -1.681934637451238279, -1.009743211781432670 ) ) ;
#64966=CARTESIAN_POINT ( 'NONE',  ( 4.798203786142633653, -1.844427309015805649, 0.8145022673629878085 ) ) ;
#64967=CARTESIAN_POINT ( 'NONE',  ( 3.942530958389865781, -1.415603592240498365, 1.290913190617749118 ) ) ;
#64969=CARTESIAN_POINT ( 'NONE',  ( 1.488088480104592826, -2.181432686776756835, -0.2102995727721947705 ) ) ;
#64971=CARTESIAN_POINT ( 'NONE',  ( 3.725732288501612199, -1.111853074318921664, -1.504101509696729400 ) ) ;
#64975=CARTESIAN_POINT ( 'NONE',  ( 5.255504845270437819, 2.040225721616812482, -0.5655070190290175658 ) ) ;
#64976=CARTESIAN_POINT ( 'NONE',  ( 1.892240118738715005, -0.5608018070641508368, -2.014042591102585877 ) ) ;
#64978=CARTESIAN_POINT ( 'NONE',  ( 0.6391468373067762387, -1.214715217071378195, -1.224744053251116904 ) ) ;
#64988=CARTESIAN_POINT ( 'NONE',  ( 2.051130129875160968, -1.617795175136220509, 0.8151331081446986371 ) ) ;
#64993=CARTESIAN_POINT ( 'NONE',  ( 6.639320575229252341, 2.457876053485750223, 2.280608551775892501 ) ) ;
#64998=CARTESIAN_POINT ( 'NONE',  ( 2.699463648093935575, -1.376791127151571592, -1.252357159445316670 ) ) ;
#64999=CARTESIAN_POINT ( 'NONE',  ( 0.3685665480608457667, -0.2352240095614567816, -1.901051784579368187 ) ) ;
#65000=CARTESIAN_POINT ( 'NONE',  ( 6.405299695295086693, 1.602013123205116019, 1.069544239394400797 ) ) ;
#65008=CARTESIAN_POINT ( 'NONE',  ( 4.575031941739591268, 1.798972412501558260, 0.8019633677735745758 ) ) ;
#65009=CARTESIAN_POINT ( 'NONE',  ( 1.295735140135088281, 1.957893036122235531, -0.8148005001323217478 ) ) ;
#65013=CARTESIAN_POINT ( 'NONE',  ( 6.105464321129510097, -2.175355461714892691, 0.2646407054325700670 ) ) ;
#65015=CARTESIAN_POINT ( 'NONE',  ( 4.665017848976360071, -1.720483299173672043, -0.8667214970639931515 ) ) ;
#65018=CARTESIAN_POINT ( 'NONE',  ( 0.5927436934281339331, -2.190715567557582677, -0.2661302102612560505 ) ) ;
#65022=CARTESIAN_POINT ( 'NONE',  ( 6.526221542235329132, 1.009325857860805087, 1.690966299934024031 ) ) ;
#65023=CARTESIAN_POINT ( 'NONE',  ( 0.9603743489425471402, -1.756279846738018291, -0.8291483874790173125 ) ) ;
#65024=CARTESIAN_POINT ( 'NONE',  ( 0.2103132415818432799, -1.556605082263945228, -1.280954711483893727 ) ) ;
#65026=CARTESIAN_POINT ( 'NONE',  ( 5.875803118876519626, -1.815897848738392106, 0.4062362408630160737 ) ) ;
#65032=CARTESIAN_POINT ( 'NONE',  ( 0.9256184737543894370, -1.394389637717853514, -1.690728713229103342 ) ) ;
#65036=CARTESIAN_POINT ( 'NONE',  ( 1.523764310407935030, -1.012771255265769943, -1.518815351243132383 ) ) ;
#65042=CARTESIAN_POINT ( 'NONE',  ( 0.2406815423939384080, 0.3279693432677989184, 1.898232506199586167 ) ) ;
#65043=CARTESIAN_POINT ( 'NONE',  ( 4.662917994108885189, 1.519075486231920458, -1.241376779329693258 ) ) ;
#65046=CARTESIAN_POINT ( 'NONE',  ( 4.282901435897610298, 1.957309562236182021, -0.9860176978964061423 ) ) ;
#65047=CARTESIAN_POINT ( 'NONE',  ( 6.609000000000015973, 2.967897204652647059, 2.453190122791535366 ) ) ;
#65048=CARTESIAN_POINT ( 'NONE',  ( 3.414952709633051864, -1.570776679111930640, 1.348709175982481856 ) ) ;
#65053=CARTESIAN_POINT ( 'NONE',  ( 3.059543388688467314, -1.367113599135186819, 1.847867383329027335 ) ) ;
#65057=CARTESIAN_POINT ( 'NONE',  ( 6.720655732516669367, 7.629137130509068498, 2.426260288887295058 ) ) ;
#65059=CARTESIAN_POINT ( 'NONE',  ( 3.697155016903285407, -0.5626119583077812125, 1.858668453590556213 ) ) ;
#65062=CARTESIAN_POINT ( 'NONE',  ( 3.709155072767254868, 1.612916391665040416, -1.027221078234448859 ) ) ;
#65064=CARTESIAN_POINT ( 'NONE',  ( 5.350533963330765808, 0.5041449683875122156, 1.649457517733200040 ) ) ;
#65065=CARTESIAN_POINT ( 'NONE',  ( 3.661342437515973547, 1.897110692972364454, -0.6839366698164970337 ) ) ;
#65066=CARTESIAN_POINT ( 'NONE',  ( 4.553568368667338717, -1.501836741657993191, 1.740358071397982265 ) ) ;
#65068=CARTESIAN_POINT ( 'NONE',  ( 0.8036966383840878914, 1.806304194667744500, 1.267646993260997723 ) ) ;
#65070=CARTESIAN_POINT ( 'NONE',  ( 5.958207135543601041, 0.7187401461678426529, 1.617382982224302879 ) ) ;
#65073=CARTESIAN_POINT ( 'NONE',  ( 2.449550052152906332, 0.6095859302821411418, -2.209661595554306412 ) ) ;
#65074=CARTESIAN_POINT ( 'NONE',  ( 0.8315134001313486678, 1.713846476070936653, 0.3014184826048373900 ) ) ;
#65076=CARTESIAN_POINT ( 'NONE',  ( 0.8426186123336505407, -0.9696909581486823360, 1.437080622210512360 ) ) ;
#65080=CARTESIAN_POINT ( 'NONE',  ( 0.8015275938294207370, -1.862055209299150249, 1.116337150347948892 ) ) ;
#65081=CARTESIAN_POINT ( 'NONE',  ( 2.712125330650519750, 1.116209241849321465, -1.679223868463100011 ) ) ;
#65083=CARTESIAN_POINT ( 'NONE',  ( 5.584577364790731302, -1.880054400457907171, -0.4198111936028568469 ) ) ;
#65085=CARTESIAN_POINT ( 'NONE',  ( 2.215342456320268383, 1.781105875021117502, -1.327318755304232933 ) ) ;
#65091=CARTESIAN_POINT ( 'NONE',  ( 5.126372767375061201, 0.1352161506754517850, 1.735264446013358608 ) ) ;
#65092=CARTESIAN_POINT ( 'NONE',  ( 3.789464544343919883, -1.813617537123424661, 0.7486148740368094856 ) ) ;
#65096=CARTESIAN_POINT ( 'NONE',  ( 4.534621088391048715, 2.217606307645642261, 0.4472613530076152699 ) ) ;
#65097=CARTESIAN_POINT ( 'NONE',  ( 1.100133984900531825, 0.8377775336174065890, -1.885062252648894265 ) ) ;
#65101=CARTESIAN_POINT ( 'NONE',  ( 2.413256113406063275, 2.020865564879420262, 1.017551375885389131 ) ) ;
#65102=VERTEX_POINT ( 'NONE', #117088 ) ;
#65104=CARTESIAN_POINT ( 'NONE',  ( 2.776451973220807279, -1.788819259240326698, -0.5467896145717602296 ) ) ;
#65105=CARTESIAN_POINT ( 'NONE',  ( 1.265804362365889668, 1.602598504008081237, -0.6630416328189077113 ) ) ;
#65106=CARTESIAN_POINT ( 'NONE',  ( 5.689076433642084041, 1.658752129386225516, 1.432425853890168188 ) ) ;
#65107=CARTESIAN_POINT ( 'NONE',  ( 6.440458288041322810, 2.281167638128688946, 0.3475669597150666257 ) ) ;
#65108=CARTESIAN_POINT ( 'NONE',  ( 4.416967121957662279, 1.975198431823081302, 0.8787980929093119897 ) ) ;
#65109=CARTESIAN_POINT ( 'NONE',  ( 4.101460596356475641, -1.936652220471976937, 0.1442349196467233863 ) ) ;
#65112=CARTESIAN_POINT ( 'NONE',  ( 0.9687500000000008882, 0.7852924748299362490, -1.895863743164110327 ) ) ;
#65116=CARTESIAN_POINT ( 'NONE',  ( 5.186172726741035355, 1.650080556555008293, 1.158690440749516881 ) ) ;
#65120=CARTESIAN_POINT ( 'NONE',  ( 3.439906511156048285, 0.8199118703316324863, -1.631291955839441865 ) ) ;
#65127=CARTESIAN_POINT ( 'NONE',  ( 6.410808175004245157, -0.5408338447881118061, -1.945826018873537455 ) ) ;
#65128=CARTESIAN_POINT ( 'NONE',  ( 1.647299267346370444, 0.2110521635003380359, 2.109970702148834754 ) ) ;
#65132=CARTESIAN_POINT ( 'NONE',  ( 6.385628592921421820, 1.419324251362139133, 1.494494355598655622 ) ) ;
#65133=CARTESIAN_POINT ( 'NONE',  ( 4.746720300533005421, 1.994071680685698400, -0.2986252114312442640 ) ) ;
#65142=CARTESIAN_POINT ( 'NONE',  ( 5.624374986212743011, 0.3960386850128463920, -1.976653645673176474 ) ) ;
#65143=CARTESIAN_POINT ( 'NONE',  ( 5.156134521940135329, -1.331146486249596306, 1.272188372451001026 ) ) ;
#65144=CARTESIAN_POINT ( 'NONE',  ( -0.02338929933905566777, 0.2563879980532010605, -1.746150209723141167 ) ) ;
#65145=CARTESIAN_POINT ( 'NONE',  ( 3.633692980683305152, -2.132556294031516142, 0.8823059210255141949 ) ) ;
#65147=CARTESIAN_POINT ( 'NONE',  ( 5.782550318682353918, -2.107506929020441788, -0.4798289361013233223 ) ) ;
#65149=CARTESIAN_POINT ( 'NONE',  ( 1.013109794239855699, -1.894405189233986597, 0.4268842903399574507 ) ) ;
#65154=CARTESIAN_POINT ( 'NONE',  ( 3.344469905398727239, 0.4532862802011444758, 1.814783984445811127 ) ) ;
#65157=CARTESIAN_POINT ( 'NONE',  ( 1.775505761281343631, 0.3235837346332003372, -1.884644527778083001 ) ) ;
#65160=CARTESIAN_POINT ( 'NONE',  ( 2.666872310945223923, -1.521158656661812714, 1.599105504226288499 ) ) ;
#65161=CARTESIAN_POINT ( 'NONE',  ( 6.983263157960407419, 1.286439435963281142, 1.962168536134776931 ) ) ;
#65166=CARTESIAN_POINT ( 'NONE',  ( 1.089067603693228525, 1.740485041285372958, -0.9256802945506740210 ) ) ;
#65167=CARTESIAN_POINT ( 'NONE',  ( 0.8862589459083686227, 1.552251447166236975, 1.707653507296547968 ) ) ;
#65168=CARTESIAN_POINT ( 'NONE',  ( 1.152704166800899932, -0.4732522875653189520, -1.903817266927515961 ) ) ;
#65169=CARTESIAN_POINT ( 'NONE',  ( 5.506706524517535506, 0.5933582781832097419, 1.975413352875006856 ) ) ;
#65176=CARTESIAN_POINT ( 'NONE',  ( 1.147616990042895191, 1.915638116573715743, -1.021621585119661058 ) ) ;
#65178=CARTESIAN_POINT ( 'NONE',  ( 6.356982874815331641, 0.3076174260261410054, -1.815216213958574132 ) ) ;
#65181=CARTESIAN_POINT ( 'NONE',  ( 1.370139650511486007, -1.190941340819328564, 1.442406204513801971 ) ) ;
#65182=CARTESIAN_POINT ( 'NONE',  ( 5.149776166300943814, 0.6834882490109328579, -2.050742609271530181 ) ) ;
#65184=CARTESIAN_POINT ( 'NONE',  ( 0.07735805125223899070, 6.946777552644263665, -2.683974465663693021 ) ) ;
#65186=CARTESIAN_POINT ( 'NONE',  ( 1.857924044808876074, 0.7306008629870773818, -1.767408594711167735 ) ) ;
#65187=CARTESIAN_POINT ( 'NONE',  ( 3.133429157788733654, -1.187652617478820227, -1.312364946228376628 ) ) ;
#65188=CARTESIAN_POINT ( 'NONE',  ( 0.4340482808194641162, -1.023182136338888659, -1.615339470012015166 ) ) ;
#65190=CARTESIAN_POINT ( 'NONE',  ( 5.782812685692425347, 1.563071972524389786, -1.107110302061852236 ) ) ;
#65191=CARTESIAN_POINT ( 'NONE',  ( 6.865690646733241032, -0.4297541067138924697, 1.928966555396218752 ) ) ;
#65194=CARTESIAN_POINT ( 'NONE',  ( 1.195735321641926197, 1.957225868588155837, -0.8166992996602240318 ) ) ;
#65196=CARTESIAN_POINT ( 'NONE',  ( 4.662891624058607576, -1.671085903211678270, -0.8408918736509605196 ) ) ;
#65197=CARTESIAN_POINT ( 'NONE',  ( 1.049113529465800054, -1.437755431736492673, -1.125068434497819680 ) ) ;
#65199=CARTESIAN_POINT ( 'NONE',  ( 5.145248760827346501, -1.894204247122273088, 1.132176536499051700 ) ) ;
#65203=CARTESIAN_POINT ( 'NONE',  ( 1.732955346664406537, -1.957976925384408817, -0.6489628464096306448 ) ) ;
#65211=CARTESIAN_POINT ( 'NONE',  ( 4.352052382902608763, -0.7952921280917917279, 1.911720769834825973 ) ) ;
#65213=CARTESIAN_POINT ( 'NONE',  ( 1.353037089713942320, -1.704917477850418805, 1.328741451194020762 ) ) ;
#65215=CARTESIAN_POINT ( 'NONE',  ( 1.735027068915934167, 1.885295237280168790, 0.7248928932378613244 ) ) ;
#65219=CARTESIAN_POINT ( 'NONE',  ( 6.883263157960366030, 0.5727201817382967519, 2.105997115537924902 ) ) ;
#65220=CARTESIAN_POINT ( 'NONE',  ( 0.2160302486270138655, 1.032475520995678853, -1.731998313101141163 ) ) ;
#65221=CARTESIAN_POINT ( 'NONE',  ( 4.915667883426772633, -1.172277214026868464, -1.851500752446763709 ) ) ;
#65222=( BOUNDED_CURVE ( )  B_SPLINE_CURVE ( 3, ( #114665, #79956, #211012, #163359 ),
 .UNSPECIFIED., .F., .T. ) 
 B_SPLINE_CURVE_WITH_KNOTS ( ( 4, 4 ),
 ( 0.4999999999999939493, 1.000000000000000000 ),
 .UNSPECIFIED. ) 
 CURVE ( )  GEOMETRIC_REPRESENTATION_ITEM ( )  RATIONAL_B_SPLINE_CURVE ( ( 1.000000000000007994, 0.3333333333333333148, 0.3333333333333252657, 1.000000000000000000 ) ) 
 REPRESENTATION_ITEM ( '' )  );
#65223=B_SPLINE_CURVE_WITH_KNOTS ( 'NONE', 3,
 ( #85254, #87405, #184876, #201116, #105824, #54900, #48783, #168641, #154539, #20243, #121053, #118892, #170778, #36502, #171850, #122122, #6120, #2911, #137235, #155606, #86329, #152400, #52757, #151342, #203257, #103660, #72188, #138297, #39716, #187019, #202180, #7190, #3979, #70048, #136162, #119968, #185945, #114899, #37578, #68984, #22367, #23445, #180897, #135102, #204312, #89555, #169709, #21299, #153470, #5043, #55969, #38652, #104731, #188086, #32519, #131155, #197145, #164656, #19179, #176134, #77544, #94890, #107989, #8273, #127463, #42945, #126385, #60226, #93828, #76475, #159869, #205398, #9349, #11473, #91698, #74356, #41878, #191278, #75421, #160942, #73263, #174017, #10402, #142586, #206472, #45078, #109053, #139367, #141533, #157751, #140460, #58101, #110122, #189165, #209660, #28805, #124260, #40804, #193434, #125319, #24513, #27734, #57037, #175071, #111187, #190219, #143666, #61301, #92761, #123204, #158805, #25587, #106911, #172936, #207541, #90623, #177190, #156681, #59161, #26658, #208594, #192345, #44003, #63437, #198733, #518, #99143, #95963, #164143, #34120, #129588, #210741, #79681, #145794, #196636, #47213, #62365, #182491, #195575, #100191, #113327, #12536, #179334, #211800, #30955, #97030, #163084, #128527, #14665, #178268, #115445, #194496, #81813, #48276, #80757, #162017, #46140, #15727, #114389, #146846, #147896, #180384, #64501, #212865, #112255, #78608, #130644, #197683, #29879, #181436, #16786, #13606, #32008, #98090, #213912, #65535, #131681, #49328, #33065, #165192, #144730, #82869, #148947, #66586, #132729, #50379, #116501, #121858, #17846, #118638, #199806, #83931, #5857, #2657, #200858, #68731, #150020, #184623, #117571, #54638, #1590, #67651, #167332, #38389, #138039, #134852, #183566, #35172, #52505, #22099, #53573, #3717, #19988, #133797, #187829, #36240, #136971, #101249, #120787, #170517, #18918, #85002, #168392, #102318, #151094, #103393, #153209, #86073, #51451, #152148, #169454, #69793, #135902, #39455, #166257, #201920, #119706, #71928, #186764, #185689, #104470, #88212, #21040, #154283, #37318, #87138, #204052, #4779, #70857, #202999, #55703, #107731, #127205, #105551, #56777, #173757, #142332, #172673, #8008, #11211, #193172, #25334, #189969, #106645, #40542, #208343, #6928, #27470, #61044, #24250, #73006, #159613, #157496, #122943, #171585, #125067, #59974, #23179, #209400, #90353, #143404, #191025, #89294, #42692, #156422, #155345, #139106, #91435, #205134, #77292, #188899, #74099, #140191, #141276, #9090, #93568, #206212, #41618, #57839, #92512, #76222, #108797, #124001, #75167, #207285, #58912, #174824, #26400, #158550, #10147, #126128, #192088, #43754, #109868, #175880, #178007, #66339, #195321, #65284, #63178, #194240, #129343, #179075, #146594, #131431, #45885, #145546, #196385, #48026, #29624, #16533, #162829, #44822, #113069, #46952, #112006, #95708, #81557, #160682, #181187, #269, #210481, #78353, #197433, #163897, #144476, #147640, #132485, #96778, #98888, #161762, #213659, #32813, #64252, #110927, #130394, #13353, #176931, #28549, #30696, #94638, #12277, #79428, #49074, #211543, #180134, #14406, #115194, #80497, #82615, #164940, #148700, #128279, #114142, #62119, #212612, #31761, #97832, #15473, #168144, #18677, #4534, #202747, #104220, #119456, #52261, #71680 ),
 .UNSPECIFIED., .F., .F.,
 ( 4, 1, 1, 1, 1, 1, 1, 1, 1, 1, 1, 1, 1, 1, 1, 1, 1, 1, 1, 1, 1, 1, 1, 1, 1, 1, 1, 1, 1, 1, 1, 1, 1, 1, 1, 1, 1, 1, 1, 1, 1, 1, 1, 1, 1, 1, 1, 1, 1, 1, 1, 1, 1, 1, 1, 1, 1, 1, 1, 1, 1, 1, 1, 1, 1, 1, 1, 1, 1, 1, 1, 1, 1, 1, 1, 1, 1, 1, 1, 1, 1, 1, 1, 1, 1, 1, 1, 1, 1, 1, 1, 1, 1, 1, 1, 1, 1, 1, 1, 1, 1, 1, 1, 1, 1, 1, 1, 1, 1, 1, 1, 1, 1, 1, 1, 1, 1, 1, 1, 1, 1, 1, 1, 1, 1, 1, 1, 1, 1, 1, 1, 1, 1, 1, 1, 1, 1, 1, 1, 1, 1, 1, 1, 1, 1, 1, 1, 1, 1, 1, 1, 1, 1, 1, 1, 1, 1, 1, 1, 1, 1, 1, 1, 1, 1, 1, 1, 1, 1, 1, 1, 1, 1, 1, 1, 1, 1, 1, 1, 1, 1, 1, 1, 1, 1, 1, 1, 1, 1, 1, 1, 1, 1, 1, 1, 1, 1, 1, 1, 1, 1, 1, 1, 1, 1, 1, 1, 1, 1, 1, 1, 1, 1, 1, 1, 1, 1, 1, 1, 1, 1, 1, 1, 1, 1, 1, 1, 1, 1, 1, 1, 1, 1, 1, 1, 1, 1, 1, 1, 1, 1, 1, 1, 1, 1, 1, 1, 1, 1, 1, 1, 1, 1, 1, 1, 1, 1, 1, 1, 1, 1, 1, 1, 1, 1, 1, 1, 1, 1, 1, 1, 1, 1, 1, 1, 1, 1, 1, 1, 1, 1, 1, 1, 1, 1, 1, 1, 1, 1, 1, 1, 1, 1, 1, 1, 1, 1, 1, 1, 1, 1, 1, 1, 1, 1, 1, 1, 1, 1, 1, 1, 1, 1, 1, 1, 1, 1, 1, 1, 1, 1, 1, 1, 1, 1, 1, 1, 1, 1, 1, 1, 1, 1, 1, 1, 1, 1, 1, 1, 1, 1, 1, 1, 1, 1, 1, 1, 1, 1, 1, 1, 1, 1, 1, 1, 1, 1, 1, 1, 1, 1, 1, 1, 1, 1, 1, 1, 1, 1, 1, 1, 1, 1, 1, 1, 1, 1, 1, 1, 1, 1, 1, 1, 1, 4 ),
 ( 0.000000000000000000, 0.002599974731368114196, 0.005208790931971673047, 0.007813145979665977320, 0.01041652777592116073, 0.01302061325022423749, 0.01562498222773845216, 0.01822909327250534645, 0.02083329118620782031, 0.02343750764584028035, 0.02604160881127103033, 0.02864587273906003470, 0.03124992668191499748, 0.03385418289307650513, 0.03645825757725845717, 0.03906249379052053466, 0.04166666320740203266, 0.04427081823557592333, 0.04687506849204003262, 0.04947913642841410276, 0.05208339700068515682, 0.05468745344639398126, 0.05729170333903113588, 0.05989581325979084075, 0.06250002080062810883, 0.06510424464624173235, 0.06770834408375023261, 0.07031260355790951155, 0.07291665769283758869, 0.07552091454841564078, 0.07812498837240108851, 0.08072922377910608793, 0.08333339284475561881, 0.08593754734057650058, 0.08854179710653446722, 0.09114586450482109470, 0.09375012458370637902, 0.09635418052565795921, 0.09895842987840544613, 0.1015625393267825388, 0.1041667463075427041, 0.1067709697059155277, 0.1093750686050062593, 0.1119793276133541904, 0.1145833812402851093, 0.1171876375884709082, 0.1197917109360151500, 0.1223959458003068407, 0.1250001144218755300, 0.1276042683764700425, 0.1302085177025434359, 0.1328125845892443313, 0.1354168441945610146, 0.1380208996559441903, 0.1406251484930516882, 0.1432292574929059925, 0.1458334639374244401, 0.1484376869122458475, 0.1510417852965526830, 0.1536460438630466996, 0.1562500970055218374, 0.1588543528702505148, 0.1614584257649260002, 0.1640626601106844606, 0.1666668283118819260, 0.1692709817489688462, 0.1718752306590244638, 0.1744792970577103974, 0.1770835562133957763, 0.1796876112177483997, 0.1822918595631332073, 0.1848959681380851483, 0.1875001740701665309, 0.1901043966452301559, 0.1927084945383780445, 0.1953127526869259389, 0.1979168053684795814, 0.2005210607736844508, 0.2031251332390507092, 0.2057293670901427229, 0.2083335348946688259, 0.2109376878379560227, 0.2135419363558502259, 0.2161460022900811573, 0.2187502610200618980, 0.2213543155909112325, 0.2239585634684796434, 0.2265626716421396125, 0.2291668770855771753, 0.2317710992846666596, 0.2343751967102698508, 0.2369794544647692847, 0.2395835067089256143, 0.2421877616785296505, 0.2447918337381362330, 0.2473960671184182170, 0.2500002345499632850, 0.2526043870231480248, 0.2552086351727278490, 0.2578127006660536624, 0.2604169589942467167, 0.2630210131551104502, 0.2656252605887587936, 0.2682293683847277177, 0.2708335733633049913, 0.2734377952101950116, 0.2760418921918580404, 0.2786461495761977103, 0.2812502014064713896, 0.2838544559643880194, 0.2864585276417753179, 0.2890627605750938911, 0.2916669276573394809, 0.2942710796841097043, 0.2968753274892133587, 0.2994793925651746958, 0.3020836505154881335, 0.3046877042898750165, 0.3072919513034905736, 0.3098960587453611915, 0.3125002632828523530, 0.3151044848013095923, 0.3177085813626279731, 0.3203128384006882490, 0.3229168898405855304, 0.3255211440107198539, 0.3281252153294201834, 0.3307294478396133885, 0.3333336145962333963, 0.3359377662002681064, 0.3385420136847264727, 0.3411460783668558427, 0.3437503359631899347, 0.3463543893746011126, 0.3489586359920627823, 0.3515627431034201722, 0.3541669472235909888, 0.3567711684373747749, 0.3593752646019360286, 0.3619795213175900916, 0.3645835723906095116, 0.3671878261968588575, 0.3697918971803975663, 0.3723961292912953969, 0.3750002957459567798, 0.3776044469509276524, 0.3802086941385645069, 0.3828127584503868142, 0.3854170157166348365, 0.3880210687885642384, 0.3906253150337437030, 0.3932294218381663375, 0.3958336255647753599, 0.3984378464976386924, 0.4010419422890235119, 0.4036461987061379930, 0.4062502494357712601, 0.4088545029020263510, 0.4114585735739221262, 0.4140628053093475813, 0.4166669714857112461, 0.4192711223152827404, 0.4218753692299160307, 0.4244794331949501842, 0.4270836901549991405, 0.4296877429109347002, 0.4322919888076972583, 0.4348960953287579478, 0.4375002986855570652, 0.4401045193612476147, 0.4427086148030301427, 0.4453128709454660106, 0.4479169213551993378, 0.4505211745053449013, 0.4531252448891109341, 0.4557294762728811288, 0.4583336421946030970, 0.4609377926724337327, 0.4635420393378766879, 0.4661461029796354349, 0.4687503596573671660, 0.4713544121207915438, 0.4739586576929967765, 0.4765627639542633909, 0.4791669669649988861, 0.4817711874072597711, 0.4843752825230089321, 0.4869795384146229367, 0.4895835885279371524, 0.4921878413858530310, 0.4947919115049980165, 0.4973961425609249032, 0.5000003082516567554, 0.5026044584014001115, 0.5052087048414615200, 0.5078127681834534446, 0.5104170246027455171, 0.5130210767971369323, 0.5156253220686399796, 0.5182294280936764475, 0.5208336307820899957, 0.5234378510146604491, 0.5260419458279406157, 0.5286462014925853437, 0.5312502513329574461, 0.5338545039225196520, 0.5364585738005485105, 0.5390628045524396006, 0.5416669700358295314, 0.5442711198811350792, 0.5468753661196208427, 0.5494794291853500878, 0.5520836853700766822, 0.5546877373189100791, 0.5572919823135623618, 0.5598960881259297251, 0.5625002905157588939, 0.5651045105623757614, 0.5677086050967478092, 0.5703128605582734600, 0.5729169101491768945, 0.5755211624942581095, 0.5781252321546730411, 0.5807294626263322934, 0.5833336279260263879, 0.5859377774905402125, 0.5885420235512536236, 0.5911460863642216124, 0.5937503423382545220, 0.5963543940650019026, 0.5989586388066517886, 0.6015627444299086468, 0.6041669465448881171, 0.6067711664292861906, 0.6093752607083083861, 0.6119795159905627724, 0.6145835653554690969, 0.6171878174799397820, 0.6197918869462408775, 0.6223961171614702526, 0.6250002823011129305, 0.6276044316084782304, 0.6302086775152213605, 0.6328127400989277396, 0.6354169958861367595, 0.6380210474142689048, 0.6406252919267632073, 0.6432293973844667168, 0.6458335992483292820, 0.6484378189942425763, 0.6510419130414711875, 0.6536461681683013447, 0.6562502173306804520, 0.6588544692584096252, 0.6614585385540960871, 0.6640627685366956579, 0.6666669335399304508, 0.6692710826137896474, 0.6718753283903641238, 0.6744793907683068745, 0.6770836463925611337, 0.6796876977455479363, 0.6822919420527318035, 0.6848960473684391204, 0.6875002490049163528, 0.6901044686360783276, 0.6927085624750688453, 0.6953128174703216979, 0.6979168664536427036, 0.7005211182084990496, 0.7031251873570698585, 0.7057294171308388098, 0.7083335820213095824, 0.7109377308853042088, 0.7135419765555117699, 0.7161460387511890957, 0.7187502942363581671, 0.7213543454376690756, 0.7239585895633880996, 0.7265626947606567132, 0.7291668961934797411, 0.7317711157336249661, 0.7343752093879328813, 0.7369794642754557978, 0.7395835131031885945, 0.7421877647090413532, 0.7447918337339959338, 0.7473960633227341166, 0.7500002281240860658, 0.7526043768018576552, 0.7552086223895014827, 0.7578126844264116979, 0.7604169397963658206, 0.7630209908694718379, 0.7656252348375721661, 0.7682293399399604539, 0.7708335411928610714, 0.7734377606657260040, 0.7760418541589074737, 0.7786461089625497101, 0.7812501576581653007, 0.7838544091388848223, 0.7864584780637244865, 0.7890627074912324179, 0.7916668722271122949, 0.7942710207423038238, 0.7968752662711893198, 0.7994793281728324041, 0.8020835834514440377, 0.8046876344198176101, 0.8072918782541467220, 0.8098959832852158369, 0.8125001843819276148, 0.8151044038112509327, 0.8177084971668638902, 0.8203127519104773668, 0.8229168004974481976, 0.8255210518769072747, 0.8281251207251358881, 0.8307293500152160837, 0.8333335147092740813, 0.8359376630855301915, 0.8385419085794658667, 0.8411459703693440204, 0.8437502255804886220, 0.8463542764676049712, 0.8489585201920134550, 0.8515626251753276588, 0.8541668261395859441, 0.8567710455491102106, 0.8593751387907155870, 0.8619793934981552219, 0.8645834419999574028, 0.8671876933020320477, 0.8697917620971562513, 0.8723959912736143352, 0.8750001559495040881, 0.8776043042104727521, 0.8802085496932706699, 0.8828126113948897569, 0.8854168665624462253, 0.8880209173917842369, 0.8906251610301256783, 0.8932292659892527853, 0.8958334668447968108, 0.8984376862582688084, 0.9010417794094305322, 0.9036460341045560174, 0.9062500825446693220, 0.9088543337932389887, 0.9114584025587700866, 0.9140626316454156797, 0.9166667963267953745, 0.9192709444961273402, 0.9218751899916067805, 0.9244792516284782158, 0.9270835067763207871, 0.9296875575713596795, 0.9322918011475309630, 0.9348959061060417852, 0.9375001068764983181, 0.9401043263176916964, 0.9427084194022110619, 0.9453126741091559815, 0.9479167225106870376, 0.9505209737258253355, 0.9531250424882484751, 0.9557292715345466760, 0.9583334362123939743, 0.9609375841976093291, 0.9635418299546441023, 0.9661458919105455623, 0.9687501459642621215, 0.9713541960184646218, 0.9739584433044384815, 0.9765625494917742344, 0.9791667425299969141, 0.9817709508269629737, 0.9843750450459556323, 0.9869794226472197174, 0.9895834977571079660, 0.9921868632736227100, 0.9947912224625704569, 0.9974000159472320437, 1.000000000000000000 ),
 .UNSPECIFIED. ) ;
#65225=CARTESIAN_POINT ( 'NONE',  ( 4.007995338699683607, -0.7271224857151190601, 1.768968726348684406 ) ) ;
#65229=CARTESIAN_POINT ( 'NONE',  ( 1.915638884950950027, -1.319244919589783516, -1.525031147761625405 ) ) ;
#65232=CARTESIAN_POINT ( 'NONE',  ( 1.013678699313476095, -2.235087565253154107, 0.5086484811528817485 ) ) ;
#65234=CARTESIAN_POINT ( 'NONE',  ( 4.225434206992398245, -1.650187577572001629, 0.5017251585606904429 ) ) ;
#65235=CARTESIAN_POINT ( 'NONE',  ( -0.1394461523060883668, 1.988389203256015536, -2.694605331112149393 ) ) ;
#65238=CARTESIAN_POINT ( 'NONE',  ( 0.1755611466353811378, 5.720003923744535257, -2.838048273117784959 ) ) ;
#65241=CARTESIAN_POINT ( 'NONE',  ( 5.303285216261115487, 1.594816061929973827, -0.8590795265051922591 ) ) ;
#65246=CARTESIAN_POINT ( 'NONE',  ( 5.830666647502705580, 1.211628268937942066, -1.346810592849301047 ) ) ;
#65250=CARTESIAN_POINT ( 'NONE',  ( 2.589988673929614738, -2.185656584452956075, -0.1600571409424780822 ) ) ;
#65251=CARTESIAN_POINT ( 'NONE',  ( 6.320743865583476229, -1.315316497155760489, 1.316877014833318649 ) ) ;
#65253=CARTESIAN_POINT ( 'NONE',  ( 4.095261013068919098, -0.3237038700398958690, 1.887879439767611744 ) ) ;
#65260=CARTESIAN_POINT ( 'NONE',  ( 5.964083501069187498, -1.130735325014235793, 1.789944102876602328 ) ) ;
#65261=CARTESIAN_POINT ( 'NONE',  ( 1.270647086845246188, -1.370953960119488668, 1.671340013135722335 ) ) ;
#65265=CARTESIAN_POINT ( 'NONE',  ( 1.113953379265147925, -0.8168401028521531382, -1.632710947565917170 ) ) ;
#65267=CARTESIAN_POINT ( 'NONE',  ( 4.032112419961201510, 0.9767663869549062516, -1.542106374223570553 ) ) ;
#65270=CARTESIAN_POINT ( 'NONE',  ( 2.875404442980381781, -0.1956706474990059230, 1.959820717905029097 ) ) ;
#65272=CARTESIAN_POINT ( 'NONE',  ( 4.528815305949091652, -1.774144813887452266, 0.7903587577767021699 ) ) ;
#65275=CARTESIAN_POINT ( 'NONE',  ( 5.537388447972660721, -0.05000006065614125139, 2.120159173171487055 ) ) ;
#65277=CARTESIAN_POINT ( 'NONE',  ( 2.754443878939544454, 1.898071056134968959, 0.2320119769325945103 ) ) ;
#65281=CARTESIAN_POINT ( 'NONE',  ( 4.125643262898153196, -0.3419791877451948681, 1.983678759314363438 ) ) ;
#65283=CARTESIAN_POINT ( 'NONE',  ( 4.881388680972560401, 1.702354803207173584, -0.6601141376258444771 ) ) ;
#65284=CARTESIAN_POINT ( 'NONE',  ( 1.311079954825690619, -1.633285661836245906, 1.272233187909928454 ) ) ;
#65288=CARTESIAN_POINT ( 'NONE',  ( 5.981297838379462384, 1.727768277425823396, -0.7175292643646775659 ) ) ;
#65298=CARTESIAN_POINT ( 'NONE',  ( 1.516557075436252733, 0.8353943144701718726, 1.894387172633307692 ) ) ;
#65299=CARTESIAN_POINT ( 'NONE',  ( 2.372804174479496986, -0.3651721903723912921, -2.085361659519912259 ) ) ;
#65301=CARTESIAN_POINT ( 'NONE',  ( 1.147236149642312242, 1.739494102415694243, -0.9234435978164361458 ) ) ;
#65306=CARTESIAN_POINT ( 'NONE',  ( 2.256202855815407915, 0.9821592622454662358, 2.071323110799852873 ) ) ;
#65308=CARTESIAN_POINT ( 'NONE',  ( 2.425908952446104827, -1.891012092455180760, 0.2844710172774585488 ) ) ;
#65311=CARTESIAN_POINT ( 'NONE',  ( 0.8791531640492165067, -1.821740142837099174, -0.8571184184497283587 ) ) ;
#65312=CARTESIAN_POINT ( 'NONE',  ( 1.323018481131872370, -1.771187822987334570, -0.8437873667686208723 ) ) ;
#65316=CARTESIAN_POINT ( 'NONE',  ( 4.136730066327800159, -1.819077861029708032, 1.030257495502053589 ) ) ;
#65317=CARTESIAN_POINT ( 'NONE',  ( 2.764225215535959457, -1.222102382295175760, 1.280393980213704763 ) ) ;
#65321=CARTESIAN_POINT ( 'NONE',  ( 5.068466688948791266, -2.157128183272677191, -0.7757897288535390290 ) ) ;
#65322=CARTESIAN_POINT ( 'NONE',  ( 4.698987106650459822, -0.4602053158732459237, 1.678299975232977026 ) ) ;
#65326=CARTESIAN_POINT ( 'NONE',  ( 4.411323335215872277, 0.4626541248624673752, 1.670896574705359461 ) ) ;
#65327=CARTESIAN_POINT ( 'NONE',  ( 4.914598841593178946, 0.8265366316180179362, 2.007889688367751724 ) ) ;
#65329=CARTESIAN_POINT ( 'NONE',  ( 5.647672796105281279, 1.985869605424210649, -0.3494789899042491932 ) ) ;
#65330=CARTESIAN_POINT ( 'NONE',  ( 0.3124999997796079620, 1.451031294483781764, 1.451031289061110341 ) ) ;
#65332=CARTESIAN_POINT ( 'NONE',  ( 2.643477790179576292, -1.426271481392614948, -1.295054687222449541 ) ) ;
#65334=CARTESIAN_POINT ( 'NONE',  ( 5.291355414077095531, -0.05489642510923819357, -2.220905102120291019 ) ) ;
#65336=CARTESIAN_POINT ( 'NONE',  ( 6.983263157960404754, 0.5693283498368858497, 2.097578288773850552 ) ) ;
#65339=CARTESIAN_POINT ( 'NONE',  ( 2.034109888970101920, -2.153751770765993001, 0.5431444268512666262 ) ) ;
#65345=CARTESIAN_POINT ( 'NONE',  ( -0.05211191391743182078, -1.802403943428915412, -0.9041556775107384425 ) ) ;
#65347=CARTESIAN_POINT ( 'NONE',  ( 4.896965771356657449, 0.3494220250804170314, 2.032713711554866354 ) ) ;
#65351=CARTESIAN_POINT ( 'NONE',  ( 6.274654046616443992, -1.776150972019393093, -0.5868208112121618969 ) ) ;
#65352=CARTESIAN_POINT ( 'NONE',  ( 5.080564943346563389, -0.6172752100359213401, 1.620779670503540659 ) ) ;
#65353=CARTESIAN_POINT ( 'NONE',  ( 4.862738897425579410, 0.1637244223539826016, -1.732714468228998994 ) ) ;
#65355=CARTESIAN_POINT ( 'NONE',  ( 2.296762559223310074, 1.838876890742843884, -1.368561501106011713 ) ) ;
#65358=CARTESIAN_POINT ( 'NONE',  ( 5.302318524065624317, 1.582279558761565452, -1.366676729786527211 ) ) ;
#65359=CARTESIAN_POINT ( 'NONE',  ( 1.359045109759978498, 1.814150759811587355, -0.3131490413979670651 ) ) ;
#65361=CARTESIAN_POINT ( 'NONE',  ( 2.303361484738715159, 1.314996338066702242, -1.528741580717301263 ) ) ;
#65362=CARTESIAN_POINT ( 'NONE',  ( 1.008081207548201741, -0.9882381260516819310, -1.956047874660173047 ) ) ;
#65365=CARTESIAN_POINT ( 'NONE',  ( 1.574760213118006735, 1.391939136705011348, -1.532762857463897843 ) ) ;
#65368=CARTESIAN_POINT ( 'NONE',  ( 3.510498622083501719, -2.118129049236017192, -0.1023006277712720374 ) ) ;
#65370=CARTESIAN_POINT ( 'NONE',  ( -0.005450286198350333053, -0.4226363183827580583, -1.886779976948229853 ) ) ;
#65378=CARTESIAN_POINT ( 'NONE',  ( 3.164323975240455944, 2.019972749466778073, -0.004219792236043878007 ) ) ;
#65379=CARTESIAN_POINT ( 'NONE',  ( 0.5695303461548965052, 0.2060630844733425115, -2.095861547610248454 ) ) ;
#65382=CARTESIAN_POINT ( 'NONE',  ( 5.418752549068918789, -1.349321427123598038, 1.281850857350794959 ) ) ;
#65387=CARTESIAN_POINT ( 'NONE',  ( 6.280161615599199720, -1.104627599893250434, 1.739653883609869833 ) ) ;
#65391=CARTESIAN_POINT ( 'NONE',  ( 2.284178307277694664, -1.682821195468919395, 0.4169209145809901762 ) ) ;
#65392=CARTESIAN_POINT ( 'NONE',  ( 1.253398004092287854, 0.7024035357156286352, 1.592479786115083229 ) ) ;
#65394=CARTESIAN_POINT ( 'NONE',  ( 6.428381082836107652, 1.334599446741807638, -1.882477381066828936 ) ) ;
#65397=CARTESIAN_POINT ( 'NONE',  ( 2.477870184918748997, 1.265364588504451548, 1.626488340418334566 ) ) ;
#65399=CARTESIAN_POINT ( 'NONE',  ( 1.370470000664014254, -0.4925687793003556969, 1.954872606163795989 ) ) ;
#65402=CARTESIAN_POINT ( 'NONE',  ( 1.094530253197498526, -0.4767503703589200392, -1.912843428949811075 ) ) ;
#65403=CARTESIAN_POINT ( 'NONE',  ( 4.412309042748480792, -1.912102599942141268, -0.04143165621695726192 ) ) ;
#65405=CARTESIAN_POINT ( 'NONE',  ( 5.725267921653402148, -0.05769419298589681389, 2.206291853148376170 ) ) ;
#65409=CARTESIAN_POINT ( 'NONE',  ( 0.1354234094306828728, -0.09670520914860020190, 2.017474364592846570 ) ) ;
#65411=CARTESIAN_POINT ( 'NONE',  ( 4.137936126805092485, -1.588447180316322260, -1.674080592224574504 ) ) ;
#65412=CARTESIAN_POINT ( 'NONE',  ( 4.738696794244872557, -1.902450960283699199, -0.4786090228221794307 ) ) ;
#65413=CARTESIAN_POINT ( 'NONE',  ( 1.955835763735654487, -0.6658547638305843952, 1.845409454533278648 ) ) ;
#65417=CARTESIAN_POINT ( 'NONE',  ( 0.3568547849697421004, -1.996003273109921983, -0.7069239421778094057 ) ) ;
#65420=CARTESIAN_POINT ( 'NONE',  ( 0.5679803739370090643, -1.732728882149033645, -0.6228371021387222317 ) ) ;
#65422=CARTESIAN_POINT ( 'NONE',  ( 3.784171691162826701, -1.288926714175726129, -1.746948845794197958 ) ) ;
#65424=CARTESIAN_POINT ( 'NONE',  ( 2.057031522680652369, 0.4693188842763912905, 2.067847215655476134 ) ) ;
#65428=CARTESIAN_POINT ( 'NONE',  ( 2.161468745749118625, 0.3553341821136410950, -2.029755476197503850 ) ) ;
#65432=CARTESIAN_POINT ( 'NONE',  ( -0.02244404828157658613, 0.6916080914694566761, -2.270927585766496559 ) ) ;
#65433=CARTESIAN_POINT ( 'NONE',  ( 5.233030847706650057, 1.768443763404730307, 0.7281017474275592871 ) ) ;
#65435=CARTESIAN_POINT ( 'NONE',  ( 1.599281762659544137, 1.849886183345637258, -1.302228464298058830 ) ) ;
#65437=CARTESIAN_POINT ( 'NONE',  ( 1.722643027415799999, 1.340613184126436597, -1.218586174478804907 ) ) ;
#65439=CARTESIAN_POINT ( 'NONE',  ( 1.674859764755828095, 1.664904793830531027, -0.9475745862929999541 ) ) ;
#65440=CARTESIAN_POINT ( 'NONE',  ( 3.104029480343179603, 0.7476448069429382226, -1.930825944200013966 ) ) ;
#65442=CARTESIAN_POINT ( 'NONE',  ( 1.112115884188523918, -0.8845927946041342027, -1.761928416731074476 ) ) ;
#65443=CARTESIAN_POINT ( 'NONE',  ( 5.830678075864223153, 1.857343136638961445, 0.5113247108688694365 ) ) ;
#65444=CARTESIAN_POINT ( 'NONE',  ( 0.6457025891282016650, -1.976290545051001768, 1.191322501153786906 ) ) ;
#65448=CARTESIAN_POINT ( 'NONE',  ( 5.670399732568969675, -0.9243551164253935859, -1.844019960785907797 ) ) ;
#65452=CARTESIAN_POINT ( 'NONE',  ( 6.405314555823123257, 1.748765893162683271, 1.173091541056320297 ) ) ;
#65455=CARTESIAN_POINT ( 'NONE',  ( 4.640002929648442631, 0.9288797265196678810, -1.951996720969489951 ) ) ;
#65456=CARTESIAN_POINT ( 'NONE',  ( 5.408855464265644564, -0.4929012147626107843, -1.958461550952787844 ) ) ;
#65457=FACE_OUTER_BOUND ( 'NONE', #146408, .T. ) ;
#65464=CARTESIAN_POINT ( 'NONE',  ( 3.731657894805060938, 0.6748485617756972976, -1.900415309456899182 ) ) ;
#65469=CARTESIAN_POINT ( 'NONE',  ( 4.663041391408608405, -1.929494027986548454, -0.9748474430888448561 ) ) ;
#65475=CARTESIAN_POINT ( 'NONE',  ( 6.011342256177334420, -1.897693555989588887, 0.6820111564242032909 ) ) ;
#65477=CARTESIAN_POINT ( 'NONE',  ( 0.6446037793155032780, -1.481899804082789984, 0.8824728545121940382 ) ) ;
#65483=CARTESIAN_POINT ( 'NONE',  ( 6.626239551081194001, 1.076695052409048614, -1.529385127534782951 ) ) ;
#65484=CARTESIAN_POINT ( 'NONE',  ( 0.8736902326584498057, 0.3905749221770152269, -1.974679160882378826 ) ) ;
#65487=CARTESIAN_POINT ( 'NONE',  ( 3.452368941479638131, 2.206952907609287973, 0.002057427529567057434 ) ) ;
#65491=CARTESIAN_POINT ( 'NONE',  ( 2.069135417989849568, -1.637292086295978111, 1.347470637625711731 ) ) ;
#65492=CARTESIAN_POINT ( 'NONE',  ( 2.179314750421776026, 1.560514648525725745, 1.277027416600539533 ) ) ;
#65493=CARTESIAN_POINT ( 'NONE',  ( 2.390610142633019741, -1.734584137932100312, -0.5226098844451251280 ) ) ;
#65498=CARTESIAN_POINT ( 'NONE',  ( 0.4971116367980681350, -0.2779505141972256066, 1.895288638825567862 ) ) ;
#65506=CARTESIAN_POINT ( 'NONE',  ( 3.608425205800522839, -0.8741791752944136906, -1.977237025433141504 ) ) ;
#65510=CARTESIAN_POINT ( 'NONE',  ( 2.426173717206762781, -2.096881089210366422, 0.3156149858808757203 ) ) ;
#65511=CARTESIAN_POINT ( 'NONE',  ( 6.510779352739587189, 1.350450193652263930, -1.228632259304612839 ) ) ;
#65512=CARTESIAN_POINT ( 'NONE',  ( 3.145733524295030836, 0.7127697582950813793, -1.838151395584181058 ) ) ;
#65513=CARTESIAN_POINT ( 'NONE',  ( 5.941656858135131891, -1.798430535887390658, 0.6506349336675710804 ) ) ;
#65517=CARTESIAN_POINT ( 'NONE',  ( 6.496546994228061145, 1.947915994809066076, 0.2903317952503216559 ) ) ;
#65518=CARTESIAN_POINT ( 'NONE',  ( 1.658044662407763381, -1.373417096361102097, 1.373162012216273320 ) ) ;
#65523=CARTESIAN_POINT ( 'NONE',  ( 2.589882131170073709, -2.085102945988726031, -0.1528390284690275547 ) ) ;
#65527=CARTESIAN_POINT ( 'NONE',  ( 5.619756671179353624, -0.4603523440993940175, 1.855926886426212175 ) ) ;
#65529=CARTESIAN_POINT ( 'NONE',  ( 4.248781725523794073, 0.5872999373685274804, 2.127227798101683387 ) ) ;
#65530=CARTESIAN_POINT ( 'NONE',  ( 1.536444635327537833, 1.086998388645914027, -1.920427013416255768 ) ) ;
#65532=CARTESIAN_POINT ( 'NONE',  ( 0.06490398442321809735, -1.535895564731554863, 1.139000086266952483 ) ) ;
#65535=CARTESIAN_POINT ( 'NONE',  ( 3.824723168590526523, -1.392635068473629500, 1.532133406949770960 ) ) ;
#65537=CARTESIAN_POINT ( 'NONE',  ( 2.290102563249151402, -0.9248296759884739870, 1.954025333243500917 ) ) ;
#65538=CARTESIAN_POINT ( 'NONE',  ( 3.175498511859841333, 1.392037702009111033, 1.692654053968026151 ) ) ;
#65545=CARTESIAN_POINT ( 'NONE',  ( 6.592404480832670721, -0.3601991968599608795, 1.702173051257379832 ) ) ;
#65547=CARTESIAN_POINT ( 'NONE',  ( 4.926661076633905623, -1.356332079400805135, 1.564123780295342492 ) ) ;
#65548=CARTESIAN_POINT ( 'NONE',  ( 6.028941913163482269, -1.788401068206580957, 1.133005349186385402 ) ) ;
#65551=CARTESIAN_POINT ( 'NONE',  ( 3.643367292660666390, 1.782436080146361013, -0.8378801856493125477 ) ) ;
#65552=CARTESIAN_POINT ( 'NONE',  ( 5.841781729209135854, 2.289337533263948288, 0.1180171966539828449 ) ) ;
#65553=CARTESIAN_POINT ( 'NONE',  ( 3.299243935302543118, 1.439784963707075649, 1.122460502641378755 ) ) ;
#65559=CARTESIAN_POINT ( 'NONE',  ( 3.849861664782163739, -1.391318219759619002, -1.455273641467175860 ) ) ;
#65560=CARTESIAN_POINT ( 'NONE',  ( 0.1932713599902321500, -1.417659354009516148, -1.810318517150938389 ) ) ;
#65561=CARTESIAN_POINT ( 'NONE',  ( 4.944172655442597986, -0.9282843415348587257, 1.728263438747809078 ) ) ;
#65566=CARTESIAN_POINT ( 'NONE',  ( 0.5387614761330473678, -1.791220285616751173, 1.078087367808887365 ) ) ;
#65567=CARTESIAN_POINT ( 'NONE',  ( 6.016413156365523207, 1.185731173915012038, -1.314077388775713784 ) ) ;
#65569=CARTESIAN_POINT ( 'NONE',  ( 1.447511513890851864, 0.6336015447323711802, -2.097855558553712196 ) ) ;
#65570=CARTESIAN_POINT ( 'NONE',  ( 0.9600616587607477825, -1.572830678042375974, -0.7454570610717390355 ) ) ;
#65573=CARTESIAN_POINT ( 'NONE',  ( 1.435739417030171605, 0.8527202394775310612, -1.499263083578871836 ) ) ;
#65574=CARTESIAN_POINT ( 'NONE',  ( 1.628746693258641853, 0.2190750365392846177, 2.180598679842937759 ) ) ;
#65575=CARTESIAN_POINT ( 'NONE',  ( 4.073040751519330094, -2.058760688187323495, -0.7953439701907027981 ) ) ;
#65576=CARTESIAN_POINT ( 'NONE',  ( 1.920994505713587541, -1.537477318048833475, 1.533119463567463203 ) ) ;
#65578=CARTESIAN_POINT ( 'NONE',  ( 2.097004163592118164, 1.893647498693065589, 0.9473067498170744116 ) ) ;
#65581=CARTESIAN_POINT ( 'NONE',  ( 2.314399336204819857, 1.494381390340574489, -1.738437040929841082 ) ) ;
#65585=CARTESIAN_POINT ( 'NONE',  ( 4.477308758892056595, -1.984000869926884736, -0.9990560778978144763 ) ) ;
#65592=CARTESIAN_POINT ( 'NONE',  ( 3.199842427594956185, 1.824118962040650604, 0.8596310190432245868 ) ) ;
#65594=CARTESIAN_POINT ( 'NONE',  ( 0.7079710255328255375, 0.6504495457556063176, -1.957355765043818696 ) ) ;
#65599=CARTESIAN_POINT ( 'NONE',  ( 4.189532503254236318, -0.8396404696654431454, 2.024412170900617092 ) ) ;
#65600=CARTESIAN_POINT ( 'NONE',  ( 1.740861508391436274, 2.010826320759526720, -0.1511413081683593562 ) ) ;
#65601=CARTESIAN_POINT ( 'NONE',  ( 0.8898994657863326108, -0.4472179738511591895, -1.785967584704901912 ) ) ;
#65603=CARTESIAN_POINT ( 'NONE',  ( 5.614214418409627427, -0.8227427255552112184, -1.629729119005427496 ) ) ;
#65604=CARTESIAN_POINT ( 'NONE',  ( 5.766250055133458119, 1.862018000461727052, -0.7743128548072516493 ) ) ;
#65606=CARTESIAN_POINT ( 'NONE',  ( 4.118261297349164352, -1.160217402330826042, -1.942256231939092137 ) ) ;
#65608=CARTESIAN_POINT ( 'NONE',  ( 0.6980488080095709202, -0.7561646473010454894, 1.965825473679798652 ) ) ;
#65610=CARTESIAN_POINT ( 'NONE',  ( 5.143061708805018561, -0.2499388813127951525, -2.055141626981969338 ) ) ;
#65614=SHAPE_DEFINITION_REPRESENTATION ( #206145, #149737 ) ;
#65619=CARTESIAN_POINT ( 'NONE',  ( 2.589077643123653072, 1.706113014995232380, 1.074661422923957055 ) ) ;
#65621=CARTESIAN_POINT ( 'NONE',  ( 0.3344391967911933272, -1.139684030083350841, -1.788147294700337397 ) ) ;
#65622=CARTESIAN_POINT ( 'NONE',  ( 2.215342456320268383, 1.781105875021117502, -1.327318755304232933 ) ) ;
#65625=COLOUR_RGB ( '', 0.66274510, 0.83137255, 0.94901961) ;
#65627=CARTESIAN_POINT ( 'NONE',  ( 3.279693232472491893, -1.891448704997201302, 0.5207070127687256633 ) ) ;
#65634=CARTESIAN_POINT ( 'NONE',  ( 1.828540510153942922, -1.004066958311781832, -1.867862179375394005 ) ) ;
#65636=CARTESIAN_POINT ( 'NONE',  ( 6.004347769543215030, 1.959566550440184907, 0.09775035808561728656 ) ) ;
#65637=CARTESIAN_POINT ( 'NONE',  ( 2.887745953747706373, 1.527789104365802286, 1.529575784674996886 ) ) ;
#65638=CARTESIAN_POINT ( 'NONE',  ( 2.419273308677453826, -1.061688697878185206, -1.504126257600538974 ) ) ;
#65641=CARTESIAN_POINT ( 'NONE',  ( 5.015436155323918399, -0.9350583589616268121, -1.467585299639478702 ) ) ;
#65645=CARTESIAN_POINT ( 'NONE',  ( 2.026462046419864826, 1.244889377058140845, -1.767065586814352773 ) ) ;
#65648=CARTESIAN_POINT ( 'NONE',  ( 4.306017418194902469, -1.755500069608874281, 0.9912479507018998603 ) ) ;
#65650=CARTESIAN_POINT ( 'NONE',  ( 1.042116488573753497, 0.8753402851892390091, -1.976733581976031218 ) ) ;
#65651=CARTESIAN_POINT ( 'NONE',  ( 2.495336804025758859, 1.521579944813663099, 1.253379492226768477 ) ) ;
#65653=CARTESIAN_POINT ( 'NONE',  ( 3.122533544175498221, 0.05045625456868290531, 1.941573572215535393 ) ) ;
#65662=CARTESIAN_POINT ( 'NONE',  ( 1.237671066534186792, -1.994493743981802680, 0.9446329514863486265 ) ) ;
#65664=CARTESIAN_POINT ( 'NONE',  ( 5.278158119090741174, -1.046208158741080529, -1.659298866772864534 ) ) ;
#65666=CARTESIAN_POINT ( 'NONE',  ( 3.626253288856711610, 2.107507776945900524, 0.2035006255925037866 ) ) ;
#65668=CARTESIAN_POINT ( 'NONE',  ( 0.1745949693968328886, 2.059235863126197774, -2.173049245862024303 ) ) ;
#65669=CARTESIAN_POINT ( 'NONE',  ( 4.294743845541324490, 1.480121740587354573, 1.094796260939827404 ) ) ;
#65674=CARTESIAN_POINT ( 'NONE',  ( 5.625269520628737752, 1.871107552910089122, 0.9978724776121964402 ) ) ;
#65678=CARTESIAN_POINT ( 'NONE',  ( 5.641890011675567251, 0.8391073529228080252, -1.882412581722334943 ) ) ;
#65680=CARTESIAN_POINT ( 'NONE',  ( 0.7130641938532373825, -1.569203791704287809, -1.000260708767531481 ) ) ;
#65681=CARTESIAN_POINT ( 'NONE',  ( 3.667381569930192597, 1.025862638139760419, 1.528780434079744843 ) ) ;
#65686=CARTESIAN_POINT ( 'NONE',  ( 3.510573375967055654, -0.8941257848905452832, -2.017821460644920073 ) ) ;
#65687=CARTESIAN_POINT ( 'NONE',  ( 4.692800188189328203, -0.4894541170284586462, -2.208696565397149314 ) ) ;
#65689=CARTESIAN_POINT ( 'NONE',  ( 4.711091175174894730, 1.502108783192051877, -1.012348896329213765 ) ) ;
#65690=CARTESIAN_POINT ( 'NONE',  ( 5.577321932364699641, 1.455147452656019524, 1.246156846922679584 ) ) ;
#65692=CARTESIAN_POINT ( 'NONE',  ( 6.666881909320486521, -1.711340306973156977, -0.7558587634414122292 ) ) ;
#65693=CARTESIAN_POINT ( 'NONE',  ( 5.406657457964442415, 0.5403815791694633885, 1.780887135367102303 ) ) ;
#65695=CARTESIAN_POINT ( 'NONE',  ( 6.192257685097896314, -1.761771181780842577, -0.1690057029742654260 ) ) ;
#65696=CARTESIAN_POINT ( 'NONE',  ( 0.1984543448181053105, 1.387095780679182377, -1.463931301963219855 ) ) ;
#65698=CARTESIAN_POINT ( 'NONE',  ( 2.824945763694948653, 1.983238121251710950, 0.7091105908984902673 ) ) ;
#65703=CARTESIAN_POINT ( 'NONE',  ( 1.670181813679386007, 2.014099715005359670, -0.1526998803580876252 ) ) ;
#65707=CARTESIAN_POINT ( 'NONE',  ( 2.794378387653595475, -2.155598273342887339, -0.1620501260681943834 ) ) ;
#65708=CARTESIAN_POINT ( 'NONE',  ( 6.620655732516647518, 0.007553340620044743381, 1.826407896915738238 ) ) ;
#65716=CARTESIAN_POINT ( 'NONE',  ( 0.9256184737543894370, -1.394389637717853514, -1.690728713229103342 ) ) ;
#65718=CARTESIAN_POINT ( 'NONE',  ( 1.499281897245376527, 1.848817473390499844, -1.303928773892924609 ) ) ;
#65726=CARTESIAN_POINT ( 'NONE',  ( 3.356489944714312834, -1.342140201951192102, 1.153657164820639958 ) ) ;
#65728=CARTESIAN_POINT ( 'NONE',  ( 6.370183515248876382, 1.128980158350336049, 1.895982279999992359 ) ) ;
#65732=CARTESIAN_POINT ( 'NONE',  ( 5.290638740200858336, 1.525033539048275655, -1.319242139327673202 ) ) ;
#65734=CARTESIAN_POINT ( 'NONE',  ( 2.395189659270926086, 1.444574673180216706, 1.188490415850687487 ) ) ;
#65735=CARTESIAN_POINT ( 'NONE',  ( 3.063400401570901543, 1.746483293306470674, 1.111379191485066364 ) ) ;
#65737=CARTESIAN_POINT ( 'NONE',  ( 2.373185085050379506, -1.665764800640230803, -0.9392108107411781814 ) ) ;
#65743=CARTESIAN_POINT ( 'NONE',  ( 1.511816067030671729, -0.6413169068853613597, 1.801808535584384252 ) ) ;
#65744=CARTESIAN_POINT ( 'NONE',  ( 3.121486724888074882, 0.2905151309811822569, -1.940125473959073421 ) ) ;
#65750=CARTESIAN_POINT ( 'NONE',  ( 6.344996225704436554, -1.666636976361988154, 1.052594414163325220 ) ) ;
#65752=CARTESIAN_POINT ( 'NONE',  ( 2.197523118450269486, 1.838911438263282738, -0.8198142501213819822 ) ) ;
#65754=CARTESIAN_POINT ( 'NONE',  ( 2.777094422528699535, 1.814377389300044330, -1.091000554854235638 ) ) ;
#65756=CARTESIAN_POINT ( 'NONE',  ( 3.561042923925850978, 1.633862107263984065, -1.271492733312264090 ) ) ;
#65758=CARTESIAN_POINT ( 'NONE',  ( 6.369093512601681439, 2.000948562089053695, -0.6057377149290378293 ) ) ;
#65760=CARTESIAN_POINT ( 'NONE',  ( 3.856323340278215106, 0.6566615474184741563, 1.703573633380930152 ) ) ;
#65761=ORIENTED_EDGE ( 'NONE', *, *, #85738, .F. ) ;
#65765=CARTESIAN_POINT ( 'NONE',  ( 5.262800499965147871, -1.601618428465928057, 1.518362080380669221 ) ) ;
#65767=CARTESIAN_POINT ( 'NONE',  ( 3.457576163436149486, -1.449788379102138869, -1.247086912153513749 ) ) ;
#65774=CARTESIAN_POINT ( 'NONE',  ( 0.5910386730991653570, -0.6632029860377097741, 1.717849102829023922 ) ) ;
#65777=CARTESIAN_POINT ( 'NONE',  ( 5.202362286721474050, -0.6290170809866748591, -1.761763226176292996 ) ) ;
#65782=CARTESIAN_POINT ( 'NONE',  ( 1.533974946755271240, 1.168952700103634390, 1.584878304665905180 ) ) ;
#65783=CARTESIAN_POINT ( 'NONE',  ( 2.566029989117986077, -1.034146858587611906, 1.730878619409223163 ) ) ;
#65787=CARTESIAN_POINT ( 'NONE',  ( 2.625153213768507854, -2.044362554934661791, 0.7897752707372793779 ) ) ;
#65800=CARTESIAN_POINT ( 'NONE',  ( 5.056134578334451568, -1.329838508726857382, 1.273713382018211382 ) ) ;
#65801=CARTESIAN_POINT ( 'NONE',  ( 1.383448652483735941, 0.1460618955802815977, -2.007835497447094664 ) ) ;
#65802=CARTESIAN_POINT ( 'NONE',  ( 3.321888608656462072, -1.742702400767569992, 1.498638621658739511 ) ) ;
#65804=CARTESIAN_POINT ( 'NONE',  ( 1.322862136463611504, -1.679459703857703268, -0.8019484745323454122 ) ) ;
#65807=CARTESIAN_POINT ( 'NONE',  ( 6.064708884584704585, 0.6063723501847050334, 1.813766235492550560 ) ) ;
#65810=CARTESIAN_POINT ( 'NONE',  ( 3.913685052542864362, -1.076426932671892711, -1.792217407939109552 ) ) ;
#65811=CARTESIAN_POINT ( 'NONE',  ( 2.272138710904994863, -1.152746988206950096, 1.473173409640892162 ) ) ;
#65814=CARTESIAN_POINT ( 'NONE',  ( 6.251489360189885325, 1.835807759842246423, -0.1425652098738516838 ) ) ;
#65817=CARTESIAN_POINT ( 'NONE',  ( 4.617633504863215776, -1.690751803285206245, 0.3404669814689939011 ) ) ;
#65819=CARTESIAN_POINT ( 'NONE',  ( 0.5099215751255279372, -1.647279052675547861, 0.5420907402255652485 ) ) ;
#65824=CARTESIAN_POINT ( 'NONE',  ( 4.258752264053907055, -0.6753675163390076008, -2.063452119831588494 ) ) ;
#65825=CARTESIAN_POINT ( 'NONE',  ( 3.281694405262673087, 1.158851912627656189, 1.410738560442346801 ) ) ;
#65826=CARTESIAN_POINT ( 'NONE',  ( 1.551531708069888937, 1.481957716508151668, 1.285475804911541120 ) ) ;
#65827=CARTESIAN_POINT ( 'NONE',  ( 5.524650688480493343, 0.4156912398748518478, 2.075975271109116171 ) ) ;
#65829=CARTESIAN_POINT ( 'NONE',  ( 6.005493137707444973, -2.275576565988911337, 0.2767016799969032603 ) ) ;
#65834=CARTESIAN_POINT ( 'NONE',  ( 1.823052125313682215, 1.569171740784220281, -1.426411057285102979 ) ) ;
#65838=CARTESIAN_POINT ( 'NONE',  ( 5.963789030284865511, -0.5350816163755196531, 2.103975319158644552 ) ) ;
#65841=CARTESIAN_POINT ( 'NONE',  ( 2.543850053281167423, -2.071606161961367043, 0.8020612402455605805 ) ) ;
#65843=CARTESIAN_POINT ( 'NONE',  ( 6.152970239395502361, 1.038990588714868490, 1.728003889287746286 ) ) ;
#65845=CARTESIAN_POINT ( 'NONE',  ( 4.153227615898272163, 1.745077553047107433, -1.099210343703932669 ) ) ;
#65851=CARTESIAN_POINT ( 'NONE',  ( 4.458453498679889826, -1.646799808365447149, -0.8236825204945982248 ) ) ;
#65853=CARTESIAN_POINT ( 'NONE',  ( 1.342334339533798104, 0.3310447913058271463, 1.692513552724637771 ) ) ;
#65854=CARTESIAN_POINT ( 'NONE',  ( -0.1531117392989979065, -1.803405091603600185, -0.9023890051431044945 ) ) ;
#65855=CARTESIAN_POINT ( 'NONE',  ( 2.250986472945924355, 2.253575863342609065, -0.4525425749238082829 ) ) ;
#65857=CARTESIAN_POINT ( 'NONE',  ( 1.335668079023267119, -2.045225487398461883, 0.9674528744543411385 ) ) ;
#65858=CARTESIAN_POINT ( 'NONE',  ( 3.809285178775764447, 1.806332912941556623, 1.082654235687771749 ) ) ;
#65860=CARTESIAN_POINT ( 'NONE',  ( 1.967667936517076166, 0.9046490693802499150, 1.520878277628298303 ) ) ;
#65868=CARTESIAN_POINT ( 'NONE',  ( 4.588250468535750137, 1.280153277506433707, 1.815263839992816042 ) ) ;
#65869=CARTESIAN_POINT ( 'NONE',  ( 3.240350661220792183, 0.5327334615983710941, 2.125583950146384904 ) ) ;
#65875=CARTESIAN_POINT ( 'NONE',  ( 6.610000000000021636, 3.695490760540712127, 2.514297579034238783 ) ) ;
#65877=CARTESIAN_POINT ( 'NONE',  ( 5.431924468521282634, -2.068440459917933794, 0.4666711972392265650 ) ) ;
#65883=CARTESIAN_POINT ( 'NONE',  ( 6.550350952284553330, -1.418464805562440922, 1.173678288350611609 ) ) ;
#65886=CARTESIAN_POINT ( 'NONE',  ( 1.452286687950472999, -1.492487064643189809, -0.8950295028009451759 ) ) ;
#65888=CARTESIAN_POINT ( 'NONE',  ( 0.1507198084474276056, -0.4258245693303016610, -1.922078969575198526 ) ) ;
#65892=CARTESIAN_POINT ( 'NONE',  ( 4.873979933848565871, 1.241796773192262116, 1.769252301715443565 ) ) ;
#65896=CARTESIAN_POINT ( 'NONE',  ( 4.522454563201145028, 1.332364063043836033, -1.702191164408660251 ) ) ;
#65900=CARTESIAN_POINT ( 'NONE',  ( 5.553970887368382847, 1.969207887765548559, -0.09415503477229987539 ) ) ;
#65901=CARTESIAN_POINT ( 'NONE',  ( 5.518767629808705166, 1.731759826824400106, -0.08707812323833011292 ) ) ;
#65903=CARTESIAN_POINT ( 'NONE',  ( 2.085717061910817183, -0.9337068281064246911, 1.982830571388309204 ) ) ;
#65904=CARTESIAN_POINT ( 'NONE',  ( 3.364621831457567769, 1.035725732715401470, 2.062151656813861145 ) ) ;
#65905=CARTESIAN_POINT ( 'NONE',  ( 4.270816029187285423, -1.921422972303673093, -0.7454010919232464394 ) ) ;
#65906=CARTESIAN_POINT ( 'NONE',  ( 0.6033350840282033500, -1.932664299774440098, 0.1897328419256556487 ) ) ;
#65910=CARTESIAN_POINT ( 'NONE',  ( 4.148766697842418694, 2.080301416381886703, 0.4105806053946169376 ) ) ;
#65912=CARTESIAN_POINT ( 'NONE',  ( 1.582657950916711131, -0.6767122143778031562, 1.899619169727875700 ) ) ;
#65914=CARTESIAN_POINT ( 'NONE',  ( 4.348781676370103710, 0.5853419563807431558, 2.127667884090424621 ) ) ;
#65923=CARTESIAN_POINT ( 'NONE',  ( 4.627839754413318296, -1.266395719900258232, -1.625807017514354191 ) ) ;
#65926=CARTESIAN_POINT ( 'NONE',  ( 3.334632977657724151, 1.279679970181834436, -1.562544408365494686 ) ) ;
#65929=CARTESIAN_POINT ( 'NONE',  ( 2.606383665309390363, -0.7875068868475536554, -1.904698518741376079 ) ) ;
#65932=CARTESIAN_POINT ( 'NONE',  ( -0.2409995289980037536, -0.004801160710915518791, -2.000252362011435192 ) ) ;
#65933=CARTESIAN_POINT ( 'NONE',  ( 1.218424693763892730, -0.04700249260505655335, 1.840701667592301138 ) ) ;
#65934=CARTESIAN_POINT ( 'NONE',  ( 6.375609195709820654, 2.113139023092651225, -0.6363509056886568205 ) ) ;
#65936=CARTESIAN_POINT ( 'NONE',  ( 1.687033600898584895, -0.3153356727807927196, -2.138329785107299319 ) ) ;
#65938=CARTESIAN_POINT ( 'NONE',  ( 1.745327705122714956, 0.3399549603602426417, -1.987498286102694411 ) ) ;
#65940=CARTESIAN_POINT ( 'NONE',  ( 0.2681426532152464959, -1.225442487749365483, 1.413462724991432218 ) ) ;
#65943=CARTESIAN_POINT ( 'NONE',  ( 4.522318884118472049, 1.213545612936163032, -1.553610194691892765 ) ) ;
#65944=CARTESIAN_POINT ( 'NONE',  ( 4.891814693739657827, -2.006371927678828104, 0.2024599332275459629 ) ) ;
#65948=CARTESIAN_POINT ( 'NONE',  ( -0.004863692847738298151, -0.4900785244342681368, -2.159743284330918112 ) ) ;
#65949=CARTESIAN_POINT ( 'NONE',  ( 5.828598057497599960, -1.316348130051235410, 1.597988563933512074 ) ) ;
#65953=CARTESIAN_POINT ( 'NONE',  ( 5.519787823685118333, -0.4868164491665989413, 1.960129884169951708 ) ) ;
#65955=CARTESIAN_POINT ( 'NONE',  ( 3.686388391042205726, -1.138424198849327107, 2.007274438705310970 ) ) ;
#65956=CARTESIAN_POINT ( 'NONE',  ( 1.112259789790952746, 2.060362754584772471, -0.09740899567091049205 ) ) ;
#65964=CARTESIAN_POINT ( 'NONE',  ( 4.492743645254620333, 2.128474237214292852, 0.4277247895240059994 ) ) ;
#65966=CARTESIAN_POINT ( 'NONE',  ( 3.175182228840720988, 1.170341537027960843, 1.421418621496411516 ) ) ;
#65968=CARTESIAN_POINT ( 'NONE',  ( 4.739868811304373430, 2.185674081084403753, 0.1610935195608814985 ) ) ;
#65970=CARTESIAN_POINT ( 'NONE',  ( 5.313438862022389131, -0.3376633510823018880, 2.237075724153537504 ) ) ;
#65976=CARTESIAN_POINT ( 'NONE',  ( 6.169200886764430791, 0.1279487620423936933, -1.765195888111121159 ) ) ;
#65977=CARTESIAN_POINT ( 'NONE',  ( 4.600248117428091810, -0.9470982757478171310, 1.776368884175743235 ) ) ;
#65979=CARTESIAN_POINT ( 'NONE',  ( 3.135867587238525100, -1.413284743790550468, -1.561492743641406999 ) ) ;
#65980=CARTESIAN_POINT ( 'NONE',  ( 2.407709352951839854, -1.104968261951447595, -1.564578956373291696 ) ) ;
#65982=CARTESIAN_POINT ( 'NONE',  ( 3.156658437648862225, -0.5693117071641734528, -1.885488911330883255 ) ) ;
#65983=CARTESIAN_POINT ( 'NONE',  ( 4.763928514684708126, 0.6297656808758389513, -1.919195086291412888 ) ) ;
#65984=CARTESIAN_POINT ( 'NONE',  ( 0.9713206009373563932, 1.803875226702996049, -0.4951341686536685494 ) ) ;
#65985=CARTESIAN_POINT ( 'NONE',  ( 1.310910670669521272, -1.548711629584406113, 1.204245502051364936 ) ) ;
#65986=CARTESIAN_POINT ( 'NONE',  ( 0.7207899753199145110, 1.446443371814851941, -1.251069288267861346 ) ) ;
#65991=CARTESIAN_POINT ( 'NONE',  ( 5.946149726614578412, 1.868617323842229894, 0.09011704611043556967 ) ) ;
#65994=CARTESIAN_POINT ( 'NONE',  ( 6.227406488038683463, 0.1581931229415085571, -2.064300627111631314 ) ) ;
#65996=CARTESIAN_POINT ( 'NONE',  ( 1.451716722110554025, 1.566445173006292935, 1.353826630019476562 ) ) ;
#66001=CARTESIAN_POINT ( 'NONE',  ( 6.006510593949522026, -2.110231943656666331, -0.2080817731764383061 ) ) ;
#66006=CARTESIAN_POINT ( 'NONE',  ( 6.654749070045313353, -0.5220710138904552933, -1.891073168474053823 ) ) ;
#66009=CARTESIAN_POINT ( 'NONE',  ( 3.356795910091507906, -0.8196482158769200499, 1.842165019812888049 ) ) ;
#66010=CARTESIAN_POINT ( 'NONE',  ( 3.151485257178482158, 1.867856130240726387, -0.4247363484005464151 ) ) ;
#66012=CARTESIAN_POINT ( 'NONE',  ( 1.892365914234435120, -0.5883382831698009685, -2.111031122750434363 ) ) ;
#66014=CARTESIAN_POINT ( 'NONE',  ( 3.233525009082056201, -1.253693836546897700, -1.388425355430204622 ) ) ;
#66018=CARTESIAN_POINT ( 'NONE',  ( 5.273117041167244778, 1.866726688708058690, -0.9990383793265914525 ) ) ;
#66020=CARTESIAN_POINT ( 'NONE',  ( 6.848098043024292814, -0.8888149443028300345, 1.868052569137634400 ) ) ;
#66021=CARTESIAN_POINT ( 'NONE',  ( 2.155913254374627552, 0.8966022695893551830, 1.888892756932699646 ) ) ;
#66023=CARTESIAN_POINT ( 'NONE',  ( 0.5512174377280190107, 0.5480947683692177774, -1.635447244754190788 ) ) ;
#66033=CARTESIAN_POINT ( 'NONE',  ( 1.541375357114631806, -1.705629342057282560, 0.6104535550692562484 ) ) ;
#66039=CARTESIAN_POINT ( 'NONE',  ( 6.639320575229240795, 2.471732717405307422, 2.181477732991484064 ) ) ;
#66044=ORIENTED_EDGE ( 'NONE', *, *, #204596, .T. ) ;
#66046=CARTESIAN_POINT ( 'NONE',  ( 2.822522581191502677, -1.285663882657582580, 1.345810825326615223 ) ) ;
#66047=CARTESIAN_POINT ( 'NONE',  ( -0.03574161356561295771, -1.858227405880557015, -0.4649775414454700995 ) ) ;
#66048=CARTESIAN_POINT ( 'NONE',  ( 6.598663746767657656, -0.5144617408539242653, -1.856373320315672037 ) ) ;
#66054=CARTESIAN_POINT ( 'NONE',  ( 4.082825143736307005, 1.868653194780546922, 0.6220825103698603975 ) ) ;
#66055=CARTESIAN_POINT ( 'NONE',  ( 1.471502243059899850, -1.820439715282649251, -1.087164402369590555 ) ) ;
#66057=DIRECTION ( 'NONE',  ( -1.000000000000000000, 0.000000000000000000, 0.000000000000000000 ) ) ;
#66059=CARTESIAN_POINT ( 'NONE',  ( 5.789076383285488347, 1.657349226701849476, 1.433863557930945332 ) ) ;
#66061=CARTESIAN_POINT ( 'NONE',  ( 3.926716319054617266, 1.828954700887480245, 0.6050711068611572818 ) ) ;
#66063=CARTESIAN_POINT ( 'NONE',  ( 0.6920833903016985200, -1.811158644599793810, -0.2285449354127722099 ) ) ;
#66064=CARTESIAN_POINT ( 'NONE',  ( 1.594636444620714633, -2.196503929104542951, -0.2137616909994101699 ) ) ;
#66069=CARTESIAN_POINT ( 'NONE',  ( 6.157084851585769236, 1.612115889470520314, -1.131004145815546424 ) ) ;
#66070=CARTESIAN_POINT ( 'NONE',  ( 1.101004982060274751, -0.4702163980460572490, 1.884172457509038834 ) ) ;
#66071=CARTESIAN_POINT ( 'NONE',  ( 6.204520426337317929, -1.658329656736241553, -1.591615412813138564 ) ) ;
#66073=CARTESIAN_POINT ( 'NONE',  ( 4.276097919418925031, -0.9535845961709583651, -1.597878833905818086 ) ) ;
#66079=CARTESIAN_POINT ( 'NONE',  ( 0.3807642395799659130, -0.2741851280289032688, -2.174293136291181483 ) ) ;
#66083=CARTESIAN_POINT ( 'NONE',  ( 1.822601884235462766, 1.703052241681313861, 0.6583118566880485911 ) ) ;
#66085=CARTESIAN_POINT ( 'NONE',  ( 3.480872026922664286, -1.732388960670039113, -0.08070120533314528721 ) ) ;
#66087=CARTESIAN_POINT ( 'NONE',  ( 6.509000000000039421, 2.968845098214093703, 2.453284407971462411 ) ) ;
#66090=CARTESIAN_POINT ( 'NONE',  ( 6.393173274427864428, 1.585754722747900969, -0.9045919592586546543 ) ) ;
#66091=CARTESIAN_POINT ( 'NONE',  ( 4.416819765676714304, -1.456490764316048292, 1.314424223973278183 ) ) ;
#66094=CARTESIAN_POINT ( 'NONE',  ( 4.266349992362879817, 2.119992548681798095, -0.05317809935000831351 ) ) ;
#66098=CARTESIAN_POINT ( 'NONE',  ( 2.518496159030516601, 0.8812310945605882351, 1.873447404777649261 ) ) ;
#66102=CARTESIAN_POINT ( 'NONE',  ( 2.497091698460200071, -2.273154071007321697, 0.3411551791231131059 ) ) ;
#66110=CARTESIAN_POINT ( 'NONE',  ( 3.955252344019274169, -1.661368509396843995, 0.9470704235666274062 ) ) ;
#66111=CARTESIAN_POINT ( 'NONE',  ( 4.911038474854160896, 1.501934305467259145, 0.8478258478515336982 ) ) ;
#66112=CARTESIAN_POINT ( 'NONE',  ( 3.854704076794239764, -1.883312302057647880, -0.7212934815618715634 ) ) ;
#66113=CARTESIAN_POINT ( 'NONE',  ( 4.922631952865072158, -1.624392127635465144, -1.626674183726722678 ) ) ;
#66115=CARTESIAN_POINT ( 'NONE',  ( 1.102499568101540817, -2.207063161980229005, 0.003256074490760872773 ) ) ;
#66117=CARTESIAN_POINT ( 'NONE',  ( 5.536323748068817885, 1.743679661707888018, 0.3015777700523143978 ) ) ;
#66119=CARTESIAN_POINT ( 'NONE',  ( 1.693750089093534861, -0.7690282282955845927, 2.159540072747981654 ) ) ;
#66120=CARTESIAN_POINT ( 'NONE',  ( 6.298766309436587996, 1.533505995929709487, 1.018591839899836371 ) ) ;
#66122=CARTESIAN_POINT ( 'NONE',  ( 6.615165563918417924, -2.126712762998611783, 0.5283135293715838232 ) ) ;
#66126=CARTESIAN_POINT ( 'NONE',  ( 6.566853775770633561, 1.536883091774071453, -1.387433097640700774 ) ) ;
#66127=CARTESIAN_POINT ( 'NONE',  ( 1.815639016007553730, -1.320828798922760949, -1.523793687088881299 ) ) ;
#66129=CARTESIAN_POINT ( 'NONE',  ( 5.443948574151852959, 0.7788650187186187956, -1.762213160536057144 ) ) ;
#66131=CARTESIAN_POINT ( 'NONE',  ( 1.881385292706035051, -2.033259550720186049, -0.8950972351880029931 ) ) ;
#66136=CARTESIAN_POINT ( 'NONE',  ( 5.003314770209169815, -1.731378854590956307, 0.1774945436790342501 ) ) ;
#66138=CARTESIAN_POINT ( 'NONE',  ( 3.191801227909254912, -1.315628469008291557, -1.455533501494077342 ) ) ;
#66143=CARTESIAN_POINT ( 'NONE',  ( 4.517028817706403743, 2.066010597640522750, 0.9224273224419097250 ) ) ;
#66144=CARTESIAN_POINT ( 'NONE',  ( 0.6782753517312088976, -1.101985112813896883, -1.743456004656674718 ) ) ;
#66147=CARTESIAN_POINT ( 'NONE',  ( 2.624197652063056996, -1.302182479666073700, -1.850046142848650321 ) ) ;
#66150=CARTESIAN_POINT ( 'NONE',  ( 2.952262541859524969, 0.6266372353985818489, 1.762611677789377440 ) ) ;
#66151=CARTESIAN_POINT ( 'NONE',  ( 1.213026639236804316, 1.670944716536880259, 0.4636423645143650241 ) ) ;
#66152=CARTESIAN_POINT ( 'NONE',  ( 5.478137895480934105, -2.137967713159651506, -0.4810252310911074525 ) ) ;
#66153=CARTESIAN_POINT ( 'NONE',  ( 6.651428954171766605, -1.847749378774863560, -1.382155756676258784 ) ) ;
#66154=CARTESIAN_POINT ( 'NONE',  ( 1.498976495884283056, 1.685333290510768744, -1.185852821821014702 ) ) ;
#66155=CARTESIAN_POINT ( 'NONE',  ( 4.611236491138351212, -1.904185011576609465, 0.3803074441277309314 ) ) ;
#66157=CARTESIAN_POINT ( 'NONE',  ( 6.907498162232361238, -0.4094499450241483318, 1.831839262316947270 ) ) ;
#66158=CARTESIAN_POINT ( 'NONE',  ( 0.9062500000000004441, 1.895863743164069470, -0.7852924748300356139 ) ) ;
#66160=CARTESIAN_POINT ( 'NONE',  ( 6.292342264464226176, -1.899326897351862664, 0.6766127494588560776 ) ) ;
#66164=CARTESIAN_POINT ( 'NONE',  ( 5.010388774477189777, -1.913804350592800629, 0.6351971752796632398 ) ) ;
#66168=CARTESIAN_POINT ( 'NONE',  ( 2.226930044512597906, -0.0006860120723567450030, 1.825872481329051222 ) ) ;
#66169=DIRECTION ( 'NONE',  ( -1.000000000000000000, 0.000000000000000000, 0.000000000000000000 ) ) ;
#66177=CARTESIAN_POINT ( 'NONE',  ( 0.1936255187755825669, 1.883021768735486434, -0.7310382463305180600 ) ) ;
#66178=CARTESIAN_POINT ( 'NONE',  ( 6.498696386931579028, -2.177790866848747342, -0.4366942510913833231 ) ) ;
#66182=CARTESIAN_POINT ( 'NONE',  ( 6.051650376505027573, 0.6007964193008934473, -1.971360088487213780 ) ) ;
#66183=CARTESIAN_POINT ( 'NONE',  ( 5.485000066852382616, -2.016597020608828839, 0.002808655738886777897 ) ) ;
#66193=CARTESIAN_POINT ( 'NONE',  ( 5.641953822799152363, -0.04667112846407085042, -2.015725140939367943 ) ) ;
#66194=CARTESIAN_POINT ( 'NONE',  ( 5.015489797737916255, -0.9877249803392706973, -1.553577481828890106 ) ) ;
#66197=CARTESIAN_POINT ( 'NONE',  ( 3.299772510450727836, 1.819142665603549425, 1.419829399881943566 ) ) ;
#66199=CARTESIAN_POINT ( 'NONE',  ( 4.780646861661003832, -2.095393720161139228, -0.5303334973314683953 ) ) ;
#66201=CARTESIAN_POINT ( 'NONE',  ( 0.9779546479521743496, -1.895077795344397575, -0.4239509559331255395 ) ) ;
#66205=CARTESIAN_POINT ( 'NONE',  ( 3.485083742438867649, 1.691615344724434200, -0.7988839237506044633 ) ) ;
#66207=CARTESIAN_POINT ( 'NONE',  ( 1.546972149855216472, 0.1906517044060058730, 1.902890584052991940 ) ) ;
#66210=CARTESIAN_POINT ( 'NONE',  ( 2.543839704335303153, -1.636039663378138886, -1.481301067789652537 ) ) ;
#66216=CARTESIAN_POINT ( 'NONE',  ( 0.9132762689940625567, -0.2936195204277583515, 1.949272377766637643 ) ) ;
#66217=CARTESIAN_POINT ( 'NONE',  ( 0.1832606990049808204, -2.239562280805599492, -0.5557475372391910140 ) ) ;
#66218=CARTESIAN_POINT ( 'NONE',  ( 1.609737659951641309, 0.5726723138891121057, -1.876404140693301414 ) ) ;
#66219=CARTESIAN_POINT ( 'NONE',  ( 4.873915701820059176, -2.023805994998853830, 0.3972042427494940076 ) ) ;
#66227=CARTESIAN_POINT ( 'NONE',  ( 1.428853742479018862, -1.379120938454091227, 1.676725645940212894 ) ) ;
#66229=CARTESIAN_POINT ( 'NONE',  ( 6.110883706712432861, -0.2185277653131960651, 1.828168259763853776 ) ) ;
#66232=CARTESIAN_POINT ( 'NONE',  ( 1.669004442688322154, 0.1428430569143137041, -1.865171992484420338 ) ) ;
#66233=CARTESIAN_POINT ( 'NONE',  ( 5.290363030411685763, -2.144575937485785566, -0.2703735795691122323 ) ) ;
#66238=CARTESIAN_POINT ( 'NONE',  ( 1.084454188491505988, -1.212558158303608913, 1.478703618145213783 ) ) ;
#66239=CARTESIAN_POINT ( 'NONE',  ( 3.186155166506371650, -1.743393047566743181, -0.3038327287053984027 ) ) ;
#66240=CARTESIAN_POINT ( 'NONE',  ( 0.7680391878876170475, 1.910087531778673187, -0.09433495293535018589 ) ) ;
#66242=CARTESIAN_POINT ( 'NONE',  ( 5.132410944242819184, 0.5605724621733051416, 1.831730044279370029 ) ) ;
#66244=CARTESIAN_POINT ( 'NONE',  ( 6.039503384146654774, 1.820429283694004141, -0.7522724601281975954 ) ) ;
#66246=CARTESIAN_POINT ( 'NONE',  ( 0.6684183810189650021, 2.117893379942568988, -0.1100008709709817956 ) ) ;
#66248=CARTESIAN_POINT ( 'NONE',  ( 4.311305935566238645, -0.3199438451688824125, 1.842931056080451935 ) ) ;
#66249=CARTESIAN_POINT ( 'NONE',  ( 0.8557438351849018243, 1.823752217391808372, -0.08689656109241167270 ) ) ;
#66251=CARTESIAN_POINT ( 'NONE',  ( 4.354274438496381627, 2.206422198305586058, -0.05263853172451230661 ) ) ;
#66254=CARTESIAN_POINT ( 'NONE',  ( 2.084505489600170680, 1.189443612574309084, -1.685003561244757364 ) ) ;
#66260=CARTESIAN_POINT ( 'NONE',  ( 6.504189997394580480, -0.8109953713257547214, 1.730197269205424160 ) ) ;
#66262=CARTESIAN_POINT ( 'NONE',  ( 3.895033709675084221, 0.3008086390649654662, 2.048262060622765279 ) ) ;
#66264=CARTESIAN_POINT ( 'NONE',  ( 1.950665695202157046, 0.6760947502928333908, 2.053231632317173538 ) ) ;
#66266=CARTESIAN_POINT ( 'NONE',  ( 1.858075313305072473, 0.7708903827231723405, -1.866970155298973921 ) ) ;
#66273=CARTESIAN_POINT ( 'NONE',  ( -0.2351498743046881446, -0.1506043639611966134, -1.983733596389973597 ) ) ;
#66274=CARTESIAN_POINT ( 'NONE',  ( 6.539320575229276677, 6.035451701470580410, 2.698157228745074576 ) ) ;
#66275=CARTESIAN_POINT ( 'NONE',  ( 4.405938146338868933, -0.9375679901368579872, -1.981035393479456008 ) ) ;
#66277=CARTESIAN_POINT ( 'NONE',  ( 4.043146078444789460, 0.09904687726844901841, 1.909973672635330910 ) ) ;
#66282=CARTESIAN_POINT ( 'NONE',  ( 2.548454031204652637, -1.388473193742698619, 1.462459214312331168 ) ) ;
#66284=CARTESIAN_POINT ( 'NONE',  ( 0.8379086502938500880, 0.9226890658239239595, -2.098657079483890353 ) ) ;
#66286=CARTESIAN_POINT ( 'NONE',  ( 4.489066604428880503, 1.540008836363685241, -0.7767696631951895858 ) ) ;
#66287=CARTESIAN_POINT ( 'NONE',  ( -0.1394461523061196473, 5.719344608737997326, -2.874279450258274249 ) ) ;
#66291=CARTESIAN_POINT ( 'NONE',  ( 0.7659737006216191801, -1.952758744216346765, 0.1886366088557633325 ) ) ;
#66292=CARTESIAN_POINT ( 'NONE',  ( 0.7779422811538607707, -1.042605501850740080, 1.552959968518424771 ) ) ;
#66294=CARTESIAN_POINT ( 'NONE',  ( 0.1755611466353291517, 7.629137130509040077, -2.844001552353003781 ) ) ;
#66298=CARTESIAN_POINT ( 'NONE',  ( 4.828658830049068484, 1.245459390374216380, -1.315641719143684885 ) ) ;
#66302=CARTESIAN_POINT ( 'NONE',  ( 5.496671973222438723, -1.768653292081886708, -0.3907654940887676509 ) ) ;
#66308=CARTESIAN_POINT ( 'NONE',  ( 6.144940932578938586, -0.2738450275633330100, -1.840644705263774217 ) ) ;
#66310=CARTESIAN_POINT ( 'NONE',  ( 3.339363673285804079, 0.4624358396413058570, -1.858828564233159675 ) ) ;
#66317=CARTESIAN_POINT ( 'NONE',  ( 5.524650688480493343, 0.4156912398748518478, 2.075975271109116171 ) ) ;
#66318=CARTESIAN_POINT ( 'NONE',  ( 0.2335756976950612018, -1.975703151049061024, 0.8776370805363906680 ) ) ;
#66321=CARTESIAN_POINT ( 'NONE',  ( 0.6041866639863550104, -0.6101368697832668664, -1.720745249832649870 ) ) ;
#66323=CARTESIAN_POINT ( 'NONE',  ( 3.610199614654508338, -0.7391254383575728282, -1.669438027971142047 ) ) ;
#66326=CARTESIAN_POINT ( 'NONE',  ( 3.033609518001907368, 1.871031307821906964, -0.6153852250644732402 ) ) ;
#66327=CARTESIAN_POINT ( 'NONE',  ( 5.126486101458046285, 0.1468865524030492364, 1.936578770319798748 ) ) ;
#66331=CARTESIAN_POINT ( 'NONE',  ( 2.420441844550869526, -0.7335502799032425081, -1.766186906296034698 ) ) ;
#66338=CARTESIAN_POINT ( 'NONE',  ( 4.863791234866603475, 1.805334366393744450, -0.2710410529033688842 ) ) ;
#66339=CARTESIAN_POINT ( 'NONE',  ( 1.346235217667652417, -0.9325981557438846048, 1.848514419461377845 ) ) ;
#66345=CARTESIAN_POINT ( 'NONE',  ( 5.471519871388384360, 1.802534880541529994, -0.5000026934619330454 ) ) ;
#66355=CARTESIAN_POINT ( 'NONE',  ( 6.596539238361469160, 2.146192635953731553, 0.3271905807876190897 ) ) ;
#66356=CARTESIAN_POINT ( 'NONE',  ( 2.021262997689095897, -1.889599275135231071, 0.9552078933684378104 ) ) ;
#66359=CARTESIAN_POINT ( 'NONE',  ( 5.823117640241993520, -1.869163851432435575, -0.8903994044791310181 ) ) ;
#66363=CARTESIAN_POINT ( 'NONE',  ( 2.941680396524527286, 0.8243158943622121981, -2.139088555740241038 ) ) ;
#66366=CARTESIAN_POINT ( 'NONE',  ( 2.513799616133075343, -0.5961229146635020903, 1.817204401178821760 ) ) ;
#66369=CARTESIAN_POINT ( 'NONE',  ( 0.4396980093101590659, -1.910362728465137439, 0.6353400594101745735 ) ) ;
#66370=CARTESIAN_POINT ( 'NONE',  ( 0.8659734994756922433, -1.952832785578303199, 0.1866259229855102009 ) ) ;
#66374=CARTESIAN_POINT ( 'NONE',  ( 3.380887635974954453, 1.889918501611790536, -0.8941524261326051493 ) ) ;
#66375=CARTESIAN_POINT ( 'NONE',  ( 2.412676795855304590, 1.579722209848779313, 0.7981720169879211735 ) ) ;
#66378=CARTESIAN_POINT ( 'NONE',  ( 5.490252784120214002, -0.5523235152877626897, -2.224609438220140234 ) ) ;
#66379=CARTESIAN_POINT ( 'NONE',  ( 3.239928156850964580, 0.4239778953066320466, 1.687749859276384878 ) ) ;
#66383=CARTESIAN_POINT ( 'NONE',  ( 2.917049273830461864, 0.5812832248327322038, 1.633648419047509792 ) ) ;
#66384=CARTESIAN_POINT ( 'NONE',  ( 3.508415132820621007, 2.171350060761201295, 0.003086831990101178078 ) ) ;
#66386=CARTESIAN_POINT ( 'NONE',  ( 5.577361344084559747, 1.530155114678043660, 1.313547687611632764 ) ) ;
#66387=CARTESIAN_POINT ( 'NONE',  ( 0.1249994045006353610, -2.052053476427470269, 7.016016019767730053E-15 ) ) ;
#66389=CARTESIAN_POINT ( 'NONE',  ( 2.538006180297863068, 0.9099634639774205613, -1.697936525022441190 ) ) ;
#66391=CARTESIAN_POINT ( 'NONE',  ( 5.168325547630102434, 2.218848025724213802, -0.1096118590232265239 ) ) ;
#66393=CARTESIAN_POINT ( 'NONE',  ( 6.983263157960366563, 2.056882910316945701, 2.252511522010155698 ) ) ;
#66397=CARTESIAN_POINT ( 'NONE',  ( 1.471644961476214597, -1.907451222982279093, -1.138109381883713578 ) ) ;
#66398=CARTESIAN_POINT ( 'NONE',  ( 6.725062055625550705, -1.793239977796506457, -0.7961783947641184467 ) ) ;
#66399=EDGE_CURVE ( 'NONE', #150774, #111149, #7052, .T. ) ;
#66405=CARTESIAN_POINT ( 'NONE',  ( 4.193840287544727374, -1.420164769765386303, -1.496150262111215934 ) ) ;
#66409=CARTESIAN_POINT ( 'NONE',  ( 5.993391575003322203, 1.416176893967495687, 1.222094818194748189 ) ) ;
#66410=CARTESIAN_POINT ( 'NONE',  ( 4.447759528527571504, -1.551977624003277212, -0.7738437340010505539 ) ) ;
#66411=CARTESIAN_POINT ( 'NONE',  ( 4.265022598847971302, 1.686782405526715545, -0.4282675217706712889 ) ) ;
#66413=CARTESIAN_POINT ( 'NONE',  ( 1.822231264363738834, 1.315867814366477484, -1.876927872033665956 ) ) ;
#66415=CARTESIAN_POINT ( 'NONE',  ( 5.583562150179168349, -0.9389753047652232842, 1.868084059271076347 ) ) ;
#66416=CARTESIAN_POINT ( 'NONE',  ( 1.534833434108737515, -1.332603482217321389, -1.270662175854364362 ) ) ;
#66419=CARTESIAN_POINT ( 'NONE',  ( 1.899064777474347654, -0.9530127170578571727, -1.777010740487514173 ) ) ;
#66420=CARTESIAN_POINT ( 'NONE',  ( -0.02321191073820921824, -0.1601477211686137825, -2.156400265872604471 ) ) ;
#66425=CARTESIAN_POINT ( 'NONE',  ( 3.457788318579996467, -1.606868461378293755, -1.383752881913953292 ) ) ;
#66427=CARTESIAN_POINT ( 'NONE',  ( 5.584540971669589737, -1.782103179330214449, -0.3958202769075992444 ) ) ;
#66433=CARTESIAN_POINT ( 'NONE',  ( 3.656514325482379757, 2.010451960178538222, 0.1936393378089220907 ) ) ;
#66434=CARTESIAN_POINT ( 'NONE',  ( 0.3410288278610376089, 0.3603064943271740428, 2.074735154451929020 ) ) ;
#66438=CARTESIAN_POINT ( 'NONE',  ( 4.680409711739222267, 1.147293496411544433, -1.465074471950976953 ) ) ;
#66444=CARTESIAN_POINT ( 'NONE',  ( 6.684453628662900826, -2.020573120193806638, -0.4047117086388977714 ) ) ;
#66448=CARTESIAN_POINT ( 'NONE',  ( 1.246934265006810927, -1.689945720101847293, -0.3868003843893202953 ) ) ;
#66449=CARTESIAN_POINT ( 'NONE',  ( 0.7611566575390321665, 0.8540426286860869354, 1.516288903859766890 ) ) ;
#66450=CARTESIAN_POINT ( 'NONE',  ( 0.3238087740765641653, -0.1086241252120211664, 2.305164108462977701 ) ) ;
#66453=CARTESIAN_POINT ( 'NONE',  ( 3.005207323352117488, 1.739114039596071803, 1.105284290502930089 ) ) ;
#66455=CARTESIAN_POINT ( 'NONE',  ( 1.282577132041575529, -1.967586879516727061, 0.4389604359977539172 ) ) ;
#66458=CARTESIAN_POINT ( 'NONE',  ( 6.403191318657627029, 1.556466930477506505, 1.037356966126230517 ) ) ;
#66459=CARTESIAN_POINT ( 'NONE',  ( 4.957238921819991262, -1.637161358497842389, 0.9882132959125531357 ) ) ;
#66461=CARTESIAN_POINT ( 'NONE',  ( 6.024089167411393220, -1.222679950896175205, -1.837027303407394507 ) ) ;
#66465=CARTESIAN_POINT ( 'NONE',  ( 6.621762855810419346, -0.4656160214656123175, 2.076383538966434017 ) ) ;
#66467=CARTESIAN_POINT ( 'NONE',  ( 3.048224541365350593, 0.8318171267079670361, -2.152611968481593419 ) ) ;
#66468=CARTESIAN_POINT ( 'NONE',  ( 4.615648854252428102, 0.4318217149890530848, -1.913582009320368371 ) ) ;
#66469=CARTESIAN_POINT ( 'NONE',  ( 1.674581101246939374, 1.321464807213859505, -1.450045219730737633 ) ) ;
#66473=CARTESIAN_POINT ( 'NONE',  ( 0.05801502780489272565, 1.224741999009547833, 1.726997829920233540 ) ) ;
#66477=CARTESIAN_POINT ( 'NONE',  ( 0.4273693582952375891, 0.9489586001507933632, -1.577591209259328275 ) ) ;
#66478=CARTESIAN_POINT ( 'NONE',  ( 4.329095027809041873, -2.023602029403932079, -0.7869089946421561343 ) ) ;
#66480=CARTESIAN_POINT ( 'NONE',  ( 1.353939357992512305, -1.539690173578952770, -1.458446627980537480 ) ) ;
#66485=CARTESIAN_POINT ( 'NONE',  ( 2.600915689618611193, 1.657045147975671817, -1.224973224035642794 ) ) ;
#66489=CARTESIAN_POINT ( 'NONE',  ( -0.02244404828157658613, 7.629137130509074716, -2.789100637983293662 ) ) ;
#66491=CARTESIAN_POINT ( 'NONE',  ( 4.529883686416775745, -1.874680353417649492, 0.3764776581506729114 ) ) ;
#66494=CARTESIAN_POINT ( 'NONE',  ( 1.581717252844972998, 2.090516975186909487, -0.8654489506779092789 ) ) ;
#66497=CARTESIAN_POINT ( 'NONE',  ( 1.195247182365884564, 1.673216051897677747, -0.6948750315247439469 ) ) ;
#66498=CARTESIAN_POINT ( 'NONE',  ( 2.167068266397979670, 1.749796802513942318, -0.7803250849751103280 ) ) ;
#66499=CARTESIAN_POINT ( 'NONE',  ( 2.998552181135270001, 2.054425100943928051, 0.2560010573490826835 ) ) ;
#66501=CARTESIAN_POINT ( 'NONE',  ( 0.7253841367629434433, -1.872807053274931244, 0.6160819575430801498 ) ) ;
#66502=CARTESIAN_POINT ( 'NONE',  ( 5.725206259757900540, -0.04501307181254722567, 1.926136320475122288 ) ) ;
#66503=CARTESIAN_POINT ( 'NONE',  ( 1.296046498377702472, 1.750325484892759409, 1.504033841696296836 ) ) ;
#66506=CARTESIAN_POINT ( 'NONE',  ( 5.600070422683368854, 0.8392489243487236683, -1.884408887491027196 ) ) ;
#66509=CARTESIAN_POINT ( 'NONE',  ( 5.754936497916005145, -1.662164095216655202, 1.293063917272518015 ) ) ;
#66512=CARTESIAN_POINT ( 'NONE',  ( 4.393933622532245842, -0.8317529007547799225, 1.995363109761492337 ) ) ;
#66513=CARTESIAN_POINT ( 'NONE',  ( 5.479167871109219767, -1.826835719847461847, -0.8615247647300682265 ) ) ;
#66514=CARTESIAN_POINT ( 'NONE',  ( -0.1399997263889611598, 2.874570648431204578, -2.488748559936367233 ) ) ;
#66520=CARTESIAN_POINT ( 'NONE',  ( 3.239470508323912146, 0.4852670486454255250, -1.957170429962351577 ) ) ;
#66525=CARTESIAN_POINT ( 'NONE',  ( 4.715790015261832835, -2.120648752638915724, 0.4184459369844309440 ) ) ;
#66531=CARTESIAN_POINT ( 'NONE',  ( 5.431267612114304200, -1.591330327768199382, -1.238307421737715019 ) ) ;
#66533=CARTESIAN_POINT ( 'NONE',  ( 1.101696929656799995, -1.725068445828933594, -0.003817819714259720019 ) ) ;
#66539=CARTESIAN_POINT ( 'NONE',  ( 6.327412175546781370, -1.761338861328298089, 0.6302073946208713862 ) ) ;
#66540=CARTESIAN_POINT ( 'NONE',  ( 1.031890287230966985, -1.963566467742537069, 0.4430998199175004704 ) ) ;
#66543=CARTESIAN_POINT ( 'NONE',  ( 2.086737175084628859, -1.302296122868449535, 1.673399772156684895 ) ) ;
#66544=CARTESIAN_POINT ( 'NONE',  ( 2.267204043252795120, 1.842440753109304330, -0.8197907266209792931 ) ) ;
#66545=CARTESIAN_POINT ( 'NONE',  ( 2.671877653990344381, 1.802496804585513868, -0.1814095246875074008 ) ) ;
#66547=CARTESIAN_POINT ( 'NONE',  ( 6.789893189004300389, -0.9291300992274166282, 1.949920244826188309 ) ) ;
#66552=CARTESIAN_POINT ( 'NONE',  ( 0.4795166263942132745, -0.6867406401212177158, 1.788596380544268616 ) ) ;
#66560=CARTESIAN_POINT ( 'NONE',  ( 3.907220446582274853, 1.852832235905249370, 1.113321777468062823 ) ) ;
#66563=CARTESIAN_POINT ( 'NONE',  ( 1.863691559860299884, -1.706161385809309650, -1.259181899442491037 ) ) ;
#66565=CARTESIAN_POINT ( 'NONE',  ( 3.514874812717229347, 1.780701125067783108, 0.8461077801947043397 ) ) ;
#66566=CARTESIAN_POINT ( 'NONE',  ( 5.906500813101932756, -1.903809282439900219, -0.1807861040028224398 ) ) ;
#66569=CARTESIAN_POINT ( 'NONE',  ( 5.898876253247024692, 0.3825491175142159417, 1.931855958600266154 ) ) ;
#66570=CARTESIAN_POINT ( 'NONE',  ( 1.060374178334378303, -1.755330386401842802, -0.8309217204432550741 ) ) ;
#66578=CARTESIAN_POINT ( 'NONE',  ( 6.270165159132718991, 1.906809857242173445, -0.1455798257045255728 ) ) ;
#66580=CARTESIAN_POINT ( 'NONE',  ( 4.828867971087246858, 2.111205472107956282, 0.6427781511747706622 ) ) ;
#66581=CARTESIAN_POINT ( 'NONE',  ( 2.151677955860908487, -1.772288797910109404, -1.314638326115322053 ) ) ;
#66583=CARTESIAN_POINT ( 'NONE',  ( 0.8383554657987003500, 1.138622818284718008, -1.536203910471350298 ) ) ;
#66586=CARTESIAN_POINT ( 'NONE',  ( 3.684089399883890614, -1.230936008959164996, -1.664559344884769088 ) ) ;
#66589=CARTESIAN_POINT ( 'NONE',  ( 2.237400686453533183, -1.931180590798301955, 0.9714560045831142077 ) ) ;
#66590=CARTESIAN_POINT ( 'NONE',  ( 3.702820756938397295, 1.880440254450808757, 1.125299312022425280 ) ) ;
#66596=CARTESIAN_POINT ( 'NONE',  ( 6.346334349054894908, 0.2861236430486256421, -1.710204530248355059 ) ) ;
#66598=CARTESIAN_POINT ( 'NONE',  ( 3.362232293424003426, -2.068089847843882279, 0.09686330349460009481 ) ) ;
#66599=CARTESIAN_POINT ( 'NONE',  ( 5.290659027526918301, 1.602671996148979483, -1.383575156158120878 ) ) ;
#66602=CARTESIAN_POINT ( 'NONE',  ( 2.676555125969529048, 1.290216341703333436, -1.488019019629209572 ) ) ;
#66603=CARTESIAN_POINT ( 'NONE',  ( 5.437530556340149701, 0.9332327497303912756, -2.093863557220442484 ) ) ;
#66604=CARTESIAN_POINT ( 'NONE',  ( 2.473051018021198200, 0.08991741065280876855, -1.823594477012622006 ) ) ;
#66609=CARTESIAN_POINT ( 'NONE',  ( 4.429943789601535009, -1.973532241649661678, 0.3969061482532297291 ) ) ;
#66610=CARTESIAN_POINT ( 'NONE',  ( 4.662917994108885189, 1.519075486231920458, -1.241376779329693258 ) ) ;
#66613=CARTESIAN_POINT ( 'NONE',  ( 0.07536363704235481131, 0.6997989235110781969, -2.226667633679416447 ) ) ;
#66614=CARTESIAN_POINT ( 'NONE',  ( -0.04130929284668418550, -1.869521504948624235, -0.9361258523304989421 ) ) ;
#66615=CARTESIAN_POINT ( 'NONE',  ( 5.752768645092715794, -1.392961553103783112, 1.091694246300749738 ) ) ;
#66617=CARTESIAN_POINT ( 'NONE',  ( 1.886939110189549185, 1.905679594745551819, -1.081921739459410059 ) ) ;
#66618=CARTESIAN_POINT ( 'NONE',  ( 0.6084659026615606425, -0.2575236531317924293, 1.721126145854386946 ) ) ;
#66620=CARTESIAN_POINT ( 'NONE',  ( 0.1335669894368343991, 0.2365985627143319114, -2.188050374159770772 ) ) ;
#66621=CARTESIAN_POINT ( 'NONE',  ( 0.7324925891301607983, 0.1221277223508714788, 1.720630200619164496 ) ) ;
#66622=CARTESIAN_POINT ( 'NONE',  ( 0.7908558668072614983, -2.181831595417762504, 0.7228866375666581634 ) ) ;
#66623=CARTESIAN_POINT ( 'NONE',  ( 0.7322823680011962821, 2.160084099745246178, 0.3691886501416344335 ) ) ;
#66624=CARTESIAN_POINT ( 'NONE',  ( 6.257189190585941141, -1.725921076436988111, -0.1656679613657590366 ) ) ;
#66625=CARTESIAN_POINT ( 'NONE',  ( 3.317197348578094562, 1.995112415077514356, 0.9436014139095407760 ) ) ;
#66627=CARTESIAN_POINT ( 'NONE',  ( 0.9015274132509668581, -1.862984440646279438, 1.114554472006025865 ) ) ;
#66628=CARTESIAN_POINT ( 'NONE',  ( -0.005637892868452093476, -0.3948761927005627337, -1.788892068844874395 ) ) ;
#66629=CARTESIAN_POINT ( 'NONE',  ( 2.589187231636483233, 1.791351791295469731, 1.128514814827277002 ) ) ;
#66631=CARTESIAN_POINT ( 'NONE',  ( 6.620655732516668834, 6.034240673559561507, 2.768629221164942145 ) ) ;
#66632=CARTESIAN_POINT ( 'NONE',  ( 5.772470297455748245, -1.221717764600898981, 1.489408783192472052 ) ) ;
#66634=CARTESIAN_POINT ( 'NONE',  ( 2.912002956782848262, -1.132189443809348273, -1.993217883792548495 ) ) ;
#66638=CARTESIAN_POINT ( 'NONE',  ( 5.285853969472154468, 2.141190784740894415, -0.5908706489107099502 ) ) ;
#66646=CARTESIAN_POINT ( 'NONE',  ( 2.654922836763852878, 1.081066371885472277, 1.701947380796410059 ) ) ;
#66648=CARTESIAN_POINT ( 'NONE',  ( 1.164971494057164492, 1.564520514315300481, -1.344193796132137964 ) ) ;
#66649=CARTESIAN_POINT ( 'NONE',  ( 6.883263157960391787, -0.001104538646235289417, 1.946037152736757925 ) ) ;
#66653=CARTESIAN_POINT ( 'NONE',  ( 3.750093249908572623, 0.7883579158753216687, 2.044908353623323016 ) ) ;
#66654=CARTESIAN_POINT ( 'NONE',  ( 1.037732671793228700, -1.587836052788630603, 1.242728777923551409 ) ) ;
#66655=CARTESIAN_POINT ( 'NONE',  ( 0.7140992756325339474, 1.701125707204936166, 0.7050099338341904165 ) ) ;
#66656=CARTESIAN_POINT ( 'NONE',  ( 4.734224819668921391, 0.3176365174208677367, 1.813369535050498360 ) ) ;
#66659=CARTESIAN_POINT ( 'NONE',  ( 5.825187583072056974, -0.04236064406601056098, 1.825263316621673848 ) ) ;
#66660=CARTESIAN_POINT ( 'NONE',  ( 6.223279759862190730, 1.994869330463379331, 0.2930738960792296233 ) ) ;
#66662=CARTESIAN_POINT ( 'NONE',  ( 4.047957556655322087, 0.7652766760943878754, -2.129282649148962925 ) ) ;
#66664=CARTESIAN_POINT ( 'NONE',  ( 6.581095821095639842, -0.09928302661296910248, -2.103742297734310984 ) ) ;
#66666=CARTESIAN_POINT ( 'NONE',  ( 4.334477209444560053, -1.194628513295314942, 1.690740121169509447 ) ) ;
#66670=CARTESIAN_POINT ( 'NONE',  ( 2.613793455771874719, -1.905494007693061098, 0.2829725131217008527 ) ) ;
#66676=CARTESIAN_POINT ( 'NONE',  ( 1.072698285844303934, 0.8645715524648779349, 1.936551149067309741 ) ) ;
#66677=CARTESIAN_POINT ( 'NONE',  ( 1.195894564581518660, 2.049875489592466238, -0.8564406981130603391 ) ) ;
#66679=CARTESIAN_POINT ( 'NONE',  ( 3.874133602078254413, 1.168181435743149921, 1.752046721337781054 ) ) ;
#66682=CARTESIAN_POINT ( 'NONE',  ( 2.769914238037580745, -1.940913097850523128, 0.2850433363836765155 ) ) ;
#66688=CARTESIAN_POINT ( 'NONE',  ( 2.021885665735908333, -0.4598567139443253682, 2.069992740399699382 ) ) ;
#66690=CARTESIAN_POINT ( 'NONE',  ( 4.932062528313536198, 1.127988425013145779, 1.604980062286972542 ) ) ;
#66691=CARTESIAN_POINT ( 'NONE',  ( 3.168983506954273999, -1.996715753333128118, -0.8287754370841573515 ) ) ;
#66692=CARTESIAN_POINT ( 'NONE',  ( 2.700538275128167687, 1.556679782967337999, 0.9830204120172959525 ) ) ;
#66695=DIRECTION ( 'NONE',  ( 1.214306433183764966E-17, 1.000000000000000000, 5.200010849845536803E-32 ) ) ;
#66696=CARTESIAN_POINT ( 'NONE',  ( 4.347407756490777153, 1.739891706657967552, -0.04609750694275702165 ) ) ;
#66699=CARTESIAN_POINT ( 'NONE',  ( 1.868271315571629509, 1.111147431007172726, 1.854118885846419262 ) ) ;
#66700=CARTESIAN_POINT ( 'NONE',  ( 4.147814418418220406, -0.1948115906579734602, -2.006652602119996853 ) ) ;
#66702=CARTESIAN_POINT ( 'NONE',  ( 1.710078970767275885, -2.145365142986368934, 0.2646356489638818088 ) ) ;
#66703=CARTESIAN_POINT ( 'NONE',  ( 2.993000350225515138, 1.691612214138412007, -1.012252976823005968 ) ) ;
#66704=CARTESIAN_POINT ( 'NONE',  ( 3.110573765929941725, 1.430363465515383625, -1.356829130874689815 ) ) ;
#66707=CARTESIAN_POINT ( 'NONE',  ( 3.825673241664818036, 1.036335792742661299, -1.642260645495984495 ) ) ;
#66717=CARTESIAN_POINT ( 'NONE',  ( 0.7630613749609324037, -1.597064910551798667, 1.523150255686569254 ) ) ;
#66720=CARTESIAN_POINT ( 'NONE',  ( 4.926587646396720643, -1.284401507782207963, 1.482881906352449874 ) ) ;
#66721=CARTESIAN_POINT ( 'NONE',  ( 2.830704105008190030, 0.7231396562890277657, -1.882474209725725434 ) ) ;
#66723=CARTESIAN_POINT ( 'NONE',  ( 3.257133915093980203, 0.04755548373316278304, -2.116953498886654295 ) ) ;
#66725=CARTESIAN_POINT ( 'NONE',  ( 0.07479286986303290696, 5.725009232006174287, -2.449550298930736059 ) ) ;
#66727=CARTESIAN_POINT ( 'NONE',  ( 4.628748294741646951, -1.682209325509572473, 0.7487199040775436298 ) ) ;
#66731=CARTESIAN_POINT ( 'NONE',  ( 5.642871316567687145, 2.044259226470702462, 0.5637153772257290640 ) ) ;
#66736=CARTESIAN_POINT ( 'NONE',  ( 5.817669245088300300, -2.011504375995844196, 0.4472435552253516411 ) ) ;
#66738=CARTESIAN_POINT ( 'NONE',  ( 0.6075646283644918766, 0.5893627863808469369, -1.765331146162614662 ) ) ;
#66739=CARTESIAN_POINT ( 'NONE',  ( 3.016969003575611818, -1.773741936391802332, 0.4936923545346691977 ) ) ;
#66744=CARTESIAN_POINT ( 'NONE',  ( 1.893488989520499377, 1.919108310403025985, -1.089527612406354873 ) ) ;
#66745=CARTESIAN_POINT ( 'NONE',  ( 5.132209903004834928, 1.169260703421838743, -1.936728657785217411 ) ) ;
#66746=CARTESIAN_POINT ( 'NONE',  ( 3.608611488583326032, 1.916353073142588403, 0.6279913346786819561 ) ) ;
#66748=CARTESIAN_POINT ( 'NONE',  ( 4.271601952734533469, 0.3905692737867596520, -1.768816315278500584 ) ) ;
#66749=CARTESIAN_POINT ( 'NONE',  ( 5.278507882932355955, -0.4720989235634742154, -1.856488224439522439 ) ) ;
#66751=CARTESIAN_POINT ( 'NONE',  ( 4.856247981345184428, 0.7163626499266174674, 1.728251504774950709 ) ) ;
#66752=CARTESIAN_POINT ( 'NONE',  ( 4.650750022344506185, -0.4068995778509130190, -1.815856201304208550 ) ) ;
#66754=CARTESIAN_POINT ( 'NONE',  ( 6.526229032160782317, 1.014938005144504274, -1.449696215517197961 ) ) ;
#66755=CARTESIAN_POINT ( 'NONE',  ( -0.1003747550864658999, -1.976661868047492998, 0.3981153667176607902 ) ) ;
#66757=CARTESIAN_POINT ( 'NONE',  ( 2.350341522438728514, 2.105628791459000393, 0.05071553880554508648 ) ) ;
#66762=CARTESIAN_POINT ( 'NONE',  ( 1.951431513787309724, -1.802353211750299167, 0.9118321038049399530 ) ) ;
#66764=CARTESIAN_POINT ( 'NONE',  ( 6.720655732516647163, 0.002698097948191854455, 1.926293798961113080 ) ) ;
#66767=CARTESIAN_POINT ( 'NONE',  ( 2.706508253401081809, -0.8245430293080566742, -1.998349536214229616 ) ) ;
#66768=CARTESIAN_POINT ( 'NONE',  ( 6.610000000000021636, 3.695490760540712127, 2.514297579034238783 ) ) ;
#66773=CARTESIAN_POINT ( 'NONE',  ( 6.509000000000012776, 0.004788705324892602276, 2.000274819378269342 ) ) ;
#66775=CARTESIAN_POINT ( 'NONE',  ( 1.523247060345904291, -2.062048068855956373, 0.7425582295156886170 ) ) ;
#66777=CARTESIAN_POINT ( 'NONE',  ( 1.007111469781604596, 1.711705730394815106, -1.479659443445595413 ) ) ;
#66785=CARTESIAN_POINT ( 'NONE',  ( 2.793947764029936831, -1.764715128225034180, -0.1343432132955291736 ) ) ;
#66787=CARTESIAN_POINT ( 'NONE',  ( 0.1652458694026041341, -1.881425287724652673, -0.9463707761560661291 ) ) ;
#66792=CARTESIAN_POINT ( 'NONE',  ( 5.009388752257521560, -1.913799287717246500, 0.6352160319311253023 ) ) ;
#66794=CARTESIAN_POINT ( 'NONE',  ( 2.869827659178546764, 0.9992216309704025079, 1.581230272166146644 ) ) ;
#66795=CARTESIAN_POINT ( 'NONE',  ( 2.360293207207576849, -2.069885933316969240, 0.04650197241463926989 ) ) ;
#66797=CARTESIAN_POINT ( 'NONE',  ( 2.478646075381494285, -1.315928518397539548, 1.387899491812602859 ) ) ;
#66802=CARTESIAN_POINT ( 'NONE',  ( 1.617294888471169312, 1.591762500684265946, 1.059657513450793953 ) ) ;
#66804=CARTESIAN_POINT ( 'NONE',  ( 2.506241959165692812, 1.961374882610424919, 0.05109738790698423877 ) ) ;
#66807=CARTESIAN_POINT ( 'NONE',  ( 5.836213162209912930, -1.179542664122106510, -1.762073437084572314 ) ) ;
#66810=CARTESIAN_POINT ( 'NONE',  ( 0.3681424317822541425, -1.226883886190757611, 1.412057460252094554 ) ) ;
#66812=CARTESIAN_POINT ( 'NONE',  ( 1.828386956846822509, -0.9528715280972717139, -1.773455306963005462 ) ) ;
#66814=CARTESIAN_POINT ( 'NONE',  ( 0.5974486649760869517, -0.3061723685214760016, 2.094854868064464970 ) ) ;
#66816=CARTESIAN_POINT ( 'NONE',  ( 2.207561477879273593, -1.661462528888792090, -1.235070534849058266 ) ) ;
#66820=CARTESIAN_POINT ( 'NONE',  ( 6.263634082940216175, 1.073540726731788908, 1.793809194602818735 ) ) ;
#66822=CARTESIAN_POINT ( 'NONE',  ( 3.944226942909400346, 1.816763600636053688, 0.1792749827478901103 ) ) ;
#66823=CARTESIAN_POINT ( 'NONE',  ( 2.666445455534327102, 0.6121260541337695260, 1.705033028387469285 ) ) ;
#66828=CARTESIAN_POINT ( 'NONE',  ( 4.876106637443972325, 1.267215935518750669, 1.806476597341267087 ) ) ;
#66831=CARTESIAN_POINT ( 'NONE',  ( 3.756429630051653312, 1.903336793139896788, 0.1845653119916731144 ) ) ;
#66838=CARTESIAN_POINT ( 'NONE',  ( 0.9074547957551477584, -0.8278116715597811925, -1.644758345054016191 ) ) ;
#66841=CARTESIAN_POINT ( 'NONE',  ( 4.868341698904518289, -1.223052743625025141, 1.415352931214426846 ) ) ;
#66847=CARTESIAN_POINT ( 'NONE',  ( 1.762491902426995605, -0.7040454445105134296, -1.839503732180563844 ) ) ;
#66848=CARTESIAN_POINT ( 'NONE',  ( 1.810172953844836341, 1.158670025852935437, -1.650096248209935945 ) ) ;
#66852=CARTESIAN_POINT ( 'NONE',  ( 2.537292984272555785, -1.624655320356691801, -1.470880813658273389 ) ) ;
#66853=CARTESIAN_POINT ( 'NONE',  ( 6.129513044595951143, -1.717388127611047421, 0.6198453807191862674 ) ) ;
#66855=CARTESIAN_POINT ( 'NONE',  ( 6.825078400183544503, 2.075476428726834577, 2.163873318353096931 ) ) ;
#66863=CARTESIAN_POINT ( 'NONE',  ( 3.649809678215182096, 0.6660801477775115664, 1.716721118343276453 ) ) ;
#66864=CARTESIAN_POINT ( 'NONE',  ( 1.207682405589046937, 1.525905122249699319, 1.313188400431253955 ) ) ;
#66865=CARTESIAN_POINT ( 'NONE',  ( 3.251609920728415037, -2.263897172838242877, -0.3959942320375854918 ) ) ;
#66867=CARTESIAN_POINT ( 'NONE',  ( 0.7427237327431088776, -0.2200284318808701234, -1.847805914472876232 ) ) ;
#66871=CARTESIAN_POINT ( 'NONE',  ( 4.799029005866479736, -0.2398712174674077491, -1.897248949554980024 ) ) ;
#66874=CARTESIAN_POINT ( 'NONE',  ( 3.650014318109519262, 0.7545864325827613683, 1.950000943494380135 ) ) ;
#66875=CARTESIAN_POINT ( 'NONE',  ( 2.465516990510143280, 1.834972510290140191, -0.3627323784974947340 ) ) ;
#66878=EDGE_CURVE ( 'NONE', #21442, #202900, #12048, .T. ) ;
#66879=CARTESIAN_POINT ( 'NONE',  ( 5.583513413114173041, -0.8223277247318347971, 1.647484189299788682 ) ) ;
#66882=CARTESIAN_POINT ( 'NONE',  ( 5.039546052477672511, -1.223360384887246743, -1.216254805912063919 ) ) ;
#66885=CARTESIAN_POINT ( 'NONE',  ( 0.2461560209003906818, 1.715711078377361032, -0.2512605247984560086 ) ) ;
#66886=CARTESIAN_POINT ( 'NONE',  ( 6.305322857734435793, 1.832379230283949667, 1.229636283518860118 ) ) ;
#66890=CARTESIAN_POINT ( 'NONE',  ( 5.120078768083678789, 2.148437930330206136, -0.3118015998682179823 ) ) ;
#66891=CARTESIAN_POINT ( 'NONE',  ( 2.930095790256614485, 1.013914413367119627, -1.518051517300327502 ) ) ;
#66892=CARTESIAN_POINT ( 'NONE',  ( 1.657006586592904673, 1.606862555911577006, -1.125131163738995577 ) ) ;
#66893=CARTESIAN_POINT ( 'NONE',  ( 5.260995011843273339, -0.05493784808423751720, -2.116803055475650730 ) ) ;
#66896=CARTESIAN_POINT ( 'NONE',  ( 6.251568577072929678, 2.286574220100371591, -0.1642174239346057829 ) ) ;
#66899=CARTESIAN_POINT ( 'NONE',  ( 1.647299267346370444, 0.2110521635003380359, 2.109970702148834754 ) ) ;
#66903=CARTESIAN_POINT ( 'NONE',  ( 6.139545750997863927, 2.009069680886385267, -0.8233997750264672177 ) ) ;
#66904=CARTESIAN_POINT ( 'NONE',  ( 6.983263157960387879, 4.689051080487334211, 2.716346346018564617 ) ) ;
#66906=CARTESIAN_POINT ( 'NONE',  ( 2.754761814426693434, 2.204812966250285999, 0.2695357242936818332 ) ) ;
#66908=CARTESIAN_POINT ( 'NONE',  ( 0.03630054827139220924, -1.841026678340401679, 1.376304820193236189 ) ) ;
#66910=CARTESIAN_POINT ( 'NONE',  ( 4.750865691763131338, -0.4467450692671371959, -2.013472809446889666 ) ) ;
#66915=CARTESIAN_POINT ( 'NONE',  ( 0.1329588055935396196, 2.886534925058126699, -2.334852352984605695 ) ) ;
#66916=CARTESIAN_POINT ( 'NONE',  ( 0.7442207691023922100, 0.6088243375477386810, 2.000016368695969327 ) ) ;
#66917=CARTESIAN_POINT ( 'NONE',  ( 4.606092368833686557, -0.09613688574180989654, 2.014232646917232916 ) ) ;
#66918=CARTESIAN_POINT ( 'NONE',  ( 4.001369526190221571, -1.836035423186295201, 0.1395379388276704880 ) ) ;
#66922=CARTESIAN_POINT ( 'NONE',  ( 2.203723468020501119, -1.724507683567375826, 0.03868650182545228799 ) ) ;
#66923=CARTESIAN_POINT ( 'NONE',  ( -0.1179535434602772825, -2.016182236903838465, -0.04464881524945257807 ) ) ;
#66924=CARTESIAN_POINT ( 'NONE',  ( 1.688534781859708067, 1.914194972067848832, 1.272504748915660899 ) ) ;
#66926=CARTESIAN_POINT ( 'NONE',  ( 1.107111304455286049, 1.712943910497457756, -1.478075018494163118 ) ) ;
#66927=CARTESIAN_POINT ( 'NONE',  ( 3.756553094297815143, 0.7580258897690328457, 1.965105124105433809 ) ) ;
#66931=CARTESIAN_POINT ( 'NONE',  ( 0.000000000000000000, 7.629137130509076492, -2.599999999999999201 ) ) ;
#66936=CARTESIAN_POINT ( 'NONE',  ( 5.203485844055394161, 1.958870149131001881, -1.047680120605886556 ) ) ;
#66937=CARTESIAN_POINT ( 'NONE',  ( 3.925867417771063739, 1.172880473742785812, -1.850976771919823793 ) ) ;
#66940=CARTESIAN_POINT ( 'NONE',  ( 5.865915527372128402, 0.6157079936559419764, -2.029145397309819021 ) ) ;
#66943=CARTESIAN_POINT ( 'NONE',  ( 6.890000000000029878, 7.629137130509094256, 2.600000000000001421 ) ) ;
#66945=CARTESIAN_POINT ( 'NONE',  ( 5.695592476053609410, 1.958610405324921588, -0.8133567297157192622 ) ) ;
#66949=CARTESIAN_POINT ( 'NONE',  ( 6.245025451202089073, -1.828886558906620774, 1.152162773130911644 ) ) ;
#66952=CARTESIAN_POINT ( 'NONE',  ( 6.339398910184078417, 0.6979989802004606947, -1.704029730133400866 ) ) ;
#66955=CARTESIAN_POINT ( 'NONE',  ( 0.8545597497816240784, 0.3412253653619911065, -1.706464705969434670 ) ) ;
#66960=CARTESIAN_POINT ( 'NONE',  ( 4.821240550277555492, -0.1094919189667045711, 2.159058991224649393 ) ) ;
#66964=CARTESIAN_POINT ( 'NONE',  ( 4.979442225389012933, 2.018306902694905425, -0.7746836383674888804 ) ) ;
#66967=CARTESIAN_POINT ( 'NONE',  ( 6.221945801152132027, -1.093087313283289230, -1.640361058829779228 ) ) ;
#66968=CARTESIAN_POINT ( 'NONE',  ( 5.325445489366991580, -1.254443461812755789, 1.197174301038748334 ) ) ;
#66971=CARTESIAN_POINT ( 'NONE',  ( 2.279091853667324141, 2.002311374866962979, -0.8913168663882904408 ) ) ;
#66972=CARTESIAN_POINT ( 'NONE',  ( 2.608792587697115639, -0.8827421749361822334, -2.132256252471361524 ) ) ;
#66973=CARTESIAN_POINT ( 'NONE',  ( 4.938775350723108026, 0.3481798140595788738, 2.030979325763365928 ) ) ;
#66974=CARTESIAN_POINT ( 'NONE',  ( 0.5154417807694658960, -1.038215432012145056, -1.640949389817857984 ) ) ;
#66979=CARTESIAN_POINT ( 'NONE',  ( 3.269896953881154644, 0.5115095171020591636, -2.057881918134551125 ) ) ;
#66980=CARTESIAN_POINT ( 'NONE',  ( 1.459611520199757706, -1.915600648959712382, -0.6298732728240025169 ) ) ;
#66982=CARTESIAN_POINT ( 'NONE',  ( 4.559734661428293201, 0.4870809927834463537, -2.152189095746533720 ) ) ;
#66984=CARTESIAN_POINT ( 'NONE',  ( 1.674410341579468442, 1.254762736130067502, -1.374450116433557856 ) ) ;
#66985=CARTESIAN_POINT ( 'NONE',  ( -0.1290005225502675879, 5.719648796287211567, -2.768066027128403217 ) ) ;
#66989=CARTESIAN_POINT ( 'NONE',  ( 6.825078400183582694, 6.033236438919748146, 2.839236806905225841 ) ) ;
#66992=CARTESIAN_POINT ( 'NONE',  ( 2.957942382388091040, 2.051108442962752409, -0.2004023863233852509 ) ) ;
#66995=CARTESIAN_POINT ( 'NONE',  ( 3.861976953351463848, 0.6784905939434657807, -1.902444917487989606 ) ) ;
#66998=CARTESIAN_POINT ( 'NONE',  ( 2.307559741017367383, -0.4527674059561050401, 2.010364544233154138 ) ) ;
#67003=CARTESIAN_POINT ( 'NONE',  ( -0.1409997244346088141, 1.357410162930408504, -2.254437325861287533 ) ) ;
#67004=CARTESIAN_POINT ( 'NONE',  ( 1.517261703430743625, -1.021610662766696764, -1.531488883528262512 ) ) ;
#67005=CARTESIAN_POINT ( 'NONE',  ( 6.182275136424624229, -1.184133725572718676, 1.862117674348878760 ) ) ;
#67007=CARTESIAN_POINT ( 'NONE',  ( 1.757319832705085627, -1.853012815387704570, -1.112828241397870066 ) ) ;
#67009=CARTESIAN_POINT ( 'NONE',  ( 2.219935720625454412, 0.9462983093676997637, -1.780669029686342331 ) ) ;
#67014=CARTESIAN_POINT ( 'NONE',  ( 4.188322375386017704, -1.949839058108787437, -0.2904977467932718382 ) ) ;
#67015=CARTESIAN_POINT ( 'NONE',  ( 2.993375309983861143, -0.3886322325962355273, 1.978555244300662874 ) ) ;
#67019=CARTESIAN_POINT ( 'NONE',  ( 6.463511354401173747, 0.3618736704080193212, -2.074577690073164060 ) ) ;
#67021=CARTESIAN_POINT ( 'NONE',  ( 5.055165704564410944, 1.723227314588217318, -1.147259442322377865 ) ) ;
#67024=CARTESIAN_POINT ( 'NONE',  ( 6.539320575229276677, 2.966918982532817051, 2.456386401752636672 ) ) ;
#67025=CARTESIAN_POINT ( 'NONE',  ( 4.834242814930416188, -1.083969679716361156, -1.704088710659272810 ) ) ;
#67027=CARTESIAN_POINT ( 'NONE',  ( 0.4618802912403723870, -0.5535076142849646441, 1.986819116141485653 ) ) ;
#67033=CARTESIAN_POINT ( 'NONE',  ( 6.827182134110234557, 2.482032550715262964, 2.096239902261677113 ) ) ;
#67035=CARTESIAN_POINT ( 'NONE',  ( 2.840461511066312728, -1.118188532415839598, 1.860977255340636516 ) ) ;
#67039=CARTESIAN_POINT ( 'NONE',  ( 2.577489280727011778, -0.9446877197298314544, 1.580272903027237774 ) ) ;
#67041=CARTESIAN_POINT ( 'NONE',  ( 4.845371438081495619, 0.6875289519675978900, -2.081009137124201658 ) ) ;
#67043=CARTESIAN_POINT ( 'NONE',  ( 4.575235619729528302, 0.004297453766812646056, -2.262689076577176106 ) ) ;
#67048=CARTESIAN_POINT ( 'NONE',  ( 6.766889846978989986, -1.619426471845460069, -0.7142080874563813131 ) ) ;
#67049=CARTESIAN_POINT ( 'NONE',  ( 4.020185130887462321, -2.007537125943322120, 0.1504822817294942383 ) ) ;
#67051=CARTESIAN_POINT ( 'NONE',  ( 2.819468948711697287, -0.2076110458819386551, 2.095707187103168945 ) ) ;
#67052=CARTESIAN_POINT ( 'NONE',  ( 0.4564612863584472380, -1.804040949374663194, -0.6446129174930875783 ) ) ;
#67055=CARTESIAN_POINT ( 'NONE',  ( 1.592182281804704003, 0.9734619808988297374, -1.712098776470400763 ) ) ;
#67056=CARTESIAN_POINT ( 'NONE',  ( 0.6021629784135495989, -0.6261829430146518272, -1.762877433595814614 ) ) ;
#67057=CARTESIAN_POINT ( 'NONE',  ( 1.275752070009423367, -1.914805681740685106, 0.4264308320794732432 ) ) ;
#67058=CARTESIAN_POINT ( 'NONE',  ( -0.1229892814952095459, -1.709044814581164973, -0.8582256167319823881 ) ) ;
#67062=CARTESIAN_POINT ( 'NONE',  ( 5.998880656844745474, 1.528293836345222312, -1.078463600801618405 ) ) ;
#67065=CARTESIAN_POINT ( 'NONE',  ( 6.403194803628889709, -1.752124481401344358, 1.102429006916323395 ) ) ;
#67067=CARTESIAN_POINT ( 'NONE',  ( 0.7310241076574041097, -1.948878508384953356, -0.6990896207654460071 ) ) ;
#67076=CARTESIAN_POINT ( 'NONE',  ( 5.775826483351648832, -1.914393393812302113, 0.4282712878391075062 ) ) ;
#67078=CARTESIAN_POINT ( 'NONE',  ( 2.723982329760873178, -1.752761823190003287, -0.9961495992579154635 ) ) ;
#67079=CARTESIAN_POINT ( 'NONE',  ( 3.467908617337426502, -0.9394263201649171169, 1.669454279737823343 ) ) ;
#67081=CARTESIAN_POINT ( 'NONE',  ( 1.822082775007987543, 1.258534617508931586, -1.793986466278547853 ) ) ;
#67083=CARTESIAN_POINT ( 'NONE',  ( 0.2333690889706925009, 5.722554199285137422, -2.647406232470352894 ) ) ;
#67084=CARTESIAN_POINT ( 'NONE',  ( 3.760894150569486616, -1.648321677062795976, -0.8843367818652316803 ) ) ;
#67088=CARTESIAN_POINT ( 'NONE',  ( 4.605136521778616654, -0.1025035295275648906, 2.114849348554531883 ) ) ;
#67090=CARTESIAN_POINT ( 'NONE',  ( 6.303194806757332458, -1.751150776259063457, 1.104182018118210262 ) ) ;
#67091=CARTESIAN_POINT ( 'NONE',  ( 2.525039811729863359, -1.949768895325499463, 0.7551890176837258162 ) ) ;
#67093=CARTESIAN_POINT ( 'NONE',  ( 1.078623681775535914, -0.03615993657634165859, -1.724571457899269911 ) ) ;
#67102=CARTESIAN_POINT ( 'NONE',  ( 0.8030048707254822116, 1.598173448761495585, -0.8528199064772985505 ) ) ;
#67107=CARTESIAN_POINT ( 'NONE',  ( 6.639320575229276322, 3.701785489019034259, 2.411212692025939131 ) ) ;
#67114=CARTESIAN_POINT ( 'NONE',  ( 2.558860573628952473, 1.496680913221506870, -1.105902276818030217 ) ) ;
#67116=CARTESIAN_POINT ( 'NONE',  ( 0.7377199025260212650, 1.913388251642001103, -0.09504988074141537679 ) ) ;
#67117=CARTESIAN_POINT ( 'NONE',  ( 0.7859742890132662696, 2.042544534415400737, -0.5693509180391894686 ) ) ;
#67124=CARTESIAN_POINT ( 'NONE',  ( 4.979337304519595442, -0.1005905848140927622, 1.967025916208066327 ) ) ;
#67125=CARTESIAN_POINT ( 'NONE',  ( 1.893382502257603850, -0.1070854039621378373, -2.117916637519041689 ) ) ;
#67129=CARTESIAN_POINT ( 'NONE',  ( 5.490230790444213582, -0.5297859672059505032, -2.126319610106224278 ) ) ;
#67131=CARTESIAN_POINT ( 'NONE',  ( 4.717753586115435382, -1.889304338648789106, 0.3753660715558500005 ) ) ;
#67134=CARTESIAN_POINT ( 'NONE',  ( 1.471597369358583096, 0.1596246592955492538, -2.201166978212334424 ) ) ;
#67139=CARTESIAN_POINT ( 'NONE',  ( 6.403175662787183420, -1.665661181276241853, 1.050507712364300072 ) ) ;
#67140=CARTESIAN_POINT ( 'NONE',  ( 1.470153547685297823, -1.844723335029124112, -0.6073778784492619431 ) ) ;
#67141=CARTESIAN_POINT ( 'NONE',  ( 6.749376085230743172, -2.252018642839793472, -0.4587488502729390460 ) ) ;
#67143=CARTESIAN_POINT ( 'NONE',  ( 4.451900780290086956, -0.7152352812324501707, 1.718214207458491849 ) ) ;
#67148=CARTESIAN_POINT ( 'NONE',  ( 0.09952931447375359952, -0.5783855404800625211, 2.113812074898171023 ) ) ;
#67152=CARTESIAN_POINT ( 'NONE',  ( 1.629252094361890890, -1.719607636260962025, 0.6136192449261099746 ) ) ;
#67154=CARTESIAN_POINT ( 'NONE',  ( 3.779676010894826188, 1.462474260537292681, -0.9315460551484288088 ) ) ;
#67156=CARTESIAN_POINT ( 'NONE',  ( 6.509000000000014552, 2.444259026362519904, 2.383015625331697862 ) ) ;
#67157=CARTESIAN_POINT ( 'NONE',  ( 0.1331565106231606399, 5.723858289613107608, -2.539976893513963052 ) ) ;
#67158=CARTESIAN_POINT ( 'NONE',  ( 0.1527873662319845505, -1.548267161427993255, 1.146224303156289093 ) ) ;
#67159=CARTESIAN_POINT ( 'NONE',  ( 4.082823661314609609, 1.861412734803047142, 0.6194944872321900275 ) ) ;
#67162=CARTESIAN_POINT ( 'NONE',  ( 4.512424090126602394, -2.120028616272570332, -0.05109941365945279423 ) ) ;
#67168=CARTESIAN_POINT ( 'NONE',  ( 3.186448005867897670, 1.153939711166888982, -1.718631068965512210 ) ) ;
#67172=CARTESIAN_POINT ( 'NONE',  ( 2.778317543532899947, 1.969881296151472894, -1.184559908770227432 ) ) ;
#67182=CARTESIAN_POINT ( 'NONE',  ( 4.148624843374196125, 1.876505540506741010, 0.3678670841067502861 ) ) ;
#67183=CARTESIAN_POINT ( 'NONE',  ( 5.174679765213248572, -1.625057609515182078, -0.5782863776828560676 ) ) ;
#67184=CARTESIAN_POINT ( 'NONE',  ( 3.257046257486408969, 0.04465439498414420366, -2.016188763087948033 ) ) ;
#67185=CARTESIAN_POINT ( 'NONE',  ( 5.362068906036296490, -0.05402111011005260310, -2.298215290733228500 ) ) ;
#67187=CARTESIAN_POINT ( 'NONE',  ( 1.172829962703396456, -1.397616723802884708, 1.707921395779465890 ) ) ;
#67189=CARTESIAN_POINT ( 'NONE',  ( 6.134039733390581617, 0.8703851191177320867, -1.540848210998513990 ) ) ;
#67191=CARTESIAN_POINT ( 'NONE',  ( 2.238584135424640298, 0.5043332063416061661, 2.235947581072089907 ) ) ;
#67192=CARTESIAN_POINT ( 'NONE',  ( 6.703072984701052839, -0.3981723446819797063, 1.804146177254343009 ) ) ;
#67197=CARTESIAN_POINT ( 'NONE',  ( -0.02968770228140016343, 0.003472272166151618711, -1.826291111852257343 ) ) ;
#67198=CARTESIAN_POINT ( 'NONE',  ( 6.496543107701719499, 2.047251205643263017, 0.3077783505985449142 ) ) ;
#67199=CARTESIAN_POINT ( 'NONE',  ( 0.9015777671340443611, -1.966303774932298021, 0.4465067697373495403 ) ) ;
#67201=CARTESIAN_POINT ( 'NONE',  ( 5.127533266204091333, -1.828772253489078237, 0.6060055780525953617 ) ) ;
#67203=CARTESIAN_POINT ( 'NONE',  ( 2.092296997076743548, 1.370790743785160970, 1.747926019109148799 ) ) ;
#67211=CARTESIAN_POINT ( 'NONE',  ( 4.774825072940077852, 1.621577360410943802, -0.6326411939767513370 ) ) ;
#67212=CARTESIAN_POINT ( 'NONE',  ( 2.699599903323801620, -1.451799986561516764, -1.319707477925702310 ) ) ;
#67217=CARTESIAN_POINT ( 'NONE',  ( 0.7310139678005268538, -1.941628062548940381, -0.6965263486069167564 ) ) ;
#67221=CARTESIAN_POINT ( 'NONE',  ( 1.745381597357411385, -1.910777759476259163, 1.211296049258607788 ) ) ;
#67224=CARTESIAN_POINT ( 'NONE',  ( 2.424885678431305092, -0.004389691185376768875, 1.870726058193001196 ) ) ;
#67225=CARTESIAN_POINT ( 'NONE',  ( 1.125167334363995852, 0.3372632679971860337, 1.700812921812058454 ) ) ;
#67227=CARTESIAN_POINT ( 'NONE',  ( 5.548420995840112724, -1.728225626343689925, 1.347513067664840358 ) ) ;
#67228=CARTESIAN_POINT ( 'NONE',  ( 5.737451576302465384, -2.089288847444936259, 0.9800045452074584995 ) ) ;
#67229=CARTESIAN_POINT ( 'NONE',  ( 1.164996006578455923, -1.862832630767555120, -0.8818606138344189382 ) ) ;
#67230=CARTESIAN_POINT ( 'NONE',  ( 3.240110121693033474, 0.4724093276110411521, 1.883494029347228871 ) ) ;
#67233=CARTESIAN_POINT ( 'NONE',  ( 6.028550586359523678, 1.802609027081774951, 0.4991829554215552744 ) ) ;
#67234=CARTESIAN_POINT ( 'NONE',  ( 0.8437500000000005551, 1.895863743164106774, 0.7852924748299443536 ) ) ;
#67237=CARTESIAN_POINT ( 'NONE',  ( 6.222029796014385106, -1.727739227931901489, -1.038831587593692873 ) ) ;
#67239=CARTESIAN_POINT ( 'NONE',  ( 4.693982515131527755, 1.755768268644173791, 0.9914009648221073778 ) ) ;
#67243=CARTESIAN_POINT ( 'NONE',  ( 2.103868193876055503, -1.825329726703457833, 0.04394198290156441783 ) ) ;
#67245=CARTESIAN_POINT ( 'NONE',  ( -0.1296875068448125334, 2.048176110289974261, -2.243787855586779401 ) ) ;
#67251=CARTESIAN_POINT ( 'NONE',  ( 0.3166733070498818359, -0.6846287639105748113, -1.900330225253379801 ) ) ;
#67252=CARTESIAN_POINT ( 'NONE',  ( 6.586594613159782341, -1.369803613283290700, 1.749543456560544552 ) ) ;
#67255=CARTESIAN_POINT ( 'NONE',  ( 5.454002199308585652, 2.058645617578058751, -0.09870700237277732492 ) ) ;
#67256=CARTESIAN_POINT ( 'NONE',  ( 5.010388774477188889, -1.913804350592800407, 0.6351971752796631288 ) ) ;
#67263=CARTESIAN_POINT ( 'NONE',  ( 5.255232437486731634, -2.000551055875991580, -0.2495666058281582056 ) ) ;
#67264=CARTESIAN_POINT ( 'NONE',  ( 4.611176429654996412, -1.805050139478355353, 0.3618648703537508671 ) ) ;
#67266=CARTESIAN_POINT ( 'NONE',  ( 3.791899867668945490, 1.670594791088287678, 1.592266751676748582 ) ) ;
#67268=CARTESIAN_POINT ( 'NONE',  ( 5.184929619776310616, -0.2588774643964042999, -2.145956309214678726 ) ) ;
#67269=CARTESIAN_POINT ( 'NONE',  ( 3.467982673848205355, -0.9896861206786079501, 1.756853968756578066 ) ) ;
#67271=CARTESIAN_POINT ( 'NONE',  ( 0.5560688330792910028, -1.405822068596472407, 1.340092691751965770 ) ) ;
#67273=CARTESIAN_POINT ( 'NONE',  ( 3.989890550291860016, 2.181093686755405603, 0.7249921343481547931 ) ) ;
#67276=CARTESIAN_POINT ( 'NONE',  ( 3.379631771358857950, 1.185797501207178861, 1.446808710765794315 ) ) ;
#67277=CARTESIAN_POINT ( 'NONE',  ( 0.9317291061951762376, -1.865162313430932750, 0.4216105838140621342 ) ) ;
#67280=CARTESIAN_POINT ( 'NONE',  ( 2.877765823869771644, 2.095344539500657799, -0.6929138170133213315 ) ) ;
#67286=CARTESIAN_POINT ( 'NONE',  ( 0.2980362317399931626, -1.970818609879662953, -0.05296617050038961161 ) ) ;
#67287=CARTESIAN_POINT ( 'NONE',  ( 6.586558022634583232, -2.261718397432868066, -0.4576183726279075548 ) ) ;
#67288=CARTESIAN_POINT ( 'NONE',  ( 1.381223342121252085, -0.05156877537583307025, 1.961363007973878858 ) ) ;
#67289=CARTESIAN_POINT ( 'NONE',  ( 4.452046733557501135, -0.7940950990443145230, 1.903769949380555770 ) ) ;
#67295=CARTESIAN_POINT ( 'NONE',  ( 6.933263157960373846, 7.629137130509066722, 2.546189081643289942 ) ) ;
#67297=CARTESIAN_POINT ( 'NONE',  ( 0.3038947965873342039, -1.677446906807459337, -1.377854473705003580 ) ) ;
#67301=CARTESIAN_POINT ( 'NONE',  ( 1.036156370570060270, 1.841834720703208639, 0.3256331921374157057 ) ) ;
#67303=CARTESIAN_POINT ( 'NONE',  ( -0.02264175331119500090, 1.349762599094967763, -2.344447671987642146 ) ) ;
#67306=CARTESIAN_POINT ( 'NONE',  ( 1.242663310189826564, 1.843194135250892707, 0.5091577964371831744 ) ) ;
#67307=CARTESIAN_POINT ( 'NONE',  ( 2.975218959772182536, 1.681091501613757533, -0.5536541633112538330 ) ) ;
#67308=CARTESIAN_POINT ( 'NONE',  ( 1.172351427048579531, 0.7757545017167380985, 1.748050575570128329 ) ) ;
#67310=CARTESIAN_POINT ( 'NONE',  ( 4.218306492681688447, 1.879367783149912929, 0.3698934672397135581 ) ) ;
#67311=CARTESIAN_POINT ( 'NONE',  ( 5.230891393285493685, -1.853837313009810028, -0.6654804215649990917 ) ) ;
#67312=CARTESIAN_POINT ( 'NONE',  ( 1.019968326173793960, -0.5097545255977399270, 2.058319881341897695 ) ) ;
#67314=CARTESIAN_POINT ( 'NONE',  ( 3.432352559540859271, 1.824792983844251371, 0.4109263881779609551 ) ) ;
#67315=CARTESIAN_POINT ( 'NONE',  ( 0.3635304476994546952, 1.806310985241452949, -0.2645042207462811046 ) ) ;
#67316=EDGE_LOOP ( 'NONE', ( #95690, #86401 ) ) ;
#67317=CARTESIAN_POINT ( 'NONE',  ( 3.967548030458594166, 0.2710504330169676845, -2.190103208553782821 ) ) ;
#67320=CARTESIAN_POINT ( 'NONE',  ( 2.348159106025033083, -0.8842165242596754515, 1.863692774951962727 ) ) ;
#67326=CARTESIAN_POINT ( 'NONE',  ( 6.363533315466952445, -1.540175188624912428, -1.133462061071670579 ) ) ;
#67328=CARTESIAN_POINT ( 'NONE',  ( 4.773920332862017446, -2.031068740936771366, 0.4005940302675218834 ) ) ;
#67331=CARTESIAN_POINT ( 'NONE',  ( 1.933122032479916985, 0.2097677157741582865, 2.151362962771664833 ) ) ;
#67333=CARTESIAN_POINT ( 'NONE',  ( 1.559246255342447984, -1.705015668849844124, 1.082290385971399926 ) ) ;
#67337=CARTESIAN_POINT ( 'NONE',  ( 6.766953912288387940, -2.015720078709513086, 0.04667315333419658208 ) ) ;
#67338=CARTESIAN_POINT ( 'NONE',  ( 0.5851731681005939434, 1.651346252830317551, 1.157095189655330314 ) ) ;
#67339=CARTESIAN_POINT ( 'NONE',  ( 6.639320575229263888, 1.250520135805782251, 2.217830841512329787 ) ) ;
#67340=CARTESIAN_POINT ( 'NONE',  ( 4.616832073239669043, -0.1072513232249286408, 2.189039617437993357 ) ) ;
#67342=CARTESIAN_POINT ( 'NONE',  ( 4.025576834063953946, -0.3218090080209669024, 1.884953445776993863 ) ) ;
#67346=CARTESIAN_POINT ( 'NONE',  ( 1.634388897023292486, 0.6352195160324504153, 1.913798142305182415 ) ) ;
#67348=CARTESIAN_POINT ( 'NONE',  ( 0.2579210422260198587, 2.266244506498811706, -0.3445303224042794432 ) ) ;
#67350=CARTESIAN_POINT ( 'NONE',  ( 4.348488605181799471, 0.4613061074445113374, 1.661866727659202736 ) ) ;
#67351=CARTESIAN_POINT ( 'NONE',  ( -0.1399997263889559695, 7.629137130509076492, -2.600276787041354343 ) ) ;
#67354=CARTESIAN_POINT ( 'NONE',  ( 1.223018651738450480, -1.772137153356953432, -0.8420139538000551704 ) ) ;
#67357=CARTESIAN_POINT ( 'NONE',  ( 0.07536363704233049743, 0.2309889609098912111, -2.177957698420322163 ) ) ;
#67361=CARTESIAN_POINT ( 'NONE',  ( 4.441949062027584993, -1.118158961774197380, -1.425077651336349227 ) ) ;
#67366=CARTESIAN_POINT ( 'NONE',  ( 4.389189793862141364, -0.004542125399705549196, -1.811656973097997447 ) ) ;
#67372=CARTESIAN_POINT ( 'NONE',  ( 6.602007162813277041, 0.7109360278478898953, -1.720114357745919476 ) ) ;
#67374=CARTESIAN_POINT ( 'NONE',  ( 4.288635103545942684, 1.478190772419993415, -1.218367487985058339 ) ) ;
#67382=CARTESIAN_POINT ( 'NONE',  ( 5.208266738515407113, 1.258803676730145371, -1.702402541353124077 ) ) ;
#67383=CARTESIAN_POINT ( 'NONE',  ( 0.4796413896344040029, 2.016494124141111399, -0.7793912508547717888 ) ) ;
#67386=CARTESIAN_POINT ( 'NONE',  ( 1.149113351018778539, -1.436424422225426767, -1.126575773451453433 ) ) ;
#67388=CARTESIAN_POINT ( 'NONE',  ( 3.205874166558682514, -1.823564452915670042, 0.08818595847179949709 ) ) ;
#67392=CARTESIAN_POINT ( 'NONE',  ( 2.295301284060722313, -1.760697607696968037, 0.8827641120334356328 ) ) ;
#67393=CARTESIAN_POINT ( 'NONE',  ( 4.317874670498635048, 1.191976824791032064, -1.533171632797071693 ) ) ;
#67396=CARTESIAN_POINT ( 'NONE',  ( 3.849942018323779358, -1.464806807754112539, -1.533599281611098597 ) ) ;
#67398=CARTESIAN_POINT ( 'NONE',  ( 2.631394046745598736, -0.1854624247320437458, 1.903247139735386284 ) ) ;
#67405=CARTESIAN_POINT ( 'NONE',  ( 4.617693566336190436, -1.789886777702164089, 0.3589094947460610974 ) ) ;
#67410=CARTESIAN_POINT ( 'NONE',  ( 5.700035372616791385, -1.870836310086241294, 0.001406584917262864625 ) ) ;
#67419=CARTESIAN_POINT ( 'NONE',  ( 0.4970418144054839504, 0.3504251219754518365, 2.040211723117946629 ) ) ;
#67420=CARTESIAN_POINT ( 'NONE',  ( 1.036884384669316539, -1.666496236897334615, 1.305811245984341173 ) ) ;
#67423=CARTESIAN_POINT ( 'NONE',  ( 6.737176827083626307, -0.09545985418329960837, -2.068160202195384656 ) ) ;
#67424=CARTESIAN_POINT ( 'NONE',  ( 1.364538772237647413, 0.1349417713633893900, -1.836341338755695940 ) ) ;
#67429=CARTESIAN_POINT ( 'NONE',  ( 1.535548486519675571, -1.662869323620078665, -1.577994866025609566 ) ) ;
#67431=CARTESIAN_POINT ( 'NONE',  ( 0.2333690889706820926, 2.873202992247088083, -2.541887414127189881 ) ) ;
#67435=CARTESIAN_POINT ( 'NONE',  ( 0.9318904303841836212, -1.963229875443720074, 0.4450799344311164862 ) ) ;
#67436=CARTESIAN_POINT ( 'NONE',  ( 0.7956631384608278124, -1.383255022760669251, -1.391342014947573924 ) ) ;
#67441=CARTESIAN_POINT ( 'NONE',  ( 4.083990600187762610, -2.067889708199427190, -0.3066597852425279047 ) ) ;
#67442=CARTESIAN_POINT ( 'NONE',  ( 2.395042364772178356, 1.366200922416866526, 1.125074557178520118 ) ) ;
#67445=CARTESIAN_POINT ( 'NONE',  ( 5.613300874620239078, -2.237517390240588711, 0.4973276143641935931 ) ) ;
#67446=CARTESIAN_POINT ( 'NONE',  ( 3.591523995615089948, -1.738451970352115961, -0.08344189160913899339 ) ) ;
#67448=CARTESIAN_POINT ( 'NONE',  ( 2.846726617453724906, -0.8940771029739991160, 1.485372309294562543 ) ) ;
#67449=CARTESIAN_POINT ( 'NONE',  ( 3.086559893568251223, 1.208301842568102247, -1.803703480758335642 ) ) ;
#67451=CARTESIAN_POINT ( 'NONE',  ( 6.175017591530616023, 1.752142144017948100, -0.9981200475188132248 ) ) ;
#67452=CARTESIAN_POINT ( 'NONE',  ( 6.750000000000005329, 0.5343081985527837752, 2.030663454312888305 ) ) ;
#67454=CARTESIAN_POINT ( 'NONE',  ( 2.590742828618552984, -0.3275076452619613554, -1.898194946008352035 ) ) ;
#67456=CARTESIAN_POINT ( 'NONE',  ( 5.853820293109783357, -1.608621682386938589, -1.532244055152881312 ) ) ;
#67458=CARTESIAN_POINT ( 'NONE',  ( -0.1108833634137010027, 2.037774818562386514, -2.313487243312782216 ) ) ;
#67463=CARTESIAN_POINT ( 'NONE',  ( 1.401376347886007068, -0.3305552470432049916, -2.196467622588905932 ) ) ;
#67467=CARTESIAN_POINT ( 'NONE',  ( 6.766858430912646938, -2.064281441484459023, -0.9263300772878214628 ) ) ;
#67470=CARTESIAN_POINT ( 'NONE',  ( 4.000476411064065374, 2.052455503700638229, 0.2052804401120340017 ) ) ;
#67476=CARTESIAN_POINT ( 'NONE',  ( 5.958239543830243790, 0.7576973323653664050, 1.710380810381225913 ) ) ;
#67477=CARTESIAN_POINT ( 'NONE',  ( 4.535645802837630747, -1.388783131305007634, 1.038275480396163353 ) ) ;
#67478=CARTESIAN_POINT ( 'NONE',  ( 4.757210230733205591, 1.720523950154304371, -0.2617468875206073742 ) ) ;
#67480=ADVANCED_FACE ( 'NONE', ( #88596 ), #97313, .F. ) ;
#67481=CARTESIAN_POINT ( 'NONE',  ( 1.488225144363482189, -2.281859108288700089, -0.2192131398826550337 ) ) ;
#67483=CARTESIAN_POINT ( 'NONE',  ( 6.128480205876102538, 0.2055166225264984381, 2.080635545183810553 ) ) ;
#67484=CARTESIAN_POINT ( 'NONE',  ( 0.1812672858593766811, -0.8707521589867758260, 1.622202602641155345 ) ) ;
#67486=CARTESIAN_POINT ( 'NONE',  ( 2.092422861153935276, -0.4390285686692517175, 1.967888031366466395 ) ) ;
#67493=CARTESIAN_POINT ( 'NONE',  ( 3.123802294713691641, -0.4116375371931815796, 2.079978743196985391 ) ) ;
#67496=CARTESIAN_POINT ( 'NONE',  ( 5.461492464141177727, 0.3521552718798379722, -1.791230276788812414 ) ) ;
#67502=CARTESIAN_POINT ( 'NONE',  ( 3.304948908139183406, -0.3981353638667082806, -1.979975013379015936 ) ) ;
#67503=CARTESIAN_POINT ( 'NONE',  ( 6.598651186688741177, -0.5821561243712966016, -2.128545807824663960 ) ) ;
#67504=CARTESIAN_POINT ( 'NONE',  ( 3.555356577358064207, 1.464247429212956808, 1.148356018212342233 ) ) ;
#67514=CARTESIAN_POINT ( 'NONE',  ( 1.598581759805017155, 0.8596790983186454183, -1.505624278722474951 ) ) ;
#67515=CARTESIAN_POINT ( 'NONE',  ( 0.7084657485305994040, -0.2594935844701939387, 1.720731466566546519 ) ) ;
#67516=CARTESIAN_POINT ( 'NONE',  ( 0.2007804849885147513, -2.307177064702860214, -0.05170730859792996986 ) ) ;
#67519=CARTESIAN_POINT ( 'NONE',  ( 1.247419646546283234, -1.622699693697586820, -1.270148745232473564 ) ) ;
#67521=CARTESIAN_POINT ( 'NONE',  ( 6.292345239091892140, -2.167472901860421519, 0.7650227848022586041 ) ) ;
#67525=CARTESIAN_POINT ( 'NONE',  ( 6.508674657442179878, 1.384610780642284711, -1.258058027910214927 ) ) ;
#67527=CARTESIAN_POINT ( 'NONE',  ( 5.115449499555525747, 1.566912803841558732, 1.096118974231160781 ) ) ;
#67529=CARTESIAN_POINT ( 'NONE',  ( 6.586557750117827403, -2.163372447211810989, -0.4352210726449382006 ) ) ;
#67534=CARTESIAN_POINT ( 'NONE',  ( -0.05793207083453711520, -1.244369569480655136, -1.591280167384064637 ) ) ;
#67536=CARTESIAN_POINT ( 'NONE',  ( 3.223938161889360110, -2.224449554215703895, 0.6136290147475926826 ) ) ;
#67537=CARTESIAN_POINT ( 'NONE',  ( 4.896903505236655185, 0.3334610245491422265, 1.933150054703360432 ) ) ;
#67538=CARTESIAN_POINT ( 'NONE',  ( 1.217545072937670225, 0.3881152535412414339, -1.922811240370206232 ) ) ;
#67542=CARTESIAN_POINT ( 'NONE',  ( 0.5502106600992883179, 1.049441996780882125, 1.838938355043976847 ) ) ;
#67545=CARTESIAN_POINT ( 'NONE',  ( 3.907220266852969637, -1.778082601562074094, 1.245552836545896769 ) ) ;
#67547=CARTESIAN_POINT ( 'NONE',  ( 2.250376613284802207, 0.9954810856505689198, -1.872389709364124188 ) ) ;
#67552=CARTESIAN_POINT ( 'NONE',  ( 1.985689569138231914, 1.418919563317089017, 1.494737215543304965 ) ) ;
#67559=CARTESIAN_POINT ( 'NONE',  ( 4.178302048780179412, 0.9043031410675538284, 1.684961085834511874 ) ) ;
#67560=( BOUNDED_SURFACE ( )  B_SPLINE_SURFACE ( 3, 3, ( 
 ( #68196, #200333, #53031, #171045, #118109, #88752, #54111, #35713, #167859, #19456, #120246 ),
 ( #58372, #60490, #141797, #95153, #208859, #140728, #29070, #44266, #45332, #127730, #124526 ),
 ( #108257, #177456, #8542, #94095, #175336, #191547, #189433, #206741, #74624, #173208, #90891 ),
 ( #77809, #11733, #190483, #193688, #109328, #76736, #111451, #174278, #93027, #10664, #159068 ),
 ( #41075, #142855, #61564, #126648, #192613, #110388, #176393, #207801, #73545, #26918, #27998 ),
 ( #42142, #143930, #7466, #139648, #43212, #25853, #91963, #156950, #160134, #158022, #9610 ),
 ( #209925, #205669, #75687, #59429, #125587, #57307, #123470, #107182, #24788, #33321, #96222 ) ),
 .UNSPECIFIED., .T., .F., .T. ) 
 B_SPLINE_SURFACE_WITH_KNOTS ( ( 4, 3, 4 ),
 ( 4, 1, 1, 1, 1, 1, 1, 1, 4 ),
 ( 0.000000000000000000, 0.5000000000000000000, 1.000000000000000000 ),
 ( 0.000000000000000000, 0.2256926809922864541, 0.3979886288388991278, 0.5260859906349554249, 0.6192013483571605637, 0.6864504996671639825, 0.7364865548622955282, 0.7772638159577213157, 1.000000000000000000 ),
 .UNSPECIFIED. ) 
 GEOMETRIC_REPRESENTATION_ITEM ( )  RATIONAL_B_SPLINE_SURFACE ( (
 ( 1.000000000000000222, 1.000000000000000222, 0.9999999999999997780, 1.000000000000000222, 0.9999999999999996669, 1.000000000000000000, 1.000000000000000222, 0.9999999999999996669, 1.000000000000000444, 1.000000000000000222, 1.000000000000000222),
 ( 0.3333333333333334259, 0.3333333333333334259, 0.3333333333333333148, 0.3333333333333333703, 0.3333333333333333703, 0.3333333333333332593, 0.3333333333333334814, 0.3333333333333332038, 0.3333333333333335924, 0.3333333333333334259, 0.3333333333333334259),
 ( 0.3333333333333334259, 0.3333333333333334259, 0.3333333333333333148, 0.3333333333333333703, 0.3333333333333333703, 0.3333333333333332593, 0.3333333333333334814, 0.3333333333333332038, 0.3333333333333335924, 0.3333333333333334259, 0.3333333333333334259),
 ( 1.000000000000000222, 1.000000000000000222, 0.9999999999999997780, 1.000000000000000222, 0.9999999999999996669, 1.000000000000000000, 1.000000000000000222, 0.9999999999999996669, 1.000000000000000444, 1.000000000000000222, 1.000000000000000222),
 ( 0.3333333333333334259, 0.3333333333333334259, 0.3333333333333333148, 0.3333333333333333703, 0.3333333333333333703, 0.3333333333333332593, 0.3333333333333334814, 0.3333333333333332038, 0.3333333333333335924, 0.3333333333333334259, 0.3333333333333334259),
 ( 0.3333333333333334259, 0.3333333333333334259, 0.3333333333333333148, 0.3333333333333333703, 0.3333333333333333703, 0.3333333333333332593, 0.3333333333333334814, 0.3333333333333332038, 0.3333333333333335924, 0.3333333333333334259, 0.3333333333333334259),
 ( 1.000000000000000222, 1.000000000000000222, 0.9999999999999997780, 1.000000000000000222, 0.9999999999999996669, 1.000000000000000000, 1.000000000000000222, 0.9999999999999996669, 1.000000000000000444, 1.000000000000000222, 1.000000000000000222) ) ) 
 REPRESENTATION_ITEM ( '' )  SURFACE ( )  );
#67562=CARTESIAN_POINT ( 'NONE',  ( 1.950798113461976735, 0.7085273209575352338, 2.148688966898488761 ) ) ;
#67564=CARTESIAN_POINT ( 'NONE',  ( 1.740194394521710430, 1.041001882027743353, -1.482411077883559747 ) ) ;
#67565=CARTESIAN_POINT ( 'NONE',  ( 2.254979328032254760, 0.08947561643129221809, -1.913730806789506245 ) ) ;
#67566=CARTESIAN_POINT ( 'NONE',  ( 2.717306809760032138, -1.800131872397674471, -1.022606600864908399 ) ) ;
#67568=CARTESIAN_POINT ( 'NONE',  ( 0.3914019522827461017, 1.459281966464224256, 1.325753552615087871 ) ) ;
#67569=CARTESIAN_POINT ( 'NONE',  ( 5.988885569479125870, -0.2852814255829403955, -1.905149068243816579 ) ) ;
#67570=CARTESIAN_POINT ( 'NONE',  ( 6.463508838306311510, 0.3818026259072569983, -2.173449913608487716 ) ) ;
#67573=CARTESIAN_POINT ( 'NONE',  ( 4.809062498722087575, -1.658680843151142392, 1.225972815312638353 ) ) ;
#67577=CARTESIAN_POINT ( 'NONE',  ( 4.717860591023939953, -2.065837571889141078, 0.4082076317219375250 ) ) ;
#67579=CARTESIAN_POINT ( 'NONE',  ( 0.7312207505087648940, -2.044463659613379392, -0.7311735514200778940 ) ) ;
#67581=CARTESIAN_POINT ( 'NONE',  ( 5.378265110509337532, -1.205767192478784500, 1.793856531414832256 ) ) ;
#67582=CARTESIAN_POINT ( 'NONE',  ( 5.268225494782738494, 2.017278875131154336, -0.1011536798302767465 ) ) ;
#67584=PRODUCT ( 'coil', 'coil', '', ( #117663 ) ) ;
#67589=CARTESIAN_POINT ( 'NONE',  ( 3.643767777461913493, 2.000731686840724333, -0.2516315899964287617 ) ) ;
#67593=CARTESIAN_POINT ( 'NONE',  ( 5.366167234668930419, 1.061923416652654550, 1.882811416686725359 ) ) ;
#67595=( LENGTH_UNIT ( ) NAMED_UNIT ( * ) SI_UNIT ( .MILLI., .METRE. ) );
#67597=CARTESIAN_POINT ( 'NONE',  ( 5.114861317887108072, 0.1511565883688982259, 2.010826320608386730 ) ) ;
#67599=CARTESIAN_POINT ( 'NONE',  ( 0.7324925891301607983, 0.1221277223508714788, 1.720630200619164496 ) ) ;
#67604=CARTESIAN_POINT ( 'NONE',  ( 5.694569522353672753, -0.4537686991618712362, -1.814561337198366875 ) ) ;
#67605=CARTESIAN_POINT ( 'NONE',  ( 5.994395146102541538, -1.073393154543872852, 1.702996195706570681 ) ) ;
#67606=CARTESIAN_POINT ( 'NONE',  ( 6.539320575229249144, 0.007148032025052972194, 1.896977914940492393 ) ) ;
#67610=CARTESIAN_POINT ( 'NONE',  ( 1.735180256192244919, 1.979698633766859395, 0.7602586827493148514 ) ) ;
#67611=CARTESIAN_POINT ( 'NONE',  ( 1.845327587665198443, 0.3419125196015109225, -1.987051676161588620 ) ) ;
#67612=CARTESIAN_POINT ( 'NONE',  ( 1.212835290986268300, 1.479965279312319693, -1.044435387019273742 ) ) ;
#67614=CARTESIAN_POINT ( 'NONE',  ( 5.928642344448160628, 2.082074431819755045, 0.5810635428650026135 ) ) ;
#67619=CARTESIAN_POINT ( 'NONE',  ( -0.03024393743376960902, -0.9005804071154848156, 1.690789300719280908 ) ) ;
#67626=CARTESIAN_POINT ( 'NONE',  ( 4.346650381253648554, 0.5737703434565506466, 2.084106190491950006 ) ) ;
#67629=CARTESIAN_POINT ( 'NONE',  ( 2.004293344102888508, -0.9022931611136343344, 1.919180038594799687 ) ) ;
#67630=CARTESIAN_POINT ( 'NONE',  ( 6.545924712158827319, 0.6954503440314525609, -1.688125835592364066 ) ) ;
#67631=CARTESIAN_POINT ( 'NONE',  ( 3.655507913172794332, 0.4821067936548150135, -1.911365640376050612 ) ) ;
#67634=CARTESIAN_POINT ( 'NONE',  ( 6.303175665915636827, -1.664687476133955846, 1.052260723566181833 ) ) ;
#67635=CARTESIAN_POINT ( 'NONE',  ( 1.552571996792909248, -1.665377644223103637, -0.9986158231547156428 ) ) ;
#67643=CARTESIAN_POINT ( 'NONE',  ( 6.375647946566726176, 0.3219878414668366773, -1.884816399834337908 ) ) ;
#67645=CARTESIAN_POINT ( 'NONE',  ( 2.737190076726934151, 0.2709513247245790013, 2.190122135706531914 ) ) ;
#67646=CARTESIAN_POINT ( 'NONE',  ( 2.081372155488591780, -0.1082299263688718260, -2.204229314041641352 ) ) ;
#67648=CARTESIAN_POINT ( 'NONE',  ( 0.2758376730330712734, 1.891454726169951250, -0.2806862973558504892 ) ) ;
#67651=CARTESIAN_POINT ( 'NONE',  ( 3.367693471486675083, -0.4065805204805824635, 2.029877954327436118 ) ) ;
#67655=CARTESIAN_POINT ( 'NONE',  ( 1.428841412761387986, 2.083414371474631377, 0.5762002773818803991 ) ) ;
#67656=CARTESIAN_POINT ( 'NONE',  ( 3.984055765753656164, -2.167877601896048390, -0.3204034371554059235 ) ) ;
#67657=DIRECTION ( 'NONE',  ( -0.9999980456341538426, 0.000000000000000000, -0.001977050295949953074 ) ) ;
#67662=UNCERTAINTY_MEASURE_WITH_UNIT (LENGTH_MEASURE( 1.000000000000000082E-05 ), #86424, 'distance_accuracy_value', 'NONE');
#67663=CARTESIAN_POINT ( 'NONE',  ( 5.977189187444425400, -1.726741413813812631, -0.1601111783383553921 ) ) ;
#67665=CARTESIAN_POINT ( 'NONE',  ( 4.100488025649267954, 2.059819936833905185, 0.2079151390043249559 ) ) ;
#67666=CARTESIAN_POINT ( 'NONE',  ( 4.605136521778616654, -0.1025035295275648906, 2.114849348554531883 ) ) ;
#67669=CARTESIAN_POINT ( 'NONE',  ( 2.729305274051788022, 0.1014009245450513547, -1.966985261555218800 ) ) ;
#67670=CARTESIAN_POINT ( 'NONE',  ( 0.9141475326900462273, -1.912571728325639153, 0.002704284578637640348 ) ) ;
#67671=CARTESIAN_POINT ( 'NONE',  ( 5.103627735775233987, -2.281604237428825233, 0.2209099425345140144 ) ) ;
#67672=CARTESIAN_POINT ( 'NONE',  ( 3.123480263227970344, -1.759325740769552393, 0.4874977319994436287 ) ) ;
#67679=CARTESIAN_POINT ( 'NONE',  ( 3.533450910810581824, -0.1440131911168585910, 2.008084626805274997 ) ) ;
#67680=CARTESIAN_POINT ( 'NONE',  ( 4.188298518248589453, 1.053080760608171129, -1.654974388233184657 ) ) ;
#67683=CARTESIAN_POINT ( 'NONE',  ( 0.07536363704233049743, 2.002983476668462881, -2.558365315478607904 ) ) ;
#67684=CARTESIAN_POINT ( 'NONE',  ( 0.8375780558756993344, 0.8438101838260108067, -1.913087135030653974 ) ) ;
#67685=CARTESIAN_POINT ( 'NONE',  ( 5.225387627957367442, -1.679756879107903833, 0.5577133518330120721 ) ) ;
#67687=CARTESIAN_POINT ( 'NONE',  ( 1.763894328224338448, 1.128481436294457740, 1.878420861880884862 ) ) ;
#67688=CARTESIAN_POINT ( 'NONE',  ( 6.474529609311859168, -0.09325562727019585940, -1.737965710822095389 ) ) ;
#67690=CARTESIAN_POINT ( 'NONE',  ( 0.2331713839410628208, 0.2432647426263275514, -1.987790486660771627 ) ) ;
#67691=CARTESIAN_POINT ( 'NONE',  ( 0.1347971297303695026, -1.579520332396977089, 0.6935263066737175075 ) ) ;
#67692=CARTESIAN_POINT ( 'NONE',  ( 1.212782571277282395, -1.812964642495185963, -1.412582873482233659 ) ) ;
#67693=CARTESIAN_POINT ( 'NONE',  ( 1.066276686178056377, -1.386418637449363889, 1.697306931840412370 ) ) ;
#67694=CARTESIAN_POINT ( 'NONE',  ( 2.649284799151204073, -1.834272514977531632, 1.226802785254533568 ) ) ;
#67695=CARTESIAN_POINT ( 'NONE',  ( 0.2335667940002684184, 0.001055507091213009818, -2.153566573614831281 ) ) ;
#67697=CARTESIAN_POINT ( 'NONE',  ( 1.745463160119866686, 0.3564436455325488695, -2.086969855494016368 ) ) ;
#67698=CARTESIAN_POINT ( 'NONE',  ( 6.827182134110238110, 0.5514785450725538940, 2.340047124761033714 ) ) ;
#67699=CARTESIAN_POINT ( 'NONE',  ( 5.139640169905585587, -1.362188071541370116, -1.362388069303143823 ) ) ;
#67701=CARTESIAN_POINT ( 'NONE',  ( 2.648291651658631007, 0.7751803744074429181, 2.157441745960963164 ) ) ;
#67705=CARTESIAN_POINT ( 'NONE',  ( 4.407017973072342443, -0.4864924038828158381, -2.167217472756521879 ) ) ;
#67712=CARTESIAN_POINT ( 'NONE',  ( 2.813125141109920069, 1.117832431973438734, -1.678005364621336426 ) ) ;
#67714=CARTESIAN_POINT ( 'NONE',  ( 0.5321751443473606846, 1.184493745614173310, 1.688377367428809173 ) ) ;
#67715=CARTESIAN_POINT ( 'NONE',  ( 6.983263157960402090, -0.0002233252893329333382, 1.845923184817334084 ) ) ;
#67719=CARTESIAN_POINT ( 'NONE',  ( 4.365290731249091394, 2.125951747006165959, -0.5312598475561494116 ) ) ;
#67720=CARTESIAN_POINT ( 'NONE',  ( 1.793592486599729252, 1.492254607734722072, -1.356300734917381678 ) ) ;
#67721=CARTESIAN_POINT ( 'NONE',  ( 1.487592393518050837, -1.832424703912252317, -0.1798031890194173865 ) ) ;
#67722=CARTESIAN_POINT ( 'NONE',  ( 4.810265146351084375, 1.581823803905563430, -1.659390399702101337 ) ) ;
#67723=CARTESIAN_POINT ( 'NONE',  ( 5.050657991863417351, -1.557144343216086968, -0.9820927893566462341 ) ) ;
#67725=CARTESIAN_POINT ( 'NONE',  ( 4.348545414961950684, 0.4871326187540457875, 1.759326811173238303 ) ) ;
#67726=CARTESIAN_POINT ( 'NONE',  ( 4.395157833011634096, -0.8647231026696032830, -1.821742675176166060 ) ) ;
#67728=CARTESIAN_POINT ( 'NONE',  ( 4.329186484417943959, 0.1072846252610352574, 2.260086081085868948 ) ) ;
#67730=CARTESIAN_POINT ( 'NONE',  ( 0.1531350777018150311, -1.689991139269167109, 1.256553844878212978 ) ) ;
#67732=CARTESIAN_POINT ( 'NONE',  ( 4.457524453155742528, 1.660904245173303373, 1.235824716467534889 ) ) ;
#67737=CARTESIAN_POINT ( 'NONE',  ( 2.297378195909089982, 1.489297080225897574, 1.222053532002062903 ) ) ;
#67740=CARTESIAN_POINT ( 'NONE',  ( 6.368014371105396698, -1.954979222910321557, 0.2374047605521299453 ) ) ;
#67744=CARTESIAN_POINT ( 'NONE',  ( 0.8441712343106638761, -1.349783269286155774, -1.635521010841307410 ) ) ;
#67745=CARTESIAN_POINT ( 'NONE',  ( 2.074768627854159053, 0.9548037322763336388, 2.005906060693471993 ) ) ;
#67746=CARTESIAN_POINT ( 'NONE',  ( 3.171027762369707848, -1.945216043820027663, -0.8074606443248407706 ) ) ;
#67749=CARTESIAN_POINT ( 'NONE',  ( 6.983263157960402090, -0.0002233252893329463486, 1.845923184817334084 ) ) ;
#67755=CARTESIAN_POINT ( 'NONE',  ( 1.266058358664986949, 0.6103625328083387425, -2.030891291126469600 ) ) ;
#67758=CARTESIAN_POINT ( 'NONE',  ( 4.387127823891323608, 0.09410986116351567621, 1.959716250186482434 ) ) ;
#67759=CARTESIAN_POINT ( 'NONE',  ( 3.133815226704575796, -1.450665623810345473, -1.602838778681405785 ) ) ;
#67760=CARTESIAN_POINT ( 'NONE',  ( 1.346931166825489967, 0.5339940059071214273, -1.762130705996706181 ) ) ;
#67763=CARTESIAN_POINT ( 'NONE',  ( 4.365022556061240344, 1.687170946148343953, -0.4262992432423305389 ) ) ;
#67767=CARTESIAN_POINT ( 'NONE',  ( 1.446389902895691693, 2.159248346720197276, 0.1057134262518744372 ) ) ;
#67769=CARTESIAN_POINT ( 'NONE',  ( 3.233749808020690342, -1.861731463674856979, -0.7741979076196570109 ) ) ;
#67771=CARTESIAN_POINT ( 'NONE',  ( 1.253037233087474611, -1.703760181015579134, 1.330383891403746688 ) ) ;
#67773=CARTESIAN_POINT ( 'NONE',  ( 3.432457938460992342, 1.923125764579440844, 0.4332125842720236375 ) ) ;
#67775=CARTESIAN_POINT ( 'NONE',  ( 6.609000000000015085, -6.653734696158637751E-05, 2.100160721423645960 ) ) ;
#67776=CARTESIAN_POINT ( 'NONE',  ( 3.034642427012054444, -1.711418951474739991, 0.9179939537737377142 ) ) ;
#67785=CARTESIAN_POINT ( 'NONE',  ( 6.282281253371452934, -1.241832687457484985, 1.944794379655417682 ) ) ;
#67787=CARTESIAN_POINT ( 'NONE',  ( 5.242999579849755953, -0.2363135928187160284, -1.947375393322479109 ) ) ;
#67788=CARTESIAN_POINT ( 'NONE',  ( 1.846327496167538884, 0.3419342931599393398, -1.987046799686801757 ) ) ;
#67790=CARTESIAN_POINT ( 'NONE',  ( 2.940728227222836111, -1.600293368184166898, 1.386485470145684351 ) ) ;
#67792=CARTESIAN_POINT ( 'NONE',  ( 0.1747926744264920174, 4.095712681614646300, -2.410328719303979739 ) ) ;
#67794=CARTESIAN_POINT ( 'NONE',  ( 4.734224819668921391, 0.3176365174208677367, 1.813369535050498360 ) ) ;
#67799=CARTESIAN_POINT ( 'NONE',  ( 5.361630242575341931, -1.673063676233761621, -1.302930760576012092 ) ) ;
#67802=CARTESIAN_POINT ( 'NONE',  ( 5.149710871190182893, 0.6505453885284390170, -1.955453191944044766 ) ) ;
#67804=CARTESIAN_POINT ( 'NONE',  ( 0.9943274703284404881, 1.832596168249778446, 0.3232805840463324198 ) ) ;
#67805=CARTESIAN_POINT ( 'NONE',  ( 2.225889136967126536, 1.786374552192676823, 0.4457033907802817052 ) ) ;
#67811=CARTESIAN_POINT ( 'NONE',  ( 2.280145854635793334, 1.358931147977986420, 1.738775483816151768 ) ) ;
#67812=CARTESIAN_POINT ( 'NONE',  ( 4.622535034725678393, 1.396675434457357756, -1.779734664907887343 ) ) ;
#67814=CARTESIAN_POINT ( 'NONE',  ( 5.273626195773981173, 0.3454419319289269708, -1.778163250140889717 ) ) ;
#67815=CARTESIAN_POINT ( 'NONE',  ( 4.909359874374886523, -1.816983420234472790, 0.6072180050544163654 ) ) ;
#67818=CARTESIAN_POINT ( 'NONE',  ( 3.660970522598467891, -1.737989841360635834, -0.9306492429120606369 ) ) ;
#67819=CARTESIAN_POINT ( 'NONE',  ( 5.242975984329111050, -1.603930480038592510, 0.9624218375651683033 ) ) ;
#67820=CARTESIAN_POINT ( 'NONE',  ( 4.316758383393053400, -1.379848157930125829, 1.249026149535825914 ) ) ;
#67822=CARTESIAN_POINT ( 'NONE',  ( 4.803428869931958722, -0.4704684023625771983, 1.706073424435787134 ) ) ;
#67823=CARTESIAN_POINT ( 'NONE',  ( -0.01248194115436446205, -0.5331630387654020531, 1.944732228473695868 ) ) ;
#67825=CARTESIAN_POINT ( 'NONE',  ( 1.946058636591390334, 0.8049280153260234272, -1.946384432229040673 ) ) ;
#67829=CARTESIAN_POINT ( 'NONE',  ( 3.146849984228027974, 2.069795010335002239, 0.4607391970517027979 ) ) ;
#67831=CARTESIAN_POINT ( 'NONE',  ( 1.476825778181306559, -1.425320297365587408, 1.431352559222300203 ) ) ;
#67834=CARTESIAN_POINT ( 'NONE',  ( 6.620655732516623537, 7.629137130509068498, 2.426260288887295058 ) ) ;
#67837=CARTESIAN_POINT ( 'NONE',  ( 1.757319832705085627, -1.853012815387704570, -1.112828241397870066 ) ) ;
#67838=CARTESIAN_POINT ( 'NONE',  ( 6.610000000000010090, 0.5825982378308904863, 2.053072689460200273 ) ) ;
#67845=CARTESIAN_POINT ( 'NONE',  ( 0.5565083568685527116, -1.583368386835169783, 1.515454571103365344 ) ) ;
#67847=CARTESIAN_POINT ( 'NONE',  ( 1.446537619816448572, 2.259995149683653448, 0.1094724083178944679 ) ) ;
#67854=CARTESIAN_POINT ( 'NONE',  ( 4.529763579968347997, -1.064299448457445729, -1.357287084437068803 ) ) ;
#67856=CARTESIAN_POINT ( 'NONE',  ( 3.743183411477500222, -1.338374212114415762, -1.157953421578450381 ) ) ;
#67857=CARTESIAN_POINT ( 'NONE',  ( 5.702238492974306183, -2.206952906645575307, -0.005361432510411765114 ) ) ;
#67860=CARTESIAN_POINT ( 'NONE',  ( 5.150017624212761547, 0.9963180513538304472, 1.753022482293864481 ) ) ;
#67863=CARTESIAN_POINT ( 'NONE',  ( 3.098369316282158614, -0.5415621961667067552, -1.790553177708480215 ) ) ;
#67864=CARTESIAN_POINT ( 'NONE',  ( 2.043885321627556095, 1.424625833772466432, 1.502381739045772546 ) ) ;
#67866=CARTESIAN_POINT ( 'NONE',  ( 2.355592738034977263, -1.419685808644566949, -1.281520755053264571 ) ) ;
#67871=CARTESIAN_POINT ( 'NONE',  ( 0.1582721923853447621, 1.907395734848855051, 0.1385995803297388196 ) ) ;
#67874=CARTESIAN_POINT ( 'NONE',  ( 2.154674626568295892, -0.5202524484802829585, -1.891573884155263396 ) ) ;
#67875=DIRECTION ( 'NONE',  ( 1.014813233446432150E-15, 1.000000000000000000, -4.583713267641621330E-32 ) ) ;
#67877=CARTESIAN_POINT ( 'NONE',  ( 5.554972086574996304, 0.4156608669513595089, 2.079290889414136423 ) ) ;
#67880=CARTESIAN_POINT ( 'NONE',  ( 6.327413238363588377, -1.857107522167710245, 0.6617740914907597194 ) ) ;
#67882=CARTESIAN_POINT ( 'NONE',  ( 1.441653692521651653, -1.894234556111865420, 0.6821031695033189513 ) ) ;
#67886=CARTESIAN_POINT ( 'NONE',  ( 1.142374532877686644, 0.8619398222155623124, 1.934021905983105416 ) ) ;
#67888=CARTESIAN_POINT ( 'NONE',  ( 2.119664376568120012, 0.3561266789769075292, -2.039353370234835872 ) ) ;
#67892=CARTESIAN_POINT ( 'NONE',  ( 4.171883282844288665, -1.203828960760118694, 1.709054251895093746 ) ) ;
#67894=CARTESIAN_POINT ( 'NONE',  ( 3.733261478165556646, -1.687024869733319221, 0.6981082995600741414 ) ) ;
#67895=CARTESIAN_POINT ( 'NONE',  ( 2.648825499136245654, 0.2233988552288330709, 1.797577217741084921 ) ) ;
#67898=CARTESIAN_POINT ( 'NONE',  ( 6.889999999999997016, 3.693514451062899884, 2.514185260296258662 ) ) ;
#67900=CARTESIAN_POINT ( 'NONE',  ( 5.210101597250164751, -2.196594437182074255, 0.2116553293704941940 ) ) ;
#67903=CARTESIAN_POINT ( 'NONE',  ( 4.459560945705238311, -1.480416612418914424, -1.210464771850598975 ) ) ;
#67911=CARTESIAN_POINT ( 'NONE',  ( 0.6965153189463432204, 1.505040478001760107, 1.060415605250275339 ) ) ;
#67913=CARTESIAN_POINT ( 'NONE',  ( 3.514787476322968285, 1.689724804184733253, 0.8026845837263293371 ) ) ;
#67919=CARTESIAN_POINT ( 'NONE',  ( 0.3913703952206915027, -1.802969083500185477, 0.7928767443170018359 ) ) ;
#67921=CARTESIAN_POINT ( 'NONE',  ( 2.267204043252795120, 1.842440753109304330, -0.8197907266209791821 ) ) ;
#67924=CARTESIAN_POINT ( 'NONE',  ( 2.836070844659248191, 2.175002134116140518, 0.2674123886829762875 ) ) ;
#67925=CARTESIAN_POINT ( 'NONE',  ( 5.953692858212230377, 0.5253669772854427933, -1.748464709795935157 ) ) ;
#67932=CARTESIAN_POINT ( 'NONE',  ( 4.142028884782995135, 0.4951553702221401232, 1.773339192993342639 ) ) ;
#67933=CARTESIAN_POINT ( 'NONE',  ( 0.9088405895168538695, -0.4911093815175514021, -1.952142171939993842 ) ) ;
#67934=CARTESIAN_POINT ( 'NONE',  ( 2.601245504928787700, 1.085180258111384077, -2.026094289238103752 ) ) ;
#67936=CARTESIAN_POINT ( 'NONE',  ( 1.445918188014534422, -0.8427435445049488161, 1.659298548423918884 ) ) ;
#67940=CARTESIAN_POINT ( 'NONE',  ( 4.658414424252744546, 1.907665749568526747, 0.1350064596054162680 ) ) ;
#67944=CARTESIAN_POINT ( 'NONE',  ( 3.808215996505484036, 1.477046120823837683, -1.479981065426434483 ) ) ;
#67945=CARTESIAN_POINT ( 'NONE',  ( 2.676452114398766291, -1.789519730395791486, -0.5449050523786898026 ) ) ;
#67948=CARTESIAN_POINT ( 'NONE',  ( 3.737644501653397455, 1.732476483319781657, 0.1661042753308156761 ) ) ;
#67951=CARTESIAN_POINT ( 'NONE',  ( 4.055083665587292607, -1.435586732866575010, -0.9558459365816800446 ) ) ;
#67953=CARTESIAN_POINT ( 'NONE',  ( 6.709632191794143274, -0.4886956906769434061, 2.160084693451309601 ) ) ;
#67954=CARTESIAN_POINT ( 'NONE',  ( 6.983263157960365675, -0.006178392973848687020, 2.053544886540019210 ) ) ;
#67957=CARTESIAN_POINT ( 'NONE',  ( 3.942362285364631624, -1.074967207919340861, 1.886227828529878803 ) ) ;
#67958=CARTESIAN_POINT ( 'NONE',  ( 3.738726038629454074, 0.2694068579384528150, 1.805578518607708016 ) ) ;
#67960=CARTESIAN_POINT ( 'NONE',  ( 5.630101985619759830, 2.115003628044552553, 0.1013798475145138156 ) ) ;
#67962=CARTESIAN_POINT ( 'NONE',  ( 5.653944246587851552, 0.9260977375703757231, 2.097164529332084637 ) ) ;
#67966=CARTESIAN_POINT ( 'NONE',  ( 1.682450335255514240, 1.092831414372618326, 1.817064408815848964 ) ) ;
#67970=CARTESIAN_POINT ( 'NONE',  ( 6.860228214211484321, -2.170771502548960452, 0.04436455139915015944 ) ) ;
#67974=CARTESIAN_POINT ( 'NONE',  ( 0.8389114244844765311, 1.318684809372525857, -1.787403929136616165 ) ) ;
#67976=CARTESIAN_POINT ( 'NONE',  ( 0.07143917554365029898, -1.076037094620578616, 2.031297111741585226 ) ) ;
#67978=CARTESIAN_POINT ( 'NONE',  ( 3.959878945198321620, -0.6033026367360559972, 1.972334540003743530 ) ) ;
#67984=CARTESIAN_POINT ( 'NONE',  ( 0.1641640845322315523, -1.364019775510204369, 1.584451847793943324 ) ) ;
#67985=CARTESIAN_POINT ( 'NONE',  ( 4.324842380567116784, 0.8596320953860696612, -1.824118450417112847 ) ) ;
#67986=CARTESIAN_POINT ( 'NONE',  ( 3.913478945735289205, -0.9499487412085620974, -1.577145280185827447 ) ) ;
#67990=CARTESIAN_POINT ( 'NONE',  ( 0.7973487315477224557, -0.6271472479968034364, 1.606907058918445985 ) ) ;
#67991=CARTESIAN_POINT ( 'NONE',  ( 0.3742329010679063539, -2.001858617179689492, -0.2420261300371470137 ) ) ;
#67992=CARTESIAN_POINT ( 'NONE',  ( 1.038157343047078296, -1.808118644657311203, 1.419311033984706816 ) ) ;
#67994=CARTESIAN_POINT ( 'NONE',  ( 1.195004664211458456, -0.5499296976853912389, -2.194457269061194982 ) ) ;
#67995=CARTESIAN_POINT ( 'NONE',  ( 3.475310780013381340, 0.05149396089606420035, -2.105609240523627967 ) ) ;
#67999=CARTESIAN_POINT ( 'NONE',  ( 6.000000000000004441, -3.414667428843525066E-13, -2.052068128417939619 ) ) ;
#68005=CARTESIAN_POINT ( 'NONE',  ( 5.344044365905453731, -1.409322151232726750, -1.717068368634220299 ) ) ;
#68006=CARTESIAN_POINT ( 'NONE',  ( 3.486445073788289051, -0.4274320362823453290, -2.149191018322317515 ) ) ;
#68010=CARTESIAN_POINT ( 'NONE',  ( 6.889999999999997016, 3.693514451062899884, 2.514185260296258217 ) ) ;
#68012=CARTESIAN_POINT ( 'NONE',  ( 5.010073305087408002, -0.7609581946756528437, 1.979555329295646260 ) ) ;
#68014=VERTEX_POINT ( 'NONE', #133915 ) ;
#68016=CARTESIAN_POINT ( 'NONE',  ( 6.719591497160966931, -2.098179372288328182, 0.5198544864785522579 ) ) ;
#68018=CARTESIAN_POINT ( 'NONE',  ( 5.759284750224211713, 1.812880138157666465, -0.3211251414683007899 ) ) ;
#68022=CARTESIAN_POINT ( 'NONE',  ( 0.7666889417085223091, 1.677783727127066804, -0.4624100818488885434 ) ) ;
#68026=CARTESIAN_POINT ( 'NONE',  ( 5.032170685167933755, 1.114402916724830161, -1.852182961850391774 ) ) ;
#68030=CARTESIAN_POINT ( 'NONE',  ( 4.258765444007106105, -1.603684720688375975, 1.449730421305382544 ) ) ;
#68032=CARTESIAN_POINT ( 'NONE',  ( 6.151636724293027214, 0.5744773170833740172, -1.885769548957224817 ) ) ;
#68033=CARTESIAN_POINT ( 'NONE',  ( 5.430864382934267987, 0.8560856307190685133, 1.507619432454242681 ) ) ;
#68034=CARTESIAN_POINT ( 'NONE',  ( 1.523247060345904291, -2.062048068855956373, 0.7425582295156886170 ) ) ;
#68035=CARTESIAN_POINT ( 'NONE',  ( 2.468180027558197320, 2.263118346622743360, -0.4500467933809069176 ) ) ;
#68036=CARTESIAN_POINT ( 'NONE',  ( 4.305972304023081954, -2.055534471369814487, 0.1475827967423407050 ) ) ;
#68037=CARTESIAN_POINT ( 'NONE',  ( 6.462452672982783142, -1.777441430900746688, -0.7828909329169189135 ) ) ;
#68044=CARTESIAN_POINT ( 'NONE',  ( 1.565077508395201988, -1.076315722900993643, 1.704939445326451475 ) ) ;
#68046=CARTESIAN_POINT ( 'NONE',  ( 3.469938103458301892, 2.153457811087633011, -0.4814610123115290463 ) ) ;
#68048=CARTESIAN_POINT ( 'NONE',  ( 1.744728380183872218, -0.2665191970635071295, -1.841615994452956873 ) ) ;
#68052=CARTESIAN_POINT ( 'NONE',  ( 6.925078400183575233, 4.688909937558557672, 2.706876980850602354 ) ) ;
#68056=CARTESIAN_POINT ( 'NONE',  ( 3.485278940986863638, 1.863876800102952203, -0.8796150190680316339 ) ) ;
#68060=CARTESIAN_POINT ( 'NONE',  ( 2.069016002695713397, -1.559697248980717266, 1.283103002569847106 ) ) ;
#68063=CARTESIAN_POINT ( 'NONE',  ( 1.956002958106726419, 2.055451868484101219, -0.1503645474096800549 ) ) ;
#68067=CARTESIAN_POINT ( 'NONE',  ( -0.1411974294641681893, 1.383765339824583052, -2.157932961605046440 ) ) ;
#68068=CARTESIAN_POINT ( 'NONE',  ( 6.650339433524894872, -1.499410535642144549, 1.233700977392115705 ) ) ;
#68070=CARTESIAN_POINT ( 'NONE',  ( 5.338574060078519423, 2.173733305800494175, 0.3801736985692484305 ) ) ;
#68072=CARTESIAN_POINT ( 'NONE',  ( 1.353037089713942320, -1.704917477850418805, 1.328741451194020762 ) ) ;
#68074=CARTESIAN_POINT ( 'NONE',  ( 1.850796360583713884, -1.845628094615419768, -0.8128149310912060610 ) ) ;
#68076=CARTESIAN_POINT ( 'NONE',  ( 2.073957380999270850, 1.703569143382680506, -1.543048383257297207 ) ) ;
#68079=CARTESIAN_POINT ( 'NONE',  ( 0.2505829665140328899, -1.505242420826727656, 1.110479572284161831 ) ) ;
#68080=CARTESIAN_POINT ( 'NONE',  ( 2.149089010626914931, -1.500894351328721621, -1.116326037436713881 ) ) ;
#68082=CARTESIAN_POINT ( 'NONE',  ( 3.995327539805045181, -0.3399590882401174463, 1.987497567597557468 ) ) ;
#68086=CARTESIAN_POINT ( 'NONE',  ( 4.670599442626208742, -1.376304852316366789, 1.594240983682773782 ) ) ;
#68087=CARTESIAN_POINT ( 'NONE',  ( 5.670397268163976712, -0.9275489576153757021, -1.851018422006404096 ) ) ;
#68091=CARTESIAN_POINT ( 'NONE',  ( 5.554946522049384328, 0.3980760423633997180, 1.979986811436624805 ) ) ;
#68093=CARTESIAN_POINT ( 'NONE',  ( 0.7079710255328255375, 0.6504495457556063176, -1.957355765043818696 ) ) ;
#68099=( NAMED_UNIT ( * ) SI_UNIT ( $, .STERADIAN. ) SOLID_ANGLE_UNIT ( ) );
#68101=CARTESIAN_POINT ( 'NONE',  ( 2.735037655519993560, -2.077075009683257090, -0.6322084445426826571 ) ) ;
#68104=CARTESIAN_POINT ( 'NONE',  ( 3.122423488780329492, 0.04808623196613136253, 1.840796284283818585 ) ) ;
#68106=CARTESIAN_POINT ( 'NONE',  ( 4.915667883426772633, -1.172277214026868464, -1.851500752446763709 ) ) ;
#68108=CARTESIAN_POINT ( 'NONE',  ( 5.348581951612152885, 0.6511601234850499242, 2.166799557567296919 ) ) ;
#68114=CARTESIAN_POINT ( 'NONE',  ( 6.591055360535956531, 1.538344802651976373, -0.8746889052434738687 ) ) ;
#68116=CARTESIAN_POINT ( 'NONE',  ( 4.354156267015011572, 0.8588168762691525959, -1.820826276449886150 ) ) ;
#68118=CARTESIAN_POINT ( 'NONE',  ( 2.538226622342924177, 0.9936286567288643568, -1.856823529840909481 ) ) ;
#68119=CARTESIAN_POINT ( 'NONE',  ( 1.546349530022947727, -1.353405651413071453, 1.355934989043396044 ) ) ;
#68123=CARTESIAN_POINT ( 'NONE',  ( 2.400782916097830455, 0.4286735998642232648, 1.922169311629307931 ) ) ;
#68125=CARTESIAN_POINT ( 'NONE',  ( 0.07479286986305370977, 0.004866263145587856019, -1.855573292446038414 ) ) ;
#68126=CARTESIAN_POINT ( 'NONE',  ( 0.7484013653801385724, -1.946605496936428370, -0.2438083268051088881 ) ) ;
#68127=CARTESIAN_POINT ( 'NONE',  ( 0.6328886395040033142, 1.767934563615305432, 0.7296191750566642931 ) ) ;
#68128=ORIENTED_EDGE ( 'NONE', *, *, #17772, .F. ) ;
#68132=CARTESIAN_POINT ( 'NONE',  ( 5.471519871388384360, 1.802534880541529994, -0.5000026934619330454 ) ) ;
#68135=CARTESIAN_POINT ( 'NONE',  ( 5.489151832033660305, 0.1466973765328460355, 2.065091666743318122 ) ) ;
#68138=CARTESIAN_POINT ( 'NONE',  ( 0.2036857628631080219, -1.599406074100502506, -1.314310892166506095 ) ) ;
#68148=CARTESIAN_POINT ( 'NONE',  ( 4.773855682050706761, -1.924389145058275963, 0.3807478752155256663 ) ) ;
#68150=CARTESIAN_POINT ( 'NONE',  ( 3.550157523342876154, 1.823840110401256931, -0.8594984857327038208 ) ) ;
#68151=CARTESIAN_POINT ( 'NONE',  ( 2.940549639715861030, -1.447296733178250250, 1.255168957218324666 ) ) ;
#68152=CARTESIAN_POINT ( 'NONE',  ( 0.02921319935947005314, -2.001080581411585513, 0.8940957790435491992 ) ) ;
#68153=CARTESIAN_POINT ( 'NONE',  ( 0.1331715793776600265, 0.003733371859311259821, -1.953671397793784070 ) ) ;
#68154=CARTESIAN_POINT ( 'NONE',  ( 3.514787476322968285, 1.689724804184733253, 0.8026845837263293371 ) ) ;
#68158=CARTESIAN_POINT ( 'NONE',  ( 4.464542613241986757, -2.054094600764106548, -0.5127786416893320709 ) ) ;
#68161=CARTESIAN_POINT ( 'NONE',  ( 5.600075274486990828, 0.8424382930321882013, -1.891409743246947217 ) ) ;
#68162=CARTESIAN_POINT ( 'NONE',  ( 2.665665183201745947, 1.120710701610077908, 1.764813211807507942 ) ) ;
#68163=CARTESIAN_POINT ( 'NONE',  ( 6.620655732516651071, 2.021119449029490589, 2.477762541108457839 ) ) ;
#68164=CARTESIAN_POINT ( 'NONE',  ( 0.7270763493693053192, -1.639898566368836130, 0.5346300883638678281 ) ) ;
#68175=CARTESIAN_POINT ( 'NONE',  ( 0.4338566731940462495, -0.9675643781421030543, -1.531218756180543927 ) ) ;
#68184=CARTESIAN_POINT ( 'NONE',  ( 0.8783700953360704666, -0.4667435877003899836, -1.857722024819864037 ) ) ;
#68185=CARTESIAN_POINT ( 'NONE',  ( 0.1356056236470788157, -0.09959319089659908475, 2.118264760961988458 ) ) ;
#68191=CARTESIAN_POINT ( 'NONE',  ( 3.028127619189690201, 1.049479266250245901, 1.666313143567710542 ) ) ;
#68193=CARTESIAN_POINT ( 'NONE',  ( 1.998837940877351116, -2.080155006269391205, -0.4107514010402503746 ) ) ;
#68196=CARTESIAN_POINT ( 'NONE',  ( 6.727182134110222478, 7.629137130509071163, 2.789055895399249252 ) ) ;
#68197=CARTESIAN_POINT ( 'NONE',  ( 6.123007039855313138, -2.064672272812938747, 0.7349105657750015785 ) ) ;
#68199=CARTESIAN_POINT ( 'NONE',  ( 3.750929837476246753, -1.575545889128293853, 1.108190883620339795 ) ) ;
#68203=CARTESIAN_POINT ( 'NONE',  ( 0.5048604690408053930, -0.7474223562033956991, -2.076596198196341003 ) ) ;
#68207=CARTESIAN_POINT ( 'NONE',  ( 5.875830846898042914, -1.922239612846994294, 0.4278824943488717114 ) ) ;
#68208=CARTESIAN_POINT ( 'NONE',  ( 0.7845916355662507780, 1.712027273464492350, -0.9168598982515554496 ) ) ;
#68210=CARTESIAN_POINT ( 'NONE',  ( 6.239697403921985241, -2.179564881273305943, -0.7296402976008103947 ) ) ;
#68212=CARTESIAN_POINT ( 'NONE',  ( 4.363987150452108388, -1.856190122274929077, 0.1334137851533196695 ) ) ;
#68219=CARTESIAN_POINT ( 'NONE',  ( -0.1290005225502675879, -0.006633637972621592160, -2.173875058097324064 ) ) ;
#68224=CARTESIAN_POINT ( 'NONE',  ( 0.2580658466875830337, 0.6954254843183353962, 1.688255465954719536 ) ) ;
#68226=CARTESIAN_POINT ( 'NONE',  ( 2.197566421822871874, 1.549772363009613407, 0.7782106121714903457 ) ) ;
#68228=CARTESIAN_POINT ( 'NONE',  ( 6.509000000000034092, 7.052765612591089806, 2.598154238703707541 ) ) ;
#68229=CARTESIAN_POINT ( 'NONE',  ( 0.1176308287326099516, -1.889623933557175617, 0.3742946393059803367 ) ) ;
#68230=CARTESIAN_POINT ( 'NONE',  ( 3.502741298630154709, 0.4721981695934416856, 1.903977903881831191 ) ) ;
#68234=CARTESIAN_POINT ( 'NONE',  ( 5.162787349232583090, 0.6159572760087471677, 2.029033592890214788 ) ) ;
#68237=CARTESIAN_POINT ( 'NONE',  ( 3.204029340230400091, 0.7494766052340908757, -1.929994576353490032 ) ) ;
#68240=CARTESIAN_POINT ( 'NONE',  ( 4.477308758892056595, -1.984000869926884736, -0.9990560778978144763 ) ) ;
#68242=CARTESIAN_POINT ( 'NONE',  ( 2.936492027000091376, -1.880918663215241926, -1.321213444053377373 ) ) ;
#68251=CARTESIAN_POINT ( 'NONE',  ( 4.289254230599209627, -0.005406649120142519548, -1.912571728590661380 ) ) ;
#68253=CARTESIAN_POINT ( 'NONE',  ( 5.561458258421018819, 0.3325557151471290052, -1.692213012293216190 ) ) ;
#68254=CARTESIAN_POINT ( 'NONE',  ( 2.975796278104339887, -0.8128168404246680634, 1.845627246706407432 ) ) ;
#68255=CARTESIAN_POINT ( 'NONE',  ( 5.274211419651455124, 2.028235465341983623, -1.081840468886515305 ) ) ;
#68257=CARTESIAN_POINT ( 'NONE',  ( 6.674446291637649686, -1.297315479741867117, 1.659578660624160706 ) ) ;
#68260=CARTESIAN_POINT ( 'NONE',  ( 5.940640833738206616, 0.3468769465994473444, 1.735210755170372376 ) ) ;
#68262=CARTESIAN_POINT ( 'NONE',  ( 1.764052804016162268, 1.181211026566388211, 1.964360346841328209 ) ) ;
#68263=CARTESIAN_POINT ( 'NONE',  ( 6.544863656343847147, -1.481929198830441274, -1.092355128777318107 ) ) ;
#68269=CARTESIAN_POINT ( 'NONE',  ( 6.725056259267968350, -1.891221747171191403, -0.8428681758992571105 ) ) ;
#68270=CARTESIAN_POINT ( 'NONE',  ( 1.675017921984035096, 1.752138005693338441, -0.9981273289914743829 ) ) ;
#68273=CARTESIAN_POINT ( 'NONE',  ( 5.760362637647353345, 0.7829873311157690141, 1.760386188003287611 ) ) ;
#68275=CARTESIAN_POINT ( 'NONE',  ( 1.811064542976594360, -0.5979718353220222493, -2.139333889645285147 ) ) ;
#68282=CARTESIAN_POINT ( 'NONE',  ( 4.809955069398625938, 1.195453170786121788, -1.265177307932338513 ) ) ;
#68284=CARTESIAN_POINT ( 'NONE',  ( 2.172246964874047670, -0.9220853831424129510, -1.731647142839589870 ) ) ;
#68289=CARTESIAN_POINT ( 'NONE',  ( 1.328664801108740523, -1.309985447229580213, 1.593267124675311841 ) ) ;
#68292=CARTESIAN_POINT ( 'NONE',  ( 1.305971919559431704, -0.5478059591418303897, 2.195072679011981442 ) ) ;
#68295=CARTESIAN_POINT ( 'NONE',  ( 2.495189509527053762, 1.443206194050347557, 1.189963633554675937 ) ) ;
#68296=CARTESIAN_POINT ( 'NONE',  ( 1.054805789555151696, -1.101345310128332367, 1.339526040370845772 ) ) ;
#68297=CARTESIAN_POINT ( 'NONE',  ( 5.056268342064010213, -1.587557771011731678, 1.511049258477934032 ) ) ;
#68298=CARTESIAN_POINT ( 'NONE',  ( 5.473738792520003393, 2.225791634824420218, -0.6087584347118053518 ) ) ;
#68299=CARTESIAN_POINT ( 'NONE',  ( 1.762645127485995555, -1.458140857472267626, 1.456663342728149901 ) ) ;
#68300=CARTESIAN_POINT ( 'NONE',  ( 3.081904124835439074, -1.913310220277367080, -0.3314154666464886323 ) ) ;
#68303=CARTESIAN_POINT ( 'NONE',  ( 5.694569522353671864, -0.4537686991618711807, -1.814561337198366653 ) ) ;
#68304=CARTESIAN_POINT ( 'NONE',  ( 1.968750000000001332, 0.7852924748298835134, -1.895863743164130755 ) ) ;
#68307=CARTESIAN_POINT ( 'NONE',  ( 6.890000000000050306, -0.002781820520068867264, 1.999840353888074240 ) ) ;
#68310=CARTESIAN_POINT ( 'NONE',  ( 4.447888798048591497, -1.802416534049579910, -0.9041112711936499791 ) ) ;
#68314=CARTESIAN_POINT ( 'NONE',  ( 2.191784710619415044, -0.7813054520266484726, 1.650194661559079456 ) ) ;
#68315=DIRECTION ( 'NONE',  ( 1.039099362110107450E-15, 1.000000000000000000, -4.583713267641621330E-32 ) ) ;
#68323=CARTESIAN_POINT ( 'NONE',  ( 5.883464967995201356, 0.1463045851861736191, -2.014419601194089804 ) ) ;
#68324=CARTESIAN_POINT ( 'NONE',  ( 0.1707708301344288138, 0.8156354886642532831, 1.957547177562010354 ) ) ;
#68328=CARTESIAN_POINT ( 'NONE',  ( 5.049710947255391602, 0.6486796242286404501, -1.956199288699921768 ) ) ;
#68329=CARTESIAN_POINT ( 'NONE',  ( 4.975232503164924935, -2.001511053420693020, -0.2440319332882301961 ) ) ;
#68337=CARTESIAN_POINT ( 'NONE',  ( 4.727888646976695419, -1.799647678597478206, -0.9090046787488814672 ) ) ;
#68338=CARTESIAN_POINT ( 'NONE',  ( 4.540845788227630742, -1.424921066559198257, -1.165926479108070346 ) ) ;
#68340=CARTESIAN_POINT ( 'NONE',  ( 1.752963477315866658, 0.7269187894614470569, 2.190284518487267906 ) ) ;
#68342=CARTESIAN_POINT ( 'NONE',  ( 5.272814564875167420, -2.033366364591123521, -0.7337546567489708904 ) ) ;
#68344=CARTESIAN_POINT ( 'NONE',  ( 0.3275467377269140057, 0.9974989819340736030, -1.666164454441501297 ) ) ;
#68349=CARTESIAN_POINT ( 'NONE',  ( 3.397188523315307407, 1.473948685399184333, 1.151750840393983344 ) ) ;
#68350=CARTESIAN_POINT ( 'NONE',  ( 0.1406777020166137260, 1.830675540527426648, 0.5531436448603862521 ) ) ;
#68353=CARTESIAN_POINT ( 'NONE',  ( 2.332911791115964473, 2.140974936812658935, 0.5348262304398290201 ) ) ;
#68359=CARTESIAN_POINT ( 'NONE',  ( 0.3507686748964663481, -1.586079953665324060, 1.170567870040557290 ) ) ;
#68360=CARTESIAN_POINT ( 'NONE',  ( 0.2007804849885147513, -2.307177064702860214, -0.05170730859792996986 ) ) ;
#68361=CARTESIAN_POINT ( 'NONE',  ( 1.012071980069819910, 1.959787197952606252, -0.09269708818125664551 ) ) ;
#68362=CARTESIAN_POINT ( 'NONE',  ( 3.784078317859154605, -1.224626257592566159, -1.659553996539532283 ) ) ;
#68371=CARTESIAN_POINT ( 'NONE',  ( 6.391115334191724173, 0.2064332055253786102, 2.161336459811058042 ) ) ;
#68373=CARTESIAN_POINT ( 'NONE',  ( 6.181194517112824194, 1.274813594131599226, 1.328792456347933637 ) ) ;
#68376=CARTESIAN_POINT ( 'NONE',  ( 0.9306671693925671063, 0.1315677519515070781, 1.865966016356377821 ) ) ;
#68382=CARTESIAN_POINT ( 'NONE',  ( 0.7153071762652126742, 1.563590412251715911, 1.100639817434710954 ) ) ;
#68383=CARTESIAN_POINT ( 'NONE',  ( 2.764225215535959457, -1.222102382295175760, 1.280393980213704763 ) ) ;
#68385=CARTESIAN_POINT ( 'NONE',  ( 0.1879522776407696050, 1.101030317643518330, 1.563299796079109072 ) ) ;
#68387=CARTESIAN_POINT ( 'NONE',  ( 4.780823714695519477, 1.590225366507077354, -1.067722475238532365 ) ) ;
#68389=CARTESIAN_POINT ( 'NONE',  ( 5.019951571474082996, 1.948400538373602497, -0.2868881896359152806 ) ) ;
#68390=CARTESIAN_POINT ( 'NONE',  ( 0.4750491441844888474, -1.531729482103380224, 1.466773057065169361 ) ) ;
#68392=CARTESIAN_POINT ( 'NONE',  ( 3.924554409752772699, 1.776107677202539925, 0.5873546117282567591 ) ) ;
#68393=CARTESIAN_POINT ( 'NONE',  ( 0.5920835508136900183, -1.811502216344462735, -0.2265648652611390590 ) ) ;
#68395=CARTESIAN_POINT ( 'NONE',  ( 3.668774463136436736, -1.482526648764719734, 1.634931011441637771 ) ) ;
#68398=CARTESIAN_POINT ( 'NONE',  ( 0.7134213396373456639, -1.741552128810987421, -1.105017490550715742 ) ) ;
#68406=CARTESIAN_POINT ( 'NONE',  ( 3.402844027952243167, 0.5003511028610057032, 2.008882729757965890 ) ) ;
#68408=CARTESIAN_POINT ( 'NONE',  ( 1.335488691732108046, -1.954760257947166568, 0.9229496955955732718 ) ) ;
#68410=CARTESIAN_POINT ( 'NONE',  ( 0.7506560300556723853, 1.990167900158135605, 0.3429568431373567483 ) ) ;
#68412=ORIENTED_EDGE ( 'NONE', *, *, #162518, .F. ) ;
#68416=CARTESIAN_POINT ( 'NONE',  ( 6.503279807981922289, 1.993766592317405273, 0.2985777636397292101 ) ) ;
#68417=CARTESIAN_POINT ( 'NONE',  ( 0.04025042243083893495, 0.7762349914572730381, 1.861342399428978389 ) ) ;
#68419=CARTESIAN_POINT ( 'NONE',  ( 5.478137895480934105, -2.137967713159651506, -0.4810252310911074525 ) ) ;
#68421=CARTESIAN_POINT ( 'NONE',  ( 3.093911922779784440, 1.216618333484908998, 1.475457842794763996 ) ) ;
#68425=CARTESIAN_POINT ( 'NONE',  ( 1.599232692168949699, -0.2440074622011619843, 2.001515180871694888 ) ) ;
#68427=CARTESIAN_POINT ( 'NONE',  ( 0.09973926083830295108, -0.6030689337076476919, 2.211586693686658389 ) ) ;
#68429=CARTESIAN_POINT ( 'NONE',  ( 3.610098185430905104, -0.6985691267104906510, -1.577150584296799440 ) ) ;
#68430=CARTESIAN_POINT ( 'NONE',  ( 0.1394461523057501928, 1.435241935670927171, -1.984817279021661829 ) ) ;
#68433=CARTESIAN_POINT ( 'NONE',  ( 0.8011316787140990714, -1.684513426579350659, 1.005393624328714264 ) ) ;
#68437=CARTESIAN_POINT ( 'NONE',  ( 0.1751657365761521701, 1.361037063587458906, -2.300812366989886559 ) ) ;
#68440=FACE_OUTER_BOUND ( 'NONE', #189568, .T. ) ;
#68442=CARTESIAN_POINT ( 'NONE',  ( 3.439928307436474597, -1.081519596823855345, -1.453003583242311381 ) ) ;
#68446=CARTESIAN_POINT ( 'NONE',  ( 4.898965649768390662, -0.2269230896460339986, -1.797137895798770479 ) ) ;
#68448=( LENGTH_UNIT ( ) NAMED_UNIT ( * ) SI_UNIT ( .MILLI., .METRE. ) );
#68451=CARTESIAN_POINT ( 'NONE',  ( 6.197681965292040296, -1.348592564218813905, -1.282738352563756123 ) ) ;
#68453=CARTESIAN_POINT ( 'NONE',  ( 3.269047429782430125, 1.730524700466531396, -0.8218109994902050852 ) ) ;
#68461=CARTESIAN_POINT ( 'NONE',  ( 1.042116488573753497, 0.8753402851892390091, -1.976733581976031218 ) ) ;
#68464=CARTESIAN_POINT ( 'NONE',  ( 1.377666516899571647, 1.084121917808708035, 1.468671923017292658 ) ) ;
#68467=CARTESIAN_POINT ( 'NONE',  ( 3.698116152863577977, -1.823479002399010396, -0.09026698595545472326 ) ) ;
#68469=CARTESIAN_POINT ( 'NONE',  ( 1.916128293556786044, -1.911906470838855343, 0.05044092668918254141 ) ) ;
#68470=CARTESIAN_POINT ( 'NONE',  ( 2.646873730718673379, -0.3338169989568114948, -1.940879108454116375 ) ) ;
#68471=CARTESIAN_POINT ( 'NONE',  ( 4.282717048480193078, 1.733172068543160416, -0.8763712590400226654 ) ) ;
#68474=CARTESIAN_POINT ( 'NONE',  ( 4.342108446431157454, -1.306982937058022820, -1.669832246961988176 ) ) ;
#68482=CARTESIAN_POINT ( 'NONE',  ( 3.861776535121093090, 1.811678901967550326, -0.2252020330209548171 ) ) ;
#68483=CARTESIAN_POINT ( 'NONE',  ( 6.069546051295945155, 1.394081536189460069, 1.457239770841619597 ) ) ;
#68488=CARTESIAN_POINT ( 'NONE',  ( 6.121928861531041655, -1.040746078065577063, -1.554202398018275755 ) ) ;
#68490=CARTESIAN_POINT ( 'NONE',  ( 3.668508669297173341, -1.293070320541231721, 1.428231264829373126 ) ) ;
#68497=CARTESIAN_POINT ( 'NONE',  ( 1.652128961607162827, 1.091750937195800519, 1.813926670343589898 ) ) ;
#68500=CARTESIAN_POINT ( 'NONE',  ( 5.875854205266583641, -2.021069926245163906, 0.4479438709683660202 ) ) ;
#68501=CARTESIAN_POINT ( 'NONE',  ( 1.557894219809667247, -1.301531972126177772, 1.302644501960325885 ) ) ;
#68506=CARTESIAN_POINT ( 'NONE',  ( 1.465189672511356900, 0.1648890142370383061, -2.286389102023842490 ) ) ;
#68508=CARTESIAN_POINT ( 'NONE',  ( 5.824156380204161820, 1.872177270857039000, 0.5156464658115608168 ) ) ;
#68511=CARTESIAN_POINT ( 'NONE',  ( 0.3693899063928334781, -1.702925086422102163, -1.073505336752482053 ) ) ;
#68512=CARTESIAN_POINT ( 'NONE',  ( 6.456263137377812988, -1.236968576560823818, 1.593241027169019830 ) ) ;
#68516=CARTESIAN_POINT ( 'NONE',  ( 3.679701837385487284, -1.030134525132427203, 1.819138145232774839 ) ) ;
#68517=CARTESIAN_POINT ( 'NONE',  ( 1.814973546968738027, -0.2204486908502552300, 1.755991699180702748 ) ) ;
#68520=CARTESIAN_POINT ( 'NONE',  ( 5.173897996269102961, -1.276782452619073860, 1.903577390058891261 ) ) ;
#68521=CARTESIAN_POINT ( 'NONE',  ( 3.767295573485733851, 0.9686143178696275946, 1.445635114442943348 ) ) ;
#68524=CARTESIAN_POINT ( 'NONE',  ( 3.479597601185040912, 1.566717760139114901, 0.7430284921127163766 ) ) ;
#68525=CARTESIAN_POINT ( 'NONE',  ( 3.613895077877467443, 0.5305607931336644434, -2.105228361949755378 ) ) ;
#68528=CARTESIAN_POINT ( 'NONE',  ( 4.592982591267942283, 1.756852934926198317, 0.9896879400849432074 ) ) ;
#68529=CARTESIAN_POINT ( 'NONE',  ( 0.9062500000000004441, 1.895863743164069470, -0.7852924748300356139 ) ) ;
#68531=CARTESIAN_POINT ( 'NONE',  ( 1.711812753757115502, -1.912122584522325086, 0.2334695860961126246 ) ) ;
#68533=CARTESIAN_POINT ( 'NONE',  ( 5.554997651100567424, 0.4332456915393156915, 2.178594967391647597 ) ) ;
#68535=CARTESIAN_POINT ( 'NONE',  ( -0.2106854629475426177, 0.2415373081153374957, -2.031805921504933554 ) ) ;
#68540=CARTESIAN_POINT ( 'NONE',  ( 0.5225339808294949817, -2.210013125053798433, 0.2238140636349055246 ) ) ;
#68541=CARTESIAN_POINT ( 'NONE',  ( 5.670351692713981429, -0.8806477319739226539, -1.753155087565357428 ) ) ;
#68544=CARTESIAN_POINT ( 'NONE',  ( 6.397788901632932124, -0.7711469528366134973, 2.127058432633963658 ) ) ;
#68549=CARTESIAN_POINT ( 'NONE',  ( 3.895030958483152173, 0.2998364479755392664, 2.040644712996171339 ) ) ;
#68553=CARTESIAN_POINT ( 'NONE',  ( 6.257094453949625823, -1.604276942902042480, -0.9616840659161307592 ) ) ;
#68554=CARTESIAN_POINT ( 'NONE',  ( 4.307042110543488178, 1.062484115506344473, -1.370455642081182646 ) ) ;
#68555=CARTESIAN_POINT ( 'NONE',  ( 4.229842819227870976, 1.707864474872609062, 0.3341882380870179192 ) ) ;
#68557=CARTESIAN_POINT ( 'NONE',  ( 1.945279335750784711, -1.843959696387540204, -1.361743503316152681 ) ) ;
#68559=CARTESIAN_POINT ( 'NONE',  ( 5.548407312280490444, -1.647412313956169605, 1.287198389022710998 ) ) ;
#68560=CARTESIAN_POINT ( 'NONE',  ( 6.685517510867199142, -0.8268063683338886527, 1.755141085440144355 ) ) ;
#68562=CARTESIAN_POINT ( 'NONE',  ( 1.951796282902381163, -1.844710420878793444, -0.8146254186931353169 ) ) ;
#68563=CARTESIAN_POINT ( 'NONE',  ( 0.6565081633774123571, -1.584678946828571133, 1.513927167823600595 ) ) ;
#68567=CARTESIAN_POINT ( 'NONE',  ( 2.596466591541984226, -1.087938976695131066, 1.819974527870950265 ) ) ;
#68569=CARTESIAN_POINT ( 'NONE',  ( 5.180226163740526246, -1.011166736308216629, 1.519887457628710248 ) ) ;
#68570=ORIENTED_EDGE ( 'NONE', *, *, #26940, .T. ) ;
#68575=CARTESIAN_POINT ( 'NONE',  ( 2.795180614130913010, -0.1526695769738794506, -2.014101982623817566 ) ) ;
#68576=CARTESIAN_POINT ( 'NONE',  ( 6.475609205405274515, 2.113627995098281254, -0.6344055572156809264 ) ) ;
#68579=CARTESIAN_POINT ( 'NONE',  ( 4.416758307032777608, -1.381121683685157642, 1.247472197611438016 ) ) ;
#68588=CARTESIAN_POINT ( 'NONE',  ( 1.651252135258261422, -0.2480751513778757522, -1.715843305285965403 ) ) ;
#68589=CARTESIAN_POINT ( 'NONE',  ( 1.675334203684273771, -0.9328193774022232043, 1.469000774227617434 ) ) ;
#68590=CARTESIAN_POINT ( 'NONE',  ( 5.180430901434020186, -1.285682204016626029, 1.916193241175147666 ) ) ;
#68593=CARTESIAN_POINT ( 'NONE',  ( 0.8607048193125128588, -1.494471031236654257, 1.419199468611084480 ) ) ;
#68598=CARTESIAN_POINT ( 'NONE',  ( 6.679114621301890153, -1.074570768553984479, -2.031732957927368410 ) ) ;
#68601=CARTESIAN_POINT ( 'NONE',  ( 0.07499057489264608634, 0.002531239327739977750, -1.955573237620360949 ) ) ;
#68602=CARTESIAN_POINT ( 'NONE',  ( 4.711142613322857109, 1.586760866459841379, -1.067142987418716604 ) ) ;
#68604=CARTESIAN_POINT ( 'NONE',  ( 6.498651167236064730, -0.5841124237929047336, -2.128106146270396071 ) ) ;
#68609=CARTESIAN_POINT ( 'NONE',  ( 0.2408861781304712513, 1.933338575160881367, 0.5842326518414300285 ) ) ;
#68610=CARTESIAN_POINT ( 'NONE',  ( 3.997355382689435466, 1.951332032848082099, -1.231501813138028423 ) ) ;
#68611=CARTESIAN_POINT ( 'NONE',  ( 5.072687121480487171, 1.354251660176824856, -1.419695456575476689 ) ) ;
#68612=CARTESIAN_POINT ( 'NONE',  ( 0.5319879461419263489, 1.124744735265088780, 1.607134405190835391 ) ) ;
#68616=CARTESIAN_POINT ( 'NONE',  ( 0.005274918996244109745, -0.09700444455036473512, 2.115223206416060098 ) ) ;
#68620=CARTESIAN_POINT ( 'NONE',  ( 2.711994142844989408, 0.5828001693900261015, -2.091290491527279194 ) ) ;
#68622=CARTESIAN_POINT ( 'NONE',  ( 0.8617730121942971389, -1.675286201960282995, -1.300076073212981242 ) ) ;
#68628=CARTESIAN_POINT ( 'NONE',  ( 1.774756598535260466, -1.955815263226182932, -0.6494449766335576024 ) ) ;
#68633=ORIENTED_EDGE ( 'NONE', *, *, #155535, .F. ) ;
#68634=CARTESIAN_POINT ( 'NONE',  ( 4.125576785117724299, -0.3237648511281773778, 1.884507068624697190 ) ) ;
#68636=CARTESIAN_POINT ( 'NONE',  ( 1.546537457781042235, 2.259796958156198077, 0.1114739384607699862 ) ) ;
#68638=CARTESIAN_POINT ( 'NONE',  ( 1.634716215409822260, 1.691188361570634235, 0.6499044650936767198 ) ) ;
#68639=CARTESIAN_POINT ( 'NONE',  ( 1.358442855636652791, -1.820242846481026078, -0.5975442777857197241 ) ) ;
#68641=CARTESIAN_POINT ( 'NONE',  ( 2.313015868914463091, -1.601887806243259771, 1.311650804931147274 ) ) ;
#68643=CARTESIAN_POINT ( 'NONE',  ( 0.4265601315296633778, 1.885908329847274745, 0.5744540738892388587 ) ) ;
#68644=CARTESIAN_POINT ( 'NONE',  ( 5.742784330379758551, 0.3781152824756833231, 1.888869927322960329 ) ) ;
#68645=CARTESIAN_POINT ( 'NONE',  ( 0.1711457161924005987, -1.502117798334397403, 1.751973695569712497 ) ) ;
#68648=CARTESIAN_POINT ( 'NONE',  ( 4.510253362402360189, 2.062282729996979924, -0.04753222776765659435 ) ) ;
#68653=CARTESIAN_POINT ( 'NONE',  ( 5.051841681570322429, 0.6635009534815727861, -1.998768678292896839 ) ) ;
#68655=CARTESIAN_POINT ( 'NONE',  ( 0.1393978552833140261, -0.1497620924123649333, -2.137132186964474378 ) ) ;
#68657=CARTESIAN_POINT ( 'NONE',  ( 4.569695524216377258, 2.097929177840287540, -0.5203329012281321386 ) ) ;
#68658=CARTESIAN_POINT ( 'NONE',  ( 5.531901104011129000, -1.969946598288346618, 0.4446316349850876759 ) ) ;
#68659=CARTESIAN_POINT ( 'NONE',  ( -0.1399997263889594112, -0.002789056014654289761, -2.000146600338557956 ) ) ;
#68665=CARTESIAN_POINT ( 'NONE',  ( 3.292204118033771110, -0.8216723425069611952, -1.841733987974409237 ) ) ;
#68669=CARTESIAN_POINT ( 'NONE',  ( 5.454052192070485638, 2.159419290912270029, -0.1019294599445344784 ) ) ;
#68671=( NAMED_UNIT ( * ) PLANE_ANGLE_UNIT ( ) SI_UNIT ( $, .RADIAN. ) );
#68672=DIRECTION ( 'NONE',  ( -1.000000000000000000, 0.000000000000000000, 0.000000000000000000 ) ) ;
#68674=CARTESIAN_POINT ( 'NONE',  ( 4.499625164952708367, -1.976952908697379607, 0.3961224619316304763 ) ) ;
#68676=CARTESIAN_POINT ( 'NONE',  ( 0.5391470445266118849, -1.216214603651460724, -1.223400588829765878 ) ) ;
#68681=CARTESIAN_POINT ( 'NONE',  ( 5.536355731483205922, 1.842701317132239724, 0.3206550288221421963 ) ) ;
#68682=CARTESIAN_POINT ( 'NONE',  ( 6.135026823787811168, 1.880036687389478489, 0.7205229627402914838 ) ) ;
#68685=CIRCLE ( 'NONE', #48029, 0.04999999999999969746 ) ;
#68689=CARTESIAN_POINT ( 'NONE',  ( 0.1929827526203631294, 1.755782054984224683, 0.9913788669043410717 ) ) ;
#68690=CARTESIAN_POINT ( 'NONE',  ( 1.124954419467529831, 1.598432135740068372, 0.8524628987082534248 ) ) ;
#68692=CARTESIAN_POINT ( 'NONE',  ( 5.858325616802108726, 0.8718737102157668728, 1.978260574764856283 ) ) ;
#68695=CARTESIAN_POINT ( 'NONE',  ( 0.6904808011564408377, 1.448434100015457693, -1.253846941973751683 ) ) ;
#68703=CARTESIAN_POINT ( 'NONE',  ( 4.416967121957662279, 1.975198431823081302, 0.8787980929093121008 ) ) ;
#68706=CARTESIAN_POINT ( 'NONE',  ( 0.8266187642571948269, -0.9586779626098644869, -1.891633453305548773 ) ) ;
#68708=CARTESIAN_POINT ( 'NONE',  ( 2.512907010818050679, 1.759183109745281692, 0.8898679072262619671 ) ) ;
#68709=CARTESIAN_POINT ( 'NONE',  ( 4.957238921819991262, -1.637161358497842389, 0.9882132959125531357 ) ) ;
#68712=EDGE_CURVE ( 'NONE', #144405, #8531, #101612, .T. ) ;
#68713=CARTESIAN_POINT ( 'NONE',  ( 6.180130249528606790, -1.092802789126966934, -1.638350696670291651 ) ) ;
#68714=CARTESIAN_POINT ( 'NONE',  ( 1.183423309950997870, -0.8736912582980368436, 1.734375191483277900 ) ) ;
#68721=CARTESIAN_POINT ( 'NONE',  ( 4.775979982822478931, 1.890921987351320777, -0.2842533987747336566 ) ) ;
#68723=CARTESIAN_POINT ( 'NONE',  ( 3.774219598512587037, 1.225428716765289527, 1.835190637982798023 ) ) ;
#68724=CARTESIAN_POINT ( 'NONE',  ( 2.432911661931828284, 2.140371652790736601, 0.5367425311649312025 ) ) ;
#68727=CARTESIAN_POINT ( 'NONE',  ( 0.7153071762652126742, 1.563590412251715911, 1.100639817434710954 ) ) ;
#68728=CARTESIAN_POINT ( 'NONE',  ( -0.02338929933906607611, 7.629137130509112907, -2.310989781590186976 ) ) ;
#68731=CARTESIAN_POINT ( 'NONE',  ( 3.473154722801426786, 1.870513717286937716, 0.8877811045280564750 ) ) ;
#68735=CARTESIAN_POINT ( 'NONE',  ( 0.6378455412261313517, -1.529572671500577297, -1.527792216034072670 ) ) ;
#68736=CARTESIAN_POINT ( 'NONE',  ( 3.298540952264991777, 1.726358142885858316, -1.349911518210664241 ) ) ;
#68742=CARTESIAN_POINT ( 'NONE',  ( 5.678250988984351544, 1.318717643421193575, 1.126304846749843769 ) ) ;
#68745=CARTESIAN_POINT ( 'NONE',  ( 3.450112209602332669, -0.8433740631265237431, 1.890881698631073249 ) ) ;
#68746=CARTESIAN_POINT ( 'NONE',  ( 5.097310499321968003, -0.3096355862501755096, 2.094337834851481617 ) ) ;
#68749=CARTESIAN_POINT ( 'NONE',  ( 3.010559277710533888, 0.6591459557328577246, 1.856027811050243947 ) ) ;
#68750=CARTESIAN_POINT ( 'NONE',  ( 1.002048865836258518, -0.8573748960705518396, 1.709468765625526521 ) ) ;
#68751=CARTESIAN_POINT ( 'NONE',  ( 5.296947879282962290, 1.871547875688117424, 1.323312301801358393 ) ) ;
#68752=CARTESIAN_POINT ( 'NONE',  ( 2.560947663861262491, -1.588335953301520220, -0.9000364273514870339 ) ) ;
#68756=B_SPLINE_CURVE_WITH_KNOTS ( 'NONE', 3,
 ( #162566, #79164, #95455, #177745, #114927, #211286, #112806, #29360, #82352, #213407, #163631 ),
 .UNSPECIFIED., .F., .F.,
 ( 4, 1, 1, 1, 1, 1, 1, 1, 4 ),
 ( 0.000000000000000000, 0.2256085737580844630, 0.3975982043691296264, 0.5251069566405043298, 0.6172860083021659561, 0.6832860984239963464, 0.7321959383537668398, 0.7728624839797392232, 1.000000000000000000 ),
 .UNSPECIFIED. ) ;
#68757=CARTESIAN_POINT ( 'NONE',  ( 4.201435496602879738, 1.796340046740346086, -0.9091319694144882613 ) ) ;
#68759=CARTESIAN_POINT ( 'NONE',  ( 3.959774770350584561, -0.5736532364168048792, 1.875976257969473648 ) ) ;
#68762=CARTESIAN_POINT ( 'NONE',  ( 0.1755611466353265426, 6.947017789483680872, -2.839095415174418768 ) ) ;
#68763=CARTESIAN_POINT ( 'NONE',  ( 0.4684514965578719381, -1.969967889910573033, -0.7007429371770137472 ) ) ;
#68764=CARTESIAN_POINT ( 'NONE',  ( 5.559369761212399119, 0.3421458929979518948, -1.736264261622854743 ) ) ;
#68766=CARTESIAN_POINT ( 'NONE',  ( 1.640847625397081622, -1.850035366842089024, 1.174371965539475093 ) ) ;
#68767=CARTESIAN_POINT ( 'NONE',  ( 6.281193118957388855, 1.205677877666534892, 1.255287683557136491 ) ) ;
#68770=CARTESIAN_POINT ( 'NONE',  ( 0.9434950454815290710, 0.7028112840000885209, -1.575391610592514757 ) ) ;
#68771=CARTESIAN_POINT ( 'NONE',  ( 0.6326644773376333131, 0.2229630159884201934, -2.287572974657641645 ) ) ;
#68773=CARTESIAN_POINT ( 'NONE',  ( 0.5213437761196970666, -2.079166062760181788, 0.6930039600180630810 ) ) ;
#68774=CARTESIAN_POINT ( 'NONE',  ( 6.134130222960958889, 0.1235499018571624141, -1.729521282446895070 ) ) ;
#68775=CARTESIAN_POINT ( 'NONE',  ( 3.440233207309027375, 0.9924059104887033023, -1.971224004288201881 ) ) ;
#68776=CARTESIAN_POINT ( 'NONE',  ( 6.478989045741552211, 2.023467559352111866, 0.7875856005067942700 ) ) ;
#68778=CARTESIAN_POINT ( 'NONE',  ( 0.9368845280443529600, -1.665339089426773000, 1.307453795268032071 ) ) ;
#68779=CARTESIAN_POINT ( 'NONE',  ( 6.827182134110200806, 4.685259207053684705, 2.851548537572299313 ) ) ;
#68780=CARTESIAN_POINT ( 'NONE',  ( 5.491212607897098863, 1.698784202212012762, -0.9083314536618128932 ) ) ;
#68782=CARTESIAN_POINT ( 'NONE',  ( 1.242159777398026410, 2.290014686995527793, 0.1064554428192917290 ) ) ;
#68786=CARTESIAN_POINT ( 'NONE',  ( 4.565202069552391606, -1.784334575089935981, 1.322790477621762051 ) ) ;
#68792=CARTESIAN_POINT ( 'NONE',  ( 2.391250195717840477, -0.7743161457766101208, -1.862016636315230844 ) ) ;
#68794=CARTESIAN_POINT ( 'NONE',  ( 1.604420861476773208, 2.060019368494928838, 0.1054051996416793119 ) ) ;
#68800=CARTESIAN_POINT ( 'NONE',  ( 3.873126987144244193, 2.063651454400210028, -0.7377723227853100196 ) ) ;
#68801=CARTESIAN_POINT ( 'NONE',  ( 0.8619541869999207684, -0.05229984143813663777, -2.015912905633105101 ) ) ;
#68802=CARTESIAN_POINT ( 'NONE',  ( 0.9426144736941791669, -1.451487892885485742, -1.132780452900377099 ) ) ;
#68803=CARTESIAN_POINT ( 'NONE',  ( 5.425394459833968064, -1.452027641166652172, -1.773832485185691032 ) ) ;
#68804=CARTESIAN_POINT ( 'NONE',  ( 3.521284115754549582, -1.097709940230184200, -1.477957507169822104 ) ) ;
#68806=CARTESIAN_POINT ( 'NONE',  ( 4.418855976699648025, 1.669273799801282765, 0.7395231729718022562 ) ) ;
#68807=CARTESIAN_POINT ( 'NONE',  ( 5.502577337681268332, -1.966645332631598908, 0.4444998760482973821 ) ) ;
#68809=CARTESIAN_POINT ( 'NONE',  ( 4.311571290614625518, -0.3905533787264577894, 2.228413237907675537 ) ) ;
#68811=CARTESIAN_POINT ( 'NONE',  ( 6.194376850977553417, -2.095475641407635425, -0.2099330270173524471 ) ) ;
#68812=CARTESIAN_POINT ( 'NONE',  ( 3.121598655985452275, 0.3063859900464052100, -2.047459029603612368 ) ) ;
#68817=CARTESIAN_POINT ( 'NONE',  ( 2.385270436692279006, 1.761333987333755013, -0.7808530812865380755 ) ) ;
#68819=CARTESIAN_POINT ( 'NONE',  ( 6.772316245210458163, -0.9252316606085030370, -1.738535334629727647 ) ) ;
#68824=CARTESIAN_POINT ( 'NONE',  ( 1.266231527720959926, 0.6383494478915030523, -2.127751457625071563 ) ) ;
#68825=CARTESIAN_POINT ( 'NONE',  ( 3.698352234880129874, -2.103465879664846216, -0.1051872838587295522 ) ) ;
#68828=CARTESIAN_POINT ( 'NONE',  ( 0.4845113730182957767, 1.779151863920569232, 0.5459849130424464514 ) ) ;
#68835=CARTESIAN_POINT ( 'NONE',  ( 0.9144942500491148873, -2.120778211678171488, 0.005759991200282587286 ) ) ;
#68838=CARTESIAN_POINT ( 'NONE',  ( 4.633228507203630997, 0.002057781214020309134, -1.962046631861932067 ) ) ;
#68839=CARTESIAN_POINT ( 'NONE',  ( 3.362350911093567873, 0.9703303321016673033, 1.931748911306984784 ) ) ;
#68840=CARTESIAN_POINT ( 'NONE',  ( 1.593040506729075823, -0.6195558395927207584, 1.734028948791266345 ) ) ;
#68843=CARTESIAN_POINT ( 'NONE',  ( 4.083748955185668272, -1.721791984697383482, -0.2523947965055831633 ) ) ;
#68848=CARTESIAN_POINT ( 'NONE',  ( 2.360439101503517101, 0.9236781337260314695, 1.954550705658316456 ) ) ;
#68849=CARTESIAN_POINT ( 'NONE',  ( 3.479842141819572632, 1.821463063354014533, 0.8645922719773959653 ) ) ;
#68851=CARTESIAN_POINT ( 'NONE',  ( 1.762795743007524063, -1.528684080660724920, 1.528680807790387286 ) ) ;
#68852=CARTESIAN_POINT ( 'NONE',  ( 3.784019197727214401, -0.9729451851334305346, 1.714598810357757630 ) ) ;
#68853=CARTESIAN_POINT ( 'NONE',  ( 6.608999999999983999, 4.692729314731947099, 2.662616042240486536 ) ) ;
#68854=CARTESIAN_POINT ( 'NONE',  ( 3.438947998021203656, -1.472602994093423545, -1.266235326041851961 ) ) ;
#68857=ORIENTED_EDGE ( 'NONE', *, *, #134927, .F. ) ;
#68859=CARTESIAN_POINT ( 'NONE',  ( -0.1108833634136767443, 0.0002062650063822807356, -1.896853557917008271 ) ) ;
#68864=CARTESIAN_POINT ( 'NONE',  ( 6.704155097142892927, -2.307279366673311127, 0.04705588035085367382 ) ) ;
#68866=CARTESIAN_POINT ( 'NONE',  ( 4.364078322825436729, -1.956782558839207375, 0.1401112987177987601 ) ) ;
#68868=CARTESIAN_POINT ( 'NONE',  ( 2.180314765559120183, 1.560501322096979449, 1.277041908422072991 ) ) ;
#68870=CARTESIAN_POINT ( 'NONE',  ( 3.292305547686771305, -0.8622227623886582482, -1.934024985413025810 ) ) ;
#68874=CARTESIAN_POINT ( 'NONE',  ( 3.046634964419430158, -1.505538468004435027, -1.059505732788845966 ) ) ;
#68878=CARTESIAN_POINT ( 'NONE',  ( 5.150683391976684788, 2.089615912265533559, 0.3601871064465370087 ) ) ;
#68880=CARTESIAN_POINT ( 'NONE',  ( 5.466112512051848782, 1.011855222795062348, 1.795159749414678929 ) ) ;
#68882=CARTESIAN_POINT ( 'NONE',  ( 0.3439184179485414439, -0.8825062887024995861, 1.638522830676287789 ) ) ;
#68883=CARTESIAN_POINT ( 'NONE',  ( 3.069684041021227827, -1.094477399149307306, 1.480508570315848482 ) ) ;
#68888=CARTESIAN_POINT ( 'NONE',  ( 2.526237079854487089, -1.271617311931704686, -1.803507373242494438 ) ) ;
#68889=CARTESIAN_POINT ( 'NONE',  ( 4.815850035042070765, -2.220064692501269477, 0.4349022163744782343 ) ) ;
#68891=CARTESIAN_POINT ( 'NONE',  ( 4.763805435907580765, 0.5614848394812530508, -1.722472548925155778 ) ) ;
#68892=CARTESIAN_POINT ( 'NONE',  ( 4.663251631000405517, 1.785207739607551414, -0.6954431434487169383 ) ) ;
#68894=CARTESIAN_POINT ( 'NONE',  ( 3.959811223838666905, 1.956698650606549350, -0.2402693447622703815 ) ) ;
#68895=CARTESIAN_POINT ( 'NONE',  ( 5.102362337376947998, -0.6309395149336484154, -1.761181640970375106 ) ) ;
#68897=CARTESIAN_POINT ( 'NONE',  ( 5.142936340713559318, -0.2273772366201456396, -1.847015746109672119 ) ) ;
#68899=CARTESIAN_POINT ( 'NONE',  ( 0.4093891192313535710, -1.913260280790154866, 0.6371585790938688598 ) ) ;
#68901=CARTESIAN_POINT ( 'NONE',  ( 1.190214010286832602, -0.9452824899213798648, 1.882083610947625107 ) ) ;
#68905=CARTESIAN_POINT ( 'NONE',  ( 3.498385214435925317, -1.041973313016024472, 1.846846941210858351 ) ) ;
#68907=CARTESIAN_POINT ( 'NONE',  ( 1.353777543752776591, -1.465856132443652760, -1.389804628120022478 ) ) ;
#68912=CARTESIAN_POINT ( 'NONE',  ( 2.337400524717429207, -1.931973293601353392, 0.9696072025056484689 ) ) ;
#68920=CARTESIAN_POINT ( 'NONE',  ( 0.7850416839378616674, 1.930235501049954339, -1.037882601892345713 ) ) ;
#68922=CARTESIAN_POINT ( 'NONE',  ( 1.885968558009487595, 1.560753693757486849, 1.638220756346415508 ) ) ;
#68930=CARTESIAN_POINT ( 'NONE',  ( 3.984733165684080092, -0.1715787546078418324, -1.716317334075837975 ) ) ;
#68932=CARTESIAN_POINT ( 'NONE',  ( 2.108344674345350445, 1.315072395666099236, -1.184512757523252358 ) ) ;
#68933=CARTESIAN_POINT ( 'NONE',  ( 5.631908123138919642, -1.395923778694251105, -1.709176034821748624 ) ) ;
#68936=CARTESIAN_POINT ( 'NONE',  ( 4.324476463189423470, -0.8673186339709404447, -1.824254535609586725 ) ) ;
#68938=CARTESIAN_POINT ( 'NONE',  ( 4.446888776373093322, -1.802426293348384334, -0.9040943451460029534 ) ) ;
#68940=STYLED_ITEM ( 'NONE', ( #459 ), #158894 ) ;
#68941=CARTESIAN_POINT ( 'NONE',  ( 2.535844406030359544, 0.8837261853790435717, -1.648756255988912178 ) ) ;
#68943=CARTESIAN_POINT ( 'NONE',  ( 1.705181254219298115, 1.662258477346746588, -0.9455041445245655485 ) ) ;
#68948=CARTESIAN_POINT ( 'NONE',  ( -0.1933232215488022709, -0.4202133615931051835, -1.872389726556406897 ) ) ;
#68951=CARTESIAN_POINT ( 'NONE',  ( 1.978885927095444863, 1.829411362569667743, 0.7090815385668995940 ) ) ;
#68954=CARTESIAN_POINT ( 'NONE',  ( 5.238584497427841491, 1.261362679698872169, -1.704546977916908457 ) ) ;
#68957=CARTESIAN_POINT ( 'NONE',  ( 5.835224730271552751, -1.783237572924928127, 0.8406590917669158891 ) ) ;
#68960=CARTESIAN_POINT ( 'NONE',  ( 0.3166526355253923009, -0.6820779544549429030, -1.894243553402875202 ) ) ;
#68962=CARTESIAN_POINT ( 'NONE',  ( 1.458780272697857594, -2.011719176664223951, -0.6602987507247930488 ) ) ;
#68965=CARTESIAN_POINT ( 'NONE',  ( 3.104029480343179603, 0.7476448069429382226, -1.930825944200013966 ) ) ;
#68969=CARTESIAN_POINT ( 'NONE',  ( 4.505862177948306346, -0.8935697331868618365, -1.890194782795044492 ) ) ;
#68971=CARTESIAN_POINT ( 'NONE',  ( 2.907047201455060570, 1.541221212934189344, 0.9781624729086122461 ) ) ;
#68972=CARTESIAN_POINT ( 'NONE',  ( 2.947712979364258690, -1.218347856841961452, -1.340696891046004868 ) ) ;
#68977=CARTESIAN_POINT ( 'NONE',  ( 5.842855468016632692, 0.4250294216477692455, 2.165293060021292515 ) ) ;
#68980=CARTESIAN_POINT ( 'NONE',  ( 4.354103434560454566, 0.8146061972254794448, -1.730223316255767196 ) ) ;
#68984=CARTESIAN_POINT ( 'NONE',  ( 6.215297738502283842, -1.773692237561547147, -1.067698627785176768 ) ) ;
#68992=CARTESIAN_POINT ( 'NONE',  ( 3.110468855859845672, 1.357358932127524120, -1.287316363804760888 ) ) ;
#68997=CARTESIAN_POINT ( 'NONE',  ( -0.1757481403069499348, -0.8193859263425256056, -1.726394157293544840 ) ) ;
#68999=CARTESIAN_POINT ( 'NONE',  ( 6.912946559606852226, -1.604190412254998810, 1.308348183162249434 ) ) ;
#69000=CARTESIAN_POINT ( 'NONE',  ( 1.669546221992053603, 1.392560760841387246, 1.458543886677300394 ) ) ;
#69004=CARTESIAN_POINT ( 'NONE',  ( 1.763894328224338448, 1.128481436294457740, 1.878420861880884862 ) ) ;
#69005=CARTESIAN_POINT ( 'NONE',  ( 6.639283661800273961, -1.628176093627232479, 0.8261057939347239421 ) ) ;
#69012=CARTESIAN_POINT ( 'NONE',  ( 3.368544699895597461, 0.04196216268675251326, -1.840931771443871101 ) ) ;
#69013=CARTESIAN_POINT ( 'NONE',  ( 0.1354021741525688050, -0.09674683032310191222, 2.010873914455484801 ) ) ;
#69014=CARTESIAN_POINT ( 'NONE',  ( 2.284880952019330280, -2.229702823797473865, 0.5573334316414603196 ) ) ;
#69016=CARTESIAN_POINT ( 'NONE',  ( 0.7075644152179439983, 0.5912319408809820764, -1.764584214936999684 ) ) ;
#69020=CARTESIAN_POINT ( 'NONE',  ( 4.465046277278037934, -1.532637281380120564, 1.143568071694904598 ) ) ;
#69024=CARTESIAN_POINT ( 'NONE',  ( 3.439088004391201991, -1.584594249056283877, -1.364047514679037620 ) ) ;
#69025=CARTESIAN_POINT ( 'NONE',  ( 1.815107966846595255, -0.2319292346777863389, 1.856160199827073587 ) ) ;
#69028=CARTESIAN_POINT ( 'NONE',  ( 3.438731153704393417, -1.320290108414169605, -1.134124902983554062 ) ) ;
#69032=CARTESIAN_POINT ( 'NONE',  ( 3.826516835200497457, 1.638561065401537897, 0.5390252620694930830 ) ) ;
#69034=CARTESIAN_POINT ( 'NONE',  ( 3.597391730528697540, -0.6346259394694170330, 2.097678010650514402 ) ) ;
#69035=CARTESIAN_POINT ( 'NONE',  ( 6.375609195709820654, 2.113139023092651225, -0.6363509056886568205 ) ) ;
#69036=CARTESIAN_POINT ( 'NONE',  ( 4.083024739667787451, 2.059781850948108506, 0.6862965400120830672 ) ) ;
#69037=CARTESIAN_POINT ( 'NONE',  ( 1.910518402784128433, 1.353611321597010253, -1.225282022559864625 ) ) ;
#69039=CARTESIAN_POINT ( 'NONE',  ( 5.770749444886737578, -0.3132382886438951908, -2.093953712743265694 ) ) ;
#69041=CARTESIAN_POINT ( 'NONE',  ( 6.427265082780700745, -1.493544900618107185, -1.739104490089713462 ) ) ;
#69043=CARTESIAN_POINT ( 'NONE',  ( 6.720655732516646275, 4.698042323276835575, 2.488944259588221186 ) ) ;
#69045=CARTESIAN_POINT ( 'NONE',  ( 1.401209248766785542, -0.3145075555085960484, -2.096923750572597722 ) ) ;
#69050=CARTESIAN_POINT ( 'NONE',  ( 6.883263157960358924, 7.052235917045241997, 2.651962373728885325 ) ) ;
#69053=CARTESIAN_POINT ( 'NONE',  ( 6.539686446881147752, -1.556848207870220602, 1.281141925495055123 ) ) ;
#69055=CARTESIAN_POINT ( 'NONE',  ( 4.856332268735650715, -2.061987677746464076, -0.05593471103338721467 ) ) ;
#69061=CARTESIAN_POINT ( 'NONE',  ( 0.7969595931820300239, 1.710167217185576183, 1.202247156440580556 ) ) ;
#69062=CARTESIAN_POINT ( 'NONE',  ( 4.588517629802620235, -0.5350896943857390564, 1.944070981013111155 ) ) ;
#69063=CARTESIAN_POINT ( 'NONE',  ( 4.300242120186610784, 1.420457692841030850, -1.171515996850613694 ) ) ;
#69066=CARTESIAN_POINT ( 'NONE',  ( 0.4633286609967076086, 1.707074611214503435, -0.2455724507211871910 ) ) ;
#69067=CARTESIAN_POINT ( 'NONE',  ( 0.2511858651975951151, 0.1928294586405615574, -2.007256720055437871 ) ) ;
#69068=CARTESIAN_POINT ( 'NONE',  ( 1.003029240585759263, -2.241230121681879073, 0.5102270476868026039 ) ) ;
#69070=CARTESIAN_POINT ( 'NONE',  ( 1.757462551082995095, -1.940025152074912551, -1.163771565304895450 ) ) ;
#69071=CARTESIAN_POINT ( 'NONE',  ( 2.754625382576633807, 0.7102545713932090221, 1.982823988820613170 ) ) ;
#69075=FILL_AREA_STYLE_COLOUR ( '', #48610 ) ;
#69080=CARTESIAN_POINT ( 'NONE',  ( 4.781579470667713494, 0.2167243770262658464, -2.210780252931910717 ) ) ;
#69081=CARTESIAN_POINT ( 'NONE',  ( 2.783357461837578484, 1.550338952211056220, 1.549093164327268068 ) ) ;
#69084=CARTESIAN_POINT ( 'NONE',  ( 5.617619635959271385, 0.3843197845415853853, -1.923678648292715732 ) ) ;
#69086=CARTESIAN_POINT ( 'NONE',  ( 6.890000000000015667, 0.5768591945385994624, 2.052260346930290247 ) ) ;
#69088=CARTESIAN_POINT ( 'NONE',  ( 5.115537534566190203, 1.735013203181461350, 1.219038288318145646 ) ) ;
#69094=CARTESIAN_POINT ( 'NONE',  ( 5.407694413872749628, -0.8332299576223768378, -1.642021276980778932 ) ) ;
#69097=CARTESIAN_POINT ( 'NONE',  ( 0.8721245864499425071, -0.04093463707061052725, -1.740139661330299514 ) ) ;
#69103=CARTESIAN_POINT ( 'NONE',  ( 5.489210439962995736, 1.908424935776025455, -1.015307555102950010 ) ) ;
#69106=CARTESIAN_POINT ( 'NONE',  ( 4.153314892778156242, -1.795761387672462961, -1.203114871582221079 ) ) ;
#69108=CARTESIAN_POINT ( 'NONE',  ( 4.305907937463241630, -1.966273716216637046, 0.1420514027590073225 ) ) ;
#69109=CARTESIAN_POINT ( 'NONE',  ( 4.253097392439049607, -1.714905526014463666, -0.2545648513426115311 ) ) ;
#69110=CARTESIAN_POINT ( 'NONE',  ( 0.5916818631664167993, -0.7834642122952638621, 2.046923429677327100 ) ) ;
#69111=CARTESIAN_POINT ( 'NONE',  ( 2.116686800396328838, -1.088458544310743736, -2.034734824932447506 ) ) ;
#69112=CARTESIAN_POINT ( 'NONE',  ( 4.921196286130338216, -0.1051130969715245306, 2.058245376175421804 ) ) ;
#69113=CARTESIAN_POINT ( 'NONE',  ( 6.444875487053635332, -1.562622460104126310, -1.153009275138028089 ) ) ;
#69118=CARTESIAN_POINT ( 'NONE',  ( 0.9674229098759130618, -1.967888300253183953, -0.4390273639364171698 ) ) ;
#69120=CARTESIAN_POINT ( 'NONE',  ( 3.786314268594536347, -1.089870966172037825, 1.918795532666245363 ) ) ;
#69122=CARTESIAN_POINT ( 'NONE',  ( 0.6548463511123479019, 1.551493821935068906, -1.027296181188163571 ) ) ;
#69124=CARTESIAN_POINT ( 'NONE',  ( 6.539320575229249144, 0.007148032025052972194, 1.896977914940492393 ) ) ;
#69127=CARTESIAN_POINT ( 'NONE',  ( 6.925078400183550364, 3.684205305355064297, 2.658256427561227486 ) ) ;
#69130=CARTESIAN_POINT ( 'NONE',  ( 3.538010501442095723, 0.9279861380482921085, -1.840221436749614803 ) ) ;
#69133=CARTESIAN_POINT ( 'NONE',  ( 2.051431352050979040, -1.803145959232739237, 0.9099833227969624794 ) ) ;
#69136=CARTESIAN_POINT ( 'NONE',  ( 1.674756777405971064, -1.956562173829911044, -0.6475767382677873885 ) ) ;
#69141=CARTESIAN_POINT ( 'NONE',  ( -0.1411974294642098227, 4.091293698307607585, -2.455098582995118406 ) ) ;
#69143=CARTESIAN_POINT ( 'NONE',  ( 5.408869034151480903, 1.673104959687292448, -1.439203791633147267 ) ) ;
#69144=CARTESIAN_POINT ( 'NONE',  ( 1.370646902836635261, -1.372427557409527488, 1.669970663979184256 ) ) ;
#69146=CARTESIAN_POINT ( 'NONE',  ( 0.5324358445358172709, 0.5899921999869184308, 1.928256190492839028 ) ) ;
#69147=CARTESIAN_POINT ( 'NONE',  ( 2.161834534229470695, -0.6120774379556602751, -2.215351195248612459 ) ) ;
#69151=CARTESIAN_POINT ( 'NONE',  ( 1.885419139999934934, 1.287927767047767125, 1.356919574424742203 ) ) ;
#69152=CARTESIAN_POINT ( 'NONE',  ( 4.012907874177486178, 0.1037781579101039742, 2.014008197856680393 ) ) ;
#69157=CARTESIAN_POINT ( 'NONE',  ( 4.828798294617491216, 2.015104956129540881, 0.6122756557535751210 ) ) ;
#69161=CARTESIAN_POINT ( 'NONE',  ( 5.414321571020942692, -2.019972751022606872, 0.004158903309840755735 ) ) ;
#69163=CARTESIAN_POINT ( 'NONE',  ( 0.8661725458788569476, -2.052963606700756394, 0.1985000389403013821 ) ) ;
#69171=CARTESIAN_POINT ( 'NONE',  ( 3.332658328316660423, -1.295540365661397297, 1.742140367482351238 ) ) ;
#69174=CARTESIAN_POINT ( 'NONE',  ( 1.540310226958538475, -1.555040833713853710, 0.9856339240054690087 ) ) ;
#69176=CARTESIAN_POINT ( 'NONE',  ( 4.335597073515660149, 0.9364531651635084053, -1.981528385891350386 ) ) ;
#69177=CARTESIAN_POINT ( 'NONE',  ( 6.983263157960391432, 4.691677264508577139, 2.616375093613742209 ) ) ;
#69178=CARTESIAN_POINT ( 'NONE',  ( 5.278307949308306490, -1.261584246701217715, 1.877956315871305071 ) ) ;
#69185=CARTESIAN_POINT ( 'NONE',  ( 5.887929786387328335, -0.7941975946151798027, 1.581623468068603433 ) ) ;
#69186=CARTESIAN_POINT ( 'NONE',  ( 3.211590615979207364, 1.588433223196554778, 1.236618793847492626 ) ) ;
#69188=CARTESIAN_POINT ( 'NONE',  ( 2.098786246049421766, -0.5609894644466472124, -2.029802036486601846 ) ) ;
#69191=CARTESIAN_POINT ( 'NONE',  ( 2.101947443238092017, 0.7566099462053441638, -1.818632640566263614 ) ) ;
#69193=CARTESIAN_POINT ( 'NONE',  ( 0.4319881149899909567, 1.126445828788334991, 1.606065282034954578 ) ) ;
#69194=CARTESIAN_POINT ( 'NONE',  ( 6.152603492317154199, 1.793228361101945056, 0.2563216274220745938 ) ) ;
#69199=CARTESIAN_POINT ( 'NONE',  ( 6.297708355432167338, -0.6282832542035889922, 1.762108908958268216 ) ) ;
#69202=CARTESIAN_POINT ( 'NONE',  ( 5.612195314557796522, 2.068136773602911038, -0.09592777784667855245 ) ) ;
#69213=CARTESIAN_POINT ( 'NONE',  ( 4.967221142815226642, 1.706001049663580460, 0.9686458024478412643 ) ) ;
#69215=CARTESIAN_POINT ( 'NONE',  ( 3.427111092251767133, 0.9039706872599994059, 1.802141633730186543 ) ) ;
#69216=CARTESIAN_POINT ( 'NONE',  ( 2.430754934859931549, -1.590173441703069956, 1.067998681346548961 ) ) ;
#69218=CARTESIAN_POINT ( 'NONE',  ( 0.5213437761196969555, -2.079166062760181788, 0.6930039600180629700 ) ) ;
#69219=CARTESIAN_POINT ( 'NONE',  ( 0.1331715793776418189, 1.377430125279802686, -2.211494238769554865 ) ) ;
#69220=CARTESIAN_POINT ( 'NONE',  ( 3.321420150926617687, -1.803644938814071175, 0.4956094624995326381 ) ) ;
#69222=CARTESIAN_POINT ( 'NONE',  ( 4.218997895827368616, 1.553599190986540091, -1.280318274872578543 ) ) ;
#69225=CARTESIAN_POINT ( 'NONE',  ( 4.042653799040228257, -1.567611697763098055, 1.423267961261857950 ) ) ;
#69228=CARTESIAN_POINT ( 'NONE',  ( 5.582505937350194181, 1.236201877336528643, -1.660625051266072960 ) ) ;
#69229=CARTESIAN_POINT ( 'NONE',  ( 1.171554334673271303, 1.248344470866637135, 1.676987088486236566 ) ) ;
#69230=CARTESIAN_POINT ( 'NONE',  ( 6.720655732516649827, 2.940181725866806151, 2.725612257524675730 ) ) ;
#69231=CARTESIAN_POINT ( 'NONE',  ( 6.545924712158827319, 0.6954503440314525609, -1.688125835592364066 ) ) ;
#69239=CARTESIAN_POINT ( 'NONE',  ( 0.6799528615496954753, 0.8915946574989388473, 1.576789060086491778 ) ) ;
#69247=MECHANICAL_DESIGN_GEOMETRIC_PRESENTATION_REPRESENTATION('',(#131643),#103922);
#69248=CARTESIAN_POINT ( 'NONE',  ( 6.046499952770106212, -1.423952032562772807, 1.427948417171531759 ) ) ;
#69249=CARTESIAN_POINT ( 'NONE',  ( 0.3465379015402513252, 1.086389676674501148, -1.820904993421072371 ) ) ;
#69251=CARTESIAN_POINT ( 'NONE',  ( 0.1405533004714799583, 4.081756738537394291, -2.834601852798774413 ) ) ;
#69255=CARTESIAN_POINT ( 'NONE',  ( 3.274220328336883146, -0.9665011448860871823, -1.715865690870149285 ) ) ;
#69256=CARTESIAN_POINT ( 'NONE',  ( 4.991814629660241920, -2.006445540622634915, 0.2004526995145126111 ) ) ;
#69258=( NAMED_UNIT ( * ) SI_UNIT ( $, .STERADIAN. ) SOLID_ANGLE_UNIT ( ) );
#69260=CARTESIAN_POINT ( 'NONE',  ( 4.347736757272718577, 2.190986304709115373, -0.05254992341368477232 ) ) ;
#69262=CARTESIAN_POINT ( 'NONE',  ( 3.838824069632059910, 0.2817418319709265040, 1.905555271966542952 ) ) ;
#69264=CARTESIAN_POINT ( 'NONE',  ( -0.1296875068448125334, 2.048176110289974261, -2.243787855586779401 ) ) ;
#69265=CARTESIAN_POINT ( 'NONE',  ( 0.08304785351339466493, -2.141800023564765620, -0.5316218738360134477 ) ) ;
#69269=CARTESIAN_POINT ( 'NONE',  ( 5.330891317213126257, -1.853047821147445484, -0.6673286768130722857 ) ) ;
#69270=CARTESIAN_POINT ( 'NONE',  ( 0.6439600106935819968, 0.5648315236305987419, 1.858087668232853984 ) ) ;
#69271=CARTESIAN_POINT ( 'NONE',  ( 3.914701103513482661, -0.6334807629873323576, -1.910874176753782461 ) ) ;
#69272=CARTESIAN_POINT ( 'NONE',  ( 5.993622264137510314, 2.212772176713458716, 0.6212890515704305727 ) ) ;
#69274=CARTESIAN_POINT ( 'NONE',  ( 4.873795578896718439, -1.825537460381383870, 0.3603196638213671532 ) ) ;
#69280=CARTESIAN_POINT ( 'NONE',  ( 0.8729168595149154886, -0.05911722906676297740, -2.190938979806676734 ) ) ;
#69285=CARTESIAN_POINT ( 'NONE',  ( 0.5569169099325711469, -1.540613122784354916, -0.9793164655157863274 ) ) ;
#69288=CARTESIAN_POINT ( 'NONE',  ( 3.041388834704723099, -1.310848641452688979, 1.135385315042459542 ) ) ;
#69292=CARTESIAN_POINT ( 'NONE',  ( 5.127504350819418910, -1.732488751877172772, 0.5760870007271366999 ) ) ;
#69293=CARTESIAN_POINT ( 'NONE',  ( 3.573055779259231457, 1.771592698278463107, 0.8429337356923997104 ) ) ;
#69297=CARTESIAN_POINT ( 'NONE',  ( 4.951869195850400196, -1.499954228463634465, -1.499123153458590929 ) ) ;
#69300=CARTESIAN_POINT ( 'NONE',  ( 2.782155020660907141, -1.188329515115684076, -1.695063343828225877 ) ) ;
#69304=CARTESIAN_POINT ( 'NONE',  ( 4.371885135981863790, 0.4866971690204218159, -2.167184880714991824 ) ) ;
#69306=CARTESIAN_POINT ( 'NONE',  ( 2.356409458221408126, 0.1091249688820790792, -2.296199191736052025 ) ) ;
#69314=CARTESIAN_POINT ( 'NONE',  ( 3.111475685156277038, 1.510342251817019532, 1.173009309769344588 ) ) ;
#69316=CARTESIAN_POINT ( 'NONE',  ( 4.524228514566789983, 1.059873738895898310, -1.360581713153318884 ) ) ;
#69317=CARTESIAN_POINT ( 'NONE',  ( 2.923064838257955156, -1.776166165677966591, 0.9548571111624851726 ) ) ;
#69318=CARTESIAN_POINT ( 'NONE',  ( 4.535913861531776448, -1.846855032230051208, 1.368429651993019025 ) ) ;
#69320=CARTESIAN_POINT ( 'NONE',  ( 6.287733905706966553, 1.451067878312240822, 1.526644127000365003 ) ) ;
#69323=CARTESIAN_POINT ( 'NONE',  ( 5.272599804957129876, -1.666481374185318609, -0.5959551625853221068 ) ) ;
#69325=CARTESIAN_POINT ( 'NONE',  ( 1.359778343217881602, 2.257671611795939004, -0.3959128255837316979 ) ) ;
#69326=CARTESIAN_POINT ( 'NONE',  ( 0.4271921415617612183, 0.8987490902026186168, -1.490136572063437637 ) ) ;
#69328=CARTESIAN_POINT ( 'NONE',  ( 6.509741685903361663, -1.029359178063901092, -1.934661654277470166 ) ) ;
#69332=CARTESIAN_POINT ( 'NONE',  ( 0.3621003815536598669, -0.5783089063249653439, 2.092656953901766315 ) ) ;
#69333=CARTESIAN_POINT ( 'NONE',  ( 1.042204282965590201, 0.8216761606248854655, 1.841732292558920570 ) ) ;
#69335=CARTESIAN_POINT ( 'NONE',  ( 5.320897925068237555, 1.780805307305334040, 0.7354040419824976471 ) ) ;
#69337=CARTESIAN_POINT ( 'NONE',  ( 1.301376502765494658, -0.3325571857498362260, -2.196291469625763160 ) ) ;
#69346=CARTESIAN_POINT ( 'NONE',  ( 4.124340800031966126, 0.09048578169197672716, 1.738227929847275588 ) ) ;
#69347=CARTESIAN_POINT ( 'NONE',  ( 2.242563829109287088, -1.923402688547710904, -0.3857071251459272543 ) ) ;
#69353=CARTESIAN_POINT ( 'NONE',  ( 6.777797683793751915, -1.903277019102869616, 0.4755351429900215310 ) ) ;
#69357=CARTESIAN_POINT ( 'NONE',  ( 5.137907791644652278, 2.014008302827663854, -0.1037760698975112861 ) ) ;
#69358=CARTESIAN_POINT ( 'NONE',  ( 1.112636518468415270, -1.019398372879092962, -2.019907345245135932 ) ) ;
#69362=CARTESIAN_POINT ( 'NONE',  ( 1.510794437334112672, 1.647127454408814362, 0.8865631655482277829 ) ) ;
#69363=CARTESIAN_POINT ( 'NONE',  ( 0.6856605700745866949, 1.416429869936095542, 1.000165270844357801 ) ) ;
#69364=CARTESIAN_POINT ( 'NONE',  ( 4.564136437409766600, -1.431273618155091576, 1.659743667367798103 ) ) ;
#69365=CARTESIAN_POINT ( 'NONE',  ( 5.087122877145462851, -0.2765918260761930925, -2.290891016797763413 ) ) ;
#69366=CARTESIAN_POINT ( 'NONE',  ( 0.8485939591743509869, 0.5976917523492016882, 1.972322469454860672 ) ) ;
#69367=CARTESIAN_POINT ( 'NONE',  ( 3.292849172082324305, 1.531446531863265736, 1.193990500783614905 ) ) ;
#69370=CARTESIAN_POINT ( 'NONE',  ( 5.448468942325162878, 0.5420331153751513087, 1.790312535500695024 ) ) ;
#69372=CARTESIAN_POINT ( 'NONE',  ( 0.3855818064394588851, -0.09363725165581829324, 1.731465614217362559 ) ) ;
#69375=CARTESIAN_POINT ( 'NONE',  ( 5.098279808040273586, -0.2930726886911338425, 1.994869512123042199 ) ) ;
#69378=CARTESIAN_POINT ( 'NONE',  ( 2.033574986395149775, -1.191784744093337123, -1.383114941912518159 ) ) ;
#69387=CARTESIAN_POINT ( 'NONE',  ( 6.059241617823571957, -1.705078594313869988, 1.082191098076368929 ) ) ;
#69388=CARTESIAN_POINT ( 'NONE',  ( 0.03014954708456181465, -2.078685333231004684, 0.4181070283913386199 ) ) ;
#69393=CARTESIAN_POINT ( 'NONE',  ( 4.926665654204026801, 1.971471998011574467, 0.6004258549221918040 ) ) ;
#69394=CARTESIAN_POINT ( 'NONE',  ( 5.414685466650038137, -1.281359335986744341, -1.556910257834144051 ) ) ;
#69402=CARTESIAN_POINT ( 'NONE',  ( 4.886092203009785528, -0.1017338195800701617, 2.013677658187912556 ) ) ;
#69403=CARTESIAN_POINT ( 'NONE',  ( 3.802549092506895878, 1.579937072410386278, 0.9450539169142122553 ) ) ;
#69406=CARTESIAN_POINT ( 'NONE',  ( 1.700300771062040361, -0.7742048122164610913, 2.174079040713126076 ) ) ;
#69408=CARTESIAN_POINT ( 'NONE',  ( 4.429101881081805914, 0.1011787780425543737, 2.159334005894457231 ) ) ;
#69410=CARTESIAN_POINT ( 'NONE',  ( 0.04629046987890492182, -1.559278246393133838, 1.157480633202745635 ) ) ;
#69413=CARTESIAN_POINT ( 'NONE',  ( 4.007374829128952598, 2.286843722993581185, 0.2302655642077624243 ) ) ;
#69415=CARTESIAN_POINT ( 'NONE',  ( 3.502682687546424312, 1.475339254275360279, -1.149998991230333223 ) ) ;
#69416=CARTESIAN_POINT ( 'NONE',  ( 0.1808907491311480820, -0.1332662104699660066, -1.940345832946618554 ) ) ;
#69420=CARTESIAN_POINT ( 'NONE',  ( 2.245003380770736801, 0.4850519687749441644, 2.152760086278446394 ) ) ;
#69422=CARTESIAN_POINT ( 'NONE',  ( 6.620655732516651071, -0.002413161512292844035, 2.173887093218453082 ) ) ;
#69426=CARTESIAN_POINT ( 'NONE',  ( 1.053909416342192484, 1.969286043147522980, -0.09259992539933233069 ) ) ;
#69428=CARTESIAN_POINT ( 'NONE',  ( 0.5171989335802311682, 1.588149187230869952, -1.674348222103681172 ) ) ;
#69429=CARTESIAN_POINT ( 'NONE',  ( 0.6077679335219284829, 0.6189715888181289705, -1.861716921216026055 ) ) ;
#69430=CARTESIAN_POINT ( 'NONE',  ( 3.871981579112850458, -2.032873796296597479, 0.3478246332576060973 ) ) ;
#69437=CARTESIAN_POINT ( 'NONE',  ( 6.760228240101231023, -2.170840268647770799, 0.04637219581851703687 ) ) ;
#69439=CARTESIAN_POINT ( 'NONE',  ( 5.267088776126935379, 1.772936381825638952, -0.4966186330585887210 ) ) ;
#69446=CARTESIAN_POINT ( 'NONE',  ( 0.9086806230526077721, -0.4651930584498394916, -1.854694524013176693 ) ) ;
#69448=( GEOMETRIC_REPRESENTATION_CONTEXT ( 3 ) GLOBAL_UNCERTAINTY_ASSIGNED_CONTEXT ( ( #67662 ) ) GLOBAL_UNIT_ASSIGNED_CONTEXT ( ( #86424, #70142, #158893 ) ) REPRESENTATION_CONTEXT ( 'NONE', 'WORKASPACE' ) );
#69449=CARTESIAN_POINT ( 'NONE',  ( 3.572906242625200068, 0.04398576871290219709, -1.769473305487194281 ) ) ;
#69450=CARTESIAN_POINT ( 'NONE',  ( 5.918613486546395741, -0.7266362437793117968, -1.877539736040201079 ) ) ;
#69452=CARTESIAN_POINT ( 'NONE',  ( 4.675340500466128368, 1.422229311605049507, 1.283493733622777189 ) ) ;
#69455=CARTESIAN_POINT ( 'NONE',  ( 5.353942763280384654, -0.7107094859252837127, 1.837027094894280399 ) ) ;
#69456=CARTESIAN_POINT ( 'NONE',  ( 1.037531286769650452, -0.04638328994046451298, 2.120250110247793085 ) ) ;
#69458=CARTESIAN_POINT ( 'NONE',  ( 3.906994808788874174, 1.604092888448312326, 0.9621832354540849064 ) ) ;
#69459=CARTESIAN_POINT ( 'NONE',  ( 6.498688201949993193, -0.4681372660274349951, -1.660085793416385513 ) ) ;
#69461=CARTESIAN_POINT ( 'NONE',  ( 3.826972293661185187, 2.095320012007126476, 0.6930106488920934060 ) ) ;
#69464=CARTESIAN_POINT ( 'NONE',  ( 1.117717378214663881, 0.4042816502292169711, -2.022510655824232728 ) ) ;
#69471=CARTESIAN_POINT ( 'NONE',  ( 3.350112325975619587, -0.8415805752714689003, 1.891790567983504312 ) ) ;
#69475=CARTESIAN_POINT ( 'NONE',  ( 0.9967468350138152244, -1.970926226424707606, -0.4403189329902043037 ) ) ;
#69477=CARTESIAN_POINT ( 'NONE',  ( 0.07499057489264347731, 6.948553613792602057, -2.550573651218261517 ) ) ;
#69479=CARTESIAN_POINT ( 'NONE',  ( 6.204453847213379447, -1.458334814074750740, -1.392330997281837623 ) ) ;
#69480=CARTESIAN_POINT ( 'NONE',  ( 6.350803879971770982, -1.754615558991738267, -0.7693843322766678039 ) ) ;
#69481=CARTESIAN_POINT ( 'NONE',  ( 6.639320575229257670, 1.230867875982581738, 2.315960674347458781 ) ) ;
#69482=CARTESIAN_POINT ( 'NONE',  ( 4.001666433686186686, -2.185622478633037602, 0.1623105178310546570 ) ) ;
#69484=CARTESIAN_POINT ( 'NONE',  ( 3.375170810042011915, -1.688748480992762868, -0.8973671847329609541 ) ) ;
#69488=CARTESIAN_POINT ( 'NONE',  ( 1.353138909097661768, 0.1455122274086443901, -2.011206940682720212 ) ) ;
#69491=CARTESIAN_POINT ( 'NONE',  ( -0.1230140872038130023, -0.1644519934839226150, -2.256176000670232717 ) ) ;
#69493=CARTESIAN_POINT ( 'NONE',  ( 2.590480338954644246, -0.2921314510030656453, -1.699667543312991747 ) ) ;
#69495=CARTESIAN_POINT ( 'NONE',  ( 0.1394461523057137220, 5.725876337386284654, -2.313825101289856967 ) ) ;
#69499=CARTESIAN_POINT ( 'NONE',  ( 1.363640982571033611, -0.4799814350611387725, 1.902108589862220311 ) ) ;
#69502=CARTESIAN_POINT ( 'NONE',  ( 0.07556134207192373442, 6.947017789483680872, -2.839293120204011256 ) ) ;
#69506=CARTESIAN_POINT ( 'NONE',  ( 3.650846288169238729, 0.2690317868887618369, 1.791254203397556477 ) ) ;
#69509=CARTESIAN_POINT ( 'NONE',  ( 4.828658830049068484, 1.245459390374216380, -1.315641719143684885 ) ) ;
#69513=CARTESIAN_POINT ( 'NONE',  ( 4.738624546071780408, -1.804922690063763824, -0.4530168641722984169 ) ) ;
#69516=CARTESIAN_POINT ( 'NONE',  ( 2.970226572681373689, -1.887729772399210804, -0.3245638568863758455 ) ) ;
#69524=CARTESIAN_POINT ( 'NONE',  ( 0.3741789627117291239, 1.245922373857488274, 1.766349570875298758 ) ) ;
#69526=CARTESIAN_POINT ( 'NONE',  ( 1.957086829145736173, 0.3561595965777020756, -2.059905414565963433 ) ) ;
#69528=CARTESIAN_POINT ( 'NONE',  ( 0.6569167496461197908, -1.539450689919025450, -0.9809549629347169564 ) ) ;
#69530=CARTESIAN_POINT ( 'NONE',  ( 2.520284954824199453, 1.194270260598716771, -1.380820861806408617 ) ) ;
#69532=CARTESIAN_POINT ( 'NONE',  ( 2.214975196874233720, 1.533708969217022933, -1.142120075431733994 ) ) ;
#69533=CARTESIAN_POINT ( 'NONE',  ( 2.365619736264668038, -0.4344343780767513374, 1.920862584678226348 ) ) ;
#69534=CARTESIAN_POINT ( 'NONE',  ( 3.421366544187495418, -1.159031000169882475, -1.558129983894075865 ) ) ;
#69537=CARTESIAN_POINT ( 'NONE',  ( 4.605793411009856619, 1.573235607984494688, 1.422142093439874522 ) ) ;
#69544=CARTESIAN_POINT ( 'NONE',  ( 4.318856058802469811, 1.670182456744148336, 0.7377305746401884301 ) ) ;
#69548=CARTESIAN_POINT ( 'NONE',  ( 4.662891624058607576, -1.671085903211678270, -0.8408918736509605196 ) ) ;
#69550=CARTESIAN_POINT ( 'NONE',  ( 1.893070592381540740, 1.676246824859698892, -0.9494106994061870530 ) ) ;
#69551=CARTESIAN_POINT ( 'NONE',  ( 6.842638302680405182, -1.923265442670134551, -0.3857968560932593660 ) ) ;
#69552=MECHANICAL_DESIGN_GEOMETRIC_PRESENTATION_REPRESENTATION('',(#111090),#28150);
#69557=EDGE_CURVE ( 'NONE', #2638, #36822, #151308, .T. ) ;
#69559=CARTESIAN_POINT ( 'NONE',  ( 1.212693198809017270, 2.041623912717607237, 0.5605823208302792571 ) ) ;
#69562=CARTESIAN_POINT ( 'NONE',  ( 6.473496638176248652, -0.2593738453590052617, 2.053908440964563376 ) ) ;
#69563=CARTESIAN_POINT ( 'NONE',  ( 0.06366010765614799061, -1.203631707120488947, 1.393476991864414760 ) ) ;
#69565=CARTESIAN_POINT ( 'NONE',  ( 5.801499429514798578, 1.546190052965769057, -1.701143905309614679 ) ) ;
#69569=CARTESIAN_POINT ( 'NONE',  ( 1.482826411003408840, -0.3401602582979300626, -2.266773921731002339 ) ) ;
#69572=CARTESIAN_POINT ( 'NONE',  ( 5.859312505936116189, 1.912822604199882148, -0.3342364482464658115 ) ) ;
#69575=CARTESIAN_POINT ( 'NONE',  ( 1.177990849177086075, 1.982702329297232113, -0.3483419944294365300 ) ) ;
#69580=CARTESIAN_POINT ( 'NONE',  ( 2.501997717985538383, -0.8009308590465279432, -1.931334861377894008 ) ) ;
#69581=CARTESIAN_POINT ( 'NONE',  ( 1.059032582198644601, 0.3505281480379630610, -1.734596922625891713 ) ) ;
#69582=CARTESIAN_POINT ( 'NONE',  ( 6.504528880466823537, -1.955196382115764964, 0.4926337920100053447 ) ) ;
#69584=CARTESIAN_POINT ( 'NONE',  ( 4.646573614920027850, -1.842837963294202464, 1.363044294324888162 ) ) ;
#69585=CARTESIAN_POINT ( 'NONE',  ( 3.116877616926060135, -1.676954032530679761, 0.4650628940853319682 ) ) ;
#69588=CARTESIAN_POINT ( 'NONE',  ( 3.620171223323872756, 0.4232754169638303643, -1.681204106648684693 ) ) ;
#69590=CARTESIAN_POINT ( 'NONE',  ( 3.016274402391531773, 2.160936140102893255, -0.2104436154053441199 ) ) ;
#69592=CARTESIAN_POINT ( 'NONE',  ( 4.346888830327386266, -1.803415170841724979, -0.9023466997552240798 ) ) ;
#69593=CARTESIAN_POINT ( 'NONE',  ( 2.531250000000001332, -0.7852924748301189917, -1.895863743164030613 ) ) ;
#69597=CARTESIAN_POINT ( 'NONE',  ( 1.623919080003157545, -1.068017489352061533, -1.603033266432315918 ) ) ;
#69599=CARTESIAN_POINT ( 'NONE',  ( 4.412477314457364130, -2.220925182493800776, -0.05286738749475486387 ) ) ;
#69601=CARTESIAN_POINT ( 'NONE',  ( -0.1106856583841060310, -0.002128758811529348188, -1.996853503091333470 ) ) ;
#69607=CARTESIAN_POINT ( 'NONE',  ( 1.067367041543025197, -1.747990651676500029, 1.370551686305313321 ) ) ;
#69608=CARTESIAN_POINT ( 'NONE',  ( 6.338335788673861160, -1.050647824335379399, 1.656640365463659892 ) ) ;
#69611=CARTESIAN_POINT ( 'NONE',  ( 0.3862812426984676972, -1.019270635400490121, 1.906220128828392646 ) ) ;
#69614=CARTESIAN_POINT ( 'NONE',  ( 3.367685602802727551, -0.4050715705573506575, 2.022353529335896294 ) ) ;
#69618=CARTESIAN_POINT ( 'NONE',  ( 6.485618507650338316, 1.290063292742931633, 1.354747167150817333 ) ) ;
#69619=CARTESIAN_POINT ( 'NONE',  ( 5.168516884834092551, 1.170641038942145995, 1.279587065987584982 ) ) ;
#69620=CARTESIAN_POINT ( 'NONE',  ( 3.684860642351639903, 1.263529365103865709, 1.197186439443503003 ) ) ;
#69621=CARTESIAN_POINT ( 'NONE',  ( 1.699181366971340701, 1.908771516627869147, 1.269207382326368316 ) ) ;
#69623=CARTESIAN_POINT ( 'NONE',  ( 5.372635804747151411, -0.05242855794247149731, -2.090268718351683930 ) ) ;
#69624=CARTESIAN_POINT ( 'NONE',  ( -0.02377707250108065939, -0.1326659201078099481, -1.811169398030491928 ) ) ;
#69628=CARTESIAN_POINT ( 'NONE',  ( 1.986954140179174155, -2.015912935764123670, 0.05229865529512293942 ) ) ;
#69629=CARTESIAN_POINT ( 'NONE',  ( 0.5159075615763093481, -1.175655012515547160, -1.849222068403690411 ) ) ;
#69634=CARTESIAN_POINT ( 'NONE',  ( 2.983181628360128013, -1.960071735995170927, -0.8095406527153581333 ) ) ;
#69636=CARTESIAN_POINT ( 'NONE',  ( 5.022008369909983116, -0.9795521577263366364, -1.540466923627185292 ) ) ;
#69642=CARTESIAN_POINT ( 'NONE',  ( 1.986587785418312047, -1.239364722674634933, 1.594781737346209871 ) ) ;
#69643=CARTESIAN_POINT ( 'NONE',  ( 6.821333372217227797, -0.1664864972488830641, 2.170661319153658564 ) ) ;
#69645=CARTESIAN_POINT ( 'NONE',  ( 4.223391696059366929, 0.2311737859471388323, -1.846484453672825321 ) ) ;
#69652=CARTESIAN_POINT ( 'NONE',  ( 5.180226163740526246, -1.011166736308216629, 1.519887457628710248 ) ) ;
#69656=CARTESIAN_POINT ( 'NONE',  ( 1.334805274328724867, -1.105471761691357191, 1.335692278477951689 ) ) ;
#69657=CARTESIAN_POINT ( 'NONE',  ( 6.492148756324659153, -0.4961259030743305209, -1.772972609911625419 ) ) ;
#69658=CARTESIAN_POINT ( 'NONE',  ( 5.391387774523593635, 2.037479383949382772, -1.083606018200606869 ) ) ;
#69661=CARTESIAN_POINT ( 'NONE',  ( 1.352885421680804834, -1.626251134426279332, 1.265669239494594311 ) ) ;
#69663=CARTESIAN_POINT ( 'NONE',  ( 6.802148291397191571, -2.057678525504004430, 1.024270743344313672 ) ) ;
#69667=CARTESIAN_POINT ( 'NONE',  ( 0.1453086613420169204, -1.522338971917249317, -1.252298935284136938 ) ) ;
#69668=CARTESIAN_POINT ( 'NONE',  ( 3.972844611716894736, -1.413603510852480927, 1.288168406687495215 ) ) ;
#69671=CARTESIAN_POINT ( 'NONE',  ( 5.145248760827346501, -1.894204247122273088, 1.132176536499051700 ) ) ;
#69676=CARTESIAN_POINT ( 'NONE',  ( 5.514351353798126354, -2.120667953778174741, 0.0001357579994532010219 ) ) ;
#69679=CARTESIAN_POINT ( 'NONE',  ( 3.470030448073280205, 2.251904571161921442, -0.5032320387977330389 ) ) ;
#69680=CARTESIAN_POINT ( 'NONE',  ( 4.281663391851794565, -1.878042059144067633, 0.5673916069991248312 ) ) ;
#69681=CARTESIAN_POINT ( 'NONE',  ( 1.182386158793121256, 1.172985831986381955, -1.572276950389992933 ) ) ;
#69684=ORIENTED_EDGE ( 'NONE', *, *, #37494, .T. ) ;
#69685=CARTESIAN_POINT ( 'NONE',  ( 5.225796113160614986, 0.8128206588041908542, -1.845625551132886288 ) ) ;
#69688=CARTESIAN_POINT ( 'NONE',  ( 3.239314478175295164, -0.1551929672521153158, -2.165549275587749456 ) ) ;
#69690=CARTESIAN_POINT ( 'NONE',  ( 0.8969213510382867405, -2.070190491330957006, -0.4589741369691033857 ) ) ;
#69696=CARTESIAN_POINT ( 'NONE',  ( 2.214203678495901606, -0.9685002052983943122, -1.818986401426671229 ) ) ;
#69703=CARTESIAN_POINT ( 'NONE',  ( 5.057238878282278804, -1.638088962530854786, 0.9864336689310859718 ) ) ;
#69706=CARTESIAN_POINT ( 'NONE',  ( -0.03528172390533482194, -1.455059732361897895, 1.078909735853793794 ) ) ;
#69708=CARTESIAN_POINT ( 'NONE',  ( 1.024461926017742996, 0.3770999164835596162, 1.878046770817816791 ) ) ;
#69709=CARTESIAN_POINT ( 'NONE',  ( 2.383334800519558705, -0.002349189141126820958, 2.070544812199434315 ) ) ;
#69712=CARTESIAN_POINT ( 'NONE',  ( 0.5320225927652595388, 1.015637564890453426, -1.689598002260852772 ) ) ;
#69713=CARTESIAN_POINT ( 'NONE',  ( 3.158640206316553289, -1.382037546686708973, 1.193037399656725395 ) ) ;
#69714=CARTESIAN_POINT ( 'NONE',  ( 6.340462157465731607, 2.182225300935904055, 0.3281612982340698093 ) ) ;
#69717=CARTESIAN_POINT ( 'NONE',  ( 3.648931631147700472, -0.3995851234466942792, -2.023444851274053491 ) ) ;
#69722=CARTESIAN_POINT ( 'NONE',  ( 4.981522283868931034, 1.966010104637575751, -0.7553895412903822715 ) ) ;
#69724=CARTESIAN_POINT ( 'NONE',  ( 0.1687529456618936941, -0.9278834597439933329, -1.960587321289827267 ) ) ;
#69726=CARTESIAN_POINT ( 'NONE',  ( 5.431013727915853906, 0.1530101862373678123, 2.156222312673663488 ) ) ;
#69727=CARTESIAN_POINT ( 'NONE',  ( 4.266274442087925500, 2.019191850312745284, -0.05169103710895606163 ) ) ;
#69728=CARTESIAN_POINT ( 'NONE',  ( 6.620655732516645742, 7.051964633898824886, 2.771890290588132189 ) ) ;
#69733=CARTESIAN_POINT ( 'NONE',  ( 2.307827663788959871, -1.164988201124015577, -1.645758576239789051 ) ) ;
#69738=CARTESIAN_POINT ( 'NONE',  ( 6.720655732516659597, 0.5653683226944251627, 2.225905711026022971 ) ) ;
#69740=CARTESIAN_POINT ( 'NONE',  ( 4.780875152847498200, 1.674876996157638187, -1.122516304564516565 ) ) ;
#69742=CARTESIAN_POINT ( 'NONE',  ( 0.4863796390984359008, -0.2058623683223875511, -1.712490539465325146 ) ) ;
#69747=CARTESIAN_POINT ( 'NONE',  ( 5.571519856497625156, 1.802974293077023393, -0.4980454429602265698 ) ) ;
#69748=CARTESIAN_POINT ( 'NONE',  ( 6.240495565780414644, 1.155569484861172391, -1.648366056897664800 ) ) ;
#69755=CARTESIAN_POINT ( 'NONE',  ( 0.1050925082292548940, -0.09611335402343046397, 2.014234898253919326 ) ) ;
#69756=CARTESIAN_POINT ( 'NONE',  ( 1.423755586445039745, -1.797672382977614669, 0.2236433623570739382 ) ) ;
#69762=CARTESIAN_POINT ( 'NONE',  ( 0.2510146965912671835, 0.1847738873272772309, -1.906744464555621521 ) ) ;
#69767=ORIENTED_EDGE ( 'NONE', *, *, #83695, .T. ) ;
#69769=CARTESIAN_POINT ( 'NONE',  ( 4.329101982860062314, 0.1031891237209987822, 2.159356164053369387 ) ) ;
#69772=CARTESIAN_POINT ( 'NONE',  ( 0.3168469074051638579, -0.7203255543706194031, -1.994627023381766673 ) ) ;
#69773=CARTESIAN_POINT ( 'NONE',  ( 2.038291622189229546, 1.949329857042367387, 0.2932346777646984148 ) ) ;
#69774=CARTESIAN_POINT ( 'NONE',  ( 4.500206361630255003, -0.8965733778899236395, 1.689174240301967389 ) ) ;
#69777=CARTESIAN_POINT ( 'NONE',  ( 5.881302004902690506, -0.04997076178031189392, 1.969097942535046331 ) ) ;
#69778=CARTESIAN_POINT ( 'NONE',  ( 0.8845914429877841378, 1.712865214261191316, -0.9150308779080836841 ) ) ;
#69787=CARTESIAN_POINT ( 'NONE',  ( 0.4115098346569624477, 1.921242953230850148, 1.085561749797583797 ) ) ;
#69789=CARTESIAN_POINT ( 'NONE',  ( 0.1703706300211875746, 0.7318840393725855042, 1.766877091004593225 ) ) ;
#69790=CARTESIAN_POINT ( 'NONE',  ( -0.02338929933909209696, 6.948787603726593431, -2.306014233525994772 ) ) ;
#69793=CARTESIAN_POINT ( 'NONE',  ( 2.840353284027045344, -1.066491845456703835, 1.774417039089710935 ) ) ;
#69797=CARTESIAN_POINT ( 'NONE',  ( 0.09294085500742564621, -0.4768749645070144982, -2.116232079886640971 ) ) ;
#69798=CARTESIAN_POINT ( 'NONE',  ( 2.947022816757136621, -1.793111998972513277, -1.259777465452505796 ) ) ;
#69804=CARTESIAN_POINT ( 'NONE',  ( 5.818968308277153056, 0.8464176696867716787, -1.513466976307031642 ) ) ;
#69807=CARTESIAN_POINT ( 'NONE',  ( 3.168866831888625946, 1.502704456927813403, -1.424286459396295390 ) ) ;
#69808=CARTESIAN_POINT ( 'NONE',  ( 4.130539392780770314, 0.5663510459464686786, 2.039993263092474418 ) ) ;
#69811=CARTESIAN_POINT ( 'NONE',  ( 3.239063133055252841, -0.1400698962470778297, -1.964493882382233991 ) ) ;
#69812=CARTESIAN_POINT ( 'NONE',  ( 0.8086807686161383568, -0.4671638426185490967, -1.854305266343849734 ) ) ;
#69813=CARTESIAN_POINT ( 'NONE',  ( 5.173897996269102961, -1.276782452619073860, 1.903577390058891261 ) ) ;
#69814=CARTESIAN_POINT ( 'NONE',  ( 3.246530741642670748, 0.4443377543969920795, 1.770662692542070760 ) ) ;
#69818=CARTESIAN_POINT ( 'NONE',  ( 3.955341514648374357, -1.749461739742008470, 0.9961098753780948112 ) ) ;
#69819=CARTESIAN_POINT ( 'NONE',  ( 2.764445781119912127, -0.7462812867886670087, -1.814464804917370166 ) ) ;
#69822=CARTESIAN_POINT ( 'NONE',  ( 0.1751657365761703222, 4.087554309226840488, -2.598743260590470783 ) ) ;
#69823=CARTESIAN_POINT ( 'NONE',  ( 6.527293198192279711, -1.364605693714017187, -1.583936087800744907 ) ) ;
#69824=CARTESIAN_POINT ( 'NONE',  ( 5.875818619555242428, 1.057306330162042451, 1.419162741687775231 ) ) ;
#69826=CARTESIAN_POINT ( 'NONE',  ( 1.552940555598739891, -1.880887156831068552, -1.124362282834884263 ) ) ;
#69827=CARTESIAN_POINT ( 'NONE',  ( 0.3447215323711784740, 0.5487897507440896439, -1.651745661738156734 ) ) ;
#69829=CARTESIAN_POINT ( 'NONE',  ( 0.2333690889706926119, 0.7157316027301027228, -2.136973218959358434 ) ) ;
#69830=CARTESIAN_POINT ( 'NONE',  ( 0.5391470445266118849, -1.216214603651460724, -1.223400588829765878 ) ) ;
#69831=CARTESIAN_POINT ( 'NONE',  ( 0.8260327929942178349, -1.663255926670023976, 1.586464751714482979 ) ) ;
#69832=CARTESIAN_POINT ( 'NONE',  ( 0.6092356648998223934, -0.3158941238240610128, 2.168550393043596536 ) ) ;
#69833=CARTESIAN_POINT ( 'NONE',  ( 6.802075984838630518, -1.546572159107060251, 0.7837757703139431875 ) ) ;
#69834=CARTESIAN_POINT ( 'NONE',  ( 2.789901687333019797, 1.561178712900921584, 1.560079944692857046 ) ) ;
#69835=CARTESIAN_POINT ( 'NONE',  ( 6.812935010865087015, -1.682745870255862641, 1.371614790115786908 ) ) ;
#69837=CARTESIAN_POINT ( 'NONE',  ( 0.6380961361360514283, 2.114605634092497688, -0.1105060169243020224 ) ) ;
#69838=CARTESIAN_POINT ( 'NONE',  ( 6.727182134110222478, 4.688348259194305534, 2.751590707055273199 ) ) ;
#69839=CARTESIAN_POINT ( 'NONE',  ( 5.385741010672205675, 1.293702408046822239, 1.427520146239504184 ) ) ;
#69841=CARTESIAN_POINT ( 'NONE',  ( 1.206998765908244176, 2.024556473040285187, 1.075228724532976132 ) ) ;
#69845=CARTESIAN_POINT ( 'NONE',  ( 3.826986476844072005, 1.570263387305373737, -1.571374446222243204 ) ) ;
#69852=CARTESIAN_POINT ( 'NONE',  ( 1.565077508395201988, -1.076315722900993643, 1.704939445326451475 ) ) ;
#69854=CARTESIAN_POINT ( 'NONE',  ( 1.200133799977639137, 0.8395725688425963451, -1.884152621438263342 ) ) ;
#69857=CARTESIAN_POINT ( 'NONE',  ( 6.585563763084506306, -0.7354652392584435372, 1.576171286539735705 ) ) ;
#69860=CARTESIAN_POINT ( 'NONE',  ( 2.600565598370237819, 1.424089007750706237, -1.050482986540713926 ) ) ;
#69861=CARTESIAN_POINT ( 'NONE',  ( 1.705704151892040832, 1.882474636155605507, 0.7231385473688843879 ) ) ;
#69862=CARTESIAN_POINT ( 'NONE',  ( 6.409682876116948869, -0.8291888958818021127, -1.530247525868874581 ) ) ;
#69863=CARTESIAN_POINT ( 'NONE',  ( 5.530919501969752794, -2.073650524585127997, 0.9775372349926645388 ) ) ;
#69864=CARTESIAN_POINT ( 'NONE',  ( 3.204851553285171573, -0.3583046703147829137, 1.805758307424263354 ) ) ;
#69867=CARTESIAN_POINT ( 'NONE',  ( 3.961776442328440506, 1.811803316853294765, -0.2231971713724384965 ) ) ;
#69868=CARTESIAN_POINT ( 'NONE',  ( 5.274064633610318076, 1.777012466945230962, -0.9530095070046653571 ) ) ;
#69870=CARTESIAN_POINT ( 'NONE',  ( 3.924925821460770514, 2.147445456087885063, 0.7125370657276063335 ) ) ;
#69872=CARTESIAN_POINT ( 'NONE',  ( 6.299853487814777608, -0.7131585336714525436, 1.981663801677714831 ) ) ;
#69874=CARTESIAN_POINT ( 'NONE',  ( 4.070807014193541740, 1.466255041752505539, -1.461937513464212079 ) ) ;
#69879=CARTESIAN_POINT ( 'NONE',  ( 2.455585946167909928, 0.5135756288857267204, -1.856723504524477875 ) ) ;
#69881=CARTESIAN_POINT ( 'NONE',  ( 6.684429667774410611, 1.136775344189003611, -1.608021923639752604 ) ) ;
#69885=CARTESIAN_POINT ( 'NONE',  ( 0.1413017363236251933, 2.128265657893123386, 0.6366465052881072895 ) ) ;
#69886=CARTESIAN_POINT ( 'NONE',  ( 3.294068349240862226, -0.8549715976811816942, 1.924793576080959578 ) ) ;
#69889=CARTESIAN_POINT ( 'NONE',  ( 0.2735837943700462627, -1.826300444241350851, 0.3570272679806109073 ) ) ;
#69896=CARTESIAN_POINT ( 'NONE',  ( 1.600013431492643745, 1.466117565985028515, 1.532352819790145482 ) ) ;
#69899=CARTESIAN_POINT ( 'NONE',  ( 4.228923158279327410, -1.829750178516520442, -0.7082015076659909925 ) ) ;
#69900=CARTESIAN_POINT ( 'NONE',  ( 3.625982885822197410, -1.285997354380935098, -1.737435825693343094 ) ) ;
#69901=CARTESIAN_POINT ( 'NONE',  ( 1.839159199666509759, 0.7036077657225292548, -1.701706503975081830 ) ) ;
#69905=CARTESIAN_POINT ( 'NONE',  ( 5.173663570605946838, -0.9624332111635640619, 1.449765197900940938 ) ) ;
#69909=CARTESIAN_POINT ( 'NONE',  ( 2.131903390035182255, -1.411712784473453830, -1.637176306262012826 ) ) ;
#69910=CARTESIAN_POINT ( 'NONE',  ( 3.251327214347735861, -1.985796489957316391, -0.3474142817363470304 ) ) ;
#69912=CARTESIAN_POINT ( 'NONE',  ( 1.006953172832128152, 1.636353683469338183, -1.412668763314451903 ) ) ;
#69913=CARTESIAN_POINT ( 'NONE',  ( 3.485194120740982449, 1.782821823783652837, -0.8418218905394663221 ) ) ;
#69914=CARTESIAN_POINT ( 'NONE',  ( 6.509000000000010111, 6.037005099786168394, 2.594901386363585694 ) ) ;
#69915=CARTESIAN_POINT ( 'NONE',  ( 2.876435298317912004, -0.1456031558026495976, -1.936675272211895837 ) ) ;
#69916=CARTESIAN_POINT ( 'NONE',  ( 6.533470333208203584, -0.1312131129157616261, 1.882018712217728318 ) ) ;
#69926=CARTESIAN_POINT ( 'NONE',  ( 6.598638948628339662, -0.6063221841578874116, -2.226463007350306444 ) ) ;
#69928=CARTESIAN_POINT ( 'NONE',  ( 4.627759936859944467, 1.903863570041373077, -0.4726564843360381851 ) ) ;
#69930=CARTESIAN_POINT ( 'NONE',  ( 2.127577483945505055, 0.4445034925110411539, 1.966644524931899563 ) ) ;
#69932=CARTESIAN_POINT ( 'NONE',  ( 3.239577248433673784, 0.5100137816880914166, -2.054909399002705861 ) ) ;
#69937=CARTESIAN_POINT ( 'NONE',  ( 3.644333108393753573, -1.504320797718930791, 1.061230752167609204 ) ) ;
#69940=CARTESIAN_POINT ( 'NONE',  ( 3.639029512587122372, 2.014767915268770082, 0.6618469929612482705 ) ) ;
#69943=CARTESIAN_POINT ( 'NONE',  ( 5.184866321732980232, -0.2479502356789231865, -2.045719655484798949 ) ) ;
#69945=CARTESIAN_POINT ( 'NONE',  ( 2.155570461979210428, 0.7887370375637430264, 1.663910549085621415 ) ) ;
#69951=CARTESIAN_POINT ( 'NONE',  ( 1.805583701156989518, 1.836052299496168771, 1.224139149458243425 ) ) ;
#69952=CARTESIAN_POINT ( 'NONE',  ( 3.673342012549928981, 0.05998355446043589223, -2.261782774625902714 ) ) ;
#69954=CARTESIAN_POINT ( 'NONE',  ( 4.289189881116685754, -0.006549295265783834294, -1.811767228872669389 ) ) ;
#69955=CARTESIAN_POINT ( 'NONE',  ( 4.628101268237789334, 1.911029739866540345, 0.1345505791198585988 ) ) ;
#69957=CARTESIAN_POINT ( 'NONE',  ( 3.520352277729906998, 1.251605784994310300, -1.523194303571529185 ) ) ;
#69958=CARTESIAN_POINT ( 'NONE',  ( 4.662891624058607576, -1.671085903211678270, -0.8408918736509605196 ) ) ;
#69959=CARTESIAN_POINT ( 'NONE',  ( 3.774305527563319274, 1.280948863717756847, 1.919355958833997233 ) ) ;
#69960=CARTESIAN_POINT ( 'NONE',  ( 4.580409787399508659, 1.145788356511275863, -1.466404039444089591 ) ) ;
#69964=CARTESIAN_POINT ( 'NONE',  ( -0.2351498743046881446, -0.1506043639611966134, -1.983733596389973597 ) ) ;
#69966=CARTESIAN_POINT ( 'NONE',  ( 2.016375119164611984, -0.9936656701176631579, -1.856918979450744578 ) ) ;
#69971=CARTESIAN_POINT ( 'NONE',  ( 0.3518269803744868418, -1.431374087835567632, -1.425298768015555551 ) ) ;
#69976=CARTESIAN_POINT ( 'NONE',  ( 2.671339989782473001, 0.1089736159370843782, -2.158987078831893669 ) ) ;
#69977=CARTESIAN_POINT ( 'NONE',  ( 6.610000000000009202, 6.036727194997777879, 2.594899704271665275 ) ) ;
#69982=CARTESIAN_POINT ( 'NONE',  ( 6.227749967195368441, 0.7672974224810541477, -1.865044430435198741 ) ) ;
#69984=CARTESIAN_POINT ( 'NONE',  ( 6.532766951017621615, -1.867387138063754337, 0.9404246163645290091 ) ) ;
#69986=CARTESIAN_POINT ( 'NONE',  ( 1.516897200560879178, 1.518302048914378588, -1.677564506150258206 ) ) ;
#69994=CARTESIAN_POINT ( 'NONE',  ( 4.564925566169513615, -1.542601567919573258, -0.7719000744037025630 ) ) ;
#69996=CARTESIAN_POINT ( 'NONE',  ( 2.582953972192280734, 1.619985402465830671, -0.7128798769604760555 ) ) ;
#69997=CARTESIAN_POINT ( 'NONE',  ( 4.858537417550492954, 0.8407558337346630051, 2.040536144146696707 ) ) ;
#69999=CARTESIAN_POINT ( 'NONE',  ( 4.570572472720978219, 0.7768735290680817140, 1.864611197846306911 ) ) ;
#70001=CARTESIAN_POINT ( 'NONE',  ( 4.934296419935967570, -1.134874685878878520, -1.791058398909770588 ) ) ;
#70002=CARTESIAN_POINT ( 'NONE',  ( 4.587517648402447357, -0.5350702435001615243, 1.944077497823355261 ) ) ;
#70003=CARTESIAN_POINT ( 'NONE',  ( 4.306777863985831623, -0.4033372078124509708, -1.765930869088320865 ) ) ;
#70006=CARTESIAN_POINT ( 'NONE',  ( 1.375632740723360836, 1.111493989511678881, 1.504490780774490499 ) ) ;
#70008=CARTESIAN_POINT ( 'NONE',  ( 1.459083999156213451, -1.613880964290700160, 1.025699646091532857 ) ) ;
#70015=CARTESIAN_POINT ( 'NONE',  ( 2.242563829109287088, -1.923402688547710904, -0.3857071251459272543 ) ) ;
#70018=CARTESIAN_POINT ( 'NONE',  ( 4.025719079702368752, -0.3592959752154977204, 2.089770972018199835 ) ) ;
#70021=CARTESIAN_POINT ( 'NONE',  ( 5.096930449404251107, 1.640577245564038389, -1.092763768510503608 ) ) ;
#70023=CARTESIAN_POINT ( 'NONE',  ( 0.9494776711209992337, -1.818202237497710483, 0.8646994008154506028 ) ) ;
#70025=CARTESIAN_POINT ( 'NONE',  ( 0.9841680404778062607, -2.117403155482136423, 0.004310642112759220310 ) ) ;
#70028=CARTESIAN_POINT ( 'NONE',  ( 2.682155120989743402, -1.190029146579720587, -1.693995171316540427 ) ) ;
#70032=CARTESIAN_POINT ( 'NONE',  ( 5.015614203636001633, -1.117866415629315435, -1.766478577331761723 ) ) ;
#70034=CARTESIAN_POINT ( 'NONE',  ( 2.660947563312371589, -1.587261545009664765, -0.9017329732442300738 ) ) ;
#70035=CARTESIAN_POINT ( 'NONE',  ( 1.453448513857479973, -1.311971142947904401, -1.249319819763055950 ) ) ;
#70040=CARTESIAN_POINT ( 'NONE',  ( 4.858537417550492954, 0.8407558337346630051, 2.040536144146696707 ) ) ;
#70044=CARTESIAN_POINT ( 'NONE',  ( 4.318947422894989785, 1.476084237994702786, -1.215703867470045774 ) ) ;
#70048=CARTESIAN_POINT ( 'NONE',  ( 6.320769956279724155, -1.466918727022303193, 1.461273828345016845 ) ) ;
#70050=CARTESIAN_POINT ( 'NONE',  ( 5.970311429539967740, -2.080533979117826782, -0.6889730390344513955 ) ) ;
#70057=CARTESIAN_POINT ( 'NONE',  ( 3.989402248074361612, 1.353031944225962624, 1.291829963354161892 ) ) ;
#70063=CARTESIAN_POINT ( 'NONE',  ( 6.842638490404138629, -2.029097751484234546, -0.4099019697717393163 ) ) ;
#70064=CARTESIAN_POINT ( 'NONE',  ( 0.8785300617164049086, -0.4926655378557908138, -1.955167820405806056 ) ) ;
#70068=CARTESIAN_POINT ( 'NONE',  ( 1.922082643403967506, 1.260107670313360240, -1.792737600334909365 ) ) ;
#70076=ORIENTED_EDGE ( 'NONE', *, *, #148167, .F. ) ;
#70077=CARTESIAN_POINT ( 'NONE',  ( 3.597050949361340511, -0.5310884314010614338, 1.763007376093472800 ) ) ;
#70078=CARTESIAN_POINT ( 'NONE',  ( 1.154940503102233729, 0.3948395466160973255, 1.973830874585213113 ) ) ;
#70079=CARTESIAN_POINT ( 'NONE',  ( 2.390373184264094952, -0.001117755346285650552, 2.298542322714514530 ) ) ;
#70081=CARTESIAN_POINT ( 'NONE',  ( 1.094327318609791710, 1.832149372150039479, 0.3252389950085340375 ) ) ;
#70084=CARTESIAN_POINT ( 'NONE',  ( 3.990413957267644474, -1.096855775730350757, 1.566394476586838724 ) ) ;
#70088=CARTESIAN_POINT ( 'NONE',  ( 3.280887763456251882, 1.889169395226503401, -0.8960188238960642426 ) ) ;
#70089=CARTESIAN_POINT ( 'NONE',  ( 2.729206520949432946, -1.746158693253213379, 0.6715030345267187784 ) ) ;
#70092=CARTESIAN_POINT ( 'NONE',  ( 3.456370904947672074, -1.536751586138744852, -0.8169772437159742440 ) ) ;
#70096=CARTESIAN_POINT ( 'NONE',  ( 3.545241905100663615, -1.307145164029408502, -1.125523404956897178 ) ) ;
#70097=CARTESIAN_POINT ( 'NONE',  ( 3.509492838045696672, -2.158849082856160173, 0.3763758916049686487 ) ) ;
#70098=CARTESIAN_POINT ( 'NONE',  ( 5.848300530743933301, 2.204158087718602221, 0.1119919437090263481 ) ) ;
#70100=CARTESIAN_POINT ( 'NONE',  ( 3.239314478175295164, -0.1551929672521153158, -2.165549275587749456 ) ) ;
#70101=CARTESIAN_POINT ( 'NONE',  ( 2.666400811807769777, -1.259032629953384719, 1.322343945743660543 ) ) ;
#70104=CARTESIAN_POINT ( 'NONE',  ( 5.014918053075636095, 0.1589874617720990202, 2.111459674661147368 ) ) ;
#70106=CARTESIAN_POINT ( 'NONE',  ( 4.599361256383265761, -0.6123007911535255365, 2.209042870082494225 ) ) ;
#70108=CARTESIAN_POINT ( 'NONE',  ( 6.620655732516651071, 1.309889148221474509, 1.844503626996786938 ) ) ;
#70110=CARTESIAN_POINT ( 'NONE',  ( -0.004992717928550480244, -2.057963470346049650, -0.5107951590591561786 ) ) ;
#70119=CARTESIAN_POINT ( 'NONE',  ( 5.467422714486909641, -1.967887220244109558, -0.4390321945699494632 ) ) ;
#70121=CARTESIAN_POINT ( 'NONE',  ( 4.276276908810595856, -1.056066993903046924, -1.771547272865436673 ) ) ;
#70123=CARTESIAN_POINT ( 'NONE',  ( -0.2411972340276282434, 2.878796387150697633, -2.389097370654146513 ) ) ;
#70127=CARTESIAN_POINT ( 'NONE',  ( 0.8145359132093257237, 1.932373828749304856, 0.7984225692715187783 ) ) ;
#70128=CARTESIAN_POINT ( 'NONE',  ( 4.781875055470904634, 1.674888562130649960, -1.122497055794105192 ) ) ;
#70129=CARTESIAN_POINT ( 'NONE',  ( 3.843160323004328305, 0.6166970922517557296, -1.735048075492843456 ) ) ;
#70132=CARTESIAN_POINT ( 'NONE',  ( 0.4985095413094174921, 1.438046592433483761, -0.9519660005063760311 ) ) ;
#70135=CARTESIAN_POINT ( 'NONE',  ( 0.8272591630335036639, 0.9250671760404407529, -2.104501483148725427 ) ) ;
#70137=CARTESIAN_POINT ( 'NONE',  ( 0.7028506612886147309, -0.7633063118723592000, -2.129901512202157399 ) ) ;
#70138=CARTESIAN_POINT ( 'NONE',  ( 2.807361190694975139, 1.779531611039061767, 1.126096823879179754 ) ) ;
#70142=( NAMED_UNIT ( * ) PLANE_ANGLE_UNIT ( ) SI_UNIT ( $, .RADIAN. ) );
#70148=CARTESIAN_POINT ( 'NONE',  ( 5.256174644204150148, 0.8999736644031709476, -2.031094499404682008 ) ) ;
#70149=CARTESIAN_POINT ( 'NONE',  ( 2.256057974219495499, 0.9384471748680022207, 1.980482673072603284 ) ) ;
#70152=CARTESIAN_POINT ( 'NONE',  ( 5.178158156489047315, -1.047961880893449882, -1.658324637040713867 ) ) ;
#70154=CARTESIAN_POINT ( 'NONE',  ( 6.890000000000025437, 2.478461836817289043, 2.104748632312344103 ) ) ;
#70157=CARTESIAN_POINT ( 'NONE',  ( 4.869442314738527067, -1.792836814666173062, -1.132239877606910472 ) ) ;
#70161=CARTESIAN_POINT ( 'NONE',  ( 6.332923096303629151, 0.2067577541180857514, 2.151790036905242953 ) ) ;
#70163=CARTESIAN_POINT ( 'NONE',  ( 4.862772069579198941, 0.1752732939881325724, -1.832877676746891726 ) ) ;
#70166=CARTESIAN_POINT ( 'NONE',  ( 0.7842107965865081631, 1.535900883440274090, -0.8186502264825399333 ) ) ;
#70170=CARTESIAN_POINT ( 'NONE',  ( 4.961884481312108797, 2.138711985806662330, -0.3135959325617638238 ) ) ;
#70173=CARTESIAN_POINT ( 'NONE',  ( 4.416967121957662279, 1.975198431823081302, 0.8787980929093119897 ) ) ;
#70175=CARTESIAN_POINT ( 'NONE',  ( 5.026621361268301946, 1.885657091993764745, 0.5748499752153258813 ) ) ;
#70176=CARTESIAN_POINT ( 'NONE',  ( 4.358545522520183013, -0.6637924119957930857, 1.601953373104019418 ) ) ;
#70177=CARTESIAN_POINT ( 'NONE',  ( 1.066276686178056377, -1.386418637449363889, 1.697306931840412370 ) ) ;
#70178=CARTESIAN_POINT ( 'NONE',  ( 2.362750734746793757, 0.9868518204677073635, 2.086042234993300770 ) ) ;
#70179=CARTESIAN_POINT ( 'NONE',  ( 3.427077464676528074, 0.04692547926744317088, 2.060408731095995094 ) ) ;
#70180=CARTESIAN_POINT ( 'NONE',  ( 6.339402847020720877, 0.7390441267520877489, -1.796137868246181046 ) ) ;
#70186=CARTESIAN_POINT ( 'NONE',  ( 3.856632026064894525, 0.7917978285330304900, 2.060012427959257764 ) ) ;
#70189=CARTESIAN_POINT ( 'NONE',  ( 0.8482322855925720217, -1.845984902429298025, -0.2351823381797259749 ) ) ;
#70190=CARTESIAN_POINT ( 'NONE',  ( -0.1290005225502433017, 7.629137130509076492, -2.773995091683974401 ) ) ;
#70194=CARTESIAN_POINT ( 'NONE',  ( 6.925078400183531713, 7.629137130509035636, 2.844348168701658075 ) ) ;
#70196=CARTESIAN_POINT ( 'NONE',  ( 2.817317228389113470, -0.2032538945386449802, 2.050847873933867138 ) ) ;
#70200=CARTESIAN_POINT ( 'NONE',  ( 2.719404001658455527, 1.707403962800517316, 1.078498517531191858 ) ) ;
#70203=CARTESIAN_POINT ( 'NONE',  ( 2.500915792353772815, 1.655931770628838784, -1.226644000274518476 ) ) ;
#70210=CARTESIAN_POINT ( 'NONE',  ( 5.883472226557855400, 2.040502603023553796, -0.8411249186189362348 ) ) ;
#70211=CARTESIAN_POINT ( 'NONE',  ( 1.335488691732108046, -1.954760257947166568, 0.9229496955955732718 ) ) ;
#70213=CARTESIAN_POINT ( 'NONE',  ( 0.9543149826918421175, -1.275552737861269437, 1.561884623745241951 ) ) ;
#70215=CARTESIAN_POINT ( 'NONE',  ( 1.933413756328787869, 1.181669745456917830, 1.971221161662185528 ) ) ;
#70217=CARTESIAN_POINT ( 'NONE',  ( 6.621744163077868173, -0.4141588628726756149, 1.873750786029332316 ) ) ;
#70220=CARTESIAN_POINT ( 'NONE',  ( 1.920565142479381038, 1.744437793965779582, 0.6759427408406930571 ) ) ;
#70221=CARTESIAN_POINT ( 'NONE',  ( 3.467982673848205355, -0.9896861206786079501, 1.756853968756578066 ) ) ;
#70225=CARTESIAN_POINT ( 'NONE',  ( 5.197925827040419833, -0.7590715138193807610, 1.964706065220876541 ) ) ;
#70229=CARTESIAN_POINT ( 'NONE',  ( 5.502215278945715937, -0.9042992897083046433, 1.806084391566422198 ) ) ;
#70231=CARTESIAN_POINT ( 'NONE',  ( 0.8485701241471826917, -2.046539366587364572, -0.2563945212397024109 ) ) ;
#70233=CARTESIAN_POINT ( 'NONE',  ( 5.870447946289019114, -1.376328297836002301, 1.666777564274177781 ) ) ;
#70238=CARTESIAN_POINT ( 'NONE',  ( 3.438082271139299539, 1.374976351402785513, 1.680335591205921908 ) ) ;
#70241=CARTESIAN_POINT ( 'NONE',  ( 2.225889136967126536, 1.786374552192676823, 0.4457033907802817052 ) ) ;
#70243=CARTESIAN_POINT ( 'NONE',  ( 4.142245973918059043, 0.5854081421233224836, 2.111838497463234710 ) ) ;
#70244=CARTESIAN_POINT ( 'NONE',  ( 6.883263157960330503, 2.417872181280413812, 2.534681901920758929 ) ) ;
#70245=CARTESIAN_POINT ( 'NONE',  ( 4.487383681424582882, 2.022794180288649990, -1.013680454646571638 ) ) ;
#70254=CARTESIAN_POINT ( 'NONE',  ( 5.114393831954183511, 1.220379059178023695, -1.281870188591783588 ) ) ;
#70256=CARTESIAN_POINT ( 'NONE',  ( 1.589043446250279601, -0.3083810453359912551, -2.083120927691509916 ) ) ;
#70259=CARTESIAN_POINT ( 'NONE',  ( 2.277737068081890914, -1.911112558508936354, 0.4757300241334978530 ) ) ;
#70262=CARTESIAN_POINT ( 'NONE',  ( 6.134996530155978789, 1.693739186514784167, 0.6432786700914516764 ) ) ;
#70266=CARTESIAN_POINT ( 'NONE',  ( 6.420764531294745225, 1.746252128813120086, 0.6712297951826234899 ) ) ;
#70268=CARTESIAN_POINT ( 'NONE',  ( 6.034052368894809781, 1.228512962337786174, 1.666229478724051027 ) ) ;
#70271=CARTESIAN_POINT ( 'NONE',  ( 0.2564123431100414074, -2.069877475643782994, -0.05227228806716639753 ) ) ;
#70278=CARTESIAN_POINT ( 'NONE',  ( 5.213317179658601752, -1.656387821537348426, -1.051046178410528942 ) ) ;
#70280=CARTESIAN_POINT ( 'NONE',  ( 3.233749808020690342, -1.861731463674856979, -0.7741979076196571219 ) ) ;
#70281=CARTESIAN_POINT ( 'NONE',  ( 3.063600739116902449, 1.219304168433880564, 1.477546071989847665 ) ) ;
#70284=CARTESIAN_POINT ( 'NONE',  ( -0.005964567173097347699, -2.191213315851054944, -0.04726126812268362232 ) ) ;
#70285=CARTESIAN_POINT ( 'NONE',  ( 0.2333690889706682703, 1.352610664630080839, -2.308230059406161772 ) ) ;
#70286=CARTESIAN_POINT ( 'NONE',  ( 1.827212670807505379, -1.763035892288829620, 0.6254473451912796467 ) ) ;
#70288=CARTESIAN_POINT ( 'NONE',  ( 4.605731108040309607, 1.494732351555028371, 1.348829144277723824 ) ) ;
#70291=CARTESIAN_POINT ( 'NONE',  ( 5.009417666957850734, -2.010078760914670859, 0.6651486602928055047 ) ) ;
#70293=CARTESIAN_POINT ( 'NONE',  ( 6.566853775770633561, 1.536883091774071453, -1.387433097640700774 ) ) ;
#70294=CARTESIAN_POINT ( 'NONE',  ( 0.7145361118556601276, 1.933244891618046024, 0.7966077499205433954 ) ) ;
#70296=CARTESIAN_POINT ( 'NONE',  ( 6.106453908201667780, -0.6597477751954274883, -1.702385593799011110 ) ) ;
#70305=CARTESIAN_POINT ( 'NONE',  ( 0.8733459280946423986, 0.3543511941397787801, -1.776278655377810489 ) ) ;
#70313=CARTESIAN_POINT ( 'NONE',  ( 6.064077406165095496, -1.076301619396256237, 1.704949653848472302 ) ) ;
#70314=CARTESIAN_POINT ( 'NONE',  ( 0.03014954708456181465, -2.078685333231004684, 0.4181070283913386199 ) ) ;
#70320=CARTESIAN_POINT ( 'NONE',  ( 3.063290813078624719, 1.661244007368352982, 1.057527034793050547 ) ) ;
#70321=CARTESIAN_POINT ( 'NONE',  ( 4.411732571322396268, -1.242743209197882059, -1.587826168943158089 ) ) ;
#70325=CARTESIAN_POINT ( 'NONE',  ( 5.173855182012670362, -1.219361875273092366, 1.820681821249593657 ) ) ;
#70327=CARTESIAN_POINT ( 'NONE',  ( 3.557566385928968788, 0.4691178692100838599, -1.868274323828737371 ) ) ;
#70329=CARTESIAN_POINT ( 'NONE',  ( -0.02988540731103071432, 0.005807295984020746475, -1.726291166677936362 ) ) ;
#70334=CARTESIAN_POINT ( 'NONE',  ( 4.733233314711627671, 0.004152288854553880422, -1.969629310717621040 ) ) ;
#70335=CARTESIAN_POINT ( 'NONE',  ( 0.1166052997346351955, -0.09441621361710265947, 1.939868080593883048 ) ) ;
#70336=CARTESIAN_POINT ( 'NONE',  ( 3.545567672969043294, -1.859159518717553139, 0.7725093927312511877 ) ) ;
#70337=CARTESIAN_POINT ( 'NONE',  ( 5.185072832991014735, -1.223605693886620438, -1.945460884747321151 ) ) ;
#70339=CARTESIAN_POINT ( 'NONE',  ( 3.854231730816888302, -1.858662791824859051, -0.09517680055876918954 ) ) ;
#70345=CARTESIAN_POINT ( 'NONE',  ( 0.1522426329377546128, 0.8445714516599597266, 2.022489037641273857 ) ) ;
#70350=CARTESIAN_POINT ( 'NONE',  ( 0.6447967512687136082, -1.567379569643694515, 0.9359695128687425258 ) ) ;
#70353=CARTESIAN_POINT ( 'NONE',  ( 2.830371795882984820, 0.6218406304432465559, -1.619021885657184745 ) ) ;
#70358=CARTESIAN_POINT ( 'NONE',  ( 5.725187622324654946, -0.04035785615889506128, 1.825416780793003069 ) ) ;
#70359=CARTESIAN_POINT ( 'NONE',  ( 3.819154011256303161, -1.728040176127441763, -0.9287006429716244682 ) ) ;
#70363=CARTESIAN_POINT ( 'NONE',  ( 5.268275487455277073, 2.118052368503114291, -0.1043780312826799589 ) ) ;
#70366=CARTESIAN_POINT ( 'NONE',  ( 1.534126288888465917, 1.230018689141991306, 1.665114864061276734 ) ) ;
#70369=CARTESIAN_POINT ( 'NONE',  ( 4.283969606688295961, 2.154612580813870082, -0.5396949931109666920 ) ) ;
#70371=CARTESIAN_POINT ( 'NONE',  ( 1.864337758866913441, -0.1181282521124735752, -2.295782230965204285 ) ) ;
#70376=CARTESIAN_POINT ( 'NONE',  ( 6.509000000000016328, 0.001920477310516919547, 2.100274754360693219 ) ) ;
#70378=CARTESIAN_POINT ( 'NONE',  ( 2.795058504854182946, -0.1448928079688660830, -1.906987441340234568 ) ) ;
#70380=CARTESIAN_POINT ( 'NONE',  ( 4.225434206992398245, -1.650187577572001629, 0.5017251585606904429 ) ) ;
#70381=CARTESIAN_POINT ( 'NONE',  ( 2.044158018538293042, 0.8666093899718421145, 1.820985203412978093 ) ) ;
#70382=CARTESIAN_POINT ( 'NONE',  ( 4.201969167805962968, 2.101520711257957252, 0.9317802909727909144 ) ) ;
#70384=CARTESIAN_POINT ( 'NONE',  ( 6.006491595720174104, -0.7565722652288708883, -1.965664901909335738 ) ) ;
#70386=CARTESIAN_POINT ( 'NONE',  ( 4.288192095134175652, -1.750260269857591755, -0.2610086191854649740 ) ) ;
#70388=CARTESIAN_POINT ( 'NONE',  ( 0.3402841477759439570, 2.286568017602428338, 0.1625022809590911665 ) ) ;
#70389=CARTESIAN_POINT ( 'NONE',  ( 0.02286245922865359423, -1.065969982613410583, -1.375977130364250955 ) ) ;
#70391=CARTESIAN_POINT ( 'NONE',  ( 5.806613533822880591, 1.931179984464112653, 1.035834350304319695 ) ) ;
#70395=CARTESIAN_POINT ( 'NONE',  ( 0.1393978552833140261, -0.1497620924123649333, -2.137132186964474378 ) ) ;
#70396=CARTESIAN_POINT ( 'NONE',  ( 1.499232818411553536, -0.2420282084563407654, 2.001858358113464575 ) ) ;
#70398=CARTESIAN_POINT ( 'NONE',  ( 4.494702926938664689, -0.4234472454235098104, -1.879237243589318318 ) ) ;
#70400=CARTESIAN_POINT ( 'NONE',  ( 1.090412635922506368, 1.328748260410139492, 1.780047631856091606 ) ) ;
#70408=CARTESIAN_POINT ( 'NONE',  ( 3.843067196288481480, 0.5821562417002418277, -1.640339850388317089 ) ) ;
#70409=CARTESIAN_POINT ( 'NONE',  ( 2.506241959165692812, 1.961374882610424919, 0.05109738790698423877 ) ) ;
#70416=CARTESIAN_POINT ( 'NONE',  ( 0.3794369086736723018, -0.1030016517138358095, 2.060237976199934984 ) ) ;
#70419=CARTESIAN_POINT ( 'NONE',  ( 0.8314075926023238861, 0.1693486111025067908, 2.256218002396610522 ) ) ;
#70424=CARTESIAN_POINT ( 'NONE',  ( 1.985418980784030119, 1.286400883397397221, 1.358229366437320618 ) ) ;
#70425=CARTESIAN_POINT ( 'NONE',  ( -0.03512515232485542011, -1.681152455970882809, -0.4250410675877940303 ) ) ;
#70427=CARTESIAN_POINT ( 'NONE',  ( 4.493798347139664529, -2.191065130646638437, -0.05333993539427539510 ) ) ;
#70428=CARTESIAN_POINT ( 'NONE',  ( 5.684705870536221894, -2.249774798156725986, -0.5126945500162644054 ) ) ;
#70429=CARTESIAN_POINT ( 'NONE',  ( 0.7255486961553169190, -1.957115920898297112, 0.6459669076722980297 ) ) ;
#70430=CARTESIAN_POINT ( 'NONE',  ( 3.890518024738118807, 1.639914603359222456, -1.039847546996591765 ) ) ;
#70432=CARTESIAN_POINT ( 'NONE',  ( 5.852782322939766857, -1.474943281369223147, 1.150351685248012457 ) ) ;
#70435=CARTESIAN_POINT ( 'NONE',  ( 5.115861365725078436, 0.1511377038382749338, 2.010826595755777824 ) ) ;
#70439=CARTESIAN_POINT ( 'NONE',  ( 1.312830284664792790, 1.609138963534262778, 0.8624270714618911260 ) ) ;
#70445=CARTESIAN_POINT ( 'NONE',  ( 6.825078400183568483, -0.002763825414428457399, 2.044262525762724270 ) ) ;
#70450=CARTESIAN_POINT ( 'NONE',  ( 6.182287216677275765, 1.039997956529638889, 1.731187096421077376 ) ) ;
#70451=CARTESIAN_POINT ( 'NONE',  ( 0.4695848928168535608, -1.793611485386744420, -1.130822890709509254 ) ) ;
#70455=CARTESIAN_POINT ( 'NONE',  ( 5.190332118341006051, -2.045072267241864861, -0.2543341860123843334 ) ) ;
#70456=CARTESIAN_POINT ( 'NONE',  ( 3.885388821667290493, -0.6351983117205138862, -1.913803978180687482 ) ) ;
#70463=CARTESIAN_POINT ( 'NONE',  ( 4.358749857130030492, -0.7741967591250037417, 1.861731939633674893 ) ) ;
#70464=CARTESIAN_POINT ( 'NONE',  ( 3.257574473681293270, 0.8286728953739975756, 1.644182576024610265 ) ) ;
#70466=CARTESIAN_POINT ( 'NONE',  ( 2.350585845863040646, 2.307203942772034111, 0.05475910514858049749 ) ) ;
#70468=CARTESIAN_POINT ( 'NONE',  ( 4.499409293453607184, 1.733128992574247684, 1.291583502853070886 ) ) ;
#70470=CARTESIAN_POINT ( 'NONE',  ( 0.2396544122938427390, 1.936909983681795344, 0.1419545801408238772 ) ) ;
#70471=CARTESIAN_POINT ( 'NONE',  ( 2.764861550476094276, -0.1531697945360478985, -2.010801143277194392 ) ) ;
#70475=CARTESIAN_POINT ( 'NONE',  ( 1.797508989346347619, -0.6330400025267440833, 1.760413054629046625 ) ) ;
#70477=CARTESIAN_POINT ( 'NONE',  ( 0.1925371440497048448, -0.4299567264692584212, -1.931277891087788579 ) ) ;
#70480=CARTESIAN_POINT ( 'NONE',  ( 1.752831059180045115, 0.6944836804415283060, 2.094827981560241970 ) ) ;
#70481=VERTEX_POINT ( 'NONE', #73687 ) ;
#70485=CARTESIAN_POINT ( 'NONE',  ( 6.139525842074132100, -1.427670353879314957, -1.359795004109279004 ) ) ;
#70486=CARTESIAN_POINT ( 'NONE',  ( 6.428381082836107652, 1.334599446741807638, -1.882477381066828936 ) ) ;
#70487=CARTESIAN_POINT ( 'NONE',  ( 6.549252741683062595, 1.618575325784047392, -0.9183544947665848168 ) ) ;
#70488=CARTESIAN_POINT ( 'NONE',  ( 4.188373618524662056, 1.107674127198258196, -1.739744320567500280 ) ) ;
#70496=CARTESIAN_POINT ( 'NONE',  ( 0.2335667940002684184, 0.001055507091213009818, -2.153566573614831281 ) ) ;
#70498=CARTESIAN_POINT ( 'NONE',  ( 5.073706409418358376, -1.018251046719556685, 1.533866337327425278 ) ) ;
#70501=CARTESIAN_POINT ( 'NONE',  ( 0.5263522483448194178, 1.788089326329355577, 0.5492086291003297482 ) ) ;
#70505=CARTESIAN_POINT ( 'NONE',  ( 1.383307607624170155, 0.1396965592646744470, -1.907218110473147155 ) ) ;
#70507=CARTESIAN_POINT ( 'NONE',  ( 1.744620744215353625, -1.497317806218407599, 0.9432750629611782456 ) ) ;
#70508=CARTESIAN_POINT ( 'NONE',  ( 6.633470333208185465, -0.1360683555875797923, 1.981904614263108266 ) ) ;
#70510=CARTESIAN_POINT ( 'NONE',  ( 4.429236352518686637, -1.483253864829991775, -1.212251590588450112 ) ) ;
#70512=CARTESIAN_POINT ( 'NONE',  ( 5.195741393986025969, -1.391442517743620710, -1.394189886649561227 ) ) ;
#70513=CARTESIAN_POINT ( 'NONE',  ( 0.1586465271753433603, 2.115359532055087310, 0.1496401998123952359 ) ) ;
#70515=CARTESIAN_POINT ( 'NONE',  ( 4.469519713540137218, 1.814478506493342191, -0.4545110902946307152 ) ) ;
#70516=CARTESIAN_POINT ( 'NONE',  ( 6.428329371266205072, 0.9864720512241608175, -1.414751289540659318 ) ) ;
#70518=CARTESIAN_POINT ( 'NONE',  ( 4.020313978404310262, -1.133593497508533110, -1.893353337301090233 ) ) ;
#70521=CARTESIAN_POINT ( 'NONE',  ( 0.6079712386793578727, 0.6485803912554971573, -1.958102696269433673 ) ) ;
#70525=CARTESIAN_POINT ( 'NONE',  ( 0.1747926744264668986, 7.629137130509083597, -2.455305974604498953 ) ) ;
#70528=CARTESIAN_POINT ( 'NONE',  ( 2.822784111170244525, -1.429543836668966561, 1.497820115680066344 ) ) ;
#70532=CARTESIAN_POINT ( 'NONE',  ( 1.295575897195440307, 1.865243415117883385, -0.7750591016795584931 ) ) ;
#70536=CARTESIAN_POINT ( 'NONE',  ( 0.07499057489260964326, 4.092262291754148684, -2.510514182268712702 ) ) ;
#70538=CARTESIAN_POINT ( 'NONE',  ( 6.397814513887354337, 0.1948139983735352188, 2.006652364629394114 ) ) ;
#70539=CARTESIAN_POINT ( 'NONE',  ( 6.403544266003773799, -1.856299428965903164, 0.4729442951737494183 ) ) ;
#70541=CARTESIAN_POINT ( 'NONE',  ( 3.245827600587628758, 2.191739723504753101, -0.002129563554123526260 ) ) ;
#70543=CARTESIAN_POINT ( 'NONE',  ( 2.777492966359981441, 0.2764497561681695803, -1.892163382976944419 ) ) ;
#70547=CARTESIAN_POINT ( 'NONE',  ( 1.458611474731505986, -1.915607644094442064, -0.6298556652749932594 ) ) ;
#70549=CARTESIAN_POINT ( 'NONE',  ( 6.444889499930222421, -1.758869480593090673, -1.307235502039267860 ) ) ;
#70551=CARTESIAN_POINT ( 'NONE',  ( 3.328823242065849008, 0.04121275867331047893, 1.724443917160731976 ) ) ;
#70553=CARTESIAN_POINT ( 'NONE',  ( 0.1399997263886003374, 7.629137130509076492, -2.599723212958489516 ) ) ;
#70557=CARTESIAN_POINT ( 'NONE',  ( 1.012071980069819910, 1.959787197952606252, -0.09269708818125664551 ) ) ;
#70563=CARTESIAN_POINT ( 'NONE',  ( 4.213381321868588714, 1.457370398675205569, 1.075660112967236737 ) ) ;
#70567=CARTESIAN_POINT ( 'NONE',  ( 4.635318128526639825, -0.08385371298775616544, 1.809651570580686819 ) ) ;
#70572=CARTESIAN_POINT ( 'NONE',  ( 5.318752605461887661, -1.348013374683079135, 1.283375817886179826 ) ) ;
#70574=CARTESIAN_POINT ( 'NONE',  ( 3.198755040744692302, 1.733147561012362559, 0.8161988141396243623 ) ) ;
#70586=CARTESIAN_POINT ( 'NONE',  ( 1.289138792185164251, 1.584031432202914313, 1.364508995882382170 ) ) ;
#70588=CARTESIAN_POINT ( 'NONE',  ( 6.124042008734975617, -1.070608276503826950, -1.601302156493543905 ) ) ;
#70590=CARTESIAN_POINT ( 'NONE',  ( 2.783998052563033010, -0.9402290988879957734, 1.564698673013890984 ) ) ;
#70592=CARTESIAN_POINT ( 'NONE',  ( 1.810667312839256304, -0.5133170510521027907, -1.842115474350584980 ) ) ;
#70593=CARTESIAN_POINT ( 'NONE',  ( 2.049204468142644231, 1.715183525312633517, -0.9679544390571446222 ) ) ;
#70594=CARTESIAN_POINT ( 'NONE',  ( 4.142085694530703854, 0.5209831505245207106, 1.870798910701749973 ) ) ;
#70600=CARTESIAN_POINT ( 'NONE',  ( 3.937823072884456099, -2.028283017459261650, 0.6187693826033290323 ) ) ;
#70607=CARTESIAN_POINT ( 'NONE',  ( 4.266095019097836172, 0.8626762044917112293, 1.609013669381313294 ) ) ;
#70612=CARTESIAN_POINT ( 'NONE',  ( 4.539837415608827698, 0.7997722286730184482, -1.691214532891088362 ) ) ;
#70614=CARTESIAN_POINT ( 'NONE',  ( 1.875490933414716288, 1.843686865663298091, -0.5587569667290130937 ) ) ;
#70616=CARTESIAN_POINT ( 'NONE',  ( 6.666857073735664052, 1.455856877570887109, -1.315125143065517532 ) ) ;
#70622=CARTESIAN_POINT ( 'NONE',  ( 1.634521315757204940, 0.6676430208681031209, 2.009258352967583150 ) ) ;
#70627=CARTESIAN_POINT ( 'NONE',  ( 5.418829850390409320, -1.503349927839289002, 1.423607673449282851 ) ) ;
#70628=CARTESIAN_POINT ( 'NONE',  ( 0.3625324912872701089, 0.1813134127766780901, -1.832273687604975665 ) ) ;
#70630=CARTESIAN_POINT ( 'NONE',  ( 6.205746375452622310, 2.143286971341977765, 0.8312943217957665665 ) ) ;
#70634=CARTESIAN_POINT ( 'NONE',  ( 1.676131343691760645, -1.223425685817343789, 1.938311714834321631 ) ) ;
#70637=CARTESIAN_POINT ( 'NONE',  ( 6.281195871053392388, 1.340900550492612364, 1.404911987746715774 ) ) ;
#70641=CARTESIAN_POINT ( 'NONE',  ( 6.469012471580376733, -1.473683540339595810, 1.218514635347216046 ) ) ;
#70646=CARTESIAN_POINT ( 'NONE',  ( 2.783241352837596327, 1.478939484563842610, 1.477931775543766202 ) ) ;
#70647=CARTESIAN_POINT ( 'NONE',  ( 1.164531557977426912, -1.597865870565655877, -0.7613500884297589311 ) ) ;
#70648=CARTESIAN_POINT ( 'NONE',  ( 6.539686446881147752, -1.556848207870220602, 1.281141925495055123 ) ) ;
#70650=CARTESIAN_POINT ( 'NONE',  ( 4.400488903878751579, 1.773513045242902209, -1.452268937634313417 ) ) ;
#70651=CARTESIAN_POINT ( 'NONE',  ( 3.362975788648288944, 1.697558991927169192, -0.3826393865087075463 ) ) ;
#70655=CARTESIAN_POINT ( 'NONE',  ( 2.952174690553764691, 1.223825555390768871, 1.228469256970601498 ) ) ;
#70656=CARTESIAN_POINT ( 'NONE',  ( 3.438082271139299539, 1.374976351402785513, 1.680335591205921908 ) ) ;
#70658=CARTESIAN_POINT ( 'NONE',  ( 4.821500071095637274, -1.429446227384461032, -1.422610148874188463 ) ) ;
#70659=CARTESIAN_POINT ( 'NONE',  ( 1.531250000000001110, -0.7852924748300684765, -1.895863743164053927 ) ) ;
#70661=CARTESIAN_POINT ( 'NONE',  ( 1.149297380808786517, -1.516923518071541910, -1.187294353726556562 ) ) ;
#70663=CARTESIAN_POINT ( 'NONE',  ( 4.008219027074312990, -0.8479933951243652235, 2.053374474559205520 ) ) ;
#70665=CARTESIAN_POINT ( 'NONE',  ( -0.2108831679770960255, -0.001785917861228669690, -1.896958272444612792 ) ) ;
#70670=CARTESIAN_POINT ( 'NONE',  ( 0.2061412868327249515, 1.650399489264813502, 1.486927644236696766 ) ) ;
#70671=CARTESIAN_POINT ( 'NONE',  ( 5.617619635959271385, 0.3843197845415853853, -1.923678648292715732 ) ) ;
#70674=CARTESIAN_POINT ( 'NONE',  ( 6.520815820410102326, 2.107438871474434983, 0.8233813407293107955 ) ) ;
#70675=CLOSED_SHELL ( 'NONE', ( #79519, #91112, #203731, #183898, #23463, #194422, #169621, #213186 ) ) ;
#70677=CARTESIAN_POINT ( 'NONE',  ( 3.666515279890161239, -0.8333913613888814798, -1.886988505759807921 ) ) ;
#70681=CARTESIAN_POINT ( 'NONE',  ( 5.132044594934622062, 0.9627672477196843603, -1.603626212978970900 ) ) ;
#70682=CARTESIAN_POINT ( 'NONE',  ( 3.902719751800659775, -0.8955246652143248332, -1.484863070527132622 ) ) ;
#70683=CARTESIAN_POINT ( 'NONE',  ( 3.175097308692858444, 1.106666961078702771, 1.343256515094106041 ) ) ;
#70684=CARTESIAN_POINT ( 'NONE',  ( 0.5391474206018737059, -1.962199071191613964, 1.185045521927590162 ) ) ;
#70686=CARTESIAN_POINT ( 'NONE',  ( 4.230081496780574213, 2.050754116127400106, 0.4060544076584340356 ) ) ;
#70687=CARTESIAN_POINT ( 'NONE',  ( 0.2164228883963260908, -0.09351453081237262599, 1.838880455306932227 ) ) ;
#70689=CARTESIAN_POINT ( 'NONE',  ( 1.195935645703485539, 1.779627574718087635, 0.9480385367472210500 ) ) ;
#70690=CARTESIAN_POINT ( 'NONE',  ( 0.1643758432304382178, -1.428106194732338352, 1.662303017507735570 ) ) ;
#70694=CARTESIAN_POINT ( 'NONE',  ( 2.297662419472700002, 1.937625723843895864, -0.8618613456389671024 ) ) ;
#70695=CARTESIAN_POINT ( 'NONE',  ( 5.988856447087389512, -0.2726756491404982441, -1.805090154579996442 ) ) ;
#70702=CARTESIAN_POINT ( 'NONE',  ( 1.758075477673838982, 0.7690763710625804217, -1.867840884567156357 ) ) ;
#70703=CARTESIAN_POINT ( 'NONE',  ( 6.651417122894856426, -1.768357563224710605, -1.319949637914811458 ) ) ;
#70705=CARTESIAN_POINT ( 'NONE',  ( 4.487043221128726778, 0.08799343497551150028, 1.858965402599630723 ) ) ;
#70710=( BOUNDED_CURVE ( )  B_SPLINE_CURVE ( 3, ( #172357, #156110, #41307, #56468 ),
 .UNSPECIFIED., .F., .T. ) 
 B_SPLINE_CURVE_WITH_KNOTS ( ( 4, 4 ),
 ( 0.4999999999999993894, 1.000000000000000000 ),
 .UNSPECIFIED. ) 
 CURVE ( )  GEOMETRIC_REPRESENTATION_ITEM ( )  RATIONAL_B_SPLINE_CURVE ( ( 1.000000000000000888, 0.3333333333333334259, 0.3333333333333325932, 1.000000000000000000 ) ) 
 REPRESENTATION_ITEM ( '' )  );
#70712=CARTESIAN_POINT ( 'NONE',  ( 5.215394836314163562, -0.2642288504575221464, 1.806346989861665087 ) ) ;
#70716=CARTESIAN_POINT ( 'NONE',  ( 1.967715241700284556, 1.438441333088829266, 0.9676545092154006378 ) ) ;
#70717=CARTESIAN_POINT ( 'NONE',  ( 6.474545096729185545, -0.09562278402284159207, -1.838781726270556804 ) ) ;
#70718=CARTESIAN_POINT ( 'NONE',  ( 5.004635055918612352, -0.7736033420917761694, -2.174287598079288841 ) ) ;
#70720=CARTESIAN_POINT ( 'NONE',  ( 1.686866501761717263, -0.2992900534812113489, -2.038785687196064789 ) ) ;
#70722=CARTESIAN_POINT ( 'NONE',  ( 0.2982036909132765867, -1.844429998007334648, 0.8144978490535054183 ) ) ;
#70726=CARTESIAN_POINT ( 'NONE',  ( 5.998880656844745474, 1.528293836345222312, -1.078463600801618405 ) ) ;
#70728=CARTESIAN_POINT ( 'NONE',  ( 3.621269620730773298, 1.642686141288721480, 0.9789267784374030557 ) ) ;
#70730=CARTESIAN_POINT ( 'NONE',  ( 5.338574060078519423, 2.173733305800494175, 0.3801736985692484305 ) ) ;
#70735=CARTESIAN_POINT ( 'NONE',  ( 6.270199134133584096, 2.114857618286110075, -0.1555134818699496213 ) ) ;
#70737=EDGE_CURVE ( 'NONE', #157709, #64278, #63048, .T. ) ;
#70738=CARTESIAN_POINT ( 'NONE',  ( 3.575485986712009456, 0.05928947047922557279, -2.306987226281012049 ) ) ;
#70739=CARTESIAN_POINT ( 'NONE',  ( 3.824618516750320385, -1.319357783791510697, 1.452116237791359010 ) ) ;
#70741=CARTESIAN_POINT ( 'NONE',  ( 0.3386216902839487841, -1.901412053528793722, -0.4823507731460881520 ) ) ;
#70745=CARTESIAN_POINT ( 'NONE',  ( 6.227749967195368441, 0.7672974224810541477, -1.865044430435198741 ) ) ;
#70748=CARTESIAN_POINT ( 'NONE',  ( 0.1461044202776436429, -1.480667811789614818, 1.094048858351577724 ) ) ;
#70749=CARTESIAN_POINT ( 'NONE',  ( 2.782273231148081116, -1.246650745954593464, -1.777310168556520464 ) ) ;
#70751=CARTESIAN_POINT ( 'NONE',  ( 0.3871773095200456982, -1.998849835692744659, -0.7086421328065874992 ) ) ;
#70756=CARTESIAN_POINT ( 'NONE',  ( 0.8431279278494309137, -1.768909939683245058, 1.056965710194081920 ) ) ;
#70758=CARTESIAN_POINT ( 'NONE',  ( 6.727182134110201162, 0.003007720480356981373, 1.910970182385363092 ) ) ;
#70762=CARTESIAN_POINT ( 'NONE',  ( 4.072844535355981677, -1.414876986328793329, 1.286614418101794444 ) ) ;
#70765=CARTESIAN_POINT ( 'NONE',  ( 0.4569037783100584060, -1.553534471429316666, 0.9316326570649158256 ) ) ;
#70767=CARTESIAN_POINT ( 'NONE',  ( 0.6025738811294746311, 1.771267034891465642, 0.7302799438476501592 ) ) ;
#70768=CARTESIAN_POINT ( 'NONE',  ( 1.557173632797459684, 1.693725193156172315, -1.190412882225246438 ) ) ;
#70770=CARTESIAN_POINT ( 'NONE',  ( 0.4089732319989903275, 1.714023354001862787, 0.9739579164984181192 ) ) ;
#70771=CARTESIAN_POINT ( 'NONE',  ( 2.930095790256614485, 1.013914413367119627, -1.518051517300327502 ) ) ;
#70773=CARTESIAN_POINT ( 'NONE',  ( 0.1359762249627448627, -2.107041879058098033, 0.9415998322012062438 ) ) ;
#70776=CARTESIAN_POINT ( 'NONE',  ( 4.105966297347532823, 0.6976637339557908435, -1.941222516249243579 ) ) ;
#70781=CARTESIAN_POINT ( 'NONE',  ( 5.016683434392706253, 1.454383057171860116, -1.523333715015115608 ) ) ;
#70784=CARTESIAN_POINT ( 'NONE',  ( 6.707487347292075519, -1.660346423639452951, -1.236579608897829363 ) ) ;
#70786=CARTESIAN_POINT ( 'NONE',  ( 3.216266648612066792, -1.062311135343798618, -1.882447817163131587 ) ) ;
#70787=CARTESIAN_POINT ( 'NONE',  ( 4.635418745873795210, -0.09682320349532060055, 2.017468490573450346 ) ) ;
#70794=CARTESIAN_POINT ( 'NONE',  ( 2.923064838257955156, -1.776166165677966591, 0.9548571111624851726 ) ) ;
#70799=CARTESIAN_POINT ( 'NONE',  ( 5.607647405131535479, 1.452367144367059826, 1.244281684088063944 ) ) ;
#70800=CARTESIAN_POINT ( 'NONE',  ( 6.720655732516665815, 3.683894443391816154, 2.687682123607849416 ) ) ;
#70802=CARTESIAN_POINT ( 'NONE',  ( 4.271111354109316416, 1.799915745204151429, -0.9091612155255476280 ) ) ;
#70805=CARTESIAN_POINT ( 'NONE',  ( 6.036138234293757954, 0.8456279901550376454, -1.503183349252550371 ) ) ;
#70810=CARTESIAN_POINT ( 'NONE',  ( 5.096879011283717453, 1.555924861325823416, -1.037969726935553005 ) ) ;
#70811=CARTESIAN_POINT ( 'NONE',  ( 0.02993902094421736770, -1.973830418800892161, 0.3948085296872869687 ) ) ;
#70815=CARTESIAN_POINT ( 'NONE',  ( 0.9312678054614745848, -1.591333336790928366, -1.238303555203337680 ) ) ;
#70816=CARTESIAN_POINT ( 'NONE',  ( 0.8788404743438563704, -1.638286771785288254, -0.7734350870383081000 ) ) ;
#70823=CARTESIAN_POINT ( 'NONE',  ( 5.782812685692425347, 1.563071972524389786, -1.107110302061852236 ) ) ;
#70830=CARTESIAN_POINT ( 'NONE',  ( 2.536181837661064087, 1.019768383293401248, -1.906060392209196763 ) ) ;
#70834=CARTESIAN_POINT ( 'NONE',  ( 0.8617730121942971389, -1.675286201960282995, -1.300076073212981242 ) ) ;
#70835=CARTESIAN_POINT ( 'NONE',  ( 5.790036952090301448, -0.8187086143041850672, 1.631793460665123208 ) ) ;
#70836=CARTESIAN_POINT ( 'NONE',  ( 2.548066081221173729, 1.970837879163300332, 0.05219120132928834616 ) ) ;
#70837=CARTESIAN_POINT ( 'NONE',  ( 4.570513122935188299, 0.7371126809179430195, 1.764830652192488580 ) ) ;
#70840=CARTESIAN_POINT ( 'NONE',  ( 4.668383401541156275, -0.8401123053542228769, -1.781513398035587281 ) ) ;
#70841=CARTESIAN_POINT ( 'NONE',  ( 0.7615419678954943317, 0.9566914028362738520, 1.689878795569139891 ) ) ;
#70849=CARTESIAN_POINT ( 'NONE',  ( 5.356085673312771966, 0.7711821229579116643, -1.750063228584404440 ) ) ;
#70851=CARTESIAN_POINT ( 'NONE',  ( 1.413402608508182556, 1.946665536341249503, 1.039416302365432587 ) ) ;
#70853=CARTESIAN_POINT ( 'NONE',  ( 6.358070405704149941, 0.7683137238208622710, -1.860897411154702530 ) ) ;
#70857=CARTESIAN_POINT ( 'NONE',  ( 2.541538742049511246, 1.893869637037654208, -0.8368498079355383146 ) ) ;
#70861=CARTESIAN_POINT ( 'NONE',  ( 0.4093245661422850734, 1.881582470445356314, 1.064130679222355491 ) ) ;
#70868=CARTESIAN_POINT ( 'NONE',  ( 5.467320813769629417, -1.693630324315539726, -0.3718415804769247268 ) ) ;
#70870=CARTESIAN_POINT ( 'NONE',  ( 3.625891163443736520, 2.020865133175090644, -0.4488579359705275329 ) ) ;
#70871=CARTESIAN_POINT ( 'NONE',  ( 4.569977310993092345, -0.9968198436792906625, 1.867865768302608531 ) ) ;
#70876=CARTESIAN_POINT ( 'NONE',  ( 2.940244962816233265, -1.016462931258435010, 1.686739332702111405 ) ) ;
#70877=CARTESIAN_POINT ( 'NONE',  ( 0.7735182334044669039, 0.3705173918269571431, -1.875978362188877036 ) ) ;
#70878=CARTESIAN_POINT ( 'NONE',  ( 4.418134799529137346, 1.412088972526281072, -1.805610035947482039 ) ) ;
#70879=CARTESIAN_POINT ( 'NONE',  ( 2.191784710619415044, -0.7813054520266484726, 1.650194661559079456 ) ) ;
#70885=CARTESIAN_POINT ( 'NONE',  ( 2.795184176893855899, -0.1524655061851394322, -2.007514041822997086 ) ) ;
#70886=CARTESIAN_POINT ( 'NONE',  ( 3.397265449134680981, -1.732261247800225279, 0.9206733083975682241 ) ) ;
#70891=CARTESIAN_POINT ( 'NONE',  ( 6.123005977957785007, -1.968908147963293942, 0.7033269742807277680 ) ) ;
#70892=CARTESIAN_POINT ( 'NONE',  ( 5.014393912088591421, 1.219005865285277546, -1.283338120600298726 ) ) ;
#70894=CARTESIAN_POINT ( 'NONE',  ( 0.4631483011842302266, 0.2107759881739781904, -2.181290363801504650 ) ) ;
#70895=CARTESIAN_POINT ( 'NONE',  ( 0.2744473674479709913, 1.625014162249105443, -0.6237133657705071776 ) ) ;
#70898=CARTESIAN_POINT ( 'NONE',  ( 0.3339538366646053191, -1.498446967350696379, 1.742810101306817794 ) ) ;
#70899=CARTESIAN_POINT ( 'NONE',  ( 0.04676574305502099321, -1.756316032869180921, 1.310637071781264984 ) ) ;
#70900=CARTESIAN_POINT ( 'NONE',  ( 6.503290690126083184, 1.715628873550764988, 0.2497197086974659863 ) ) ;
#70901=CARTESIAN_POINT ( 'NONE',  ( 2.983271218942393332, -0.1628219013674602478, -2.200934326520533446 ) ) ;
#70902=CARTESIAN_POINT ( 'NONE',  ( 6.408646267151912213, 0.6747503738608184864, 2.063755040143978370 ) ) ;
#70904=CARTESIAN_POINT ( 'NONE',  ( 1.587271696126206111, 1.763578281176042761, 1.171447882250826522 ) ) ;
#70905=CARTESIAN_POINT ( 'NONE',  ( 3.343750000000002220, 1.895863743164157178, 0.7852924748298092394 ) ) ;
#70907=CARTESIAN_POINT ( 'NONE',  ( 6.727182134110195832, 2.427649464305783322, 2.470530574517680655 ) ) ;
#70908=CARTESIAN_POINT ( 'NONE',  ( 6.018570082959111112, 1.293320673360508488, -1.427839425051903532 ) ) ;
#70910=CARTESIAN_POINT ( 'NONE',  ( 1.541004877621090507, -1.933652123512133114, 1.230999918854805975 ) ) ;
#70914=CARTESIAN_POINT ( 'NONE',  ( 3.194184678167404368, 1.410462778303589015, 1.716012817976236171 ) ) ;
#70920=CARTESIAN_POINT ( 'NONE',  ( 1.986954140179174155, -2.015912935764123670, 0.05229865529512293942 ) ) ;
#70922=CARTESIAN_POINT ( 'NONE',  ( 6.285603487943992818, -1.943538462464271088, 0.6912672899390749359 ) ) ;
#70926=CARTESIAN_POINT ( 'NONE',  ( 6.040530583712122592, -1.465329908677007742, 0.9388326107527265041 ) ) ;
#70929=CARTESIAN_POINT ( 'NONE',  ( 1.616075582413665002, 1.193477697079999178, -1.306907023524202183 ) ) ;
#70930=CARTESIAN_POINT ( 'NONE',  ( 0.4576579978108759050, -1.899619568183811058, -0.6767110947205197125 ) ) ;
#70931=CARTESIAN_POINT ( 'NONE',  ( 0.2570343420702363435, 1.821350608449383124, -0.2692129421619017804 ) ) ;
#70932=CARTESIAN_POINT ( 'NONE',  ( 3.597495906037956992, -0.6642907406799610781, 2.194031518130711067 ) ) ;
#70933=CARTESIAN_POINT ( 'NONE',  ( 3.767381502543519112, 1.024135474229198151, 1.529801857347697025 ) ) ;
#70936=CARTESIAN_POINT ( 'NONE',  ( 4.295794115256676982, -0.6985059363485807138, 1.686860163339451990 ) ) ;
#70937=CARTESIAN_POINT ( 'NONE',  ( 5.238907797441370029, 2.013986022392059816, -0.1017483359899013229 ) ) ;
#70939=CARTESIAN_POINT ( 'NONE',  ( 2.940562510593609513, 2.245292490812002661, 0.2782218841625680450 ) ) ;
#70941=CARTESIAN_POINT ( 'NONE',  ( 0.03009625396771432870, -1.297761387203050232, -1.659265549802463546 ) ) ;
#70942=CARTESIAN_POINT ( 'NONE',  ( 3.473154722801426786, 1.870513717286937494, 0.8877811045280564750 ) ) ;
#70945=CARTESIAN_POINT ( 'NONE',  ( 5.707716976326653757, 1.605689621071492601, 1.385122894465253829 ) ) ;
#70948=CARTESIAN_POINT ( 'NONE',  ( 1.576654987853912449, -1.829214484822901055, -0.6046830185306437677 ) ) ;
#70951=CARTESIAN_POINT ( 'NONE',  ( 0.2562226757886588713, -1.969045882358761101, -0.05199970915584737480 ) ) ;
#70956=CARTESIAN_POINT ( 'NONE',  ( 0.08853117554794007193, 1.285972019905703201, 1.811169930398129013 ) ) ;
#70957=CARTESIAN_POINT ( 'NONE',  ( 3.206187942969561000, -2.103625563118251218, 0.1016139793386036383 ) ) ;
#70960=CARTESIAN_POINT ( 'NONE',  ( 0.4669691663035968054, 1.616376026143636624, 0.9223025969757200349 ) ) ;
#70965=CARTESIAN_POINT ( 'NONE',  ( 1.582450481569739331, 1.094613367649547309, 1.816135667671102016 ) ) ;
#70968=CARTESIAN_POINT ( 'NONE',  ( 3.596105239937871456, 0.8843387906064968940, -1.751336483779348585 ) ) ;
#70969=CARTESIAN_POINT ( 'NONE',  ( 2.676834871759771417, -2.068302492614528365, -0.6285112194897370941 ) ) ;
#70970=CARTESIAN_POINT ( 'NONE',  ( 1.223879446662301307, 1.774596971308094018, 0.4907264878865265634 ) ) ;
#70973=CARTESIAN_POINT ( 'NONE',  ( 3.820004643325402238, 1.653240603489447569, 0.5438404159014453843 ) ) ;
#70977=CARTESIAN_POINT ( 'NONE',  ( 0.8312129145573650124, 0.1600495679085281175, 2.155820468135719814 ) ) ;
#70978=CARTESIAN_POINT ( 'NONE',  ( 3.725935337077026510, -1.776739457207517248, -0.9528653653038119398 ) ) ;
#70981=CARTESIAN_POINT ( 'NONE',  ( 3.045733664408939223, 0.7109379216812520275, -1.838982635421481993 ) ) ;
#70982=CARTESIAN_POINT ( 'NONE',  ( 6.509000000000016328, 7.053097208480951785, 2.498154145070859311 ) ) ;
#70983=CARTESIAN_POINT ( 'NONE',  ( 2.050241756059832721, -1.499988152044306133, 1.233518166440790598 ) ) ;
#70992=CARTESIAN_POINT ( 'NONE',  ( 6.510760317505348560, 1.716126801009032032, -1.542884448788630625 ) ) ;
#70993=CARTESIAN_POINT ( 'NONE',  ( 6.478960399985357554, 1.830089090633261417, 0.7073212282268787066 ) ) ;
#70994=CARTESIAN_POINT ( 'NONE',  ( 4.399235598239510381, -1.708881994454291675, 0.9632455365647660805 ) ) ;
#70996=CARTESIAN_POINT ( 'NONE',  ( 2.162732623366144136, 1.242727809108796322, 1.587836805404294171 ) ) ;
#70998=CARTESIAN_POINT ( 'NONE',  ( 2.255205753237074617, 0.09875464746901543855, -2.115135400419057010 ) ) ;
#71002=CARTESIAN_POINT ( 'NONE',  ( 3.222423357234116992, 0.04607595322191247039, 1.840729346561786439 ) ) ;
#71006=CARTESIAN_POINT ( 'NONE',  ( 4.271814301144261528, 0.4616217191124799002, -2.069597271375968273 ) ) ;
#71009=CARTESIAN_POINT ( 'NONE',  ( 4.727839713825126466, -1.264755334911156881, -1.626962714342747196 ) ) ;
#71011=CARTESIAN_POINT ( 'NONE',  ( 2.014959344526063845, -1.785600367564584179, 0.4486904387498573676 ) ) ;
#71017=CARTESIAN_POINT ( 'NONE',  ( 2.227434312139275896, 0.001603268854937638837, 2.207063162490217056 ) ) ;
#71018=CARTESIAN_POINT ( 'NONE',  ( 3.392113076582465858, -0.9204767452889413004, 2.066876591271109120 ) ) ;
#71020=CARTESIAN_POINT ( 'NONE',  ( 3.304753640158542893, -0.3582801770840525757, -1.775609565582184191 ) ) ;
#71021=CARTESIAN_POINT ( 'NONE',  ( 3.960093407954877520, -1.098340823217320184, 1.569403885630010320 ) ) ;
#71024=CARTESIAN_POINT ( 'NONE',  ( 3.784019197727214401, -0.9729451851334305346, 1.714598810357757630 ) ) ;
#71025=CARTESIAN_POINT ( 'NONE',  ( 0.9559316444634465837, 1.924326902252432081, -0.09161688492189544453 ) ) ;
#71026=CARTESIAN_POINT ( 'NONE',  ( 5.489076674590072535, 1.649195787720953987, -0.8828566466120502110 ) ) ;
#71028=CARTESIAN_POINT ( 'NONE',  ( 3.141587237543626454, -2.035091569058588679, 1.088060180353218165 ) ) ;
#71029=CARTESIAN_POINT ( 'NONE',  ( 4.334314691326750513, -1.072585289120084440, 1.520660633866082634 ) ) ;
#71034=CARTESIAN_POINT ( 'NONE',  ( 2.244876548131835126, 0.4624279887704956238, 2.054504457251419502 ) ) ;
#71039=CARTESIAN_POINT ( 'NONE',  ( 3.410498715577559015, -2.118327196165440185, -0.1003008382433126094 ) ) ;
#71040=CARTESIAN_POINT ( 'NONE',  ( 0.6154972907393120307, 1.653649208057221598, 1.159462664468139614 ) ) ;
#71045=CARTESIAN_POINT ( 'NONE',  ( 2.390102426918311540, -0.9266024157483061519, 1.953076554623616401 ) ) ;
#71046=CARTESIAN_POINT ( 'NONE',  ( 6.610000000000010090, 0.5825982378308904863, 2.053072689460200273 ) ) ;
#71048=CARTESIAN_POINT ( 'NONE',  ( 6.925078400183553029, 6.037155338232472523, 2.550556537725846340 ) ) ;
#71049=CARTESIAN_POINT ( 'NONE',  ( 6.539320575229289112, 0.004092658091040711314, 2.003502637948689102 ) ) ;
#71051=CARTESIAN_POINT ( 'NONE',  ( 6.298064597363540074, -0.9548514761729166578, -1.776169100128288658 ) ) ;
#71053=CARTESIAN_POINT ( 'NONE',  ( 6.497611715980437630, -2.090283427287362272, 0.05178676472679385329 ) ) ;
#71055=CARTESIAN_POINT ( 'NONE',  ( 0.3743661609300020232, 1.305675439620108458, 1.847588536312362972 ) ) ;
#71062=CARTESIAN_POINT ( 'NONE',  ( 2.578358533787118212, -1.650418691300073570, -0.5013113332296408320 ) ) ;
#71064=CARTESIAN_POINT ( 'NONE',  ( 1.950134490391452369, 0.5496875458596857111, 1.682295776093334139 ) ) ;
#71065=CARTESIAN_POINT ( 'NONE',  ( 2.983067126429808091, -1.860865636787402577, -0.7683904602088088565 ) ) ;
#71067=CARTESIAN_POINT ( 'NONE',  ( 5.421004802376033993, 2.037064969303593820, 0.8491359902737596332 ) ) ;
#71071=CARTESIAN_POINT ( 'NONE',  ( 4.776102292387626846, 2.097323840013893381, -0.3118266106481304423 ) ) ;
#71072=CARTESIAN_POINT ( 'NONE',  ( 4.359000025081374297, -0.002827702239943663542, -2.016598147179492262 ) ) ;
#71076=CARTESIAN_POINT ( 'NONE',  ( 0.9361565222895779081, 1.842281575443193375, 0.3236747858033904302 ) ) ;
#71078=CARTESIAN_POINT ( 'NONE',  ( 6.041655779063732190, -1.703243848673033023, 0.6171442250446981248 ) ) ;
#71087=CARTESIAN_POINT ( 'NONE',  ( 1.433958818539453395, 1.165882187713672247, 1.577721859592796205 ) ) ;
#71091=CARTESIAN_POINT ( 'NONE',  ( 3.639029512587122372, 2.014767915268770082, 0.6618469929612482705 ) ) ;
#71094=CARTESIAN_POINT ( 'NONE',  ( 5.641858350889248364, 0.8014469270729590589, -1.801278572543635326 ) ) ;
#71096=CARTESIAN_POINT ( 'NONE',  ( 0.7385399849154888896, 1.195762776690506790, -1.619497776973168213 ) ) ;
#71098=CARTESIAN_POINT ( 'NONE',  ( 1.370887597065591823, -0.3147031148599331307, -2.093612404753260492 ) ) ;
#71100=CARTESIAN_POINT ( 'NONE',  ( 3.191909353267761151, -1.388477207968623839, -1.535938721777901472 ) ) ;
#71105=CARTESIAN_POINT ( 'NONE',  ( 4.611325087297634795, -2.050354119209703008, 0.4075000692524420876 ) ) ;
#71107=CARTESIAN_POINT ( 'NONE',  ( 3.135583521505393545, -1.224952879796761041, -1.353777129306121818 ) ) ;
#71108=CARTESIAN_POINT ( 'NONE',  ( 1.506221797076849889, -1.802732806890252837, -0.1774259793663693907 ) ) ;
#71110=CARTESIAN_POINT ( 'NONE',  ( 6.481111342790009999, -0.1036386110354891726, -2.204582208980155222 ) ) ;
#71112=CARTESIAN_POINT ( 'NONE',  ( 4.278500955059440614, -1.273273528111932063, 1.802203266693293893 ) ) ;
#71116=CARTESIAN_POINT ( 'NONE',  ( 3.088426618631805454, -1.137173348016347063, 1.537276688398482083 ) ) ;
#71121=CARTESIAN_POINT ( 'NONE',  ( 5.812113132715003516, 1.472855484078567700, -1.623034594306454137 ) ) ;
#71126=CARTESIAN_POINT ( 'NONE',  ( 3.075316773429651818, 1.777364689479765003, -0.5833007003755164011 ) ) ;
#71131=CARTESIAN_POINT ( 'NONE',  ( 0.2683110675134177669, -0.8374301267611580224, -1.781048649993026700 ) ) ;
#71132=CARTESIAN_POINT ( 'NONE',  ( 1.317982704262925520, 0.9913799330133237220, -1.755781447868165257 ) ) ;
#71136=CARTESIAN_POINT ( 'NONE',  ( 1.693587955360946529, -0.7361150630936144079, 2.064250245950305374 ) ) ;
#71137=CARTESIAN_POINT ( 'NONE',  ( 6.305291373979137859, 1.520805759102666910, 1.009792402853857185 ) ) ;
#71145=CARTESIAN_POINT ( 'NONE',  ( 3.526749072549471453, -1.699942963128863838, 0.7078653300200200560 ) ) ;
#71146=CARTESIAN_POINT ( 'NONE',  ( 0.2057266557286231146, 1.493221433009199517, 1.350316897416648843 ) ) ;
#71147=CARTESIAN_POINT ( 'NONE',  ( 2.320019640604139788, -1.777541238149564107, 1.457059784348129217 ) ) ;
#71149=CARTESIAN_POINT ( 'NONE',  ( 6.209812062937981381, 0.5727486527220859713, -1.876249287704085722 ) ) ;
#71152=CARTESIAN_POINT ( 'NONE',  ( 4.517770118113122457, -0.5046507728132009207, 1.844564425022446885 ) ) ;
#71156=CARTESIAN_POINT ( 'NONE',  ( 3.157844376090960026, 0.9421199074126384021, 1.866540799821286845 ) ) ;
#71157=CARTESIAN_POINT ( 'NONE',  ( 0.9361565222895779081, 1.842281575443193375, 0.3236747858033904302 ) ) ;
#71158=CARTESIAN_POINT ( 'NONE',  ( 1.739611019359630584, -1.913509794028777522, -0.6351045200190530426 ) ) ;
#71161=CARTESIAN_POINT ( 'NONE',  ( 2.735604107484723269, 1.727544688213778601, 0.2106955661135938018 ) ) ;
#71165=CARTESIAN_POINT ( 'NONE',  ( 3.439825841515719240, 0.7741550462027242396, -1.541462414610708764 ) ) ;
#71166=CARTESIAN_POINT ( 'NONE',  ( 3.421585747727782678, -1.306972202059282218, -1.759028276249123168 ) ) ;
#71167=CARTESIAN_POINT ( 'NONE',  ( 6.287735281038357549, 1.518688880046001444, 1.601449620450722700 ) ) ;
#71169=CARTESIAN_POINT ( 'NONE',  ( 3.819318941869216388, -1.912159422281418220, -1.028266076255865968 ) ) ;
#71170=CARTESIAN_POINT ( 'NONE',  ( 2.349991895876184511, 1.825291697999480434, 0.04531359951509549705 ) ) ;
#71171=CARTESIAN_POINT ( 'NONE',  ( 0.2331563151865486683, 0.005903526429595904942, -1.945944850731482934 ) ) ;
#71172=CARTESIAN_POINT ( 'NONE',  ( 5.067619284625084930, 1.424172025040346679, 1.566925857267987832 ) ) ;
#71175=CARTESIAN_POINT ( 'NONE',  ( 5.232074500395570205, 2.258064205686944437, 0.3942454582816708464 ) ) ;
#71177=CARTESIAN_POINT ( 'NONE',  ( 6.620655732516659064, 6.039214117936751336, 2.421170424969817603 ) ) ;
#71179=CARTESIAN_POINT ( 'NONE',  ( 0.6980877996264934771, 1.427081234210248573, 1.568565553304770877 ) ) ;
#71187=CARTESIAN_POINT ( 'NONE',  ( 4.887342357109405455, -0.6819942819097268849, -1.897698409216505233 ) ) ;
#71189=CARTESIAN_POINT ( 'NONE',  ( 3.133693747638730098, 1.960048766001153631, -0.6424893143618380931 ) ) ;
#71191=CARTESIAN_POINT ( 'NONE',  ( -0.1411974294642124317, 6.947781193150396994, -2.495311724135263809 ) ) ;
#71195=CARTESIAN_POINT ( 'NONE',  ( 6.720655732516648939, -0.004400176169771368405, 2.173773060281408487 ) ) ;
#71196=CARTESIAN_POINT ( 'NONE',  ( 4.887342357109405455, -0.6819942819097268849, -1.897698409216505233 ) ) ;
#71197=CARTESIAN_POINT ( 'NONE',  ( 3.350949008998193257, 0.4442310927498266948, -1.786741727165648497 ) ) ;
#71200=CARTESIAN_POINT ( 'NONE',  ( 0.9555556167152472469, 1.723134239262851475, -0.07815038326265508206 ) ) ;
#71202=CARTESIAN_POINT ( 'NONE',  ( 0.5636314131802122596, -1.270468259257762966, 1.915555708879124852 ) ) ;
#71204=CARTESIAN_POINT ( 'NONE',  ( 0.1813603024932753938, -0.1560989159599696641, -2.227174003853182871 ) ) ;
#71205=CARTESIAN_POINT ( 'NONE',  ( 2.842513320990670778, 2.090244732995512944, 0.2570852942500467808 ) ) ;
#71214=CARTESIAN_POINT ( 'NONE',  ( 4.289451472217206351, -0.001904023060144560469, -2.221583672334653148 ) ) ;
#71215=CARTESIAN_POINT ( 'NONE',  ( 2.765787700092982693, 1.173089151190203294, 1.850848517565194751 ) ) ;
#71218=CARTESIAN_POINT ( 'NONE',  ( 5.441838459065293065, 1.316327937319297758, 1.454900926449454124 ) ) ;
#71220=EDGE_CURVE ( 'NONE', #30003, #12895, #43548, .T. ) ;
#71224=CARTESIAN_POINT ( 'NONE',  ( 4.553055379497691568, 0.3652949536288411791, 2.088752307168060707 ) ) ;
#71228=CARTESIAN_POINT ( 'NONE',  ( 5.963787895669664607, 2.130530397400759668, -0.3648857593604309391 ) ) ;
#71230=CARTESIAN_POINT ( 'NONE',  ( 5.495603940606402560, -1.841430844871448258, 0.006098274996368944698 ) ) ;
#71233=CARTESIAN_POINT ( 'NONE',  ( 6.351467175048743918, 1.735110083250133162, -0.1355937802150069815 ) ) ;
#71237=CARTESIAN_POINT ( 'NONE',  ( 3.590839768554392908, -0.4196827604958653923, -2.120402733634827452 ) ) ;
#71241=CARTESIAN_POINT ( 'NONE',  ( 3.661132068870280420, -1.905464569931826446, -1.020879743040298271 ) ) ;
#71242=CARTESIAN_POINT ( 'NONE',  ( 4.639890180388304586, 0.8457560770286243201, -1.780867954887039417 ) ) ;
#71243=CARTESIAN_POINT ( 'NONE',  ( 3.831122626782780927, -1.165689738437695189, 1.283648893705439331 ) ) ;
#71244=CARTESIAN_POINT ( 'NONE',  ( 1.329895901633147748, 1.076045675571284166, -1.909117696414885934 ) ) ;
#71245=CARTESIAN_POINT ( 'NONE',  ( 2.327567518148494941, 0.0001997265634129384874, 2.307758715027211416 ) ) ;
#71246=CARTESIAN_POINT ( 'NONE',  ( 3.216142984300340846, -1.012526663717785214, -1.794778392713367587 ) ) ;
#71247=CARTESIAN_POINT ( 'NONE',  ( 5.776890131463271238, 1.792767593593114439, -0.7471807142077312447 ) ) ;
#71256=CARTESIAN_POINT ( 'NONE',  ( 3.505080564089088746, 1.740947047783932611, -1.355986173033681075 ) ) ;
#71259=CARTESIAN_POINT ( 'NONE',  ( 1.111883761159220496, 1.859168010044176311, -0.08395930885315286418 ) ) ;
#71260=CARTESIAN_POINT ( 'NONE',  ( -0.02900071798683095947, 5.719935618195115978, -2.767867108847458901 ) ) ;
#71263=CARTESIAN_POINT ( 'NONE',  ( 6.825078400183582694, 7.052246674313852992, 2.642498189888539795 ) ) ;
#71264=CARTESIAN_POINT ( 'NONE',  ( 6.509700743154069436, -0.8726169035938921015, -1.621212818125779220 ) ) ;
#71266=CARTESIAN_POINT ( 'NONE',  ( 3.168876024238317601, -1.903602637213364979, -0.7901525784780991657 ) ) ;
#71269=CARTESIAN_POINT ( 'NONE',  ( 0.07680821025391608436, 0.2560392329899116026, -1.846278364303982178 ) ) ;
#71272=CARTESIAN_POINT ( 'NONE',  ( 2.430605206563386300, 1.998658846558550195, 0.5020661504441750189 ) ) ;
#71277=CARTESIAN_POINT ( 'NONE',  ( 5.426482453889071245, 1.317083479513626587, -1.770629405693980640 ) ) ;
#71278=CARTESIAN_POINT ( 'NONE',  ( 0.6499751493908960676, 0.6786997614584532323, -2.052318101833712660 ) ) ;
#71280=CARTESIAN_POINT ( 'NONE',  ( 0.2336117360935245635, 0.6279853779636718203, -1.916355031878452797 ) ) ;
#71281=CARTESIAN_POINT ( 'NONE',  ( 1.494008433901512278, 2.215370577347621328, 0.6118545706256629524 ) ) ;
#71284=CARTESIAN_POINT ( 'NONE',  ( 6.199862383955294654, 1.322219258337012704, 1.381733411008022383 ) ) ;
#71286=CARTESIAN_POINT ( 'NONE',  ( 1.709613803025863188, -1.856884215550944850, 0.2259493607114013147 ) ) ;
#71287=CARTESIAN_POINT ( 'NONE',  ( 3.415250174187448362, -1.861344788686780438, 0.7762291900053899241 ) ) ;
#71291=CARTESIAN_POINT ( 'NONE',  ( 4.934254457356054502, 1.083321712992061814, -1.805932085151832789 ) ) ;
#71296=CARTESIAN_POINT ( 'NONE',  ( 4.289322773248661846, -0.004189350761124934451, -2.019972750201783906 ) ) ;
#71298=CARTESIAN_POINT ( 'NONE',  ( 6.830530959611283315, -1.272493244265305634, 1.624195267664030995 ) ) ;
#71300=CARTESIAN_POINT ( 'NONE',  ( 5.220075184997099882, -1.151474455836385857, -1.829185309946822713 ) ) ;
#71306=CARTESIAN_POINT ( 'NONE',  ( 2.594372030776093574, 1.025359171358769306, -1.913825152921688311 ) ) ;
#71309=CARTESIAN_POINT ( 'NONE',  ( 1.856743374925871715, 0.3135980649527739250, -1.814175028193690808 ) ) ;
#71312=CARTESIAN_POINT ( 'NONE',  ( 3.720431430916489646, 2.081484170424623859, 0.6860852429351402826 ) ) ;
#71313=CARTESIAN_POINT ( 'NONE',  ( 6.983263157960363010, 6.034173670577698267, 2.748703042679788044 ) ) ;
#71314=CARTESIAN_POINT ( 'NONE',  ( 4.241306175801488720, -1.970289653591940970, 1.112044505652502346 ) ) ;
#71321=CARTESIAN_POINT ( 'NONE',  ( 5.483597806724121781, 1.189268614677735592, 1.310771863001722437 ) ) ;
#71323=CARTESIAN_POINT ( 'NONE',  ( 1.360533241671294746, 0.8531190763820644118, 1.925603555557230617 ) ) ;
#71326=CARTESIAN_POINT ( 'NONE',  ( 1.715229078707868782, -1.687648322675440626, -1.015142298990583614 ) ) ;
#71329=CARTESIAN_POINT ( 'NONE',  ( 5.677939507029830857, 1.783257022268599723, -0.3182440143107477248 ) ) ;
#71334=CARTESIAN_POINT ( 'NONE',  ( 5.067206508511894469, 0.1826785619755930679, -1.861722072867748823 ) ) ;
#71335=CARTESIAN_POINT ( 'NONE',  ( 5.102424979711988051, 2.064335680360945169, 0.1577259720206558580 ) ) ;
#71346=CARTESIAN_POINT ( 'NONE',  ( 4.650807877244386823, -0.4278111053654386486, -1.914496481071884970 ) ) ;
#71348=CARTESIAN_POINT ( 'NONE',  ( 1.950545848857932807, 1.388271641964162084, 1.462223312268404074 ) ) ;
#71350=CARTESIAN_POINT ( 'NONE',  ( 2.342874207364954220, -1.669023557642179467, -0.9401844802782586275 ) ) ;
#71352=CARTESIAN_POINT ( 'NONE',  ( 0.4334776158547505864, -1.553986563932317377, -1.545601477622601472 ) ) ;
#71353=CARTESIAN_POINT ( 'NONE',  ( 6.539320575229252697, 0.01001626003939219342, 1.796977979958066518 ) ) ;
#71354=CARTESIAN_POINT ( 'NONE',  ( 2.424885678431305092, -0.004389691185376768875, 1.870726058193001196 ) ) ;
#71356=CARTESIAN_POINT ( 'NONE',  ( 4.429943789601535009, -1.973532241649661678, 0.3969061482532297291 ) ) ;
#71359=CARTESIAN_POINT ( 'NONE',  ( 4.657876698301413043, 1.220176935102987636, 1.730081886799080593 ) ) ;
#71361=CARTESIAN_POINT ( 'NONE',  ( 5.828598057497599960, -1.316348130051235410, 1.597988563933512074 ) ) ;
#71362=CARTESIAN_POINT ( 'NONE',  ( 1.153981415136243527, 0.8505622500237058903, 1.910110313709513674 ) ) ;
#71363=CARTESIAN_POINT ( 'NONE',  ( 6.720655732516624070, 2.949086357957014570, 2.625980845328681923 ) ) ;
#71364=CARTESIAN_POINT ( 'NONE',  ( 6.616225513087798049, -0.8637638766970030524, -1.608286988965562214 ) ) ;
#71372=CARTESIAN_POINT ( 'NONE',  ( 0.8381711186948238579, 1.079942214367535680, -1.454201162973115524 ) ) ;
#71383=CARTESIAN_POINT ( 'NONE',  ( 6.538686444676896414, -1.556836737174282836, 1.281159629702780078 ) ) ;
#71389=CARTESIAN_POINT ( 'NONE',  ( 3.502752968683011225, 0.4741538486671539876, 1.911403532405174133 ) ) ;
#71390=CARTESIAN_POINT ( 'NONE',  ( 4.306267660493944049, 1.238306454277863677, -1.591331080693689781 ) ) ;
#71394=CARTESIAN_POINT ( 'NONE',  ( 4.822331674454460426, 2.096538211656114647, 0.6379635903819569354 ) ) ;
#71396=CARTESIAN_POINT ( 'NONE',  ( 3.504829168241951898, 1.519505285488613744, -1.184012928881588822 ) ) ;
#71398=CARTESIAN_POINT ( 'NONE',  ( -0.1296875068448125057, 7.629137130509072939, -2.426516348560475933 ) ) ;
#71399=CARTESIAN_POINT ( 'NONE',  ( 0.06543086261080394150, -1.973449318085427340, -0.9880335165917543128 ) ) ;
#71403=CARTESIAN_POINT ( 'NONE',  ( 5.137539950512164388, 1.839066438578255136, -0.7051811603524612559 ) ) ;
#71405=CARTESIAN_POINT ( 'NONE',  ( 0.3451281418221859854, 0.6079892978090885025, -1.844522312511005957 ) ) ;
#71406=CARTESIAN_POINT ( 'NONE',  ( 4.459639246686514902, -1.557681092447872784, -1.275236256583739403 ) ) ;
#71407=CARTESIAN_POINT ( 'NONE',  ( 5.694729993868760332, -1.451380474000956156, -1.782189233907914838 ) ) ;
#71409=CARTESIAN_POINT ( 'NONE',  ( 3.326847623520872155, -1.717698991579403422, -0.7164791247627964044 ) ) ;
#71416=CARTESIAN_POINT ( 'NONE',  ( 6.093324021728765416, -0.7037842761165017391, 1.968882989559454622 ) ) ;
#71421=CARTESIAN_POINT ( 'NONE',  ( -0.005637892868452093476, -0.3948761927005627337, -1.788892068844874395 ) ) ;
#71423=CARTESIAN_POINT ( 'NONE',  ( 2.232704217388951751, 1.733830997258398066, 0.04099941454244887540 ) ) ;
#71425=CARTESIAN_POINT ( 'NONE',  ( 6.509000000000037645, 2.054060622569788386, 2.307050226316338382 ) ) ;
#71428=CARTESIAN_POINT ( 'NONE',  ( 0.4442981077158770775, -0.9790059121952739973, 1.824179074426744762 ) ) ;
#71429=CARTESIAN_POINT ( 'NONE',  ( 5.162654993523497993, -1.319871331358621669, 1.261628347558927166 ) ) ;
#71430=CARTESIAN_POINT ( 'NONE',  ( 3.326955106232618586, -1.810811308836293598, -0.7551016064811162387 ) ) ;
#71434=CARTESIAN_POINT ( 'NONE',  ( 3.826904873358004888, 1.498484187726952799, -1.500593194838243605 ) ) ;
#71438=CARTESIAN_POINT ( 'NONE',  ( 1.288034235163344254, -1.310400469390052836, -1.602789277989056238 ) ) ;
#71441=CARTESIAN_POINT ( 'NONE',  ( 4.565202069552391606, -1.784334575089935981, 1.322790477621762051 ) ) ;
#71443=CARTESIAN_POINT ( 'NONE',  ( 1.389710824352110574, -0.8328434156393785814, -2.142668459815112669 ) ) ;
#71445=CARTESIAN_POINT ( 'NONE',  ( 0.4792544977638459880, -0.1021076105021078151, 1.959249876678282209 ) ) ;
#71449=CARTESIAN_POINT ( 'NONE',  ( 6.321814700078944860, 1.054209175812788502, -1.509406368332133930 ) ) ;
#71451=CARTESIAN_POINT ( 'NONE',  ( 2.865378420500460876, -1.565876230000915692, -1.097592462808501645 ) ) ;
#71453=CARTESIAN_POINT ( 'NONE',  ( 3.680403716343355836, -1.662106674541915075, -0.4603510507015916020 ) ) ;
#71454=CARTESIAN_POINT ( 'NONE',  ( 2.589077643123653072, 1.706113014995232380, 1.074661422923957055 ) ) ;
#71455=CARTESIAN_POINT ( 'NONE',  ( 3.692236332591435577, 1.971970683719068695, 1.181021729054130054 ) ) ;
#71456=CARTESIAN_POINT ( 'NONE',  ( 3.163607282743227334, 0.3354078767881124024, -2.237311900363625483 ) ) ;
#71457=CARTESIAN_POINT ( 'NONE',  ( 6.568975480045090798, -1.924755568788787397, -0.8553139683228675461 ) ) ;
#71459=CARTESIAN_POINT ( 'NONE',  ( 4.358513420383302694, -1.312205524322278549, 1.187683162289454142 ) ) ;
#71461=CARTESIAN_POINT ( 'NONE',  ( 1.148812421071528256, -1.804313360470580108, 1.413740901141118611 ) ) ;
#71462=CARTESIAN_POINT ( 'NONE',  ( 5.560457619783242933, -1.666209093894938764, -0.7835883864039174806 ) ) ;
#71464=CARTESIAN_POINT ( 'NONE',  ( 6.140607899229071798, -1.853288307406484536, 1.169240172944140621 ) ) ;
#71468=CARTESIAN_POINT ( 'NONE',  ( 5.371561628297467195, -0.3073141173523045167, 2.047320497149993646 ) ) ;
#71469=CARTESIAN_POINT ( 'NONE',  ( 1.024625454658374624, 0.3981145430279106057, 1.976669095394629982 ) ) ;
#71472=CARTESIAN_POINT ( 'NONE',  ( 4.705647360784301014, -0.5120751438620478879, 1.857136557572524715 ) ) ;
#71475=CARTESIAN_POINT ( 'NONE',  ( 1.037687956146810198, -0.04753379745526563338, 2.221059295257783006 ) ) ;
#71483=CARTESIAN_POINT ( 'NONE',  ( 4.634162599488286460, 0.3036646131651790093, 1.713576892981442557 ) ) ;
#71484=CARTESIAN_POINT ( 'NONE',  ( 2.031626174157370457, 1.878314540015123102, -0.5664888411779643862 ) ) ;
#71489=AXIS2_PLACEMENT_3D ( 'NONE', #73368, #105932, #124361 ) ;
#71490=CARTESIAN_POINT ( 'NONE',  ( 6.180128940399614912, -1.088687182605744042, -1.631870318916525120 ) ) ;
#71493=CARTESIAN_POINT ( 'NONE',  ( 4.891814693739657827, -2.006371927678828104, 0.2024599332275459629 ) ) ;
#71495=CARTESIAN_POINT ( 'NONE',  ( 0.7435140528431654072, -1.938958340150579662, 1.165708873083745045 ) ) ;
#71499=CARTESIAN_POINT ( 'NONE',  ( 1.264687732342294701, -1.688641954842164283, -0.8049673154429252131 ) ) ;
#71500=CARTESIAN_POINT ( 'NONE',  ( 0.7383815455153321938, 1.732312080274291732, -0.08293238807991276662 ) ) ;
#71502=CARTESIAN_POINT ( 'NONE',  ( 3.737968522918270864, 2.181131050170285857, 0.2133239450496857148 ) ) ;
#71503=CARTESIAN_POINT ( 'NONE',  ( 5.385860071389879877, 1.544758419828775153, 1.714431625121175751 ) ) ;
#71504=CARTESIAN_POINT ( 'NONE',  ( 0.6025036485793239249, -0.6938342907959176298, -1.940726168717278322 ) ) ;
#71505=CARTESIAN_POINT ( 'NONE',  ( 2.958853767740171392, 0.2844919188511252917, -1.920881014358867489 ) ) ;
#71509=CARTESIAN_POINT ( 'NONE',  ( 2.971327447312217984, -1.987046587055636637, -0.3419355124290662240 ) ) ;
#71513=CARTESIAN_POINT ( 'NONE',  ( 1.295219883412350503, 1.381147610352757127, 1.194082977437810333 ) ) ;
#71519=CARTESIAN_POINT ( 'NONE',  ( 6.350472301779563900, 0.6441285046014081361, 1.957720813820832850 ) ) ;
#71524=CARTESIAN_POINT ( 'NONE',  ( 5.356120063770971385, 0.8164924478912498618, -1.847455861782754782 ) ) ;
#71525=CARTESIAN_POINT ( 'NONE',  ( 5.479204513921561492, -2.007303783262293972, -0.9515056986081956714 ) ) ;
#71529=CARTESIAN_POINT ( 'NONE',  ( 5.120021580010623907, -1.100570584753908454, -1.742215132906791641 ) ) ;
#71530=CARTESIAN_POINT ( 'NONE',  ( 3.902970337090125419, -1.038992709432768891, -1.728002613881730376 ) ) ;
#71538=CARTESIAN_POINT ( 'NONE',  ( 4.376327261493318410, -0.3474131038204917310, 1.985796694155849362 ) ) ;
#71539=CARTESIAN_POINT ( 'NONE',  ( 3.081803158279991628, -1.813988701161291628, -0.3140598505507880556 ) ) ;
#71541=CARTESIAN_POINT ( 'NONE',  ( 2.526355290359350025, -1.329941221805782892, -1.885751665715528880 ) ) ;
#71543=CARTESIAN_POINT ( 'NONE',  ( 3.198656860129048152, -0.6241516536032962748, -2.069545307505623821 ) ) ;
#71551=CARTESIAN_POINT ( 'NONE',  ( 2.377632874612686020, 1.149002834218125102, 1.476114537088555112 ) ) ;
#71552=CARTESIAN_POINT ( 'NONE',  ( 0.6144489392437714192, 1.362578290646492718, -1.424861684082868063 ) ) ;
#71555=CARTESIAN_POINT ( 'NONE',  ( 1.823171247573553311, 2.059948494222668014, 0.7922594597074559264 ) ) ;
#71556=ORIENTED_EDGE ( 'NONE', *, *, #135726, .F. ) ;
#71562=CARTESIAN_POINT ( 'NONE',  ( 6.034049845351773023, 0.9722699467793812778, -1.714982496439126924 ) ) ;
#71563=CARTESIAN_POINT ( 'NONE',  ( 6.006511608602003172, -0.8246739634825739351, -2.155485180906725251 ) ) ;
#71564=CARTESIAN_POINT ( 'NONE',  ( 0.7308173252688826560, -1.846041318942293286, -0.6644482084196751126 ) ) ;
#71565=CARTESIAN_POINT ( 'NONE',  ( 3.625881544801349055, 2.013384979781565942, -0.4471371585693607598 ) ) ;
#71572=CARTESIAN_POINT ( 'NONE',  ( 5.986835238096758438, 2.090873126042319896, 0.5847848357620232251 ) ) ;
#71574=CARTESIAN_POINT ( 'NONE',  ( 4.774869596704574448, 1.716175909155163382, -0.6674964387535023969 ) ) ;
#71576=CARTESIAN_POINT ( 'NONE',  ( 6.110890996357365879, -0.2699588104537915534, 2.174781792473476472 ) ) ;
#71582=CARTESIAN_POINT ( 'NONE',  ( 1.920411955722916453, 1.650032497218676397, 0.6405850872945593188 ) ) ;
#71583=CARTESIAN_POINT ( 'NONE',  ( 6.428391161641624940, -0.9511404050406097044, -1.774240594045069841 ) ) ;
#71585=CARTESIAN_POINT ( 'NONE',  ( 3.919475720687201736, -1.323675617205988475, -1.384941642318695987 ) ) ;
#71587=CARTESIAN_POINT ( 'NONE',  ( 5.406690398188211510, 0.5700869393594419909, 1.885254869494409791 ) ) ;
#71588=CARTESIAN_POINT ( 'NONE',  ( 0.3695850531008069706, -1.794773754367712693, -1.129184308951653781 ) ) ;
#71590=CARTESIAN_POINT ( 'NONE',  ( 2.764352523130030548, -1.291370965961564421, 1.353630663414123969 ) ) ;
#71591=CARTESIAN_POINT ( 'NONE',  ( 6.621745524129793559, -1.670984818007285266, 0.4274731708342211500 ) ) ;
#71593=CARTESIAN_POINT ( 'NONE',  ( 3.141465813989018141, -1.946189201368169641, 1.040519825639886431 ) ) ;
#71596=CARTESIAN_POINT ( 'NONE',  ( 1.064971659385913316, 1.563282549206745475, -1.345778378556292676 ) ) ;
#71603=CARTESIAN_POINT ( 'NONE',  ( 3.367693471486675083, -0.4065805204805824635, 2.029877954327436118 ) ) ;
#71607=CARTESIAN_POINT ( 'NONE',  ( 0.5572930201490761126, -1.731111387009228952, 1.040124062761533352 ) ) ;
#71610=CARTESIAN_POINT ( 'NONE',  ( 0.1745949693968693039, 7.629137130509094256, -2.355306170041113756 ) ) ;
#71612=CARTESIAN_POINT ( 'NONE',  ( 6.028672669474048007, 1.986741788447304646, -0.3418859329693338944 ) ) ;
#71613=CARTESIAN_POINT ( 'NONE',  ( 5.717977451880697615, 0.9379096786080630688, -1.670315906950563534 ) ) ;
#71615=CARTESIAN_POINT ( 'NONE',  ( 3.562233144267571650, -1.470601008620987749, 1.625073949779440419 ) ) ;
#71618=CARTESIAN_POINT ( 'NONE',  ( 2.636851627972558454, 1.802111047976437508, 0.6404684511054498097 ) ) ;
#71622=CARTESIAN_POINT ( 'NONE',  ( 0.8082205221912192039, 1.198841770460257194, -1.621197638953228548 ) ) ;
#71624=CARTESIAN_POINT ( 'NONE',  ( 6.023007056224171762, -2.064090639567913499, 0.7368321019862942300 ) ) ;
#71626=CARTESIAN_POINT ( 'NONE',  ( 3.574969364760666846, 0.04275877055364904478, -1.724416222950067690 ) ) ;
#71628=CARTESIAN_POINT ( 'NONE',  ( 0.1399997263886037790, 2.025166351305721868, -2.415484119839182320 ) ) ;
#71631=DIRECTION ( 'NONE',  ( 2.949029909160572061E-17, 1.000000000000000000, -8.673600428462616880E-15 ) ) ;
#71632=CARTESIAN_POINT ( 'NONE',  ( 0.4495626703563436743, 1.451167377975391304, 1.320406988977901985 ) ) ;
#71639=CARTESIAN_POINT ( 'NONE',  ( 3.668453237830204827, 0.6552377326864079476, 1.688991677562341920 ) ) ;
#71643=CARTESIAN_POINT ( 'NONE',  ( 4.477109312160544974, -1.620259271022955305, -0.8101795318041657978 ) ) ;
#71646=CARTESIAN_POINT ( 'NONE',  ( 5.441811508714582857, 1.250024229543914567, 1.378945535785504051 ) ) ;
#71648=CARTESIAN_POINT ( 'NONE',  ( 3.233901216830310954, 1.915793140838128572, -0.003097617167701141160 ) ) ;
#71649=CARTESIAN_POINT ( 'NONE',  ( 6.777182134110200096, 7.629137130509070275, 2.410944104600750038 ) ) ;
#71657=CARTESIAN_POINT ( 'NONE',  ( 1.007895156502825573, -0.9414231642565270564, -1.866751856443664037 ) ) ;
#71659=CARTESIAN_POINT ( 'NONE',  ( 6.053727987682750999, 0.5585614288021992779, -1.843621721047507878 ) ) ;
#71661=CARTESIAN_POINT ( 'NONE',  ( 2.907047201455061014, 1.541221212934189344, 0.9781624729086123571 ) ) ;
#71663=CARTESIAN_POINT ( 'NONE',  ( 2.408343312057196872, -1.907530749141531423, -0.1368029246449145864 ) ) ;
#71664=CARTESIAN_POINT ( 'NONE',  ( 1.750388463564346075, -1.959780499145358679, -0.1960735186044142708 ) ) ;
#71665=CARTESIAN_POINT ( 'NONE',  ( 3.403789896209925114, -0.7897705758606025084, -1.774406015287466332 ) ) ;
#71670=CARTESIAN_POINT ( 'NONE',  ( 3.726904977748810133, 1.497142547446396410, -1.502090761940577002 ) ) ;
#71679=CARTESIAN_POINT ( 'NONE',  ( 3.404746562951189937, 1.438594061741470753, -1.123979961188771304 ) ) ;
#71680=CARTESIAN_POINT ( 'NONE',  ( 0.1333692844072559280, 0.001398348041498076455, -2.053671342968105051 ) ) ;
#71685=CARTESIAN_POINT ( 'NONE',  ( 4.627732503263369601, -1.150995203733524930, -1.474563928533303869 ) ) ;
#71687=CARTESIAN_POINT ( 'NONE',  ( 2.402848698864976207, 1.547341197487204001, -1.147474368762817498 ) ) ;
#71688=CARTESIAN_POINT ( 'NONE',  ( 6.403176761927252159, -1.659045864033869666, 1.046607237317781269 ) ) ;
#71695=CARTESIAN_POINT ( 'NONE',  ( 0.7204975843347528608, 2.086673352822054461, 0.3575386888887230885 ) ) ;
#71699=CARTESIAN_POINT ( 'NONE',  ( 5.682505902380680318, 1.237739610710282046, -1.659335868388504220 ) ) ;
#71700=CARTESIAN_POINT ( 'NONE',  ( 0.1867156058280826092, 1.363667594142993877, 1.237386390646778578 ) ) ;
#71702=CARTESIAN_POINT ( 'NONE',  ( 5.432396523169654934, -1.810675156642663541, -1.416092387804610553 ) ) ;
#71705=CARTESIAN_POINT ( 'NONE',  ( 0.9203736287852108955, 1.361359823012283865, -1.844092865855660124 ) ) ;
#71708=CARTESIAN_POINT ( 'NONE',  ( 5.349535142863500070, 1.939630122921351729, -0.09734604192479337503 ) ) ;
#71709=ORIENTED_EDGE ( 'NONE', *, *, #175445, .T. ) ;
#71712=CARTESIAN_POINT ( 'NONE',  ( 6.170165192347925931, 1.906784905861274693, -0.1475879885542986936 ) ) ;
#71713=CARTESIAN_POINT ( 'NONE',  ( 5.173064673083394460, 1.776168143800487043, -0.9548534231369476544 ) ) ;
#71717=CARTESIAN_POINT ( 'NONE',  ( 2.220754083240178645, 0.001034992482759621978, 2.090823719040376893 ) ) ;
#71718=CARTESIAN_POINT ( 'NONE',  ( 1.744620744215353625, -1.497317806218407599, 0.9432750629611782456 ) ) ;
#71721=CARTESIAN_POINT ( 'NONE',  ( 3.662334778960428139, -1.540015086033737601, 1.698051401694438800 ) ) ;
#71722=B_SPLINE_CURVE_WITH_KNOTS ( 'NONE', 3,
 ( #174172, #140617, #96116, #125479, #25744, #161097, #78762, #76633, #124416, #190375, #209820 ),
 .UNSPECIFIED., .F., .F.,
 ( 4, 1, 1, 1, 1, 1, 1, 1, 4 ),
 ( 0.000000000000000000, 0.2255619619413396781, 0.3975297875667437308, 0.5250373104567740423, 0.6172314665434700531, 0.6832587661106447330, 0.7322037845459880012, 0.7729093456892226488, 1.000000000000000000 ),
 .UNSPECIFIED. ) ;
#71723=CARTESIAN_POINT ( 'NONE',  ( 2.431276410161122392, 0.8208083392724160321, -1.534589408508793440 ) ) ;
#71726=CARTESIAN_POINT ( 'NONE',  ( 2.231429653443087080, -1.583367121652721421, -0.7069697159475217818 ) ) ;
#71727=CARTESIAN_POINT ( 'NONE',  ( 2.945941647375094785, 1.533668492858210497, 1.537084210998492795 ) ) ;
#71729=CARTESIAN_POINT ( 'NONE',  ( 5.085172837459294826, 1.651341431264556014, 1.157102043685846793 ) ) ;
#71730=CARTESIAN_POINT ( 'NONE',  ( 1.500000000000001110, -8.632537233970167800E-14, -2.052068128417951165 ) ) ;
#71732=CARTESIAN_POINT ( 'NONE',  ( 0.6922523098862876090, -1.911435030786556855, -0.2391616053641909545 ) ) ;
#71734=CARTESIAN_POINT ( 'NONE',  ( 4.236746486948286261, 1.365021424349493584, -1.752494286840690085 ) ) ;
#71735=VERTEX_POINT ( 'NONE', #154692 ) ;
#71736=CARTESIAN_POINT ( 'NONE',  ( -0.2106854629475062024, 1.349218558350977260, -2.248994321313985800 ) ) ;
#71741=CARTESIAN_POINT ( 'NONE',  ( 0.6455721646590365514, 0.1693206843514388493, 2.214916916779915201 ) ) ;
#71742=CARTESIAN_POINT ( 'NONE',  ( 5.582460749670235423, 1.169929261559121247, -1.574690175210855747 ) ) ;
#71745=CARTESIAN_POINT ( 'NONE',  ( 0.2456851981432126020, -1.670693100197045977, -1.371219901248825535 ) ) ;
#71747=CARTESIAN_POINT ( 'NONE',  ( 3.314939881033797331, -1.563807569242671613, 1.345168064507019423 ) ) ;
#71751=CARTESIAN_POINT ( 'NONE',  ( 4.973830807571049561, 1.075732564348480746, 1.530087412091485799 ) ) ;
#71752=CARTESIAN_POINT ( 'NONE',  ( 3.428057853464313798, -1.315526611184931527, -1.130013928329278494 ) ) ;
#71753=CARTESIAN_POINT ( 'NONE',  ( 3.210250486799534286, 1.574880741971116827, 0.7411356085459307463 ) ) ;
#71754=CARTESIAN_POINT ( 'NONE',  ( 0.6621918981609349331, 1.136352663792916662, 1.990853321008963395 ) ) ;
#71756=CARTESIAN_POINT ( 'NONE',  ( 4.898031494525131535, -0.7058569028579181337, -1.968109489924846356 ) ) ;
#71757=CARTESIAN_POINT ( 'NONE',  ( 6.597608361038971303, -1.941456323438792042, 0.05037571119943275166 ) ) ;
#71760=CARTESIAN_POINT ( 'NONE',  ( 0.4049229342097167006, -1.081068455937021611, -1.701946057285643743 ) ) ;
#71761=CARTESIAN_POINT ( 'NONE',  ( 1.318772358905948794, -0.7683209907942339933, -1.976687055281033611 ) ) ;
#71766=CARTESIAN_POINT ( 'NONE',  ( 2.104293207771616991, -0.9040658786637757460, 1.918231223523607865 ) ) ;
#71768=CARTESIAN_POINT ( 'NONE',  ( 4.600122369450095228, -1.825375079466069694, -0.04201004182294298950 ) ) ;
#71775=CARTESIAN_POINT ( 'NONE',  ( 1.863541707127059688, -1.624685865379692506, -1.199789887509305597 ) ) ;
#71776=CARTESIAN_POINT ( 'NONE',  ( 5.948300505803370442, 2.203960110721484789, 0.1139900122707343255 ) ) ;
#71778=CARTESIAN_POINT ( 'NONE',  ( 4.539814342829402882, 1.213294893355709503, 1.411164879910733472 ) ) ;
#71784=CARTESIAN_POINT ( 'NONE',  ( 4.529811765687052016, -1.125283923072720071, -1.437579299059896343 ) ) ;
#71788=CARTESIAN_POINT ( 'NONE',  ( 0.4383029422423733168, 0.9912079340955775031, 1.422354019259955304 ) ) ;
#71789=CARTESIAN_POINT ( 'NONE',  ( 0.1283017097272065865, -1.593451896579937355, 0.7002181395190426594 ) ) ;
#71790=CARTESIAN_POINT ( 'NONE',  ( 5.567085169132608868, -2.083932277878234096, -0.9915751667191848862 ) ) ;
#71792=CARTESIAN_POINT ( 'NONE',  ( 0.9837496482606482573, 1.382075509872608299, 1.528818673835147024 ) ) ;
#71795=CARTESIAN_POINT ( 'NONE',  ( 6.520923251934013898, 2.292922446452568597, -0.1593734864932250250 ) ) ;
#71798=CARTESIAN_POINT ( 'NONE',  ( 6.192256348250350761, -1.861847689568534081, -0.1814220289034565448 ) ) ;
#71801=CARTESIAN_POINT ( 'NONE',  ( 3.234525475359388391, 1.209690070866603406, -1.481213593849866950 ) ) ;
#71803=CARTESIAN_POINT ( 'NONE',  ( 5.514374426699260923, -0.9893691592960799364, -1.972764877262770833 ) ) ;
#71808=CARTESIAN_POINT ( 'NONE',  ( 5.725269513181780567, 1.870077439114096629, 0.9995941271150191598 ) ) ;
#71809=CARTESIAN_POINT ( 'NONE',  ( 2.679136956247138546, -2.208066087050132520, -0.6703273527271095267 ) ) ;
#71810=CARTESIAN_POINT ( 'NONE',  ( 3.648837080137564470, -0.3802854374791163616, -1.924481129451253603 ) ) ;
#71812=CARTESIAN_POINT ( 'NONE',  ( 0.7253527386562284018, 0.1980078388067410544, -1.951770168129369543 ) ) ;
#71816=CARTESIAN_POINT ( 'NONE',  ( 5.700407750362016301, 1.350738941191354625, -1.497498989668680114 ) ) ;
#71817=CARTESIAN_POINT ( 'NONE',  ( 0.1812672858593766811, -0.8707521589867758260, 1.622202602641155345 ) ) ;
#71819=CARTESIAN_POINT ( 'NONE',  ( 3.485384773837760353, 0.04839624821431457585, 2.170676210889192603 ) ) ;
#71821=CARTESIAN_POINT ( 'NONE',  ( 0.6684183810189650021, 2.117893379942568988, -0.1100008709709817956 ) ) ;
#71827=CARTESIAN_POINT ( 'NONE',  ( 1.458354148090333258, 0.8324554894755629153, 1.885337613027091352 ) ) ;
#71833=CARTESIAN_POINT ( 'NONE',  ( 3.264218543254516103, 1.912461472423479192, -0.002497826895729581952 ) ) ;
#71834=AXIS2_PLACEMENT_3D ( 'NONE', #6265, #72336, #116899 ) ;
#71835=CARTESIAN_POINT ( 'NONE',  ( 5.840640841166978348, 0.3488620263497018703, 1.734928340252988033 ) ) ;
#71838=CARTESIAN_POINT ( 'NONE',  ( 0.6503002719215627003, 1.784868618687754926, 0.3088405841149675091 ) ) ;
#71841=CARTESIAN_POINT ( 'NONE',  ( 0.5674276921618210956, 1.288973137450568407, 1.417358193720698933 ) ) ;
#71842=CARTESIAN_POINT ( 'NONE',  ( 1.979048004138800998, 1.930994533390210544, 0.7472069620131777112 ) ) ;
#71845=CARTESIAN_POINT ( 'NONE',  ( 6.631728656526095556, -1.223761959379562114, -1.414937998750566361 ) ) ;
#71846=CARTESIAN_POINT ( 'NONE',  ( 2.912524513316586461, 1.322148455168963510, -1.259233298254287536 ) ) ;
#71847=CARTESIAN_POINT ( 'NONE',  ( 0.06561565146986823860, -2.064482179495107150, -1.031447015078267304 ) ) ;
#71850=CARTESIAN_POINT ( 'NONE',  ( 3.824720269693319796, -1.387356309220557193, 1.526538889744559313 ) ) ;
#71854=CARTESIAN_POINT ( 'NONE',  ( 0.4214394802095830506, -0.1064560406111268731, 2.159113264384164399 ) ) ;
#71856=CARTESIAN_POINT ( 'NONE',  ( 0.1862956123577602652, -1.336862347539343965, -1.711682565949741885 ) ) ;
#71858=CARTESIAN_POINT ( 'NONE',  ( 3.567792053227138105, 2.109782723108716063, -0.4697668898906853796 ) ) ;
#71859=CARTESIAN_POINT ( 'NONE',  ( 3.985024733980116363, -1.885273983189727831, -0.7249480779877092163 ) ) ;
#71864=CARTESIAN_POINT ( 'NONE',  ( 2.272673044126482189, -0.3494851828299732621, -1.985868527484459634 ) ) ;
#71869=CARTESIAN_POINT ( 'NONE',  ( 5.871340715825056122, -1.643613990083541143, -0.9773822251149253404 ) ) ;
#71873=CARTESIAN_POINT ( 'NONE',  ( 3.989861366179075386, -2.010826228832915508, 0.1511578083489423796 ) ) ;
#71876=CARTESIAN_POINT ( 'NONE',  ( 6.194358799569198659, -1.717016665659231167, -0.1635641229304989064 ) ) ;
#71881=CARTESIAN_POINT ( 'NONE',  ( 5.589076619078012342, 1.650032040524500143, -0.8810306647013477210 ) ) ;
#71882=CARTESIAN_POINT ( 'NONE',  ( -0.1047997906430510606, -0.1421793342430139606, -1.981047221590222840 ) ) ;
#71884=CARTESIAN_POINT ( 'NONE',  ( 1.920843890195075510, -1.466934385316904343, 1.461102248941518855 ) ) ;
#71888=CARTESIAN_POINT ( 'NONE',  ( 0.4039230143318903177, -1.081087622585241714, -1.701935196855845822 ) ) ;
#71889=CARTESIAN_POINT ( 'NONE',  ( 1.353448696812571850, -1.313440895511051032, -1.247944760566013223 ) ) ;
#71896=CARTESIAN_POINT ( 'NONE',  ( 6.064071300241554496, -1.020233025338047383, 1.621115200587377014 ) ) ;
#71904=CARTESIAN_POINT ( 'NONE',  ( 2.870174731959000525, 1.155358403710282866, 1.826860881501219280 ) ) ;
#71907=CARTESIAN_POINT ( 'NONE',  ( 0.4926326669930108371, -1.172979896111199904, 1.766458537607276336 ) ) ;
#71908=CARTESIAN_POINT ( 'NONE',  ( 5.526323803393727196, 1.085782926936417425, -1.467421699745217190 ) ) ;
#71909=CARTESIAN_POINT ( 'NONE',  ( 2.301971997355524824, -1.971002988154029412, 0.04462483508816358219 ) ) ;
#71910=CARTESIAN_POINT ( 'NONE',  ( 4.218947473185084007, 1.474887410857337100, -1.217315437338606365 ) ) ;
#71913=CARTESIAN_POINT ( 'NONE',  ( 4.475032023839897732, 1.799880929630924165, 0.8001706733358445733 ) ) ;
#71914=CARTESIAN_POINT ( 'NONE',  ( 0.7966981359470609592, 1.587242811699969725, 1.118599961973030021 ) ) ;
#71921=CARTESIAN_POINT ( 'NONE',  ( 4.828717125059535320, 1.315996081294769304, -1.387672938220223307 ) ) ;
#71923=CARTESIAN_POINT ( 'NONE',  ( 0.8157880970438775581, -0.3219574891645953785, 2.183050487710703536 ) ) ;
#71925=CARTESIAN_POINT ( 'NONE',  ( 0.04731519813723152057, -1.748418646119804576, 0.7749314921376224685 ) ) ;
#71926=CARTESIAN_POINT ( 'NONE',  ( 0.07661050522433668353, 0.008287133257128471639, -1.710863442170395432 ) ) ;
#71928=CARTESIAN_POINT ( 'NONE',  ( 2.734898984476673789, -1.980466496001157317, -0.6033880717724802167 ) ) ;
#71933=CARTESIAN_POINT ( 'NONE',  ( 0.3917762336288696523, 1.602822130585265015, 1.450656209987542855 ) ) ;
#71938=CARTESIAN_POINT ( 'NONE',  ( 6.925078400183553029, 7.052683076116534444, 2.553806833665558162 ) ) ;
#71940=CARTESIAN_POINT ( 'NONE',  ( 4.729033670188855787, 1.730023327335796113, 0.1204123811070593880 ) ) ;
#71943=CARTESIAN_POINT ( 'NONE',  ( 2.870052101067874339, -2.048368873657464118, 0.2992715783270774588 ) ) ;
#71944=CARTESIAN_POINT ( 'NONE',  ( 4.042653799040228257, -1.567611697763098055, 1.423267961261857950 ) ) ;
#71947=CARTESIAN_POINT ( 'NONE',  ( 2.043745906638486431, 1.354474275242853798, 1.429983431767953617 ) ) ;
#71949=CARTESIAN_POINT ( 'NONE',  ( 0.9668906521006037647, -1.505869814250645478, 1.178657042999963878 ) ) ;
#71950=CARTESIAN_POINT ( 'NONE',  ( 4.892671604017262865, 1.907728271999886704, -1.270570218630202808 ) ) ;
#71951=CARTESIAN_POINT ( 'NONE',  ( 1.928079105319381314, 1.052063804484974385, -1.491885150056403653 ) ) ;
#71955=CARTESIAN_POINT ( 'NONE',  ( 2.935794159824364868, -1.939102465223912830, 0.5408614042671439082 ) ) ;
#71956=CARTESIAN_POINT ( 'NONE',  ( 3.133595828963112950, 1.864314371477162169, -0.6108997337519045390 ) ) ;
#71960=CARTESIAN_POINT ( 'NONE',  ( 5.718719656712253574, -0.05221879637645754357, 2.090152071033167136 ) ) ;
#71961=CARTESIAN_POINT ( 'NONE',  ( 5.119873625132255412, -0.9486883152997215296, -1.493885749217472636 ) ) ;
#71963=CARTESIAN_POINT ( 'NONE',  ( 0.9729166594223404019, -0.05710519180573449260, -2.190871861337650994 ) ) ;
#71964=CARTESIAN_POINT ( 'NONE',  ( 0.09860955243249854008, -0.4675299588126168859, 1.676413046982327515 ) ) ;
#71967=CARTESIAN_POINT ( 'NONE',  ( 5.695955869756449630, 2.025510559372576402, 1.086827626776807554 ) ) ;
#71968=CARTESIAN_POINT ( 'NONE',  ( -0.1290005225502675879, -0.006633637972621592160, -2.173875058097324064 ) ) ;
#71969=CARTESIAN_POINT ( 'NONE',  ( 5.360564742968721319, -0.6223997329263281086, 1.618453672356393147 ) ) ;
#71970=CARTESIAN_POINT ( 'NONE',  ( 2.262606014870732096, 0.9450075053254001212, 1.994452002680577429 ) ) ;
#71971=( BOUNDED_CURVE ( )  B_SPLINE_CURVE ( 3, ( #81428, #28413, #130262, #78224 ),
 .UNSPECIFIED., .F., .T. ) 
 B_SPLINE_CURVE_WITH_KNOTS ( ( 4, 4 ),
 ( 0.4999999999999986677, 1.000000000000000000 ),
 .UNSPECIFIED. ) 
 CURVE ( )  GEOMETRIC_REPRESENTATION_ITEM ( )  RATIONAL_B_SPLINE_CURVE ( ( 1.000000000000001998, 0.3333333333333334259, 0.3333333333333316495, 1.000000000000000222 ) ) 
 REPRESENTATION_ITEM ( '' )  );
#71972=CARTESIAN_POINT ( 'NONE',  ( 0.6905673677243575614, 1.117554423744430592, -1.861242299804190869 ) ) ;
#71974=CARTESIAN_POINT ( 'NONE',  ( 0.8314520141109645879, -1.673154641659507558, -1.297526329946703472 ) ) ;
#71975=CARTESIAN_POINT ( 'NONE',  ( 3.468750000000001776, 0.7852924748298147906, -1.895863743164155180 ) ) ;
#71977=CARTESIAN_POINT ( 'NONE',  ( 4.805647293689061961, -0.5139743781695116365, 1.856484447351488765 ) ) ;
#71978=CARTESIAN_POINT ( 'NONE',  ( 0.8740457437188209333, 0.4279768726487084285, -2.179530559632827824 ) ) ;
#71980=CARTESIAN_POINT ( 'NONE',  ( 1.330038945030669995, 1.124775647945252643, -1.997386028781794387 ) ) ;
#71985=CARTESIAN_POINT ( 'NONE',  ( 3.739129200393681796, 2.109584919444119855, 0.6958237802787976545 ) ) ;
#71991=CARTESIAN_POINT ( 'NONE',  ( 1.477185633673218534, -2.006960102380969779, -0.1948397147320118372 ) ) ;
#71993=CARTESIAN_POINT ( 'NONE',  ( 0.4442778734073973279, -0.9756673871180139290, 1.817250197203540640 ) ) ;
#71996=CARTESIAN_POINT ( 'NONE',  ( 0.2922019606856861018, 1.531309713818730822, -1.022077305420886040 ) ) ;
#71999=CARTESIAN_POINT ( 'NONE',  ( 1.176598488244801954, -0.03600270464337343435, -1.769546047349578100 ) ) ;
#72000=CARTESIAN_POINT ( 'NONE',  ( 6.522076087392383315, -1.544353836717025308, 0.7889432867928622972 ) ) ;
#72001=CARTESIAN_POINT ( 'NONE',  ( 0.3449248370967008537, 0.5783895242766275979, -1.748133987124582012 ) ) ;
#72002=CARTESIAN_POINT ( 'NONE',  ( 3.773197156129989516, 2.158245952819247471, -0.7729258541082913991 ) ) ;
#72003=CARTESIAN_POINT ( 'NONE',  ( 3.275182144284936925, 1.168729223632531733, 1.422615900182722992 ) ) ;
#72005=CARTESIAN_POINT ( 'NONE',  ( 4.682524874021861017, -1.770931954651306262, -0.4427778663074270482 ) ) ;
#72006=CARTESIAN_POINT ( 'NONE',  ( 4.746720300533005421, 1.994071680685698400, -0.2986252114312442640 ) ) ;
#72008=CARTESIAN_POINT ( 'NONE',  ( 3.995213114784367026, 1.913063998889670714, -1.207689374757703771 ) ) ;
#72010=CARTESIAN_POINT ( 'NONE',  ( 5.842829903504588529, 0.4074447676574670107, 2.065989314711280667 ) ) ;
#72012=CARTESIAN_POINT ( 'NONE',  ( 3.754400092289136737, -2.067862582909282487, -0.1045053291982081939 ) ) ;
#72015=CARTESIAN_POINT ( 'NONE',  ( 5.356147330077114077, 0.8591290142025624910, -1.938821108677920346 ) ) ;
#72017=CARTESIAN_POINT ( 'NONE',  ( 0.9789820196765993687, -0.04640813864221354085, -1.926104504880983725 ) ) ;
#72019=CARTESIAN_POINT ( 'NONE',  ( 0.3616804892651844239, -0.5289564462071428830, 1.897103703902315530 ) ) ;
#72025=CARTESIAN_POINT ( 'NONE',  ( 1.108037262132562262, 1.686735864949813202, 1.445688421275423075 ) ) ;
#72026=CARTESIAN_POINT ( 'NONE',  ( 2.573382939595921570, 0.1044104795966259297, -2.103504788083962573 ) ) ;
#72029=CARTESIAN_POINT ( 'NONE',  ( 0.9415990247386073486, 1.246032235168346380, 1.382555731526733611 ) ) ;
#72034=CARTESIAN_POINT ( 'NONE',  ( 0.6859744409541921328, 2.042103856186634925, -0.5713114342573709648 ) ) ;
#72037=CARTESIAN_POINT ( 'NONE',  ( 3.402741375674179114, 0.4741672551989496998, 1.903589013717405853 ) ) ;
#72038=CARTESIAN_POINT ( 'NONE',  ( 2.659225025413253007, -1.880336703546074073, -1.066323988048665017 ) ) ;
#72039=CARTESIAN_POINT ( 'NONE',  ( 1.891909123491273492, -0.4922293657834125313, -1.774144672653771293 ) ) ;
#72043=CARTESIAN_POINT ( 'NONE',  ( 3.468456934111513235, 0.04105959252117792613, -1.740014521098575351 ) ) ;
#72047=CARTESIAN_POINT ( 'NONE',  ( 0.6554165194554737450, -1.826866057147133349, -1.155366728873077342 ) ) ;
#72049=CARTESIAN_POINT ( 'NONE',  ( 2.829453700430568652, -1.392333688140505510, 1.458332250898628057 ) ) ;
#72050=CARTESIAN_POINT ( 'NONE',  ( 6.825078400183551608, 0.5660753733540256905, 2.196387875007102419 ) ) ;
#72051=CARTESIAN_POINT ( 'NONE',  ( 0.6026772488060898603, -0.7295331166810551382, -2.035022307366324945 ) ) ;
#72052=CARTESIAN_POINT ( 'NONE',  ( 2.676590784821473168, -1.886132711224804748, -0.5737105244360584111 ) ) ;
#72053=CARTESIAN_POINT ( 'NONE',  ( 6.609000000000012420, 2.456927087449762404, 2.283703893460458989 ) ) ;
#72054=CARTESIAN_POINT ( 'NONE',  ( 2.700647863620793121, 1.641916212795376806, 1.036879047414513755 ) ) ;
#72055=CARTESIAN_POINT ( 'NONE',  ( 6.504189997394580480, -0.8109953713257547214, 1.730197269205424160 ) ) ;
#72064=CARTESIAN_POINT ( 'NONE',  ( 0.5521677985501523001, 0.6901698128830742185, -2.096122547012829962 ) ) ;
#72066=CARTESIAN_POINT ( 'NONE',  ( 4.030091663008243508, 1.086175826233202857, 1.633415718976807041 ) ) ;
#72068=CARTESIAN_POINT ( 'NONE',  ( 1.442029965644067158, -1.730867108953790590, -1.034163949609874233 ) ) ;
#72070=CARTESIAN_POINT ( 'NONE',  ( 1.921263159425983913, -1.888806403119867916, 0.9570566162820994816 ) ) ;
#72074=CARTESIAN_POINT ( 'NONE',  ( 3.486116527793288178, -0.3603757036649730683, -1.805346353211812804 ) ) ;
#72078=CARTESIAN_POINT ( 'NONE',  ( 4.342108446431157454, -1.306982937058022820, -1.669832246961988176 ) ) ;
#72079=CARTESIAN_POINT ( 'NONE',  ( -0.02377707250108065939, -0.1326659201078099481, -1.811169398030491928 ) ) ;
#72083=CARTESIAN_POINT ( 'NONE',  ( 4.095036773856917556, 1.742982576809920303, -1.099142878725319239 ) ) ;
#72085=CARTESIAN_POINT ( 'NONE',  ( 1.680954830071922812, 1.270413995023990106, 1.332975479855981416 ) ) ;
#72091=CARTESIAN_POINT ( 'NONE',  ( 0.6982365061397632910, -0.7907169553198112322, 2.060542492664858560 ) ) ;
#72092=CARTESIAN_POINT ( 'NONE',  ( 3.603020308667020277, 1.786206176199186535, -1.388445577547703369 ) ) ;
#72094=CARTESIAN_POINT ( 'NONE',  ( 3.867288652163490159, -1.509380944159900428, -1.001465339209107075 ) ) ;
#72095=CARTESIAN_POINT ( 'NONE',  ( 4.698395719694191897, 1.316562313306284038, -1.391896452211606849 ) ) ;
#72096=CARTESIAN_POINT ( 'NONE',  ( 5.143061708805018561, -0.2499388813127951525, -2.055141626981969338 ) ) ;
#72098=CARTESIAN_POINT ( 'NONE',  ( 3.467610927914951624, 1.923740664667829225, -0.4305075535177785295 ) ) ;
#72099=CARTESIAN_POINT ( 'NONE',  ( 1.219610691686360049, -1.880083933147856934, 0.4191893400790832613 ) ) ;
#72100=CARTESIAN_POINT ( 'NONE',  ( 4.205816867194319464, -1.865656749788859647, 0.1373567816406878750 ) ) ;
#72101=CARTESIAN_POINT ( 'NONE',  ( 3.422812307543467103, 1.464285610008815963, -1.783632237398341536 ) ) ;
#72102=CARTESIAN_POINT ( 'NONE',  ( 4.263987252221818736, -1.856165113571141445, 0.1354236832897796894 ) ) ;
#72106=CARTESIAN_POINT ( 'NONE',  ( 2.227300950330353579, 0.0009978793536376256035, 2.106257355060832115 ) ) ;
#72112=CARTESIAN_POINT ( 'NONE',  ( 2.689816194747224110, 2.012238202079220439, -0.6693303307304664385 ) ) ;
#72114=CARTESIAN_POINT ( 'NONE',  ( 1.160422406460089428, 2.017671146822976880, 0.09473317391113857122 ) ) ;
#72120=CARTESIAN_POINT ( 'NONE',  ( 1.423353863051743273, -0.05456730952056210171, 2.161080666180377197 ) ) ;
#72121=CARTESIAN_POINT ( 'NONE',  ( 6.889999999999996128, 2.105039946316529242, 2.031469082812328519 ) ) ;
#72126=CARTESIAN_POINT ( 'NONE',  ( 5.612517632836664383, 1.944729323200470095, 0.5331731267440716904 ) ) ;
#72128=CARTESIAN_POINT ( 'NONE',  ( 6.286679179808664308, 1.818834136932646839, -1.030939041669608924 ) ) ;
#72130=CARTESIAN_POINT ( 'NONE',  ( 0.6204658552826959328, -1.213099742399858627, -1.909634413763374283 ) ) ;
#72134=CARTESIAN_POINT ( 'NONE',  ( 1.317839660544089853, 0.9426401379578488449, -1.667518220840451981 ) ) ;
#72138=CARTESIAN_POINT ( 'NONE',  ( 3.228823373612188519, 0.04322303627742052345, 1.724510841617853840 ) ) ;
#72141=CARTESIAN_POINT ( 'NONE',  ( 1.739140684745379195, -1.277452191371928558, -1.225025713498065549 ) ) ;
#72142=CARTESIAN_POINT ( 'NONE',  ( 5.526482418920476647, 1.318621124876094397, -1.769340128416618363 ) ) ;
#72145=CARTESIAN_POINT ( 'NONE',  ( 4.653055333535057514, 0.3633016933833124185, 2.088981207656291250 ) ) ;
#72146=CARTESIAN_POINT ( 'NONE',  ( 3.901970389206737444, -1.039011544341267745, -1.727992587138134306 ) ) ;
#72147=CARTESIAN_POINT ( 'NONE',  ( 4.605596613081209156, 1.347055988495224232, 1.211539923951672648 ) ) ;
#72151=CARTESIAN_POINT ( 'NONE',  ( 1.516246529245099284, 1.258767711876613848, -1.383943980506313398 ) ) ;
#72152=CARTESIAN_POINT ( 'NONE',  ( 6.656878040733529289, -1.407521694628325770, 1.162499734694094844 ) ) ;
#72153=CARTESIAN_POINT ( 'NONE',  ( 6.481129863841750272, -1.659422710288318115, -0.7269172754736009656 ) ) ;
#72162=CARTESIAN_POINT ( 'NONE',  ( 4.412424163657523657, -2.120181911468725033, -0.04909571644767100895 ) ) ;
#72163=CARTESIAN_POINT ( 'NONE',  ( -0.1294898018152357000, -0.0008549345193622873455, -1.926395771554180625 ) ) ;
#72166=CARTESIAN_POINT ( 'NONE',  ( 5.114510421747438862, 1.361449769532377729, -1.425934698893965402 ) ) ;
#72168=CARTESIAN_POINT ( 'NONE',  ( 0.5100215303667603450, -0.7206480643048470691, 1.879988510241884292 ) ) ;
#72170=CARTESIAN_POINT ( 'NONE',  ( 6.473823543489908516, -0.9023987703748233002, 1.913193491996653783 ) ) ;
#72172=CARTESIAN_POINT ( 'NONE',  ( 1.680221237283368696, -1.148429780529091948, -1.722445320287042447 ) ) ;
#72176=CARTESIAN_POINT ( 'NONE',  ( 4.857415893618338032, 2.067970888898474247, -0.3061586078061846461 ) ) ;
#72178=CARTESIAN_POINT ( 'NONE',  ( 2.889462524698828361, 1.289687736819044472, 1.292329967842877014 ) ) ;
#72179=CARTESIAN_POINT ( 'NONE',  ( 1.383166562764587271, 0.1333312229490003775, -1.806600723499194538 ) ) ;
#72184=CARTESIAN_POINT ( 'NONE',  ( 4.612475435721691497, -0.9401552641563456492, -1.996616816212187340 ) ) ;
#72186=CARTESIAN_POINT ( 'NONE',  ( 2.367698891403247519, 0.5082884949165042965, -1.843433491391050838 ) ) ;
#72188=CARTESIAN_POINT ( 'NONE',  ( 6.443811375169310907, 1.424792453395683500, 1.502365266013883538 ) ) ;
#72190=CARTESIAN_POINT ( 'NONE',  ( 6.005464345382193869, -2.175231771021503668, 0.2666438670960933344 ) ) ;
#72196=CARTESIAN_POINT ( 'NONE',  ( 4.042156614576187579, 1.861303109871172312, 0.1859210194900539626 ) ) ;
#72202=CARTESIAN_POINT ( 'NONE',  ( 6.948098034395241207, -0.8905871627266357393, 1.867117781285509537 ) ) ;
#72203=CARTESIAN_POINT ( 'NONE',  ( 1.564077599769473803, -1.076297475396456704, 1.704952281334138675 ) ) ;
#72207=CARTESIAN_POINT ( 'NONE',  ( 1.113517231965298837, -2.137359700923711081, 0.4831916906855234228 ) ) ;
#72208=CARTESIAN_POINT ( 'NONE',  ( 5.637271085457097541, -1.648663388651723460, 0.7845467231081537651 ) ) ;
#72216=CARTESIAN_POINT ( 'NONE',  ( 3.140019216317342376, 0.4501627324021878485, 1.785233193441162491 ) ) ;
#72217=CARTESIAN_POINT ( 'NONE',  ( 6.205343618373656334, 1.749435416034326618, -0.9961562333783975376 ) ) ;
#72218=CARTESIAN_POINT ( 'NONE',  ( 2.372814144171823791, -0.5044604469449982531, 2.242205522996820743 ) ) ;
#72220=CARTESIAN_POINT ( 'NONE',  ( 6.983263157960366563, -0.003091553303710344557, 1.945923119799706669 ) ) ;
#72223=CARTESIAN_POINT ( 'NONE',  ( 2.970861089138316036, -1.445268511421276214, 1.252435071843561731 ) ) ;
#72227=CARTESIAN_POINT ( 'NONE',  ( 2.314113491060950434, 1.363558105167931966, -1.585015408884550503 ) ) ;
#72228=CARTESIAN_POINT ( 'NONE',  ( 0.8306673739700667358, 0.1335802410974036292, 1.865940672528036304 ) ) ;
#72229=CARTESIAN_POINT ( 'NONE',  ( 2.302111043707856020, -1.802142186715177674, 0.9039695891032775155 ) ) ;
#72232=CARTESIAN_POINT ( 'NONE',  ( 3.315673178333057969, 1.101538733106369072, -1.347505558334564535 ) ) ;
#72236=CARTESIAN_POINT ( 'NONE',  ( 2.929983995618768322, 0.9579465210916816575, -1.434183166407378307 ) ) ;
#72237=CARTESIAN_POINT ( 'NONE',  ( 3.298540952264991777, 1.726358142885858316, -1.349911518210664241 ) ) ;
#72238=CARTESIAN_POINT ( 'NONE',  ( 5.514374426699260923, -0.9893691592960799364, -1.972764877262770833 ) ) ;
#72241=CARTESIAN_POINT ( 'NONE',  ( 3.432658224824499893, -1.297079494776206543, 1.740850151316934991 ) ) ;
#72242=CARTESIAN_POINT ( 'NONE',  ( 2.578497204056416692, -1.747032809129964503, -0.5301130021647950663 ) ) ;
#72244=CARTESIAN_POINT ( 'NONE',  ( 4.382099326012149909, -2.116931447088743923, -0.04843129487230694169 ) ) ;
#72247=CARTESIAN_POINT ( 'NONE',  ( 4.581715332782612116, -1.081557967857611935, 2.021163373060499424 ) ) ;
#72251=CARTESIAN_POINT ( 'NONE',  ( 0.1883438084668061507, 1.224518555304452416, 1.730999496979759300 ) ) ;
#72258=CARTESIAN_POINT ( 'NONE',  ( 5.010388774477189777, -1.913804350592800629, 0.6351971752796632398 ) ) ;
#72260=CARTESIAN_POINT ( 'NONE',  ( 3.221586243988622034, 0.3073416805365276061, -2.039453084318449072 ) ) ;
#72262=CARTESIAN_POINT ( 'NONE',  ( -0.1408020194050354501, 2.869306972054268989, -2.588546047063750688 ) ) ;
#72266=CARTESIAN_POINT ( 'NONE',  ( -0.02919842301645457147, -0.002306431287177941429, -2.073770398395402115 ) ) ;
#72267=CARTESIAN_POINT ( 'NONE',  ( 3.744767666119628746, 2.000857235306313875, -0.2496062519145719194 ) ) ;
#72268=CARTESIAN_POINT ( 'NONE',  ( 3.526749072549471453, -1.699942963128863838, 0.7078653300200200560 ) ) ;
#72271=CARTESIAN_POINT ( 'NONE',  ( 0.9907087679515521605, 1.524132375323374200, -0.8073730212512005844 ) ) ;
#72273=CARTESIAN_POINT ( 'NONE',  ( 0.4933721672778153544, -2.286813510910344682, 0.2336738355162761571 ) ) ;
#72275=CARTESIAN_POINT ( 'NONE',  ( 0.6150082408139592172, 1.559066714514239393, -1.639647465354547196 ) ) ;
#72276=CARTESIAN_POINT ( 'NONE',  ( 2.561271001754578780, -1.832848164261296597, -1.037248627104673249 ) ) ;
#72286=CARTESIAN_POINT ( 'NONE',  ( 3.902737194376978636, -2.197594379623767580, -0.3235144178719475128 ) ) ;
#72287=CARTESIAN_POINT ( 'NONE',  ( 2.414256260463796711, 1.430409426244143134, -1.660321623440104810 ) ) ;
#72291=CARTESIAN_POINT ( 'NONE',  ( 5.301206097546149465, -1.683542251207278628, 1.007010407901312465 ) ) ;
#72296=CARTESIAN_POINT ( 'NONE',  ( 4.166350089634453191, 2.120059694336435374, -0.05518752902338577848 ) ) ;
#72300=CARTESIAN_POINT ( 'NONE',  ( 5.366167234668930419, 1.061923416652654550, 1.882811416686725359 ) ) ;
#72302=CARTESIAN_POINT ( 'NONE',  ( 5.548353751603532835, -1.447698842669535413, 1.137588655622793876 ) ) ;
#72306=CARTESIAN_POINT ( 'NONE',  ( 0.4326491639514402077, -1.228936893156933330, -1.232681022120321934 ) ) ;
#72307=CARTESIAN_POINT ( 'NONE',  ( 6.827182134110200806, 4.698030009824885056, 2.473619993765368008 ) ) ;
#72310=CARTESIAN_POINT ( 'NONE',  ( 4.381803836707322652, 1.409801062080328959, 1.638821348427916602 ) ) ;
#72314=CARTESIAN_POINT ( 'NONE',  ( 3.872077330825273389, 1.198917189070296541, 1.798566189592496034 ) ) ;
#72315=CARTESIAN_POINT ( 'NONE',  ( 4.499269426148129192, 1.581550893178500727, 1.176622024725955784 ) ) ;
#72316=CARTESIAN_POINT ( 'NONE',  ( 3.461945267817592597, 1.365228559796902719, 1.068630620724864588 ) ) ;
#72317=CARTESIAN_POINT ( 'NONE',  ( 0.3807642395799659130, -0.2741851280289032688, -2.174293136291181483 ) ) ;
#72318=CARTESIAN_POINT ( 'NONE',  ( 0.8862589459083686227, 1.552251447166236975, 1.707653507296547968 ) ) ;
#72319=CARTESIAN_POINT ( 'NONE',  ( 3.462233735546389468, 0.9232262379769129446, 1.842458217425169131 ) ) ;
#72320=CARTESIAN_POINT ( 'NONE',  ( 6.128462272945822242, 0.1949450651400796986, 1.932269955005933904 ) ) ;
#72328=CARTESIAN_POINT ( 'NONE',  ( 3.540233119088306513, 0.9941544567689840628, -1.970234943098593039 ) ) ;
#72331=CARTESIAN_POINT ( 'NONE',  ( 0.4263013476871494456, -1.221759592413705908, 1.403788950402263369 ) ) ;
#72332=CARTESIAN_POINT ( 'NONE',  ( -0.02900071798685524560, -0.004641455105012376459, -2.173770343569726649 ) ) ;
#72336=DIRECTION ( 'NONE',  ( 2.949029909160572061E-17, 1.000000000000000000, -8.673600428462353400E-15 ) ) ;
#72337=CARTESIAN_POINT ( 'NONE',  ( 6.281194495005370193, 1.273289214079580622, 1.330099835651930684 ) ) ;
#72339=CARTESIAN_POINT ( 'NONE',  ( 2.360294219997323140, 0.8799647281299802781, 1.863710983410723943 ) ) ;
#72345=CARTESIAN_POINT ( 'NONE',  ( 1.305620473665240366, -0.5016907458927004626, 1.998752541464960952 ) ) ;
#72348=CARTESIAN_POINT ( 'NONE',  ( 4.933073973922719624, -1.305863698873997780, -1.298312775753200699 ) ) ;
#72352=CARTESIAN_POINT ( 'NONE',  ( 5.004599478379411437, -0.7411955310945415043, -2.078817424605138964 ) ) ;
#72353=CARTESIAN_POINT ( 'NONE',  ( 0.3335754702045168330, -1.976410766185803691, 0.8757516042032786885 ) ) ;
#72356=CARTESIAN_POINT ( 'NONE',  ( 0.2813230411330031044, 0.1852680230450229892, -1.903361379684164412 ) ) ;
#72357=CARTESIAN_POINT ( 'NONE',  ( 1.341030165941111241, -1.731997234073547220, -1.032477317303444053 ) ) ;
#72359=CARTESIAN_POINT ( 'NONE',  ( 1.423680875022467873, 0.9325134783980688624, 2.100857314651356500 ) ) ;
#72361=FACE_OUTER_BOUND ( 'NONE', #168962, .T. ) ;
#72362=CARTESIAN_POINT ( 'NONE',  ( 6.445967652843097362, -1.252902786447611883, -1.444740716957277904 ) ) ;
#72364=CARTESIAN_POINT ( 'NONE',  ( 1.604156678829884886, -0.6703249191640224813, -1.746612230856612769 ) ) ;
#72365=CARTESIAN_POINT ( 'NONE',  ( 2.606657977298726614, 1.900416011228076130, 0.6748465934659984011 ) ) ;
#72369=CARTESIAN_POINT ( 'NONE',  ( 5.180345272937711520, -1.170841012621581134, 1.750402278287941149 ) ) ;
#72375=CARTESIAN_POINT ( 'NONE',  ( 4.552993113364055766, 0.3493383367317858257, 1.989188622967730025 ) ) ;
#72378=CARTESIAN_POINT ( 'NONE',  ( 6.268047042621852860, -2.047536660891946525, 0.2488583125946699504 ) ) ;
#72380=CARTESIAN_POINT ( 'NONE',  ( 3.849029623751087481, -1.769594347601778361, 1.241129261558816754 ) ) ;
#72386=CARTESIAN_POINT ( 'NONE',  ( 2.277988012537075502, -2.106425727361205702, 0.5258826003073436839 ) ) ;
#72389=CARTESIAN_POINT ( 'NONE',  ( 1.469984750362408388, -1.748608032326857353, -0.5769476384821782267 ) ) ;
#72391=CARTESIAN_POINT ( 'NONE',  ( 2.753686713869853531, 2.180749500395392282, -0.2175628297749406803 ) ) ;
#72392=CARTESIAN_POINT ( 'NONE',  ( 6.983263157960365675, 2.037486384657179350, 2.358487060789053569 ) ) ;
#72393=CARTESIAN_POINT ( 'NONE',  ( 3.960077240414155764, 2.245805352194740756, -0.2739276486512822184 ) ) ;
#72399=CARTESIAN_POINT ( 'NONE',  ( 5.272599804957129876, -1.666481374185318609, -0.5959551625853221068 ) ) ;
#72401=CARTESIAN_POINT ( 'NONE',  ( 2.063634109657853433, 0.3607628843028657939, -2.074664996798830874 ) ) ;
#72404=CARTESIAN_POINT ( 'NONE',  ( 1.187880472884972560, -1.246972491003460748, -1.524547227783664249 ) ) ;
#72406=CARTESIAN_POINT ( 'NONE',  ( 0.3440982351944205653, -0.9282241650855774795, 1.728402704573737125 ) ) ;
#72407=CARTESIAN_POINT ( 'NONE',  ( 6.328355405667826616, -0.8624701743435190249, -1.593140579868371987 ) ) ;
#72411=CARTESIAN_POINT ( 'NONE',  ( 4.276139911362797363, -1.077190196239918851, 1.529178877381555335 ) ) ;
#72413=CARTESIAN_POINT ( 'NONE',  ( 5.998901810315325989, 0.3981486965325408134, 2.031442706791640074 ) ) ;
#72422=CARTESIAN_POINT ( 'NONE',  ( 4.545333077707183200, 1.753367681936630840, -0.8802267832125689750 ) ) ;
#72424=CARTESIAN_POINT ( 'NONE',  ( 2.354842093047845530, -0.8645933883619570937, 1.821462535208747457 ) ) ;
#72426=CARTESIAN_POINT ( 'NONE',  ( 0.6092356648998223934, -0.3158941238240610128, 2.168550393043596536 ) ) ;
#72428=CARTESIAN_POINT ( 'NONE',  ( 1.897508810457830153, -0.6348907881138059484, 1.759622905829677508 ) ) ;
#72430=CARTESIAN_POINT ( 'NONE',  ( 3.761980314931902214, 0.6741652524458006113, -1.897120442666611506 ) ) ;
#72433=CARTESIAN_POINT ( 'NONE',  ( 3.304427501237202414, 1.341129661294770958, -1.638326698864990716 ) ) ;
#72435=CARTESIAN_POINT ( 'NONE',  ( 4.580570967453869713, 1.276285970795057345, -1.630082184409971324 ) ) ;
#72437=CARTESIAN_POINT ( 'NONE',  ( 1.470382607095675143, -1.986325758040393685, -0.6527442681472686026 ) ) ;
#72438=CARTESIAN_POINT ( 'NONE',  ( 6.620655732516679493, 3.689697857139722981, 2.587825964709880910 ) ) ;
#72439=CARTESIAN_POINT ( 'NONE',  ( 0.1117072452763347851, -0.7311285168369995313, -1.561089762993218999 ) ) ;
#72449=CARTESIAN_POINT ( 'NONE',  ( -0.1110810684432986112, 0.002541288824218449188, -1.796853612742685513 ) ) ;
#72458=CARTESIAN_POINT ( 'NONE',  ( 6.362907676916636390, -0.1017654035869921675, -2.013986322929907757 ) ) ;
#72465=CARTESIAN_POINT ( 'NONE',  ( 3.256658344530354299, -0.5673638227334516504, -1.885978461452636479 ) ) ;
#72466=CARTESIAN_POINT ( 'NONE',  ( 4.042592340535226647, -1.492244431823461115, 1.356313616978216618 ) ) ;
#72469=CARTESIAN_POINT ( 'NONE',  ( 4.488337453930180132, -0.4787454259813396229, -2.138356021698713416 ) ) ;
#72471=CARTESIAN_POINT ( 'NONE',  ( 3.346621647027960833, 0.4665833272349695360, 1.868923817322089453 ) ) ;
#72480=CARTESIAN_POINT ( 'NONE',  ( -0.1294898018152357000, -0.0008549345193622873455, -1.926395771554180625 ) ) ;
#72481=CARTESIAN_POINT ( 'NONE',  ( 2.613933768341146102, -0.6292564844058865514, 1.912298747220711359 ) ) ;
#72482=CARTESIAN_POINT ( 'NONE',  ( 5.149944687579217195, -0.2746161857135383522, -2.281865060072391760 ) ) ;
#72484=CARTESIAN_POINT ( 'NONE',  ( 3.625696855625531345, 1.816486592755601315, -0.4036080491761192546 ) ) ;
#72490=CARTESIAN_POINT ( 'NONE',  ( 5.460518745505165583, -1.890641411385725501, -0.8928391682238371319 ) ) ;
#72497=CARTESIAN_POINT ( 'NONE',  ( 0.9085097582094739943, 1.384192474337717194, -1.190531929384466281 ) ) ;
#72499=CARTESIAN_POINT ( 'NONE',  ( 2.267823513004694647, 1.585025364652093760, -0.7039959249812016706 ) ) ;
#72504=CARTESIAN_POINT ( 'NONE',  ( 0.3212534483023680165, -1.847719145540312358, -0.9339786784923131968 ) ) ;
#72505=CARTESIAN_POINT ( 'NONE',  ( 5.900976575431972293, 1.489821718068456979, -1.054992404821846863 ) ) ;
#72506=CARTESIAN_POINT ( 'NONE',  ( 3.537899350542179189, 1.241011212050652679, 1.519374649786103149 ) ) ;
#72512=CARTESIAN_POINT ( 'NONE',  ( 3.563236855010095461, -1.732559338849114727, 1.222301536229251306 ) ) ;
#72516=CARTESIAN_POINT ( 'NONE',  ( 1.956005403265232978, -0.7013823251572397499, 1.947930506816720087 ) ) ;
#72519=CARTESIAN_POINT ( 'NONE',  ( 4.424628119981884211, -0.9497243516023866627, -2.008178830631357492 ) ) ;
#72521=CARTESIAN_POINT ( 'NONE',  ( 2.338912275282720277, 0.6088908215152682990, -2.216548965993940801 ) ) ;
#72523=CARTESIAN_POINT ( 'NONE',  ( 6.772339297775464395, -0.9671665324481359960, -1.821725317472399963 ) ) ;
#72527=CARTESIAN_POINT ( 'NONE',  ( 6.532758020889952277, -1.641319963461195464, 0.8346263169811756200 ) ) ;
#72529=CARTESIAN_POINT ( 'NONE',  ( 3.093911922779784440, 1.216618333484908998, 1.475457842794763996 ) ) ;
#72530=CARTESIAN_POINT ( 'NONE',  ( -0.1102773484823937195, 1.312263477441493187, -2.452793124480449283 ) ) ;
#72531=CARTESIAN_POINT ( 'NONE',  ( 4.594587176762323644, -0.3796550294026636574, -1.682289508650273602 ) ) ;
#72532=CARTESIAN_POINT ( 'NONE',  ( 2.624232735793774030, 2.001858099149746550, 0.2420302859193757539 ) ) ;
#72533=CARTESIAN_POINT ( 'NONE',  ( 3.569189921330259807, -1.132127473341357771, 2.000487910885457854 ) ) ;
#72534=CARTESIAN_POINT ( 'NONE',  ( 3.989755448363790258, 1.635235102580555155, 1.563706588500752837 ) ) ;
#72535=CARTESIAN_POINT ( 'NONE',  ( 6.410775461673044795, 1.561785836243877235, -1.413106494374539945 ) ) ;
#72538=CARTESIAN_POINT ( 'NONE',  ( 4.780378767880190338, -1.716399873034094803, -0.4305553870933165883 ) ) ;
#72540=CARTESIAN_POINT ( 'NONE',  ( 1.254322107098894801, 0.9329652568456588968, 2.093986936342966398 ) ) ;
#72541=CARTESIAN_POINT ( 'NONE',  ( 5.472543265827003012, -0.04911201564661467345, -1.840652735559132669 ) ) ;
#72543=CARTESIAN_POINT ( 'NONE',  ( 5.999973295341066049, -0.7855225714627244171, -2.046000194487001878 ) ) ;
#72547=CARTESIAN_POINT ( 'NONE',  ( 6.109843426155951107, 0.6047356833836557977, -1.980059631771100781 ) ) ;
#72548=CARTESIAN_POINT ( 'NONE',  ( 0.4972802279516430612, -0.2910764605805628014, 1.995268990643041640 ) ) ;
#72551=CARTESIAN_POINT ( 'NONE',  ( 4.160710321027959679, -1.426769435979913236, 1.294678423299196579 ) ) ;
#72554=CARTESIAN_POINT ( 'NONE',  ( 0.6158632564332514603, 1.820540700843051418, 1.272696253368794439 ) ) ;
#72564=CARTESIAN_POINT ( 'NONE',  ( 0.9769180011504545735, 1.811320799089161993, 0.7541596914439269161 ) ) ;
#72567=CARTESIAN_POINT ( 'NONE',  ( 6.865691018405424728, -0.4312029709039078007, 1.920920986087648163 ) ) ;
#72570=CARTESIAN_POINT ( 'NONE',  ( 0.1282872750541429741, -1.395696511722638977, -1.781683957999291579 ) ) ;
#72574=CARTESIAN_POINT ( 'NONE',  ( 1.756895065592100291, -1.601674646019658255, -0.9660157589584242865 ) ) ;
#72575=CARTESIAN_POINT ( 'NONE',  ( -0.1229578505166153690, -0.3670672422863025530, -1.699768244568555353 ) ) ;
#72577=CARTESIAN_POINT ( 'NONE',  ( 4.282901435897610298, 1.957309562236182021, -0.9860176978964061423 ) ) ;
#72578=CARTESIAN_POINT ( 'NONE',  ( 4.876155869083551586, 1.324110019830313734, 1.889726917317616328 ) ) ;
#72579=CARTESIAN_POINT ( 'NONE',  ( 0.2861016050247901510, -0.9718399577113141508, 1.817365962020002890 ) ) ;
#72580=CARTESIAN_POINT ( 'NONE',  ( 1.939301023820143577, 0.7432367423349227620, -1.794281902191755540 ) ) ;
#72586=CARTESIAN_POINT ( 'NONE',  ( 3.340470361411255418, 0.4872029778183216697, -1.956561305313428978 ) ) ;
#72590=CARTESIAN_POINT ( 'NONE',  ( 1.418276456094772708, 1.227529518603141190, -1.351586893430449576 ) ) ;
#72595=CARTESIAN_POINT ( 'NONE',  ( 5.805559403952022635, -0.5031923959765474130, 1.998377753082048347 ) ) ;
#72601=CARTESIAN_POINT ( 'NONE',  ( 5.373696804382912973, 0.3918686645382524203, -1.981109099827490949 ) ) ;
#72602=CARTESIAN_POINT ( 'NONE',  ( 5.567086426426935297, -1.752359028239593997, 1.364940763008470226 ) ) ;
#72607=CARTESIAN_POINT ( 'NONE',  ( 4.487218586473323612, 1.841840323776536614, -0.9247287835071598128 ) ) ;
#72608=CARTESIAN_POINT ( 'NONE',  ( 3.744767666119628746, 2.000857235306313875, -0.2496062519145719194 ) ) ;
#72616=CARTESIAN_POINT ( 'NONE',  ( 4.516953773913958692, 2.015725170860783066, -0.04666989112152990921 ) ) ;
#72617=CARTESIAN_POINT ( 'NONE',  ( 3.433393508698717511, 0.8267853122289525736, -1.645126075773599039 ) ) ;
#72619=CARTESIAN_POINT ( 'NONE',  ( 1.875998176474055423, 2.207483416130914478, -0.6726682516732527262 ) ) ;
#72621=CARTESIAN_POINT ( 'NONE',  ( 4.059979352932830743, 2.145800628424157974, -0.2601280725000321148 ) ) ;
#72625=CARTESIAN_POINT ( 'NONE',  ( 3.603114471349005754, 1.037088744013005659, -2.051189238963199379 ) ) ;
#72627=CARTESIAN_POINT ( 'NONE',  ( 2.096370420935515178, -0.4963513585865795275, -1.803540123670114736 ) ) ;
#72628=CARTESIAN_POINT ( 'NONE',  ( 0.5089730629182923627, 1.712948150172272976, 0.9756560103859630573 ) ) ;
#72632=CARTESIAN_POINT ( 'NONE',  ( 1.700138637298425737, -0.7412910010123253679, 2.078789392164873906 ) ) ;
#72635=DIRECTION ( 'NONE',  ( -1.000000000000000000, 0.000000000000000000, 0.000000000000000000 ) ) ;
#72639=CARTESIAN_POINT ( 'NONE',  ( 6.104366069677094053, -0.7090783117675543146, -1.839710284007533225 ) ) ;
#72640=CARTESIAN_POINT ( 'NONE',  ( 5.233197408665407835, 0.1653354203888204033, 2.301840570688079790 ) ) ;
#72641=CARTESIAN_POINT ( 'NONE',  ( 0.3440982351944205653, -0.9282241650855774795, 1.728402704573737125 ) ) ;
#72643=CARTESIAN_POINT ( 'NONE',  ( 3.573143115351416377, 1.862571710426489169, 0.8863520062180642034 ) ) ;
#72650=CARTESIAN_POINT ( 'NONE',  ( 5.758309058547314230, -2.171350062218261989, -0.005773456755737981470 ) ) ;
#72652=CARTESIAN_POINT ( 'NONE',  ( 4.651808992177354440, 0.7092673950449077669, 1.699362209096597187 ) ) ;
#72654=CARTESIAN_POINT ( 'NONE',  ( 6.550331612656306035, -1.695486744446069727, 1.388264742925699569 ) ) ;
#72656=CARTESIAN_POINT ( 'NONE',  ( 0.6853298295916141480, -0.2782767918169821164, -2.245138299566074913 ) ) ;
#72660=CARTESIAN_POINT ( 'NONE',  ( 0.2758376730330712734, 1.891454726169951250, -0.2806862973558504892 ) ) ;
#72661=CARTESIAN_POINT ( 'NONE',  ( 1.357869778638900904, 0.7128107867309957379, 1.620144791207811297 ) ) ;
#72662=CARTESIAN_POINT ( 'NONE',  ( 6.270187311338969671, 2.007533000635489451, -0.1505373637035074819 ) ) ;
#72664=CARTESIAN_POINT ( 'NONE',  ( 3.093272052591877763, -0.3707496286316728229, 1.879197483129394719 ) ) ;
#72665=CARTESIAN_POINT ( 'NONE',  ( -0.1409997244346088141, 2.874455162768466909, -2.488748179275114492 ) ) ;
#72666=CARTESIAN_POINT ( 'NONE',  ( 4.070725410728625704, 1.394476139410082638, -1.391156265790331581 ) ) ;
#72667=CARTESIAN_POINT ( 'NONE',  ( -0.1401555495076401980, -1.643345231473653190, -1.339971704266910812 ) ) ;
#72669=CARTESIAN_POINT ( 'NONE',  ( 2.658895327995167701, -1.626580691111865207, -0.9237732865615968514 ) ) ;
#72670=CARTESIAN_POINT ( 'NONE',  ( 6.551377187490000864, -1.390289022577213984, -1.020726160236499203 ) ) ;
#72673=CARTESIAN_POINT ( 'NONE',  ( 2.385638622766753425, 2.017150886971270651, -0.8956362484653990208 ) ) ;
#72677=CARTESIAN_POINT ( 'NONE',  ( 6.883263157960391787, -0.001104538646235289417, 1.946037152736757925 ) ) ;
#72681=CARTESIAN_POINT ( 'NONE',  ( 0.1747926744264677312, 1.388892567315727744, -2.112808070315982167 ) ) ;
#72685=CARTESIAN_POINT ( 'NONE',  ( 3.666520218671379450, -0.8364210039109070127, -1.894060025281426807 ) ) ;
#72689=CARTESIAN_POINT ( 'NONE',  ( 0.7154971248738207779, 1.652399868344236245, 1.161036454668294304 ) ) ;
#72692=CARTESIAN_POINT ( 'NONE',  ( 0.1745949693968328054, 4.098633874596197657, -2.310325329485760637 ) ) ;
#72694=CARTESIAN_POINT ( 'NONE',  ( 5.940779784064256219, 1.198679029392090589, 1.620932600025201786 ) ) ;
#72695=CARTESIAN_POINT ( 'NONE',  ( 5.928903634556547786, -1.614502157299831042, 1.030912532684091110 ) ) ;
#72696=CARTESIAN_POINT ( 'NONE',  ( 6.539320575229260690, 0.5855366995804256458, 2.057005297509428399 ) ) ;
#72697=CARTESIAN_POINT ( 'NONE',  ( 3.948915171154475878, -1.822730400009948237, -1.216494452853926322 ) ) ;
#72699=CARTESIAN_POINT ( 'NONE',  ( 2.830216799141628492, -0.9462872844297947061, -1.661813493071498726 ) ) ;
#72703=CARTESIAN_POINT ( 'NONE',  ( 1.265250157614560278, 1.862010354082012098, -0.7743342583275418800 ) ) ;
#72705=CARTESIAN_POINT ( 'NONE',  ( 5.812113132715003516, 1.472855484078567700, -1.623034594306454137 ) ) ;
#72707=CARTESIAN_POINT ( 'NONE',  ( 2.819059531128511598, -0.1711090930666993304, 1.716262065957876004 ) ) ;
#72709=CARTESIAN_POINT ( 'NONE',  ( 6.029554895997981667, -0.2579198037528374066, 2.104758538420265168 ) ) ;
#72713=CARTESIAN_POINT ( 'NONE',  ( 0.5198770262540284293, 1.941052373433370448, -0.2841105942011297736 ) ) ;
#72721=CARTESIAN_POINT ( 'NONE',  ( 2.525776224529495906, -1.791516492901791713, 0.2672755921442840354 ) ) ;
#72725=CARTESIAN_POINT ( 'NONE',  ( 3.615680081246709143, -0.5227945197113766929, 1.734396599632443525 ) ) ;
#72729=CARTESIAN_POINT ( 'NONE',  ( 5.582414374887135544, 1.108435676577405937, -1.494769603722338802 ) ) ;
#72731=CARTESIAN_POINT ( 'NONE',  ( 2.829585337313187399, 0.6869450147981278620, -1.788391637942953860 ) ) ;
#72737=CARTESIAN_POINT ( 'NONE',  ( 6.925078400183574345, 7.629137130509068498, 2.744348168701661095 ) ) ;
#72740=CARTESIAN_POINT ( 'NONE',  ( 1.605537313848971026, -2.074692111233501723, 0.2571424261670462452 ) ) ;
#72741=CARTESIAN_POINT ( 'NONE',  ( 0.2174332111963481196, -1.791455004416471430, 0.3504355335035569396 ) ) ;
#72743=CARTESIAN_POINT ( 'NONE',  ( 2.573050890253928635, 0.09191801231544716178, -1.823395950357763695 ) ) ;
#72744=CARTESIAN_POINT ( 'NONE',  ( 3.598431038176507002, -2.204323482753521635, -0.1086902067785888437 ) ) ;
#72747=CARTESIAN_POINT ( 'NONE',  ( 1.494246876672610025, -1.020364814108923213, 1.617233793950809906 ) ) ;
#72748=CARTESIAN_POINT ( 'NONE',  ( 1.205442482676940541, -1.550459043822360661, -1.214442484561629509 ) ) ;
#72749=CARTESIAN_POINT ( 'NONE',  ( 3.245582950214185303, 1.942234966672530261, -0.002794291004394599230 ) ) ;
#72753=CARTESIAN_POINT ( 'NONE',  ( 0.1680794356360598985, -0.7909032441709142880, -1.683366987590989350 ) ) ;
#72762=CARTESIAN_POINT ( 'NONE',  ( 4.336427269025699971, 1.790907886515300085, 0.3537760332646966432 ) ) ;
#72767=CARTESIAN_POINT ( 'NONE',  ( 4.469519713540137218, 1.814478506493342191, -0.4545110902946307152 ) ) ;
#72769=CARTESIAN_POINT ( 'NONE',  ( 2.139170349095420143, -1.720849962885454110, 0.8662218532024426043 ) ) ;
#72770=CARTESIAN_POINT ( 'NONE',  ( 6.385602409055195494, -1.848352663145738095, 0.6577735930803210174 ) ) ;
#72776=CARTESIAN_POINT ( 'NONE',  ( 0.4920138693931704887, -2.106576347024671225, 0.2123275358263312096 ) ) ;
#72779=CARTESIAN_POINT ( 'NONE',  ( 4.996967907133109676, 0.3485794866864948549, 2.040532872733556768 ) ) ;
#72780=CARTESIAN_POINT ( 'NONE',  ( 0.02850758872123548837, -1.683968158181762043, 0.7450552726024004535 ) ) ;
#72782=CARTESIAN_POINT ( 'NONE',  ( 4.869944851454918400, -0.2802274231045227548, -2.281517807288702127 ) ) ;
#72785=CARTESIAN_POINT ( 'NONE',  ( -0.02301423135257947214, -0.1624751001964518382, -2.256290569412158220 ) ) ;
#72788=CARTESIAN_POINT ( 'NONE',  ( 5.138593782488270811, -1.664572445771801634, 0.9999684565626990596 ) ) ;
#72794=CARTESIAN_POINT ( 'NONE',  ( 5.748291730981218706, 0.9368611416523886515, -1.667099895225135686 ) ) ;
#72795=CARTESIAN_POINT ( 'NONE',  ( 5.753138727196851043, 0.1435251449807967150, -2.011451301405759118 ) ) ;
#72799=CARTESIAN_POINT ( 'NONE',  ( 2.730511870197129820, 0.2565026084431647480, 2.074771742164283950 ) ) ;
#72800=CARTESIAN_POINT ( 'NONE',  ( 0.7953275966026486232, -0.6425790844533132429, 1.649264876520744272 ) ) ;
#72802=CARTESIAN_POINT ( 'NONE',  ( 4.382983890270373273, 2.048579214610211530, -1.028644635605566959 ) ) ;
#72803=CARTESIAN_POINT ( 'NONE',  ( 2.466429552724667129, 0.08583113499382444278, -1.738331801394930043 ) ) ;
#72807=CARTESIAN_POINT ( 'NONE',  ( 1.809482579268039126, -1.467825596939468902, 0.9224971444230285478 ) ) ;
#72809=CARTESIAN_POINT ( 'NONE',  ( 1.310759002261387529, -1.470036769156491063, 1.141183394468782364 ) ) ;
#72810=CARTESIAN_POINT ( 'NONE',  ( 2.295604378506800103, -1.940070289243904567, 0.9748468494522060102 ) ) ;
#72812=CARTESIAN_POINT ( 'NONE',  ( 4.768767694835816862, -0.2516295123269947642, -2.000731945836851544 ) ) ;
#72813=CARTESIAN_POINT ( 'NONE',  ( 3.375000000000002665, 2.052068128417946724, -1.927395870058053847E-13 ) ) ;
#72815=CARTESIAN_POINT ( 'NONE',  ( 0.8153024884889724655, -0.2858729149923607826, 1.904955193227176879 ) ) ;
#72817=CARTESIAN_POINT ( 'NONE',  ( 4.623389083599304783, 1.933371432498669273, 1.093773624979002879 ) ) ;
#72822=CARTESIAN_POINT ( 'NONE',  ( 0.7158630905677393352, 1.819291361130066287, 1.274270043568943800 ) ) ;
#72824=CARTESIAN_POINT ( 'NONE',  ( 6.355910407107248083, -0.6622273607519140182, 1.846833223631501264 ) ) ;
#72826=CARTESIAN_POINT ( 'NONE',  ( 6.257125660641059461, -1.935629482380639033, -1.171090987803388606 ) ) ;
#72828=CARTESIAN_POINT ( 'NONE',  ( 2.963389562657412046, 1.741120879107743935, 1.105697716663532892 ) ) ;
#72832=CARTESIAN_POINT ( 'NONE',  ( 4.393722961847310593, -0.7179090532695198146, 1.727491627791829742 ) ) ;
#72833=CARTESIAN_POINT ( 'NONE',  ( 3.762146167370096883, 1.631196324480500115, -0.5889743285819144525 ) ) ;
#72834=CARTESIAN_POINT ( 'NONE',  ( 3.157457554155696844, 0.7852445609939761040, 1.553317506218002464 ) ) ;
#72835=CARTESIAN_POINT ( 'NONE',  ( 0.3281778771060560040, 1.171583119817346086, -1.970250653751925762 ) ) ;
#72837=CARTESIAN_POINT ( 'NONE',  ( 5.108965175345551835, -0.3053309577524323526, 2.068188354190988676 ) ) ;
#72838=CARTESIAN_POINT ( 'NONE',  ( 6.140568862321206467, -1.639224632874112020, 1.040935801138809236 ) ) ;
#72840=CARTESIAN_POINT ( 'NONE',  ( 0.7037502660087076034, 1.864169469917423161, 0.7691187473759173443 ) ) ;
#72842=CARTESIAN_POINT ( 'NONE',  ( 0.4574861729177078229, -1.815669959853306370, 1.095388807130371900 ) ) ;
#72847=CARTESIAN_POINT ( 'NONE',  ( 4.916531288042031989, 1.256637652550334883, -1.324621001416517840 ) ) ;
#72848=ORIENTED_EDGE ( 'NONE', *, *, #176013, .T. ) ;
#72852=CARTESIAN_POINT ( 'NONE',  ( 2.320574876688247024, -0.7769297766534470906, -1.864587897788829718 ) ) ;
#72853=CARTESIAN_POINT ( 'NONE',  ( 6.071336392737415544, 0.1682094380959769098, -2.200428349287026908 ) ) ;
#72855=CARTESIAN_POINT ( 'NONE',  ( 2.869781510094356669, -1.841417136736220650, 0.2678509365347056526 ) ) ;
#72863=CARTESIAN_POINT ( 'NONE',  ( 4.723181480036696023, -0.08661695748878039947, 1.823760500460340550 ) ) ;
#72867=CARTESIAN_POINT ( 'NONE',  ( 0.3327679910518215878, -1.139612444193355278, 1.306804640533586026 ) ) ;
#72868=CARTESIAN_POINT ( 'NONE',  ( 6.667912628260062036, -1.128459271250933149, 1.455361883854713767 ) ) ;
#72869=CARTESIAN_POINT ( 'NONE',  ( 5.988978958577418688, -0.3324729122747641097, -2.283524998171110543 ) ) ;
#72871=CARTESIAN_POINT ( 'NONE',  ( 6.626263010475290649, 1.250585457657760635, -1.762915812992614129 ) ) ;
#72873=CARTESIAN_POINT ( 'NONE',  ( 6.257181701683109942, -2.286357481388684221, -0.2351346485395827413 ) ) ;
#72876=CARTESIAN_POINT ( 'NONE',  ( 6.069203928793593050, 0.1358119448514639727, -1.865795782587629681 ) ) ;
#72877=CARTESIAN_POINT ( 'NONE',  ( 3.498220628606643956, -0.9384276995785534314, 1.666209768436441419 ) ) ;
#72879=CARTESIAN_POINT ( 'NONE',  ( 4.864015066594513215, 2.183220759563545776, -0.3215228633955333759 ) ) ;
#72880=CARTESIAN_POINT ( 'NONE',  ( 4.434827806327999333, -1.698493238601869182, 1.263996378755541938 ) ) ;
#72883=CARTESIAN_POINT ( 'NONE',  ( 6.983263157960378997, 2.960795523694306652, 2.498903865360342369 ) ) ;
#72884=CARTESIAN_POINT ( 'NONE',  ( -0.1110810684433038154, 7.629137130509058728, -2.396956819904518809 ) ) ;
#72887=CARTESIAN_POINT ( 'NONE',  ( 5.707716976326653757, 1.605689621071492601, 1.385122894465253607 ) ) ;
#72888=CARTESIAN_POINT ( 'NONE',  ( 2.890017657663559891, 1.631080081281432559, 1.632583592418336282 ) ) ;
#72889=CARTESIAN_POINT ( 'NONE',  ( 3.613678190204441254, 0.4790664972640528152, -1.902336835828049244 ) ) ;
#72891=CARTESIAN_POINT ( 'NONE',  ( 6.631690664033638605, 1.975529463507015526, -0.5929735606366983713 ) ) ;
#72895=CARTESIAN_POINT ( 'NONE',  ( 6.104703911763087909, 1.883310800321544409, 0.7212973825745233603 ) ) ;
#72899=CARTESIAN_POINT ( 'NONE',  ( -0.1409997244346088141, -0.002808977843308038680, -2.000147647483838220 ) ) ;
#72900=CARTESIAN_POINT ( 'NONE',  ( 2.975608675790370583, -0.2172404834940108442, 2.160205341352925856 ) ) ;
#72902=CARTESIAN_POINT ( 'NONE',  ( 0.2816890862925770511, 0.2015970107726860194, -2.110973810222869229 ) ) ;
#72903=EDGE_CURVE ( 'NONE', #205352, #137219, #82097, .T. ) ;
#72907=CARTESIAN_POINT ( 'NONE',  ( 0.5443023342626990280, 2.055102546481206272, 0.1540600304409632249 ) ) ;
#72913=CARTESIAN_POINT ( 'NONE',  ( 3.334525359879161766, 1.211162569113528598, -1.479845612687477274 ) ) ;
#72914=CARTESIAN_POINT ( 'NONE',  ( 5.242920984569427567, -1.516648554753729616, 0.9119251698698880304 ) ) ;
#72917=CARTESIAN_POINT ( 'NONE',  ( 0.05258934297286410597, 0.3095000349466696110, 1.784779062553583984 ) ) ;
#72919=CARTESIAN_POINT ( 'NONE',  ( 6.345329912860430355, 0.3219833572893218698, -1.888178885089139669 ) ) ;
#72920=CARTESIAN_POINT ( 'NONE',  ( 0.3618904354094238385, -0.5536326762660361833, 1.994880328902041589 ) ) ;
#72922=CARTESIAN_POINT ( 'NONE',  ( 5.875831987524620992, 1.115552982110395330, 1.501486808359139946 ) ) ;
#72923=CARTESIAN_POINT ( 'NONE',  ( 3.264084022359412529, 0.8216391472936382945, 1.630427331384458833 ) ) ;
#72924=CARTESIAN_POINT ( 'NONE',  ( 5.180388087185870738, -1.228261608319089149, 1.833297759731546073 ) ) ;
#72927=CARTESIAN_POINT ( 'NONE',  ( 3.719230382982277927, -1.817711772858042751, -0.9750064267827946995 ) ) ;
#72932=CARTESIAN_POINT ( 'NONE',  ( 0.5972264258897291844, 1.797487153981947916, -1.200333582630601637 ) ) ;
#72933=CARTESIAN_POINT ( 'NONE',  ( 6.777786256569462431, -2.009253640576996514, 0.4989836931604470505 ) ) ;
#72935=CARTESIAN_POINT ( 'NONE',  ( 4.306063477043454490, -2.156128079323017754, 0.1542669963271598166 ) ) ;
#72936=CARTESIAN_POINT ( 'NONE',  ( 3.897132395768299951, -0.2000006916238558641, -2.009757592718981911 ) ) ;
#72937=CARTESIAN_POINT ( 'NONE',  ( 1.820681965693775162, -1.389665069980907441, 1.385087887197037571 ) ) ;
#72938=CARTESIAN_POINT ( 'NONE',  ( 6.720655732516649827, 4.686306134629722564, 2.836255308917837947 ) ) ;
#72944=CARTESIAN_POINT ( 'NONE',  ( 2.905482715143858030, -1.942096844255640109, 0.5424705965835219246 ) ) ;
#72948=CARTESIAN_POINT ( 'NONE',  ( 5.238497809344139000, 1.134185964801931679, -1.539638564045167080 ) ) ;
#72952=CARTESIAN_POINT ( 'NONE',  ( 4.657827466662149973, 1.163286545301238206, 1.646828140416577657 ) ) ;
#72955=CARTESIAN_POINT ( 'NONE',  ( 6.563511714949607168, 0.2886701521849396879, -1.700279369998755508 ) ) ;
#72960=CARTESIAN_POINT ( 'NONE',  ( 4.604681543780857034, 1.447206075137374759, -1.185162884121161442 ) ) ;
#72962=CARTESIAN_POINT ( 'NONE',  ( 1.797802452481820135, -1.496673605676283492, -1.430578824989765518 ) ) ;
#72963=ORIENTED_EDGE ( 'NONE', *, *, #8288, .T. ) ;
#72965=CARTESIAN_POINT ( 'NONE',  ( 0.2632962822839111650, 1.880428227362867633, -0.7283992291491694360 ) ) ;
#72966=CARTESIAN_POINT ( 'NONE',  ( 0.5975729546051986585, 1.217269667385068477, 1.341803709015822132 ) ) ;
#72973=CARTESIAN_POINT ( 'NONE',  ( 5.905858165902563073, -1.068448527453051966, -1.589740232873719128 ) ) ;
#72980=CARTESIAN_POINT ( 'NONE',  ( 3.204151765443470357, -2.159293047372488950, 0.1044485798024074874 ) ) ;
#72983=CARTESIAN_POINT ( 'NONE',  ( 0.9320672075895163333, -2.067649466203642206, 0.4702014512557165515 ) ) ;
#72984=CARTESIAN_POINT ( 'NONE',  ( 6.088856429251793934, -0.2706771573857471580, -1.805266125362497531 ) ) ;
#72985=CARTESIAN_POINT ( 'NONE',  ( 2.108605603913331183, 1.463472826393363624, -1.321001006224751917 ) ) ;
#72986=CARTESIAN_POINT ( 'NONE',  ( 3.920094060441734030, -1.906919942518231936, 0.1457910263855527466 ) ) ;
#72989=CARTESIAN_POINT ( 'NONE',  ( 5.353942763280384654, -0.7107094859252837127, 1.837027094894280399 ) ) ;
#72990=CARTESIAN_POINT ( 'NONE',  ( 0.7791178172221034925, 1.303614328124411692, 1.439515497156283796 ) ) ;
#72996=CARTESIAN_POINT ( 'NONE',  ( 4.635362334195573197, -0.09024504784891507203, 1.910265517452472084 ) ) ;
#72998=CARTESIAN_POINT ( 'NONE',  ( 0.5873203293235220723, -0.2722241568871349160, -2.189838084831654541 ) ) ;
#73000=CARTESIAN_POINT ( 'NONE',  ( -0.1049974700286886165, -0.1398519552151776535, -1.881156918050665094 ) ) ;
#73002=CARTESIAN_POINT ( 'NONE',  ( 1.506653248757179320, -2.110590818861147078, -0.2044851626497797559 ) ) ;
#73004=CARTESIAN_POINT ( 'NONE',  ( 5.524625123954316486, 0.3981063221985549072, 1.976670730632006601 ) ) ;
#73006=CARTESIAN_POINT ( 'NONE',  ( 2.154816067267216084, -0.5500195584662928017, -1.995915215819036748 ) ) ;
#73010=CARTESIAN_POINT ( 'NONE',  ( 0.3038912542124502236, -0.5749842496362895794, 2.083749421223294540 ) ) ;
#73018=CARTESIAN_POINT ( 'NONE',  ( 6.925078400183575233, 4.701279733332940580, 2.318349140213359583 ) ) ;
#73020=CARTESIAN_POINT ( 'NONE',  ( 4.922368227709418065, -1.231479607182428104, -1.221251793340462299 ) ) ;
#73022=CARTESIAN_POINT ( 'NONE',  ( 2.377862429009020229, -2.009158356589606953, 0.4988364127441884399 ) ) ;
#73023=CARTESIAN_POINT ( 'NONE',  ( 3.568056664072499995, -1.041641863948725932, 1.843179926220348541 ) ) ;
#73026=CARTESIAN_POINT ( 'NONE',  ( 1.586696308167453662, 1.896558138806573757, 0.5304675795299080843 ) ) ;
#73028=CARTESIAN_POINT ( 'NONE',  ( 3.152547991667663307, -1.735656589536422212, 1.497406435017712756 ) ) ;
#73029=CARTESIAN_POINT ( 'NONE',  ( 1.277666653898035021, 1.085793613588705853, 1.467558327050644706 ) ) ;
#73034=CARTESIAN_POINT ( 'NONE',  ( 3.041273912350466624, 0.05370876457178561797, 2.012661466405294863 ) ) ;
#73035=CARTESIAN_POINT ( 'NONE',  ( 3.326955106232618586, -1.810811308836293598, -0.7551016064811162387 ) ) ;
#73039=CARTESIAN_POINT ( 'NONE',  ( 6.175741434174033984, -1.119382356216396479, 1.765513623829425116 ) ) ;
#73040=CARTESIAN_POINT ( 'NONE',  ( 4.240886712856615226, -1.539575280908970223, 0.8727758839858139606 ) ) ;
#73042=CARTESIAN_POINT ( 'NONE',  ( 1.008081207548201741, -0.9882381260516819310, -1.956047874660173047 ) ) ;
#73043=CARTESIAN_POINT ( 'NONE',  ( 5.314300430047540935, 1.610136290765556977, 0.6609758457527656894 ) ) ;
#73045=CARTESIAN_POINT ( 'NONE',  ( 0.1333692844072316419, 7.629137130509075604, -2.653547345224521514 ) ) ;
#73046=CARTESIAN_POINT ( 'NONE',  ( 6.522148393938469901, -2.055459957301557949, 1.029436805849759828 ) ) ;
#73048=CARTESIAN_POINT ( 'NONE',  ( 5.448516766998877436, 1.166291874360864345, 1.283151444216067638 ) ) ;
#73049=CARTESIAN_POINT ( 'NONE',  ( 1.524350002934187653, -1.228176919886795782, -1.833354347511229498 ) ) ;
#73050=CARTESIAN_POINT ( 'NONE',  ( 5.283699308645180892, -2.063335151747126339, 0.6760268296895615148 ) ) ;
#73052=CARTESIAN_POINT ( 'NONE',  ( 1.376322447316252306, -2.107681897322019271, -0.2017570171880012919 ) ) ;
#73053=CARTESIAN_POINT ( 'NONE',  ( 4.406250000000002665, 1.895863743163984649, -0.7852924748302168023 ) ) ;
#73054=CARTESIAN_POINT ( 'NONE',  ( 6.827182134110199918, 2.946470958711099541, 2.641117900019366527 ) ) ;
#73055=CARTESIAN_POINT ( 'NONE',  ( 4.541967935523826938, 0.8243062533531859692, -1.741262965308258970 ) ) ;
#73056=CARTESIAN_POINT ( 'NONE',  ( 1.524421784905782618, -2.203991335649616357, 0.2763902372489163151 ) ) ;
#73061=CARTESIAN_POINT ( 'NONE',  ( 4.037882060770150439, -2.125535223720369071, 0.6451317522137323124 ) ) ;
#73067=CARTESIAN_POINT ( 'NONE',  ( 2.373672848961404735, -0.3474683332905931232, -1.986100487175908258 ) ) ;
#73069=CARTESIAN_POINT ( 'NONE',  ( 6.127400154304522673, 0.1556050751826357770, -2.056880999590751991 ) ) ;
#73071=CARTESIAN_POINT ( 'NONE',  ( 6.216323138650166058, 1.627425874425829200, 0.6175015193602851893 ) ) ;
#73073=CARTESIAN_POINT ( 'NONE',  ( 1.721574597234516890, -0.9778441516922768972, -1.474834890465251291 ) ) ;
#73074=CARTESIAN_POINT ( 'NONE',  ( 0.6334356698059575574, 0.5880228326464317368, 1.928751028484784413 ) ) ;
#73075=CARTESIAN_POINT ( 'NONE',  ( -0.006632162239710717895, -1.840811702136424088, -0.04651623371411393176 ) ) ;
#73076=CARTESIAN_POINT ( 'NONE',  ( 4.282983983471492451, 2.047787327626307441, -1.030491903107624951 ) ) ;
#73077=CARTESIAN_POINT ( 'NONE',  ( 2.185277780439310202, -0.7877041259056734024, 1.664256631099890971 ) ) ;
#73080=CARTESIAN_POINT ( 'NONE',  ( 3.469579810302122702, 1.781292651720441711, -0.3989491859636914994 ) ) ;
#73081=CARTESIAN_POINT ( 'NONE',  ( 3.779922787921150995, 1.701948043757589124, -1.081065327119046016 ) ) ;
#73083=CARTESIAN_POINT ( 'NONE',  ( 3.256942907105137230, -1.714491093362701335, 1.476422526664717072 ) ) ;
#73085=CARTESIAN_POINT ( 'NONE',  ( 5.456126526903398499, 2.103703387787753343, -0.1000602029373430374 ) ) ;
#73087=CARTESIAN_POINT ( 'NONE',  ( 2.400909748719297188, 0.4512941399696759337, 2.020426262116347349 ) ) ;
#73090=CARTESIAN_POINT ( 'NONE',  ( 5.918629486560170960, -0.7630358368452618834, -1.978611909900826582 ) ) ;
#73093=CARTESIAN_POINT ( 'NONE',  ( 1.277817996239123177, 1.146848889641904234, 1.547804080865310850 ) ) ;
#73100=CARTESIAN_POINT ( 'NONE',  ( 0.3873739525321840960, -2.094434250752406079, -0.7407286751721677831 ) ) ;
#73101=CARTESIAN_POINT ( 'NONE',  ( 2.028482804581877019, 1.213238276247522895, -1.721163102310949045 ) ) ;
#73104=CARTESIAN_POINT ( 'NONE',  ( 5.893359673372067675, -1.683065101977880840, 0.7942114673132483205 ) ) ;
#73109=CARTESIAN_POINT ( 'NONE',  ( 0.4926326669930108371, -1.172979896111199904, 1.766458537607276114 ) ) ;
#73112=CARTESIAN_POINT ( 'NONE',  ( 2.980854556682940526, 1.846358069237159949, 0.6635599008937702603 ) ) ;
#73113=CARTESIAN_POINT ( 'NONE',  ( 2.026462046419864826, 1.244889377058140845, -1.767065586814352773 ) ) ;
#73114=CARTESIAN_POINT ( 'NONE',  ( 1.100829259350871281, -0.4471758257712907247, 1.786007343351428966 ) ) ;
#73117=CARTESIAN_POINT ( 'NONE',  ( 3.310250384734690243, 1.573932026098995518, 0.7429073729697617257 ) ) ;
#73121=CARTESIAN_POINT ( 'NONE',  ( 0.6202742476981680797, -1.157488721396517040, -1.825510493854154426 ) ) ;
#73122=CARTESIAN_POINT ( 'NONE',  ( 2.249374845261054467, -1.976652949091894707, -0.3960421909960794018 ) ) ;
#73125=CARTESIAN_POINT ( 'NONE',  ( 2.694160965578366262, -1.966063403948969057, -0.1468289651068572232 ) ) ;
#73134=CARTESIAN_POINT ( 'NONE',  ( 6.018676637735699941, 1.555688181992231245, -1.704518584337791021 ) ) ;
#73136=CARTESIAN_POINT ( 'NONE',  ( 3.573055779259231457, 1.771592698278463107, 0.8429337356923997104 ) ) ;
#73138=CARTESIAN_POINT ( 'NONE',  ( 0.1412502902482688505, 0.7743183493036235321, 1.862015731718666078 ) ) ;
#73140=CARTESIAN_POINT ( 'NONE',  ( 2.641944905847165792, 2.106676525318150972, -0.2125944600365035908 ) ) ;
#73143=CARTESIAN_POINT ( 'NONE',  ( 2.308333576337255000, 1.644441489820291924, 0.8281405146027611686 ) ) ;
#73147=CARTESIAN_POINT ( 'NONE',  ( 3.586284538990120119, 1.181046903802231984, 1.761068336431830472 ) ) ;
#73149=CARTESIAN_POINT ( 'NONE',  ( 0.5855841007226803008, -1.826885663252286740, -0.2280376995877145263 ) ) ;
#73153=CARTESIAN_POINT ( 'NONE',  ( 4.692684478349196553, -0.4476203070050369104, -2.011419953914685088 ) ) ;
#73155=CARTESIAN_POINT ( 'NONE',  ( 1.874305484616908934, -0.09156810461483089192, -1.839108553062768214 ) ) ;
#73161=CARTESIAN_POINT ( 'NONE',  ( 0.6455096168876961471, -1.890800792967793686, 1.137844069391671820 ) ) ;
#73162=CARTESIAN_POINT ( 'NONE',  ( 3.304270634109522486, -2.259957100417890441, 0.1074057698594049759 ) ) ;
#73164=CARTESIAN_POINT ( 'NONE',  ( 3.462975342835975301, -1.477922853017235916, 1.047338699574466014 ) ) ;
#73165=CARTESIAN_POINT ( 'NONE',  ( 4.276519664212295346, -0.4255873229474533281, -1.867665486979957157 ) ) ;
#73166=CARTESIAN_POINT ( 'NONE',  ( 5.740704066448026666, -2.019076491677873619, -0.4572469816465085657 ) ) ;
#73168=CARTESIAN_POINT ( 'NONE',  ( 2.588696453722662660, -0.3354253448964693574, -1.942569732146891770 ) ) ;
#73169=CARTESIAN_POINT ( 'NONE',  ( 1.078981819582014445, -0.04439612541052954248, -1.926037623753373618 ) ) ;
#73170=CARTESIAN_POINT ( 'NONE',  ( 4.328871119428026049, 0.09166491666120352155, 1.868520897946590598 ) ) ;
#73171=CARTESIAN_POINT ( 'NONE',  ( 2.122082200655984074, -2.237848761721575208, 0.5630162806932179631 ) ) ;
#73172=CARTESIAN_POINT ( 'NONE',  ( 3.736619961808427259, -1.792986960150410036, -0.4983748678565723678 ) ) ;
#73179=CARTESIAN_POINT ( 'NONE',  ( 0.6804681372492230595, -1.168251705716750299, 1.752132397912719242 ) ) ;
#73183=CARTESIAN_POINT ( 'NONE',  ( 1.723052270212792836, 1.567896913533245229, -1.427966198690698851 ) ) ;
#73185=CARTESIAN_POINT ( 'NONE',  ( 0.4397206748869232351, -1.916487937148562137, 0.6377882026268544280 ) ) ;
#73190=CARTESIAN_POINT ( 'NONE',  ( 1.563986776035675819, 2.129895014553784272, -0.3678597298803277793 ) ) ;
#73191=CARTESIAN_POINT ( 'NONE',  ( 6.610000000000042952, 4.702635990354799844, 2.282722937023287102 ) ) ;
#73193=CARTESIAN_POINT ( 'NONE',  ( 6.925078400183573457, 0.5887076473912872254, 1.908330883025354030 ) ) ;
#73195=CARTESIAN_POINT ( 'NONE',  ( -0.2104748580754409182, 1.337026610731705700, -2.356057411969681326 ) ) ;
#73196=CARTESIAN_POINT ( 'NONE',  ( 5.928922775424462444, -1.700964743930567513, 1.082835439959836776 ) ) ;
#73198=CARTESIAN_POINT ( 'NONE',  ( 6.614806893291146572, -0.1579704184760947761, 2.055781730312715272 ) ) ;
#73200=CARTESIAN_POINT ( 'NONE',  ( 0.3041012005207919255, -0.5996659824250392123, 2.181524510355018265 ) ) ;
#73204=CARTESIAN_POINT ( 'NONE',  ( 1.282674911181800104, 1.565081248417903081, -1.104254300028691071 ) ) ;
#73208=CARTESIAN_POINT ( 'NONE',  ( 2.437784706471317175, 0.8137022719644730895, -1.520871857739027444 ) ) ;
#73210=CARTESIAN_POINT ( 'NONE',  ( 1.827073579719180163, -1.668441312418825095, 0.5905873696427661468 ) ) ;
#73211=CARTESIAN_POINT ( 'NONE',  ( 1.787745399045566730, 1.925802014453177557, -0.5863169366013292194 ) ) ;
#73214=CARTESIAN_POINT ( 'NONE',  ( 3.751171811254182753, -1.805526059370649028, 1.268566889074909554 ) ) ;
#73216=CARTESIAN_POINT ( 'NONE',  ( 4.658466178349073061, 2.014666459302273616, 0.1442823096002471550 ) ) ;
#73218=CARTESIAN_POINT ( 'NONE',  ( 3.932379033323248230, -1.091282289853046317, -1.817994770353311473 ) ) ;
#73219=CARTESIAN_POINT ( 'NONE',  ( 4.464470365011488973, -1.956567236562205325, -0.4871837624095613495 ) ) ;
#73223=CARTESIAN_POINT ( 'NONE',  ( 1.410794581852807150, 1.648159533202856686, 0.8848386531258023435 ) ) ;
#73231=CARTESIAN_POINT ( 'NONE',  ( 4.223842396274177347, 0.8578445224393380641, -1.825075645057252505 ) ) ;
#73235=CARTESIAN_POINT ( 'NONE',  ( 4.430007776716601953, -2.079114408633813582, 0.4165480963118637914 ) ) ;
#73238=CARTESIAN_POINT ( 'NONE',  ( 5.202397865228217455, -0.6614073030348812665, -1.857238293531390916 ) ) ;
#73240=CARTESIAN_POINT ( 'NONE',  ( 0.4748584900105623507, -1.455329053371579695, 1.391259960792426975 ) ) ;
#73242=CARTESIAN_POINT ( 'NONE',  ( 6.227753904044541322, 0.8083430201051154951, -1.957153335705215103 ) ) ;
#73244=CARTESIAN_POINT ( 'NONE',  ( 1.064989848632340363, 1.568927673159369762, -1.351003706900590018 ) ) ;
#73248=CARTESIAN_POINT ( 'NONE',  ( 3.574242788201603016, -2.014869992041759872, -0.5574694344734670848 ) ) ;
#73251=CARTESIAN_POINT ( 'NONE',  ( 2.274178591966895091, -1.125271047149905890, 1.437439779654096750 ) ) ;
#73252=CARTESIAN_POINT ( 'NONE',  ( 1.681973674898680216, 0.9313724848135003231, 1.553549296804368707 ) ) ;
#73254=CARTESIAN_POINT ( 'NONE',  ( 5.162800556355915838, -1.600310254184673431, 1.519886962452212886 ) ) ;
#73257=CARTESIAN_POINT ( 'NONE',  ( 4.366400497975233996, 1.037236317483503312, 1.947806255051434343 ) ) ;
#73260=CARTESIAN_POINT ( 'NONE',  ( 2.982959643696237784, -1.767753630637520779, -0.7297678730374329570 ) ) ;
#73263=CARTESIAN_POINT ( 'NONE',  ( 5.494608840674215955, 2.039112051642687717, 0.3575134270455831986 ) ) ;
#73265=CARTESIAN_POINT ( 'NONE',  ( 6.392125918040960642, -0.5824770489515176397, -2.112646119873210271 ) ) ;
#73276=CARTESIAN_POINT ( 'NONE',  ( 5.911005882915712384, -1.635593682349820721, 1.269112435710928688 ) ) ;
#73277=CARTESIAN_POINT ( 'NONE',  ( 4.775960602080351336, 1.110526314841601359, 1.574030653434669746 ) ) ;
#73278=CARTESIAN_POINT ( 'NONE',  ( 1.370720498019749378, -0.2986500928384462350, -1.994069080148860973 ) ) ;
#73282=CARTESIAN_POINT ( 'NONE',  ( 1.377182423176852133, 2.023737929115625445, -0.8412682346608522099 ) ) ;
#73283=CARTESIAN_POINT ( 'NONE',  ( 5.654876981934024549, -1.436564326775534806, 1.126588154728463742 ) ) ;
#73291=CARTESIAN_POINT ( 'NONE',  ( 2.753256032281672372, 1.832158412346639453, -0.1828795585285883096 ) ) ;
#73292=CARTESIAN_POINT ( 'NONE',  ( 6.293232695293600187, -0.1032093112793490142, -2.010699630015537309 ) ) ;
#73293=CARTESIAN_POINT ( 'NONE',  ( 2.443060400399544196, 1.412781429710145975, 1.812861393458516268 ) ) ;
#73294=CARTESIAN_POINT ( 'NONE',  ( 6.930524233185829885, -1.209519613549964845, 1.545115813350018241 ) ) ;
#73297=CARTESIAN_POINT ( 'NONE',  ( 2.900541297466651347, -1.884798985816903860, -0.3226963764228693576 ) ) ;
#73300=CARTESIAN_POINT ( 'NONE',  ( 0.1392002015415672034, -0.1474423581745692435, -2.037351525059682977 ) ) ;
#73302=CARTESIAN_POINT ( 'NONE',  ( 3.034800296023100419, -1.842769725714489493, 0.9876625208589999705 ) ) ;
#73303=CARTESIAN_POINT ( 'NONE',  ( 0.7779422811538607707, -1.042605501850740080, 1.552959968518424771 ) ) ;
#73304=CARTESIAN_POINT ( 'NONE',  ( 1.862657450031137474, -0.6818942500997280387, 1.897406292459068222 ) ) ;
#73308=CARTESIAN_POINT ( 'NONE',  ( 2.050002923743666550, -1.344770872215072632, 1.104816081682137963 ) ) ;
#73312=CARTESIAN_POINT ( 'NONE',  ( 2.455304126353729188, 0.4608866456157869607, -1.662088558372651903 ) ) ;
#73313=CARTESIAN_POINT ( 'NONE',  ( 2.542740116143254792, -1.820367712357463974, 1.220030464664762393 ) ) ;
#73314=CARTESIAN_POINT ( 'NONE',  ( 4.811249113497881424, 1.919052844561389692, 1.089612025192594258 ) ) ;
#73316=CARTESIAN_POINT ( 'NONE',  ( 2.395604216770229833, -1.940863096919882569, 0.9729980962204368700 ) ) ;
#73317=CARTESIAN_POINT ( 'NONE',  ( 0.5744775230259161480, -1.718042477583326066, -0.6180270036199516648 ) ) ;
#73319=CARTESIAN_POINT ( 'NONE',  ( 4.083301318022297899, 1.702923931485133879, 1.258099284506300153 ) ) ;
#73323=CARTESIAN_POINT ( 'NONE',  ( 5.214511053166543064, 2.117144789807279270, 0.8794703464902029477 ) ) ;
#73327=CARTESIAN_POINT ( 'NONE',  ( 6.621772978582266767, -0.4938884631311352691, 2.173981893038397839 ) ) ;
#73333=CARTESIAN_POINT ( 'NONE',  ( 4.817029820108094995, 1.034167108704350024, -1.730865207599366240 ) ) ;
#73335=CARTESIAN_POINT ( 'NONE',  ( 3.256738233524118620, -0.5941274279437200878, -1.975181216424357400 ) ) ;
#73337=CARTESIAN_POINT ( 'NONE',  ( -0.2409995289980246258, 1.355929887833319469, -2.254219809973062816 ) ) ;
#73342=CARTESIAN_POINT ( 'NONE',  ( 5.894512528888635750, 1.793468170635740710, -1.259063434910556500 ) ) ;
#73343=CARTESIAN_POINT ( 'NONE',  ( 4.113907844847329187, 0.1017495355152969322, 2.013985960686740295 ) ) ;
#73344=CARTESIAN_POINT ( 'NONE',  ( 2.806014743833367131, 1.331929863061011465, -1.271513748034671654 ) ) ;
#73347=CARTESIAN_POINT ( 'NONE',  ( 6.053692819838605743, 0.5272490726609192491, -1.747765065496959869 ) ) ;
#73348=CARTESIAN_POINT ( 'NONE',  ( 0.1944798361989338309, 2.004116887782161349, 1.125739740898183294 ) ) ;
#73350=CARTESIAN_POINT ( 'NONE',  ( 6.789870067575622947, -0.9739125386618008307, 2.039881742057749303 ) ) ;
#73351=CARTESIAN_POINT ( 'NONE',  ( 1.910898437428062646, 1.559696066972179107, -1.415416642437119954 ) ) ;
#73360=CARTESIAN_POINT ( 'NONE',  ( 3.726986581234917661, 1.568921747024876634, -1.572872013324580154 ) ) ;
#73361=CARTESIAN_POINT ( 'NONE',  ( 2.818527994553555516, 2.063739945100159900, 0.7375456357434084786 ) ) ;
#73364=CARTESIAN_POINT ( 'NONE',  ( 0.6806489137391663613, -1.222764829241920648, 1.836970590647703627 ) ) ;
#73366=CARTESIAN_POINT ( 'NONE',  ( 4.984793487045196869, 1.876812866478014596, 0.5713181500588762063 ) ) ;
#73368=CARTESIAN_POINT ( 'NONE',  ( 6.777182134110200096, 7.629137130509070275, 2.410944104600750038 ) ) ;
#73373=CARTESIAN_POINT ( 'NONE',  ( 3.726904977748810133, 1.497142547446396410, -1.502090761940577002 ) ) ;
#73375=CARTESIAN_POINT ( 'NONE',  ( 5.436455051933180016, 2.129025116502227810, 0.3735886874452337691 ) ) ;
#73377=CARTESIAN_POINT ( 'NONE',  ( 3.878315922200573862, -0.1843894689829879974, -1.832007427040844183 ) ) ;
#73380=CARTESIAN_POINT ( 'NONE',  ( 6.562468561866369399, -1.594522334811569131, -0.6977961348336658709 ) ) ;
#73384=CARTESIAN_POINT ( 'NONE',  ( 4.469695567000064429, 2.097540297429688838, -0.5223010940857697459 ) ) ;
#73387=CARTESIAN_POINT ( 'NONE',  ( 0.1394461523056798324, 0.009327122704651937685, -1.719853553173174232 ) ) ;
#73391=CARTESIAN_POINT ( 'NONE',  ( 3.010779355932476253, 1.566693023359872372, -1.489686202715050145 ) ) ;
#73392=CARTESIAN_POINT ( 'NONE',  ( 5.009034487593355678, 1.713717141372484765, 0.9743026824079579207 ) ) ;
#73393=CARTESIAN_POINT ( 'NONE',  ( 3.901445378353602944, 0.2529189268129055090, 1.715120161964154510 ) ) ;
#73394=CARTESIAN_POINT ( 'NONE',  ( 0.3456114054924685486, 0.6817542107791437767, -2.082909237240769151 ) ) ;
#73395=CARTESIAN_POINT ( 'NONE',  ( 0.9038794553481295235, 1.888499008566895787, 1.325839279686758632 ) ) ;
#73396=CARTESIAN_POINT ( 'NONE',  ( 3.813790581289760784, -2.030913156241159978, 0.3485601269093330234 ) ) ;
#73397=CARTESIAN_POINT ( 'NONE',  ( 5.688998805639625012, 1.473442329711650345, 1.265259504309938610 ) ) ;
#73404=CARTESIAN_POINT ( 'NONE',  ( 2.714145368365259436, -2.182908968410116834, 0.3227909207665635716 ) ) ;
#73407=CARTESIAN_POINT ( 'NONE',  ( 1.199803204733034923, 0.7606819372595281514, -1.698589668608577963 ) ) ;
#73408=CARTESIAN_POINT ( 'NONE',  ( -0.02880301295726198432, 1.985184585160368664, -2.687100061827327302 ) ) ;
#73413=CARTESIAN_POINT ( 'NONE',  ( 6.456982894382444549, 0.3095715517048603926, -1.814770079682447967 ) ) ;
#73415=CARTESIAN_POINT ( 'NONE',  ( 2.342715047087840397, 0.4503528687099351280, 2.010914609654746332 ) ) ;
#73423=CARTESIAN_POINT ( 'NONE',  ( 1.006794875882726314, 1.561001636543899673, -1.345678083183374341 ) ) ;
#73425=CARTESIAN_POINT ( 'NONE',  ( 5.056134578334451568, -1.329838508726857382, 1.273713382018211382 ) ) ;
#73429=CARTESIAN_POINT ( 'NONE',  ( 4.969440760808212509, 0.2186952961555181096, -2.196011921426939129 ) ) ;
#73430=CARTESIAN_POINT ( 'NONE',  ( 6.696538538688765918, -0.5935452916538739299, -2.183133895321730744 ) ) ;
#73432=CARTESIAN_POINT ( 'NONE',  ( 0.3867804997886997720, -1.801505969789623629, -0.6421655129100201087 ) ) ;
#73433=CARTESIAN_POINT ( 'NONE',  ( 0.6554828803995507158, 1.942095732595986890, -0.5424746339172461518 ) ) ;
#73438=CARTESIAN_POINT ( 'NONE',  ( 1.129532124359374334, -1.183843481993757774, -1.448407549327054955 ) ) ;
#73439=CARTESIAN_POINT ( 'NONE',  ( 2.237517880698642880, 0.5331670712399002587, -1.944730990508992008 ) ) ;
#73443=CARTESIAN_POINT ( 'NONE',  ( 4.248724916491292802, 0.5614479688690295900, 2.029775142636090379 ) ) ;
#73448=CARTESIAN_POINT ( 'NONE',  ( 3.849871613625083899, -1.395920841890609498, -1.459997210279185831 ) ) ;
#73452=CARTESIAN_POINT ( 'NONE',  ( 6.197729521560835231, -1.491448369540880670, -1.425081351520232964 ) ) ;
#73454=CARTESIAN_POINT ( 'NONE',  ( 4.218171724704827596, -1.107204882465680607, -1.856345114869990320 ) ) ;
#73461=CARTESIAN_POINT ( 'NONE',  ( 2.067058339702015246, 1.609816819982702985, -1.457078277656477905 ) ) ;
#73464=CARTESIAN_POINT ( 'NONE',  ( 2.296224312773272658, 1.477747569344042278, -1.098160524033331642 ) ) ;
#73466=CARTESIAN_POINT ( 'NONE',  ( 3.298540952264991777, 1.726358142885858316, -1.349911518210664241 ) ) ;
#73467=CARTESIAN_POINT ( 'NONE',  ( 6.983263157960363898, 3.684327263089666182, 2.667753665259400275 ) ) ;
#73468=CARTESIAN_POINT ( 'NONE',  ( 3.713984175222109663, -2.229511888261398678, 0.3841874803040145059 ) ) ;
#73474=CARTESIAN_POINT ( 'NONE',  ( 5.606658687911298955, 1.339352548545174937, -1.156898068784556255 ) ) ;
#73475=CARTESIAN_POINT ( 'NONE',  ( 3.545567672969043294, -1.859159518717553139, 0.7725093927312511877 ) ) ;
#73477=CARTESIAN_POINT ( 'NONE',  ( 2.186679620839627969, -2.065140684961807249, -0.4117111178513747638 ) ) ;
#73481=CARTESIAN_POINT ( 'NONE',  ( 0.6605274321102487800, -0.6603073245880388686, -1.855717402334137622 ) ) ;
#73484=CARTESIAN_POINT ( 'NONE',  ( 5.976795019380008789, -1.274598912183276589, 1.287626877918945922 ) ) ;
#73485=ORIENTED_EDGE ( 'NONE', *, *, #103038, .F. ) ;
#73488=CARTESIAN_POINT ( 'NONE',  ( 4.873830839387755631, 1.077430855447782942, 1.529020332772989210 ) ) ;
#73491=CARTESIAN_POINT ( 'NONE',  ( 4.188381925097388603, 1.111774711627441681, -1.746232563387891457 ) ) ;
#73501=CARTESIAN_POINT ( 'NONE',  ( 4.299235682465595509, -1.708000122724560477, 0.9650500775852040025 ) ) ;
#73503=CARTESIAN_POINT ( 'NONE',  ( 2.530624857006387618, 1.977747929495787371, -0.3905373530270899174 ) ) ;
#73505=CARTESIAN_POINT ( 'NONE',  ( 6.639320575229258559, 2.978120323461688645, 2.350396677589302374 ) ) ;
#73507=CARTESIAN_POINT ( 'NONE',  ( 2.442468673064964957, 0.4055347385497136137, 1.825902681341363021 ) ) ;
#73509=CARTESIAN_POINT ( 'NONE',  ( 4.359639327901571271, -1.559048523801108477, -1.273764430229076483 ) ) ;
#73512=CARTESIAN_POINT ( 'NONE',  ( 3.497769638136785986, -2.085511745926827309, 0.3643098080348127765 ) ) ;
#73514=CARTESIAN_POINT ( 'NONE',  ( 5.037584538744971141, 1.933038169019934527, -0.7419538039311265321 ) ) ;
#73516=CARTESIAN_POINT ( 'NONE',  ( 1.452797965663179314, -1.794991982752047965, -1.071751678227941929 ) ) ;
#73517=CARTESIAN_POINT ( 'NONE',  ( 6.620655732516642189, 2.417337544263608251, 2.554705107920357321 ) ) ;
#73518=CARTESIAN_POINT ( 'NONE',  ( 6.124025070245508573, -1.016541136310184390, -1.516163765885633286 ) ) ;
#73526=CARTESIAN_POINT ( 'NONE',  ( 6.340485057729076779, 1.096952271789692901, -1.566184530335120950 ) ) ;
#73534=CARTESIAN_POINT ( 'NONE',  ( 6.310172759758509109, 1.158674036163497734, -1.650093421473826316 ) ) ;
#73539=CARTESIAN_POINT ( 'NONE',  ( -0.1399997263889819488, 4.088450529495776919, -2.555104583160577203 ) ) ;
#73542=CARTESIAN_POINT ( 'NONE',  ( 2.289847402107755947, -1.282740503449712577, -1.494545344566786449 ) ) ;
#73543=CARTESIAN_POINT ( 'NONE',  ( 4.745720352911135365, 1.994069623535676961, -0.2986464557954356946 ) ) ;
#73545=CARTESIAN_POINT ( 'NONE',  ( 6.827182134110199030, 1.254919323356920025, 2.204230526214937758 ) ) ;
#73546=CARTESIAN_POINT ( 'NONE',  ( 4.892620165872568094, 1.823077252308364482, -1.215776859382920794 ) ) ;
#73548=CARTESIAN_POINT ( 'NONE',  ( 3.205993170255555302, -1.924248618553949353, 0.09317337220685062427 ) ) ;
#73550=CARTESIAN_POINT ( 'NONE',  ( -0.1294898018152357000, -0.0008549345193622873455, -1.926395771554180625 ) ) ;
#73560=CARTESIAN_POINT ( 'NONE',  ( 6.356982874815331641, 0.3076174260261410054, -1.815216213958574132 ) ) ;
#73561=CARTESIAN_POINT ( 'NONE',  ( 2.877592485514004039, 0.2932790309252801819, -1.991490711024199944 ) ) ;
#73562=CARTESIAN_POINT ( 'NONE',  ( 5.571695488097110349, 1.745893177897942738, -1.494929824115182937 ) ) ;
#73564=CARTESIAN_POINT ( 'NONE',  ( 3.115880741807099508, 1.852434257297396858, -0.1774315261868253668 ) ) ;
#73569=CARTESIAN_POINT ( 'NONE',  ( 6.128480205876102538, 0.2055166225264984381, 2.080635545183810553 ) ) ;
#73575=CARTESIAN_POINT ( 'NONE',  ( 6.024008130617486856, -0.9641997184709062418, -1.430004917837023104 ) ) ;
#73577=CARTESIAN_POINT ( 'NONE',  ( 1.617354066682510805, 0.1696363612940926524, 1.725835137016252796 ) ) ;
#73582=CARTESIAN_POINT ( 'NONE',  ( 6.543812728621629660, 1.490886027097729105, 1.578480410219210928 ) ) ;
#73583=CARTESIAN_POINT ( 'NONE',  ( 5.514214477338500231, -0.8245889995748825196, -1.628937154514856545 ) ) ;
#73584=CARTESIAN_POINT ( 'NONE',  ( 2.377722661024490147, -1.904092233959910896, 0.4717398701708991893 ) ) ;
#73588=CARTESIAN_POINT ( 'NONE',  ( 3.440189854244297241, -1.264556376030629981, -1.702001827410426049 ) ) ;
#73589=CARTESIAN_POINT ( 'NONE',  ( 6.827182134110199918, 0.5620517916639695688, 2.240906645742099190 ) ) ;
#73591=CARTESIAN_POINT ( 'NONE',  ( 1.639598513223254006, 1.914365469054382540, -0.7886191548351070280 ) ) ;
#73594=CARTESIAN_POINT ( 'NONE',  ( 2.930584098205230248, -1.096850167032170420, -1.931549987457868989 ) ) ;
#73596=CARTESIAN_POINT ( 'NONE',  ( 1.987358909443589283, -2.298030411116751992, 0.06136411900238383788 ) ) ;
#73598=CARTESIAN_POINT ( 'NONE',  ( 6.965701137139799215, -0.4614044149895025204, 2.017943399502773349 ) ) ;
#73601=EDGE_CURVE ( 'NONE', #88820, #29350, #197550, .T. ) ;
#73606=CARTESIAN_POINT ( 'NONE',  ( 3.234525475359388391, 1.209690070866603406, -1.481213593849866950 ) ) ;
#73607=CARTESIAN_POINT ( 'NONE',  ( -0.1104750535120268551, 0.2303756098476944791, -2.137063993957021513 ) ) ;
#73608=CARTESIAN_POINT ( 'NONE',  ( 4.049579987339441800, 0.5806670320154716514, -1.624208954244592773 ) ) ;
#73609=CARTESIAN_POINT ( 'NONE',  ( 1.815639016007553730, -1.320828798922760949, -1.523793687088881299 ) ) ;
#73610=CARTESIAN_POINT ( 'NONE',  ( 2.602471654445730032, -0.2222675636014606049, 2.287907847288372043 ) ) ;
#73611=CARTESIAN_POINT ( 'NONE',  ( 3.181238891614282416, -0.1630793868099291999, -2.256562113509274159 ) ) ;
#73612=CARTESIAN_POINT ( 'NONE',  ( 5.110040610736272804, -2.096041292509024156, 0.2052846074404850174 ) ) ;
#73614=CARTESIAN_POINT ( 'NONE',  ( 5.079261616685217362, 1.651278277306899911, -0.6370931631965012221 ) ) ;
#73616=CARTESIAN_POINT ( 'NONE',  ( 0.5512257746139355152, -1.939593085364198721, -1.221404215731338283 ) ) ;
#73617=B_SPLINE_CURVE_WITH_KNOTS ( 'NONE', 3,
 ( #59727, #141028, #125886, #90114, #106399, #191844, #43507, #159361, #60795, #122697 ),
 .UNSPECIFIED., .F., .F.,
 ( 4, 1, 1, 1, 1, 1, 1, 4 ),
 ( 0.000000000000000000, 0.09853459476447307130, 0.1926867929487333375, 0.2613852218134048999, 0.3629775382994345767, 0.5216635214973427415, 0.7338723600040717443, 1.000000000000000000 ),
 .UNSPECIFIED. ) ;
#73618=CARTESIAN_POINT ( 'NONE',  ( 5.542853976212075651, -1.453887124689148935, -1.129494548679485844 ) ) ;
#73621=CARTESIAN_POINT ( 'NONE',  ( 5.771465802492605768, 1.302860414194568550, 1.761948869136241047 ) ) ;
#73624=CARTESIAN_POINT ( 'NONE',  ( 5.986797818411375260, 1.994257276370488219, 0.5558945855626205024 ) ) ;
#73626=CARTESIAN_POINT ( 'NONE',  ( -0.01248194115436446205, -0.5331630387654020531, 1.944732228473695868 ) ) ;
#73629=CARTESIAN_POINT ( 'NONE',  ( 4.002502541323429419, -0.6052661472178870739, -1.829015351804675005 ) ) ;
#73632=CARTESIAN_POINT ( 'NONE',  ( 1.002519415922138002, -0.9925456330053865628, 1.987394366727333717 ) ) ;
#73643=CARTESIAN_POINT ( 'NONE',  ( 1.293326634533353170, -1.775083115552608559, 0.8357255594537355003 ) ) ;
#73646=CARTESIAN_POINT ( 'NONE',  ( 6.602011099637477010, 0.7519813002578833450, -1.812223124677159181 ) ) ;
#73649=CARTESIAN_POINT ( 'NONE',  ( 0.07556134207191073093, -0.004209888912004143384, -2.244269416743961187 ) ) ;
#73653=CARTESIAN_POINT ( 'NONE',  ( 0.8955150854165813135, -0.6789544621725839280, 1.743152336062703256 ) ) ;
#73654=CARTESIAN_POINT ( 'NONE',  ( 0.6504783628028444342, 0.8526279987398683868, 1.509985294034902337 ) ) ;
#73656=CARTESIAN_POINT ( 'NONE',  ( 4.388337494309430653, -0.4807229498768311182, -2.138019847805587403 ) ) ;
#73657=CARTESIAN_POINT ( 'NONE',  ( 4.964078638949532163, 2.283327717301757431, -0.3329734184051634238 ) ) ;
#73658=CARTESIAN_POINT ( 'NONE',  ( 6.608673410152685612, 1.530114183832030905, -1.380643333410998430 ) ) ;
#73659=CARTESIAN_POINT ( 'NONE',  ( 2.413922445368326564, 1.268163163618090561, -1.470779158573028322 ) ) ;
#73662=CARTESIAN_POINT ( 'NONE',  ( 4.887034483293543730, -1.997634423138573867, -0.7120497732875651353 ) ) ;
#73664=CARTESIAN_POINT ( 'NONE',  ( 3.656875104409584853, 1.122498086849915921, 1.674887873639265390 ) ) ;
#73668=CARTESIAN_POINT ( 'NONE',  ( 0.4690313652776016418, 0.1822212253758948297, -1.816563760317004395 ) ) ;
#73673=CARTESIAN_POINT ( 'NONE',  ( 5.049710947255391602, 0.6486796242286404501, -1.956199288699921768 ) ) ;
#73677=CARTESIAN_POINT ( 'NONE',  ( 4.986975786537023225, -1.902434985030461156, -0.6785184294546533490 ) ) ;
#73678=CARTESIAN_POINT ( 'NONE',  ( 6.041669411999269990, -2.092492953876758044, 0.7457244993839227121 ) ) ;
#73684=CARTESIAN_POINT ( 'NONE',  ( 4.153237585930975584, -1.712380083513395768, -1.146421031332397922 ) ) ;
#73685=CARTESIAN_POINT ( 'NONE',  ( 4.236954046275762664, 2.015912997090345549, -0.05229627655192746472 ) ) ;
#73687=CARTESIAN_POINT ( 'NONE',  ( 0.1753634416057497925, 0.0001173177735149660839, -2.144164757042037017 ) ) ;
#73692=CARTESIAN_POINT ( 'NONE',  ( 3.620470095612156047, 0.4925664443866035191, -1.954873191151075940 ) ) ;
#73693=CARTESIAN_POINT ( 'NONE',  ( 3.064218985076866630, -1.701416833343888824, -0.7040189834505713451 ) ) ;
#73695=CARTESIAN_POINT ( 'NONE',  ( 1.506910664365119334, -0.8341063803433286239, -2.151852887045426765 ) ) ;
#73697=CARTESIAN_POINT ( 'NONE',  ( 3.708425082824120533, -0.8722964037291662809, -1.977944213000272455 ) ) ;
#73700=CARTESIAN_POINT ( 'NONE',  ( 3.374663776259867909, -0.4515557078652779333, 2.253457335377069271 ) ) ;
#73703=CARTESIAN_POINT ( 'NONE',  ( 2.606148294764852213, -0.7140300644919925777, -1.729217693616967644 ) ) ;
#73705=CARTESIAN_POINT ( 'NONE',  ( 0.3507686748964663481, -1.586079953665324060, 1.170567870040557290 ) ) ;
#73707=CARTESIAN_POINT ( 'NONE',  ( 2.501185699981960830, -0.1928336239410358699, 2.007256303757164240 ) ) ;
#73709=CARTESIAN_POINT ( 'NONE',  ( 1.348561525465460820, 2.204488851003219896, 0.1053889787279923829 ) ) ;
#73713=CARTESIAN_POINT ( 'NONE',  ( 5.594591524781380443, -0.4782570758292312707, -1.912467619381743811 ) ) ;
#73714=CARTESIAN_POINT ( 'NONE',  ( 5.619831112054756161, -2.252673335196005766, 0.5002786026085581650 ) ) ;
#73715=CARTESIAN_POINT ( 'NONE',  ( 0.1507198084474276056, -0.4258245693303016610, -1.922078969575198526 ) ) ;
#73716=CARTESIAN_POINT ( 'NONE',  ( 3.432538798476657327, -1.232314722524804562, 1.653799735942045990 ) ) ;
#73724=CARTESIAN_POINT ( 'NONE',  ( 4.791568617006563002, -1.986896891843348723, 0.8757425373496147136 ) ) ;
#73726=CARTESIAN_POINT ( 'NONE',  ( 5.284640796330934087, 1.621094592300664328, -0.8731043043393662550 ) ) ;
#73731=CARTESIAN_POINT ( 'NONE',  ( 0.4911964603225346115, 1.381658100223854380, 1.261112594198803061 ) ) ;
#73732=CARTESIAN_POINT ( 'NONE',  ( 0.2282871097136250915, -1.394050316402313916, -1.782836666206646603 ) ) ;
#73738=CARTESIAN_POINT ( 'NONE',  ( 2.342341949348641261, 0.3848992280063111004, 1.727307115810622351 ) ) ;
#73739=CARTESIAN_POINT ( 'NONE',  ( 6.147140879040452255, 0.1997598139246952731, 2.003170966399501651 ) ) ;
#73741=CARTESIAN_POINT ( 'NONE',  ( 3.321808155663192874, 0.8583493116562285197, -1.712590381118280991 ) ) ;
#73743=CARTESIAN_POINT ( 'NONE',  ( 4.773860271397749599, -1.931934984910467890, 0.3821518213343431669 ) ) ;
#73744=CARTESIAN_POINT ( 'NONE',  ( 6.328379800955010737, -0.9556441952764772596, -1.779432800462784847 ) ) ;
#73747=CARTESIAN_POINT ( 'NONE',  ( 2.447944060942487621, 1.870205405844455049, 0.04815357881200743595 ) ) ;
#73748=CARTESIAN_POINT ( 'NONE',  ( 6.568995754424670430, -1.580519633186812767, -0.6912669513192554183 ) ) ;
#73750=CARTESIAN_POINT ( 'NONE',  ( 2.684424123961434816, -1.133677649706768431, 1.893296980138805097 ) ) ;
#73753=CARTESIAN_POINT ( 'NONE',  ( 6.654749070045313353, -0.5220710138904552933, -1.891073168474053823 ) ) ;
#73760=CARTESIAN_POINT ( 'NONE',  ( 2.154816067267216084, -0.5500195584662926906, -1.995915215819036748 ) ) ;
#73764=CARTESIAN_POINT ( 'NONE',  ( 6.024112365460934981, -2.104525519549589330, 0.2592714029671301934 ) ) ;
#73767=CARTESIAN_POINT ( 'NONE',  ( 0.07479286986305544449, 2.046156589154801253, -2.272744413733415403 ) ) ;
#73769=CARTESIAN_POINT ( 'NONE',  ( 5.536482449520531368, 1.943773098233076757, -0.5350085594507183462 ) ) ;
#73770=CARTESIAN_POINT ( 'NONE',  ( 4.733546111355320107, 0.5950593785610300834, -1.821060146467222918 ) ) ;
#73771=CARTESIAN_POINT ( 'NONE',  ( 6.539320575229251808, 7.629137130509035636, 2.603262396134010892 ) ) ;
#73772=CARTESIAN_POINT ( 'NONE',  ( 3.614928802375876771, -0.1595779646587774658, 2.185787688459623901 ) ) ;
#73774=CARTESIAN_POINT ( 'NONE',  ( 2.214975196874233720, 1.533708969217022933, -1.142120075431733994 ) ) ;
#73777=CARTESIAN_POINT ( 'NONE',  ( 6.257425474675967436, 2.026018168931587482, -0.6146651352928398371 ) ) ;
#73779=CARTESIAN_POINT ( 'NONE',  ( 5.653911837654605144, 0.8871495062587383407, 2.004161502255866090 ) ) ;
#73781=CARTESIAN_POINT ( 'NONE',  ( 3.363966847960923268, 0.7745139696748448710, 1.541148353905038126 ) ) ;
#73783=CARTESIAN_POINT ( 'NONE',  ( 6.205353461901607304, 1.844339991697005798, -1.046509186232460920 ) ) ;
#73788=CARTESIAN_POINT ( 'NONE',  ( 0.3265133270617843197, -1.284392789319420913, 1.483054880892266114 ) ) ;
#73795=CARTESIAN_POINT ( 'NONE',  ( 2.754343952779594318, 1.798010375687082218, 0.2196673718751484539 ) ) ;
#73800=CARTESIAN_POINT ( 'NONE',  ( 4.283730857329768327, 1.755957581118623434, -0.4444456398857503099 ) ) ;
#73804=CARTESIAN_POINT ( 'NONE',  ( 5.142936340713559318, -0.2273772366201456396, -1.847015746109672119 ) ) ;
#73806=CARTESIAN_POINT ( 'NONE',  ( 3.216317514422084578, 1.869562491224942224, 0.4167181705077570575 ) ) ;
#73807=CARTESIAN_POINT ( 'NONE',  ( 1.412830140145465263, 1.608106816955911178, 0.8641515426408912237 ) ) ;
#73819=CARTESIAN_POINT ( 'NONE',  ( 1.500065138910465334, -0.7538795759346494929, -1.950162888426725250 ) ) ;
#73820=CARTESIAN_POINT ( 'NONE',  ( 6.106463915388694375, -0.6937866221692154944, -1.797298315204816310 ) ) ;
#73822=CARTESIAN_POINT ( 'NONE',  ( 2.045663570152244315, 0.7015605659913305425, -1.685594894050304493 ) ) ;
#73823=CARTESIAN_POINT ( 'NONE',  ( 3.035963658818414235, -1.482449291622448095, -1.634993338104336891 ) ) ;
#73826=CARTESIAN_POINT ( 'NONE',  ( 1.300873410958070409, -0.2835801433653042380, -1.891145142470892715 ) ) ;
#73828=CARTESIAN_POINT ( 'NONE',  ( 1.416386825446398712, 0.7951318926605431825, 1.802096770617849897 ) ) ;
#73829=CARTESIAN_POINT ( 'NONE',  ( 3.104954810669264376, -0.3761875069782861236, 1.905116956637223913 ) ) ;
#73833=CARTESIAN_POINT ( 'NONE',  ( 6.825069993440997074, -1.701324435194497831, -0.7545304760708021474 ) ) ;
#73838=CARTESIAN_POINT ( 'NONE',  ( 2.366952063387484095, 0.1042156695447923470, -2.189191704635709890 ) ) ;
#73843=CARTESIAN_POINT ( 'NONE',  ( 2.578497204056416692, -1.747032809129964503, -0.5301130021647950663 ) ) ;
#73850=CARTESIAN_POINT ( 'NONE',  ( 2.684106373981818727, -0.9902706917056921521, 1.652370099195903386 ) ) ;
#73851=CARTESIAN_POINT ( 'NONE',  ( 6.315287901512626867, -1.680818388338392699, -1.011408691396285420 ) ) ;
#73860=CARTESIAN_POINT ( 'NONE',  ( 5.471561611210747245, -0.3092806512635417060, 2.046926588373791933 ) ) ;
#73861=CARTESIAN_POINT ( 'NONE',  ( -0.1121326479804653220, -0.4008509640632436088, -1.803546454093779561 ) ) ;
#73864=CARTESIAN_POINT ( 'NONE',  ( 5.309350125645185159, 1.371050412704700516, -1.844953357796705218 ) ) ;
#73868=CARTESIAN_POINT ( 'NONE',  ( 0.006404353242023088852, -0.9848532314915852126, -2.067437341614616120 ) ) ;
#73872=CARTESIAN_POINT ( 'NONE',  ( 4.488185891274095063, -0.4267898533511414461, -1.894319381339019559 ) ) ;
#73878=CARTESIAN_POINT ( 'NONE',  ( -0.03490996608559569087, -1.614503017106348581, 1.202435150695363664 ) ) ;
#73879=CARTESIAN_POINT ( 'NONE',  ( 0.6446037793155032780, -1.481899804082789984, 0.8824728545121940382 ) ) ;
#73880=CARTESIAN_POINT ( 'NONE',  ( 5.471888747823221877, -0.9023485654677811940, 1.803414228490702209 ) ) ;
#73884=CARTESIAN_POINT ( 'NONE',  ( 2.853556533831374420, 2.080516846217596250, -0.2054353837145187767 ) ) ;
#73885=CARTESIAN_POINT ( 'NONE',  ( 1.269958040854075154, -1.126728106645444205, 1.364847948389063870 ) ) ;
#73886=CARTESIAN_POINT ( 'NONE',  ( 6.522112240665402183, -1.799906897009293738, 0.9091900463213120620 ) ) ;
#73888=CARTESIAN_POINT ( 'NONE',  ( 4.488395308864603805, -0.4996631572763092222, -2.236994043316854697 ) ) ;
#73889=CARTESIAN_POINT ( 'NONE',  ( 2.624636096055412704, -1.623921194558699765, 0.6262662122848341451 ) ) ;
#73892=CARTESIAN_POINT ( 'NONE',  ( 2.178627760304178818, -0.8125915806111455586, -1.531602080710131153 ) ) ;
#73894=CARTESIAN_POINT ( 'NONE',  ( 1.592022279046673816, 0.9211323807055901147, -1.617040898905151458 ) ) ;
#73896=CARTESIAN_POINT ( 'NONE',  ( 2.717415358725610908, -1.887964963866497259, -1.072103292869843960 ) ) ;
#73898=CARTESIAN_POINT ( 'NONE',  ( 3.555875268649951959, 1.124244472066991518, 1.673854899288424347 ) ) ;
#73899=CARTESIAN_POINT ( 'NONE',  ( 2.093750000000001332, -1.895863743164132531, -0.7852924748298759638 ) ) ;
#73901=CARTESIAN_POINT ( 'NONE',  ( 1.377817859240665577, 1.145177193861897758, 1.548917676831958801 ) ) ;
#73903=CARTESIAN_POINT ( 'NONE',  ( 4.904621534589208132, -2.204716393758818782, -0.2710871420372409912 ) ) ;
#73909=CARTESIAN_POINT ( 'NONE',  ( 6.205373625529961856, 1.933303589146176948, -1.094015395867214080 ) ) ;
#73910=CARTESIAN_POINT ( 'NONE',  ( 5.142999638377217408, -0.2383176028181442918, -1.947251298587366231 ) ) ;
#73913=CARTESIAN_POINT ( 'NONE',  ( 5.202513629402051976, -0.7552652112401860851, -2.132769717564055867 ) ) ;
#73915=CARTESIAN_POINT ( 'NONE',  ( 2.840340301219072217, -1.062657783794159538, 1.767763702702547679 ) ) ;
#73919=CARTESIAN_POINT ( 'NONE',  ( 5.219927230130699591, -0.9996001844756461363, -1.580852690948472361 ) ) ;
#73920=CARTESIAN_POINT ( 'NONE',  ( 3.797271647414564910, 1.222981480435406443, -1.229749918556479304 ) ) ;
#73921=CARTESIAN_POINT ( 'NONE',  ( 1.768729326414076430, 1.665373798791164317, -0.5055230280728554293 ) ) ;
#73922=CARTESIAN_POINT ( 'NONE',  ( 0.2579210422260198587, 2.266244506498811706, -0.3445303224042794432 ) ) ;
#73923=CARTESIAN_POINT ( 'NONE',  ( 0.7103623821160671703, -2.195938746145317477, 0.2182302698266261887 ) ) ;
#73924=CARTESIAN_POINT ( 'NONE',  ( 4.335544241866786663, 0.8922555979511301860, -1.890918108395107211 ) ) ;
#73925=CARTESIAN_POINT ( 'NONE',  ( 5.367111071781861753, 1.871067490511884479, -0.5196462679451731015 ) ) ;
#73928=CARTESIAN_POINT ( 'NONE',  ( 1.020157974382044364, -1.821741137083273010, 0.8647263380179845971 ) ) ;
#73929=CARTESIAN_POINT ( 'NONE',  ( 0.05319811239242258627, 0.3688592364489845510, 2.088132107045739705 ) ) ;
#73930=CARTESIAN_POINT ( 'NONE',  ( 6.486953984781112403, -2.015912550161761629, 0.05229459904129707404 ) ) ;
#73933=CARTESIAN_POINT ( 'NONE',  ( 4.670415550810885996, -1.190324863180821646, 1.384379922071424351 ) ) ;
#73934=CARTESIAN_POINT ( 'NONE',  ( 2.415298318263587873, 1.970979330149217335, 0.9926799514654092160 ) ) ;
#73935=ORIENTED_EDGE ( 'NONE', *, *, #55279, .T. ) ;
#73940=CARTESIAN_POINT ( 'NONE',  ( 1.705338084499245843, 1.755316507598453368, -0.9991084507309263563 ) ) ;
#73942=CARTESIAN_POINT ( 'NONE',  ( 2.922522432510234136, -1.287038294151692241, 1.344341647096161996 ) ) ;
#73948=AXIS2_PLACEMENT_3D ( 'NONE', #88151, #158490, #156362 ) ;
#73950=CARTESIAN_POINT ( 'NONE',  ( 5.127504350819418910, -1.732488751877172772, 0.5760870007271366999 ) ) ;
#73955=CARTESIAN_POINT ( 'NONE',  ( 0.6492036743409674848, -0.2036512653956819019, -1.721755200737408842 ) ) ;
#73956=CARTESIAN_POINT ( 'NONE',  ( 0.4623611518889169103, 0.1752324854824957590, -1.731468860160074952 ) ) ;
#73957=CARTESIAN_POINT ( 'NONE',  ( 4.758593218111947465, 0.8799714688421821362, 2.133523255312119726 ) ) ;
#73959=CARTESIAN_POINT ( 'NONE',  ( 6.907524304660562109, -0.4813806915026208055, 2.115094849305596103 ) ) ;
#73961=CARTESIAN_POINT ( 'NONE',  ( 5.659591354751080772, -0.5502123075824224552, -2.231479479524396403 ) ) ;
#73965=CARTESIAN_POINT ( 'NONE',  ( 5.453920962983416665, 1.868457504587007545, -0.09292587778651077712 ) ) ;
#73966=CARTESIAN_POINT ( 'NONE',  ( 3.058751851047710080, 0.4689117840017149041, 1.853869267190631831 ) ) ;
#73968=CARTESIAN_POINT ( 'NONE',  ( 4.793709216081707858, 1.633822259641436903, 1.483752339651790653 ) ) ;
#73969=CARTESIAN_POINT ( 'NONE',  ( 4.276635374070654194, -0.4674139498860945263, -2.064944810692950217 ) ) ;
#73971=CARTESIAN_POINT ( 'NONE',  ( 6.983263157960365675, 7.629137130509070275, 2.446189081643288521 ) ) ;
#73974=CARTESIAN_POINT ( 'NONE',  ( 2.274872074667996458, -1.419342104801555982, 1.819364073307845997 ) ) ;
#73975=CARTESIAN_POINT ( 'NONE',  ( 3.297265573180406584, -1.731424309613574852, 0.9225008839797432802 ) ) ;
#73978=CARTESIAN_POINT ( 'NONE',  ( 6.825054090417398633, -1.883341039872712397, -0.8414091007707087400 ) ) ;
#73982=CARTESIAN_POINT ( 'NONE',  ( 5.313685493615880162, -1.282986534165726944, -1.555701818360885280 ) ) ;
#73984=DIRECTION ( 'NONE',  ( 2.949029909160572061E-17, 1.000000000000000000, -8.673600428462353400E-15 ) ) ;
#73986=CARTESIAN_POINT ( 'NONE',  ( 1.762787986429158016, -0.7786651900678620564, -2.026813006651595028 ) ) ;
#73993=CARTESIAN_POINT ( 'NONE',  ( 1.036483977676525114, 2.029821650745375905, 0.3549538351500410305 ) ) ;
#73994=CARTESIAN_POINT ( 'NONE',  ( 0.07775346131143417994, 7.629137130509094256, -2.888902737517151209 ) ) ;
#73995=CARTESIAN_POINT ( 'NONE',  ( 6.727182134110203826, 2.985950691969770254, 2.264927069331075238 ) ) ;
#73999=CARTESIAN_POINT ( 'NONE',  ( 3.510326737904199135, -1.910220267131033323, -0.09114558060911714943 ) ) ;
#74000=CARTESIAN_POINT ( 'NONE',  ( 5.453870971094811004, 1.767685242813926250, -0.08968725887432274502 ) ) ;
#74004=CARTESIAN_POINT ( 'NONE',  ( 0.2334084307264666924, 0.5983727300521198833, -1.819970363327483076 ) ) ;
#74006=CARTESIAN_POINT ( 'NONE',  ( 1.205626512970816355, -1.630946839658468983, -1.275175305487465049 ) ) ;
#74009=CARTESIAN_POINT ( 'NONE',  ( 5.682452175617663137, -1.825344843996518529, -0.4084625512627630406 ) ) ;
#74010=CARTESIAN_POINT ( 'NONE',  ( 2.771877994228102882, 0.9767612972278701955, 1.542236413651025151 ) ) ;
#74011=CARTESIAN_POINT ( 'NONE',  ( 6.076841795016812320, -2.094286673724785164, -0.6961510500591641115 ) ) ;
#74014=CARTESIAN_POINT ( 'NONE',  ( 3.033693852995589246, 1.959511903404848043, -0.6444255830786119743 ) ) ;
#74020=CARTESIAN_POINT ( 'NONE',  ( 0.2456851981432126020, -1.670693100197045977, -1.371219901248825535 ) ) ;
#74021=CARTESIAN_POINT ( 'NONE',  ( 5.617656447048144486, 0.4075009240860455462, -2.029694874052537568 ) ) ;
#74022=CIRCLE ( 'NONE', #157213, 0.04999999999999969746 ) ;
#74024=CARTESIAN_POINT ( 'NONE',  ( 3.849029623751087481, -1.769594347601778361, 1.241129261558816754 ) ) ;
#74026=CARTESIAN_POINT ( 'NONE',  ( 4.652993067401423488, 0.3473450764862345830, 1.989417523455960568 ) ) ;
#74027=CARTESIAN_POINT ( 'NONE',  ( 1.873419974815058842, -0.2433403713097622156, 1.946663811685337420 ) ) ;
#74034=CARTESIAN_POINT ( 'NONE',  ( 1.973842561262352469, -0.8578407463649927456, 1.825077436249371354 ) ) ;
#74038=CARTESIAN_POINT ( 'NONE',  ( 5.853752780977106163, -1.389761788226477002, -1.313969904969368496 ) ) ;
#74043=CARTESIAN_POINT ( 'NONE',  ( 3.163685574146878565, 1.281377625384312324, 1.556896677758594416 ) ) ;
#74046=CARTESIAN_POINT ( 'NONE',  ( 5.930603204692192598, 1.663448300781378508, 0.4554771339976750322 ) ) ;
#74050=CARTESIAN_POINT ( 'NONE',  ( 3.971829172498120286, 1.036919360001643531, 1.556626693588740062 ) ) ;
#74052=CARTESIAN_POINT ( 'NONE',  ( 2.729418486472269922, 0.1060373921930452268, -2.067687848736274869 ) ) ;
#74055=CARTESIAN_POINT ( 'NONE',  ( -0.0003749349099593791675, -1.976945657698804704, 0.3961262320883383592 ) ) ;
#74056=CARTESIAN_POINT ( 'NONE',  ( 0.5799530485631685384, 0.8934014309100688500, 1.575905833579164694 ) ) ;
#74062=CARTESIAN_POINT ( 'NONE',  ( 6.169544653506280341, 1.324940883694783578, 1.383738526680919012 ) ) ;
#74070=CARTESIAN_POINT ( 'NONE',  ( 3.467792127863758456, 2.109446376165153847, -0.4717452660116944196 ) ) ;
#74074=CARTESIAN_POINT ( 'NONE',  ( 5.368107995252269227, 0.9013511576922846880, 1.587453057759043551 ) ) ;
#74078=CARTESIAN_POINT ( 'NONE',  ( 1.528526583484477230, 1.898816187374774200, 0.5295601200957336108 ) ) ;
#74079=CARTESIAN_POINT ( 'NONE',  ( 3.832203377193269755, -0.9874410831685247469, -1.637625244210038300 ) ) ;
#74083=CARTESIAN_POINT ( 'NONE',  ( 5.107841235723004303, 0.6198312778436664283, -1.869525964861347589 ) ) ;
#74085=CARTESIAN_POINT ( 'NONE',  ( 0.3044966626061855752, 1.689057509992748729, 0.9581197715371556622 ) ) ;
#74089=CARTESIAN_POINT ( 'NONE',  ( 6.011998765391792787, -0.7129019540204998284, 1.997330473063135381 ) ) ;
#74091=CARTESIAN_POINT ( 'NONE',  ( 3.703681524037071071, 1.387051605615218008, 1.316649548728260344 ) ) ;
#74093=CARTESIAN_POINT ( 'NONE',  ( 1.395868886378356821, 1.671639904693554168, 1.440724375100350008 ) ) ;
#74095=CARTESIAN_POINT ( 'NONE',  ( 6.199863759850236633, 1.389832719217662049, 1.456544111691231658 ) ) ;
#74099=CARTESIAN_POINT ( 'NONE',  ( 1.785682506433339478, -1.950172559450613852, 0.6955597780969878796 ) ) ;
#74109=CARTESIAN_POINT ( 'NONE',  ( 6.925078400183545035, 0.003529629153843985134, 1.755452343125718073 ) ) ;
#74111=CARTESIAN_POINT ( 'NONE',  ( 4.746542152430166972, 1.714266118827989516, -0.2609391866443058206 ) ) ;
#74113=CARTESIAN_POINT ( 'NONE',  ( 2.536061329345109971, 1.270221119870031057, 1.634730569901183150 ) ) ;
#74114=CARTESIAN_POINT ( 'NONE',  ( 3.866910228754817158, -0.2097145705111657654, -2.106837283413672601 ) ) ;
#74117=CARTESIAN_POINT ( 'NONE',  ( 1.287880319801449902, -1.245359047439015932, -1.525745898539744516 ) ) ;
#74120=CARTESIAN_POINT ( 'NONE',  ( 0.07037084582631887575, 0.7337836260858082715, 1.766209603411242668 ) ) ;
#74121=CARTESIAN_POINT ( 'NONE',  ( 3.416269409239420352, 1.454353297360365449, -1.771818544839237175 ) ) ;
#74122=CARTESIAN_POINT ( 'NONE',  ( 1.435882461153328515, 0.9014729512111450127, -1.587519582607027635 ) ) ;
#74127=CARTESIAN_POINT ( 'NONE',  ( 2.443610342004947533, -1.876944004186463566, 0.7284700530331960078 ) ) ;
#74128=CARTESIAN_POINT ( 'NONE',  ( 2.834756127989654484, -1.875839772035441388, -0.5741054328185363209 ) ) ;
#74133=CARTESIAN_POINT ( 'NONE',  ( 6.667919252303131650, -1.287369299672879830, 1.647753151290908047 ) ) ;
#74134=CARTESIAN_POINT ( 'NONE',  ( 4.047515533282939337, 0.5961193180711570339, -1.666553171763493602 ) ) ;
#74137=CARTESIAN_POINT ( 'NONE',  ( 0.9201892814816803323, 1.302667801055312990, -1.762099327409505811 ) ) ;
#74138=CARTESIAN_POINT ( 'NONE',  ( 5.841712918432809154, 1.738692355929325029, 0.07866246996769517275 ) ) ;
#74140=CARTESIAN_POINT ( 'NONE',  ( 0.2331713839410394229, 1.378908429916062994, -2.211717543205340863 ) ) ;
#74141=CARTESIAN_POINT ( 'NONE',  ( 0.2108991129620274019, -1.778944881630979413, -1.454728436597878316 ) ) ;
#74143=CARTESIAN_POINT ( 'NONE',  ( 5.782511917101329502, -1.690859530023439250, 0.3827970650602616765 ) ) ;
#74144=CARTESIAN_POINT ( 'NONE',  ( 5.828641854062238892, -1.381805371539744698, 1.674691576451936781 ) ) ;
#74146=CARTESIAN_POINT ( 'NONE',  ( 0.4095560439901060334, -2.008447366592306604, 0.6704124886842844910 ) ) ;
#74147=CARTESIAN_POINT ( 'NONE',  ( 2.531250000000001332, -0.7852924748301189917, -1.895863743164030613 ) ) ;
#74148=CARTESIAN_POINT ( 'NONE',  ( 6.827182134110199030, 6.034458849223407029, 2.683941674059683979 ) ) ;
#74149=CARTESIAN_POINT ( 'NONE',  ( 4.506809989931632288, 1.489605450875215453, -1.221516061710873347 ) ) ;
#74151=CARTESIAN_POINT ( 'NONE',  ( 1.682608811002960447, 1.145563986048125704, 1.903002289297763605 ) ) ;
#74156=CARTESIAN_POINT ( 'NONE',  ( 3.914843843660667400, -0.6973054565188941956, -2.109062029434173535 ) ) ;
#74164=CARTESIAN_POINT ( 'NONE',  ( 0.9146856577476671912, -1.281363086869342194, -1.556907195799726917 ) ) ;
#74166=CARTESIAN_POINT ( 'NONE',  ( 6.654736832427365911, -0.5462217193984253427, -1.988994552010774797 ) ) ;
#74170=CARTESIAN_POINT ( 'NONE',  ( 6.163578228761874556, 0.9028020746227163329, 1.487850569839582970 ) ) ;
#74173=CARTESIAN_POINT ( 'NONE',  ( 1.704008468626088790, -0.6311095051503686770, -1.653581786927365904 ) ) ;
#74174=CARTESIAN_POINT ( 'NONE',  ( 6.557244222609861062, -1.057944526735156821, 1.374202748628235327 ) ) ;
#74175=CARTESIAN_POINT ( 'NONE',  ( 6.339394973347380002, 0.6569538336487945607, -1.611921592020611582 ) ) ;
#74176=CARTESIAN_POINT ( 'NONE',  ( 4.406014021519581547, -0.9797006336973247409, -2.072624738501188446 ) ) ;
#74178=CARTESIAN_POINT ( 'NONE',  ( 2.536835285771392279, -1.364265644482412609, -1.236541980112846550 ) ) ;
#74181=CARTESIAN_POINT ( 'NONE',  ( 3.153144192703428939, -1.491587519860730238, -1.052284964708279258 ) ) ;
#74182=CARTESIAN_POINT ( 'NONE',  ( 4.008435526009396455, -1.928752077057366732, 0.5880193435906443389 ) ) ;
#74184=CARTESIAN_POINT ( 'NONE',  ( 3.169090989670137581, -2.089828869452925009, -0.8673982956902188679 ) ) ;
#74186=CARTESIAN_POINT ( 'NONE',  ( 5.280345248378272238, -1.172444710293341963, 1.749198092158671614 ) ) ;
#74189=CARTESIAN_POINT ( 'NONE',  ( 2.787621587699981696, -1.932700977737045633, 0.7428295258242522126 ) ) ;
#74192=CARTESIAN_POINT ( 'NONE',  ( 5.549516566986255839, -1.916978305411633166, 0.9067721062034905799 ) ) ;
#74194=CARTESIAN_POINT ( 'NONE',  ( 1.436025505276457226, 0.9502256629446425018, -1.675776081635256043 ) ) ;
#74201=CARTESIAN_POINT ( 'NONE',  ( 0.2115809916233695465, 1.842269378952247738, -1.241004044093022340 ) ) ;
#74202=CARTESIAN_POINT ( 'NONE',  ( 2.643703295229280936, -1.559600718570711031, -1.415347570850413739 ) ) ;
#74205=CARTESIAN_POINT ( 'NONE',  ( 6.403157621081472683, -1.572583794901558862, 0.9946829920960180704 ) ) ;
#74209=CARTESIAN_POINT ( 'NONE',  ( -0.1753031400193918732, -0.9122597987226389593, -1.912455998546586544 ) ) ;
#74212=CARTESIAN_POINT ( 'NONE',  ( 2.787496613063783713, -1.831585881375777713, 0.7034878451678548972 ) ) ;
#74213=CARTESIAN_POINT ( 'NONE',  ( 1.903414394802248166, 1.797162532295241366, 1.201017911493490020 ) ) ;
#74217=CARTESIAN_POINT ( 'NONE',  ( 3.872797606970843631, 1.637851192275063816, -0.5887498661538635991 ) ) ;
#74220=CARTESIAN_POINT ( 'NONE',  ( 1.985703663612121472, 1.880146017696176619, 0.7282698753105636413 ) ) ;
#74223=CARTESIAN_POINT ( 'NONE',  ( 2.061341786089391004, 0.3389245507335619245, -1.941969530725436766 ) ) ;
#74233=CARTESIAN_POINT ( 'NONE',  ( 2.104171369714701534, -0.8614446868937111201, 1.826873676003283320 ) ) ;
#74235=CARTESIAN_POINT ( 'NONE',  ( 5.579250153011313884, -0.04958841179729735205, -2.307219497322360535 ) ) ;
#74237=CARTESIAN_POINT ( 'NONE',  ( 2.553501467334079678, 1.513274546892771966, 1.248348448719404757 ) ) ;
#74239=CARTESIAN_POINT ( 'NONE',  ( 0.6510177983308338412, 0.9963039324867200008, 1.753029211773032392 ) ) ;
#74241=CARTESIAN_POINT ( 'NONE',  ( 2.149754410345839251, 2.075462379332591478, -0.4182697058867020923 ) ) ;
#74244=CARTESIAN_POINT ( 'NONE',  ( 1.728195974063054141, 0.1793598003074353686, 1.832383557197496460 ) ) ;
#74248=CARTESIAN_POINT ( 'NONE',  ( 3.814780496183818315, -0.6684712460508880350, -2.012520831323429515 ) ) ;
#74249=CARTESIAN_POINT ( 'NONE',  ( 6.667919370488161412, -1.192936252400189190, 1.533121312111614065 ) ) ;
#74253=CARTESIAN_POINT ( 'NONE',  ( 4.112614458092584968, 1.460029904434188008, -1.454618372460781295 ) ) ;
#74255=CARTESIAN_POINT ( 'NONE',  ( 1.663359199420410883, 0.9473472845980964729, 1.578708189602283873 ) ) ;
#74260=CARTESIAN_POINT ( 'NONE',  ( 1.102499568101540817, -2.207063161980229005, 0.003256074490760872773 ) ) ;
#74261=CARTESIAN_POINT ( 'NONE',  ( 4.253392140805613231, -1.877938019876054243, -1.261413133637336204 ) ) ;
#74263=CARTESIAN_POINT ( 'NONE',  ( 3.480526544955347301, -1.212856340575025005, 1.345865543471187253 ) ) ;
#74264=CARTESIAN_POINT ( 'NONE',  ( 2.606530347446478046, 1.805417332896454230, 0.6411187296449465389 ) ) ;
#74265=CARTESIAN_POINT ( 'NONE',  ( 3.877443546529443452, -0.1552652338182025915, 2.064615508632794860 ) ) ;
#74267=CARTESIAN_POINT ( 'NONE',  ( 3.063307058708428787, 0.2908816738307045680, -1.949781715572605600 ) ) ;
#74269=CARTESIAN_POINT ( 'NONE',  ( 0.6746739519505640104, -1.812841073067989361, -0.6519485973254712796 ) ) ;
#74270=CARTESIAN_POINT ( 'NONE',  ( 3.555401268124198655, 0.4554524271490404952, -1.814226883376020671 ) ) ;
#74271=CARTESIAN_POINT ( 'NONE',  ( 2.034188542434863578, -1.509292173632442280, -1.745791301847523513 ) ) ;
#74272=CARTESIAN_POINT ( 'NONE',  ( 4.017883236588020601, 1.847182159994051442, -0.2260418734564421939 ) ) ;
#74277=CARTESIAN_POINT ( 'NONE',  ( 0.2410290108679030985, 0.3623031737408002884, 2.074505700167991407 ) ) ;
#74281=CARTESIAN_POINT ( 'NONE',  ( 1.810938747355747447, -0.5704394276861005642, -2.042344090522000055 ) ) ;
#74282=CARTESIAN_POINT ( 'NONE',  ( 1.125267019654611733, 1.783345095244772249, 0.9482059100444378830 ) ) ;
#74286=CARTESIAN_POINT ( 'NONE',  ( 1.071799524545346216, 2.083542002058445863, -0.5754571431841256635 ) ) ;
#74288=CARTESIAN_POINT ( 'NONE',  ( 6.825078400183572036, 4.699117039843025090, 2.418333817060664526 ) ) ;
#74290=CARTESIAN_POINT ( 'NONE',  ( -0.2104748580754391973, 0.7011259924453935310, -2.185273273056092869 ) ) ;
#74291=CARTESIAN_POINT ( 'NONE',  ( 5.454314652423888354, -1.275559214091715354, 1.561879324423600668 ) ) ;
#74295=CARTESIAN_POINT ( 'NONE',  ( 0.4271420986578051138, 2.166143833277152542, 0.6532491227348672380 ) ) ;
#74299=CARTESIAN_POINT ( 'NONE',  ( 0.7728743906838764222, 1.688931763573727540, -0.9039392725495792869 ) ) ;
#74303=CARTESIAN_POINT ( 'NONE',  ( 2.367434161175852925, 1.691737554211050210, -0.3355112704105273624 ) ) ;
#74306=CARTESIAN_POINT ( 'NONE',  ( 0.3855647087021807362, -0.8419519913594010196, 1.556653678627561543 ) ) ;
#74307=CARTESIAN_POINT ( 'NONE',  ( 2.297522961200649139, 1.839619113207457524, -0.8179307585152847393 ) ) ;
#74310=CARTESIAN_POINT ( 'NONE',  ( 3.680891063843365174, -2.126115503207156809, -0.5908918699835326027 ) ) ;
#74313=CARTESIAN_POINT ( 'NONE',  ( 4.582752651445391123, -1.384437811569695587, 1.606279107262520434 ) ) ;
#74314=CARTESIAN_POINT ( 'NONE',  ( 3.234000073275579812, 2.016598147164900823, -0.002828922958116042007 ) ) ;
#74315=CARTESIAN_POINT ( 'NONE',  ( 3.498146571883210321, -0.8881612436112231723, 1.578813691393302410 ) ) ;
#74319=CARTESIAN_POINT ( 'NONE',  ( 1.744777856283234785, -1.581906188472384400, 0.9981555316627908070 ) ) ;
#74321=CARTESIAN_POINT ( 'NONE',  ( 5.707590141996651489, -0.4392596013848491521, 1.771934311310577659 ) ) ;
#74331=CARTESIAN_POINT ( 'NONE',  ( 4.570628194609677841, 0.8141925398062774821, 1.958264201954627026 ) ) ;
#74332=CARTESIAN_POINT ( 'NONE',  ( -0.02968770228137588424, 5.725071598255107475, -2.420367217772397606 ) ) ;
#74334=CARTESIAN_POINT ( 'NONE',  ( 4.376219360443936779, -1.137518282590570751, 1.609873005976544924 ) ) ;
#74336=CARTESIAN_POINT ( 'NONE',  ( 6.381121926128928479, -1.751337275642101510, -0.7685668267764720341 ) ) ;
#74338=CARTESIAN_POINT ( 'NONE',  ( -0.1232448511370512201, -0.4725888426768353190, -2.071762565325820038 ) ) ;
#74339=CARTESIAN_POINT ( 'NONE',  ( 0.9771079587245214970, 1.912259438035465386, 0.7939916666956441382 ) ) ;
#74344=CARTESIAN_POINT ( 'NONE',  ( 3.908215892115148637, 1.478387765550030153, -1.478483494758761951 ) ) ;
#74347=CARTESIAN_POINT ( 'NONE',  ( 1.746812667857342349, -1.544096848276183209, 0.9736100143667850704 ) ) ;
#74348=CARTESIAN_POINT ( 'NONE',  ( 0.7854713186128524649, 1.746033005210102962, -0.4821264535347525859 ) ) ;
#74350=CARTESIAN_POINT ( 'NONE',  ( 6.024089167411393220, -1.222679950896175205, -1.837027303407394507 ) ) ;
#74352=CARTESIAN_POINT ( 'NONE',  ( 4.120313900606538127, -1.131812998600056241, -1.894281110011143632 ) ) ;
#74354=CARTESIAN_POINT ( 'NONE',  ( 2.350135150926917493, 0.8998847150011926033, -1.687291145760522859 ) ) ;
#74356=CARTESIAN_POINT ( 'NONE',  ( 5.582505937350194181, 1.236201877336528421, -1.660625051266072960 ) ) ;
#74360=CARTESIAN_POINT ( 'NONE',  ( 5.724229345562060089, 2.111793275502030554, 0.5857118945327836057 ) ) ;
#74366=CARTESIAN_POINT ( 'NONE',  ( -0.02319159430949970652, 4.096340798889516854, -2.366022381217198767 ) ) ;
#74371=CARTESIAN_POINT ( 'NONE',  ( 5.664915734613279241, 1.571387620024040421, -1.347999112033698266 ) ) ;
#74372=CARTESIAN_POINT ( 'NONE',  ( 4.477124871421138685, -0.001476069148669684195, -1.926676517386548992 ) ) ;
#74373=CARTESIAN_POINT ( 'NONE',  ( 6.415624682135008250, -1.382911306069923407, -1.603242893440869343 ) ) ;
#74377=CARTESIAN_POINT ( 'NONE',  ( 0.5686479265839607944, -2.064760635122906418, -0.7346842419702694915 ) ) ;
#74378=CARTESIAN_POINT ( 'NONE',  ( 5.338443970399977978, 1.799313579390570128, 0.3082849261525285600 ) ) ;
#74386=CARTESIAN_POINT ( 'NONE',  ( 2.225889136967126536, 1.786374552192676823, 0.4457033907802817052 ) ) ;
#74387=CARTESIAN_POINT ( 'NONE',  ( 6.433844876963536130, -1.951739824409718160, 0.4931976252120565118 ) ) ;
#74388=CARTESIAN_POINT ( 'NONE',  ( 0.9315567102232256147, 1.134920720140248251, 1.998545780126102844 ) ) ;
#74389=CARTESIAN_POINT ( 'NONE',  ( 6.350445966956749899, -1.952004966925089624, -0.1956573963535559180 ) ) ;
#74393=CARTESIAN_POINT ( 'NONE',  ( 0.9419464005683108043, 1.389173191389100337, 1.535309223701806447 ) ) ;
#74396=CARTESIAN_POINT ( 'NONE',  ( 2.700817844316987237, 1.767710524334182853, 1.116111477495850934 ) ) ;
#74397=CARTESIAN_POINT ( 'NONE',  ( 1.586564105604048480, -0.2713065988851799393, -1.850747533123621391 ) ) ;
#74398=CARTESIAN_POINT ( 'NONE',  ( 2.284529629648517801, -1.956262009633228605, 0.4871271731112236658 ) ) ;
#74402=CARTESIAN_POINT ( 'NONE',  ( 1.786251233324965826, 1.514223802825481302, -0.8579289008448316434 ) ) ;
#74406=CARTESIAN_POINT ( 'NONE',  ( 3.334305206967770552, 1.683047542859770429, 0.3767605245002195180 ) ) ;
#74407=CARTESIAN_POINT ( 'NONE',  ( 2.999763140970078901, -2.188934734890151113, 0.1099877568606702771 ) ) ;
#74408=CARTESIAN_POINT ( 'NONE',  ( 5.602238545945851023, -2.207063162045197924, -0.003355105161521875021 ) ) ;
#74410=CARTESIAN_POINT ( 'NONE',  ( 1.991327249661909882, 0.2097703728867078010, 2.160876515670279385 ) ) ;
#74411=CARTESIAN_POINT ( 'NONE',  ( 1.295219883412350503, 1.381147610352757127, 1.194082977437810333 ) ) ;
#74413=CARTESIAN_POINT ( 'NONE',  ( 3.608711286396129481, 2.011918449240827744, 0.6600949426460513969 ) ) ;
#74416=CARTESIAN_POINT ( 'NONE',  ( 3.368946006165595364, 0.05471657373835739357, -2.291868861755571363 ) ) ;
#74420=CARTESIAN_POINT ( 'NONE',  ( 0.5047332052380922862, -2.104974169346077506, -0.2554120829242333968 ) ) ;
#74425=CARTESIAN_POINT ( 'NONE',  ( 6.825078400183573812, 0.002648415797040087893, 1.855566311045192540 ) ) ;
#74427=CARTESIAN_POINT ( 'NONE',  ( 4.711564657724523819, 1.930417226389494090, 0.5826574956761670920 ) ) ;
#74429=CARTESIAN_POINT ( 'NONE',  ( 3.362228078103552953, -2.060403055893737623, 0.09660672959950138139 ) ) ;
#74434=CARTESIAN_POINT ( 'NONE',  ( 6.456982561897790518, 0.3786298020890948024, -2.158335565738931816 ) ) ;
#74435=CARTESIAN_POINT ( 'NONE',  ( 3.990861413484114273, -2.010826503599131065, 0.1511389102963680842 ) ) ;
#74436=CARTESIAN_POINT ( 'NONE',  ( 3.860763913883006992, 0.2215400755124704024, -1.827792592973469743 ) ) ;
#74438=CARTESIAN_POINT ( 'NONE',  ( 6.721730220878607831, -1.769880579078547012, 0.4471725050417332814 ) ) ;
#74440=CARTESIAN_POINT ( 'NONE',  ( 0.5446534387809185418, 2.256470935699141034, 0.1650129453365980214 ) ) ;
#74441=CARTESIAN_POINT ( 'NONE',  ( 2.385502688336095911, 1.925211662925530254, -0.8542917040773172488 ) ) ;
#74450=CARTESIAN_POINT ( 'NONE',  ( 3.867602925442710671, -1.848332671738551980, -1.231929692598219050 ) ) ;
#74451=CARTESIAN_POINT ( 'NONE',  ( 1.271705539736139423, 1.307743536042236920, 1.758333696453084016 ) ) ;
#74452=CARTESIAN_POINT ( 'NONE',  ( 0.3818278861203865393, 2.057605126571937060, -0.7983354260262252033 ) ) ;
#74454=CARTESIAN_POINT ( 'NONE',  ( 4.299235682465595509, -1.708000122724560477, 0.9650500775852040025 ) ) ;
#74458=CARTESIAN_POINT ( 'NONE',  ( 6.610000000000026077, 2.442988107647511509, 2.382821027452782570 ) ) ;
#74461=CARTESIAN_POINT ( 'NONE',  ( 2.971057270251746818, -1.603071526910588629, 1.388259434452358665 ) ) ;
#74463=CARTESIAN_POINT ( 'NONE',  ( 5.594645800149128156, -0.5210773734287167391, -2.097845705497362712 ) ) ;
#74464=CARTESIAN_POINT ( 'NONE',  ( 4.142028884782995135, 0.4951553702221401232, 1.773339192993342639 ) ) ;
#74467=CARTESIAN_POINT ( 'NONE',  ( 0.1337851541256071808, 0.2942392587969425155, 1.715217768732644643 ) ) ;
#74468=CARTESIAN_POINT ( 'NONE',  ( 6.727182134110170075, 7.629137130509032971, 2.510944104600740356 ) ) ;
#74471=CARTESIAN_POINT ( 'NONE',  ( 3.819328725847204620, -0.1613130240520690706, 2.155748724213396361 ) ) ;
#74473=CARTESIAN_POINT ( 'NONE',  ( 5.079453798366286854, 1.392331892589277142, -1.458333960840517696 ) ) ;
#74475=CARTESIAN_POINT ( 'NONE',  ( 3.415052781332720055, 1.953485055394106107, 0.9259690932504063277 ) ) ;
#74477=CARTESIAN_POINT ( 'NONE',  ( 3.989495051124877456, 1.425666444934305499, 1.361731899605103768 ) ) ;
#74479=CARTESIAN_POINT ( 'NONE',  ( -0.1290005225502675879, -0.006633637972621592160, -2.173875058097324064 ) ) ;
#74480=CARTESIAN_POINT ( 'NONE',  ( 0.5347316126107805045, 1.182704979252725108, -1.981343935211031138 ) ) ;
#74481=CARTESIAN_POINT ( 'NONE',  ( 3.110674321496671446, 1.495003355660160516, -1.418639704521322153 ) ) ;
#74482=CARTESIAN_POINT ( 'NONE',  ( 5.231954969198427285, 1.913977456902911767, 0.3281912247276967398 ) ) ;
#74490=CARTESIAN_POINT ( 'NONE',  ( 2.169229845753062325, -2.017539712319418310, -0.8944986170207609444 ) ) ;
#74493=CARTESIAN_POINT ( 'NONE',  ( 6.086763564210844635, 1.889667650816441391, 0.5265613530214608984 ) ) ;
#74495=CARTESIAN_POINT ( 'NONE',  ( -0.02919842301646497981, 7.629137130509056952, -2.673797582091000269 ) ) ;
#74500=CARTESIAN_POINT ( 'NONE',  ( 5.542853976212075651, -1.453887124689148935, -1.129494548679485622 ) ) ;
#74502=CARTESIAN_POINT ( 'NONE',  ( 1.885689728351304995, 1.420446345011391553, 1.493427266136108322 ) ) ;
#74507=CARTESIAN_POINT ( 'NONE',  ( 0.5146158036630330557, 1.421672375139692246, -1.492246178604545115 ) ) ;
#74510=CARTESIAN_POINT ( 'NONE',  ( 4.563899478665734755, -1.199029595066217313, 1.397436126395680267 ) ) ;
#74516=CARTESIAN_POINT ( 'NONE',  ( 4.916741810085082598, 1.523553907054091328, -1.596827639139485777 ) ) ;
#74517=CARTESIAN_POINT ( 'NONE',  ( 0.1929406647830470833, -0.4748886411078504510, -2.116594070111991410 ) ) ;
#74519=CARTESIAN_POINT ( 'NONE',  ( -0.2049973002360427898, -0.1418364932926942379, -1.881151990943498387 ) ) ;
#74520=CARTESIAN_POINT ( 'NONE',  ( 6.385945889491149607, -1.915137183225220197, 0.05458341080493907954 ) ) ;
#74524=CARTESIAN_POINT ( 'NONE',  ( 6.164708882046985750, 0.6044385376218417427, 1.814302210532907411 ) ) ;
#74526=CARTESIAN_POINT ( 'NONE',  ( 0.9185735243398345240, 1.726912363944958617, 0.7195956246372691156 ) ) ;
#74527=CARTESIAN_POINT ( 'NONE',  ( 1.938685741270998797, -1.555697844595272716, 1.282991390469834458 ) ) ;
#74531=CARTESIAN_POINT ( 'NONE',  ( 4.090527498900095260, -2.083119126933795418, -0.3091809127075405006 ) ) ;
#74536=CARTESIAN_POINT ( 'NONE',  ( 3.674085990935217261, 2.004049791156937044, -0.2512726544132165563 ) ) ;
#74540=CARTESIAN_POINT ( 'NONE',  ( 4.938837616837212785, 0.3641351946921667082, 2.130543054529559832 ) ) ;
#74546=CARTESIAN_POINT ( 'NONE',  ( 1.469425047783163407, 1.914459939344328010, 1.024175319008380658 ) ) ;
#74549=CARTESIAN_POINT ( 'NONE',  ( 0.7140992756325339474, 1.701125707204936166, 0.7050099338341904165 ) ) ;
#74551=CARTESIAN_POINT ( 'NONE',  ( 2.929422067023911502, -1.473737196803912797, -1.622193633833472814 ) ) ;
#74552=CARTESIAN_POINT ( 'NONE',  ( 3.450319916561462197, 2.262689076145682598, 0.002162386163321801912 ) ) ;
#74558=CARTESIAN_POINT ( 'NONE',  ( 3.760817854529928894, -1.559684770762577388, -0.8363013385033011282 ) ) ;
#74561=CARTESIAN_POINT ( 'NONE',  ( 1.255059265495124476, -1.660252808076821296, 1.295518548220045529 ) ) ;
#74565=CARTESIAN_POINT ( 'NONE',  ( 1.416386825446398712, 0.7951318926605431825, 1.802096770617849897 ) ) ;
#74568=CARTESIAN_POINT ( 'NONE',  ( 5.150580392983738598, 1.786086171955153068, 0.3018458199737662495 ) ) ;
#74571=CARTESIAN_POINT ( 'NONE',  ( 4.662891624058607576, -1.671085903211678270, -0.8408918736509605196 ) ) ;
#74572=CARTESIAN_POINT ( 'NONE',  ( 4.452052287080165982, -0.7971045336818067817, 1.910850710330507907 ) ) ;
#74582=CARTESIAN_POINT ( 'NONE',  ( 4.334394203492665909, -1.131343785558375226, 1.602600411086833931 ) ) ;
#74583=CARTESIAN_POINT ( 'NONE',  ( 1.897814322125553010, 0.1948091626960517242, 2.006652841580962132 ) ) ;
#74587=CARTESIAN_POINT ( 'NONE',  ( 2.143623209005097507, 0.7202431893391960660, -1.726524797105493336 ) ) ;
#74589=CARTESIAN_POINT ( 'NONE',  ( 2.584242159373177028, 1.080601423880021894, 1.698455611904861495 ) ) ;
#74591=CARTESIAN_POINT ( 'NONE',  ( 3.708711176059620751, 2.011172256762243649, 0.6619615953592747903 ) ) ;
#74593=CARTESIAN_POINT ( 'NONE',  ( 4.422371208857902580, 0.9731212702417373350, 1.827393648576709717 ) ) ;
#74595=CARTESIAN_POINT ( 'NONE',  ( 0.2926706434557576064, 1.735970642146159371, -1.164857044846574707 ) ) ;
#74596=CARTESIAN_POINT ( 'NONE',  ( 6.720655732516649827, 0.5547967289194677409, 2.325046546815363602 ) ) ;
#74597=CARTESIAN_POINT ( 'NONE',  ( 5.280226139177822908, -1.012770463184736736, 1.518683248463777113 ) ) ;
#74604=CARTESIAN_POINT ( 'NONE',  ( 6.076807558263135789, -1.348954070496380941, 1.355674883165632227 ) ) ;
#74612=CARTESIAN_POINT ( 'NONE',  ( 5.255482535091188012, 1.942537579172060047, -0.5405093616211650298 ) ) ;
#74616=CARTESIAN_POINT ( 'NONE',  ( -0.1399997263889836974, 2.022132088033218533, -2.415689637818136948 ) ) ;
#74620=CARTESIAN_POINT ( 'NONE',  ( 2.096482953606861432, 1.947282536051987201, 0.2939031187191037398 ) ) ;
#74622=CARTESIAN_POINT ( 'NONE',  ( 3.251577527157409886, 1.966640965408305686, -0.4445242805125593222 ) ) ;
#74624=CARTESIAN_POINT ( 'NONE',  ( 6.827182134110199030, 1.215541611938670608, 2.400477883804314150 ) ) ;
#74625=CARTESIAN_POINT ( 'NONE',  ( 4.154361996720875361, -1.624486827992781990, 1.471056368041193219 ) ) ;
#74627=CARTESIAN_POINT ( 'NONE',  ( 2.748949809783503451, -1.602600522849004339, 1.068665135549841771 ) ) ;
#74635=CARTESIAN_POINT ( 'NONE',  ( 6.093280168761200599, -0.6138376400152152357, 1.736067454429328416 ) ) ;
#74636=CARTESIAN_POINT ( 'NONE',  ( 3.211590615979207364, 1.588433223196554778, 1.236618793847492626 ) ) ;
#74637=CARTESIAN_POINT ( 'NONE',  ( 5.044420649243852139, 2.147057653193120252, -0.8206418397275447862 ) ) ;
#74639=CARTESIAN_POINT ( 'NONE',  ( 3.309261503611124144, -1.518638105539332317, -1.075258281928012094 ) ) ;
#74646=CARTESIAN_POINT ( 'NONE',  ( 5.829650940335100451, 1.029561424092540589, -1.819573902328343484 ) ) ;
#74651=CARTESIAN_POINT ( 'NONE',  ( 5.795441377679017236, 1.310440327830458385, 1.121692192092491380 ) ) ;
#74653=CARTESIAN_POINT ( 'NONE',  ( 1.740413025836908156, 1.729532991921935325, -0.1275185469355680501 ) ) ;
#74657=CARTESIAN_POINT ( 'NONE',  ( 6.174718801439761151, 1.464035886807094844, -1.603313688547292726 ) ) ;
#74658=CARTESIAN_POINT ( 'NONE',  ( 4.846238042176662653, 1.821038859956089606, 0.1311717439725426648 ) ) ;
#74659=CARTESIAN_POINT ( 'NONE',  ( 1.797631089865757259, -1.417250949620936895, -1.356651810197152086 ) ) ;
#74663=CARTESIAN_POINT ( 'NONE',  ( 4.037823014030429647, -2.028772383530423884, 0.6168223452112443494 ) ) ;
#74668=CARTESIAN_POINT ( 'NONE',  ( 1.569279613544020568, 1.823957739939351619, 0.9794188589333228112 ) ) ;
#74671=CARTESIAN_POINT ( 'NONE',  ( 3.774281487401151214, 2.204430612424528757, -0.2728622730414613784 ) ) ;
#74672=ORIENTED_EDGE ( 'NONE', *, *, #58676, .T. ) ;
#74673=CARTESIAN_POINT ( 'NONE',  ( 1.266696122786495904, 2.121433860451333420, -0.8855928530677835697 ) ) ;
#74675=CARTESIAN_POINT ( 'NONE',  ( 6.754736851877535031, -0.5442653458712517489, -1.989433905422931748 ) ) ;
#74679=CARTESIAN_POINT ( 'NONE',  ( 6.427308110136687347, -1.208249125052461181, -1.389453836245766016 ) ) ;
#74683=CARTESIAN_POINT ( 'NONE',  ( -0.1104750535120251204, 2.866086309876151539, -2.591737134608104842 ) ) ;
#74684=CARTESIAN_POINT ( 'NONE',  ( 3.487030103973333794, 1.559624344477263502, -0.7367539641185815169 ) ) ;
#74685=CARTESIAN_POINT ( 'NONE',  ( 1.833220611596135363, -1.622487599052296670, -1.197302888167578683 ) ) ;
#74686=CARTESIAN_POINT ( 'NONE',  ( 3.411010488035473909, -1.370397956465055245, -1.845398096504316410 ) ) ;
#74687=CARTESIAN_POINT ( 'NONE',  ( 3.321791363677785380, -2.181432725256218674, 0.5997193178089550436 ) ) ;
#74688=CARTESIAN_POINT ( 'NONE',  ( 5.567048526788405560, -1.903460050192711028, -0.9016015758830184801 ) ) ;
#74690=CARTESIAN_POINT ( 'NONE',  ( 3.813518172763687986, -1.743905005666521291, 0.3001630661942331080 ) ) ;
#74692=CARTESIAN_POINT ( 'NONE',  ( 5.952705545545641463, -1.964087939335951827, -1.181845259310390306 ) ) ;
#74693=CARTESIAN_POINT ( 'NONE',  ( 5.999929499617846496, -0.6670042279848520383, -1.716255146773135287 ) ) ;
#74696=CARTESIAN_POINT ( 'NONE',  ( 5.613277516225614328, -2.138688192980051639, 0.4772630486022874652 ) ) ;
#74699=CARTESIAN_POINT ( 'NONE',  ( 5.459458695672200435, 1.690470114046587646, 1.195012289465044564 ) ) ;
#74700=CARTESIAN_POINT ( 'NONE',  ( 0.6203277878081385754, 1.987498645412737908, 0.3399528957561820386 ) ) ;
#74702=CARTESIAN_POINT ( 'NONE',  ( 4.389231790275191614, 1.720148140252445668, -0.8676111672119514173 ) ) ;
#74705=CARTESIAN_POINT ( 'NONE',  ( 6.533471381225442798, -0.1521382079053348602, 2.086446650026114735 ) ) ;
#74715=CARTESIAN_POINT ( 'NONE',  ( 1.697631272820496307, -1.418720726069604865, -1.355276769646639901 ) ) ;
#74718=CARTESIAN_POINT ( 'NONE',  ( 5.195737816846159873, -1.386088135442983260, -1.388664821390848347 ) ) ;
#74721=CARTESIAN_POINT ( 'NONE',  ( 0.2864612384333536932, -1.063250325806489149, 1.997138572869002537 ) ) ;
#74725=CARTESIAN_POINT ( 'NONE',  ( 0.7373108528737730705, -1.318359053027039263, -1.327247110734230962 ) ) ;
#74726=CARTESIAN_POINT ( 'NONE',  ( 5.852856049955673434, -0.7765510095132116541, 1.550312759826449671 ) ) ;
#74728=CARTESIAN_POINT ( 'NONE',  ( 2.894263506066748093, -0.6386881658498286818, -2.096408367471907841 ) ) ;
#74729=CARTESIAN_POINT ( 'NONE',  ( 4.577368073103933455, 0.004851830007264032810, -2.307758714736147798 ) ) ;
#74730=CARTESIAN_POINT ( 'NONE',  ( 0.4794588345870378632, 1.923154262159839201, -0.7412630403166396986 ) ) ;
#74731=CARTESIAN_POINT ( 'NONE',  ( 2.115084705647510610, -1.883649903580833174, 0.4717843263111404783 ) ) ;
#74735=CARTESIAN_POINT ( 'NONE',  ( 4.693665235656380830, 1.977662049654808740, -0.7657889336421249693 ) ) ;
#74737=CARTESIAN_POINT ( 'NONE',  ( 3.428361437285933455, -1.528740797599713153, -1.314997250469025936 ) ) ;
#74742=CARTESIAN_POINT ( 'NONE',  ( 1.084280211047653264, -1.780658692889337091, -0.4022698149812459212 ) ) ;
#74748=CARTESIAN_POINT ( 'NONE',  ( 6.104382415481349966, -0.7394567487006579176, -1.923849829731038019 ) ) ;
#74754=CARTESIAN_POINT ( 'NONE',  ( 4.670572394037289854, 0.7749771354828223213, 1.865277368486473630 ) ) ;
#74755=CARTESIAN_POINT ( 'NONE',  ( 6.094412736144367848, -1.190704872505081946, 1.875028197947399278 ) ) ;
#74759=CARTESIAN_POINT ( 'NONE',  ( 4.381749043697905854, 1.344797980244310631, 1.561758987969330992 ) ) ;
#74760=CARTESIAN_POINT ( 'NONE',  ( 4.131482539099665452, 0.5404898895830790861, 1.942541833525657680 ) ) ;
#74767=CARTESIAN_POINT ( 'NONE',  ( 4.429064430395744267, 0.9478954142983322395, 1.779353956671766657 ) ) ;
#74768=CARTESIAN_POINT ( 'NONE',  ( 2.642321604431462578, -1.530645349967133972, 1.022873098850234141 ) ) ;
#74769=CARTESIAN_POINT ( 'NONE',  ( 1.225685606067970612, -0.05223309053147862785, 2.307267396272806970 ) ) ;
#74772=CARTESIAN_POINT ( 'NONE',  ( 3.725982817344280829, -1.284327275973631277, -1.738548686538298416 ) ) ;
#74774=CARTESIAN_POINT ( 'NONE',  ( 3.515276618313140311, 2.298542322452525877, 0.003563541299675049897 ) ) ;
#74779=CARTESIAN_POINT ( 'NONE',  ( 2.904993682805886213, 1.579364189935757778, 1.002181356900035070 ) ) ;
#74780=CARTESIAN_POINT ( 'NONE',  ( 6.121945800013044447, -1.094813031782817303, -1.639340605029938835 ) ) ;
#74785=CARTESIAN_POINT ( 'NONE',  ( 0.5400322017136415242, -1.563516176313231920, -1.557742479837947558 ) ) ;
#74790=CARTESIAN_POINT ( 'NONE',  ( 5.700065208342940615, -1.971640594297157989, -0.0006100080248323812597 ) ) ;
#74791=CARTESIAN_POINT ( 'NONE',  ( 5.742881039954627731, 0.4445991233769739925, 2.264314392639497520 ) ) ;
#74792=CARTESIAN_POINT ( 'NONE',  ( 5.687920738472253213, -1.181023890769626217, -1.438316992653262627 ) ) ;
#74794=CARTESIAN_POINT ( 'NONE',  ( 2.922777048086916629, -1.425580663919909563, 1.490811266603887963 ) ) ;
#74801=CARTESIAN_POINT ( 'NONE',  ( 5.213404077426219807, -1.831445439253748031, -1.165863444158367290 ) ) ;
#74803=CARTESIAN_POINT ( 'NONE',  ( 3.790429961727882713, 1.553415782126759792, -0.9881970032953185656 ) ) ;
#74806=CARTESIAN_POINT ( 'NONE',  ( 6.427279137517246888, -1.429865906218323435, -1.660902671979214595 ) ) ;
#74808=CARTESIAN_POINT ( 'NONE',  ( 0.6676899448993807162, 0.2205636587761065359, -2.251657551468993379 ) ) ;
#74813=CARTESIAN_POINT ( 'NONE',  ( -0.005422908085399994089, -1.854866876809873943, -0.4647201794698225252 ) ) ;
#74814=CARTESIAN_POINT ( 'NONE',  ( 0.6547154952327862709, -1.491839214215221698, -0.9519326369243490404 ) ) ;
#74816=CARTESIAN_POINT ( 'NONE',  ( 5.408844923620411471, -0.4912159631041897456, -1.952115566551455572 ) ) ;
#74818=CARTESIAN_POINT ( 'NONE',  ( 4.700279962202062123, -2.105436441984291029, -0.05427613729028049616 ) ) ;
#74820=CARTESIAN_POINT ( 'NONE',  ( 3.058105062934213692, -1.138753297271431375, 1.540237303602323804 ) ) ;
#74822=CARTESIAN_POINT ( 'NONE',  ( 4.668383401541156275, -0.8401123053542228769, -1.781513398035587281 ) ) ;
#74823=CARTESIAN_POINT ( 'NONE',  ( 5.467059065379825888, -1.589572006150547168, 1.245957840514285042 ) ) ;
#74824=CARTESIAN_POINT ( 'NONE',  ( 2.975316878787794828, 1.776827963633962559, -0.5852370025475408521 ) ) ;
#74825=CARTESIAN_POINT ( 'NONE',  ( 5.654863297658344834, -1.355735166614827625, 1.066293663406183256 ) ) ;
#74827=CARTESIAN_POINT ( 'NONE',  ( 2.614145488985010424, -2.182733025630137824, 0.3247920039054427721 ) ) ;
#74831=CARTESIAN_POINT ( 'NONE',  ( 6.443807124430430910, 1.351966286592180211, 1.421895456074427688 ) ) ;
#74838=CARTESIAN_POINT ( 'NONE',  ( 2.313015868914463091, -1.601887806243259771, 1.311650804931147274 ) ) ;
#74842=CARTESIAN_POINT ( 'NONE',  ( 6.287751673603878544, 2.029294879081492198, -0.6150919484220889188 ) ) ;
#74845=CIRCLE ( 'NONE', #213185, 0.05000000000000056483 ) ;
#74849=CARTESIAN_POINT ( 'NONE',  ( 5.378279760196133630, -0.2985789616767355326, 1.993766414912321094 ) ) ;
#74850=CARTESIAN_POINT ( 'NONE',  ( 4.803869215722607500, -1.030175745946705801, -1.614969243545740785 ) ) ;
#74852=CARTESIAN_POINT ( 'NONE',  ( 2.296645709751913955, 1.758124065145909798, -1.308193547052277861 ) ) ;
#74854=CARTESIAN_POINT ( 'NONE',  ( 2.039183100597967258, 0.003605121848727563250, 1.912571728241836633 ) ) ;
#74857=CARTESIAN_POINT ( 'NONE',  ( 0.3863424973270003226, -0.6820169105002243937, -1.897691504806876761 ) ) ;
#74859=CARTESIAN_POINT ( 'NONE',  ( 2.964485117831549665, -1.932750628810533389, -0.7978010075700513459 ) ) ;
#74861=CARTESIAN_POINT ( 'NONE',  ( 2.344387759578896890, 0.3747227385639141373, 1.683394173241028913 ) ) ;
#74863=CARTESIAN_POINT ( 'NONE',  ( 6.486587849989844834, -1.303813291173651301, 1.673118453357678392 ) ) ;
#74870=CARTESIAN_POINT ( 'NONE',  ( 3.352039220170324185, 0.8117645143102337757, -1.619458714540458866 ) ) ;
#74874=CARTESIAN_POINT ( 'NONE',  ( 3.686021078551263930, 1.009145865423091815, 1.504116352017518476 ) ) ;
#74875=CARTESIAN_POINT ( 'NONE',  ( 6.539320575229236709, 2.970193638644866851, 2.450124720169952752 ) ) ;
#74878=CARTESIAN_POINT ( 'NONE',  ( 4.474962758555542486, 1.701137449889396747, 0.7551977096921670407 ) ) ;
#74880=CARTESIAN_POINT ( 'NONE',  ( 1.018978518071847583, -1.731272710380473923, 0.8202338080745846804 ) ) ;
#74881=CARTESIAN_POINT ( 'NONE',  ( 1.149113351018778539, -1.436424422225426767, -1.126575773451453433 ) ) ;
#74889=CARTESIAN_POINT ( 'NONE',  ( 5.506690373602650901, 0.5681407172444596920, 1.885743917740757114 ) ) ;
#74892=CARTESIAN_POINT ( 'NONE',  ( 1.253981223613403806, 0.8486778832286197005, 1.910818189544212675 ) ) ;
#74893=CARTESIAN_POINT ( 'NONE',  ( 6.686557393816916495, -1.889396554722815758, -0.3748701224956552669 ) ) ;
#74895=CARTESIAN_POINT ( 'NONE',  ( 1.817148636465517164, -0.2269042555285011864, 1.811363274943120549 ) ) ;
#74896=CARTESIAN_POINT ( 'NONE',  ( 2.825073394047578734, 2.078234123670623212, 0.7428476018367863309 ) ) ;
#74898=CARTESIAN_POINT ( 'NONE',  ( 1.177825114000274898, 1.883588471398514264, -0.3297955356276888184 ) ) ;
#74899=CARTESIAN_POINT ( 'NONE',  ( 1.082395645157930852, 1.176005852300557653, -1.579744537442813401 ) ) ;
#74900=CARTESIAN_POINT ( 'NONE',  ( 2.630336588288070043, 0.2403035443280654992, 1.927090367541855365 ) ) ;
#74905=CARTESIAN_POINT ( 'NONE',  ( 6.192234700126073577, 0.9181466042854893317, -1.618627059862162376 ) ) ;
#74910=CARTESIAN_POINT ( 'NONE',  ( 2.613028500285840661, -0.2118117899099076218, 2.181281865515646068 ) ) ;
#74914=CARTESIAN_POINT ( 'NONE',  ( 2.771877994228102882, 0.9767612972278701955, 1.542236413651025151 ) ) ;
#74919=CARTESIAN_POINT ( 'NONE',  ( 0.9438256413601053829, 0.7817106414217175336, -1.760949446298063936 ) ) ;
#74920=CARTESIAN_POINT ( 'NONE',  ( 6.051606296966551390, 1.483190043545830283, 1.284043323103729595 ) ) ;
#74929=CARTESIAN_POINT ( 'NONE',  ( 5.366107254901440804, -2.060797467674013284, 0.1973761227843511823 ) ) ;
#74932=CARTESIAN_POINT ( 'NONE',  ( 5.625696599388652963, 0.4453364752643809155, 2.255009244304376992 ) ) ;
#74936=CARTESIAN_POINT ( 'NONE',  ( 6.614806897001766828, -0.1637801000826353548, 2.256214727502181994 ) ) ;
#74939=CARTESIAN_POINT ( 'NONE',  ( 5.367111071781861753, 1.871067490511884479, -0.5196462679451731015 ) ) ;
#74943=CARTESIAN_POINT ( 'NONE',  ( 5.765855477156511810, 0.5488314196105298359, -1.831976909803390896 ) ) ;
#74944=CARTESIAN_POINT ( 'NONE',  ( 6.528329376709017140, 0.9880424216301281204, -1.413504571246849695 ) ) ;
#74945=CARTESIAN_POINT ( 'NONE',  ( 6.034388706570055660, 0.6371486477873434806, 1.913263546360920220 ) ) ;
#74949=CARTESIAN_POINT ( 'NONE',  ( 1.166094707548096965, -1.325134400199390550, 1.617025002462493921 ) ) ;
#74950=CARTESIAN_POINT ( 'NONE',  ( 6.802016525601501051, -1.769270574432443510, 0.04669485764256275928 ) ) ;
#74951=CARTESIAN_POINT ( 'NONE',  ( 6.258435431136967431, 1.928752767684217106, -0.5880170417187426946 ) ) ;
#74953=CARTESIAN_POINT ( 'NONE',  ( 2.695625570186571895, -0.7177931702126126856, 2.177047689787997342 ) ) ;
#74954=CARTESIAN_POINT ( 'NONE',  ( 1.956607802488403269, 0.2990611944714368642, -1.714256857270479051 ) ) ;
#74955=CARTESIAN_POINT ( 'NONE',  ( 2.601940685209406467, 1.502730264585940168, 1.496503045097858919 ) ) ;
#74957=CARTESIAN_POINT ( 'NONE',  ( 2.055574482508758738, 1.511248224151232167, -0.8496982089122394610 ) ) ;
#74959=CARTESIAN_POINT ( 'NONE',  ( 1.996334026009699558, 1.840204857836050367, 0.2769876585018010706 ) ) ;
#74960=CARTESIAN_POINT ( 'NONE',  ( 2.225261637991797325, -1.984409513266917502, -0.8813929409505830703 ) ) ;
#74961=CARTESIAN_POINT ( 'NONE',  ( 3.432827581131673522, -1.645759781613131967, 1.164986487700324425 ) ) ;
#74962=CARTESIAN_POINT ( 'NONE',  ( 4.468750000000002665, 0.7852924748297492874, -1.895863743164178494 ) ) ;
#74964=CARTESIAN_POINT ( 'NONE',  ( 1.536025370465494921, 0.9519229637394033272, -1.674701244428679292 ) ) ;
#74966=CARTESIAN_POINT ( 'NONE',  ( 3.305138010220570521, -0.4367349056570711263, -2.177900917948209614 ) ) ;
#74968=CARTESIAN_POINT ( 'NONE',  ( -0.2110808730066961458, 1.402160971018800995, -2.056005932258188285 ) ) ;
#74972=CARTESIAN_POINT ( 'NONE',  ( 6.047183177241617358, 0.2169752325061699572, 2.210822359046988428 ) ) ;
#74974=CARTESIAN_POINT ( 'NONE',  ( 4.791432466842789673, -1.794507165602466037, 0.7932701521168731285 ) ) ;
#74979=CARTESIAN_POINT ( 'NONE',  ( 5.835331047353732536, -2.048883276207621229, 0.9597388403507837173 ) ) ;
#74981=CARTESIAN_POINT ( 'NONE',  ( 1.873554394494097997, -0.2548139927673950256, 2.046832928722150058 ) ) ;
#74986=CARTESIAN_POINT ( 'NONE',  ( 4.710133486059870478, -0.7981590245086762625, -1.691823354513532163 ) ) ;
#74987=CARTESIAN_POINT ( 'NONE',  ( 3.392920078539514162, -0.7062313252990999324, -1.584032799413936710 ) ) ;
#74988=CARTESIAN_POINT ( 'NONE',  ( 2.753125985903591477, 1.731854804227653366, -0.1727350219371779905 ) ) ;
#74989=CARTESIAN_POINT ( 'NONE',  ( 0.9082674546003096649, -1.036902680258915854, -2.044550831922228085 ) ) ;
#74990=CARTESIAN_POINT ( 'NONE',  ( 0.8157880970438775581, -0.3219574891645953785, 2.183050487710703536 ) ) ;
#74991=CARTESIAN_POINT ( 'NONE',  ( 4.142189164857057015, 0.5595570048471016911, 2.014385595549014418 ) ) ;
#74992=CARTESIAN_POINT ( 'NONE',  ( 5.490160960519338218, -0.4736594950825470107, -1.883182239726274076 ) ) ;
#74996=CARTESIAN_POINT ( 'NONE',  ( 0.05336153386781630759, -1.314994204386025434, 1.528742563917218078 ) ) ;
#74997=CARTESIAN_POINT ( 'NONE',  ( -0.1929003719821283658, -0.4722129235960635940, -2.074948700427194481 ) ) ;
#75003=CARTESIAN_POINT ( 'NONE',  ( 4.230939532379584200, 0.09184734775685021724, 1.823503176236190626 ) ) ;
#75004=CARTESIAN_POINT ( 'NONE',  ( 2.362605853119781774, 0.9431403173822919817, 1.995201469058570432 ) ) ;
#75009=CARTESIAN_POINT ( 'NONE',  ( 1.283469775389501910, 0.1441914389909859651, -2.014673257830889685 ) ) ;
#75012=CARTESIAN_POINT ( 'NONE',  ( 3.344433574756133787, -1.832611177030788685, -0.3225857369167430821 ) ) ;
#75015=ORIENTED_EDGE ( 'NONE', *, *, #4605, .F. ) ;
#75019=CARTESIAN_POINT ( 'NONE',  ( 3.686012862905340803, -0.8985999850123352894, 1.589152278004740237 ) ) ;
#75023=CARTESIAN_POINT ( 'NONE',  ( 0.8778075154764168886, -0.2618308253583972456, 1.713820766736633194 ) ) ;
#75024=CARTESIAN_POINT ( 'NONE',  ( 5.630750141678076304, -1.662707896839428434, 0.7909858098210584831 ) ) ;
#75025=CARTESIAN_POINT ( 'NONE',  ( 4.283989073270632275, 1.505461842163426933, 1.749087475023381133 ) ) ;
#75027=CARTESIAN_POINT ( 'NONE',  ( 6.679002375395027613, -0.09866081283815136826, -2.159460157733564145 ) ) ;
#75028=CARTESIAN_POINT ( 'NONE',  ( 6.239697403921985241, -2.179564881273305943, -0.7296402976008103947 ) ) ;
#75031=CARTESIAN_POINT ( 'NONE',  ( 5.717618200960680852, -1.824738551054584379, 0.4112096411929695439 ) ) ;
#75033=CARTESIAN_POINT ( 'NONE',  ( 2.461071540317420592, -1.587761714688111780, 1.065645112462119570 ) ) ;
#75035=CARTESIAN_POINT ( 'NONE',  ( 3.826972293661185187, 2.095320012007126476, 0.6930106488920934060 ) ) ;
#75036=CARTESIAN_POINT ( 'NONE',  ( 4.663340677796647071, 1.974402194736598837, -0.7651654921337573967 ) ) ;
#75038=CARTESIAN_POINT ( 'NONE',  ( 6.983263157960365675, 7.629137130509066722, 2.646189081643287810 ) ) ;
#75041=CARTESIAN_POINT ( 'NONE',  ( 2.872455039471259575, 1.233635154574242554, 1.949979759383664524 ) ) ;
#75042=CARTESIAN_POINT ( 'NONE',  ( 3.139059813392345077, -0.1416510307416830594, -1.956792864499560691 ) ) ;
#75045=CARTESIAN_POINT ( 'NONE',  ( 6.912941059211402894, -1.598140348199797556, 1.303530876689311224 ) ) ;
#75049=CARTESIAN_POINT ( 'NONE',  ( 4.557827498477605488, 1.164984774316142113, 1.645760986912048640 ) ) ;
#75054=CARTESIAN_POINT ( 'NONE',  ( 1.499139249613313574, 0.4210003976099167544, 2.129699363925404487 ) ) ;
#75060=CARTESIAN_POINT ( 'NONE',  ( 1.089218918643636069, 1.818803954151678726, -0.9688405272365168130 ) ) ;
#75066=CARTESIAN_POINT ( 'NONE',  ( 3.563058999304801411, -1.561743426874351970, 1.103242700682869781 ) ) ;
#75067=CARTESIAN_POINT ( 'NONE',  ( 5.190226478415982392, -1.756784752911320302, -0.2140884780794347908 ) ) ;
#75071=CARTESIAN_POINT ( 'NONE',  ( 6.064071300241554496, -1.020233025338047383, 1.621115200587377014 ) ) ;
#75073=CARTESIAN_POINT ( 'NONE',  ( 1.152881054890652957, -0.5012615762394446728, -2.008655542368184221 ) ) ;
#75075=CARTESIAN_POINT ( 'NONE',  ( 6.209813078548920728, -1.856259414618817383, 0.2309603555875269776 ) ) ;
#75076=CARTESIAN_POINT ( 'NONE',  ( 1.928079105319381314, 1.052063804484974385, -1.491885150056403431 ) ) ;
#75077=CARTESIAN_POINT ( 'NONE',  ( 5.479209177496175087, -0.05098606815037013545, -2.206463706674952618 ) ) ;
#75080=CARTESIAN_POINT ( 'NONE',  ( 3.332538901969614553, -1.230775513943611399, 1.655089866650825581 ) ) ;
#75084=CARTESIAN_POINT ( 'NONE',  ( 0.2808502495336914206, -2.096634173354972486, -0.5254431554712820640 ) ) ;
#75087=CARTESIAN_POINT ( 'NONE',  ( 5.477033855465498924, 1.911541192706748715, 0.7957256658025002594 ) ) ;
#75089=CARTESIAN_POINT ( 'NONE',  ( 2.882270108570818223, -1.113908571083363164, 1.852364028112465810 ) ) ;
#75091=CARTESIAN_POINT ( 'NONE',  ( 3.106122398345218638, -0.8164384046550461349, 1.847479848726358398 ) ) ;
#75092=CARTESIAN_POINT ( 'NONE',  ( 1.838261372102001800, -1.052240823716396267, 1.655630454418555830 ) ) ;
#75100=CARTESIAN_POINT ( 'NONE',  ( 0.8664231474371618669, -1.968446048378743152, -0.4370742218882398000 ) ) ;
#75102=CARTESIAN_POINT ( 'NONE',  ( 5.917560222199001352, -1.216239291071326001, -1.822900893127032962 ) ) ;
#75104=CARTESIAN_POINT ( 'NONE',  ( 6.152599605923961157, 1.892562589925715466, 0.2737767527046449101 ) ) ;
#75108=CARTESIAN_POINT ( 'NONE',  ( 3.075796161730546707, -0.8146103074460913085, 1.844718345957757188 ) ) ;
#75111=CARTESIAN_POINT ( 'NONE',  ( 6.756889588843246308, -1.328954913838266361, 1.099249449767102593 ) ) ;
#75115=CARTESIAN_POINT ( 'NONE',  ( 4.780451015977909002, -1.813929833846049666, -0.4561423458772846939 ) ) ;
#75119=CARTESIAN_POINT ( 'NONE',  ( 1.534126288888465917, 1.230018689141991306, 1.665114864061276512 ) ) ;
#75123=CARTESIAN_POINT ( 'NONE',  ( -0.1409997244346088141, -0.002808977843308038680, -2.000147647483838220 ) ) ;
#75124=CARTESIAN_POINT ( 'NONE',  ( 0.3865838573892222962, -1.705918499434391444, -0.6100900862041622741 ) ) ;
#75130=CARTESIAN_POINT ( 'NONE',  ( 1.644895634054041933, -0.2845770130874228365, -1.940982728367894206 ) ) ;
#75132=CARTESIAN_POINT ( 'NONE',  ( 6.011341193797766103, -1.801927099207595084, 0.6504362055675115828 ) ) ;
#75135=CARTESIAN_POINT ( 'NONE',  ( 6.727182134110234024, -0.002100931800118066312, 2.089081857379894824 ) ) ;
#75139=CARTESIAN_POINT ( 'NONE',  ( 2.694378501574711926, -2.155843008138720762, -0.1600555415394027403 ) ) ;
#75142=CARTESIAN_POINT ( 'NONE',  ( 0.2113915902133573221, 1.759560880827226947, -1.183302968686468226 ) ) ;
#75143=CARTESIAN_POINT ( 'NONE',  ( 5.420859398437725574, 1.687492901312273474, 0.6969783729503381542 ) ) ;
#75145=CARTESIAN_POINT ( 'NONE',  ( 1.212115688179933759, -0.8827433895065642799, -1.762721879769993283 ) ) ;
#75146=CARTESIAN_POINT ( 'NONE',  ( 3.972844611716894736, -1.413603510852480927, 1.288168406687495215 ) ) ;
#75149=CARTESIAN_POINT ( 'NONE',  ( 4.791434771068385778, -1.801603960925775016, 0.7962418042333998525 ) ) ;
#75151=CARTESIAN_POINT ( 'NONE',  ( 6.532770933798597746, -1.732582191135303651, 0.8775855664264734513 ) ) ;
#75157=CARTESIAN_POINT ( 'NONE',  ( 4.424404876070213710, -0.8207606565990737124, -1.727334472114170794 ) ) ;
#75161=CARTESIAN_POINT ( 'NONE',  ( 6.129547061768469085, -0.2442746830248194168, 1.998141925448652989 ) ) ;
#75164=CARTESIAN_POINT ( 'NONE',  ( 5.865807274569020180, 1.797851641234180509, -0.3166982042408575948 ) ) ;
#75165=CARTESIAN_POINT ( 'NONE',  ( 5.665250009225348826, 1.861346387706263261, -0.7762253298396750711 ) ) ;
#75166=CARTESIAN_POINT ( 'NONE',  ( 6.727182134110231360, 6.039168392632435989, 2.405853653942996218 ) ) ;
#75167=CARTESIAN_POINT ( 'NONE',  ( 1.574760213118006735, 1.391939136705011348, -1.532762857463897843 ) ) ;
#75177=CARTESIAN_POINT ( 'NONE',  ( 6.925078400183574345, 6.038986730273901316, 2.350556043039519150 ) ) ;
#75179=CARTESIAN_POINT ( 'NONE',  ( 4.887242738553729815, -0.5912784195612891258, -1.630374673469140223 ) ) ;
#75181=CARTESIAN_POINT ( 'NONE',  ( 2.729418486472269922, 0.1060373921930452268, -2.067687848736274869 ) ) ;
#75182=CARTESIAN_POINT ( 'NONE',  ( 3.181382749799996468, 1.670748044588391990, 1.300414933884207480 ) ) ;
#75185=CARTESIAN_POINT ( 'NONE',  ( 1.885543262503614592, -1.856164082770836110, 0.6587638493158411990 ) ) ;
#75189=CARTESIAN_POINT ( 'NONE',  ( 4.172042307184393728, -1.321354948109268346, 1.872925066384116377 ) ) ;
#75190=CARTESIAN_POINT ( 'NONE',  ( 1.752308680507021155, 0.5713779359179693706, 1.734036872924920702 ) ) ;
#75194=CARTESIAN_POINT ( 'NONE',  ( 2.601816991827472947, 1.426658649466717943, 1.420685320369071025 ) ) ;
#75195=CARTESIAN_POINT ( 'NONE',  ( 1.885527806591394961, -1.848987351811198998, 0.6559936482007987513 ) ) ;
#75200=CARTESIAN_POINT ( 'NONE',  ( 4.505862177948306346, -0.8935697331868618365, -1.890194782795044492 ) ) ;
#75201=CARTESIAN_POINT ( 'NONE',  ( 4.223360090310752213, -1.693420319160190646, 0.5144795390387302270 ) ) ;
#75203=CARTESIAN_POINT ( 'NONE',  ( 0.4807640440005828131, -0.2721776580492247799, -2.174417363000572756 ) ) ;
#75204=CARTESIAN_POINT ( 'NONE',  ( 5.472502228039195060, -0.04848951148075366507, -1.739831344048385908 ) ) ;
#75207=CARTESIAN_POINT ( 'NONE',  ( 5.994848186622900421, -2.281820642442307090, 0.2777966721622132096 ) ) ;
#75209=CARTESIAN_POINT ( 'NONE',  ( 5.694640849732851784, -1.102317705797692726, -1.338331167630167684 ) ) ;
#75210=CARTESIAN_POINT ( 'NONE',  ( 6.232918786939658062, -2.059688491082920070, -0.6869823432723211054 ) ) ;
#75212=CARTESIAN_POINT ( 'NONE',  ( 0.2865162857260491469, -0.7196341243457348158, -1.991407047551809750 ) ) ;
#75213=CARTESIAN_POINT ( 'NONE',  ( 3.593750000000001776, -1.895863743164161841, -0.7852924748297959168 ) ) ;
#75214=CARTESIAN_POINT ( 'NONE',  ( 6.827182134110205247, 2.955377424523279117, 2.541486622063714673 ) ) ;
#75215=CARTESIAN_POINT ( 'NONE',  ( 4.858382476810707118, 0.7369543258428765675, 1.780043821814878413 ) ) ;
#75217=CARTESIAN_POINT ( 'NONE',  ( 1.770501988737150922, 2.215049892327343173, -0.1675478377428234744 ) ) ;
#75223=CARTESIAN_POINT ( 'NONE',  ( 2.666879960053496479, 0.7507478997158049117, 2.090701262698462681 ) ) ;
#75229=CARTESIAN_POINT ( 'NONE',  ( 1.178361531996233280, 1.528742360773158282, 1.314995429398260196 ) ) ;
#75231=CARTESIAN_POINT ( 'NONE',  ( 6.877413164483755281, -0.1458786163922053403, 2.030295828278828374 ) ) ;
#75235=CARTESIAN_POINT ( 'NONE',  ( 0.8601951712396675997, -1.287299901140761316, 1.214705651989380852 ) ) ;
#75236=CARTESIAN_POINT ( 'NONE',  ( 0.4400775573648734174, -1.704940109561555950, -1.076314675215600314 ) ) ;
#75237=CARTESIAN_POINT ( 'NONE',  ( 5.231891002347484054, 1.715934187082169604, 0.2900348964059005774 ) ) ;
#75238=CARTESIAN_POINT ( 'NONE',  ( 4.001757606804694056, -2.286216240038071668, 0.1689928914557006778 ) ) ;
#75240=CARTESIAN_POINT ( 'NONE',  ( 1.886409237429786279, 1.602333580200336671, -0.9066872629178088783 ) ) ;
#75242=CARTESIAN_POINT ( 'NONE',  ( 2.766400663125650361, -1.260407102598060103, 1.320874842943790872 ) ) ;
#75243=CARTESIAN_POINT ( 'NONE',  ( 4.360000113718985659, -0.002809843368253156070, -2.016597020062675050 ) ) ;
#75245=CARTESIAN_POINT ( 'NONE',  ( 2.325404209529509103, -2.741642530189327160E-05, 2.262689075223401236 ) ) ;
#75247=CARTESIAN_POINT ( 'NONE',  ( 5.737368847912779124, -1.905360455185100887, 0.8973202462331535401 ) ) ;
#75249=CARTESIAN_POINT ( 'NONE',  ( 2.770052221688572125, -2.048192801557855436, 0.3012726569043902569 ) ) ;
#75252=CARTESIAN_POINT ( 'NONE',  ( 4.231183009085410340, 1.939187816756043237, 0.8583030597293441755 ) ) ;
#75253=CARTESIAN_POINT ( 'NONE',  ( 0.6274103741727736772, -1.829744589303895275, 0.6030480328435404713 ) ) ;
#75260=CARTESIAN_POINT ( 'NONE',  ( 5.888958097455845753, -2.014202512972632420, -0.6635655960139997811 ) ) ;
#75261=CARTESIAN_POINT ( 'NONE',  ( 2.169099057653073093, -1.925109178590768799, -0.8542606987168609445 ) ) ;
#75264=CARTESIAN_POINT ( 'NONE',  ( 6.508657375787280763, 0.5831478024676381988, 1.767317905175052051 ) ) ;
#75270=CARTESIAN_POINT ( 'NONE',  ( 0.08834397731360790762, 1.226219587655341448, 1.729930300845914815 ) ) ;
#75273=CARTESIAN_POINT ( 'NONE',  ( 3.385159196556942085, 0.04556868695702701727, 1.961494628812537444 ) ) ;
#75274=CARTESIAN_POINT ( 'NONE',  ( 1.235488887756378551, -1.954010380348418119, 0.9248176494114216384 ) ) ;
#75278=CARTESIAN_POINT ( 'NONE',  ( 3.011345489304529277, -0.8582029173807427247, -1.513924679874333767 ) ) ;
#75282=CARTESIAN_POINT ( 'NONE',  ( 1.757185253014027282, -2.006138798620077157, -0.2004061740628823030 ) ) ;
#75285=CARTESIAN_POINT ( 'NONE',  ( 1.973447535326333879, 1.887181058671667966, -0.5703184155462033278 ) ) ;
#75286=CARTESIAN_POINT ( 'NONE',  ( 5.431871263539022721, -1.864374737420209760, 0.4251265778823994368 ) ) ;
#75292=CARTESIAN_POINT ( 'NONE',  ( 2.772133559515827184, 2.009754670806723098, -0.2000300323863890006 ) ) ;
#75294=CARTESIAN_POINT ( 'NONE',  ( 5.210162647842351724, -2.297074225899544242, 0.2200332968223562558 ) ) ;
#75295=CARTESIAN_POINT ( 'NONE',  ( 6.619590441841329387, 0.3365870006281460047, -1.932621868259084330 ) ) ;
#75297=CARTESIAN_POINT ( 'NONE',  ( 3.362109073961420780, -1.959717995770013932, 0.09162775335717905645 ) ) ;
#75299=CARTESIAN_POINT ( 'NONE',  ( 0.8795299900376440938, -0.4926441280813895762, -1.955172062459667126 ) ) ;
#75301=CARTESIAN_POINT ( 'NONE',  ( 1.886098781581479145, -2.116736904955533571, 0.05756534462913154987 ) ) ;
#75304=CARTESIAN_POINT ( 'NONE',  ( 2.484105014303281234, -0.3146448974087300288, -1.813890345909507928 ) ) ;
#75308=CARTESIAN_POINT ( 'NONE',  ( 3.164422831683691761, 2.120778211551369807, -0.003951117757632071313 ) ) ;
#75312=CARTESIAN_POINT ( 'NONE',  ( 3.866525002278593526, -1.386861471309716265, 1.524430686435477522 ) ) ;
#75314=CARTESIAN_POINT ( 'NONE',  ( 1.083273795380396143, -0.8277460070302902206, 1.644747122058511035 ) ) ;
#75319=CARTESIAN_POINT ( 'NONE',  ( 0.8915962724085277902, 1.944627461026976034, -1.043433064090833140 ) ) ;
#75320=CARTESIAN_POINT ( 'NONE',  ( 2.618781011676008852, 1.479506999046651838, -1.711640912222348376 ) ) ;
#75322=CARTESIAN_POINT ( 'NONE',  ( 3.902463391467089426, -1.792703881930355347, -0.2598333579746092692 ) ) ;
#75323=CARTESIAN_POINT ( 'NONE',  ( 3.380013747803870316, -1.913774515330651127, -0.08860483629866824917 ) ) ;
#75324=CARTESIAN_POINT ( 'NONE',  ( 4.035645461687249913, 1.950487776689105557, -0.6946759356915442885 ) ) ;
#75326=CARTESIAN_POINT ( 'NONE',  ( 3.274254179156810274, -1.175395456433829144, 1.582609504276990320 ) ) ;
#75327=CARTESIAN_POINT ( 'NONE',  ( 0.6043602652519001195, -0.6458173669235712788, -1.815047198766789327 ) ) ;
#75328=CARTESIAN_POINT ( 'NONE',  ( 3.854256360616271415, 0.6726810918341770140, 1.745705178215435582 ) ) ;
#75329=CARTESIAN_POINT ( 'NONE',  ( 2.596638674903679167, -2.301597171833298372, -0.1684899434626195847 ) ) ;
#75331=CARTESIAN_POINT ( 'NONE',  ( 3.859670702416746924, -0.5421201558965526024, 1.780318336934373802 ) ) ;
#75336=CARTESIAN_POINT ( 'NONE',  ( 1.102331697304242297, -2.106257354988652075, 0.001776637707836397316 ) ) ;
#75339=CARTESIAN_POINT ( 'NONE',  ( 6.872347393157318685, -1.336039616365672700, 1.699942530728588919 ) ) ;
#75340=CARTESIAN_POINT ( 'NONE',  ( 2.320699612028754188, -0.8158636990020677882, -1.957571985684476212 ) ) ;
#75341=CARTESIAN_POINT ( 'NONE',  ( 6.199869188016119637, 1.394352454258035001, 1.461346697781773507 ) ) ;
#75346=CARTESIAN_POINT ( 'NONE',  ( 0.9663661119345479111, 1.064502738163356721, 1.881203019380036867 ) ) ;
#75349=CARTESIAN_POINT ( 'NONE',  ( 6.925078400183515726, -0.002206826874838820583, 1.955452213090567160 ) ) ;
#75353=CARTESIAN_POINT ( 'NONE',  ( 4.698454014923811428, 1.387101836239763131, -1.463925544105355803 ) ) ;
#75358=CARTESIAN_POINT ( 'NONE',  ( 0.1282872750541429741, -1.395696511722638977, -1.781683957999291579 ) ) ;
#75362=CARTESIAN_POINT ( 'NONE',  ( 6.521112179100128969, -1.799899466697444383, 0.9092066555835758290 ) ) ;
#75366=CARTESIAN_POINT ( 'NONE',  ( 3.140908386031955324, -1.520905784971425589, 0.8136546746303519040 ) ) ;
#75369=CARTESIAN_POINT ( 'NONE',  ( 0.6843625024184678551, -0.2082719882288592839, -1.757362784332392458 ) ) ;
#75370=CARTESIAN_POINT ( 'NONE',  ( 2.139316306618759711, 0.002201468654887753229, 2.013265973851806834 ) ) ;
#75371=CARTESIAN_POINT ( 'NONE',  ( 4.067547972739316897, 0.2730280005818259137, -2.189760481282684967 ) ) ;
#75376=CARTESIAN_POINT ( 'NONE',  ( 4.793665170694914046, 1.978287127071875151, -0.7638792978137475265 ) ) ;
#75377=CARTESIAN_POINT ( 'NONE',  ( 2.618767733003044551, 0.2496279305150179983, 2.000855661889962445 ) ) ;
#75378=CARTESIAN_POINT ( 'NONE',  ( 3.427799431637909233, -1.783865866189004556, 0.3147462633073249139 ) ) ;
#75382=CARTESIAN_POINT ( 'NONE',  ( 0.3560485870845608858, 0.7116971694140910021, 1.730184004908103867 ) ) ;
#75385=CARTESIAN_POINT ( 'NONE',  ( 5.848246728868278232, 1.823843535133644389, 0.08496628090458313576 ) ) ;
#75387=CARTESIAN_POINT ( 'NONE',  ( 2.008866915445167045, 0.004233813517278902337, 1.915903396628533706 ) ) ;
#75396=CARTESIAN_POINT ( 'NONE',  ( 3.322626870553476941, -0.8629183168706102691, -1.937285153019531414 ) ) ;
#75399=CARTESIAN_POINT ( 'NONE',  ( 4.657473197611246896, 0.4347632249906174806, -1.922659379041303129 ) ) ;
#75400=CARTESIAN_POINT ( 'NONE',  ( 0.05298979808228323346, 0.3483158054882686261, 1.982706882182909025 ) ) ;
#75402=CARTESIAN_POINT ( 'NONE',  ( 0.3513568635829470432, 0.2028739153508585802, -2.107475566755373730 ) ) ;
#75404=CARTESIAN_POINT ( 'NONE',  ( 1.486871883557450369, 1.994755712061954123, 0.5540851298423480342 ) ) ;
#75405=CARTESIAN_POINT ( 'NONE',  ( 2.695178803863579997, -0.6086341500050916897, 1.844178105057793893 ) ) ;
#75409=CARTESIAN_POINT ( 'NONE',  ( 3.679701837385487284, -1.030134525132427203, 1.819138145232774839 ) ) ;
#75412=CARTESIAN_POINT ( 'NONE',  ( 0.8030048707254822116, 1.598173448761495585, -0.8528199064772985505 ) ) ;
#75414=CARTESIAN_POINT ( 'NONE',  ( 5.426482453889071245, 1.317083479513626587, -1.770629405693980640 ) ) ;
#75416=CARTESIAN_POINT ( 'NONE',  ( 3.751171811254182753, -1.805526059370649028, 1.268566889074909554 ) ) ;
#75419=CARTESIAN_POINT ( 'NONE',  ( 3.158751774003202950, 0.4669426847015486493, 1.854258104404989060 ) ) ;
#75421=CARTESIAN_POINT ( 'NONE',  ( 5.529760519541640384, 1.996289034380031913, -0.5486624943154896350 ) ) ;
#75423=CARTESIAN_POINT ( 'NONE',  ( 2.430746436576446179, 2.096607243605509208, 0.5259719050795114148 ) ) ;
#75424=CARTESIAN_POINT ( 'NONE',  ( 4.704715985517350596, 1.906866092115505840, 1.080010033982371498 ) ) ;
#75434=CARTESIAN_POINT ( 'NONE',  ( 6.139524545372063713, 1.915082402702467101, -0.7868883245659707981 ) ) ;
#75435=CARTESIAN_POINT ( 'NONE',  ( 4.899011302651929078, 1.600714092801895472, -1.071686876026227475 ) ) ;
#75436=CARTESIAN_POINT ( 'NONE',  ( 0.3863424973270003226, -0.6820169105002243937, -1.897691504806876761 ) ) ;
#75439=CARTESIAN_POINT ( 'NONE',  ( 5.014487319174643964, 0.7500019944287477092, 1.821250405324719823 ) ) ;
#75440=CARTESIAN_POINT ( 'NONE',  ( 6.703114550498504798, -0.5130225571751775293, 2.242675272849779411 ) ) ;
#75441=CARTESIAN_POINT ( 'NONE',  ( 4.863791234866603475, 1.805334366393744450, -0.2710410529033688842 ) ) ;
#75447=CARTESIAN_POINT ( 'NONE',  ( 2.700538275128167687, 1.556679782967337999, 0.9830204120172959525 ) ) ;
#75448=CARTESIAN_POINT ( 'NONE',  ( -0.04036574886347610303, -1.557478217179044888, -1.275100411523772737 ) ) ;
#75449=CARTESIAN_POINT ( 'NONE',  ( 1.089736160853293168, 1.367490553916232754, -1.847165887925501515 ) ) ;
#75450=CARTESIAN_POINT ( 'NONE',  ( 0.3032578436052570936, -1.433215674808469009, -1.186817810889209124 ) ) ;
#75456=CARTESIAN_POINT ( 'NONE',  ( 2.753556666441462131, 2.080443298914707917, -0.2074443561481206788 ) ) ;
#75457=CARTESIAN_POINT ( 'NONE',  ( 0.8131078318618142342, -0.2785150557334699073, 1.849687307983488571 ) ) ;
#75458=CARTESIAN_POINT ( 'NONE',  ( 2.354842093047845530, -0.8645933883619570937, 1.821462535208747457 ) ) ;
#75461=CARTESIAN_POINT ( 'NONE',  ( 2.014833872101874146, -1.687939792665555494, 0.4236265878580796618 ) ) ;
#75466=CARTESIAN_POINT ( 'NONE',  ( 2.560839114378242076, -1.500511350262800470, -0.8505237462590549136 ) ) ;
#75467=CARTESIAN_POINT ( 'NONE',  ( 2.595491417077447238, -0.6846416945752286098, 2.081959150545972914 ) ) ;
#75468=CARTESIAN_POINT ( 'NONE',  ( 5.022202109028018668, -1.178465353167540197, -1.865713892744431446 ) ) ;
#75470=CARTESIAN_POINT ( 'NONE',  ( 2.536178501573463695, 1.332599179293973091, 1.713937585783622541 ) ) ;
#75471=CARTESIAN_POINT ( 'NONE',  ( 0.9436603434208358232, 0.7422609627109194586, -1.668170528445270140 ) ) ;
#75472=CARTESIAN_POINT ( 'NONE',  ( 3.468056730359007744, -1.039945921192251266, 1.844253657775334121 ) ) ;
#75476=CARTESIAN_POINT ( 'NONE',  ( 3.808379203468327034, 1.620604861375672945, -1.621544036339316985 ) ) ;
#75481=CARTESIAN_POINT ( 'NONE',  ( 5.479204513921561492, -2.007303783262293972, -0.9515056986081956714 ) ) ;
#75485=CARTESIAN_POINT ( 'NONE',  ( 6.825078400183555161, 2.980425674467933828, 2.309322343017068402 ) ) ;
#75487=CARTESIAN_POINT ( 'NONE',  ( 4.324842380567116784, 0.8596320953860696612, -1.824118450417112847 ) ) ;
#75489=CARTESIAN_POINT ( 'NONE',  ( 2.799736005369108049, -1.525370932871713547, -1.388464765246626875 ) ) ;
#75493=CARTESIAN_POINT ( 'NONE',  ( 6.562441972333600937, -2.001882313047067985, -0.8919867065708479981 ) ) ;
#75494=CARTESIAN_POINT ( 'NONE',  ( 3.199842427594956185, 1.824118962040650604, 0.8596310190432245868 ) ) ;
#75495=CARTESIAN_POINT ( 'NONE',  ( 2.665370095338463585, 0.9869154847663293983, 1.554228294351194473 ) ) ;
#75498=CARTESIAN_POINT ( 'NONE',  ( 6.106453908201667780, -0.6597477751954274883, -1.702385593799011110 ) ) ;
#75499=CARTESIAN_POINT ( 'NONE',  ( -0.01642261062154842799, -2.298356651571492826, -0.04744217504730821600 ) ) ;
#75501=CARTESIAN_POINT ( 'NONE',  ( 6.069232182892009497, 0.1736634173518056545, -2.255917496054614446 ) ) ;
#75502=CARTESIAN_POINT ( 'NONE',  ( 1.506614580823143701, -0.7594792294695625889, -1.964545455775383642 ) ) ;
#75511=CARTESIAN_POINT ( 'NONE',  ( 2.057031522680652369, 0.4693188842763912905, 2.067847215655476134 ) ) ;
#75512=CARTESIAN_POINT ( 'NONE',  ( 4.183969649472300212, 2.154223736155444602, -0.5416631952432825470 ) ) ;
#75513=CARTESIAN_POINT ( 'NONE',  ( 0.1181803206181560040, -2.163391993613572151, 0.4351206515559591370 ) ) ;
#75516=CARTESIAN_POINT ( 'NONE',  ( 4.228923158279327410, -1.829750178516520442, -0.7082015076659909925 ) ) ;
#75525=CARTESIAN_POINT ( 'NONE',  ( 3.428091063814618700, -2.088597262255381448, 0.3661859999234198249 ) ) ;
#75527=CARTESIAN_POINT ( 'NONE',  ( 5.418883921851007202, 1.995750516393671514, 0.8311057252617033431 ) ) ;
#75528=CARTESIAN_POINT ( 'NONE',  ( 3.843160323004328305, 0.6166970922517556186, -1.735048075492843234 ) ) ;
#75529=CARTESIAN_POINT ( 'NONE',  ( 4.962125165302472496, -1.116212726388360998, 1.679221540125563905 ) ) ;
#75532=CARTESIAN_POINT ( 'NONE',  ( 6.685563754570789996, -0.7372397036040450047, 1.575249959525576005 ) ) ;
#75533=CARTESIAN_POINT ( 'NONE',  ( 6.827182134110198142, 0.003888933837258023996, 1.810856214465889069 ) ) ;
#75536=CARTESIAN_POINT ( 'NONE',  ( 3.643588467267334874, -1.635511012911139650, -1.413612897787956513 ) ) ;
#75537=CARTESIAN_POINT ( 'NONE',  ( 5.852888695852590750, -0.9090035733541059759, 1.799648235488074732 ) ) ;
#75540=CARTESIAN_POINT ( 'NONE',  ( 3.221700144506876917, -2.083771231579465866, 0.5749860669421112958 ) ) ;
#75541=CARTESIAN_POINT ( 'NONE',  ( 3.426987366535645396, 0.04501397872612270673, 1.970993176858675699 ) ) ;
#75544=CARTESIAN_POINT ( 'NONE',  ( 1.466329616580586581, 2.273096917617071888, -0.3966160293069305731 ) ) ;
#75545=CARTESIAN_POINT ( 'NONE',  ( 2.741540247014317533, -1.524689737823584190, -1.386575092742351245 ) ) ;
#75546=CARTESIAN_POINT ( 'NONE',  ( 5.882362869737407074, -0.2893225776206589384, -1.920288418758001159 ) ) ;
#75554=CARTESIAN_POINT ( 'NONE',  ( 2.538337413235943973, 1.040872164564849767, -1.945885072647230318 ) ) ;
#75557=CARTESIAN_POINT ( 'NONE',  ( 6.455910365318025868, -0.6640748382394038307, 1.846044136633723243 ) ) ;
#75558=CARTESIAN_POINT ( 'NONE',  ( 6.539320575229233157, 0.001224430076711413356, 2.103502572931112091 ) ) ;
#75563=CARTESIAN_POINT ( 'NONE',  ( 5.314338895140061858, 1.702579029208791450, 0.7012131971957938914 ) ) ;
#75565=CARTESIAN_POINT ( 'NONE',  ( 2.079048039887823052, -0.09986672515850322784, -2.058587512739398662 ) ) ;
#75572=CARTESIAN_POINT ( 'NONE',  ( 0.7782833776110262836, -1.145455985629862505, 1.713024904945841254 ) ) ;
#75574=CARTESIAN_POINT ( 'NONE',  ( 1.767777038385684785, -1.847514956963384414, 0.2233714002321494363 ) ) ;
#75575=CARTESIAN_POINT ( 'NONE',  ( 4.985823801847525161, -1.827980399782932697, -0.2200341325891697619 ) ) ;
#75581=CARTESIAN_POINT ( 'NONE',  ( 4.530015419921377351, -1.356323209173672106, -1.740806116466916409 ) ) ;
#75582=CARTESIAN_POINT ( 'NONE',  ( 0.5444778865218368180, 2.155786741090206959, 0.1595364878888144988 ) ) ;
#75584=CARTESIAN_POINT ( 'NONE',  ( -0.1405747822309927342, -1.479430311965252542, -1.211566217618691210 ) ) ;
#75585=CARTESIAN_POINT ( 'NONE',  ( 6.509000000000050967, 0.007656933339270000430, 1.900274884395843022 ) ) ;
#75589=CARTESIAN_POINT ( 'NONE',  ( 5.690081826675051246, 1.142623417513729089, 1.533212917768103534 ) ) ;
#75590=CARTESIAN_POINT ( 'NONE',  ( 1.164687902950040321, -1.689591380799923215, -0.8031939614948147010 ) ) ;
#75591=CARTESIAN_POINT ( 'NONE',  ( 2.184780103950241248, 1.616692242240840960, -1.205043568535242304 ) ) ;
#75593=CARTESIAN_POINT ( 'NONE',  ( 3.440152538952054861, 0.9466726917620759130, -1.881381795136138679 ) ) ;
#75598=CARTESIAN_POINT ( 'NONE',  ( 4.148698013468838930, 1.981613772426650266, 0.3898967627796907642 ) ) ;
#75602=CARTESIAN_POINT ( 'NONE',  ( 4.534552404040613105, 2.118918870418550870, 0.4265773709258223190 ) ) ;
#75608=CARTESIAN_POINT ( 'NONE',  ( 1.873705115703153679, -0.2670016379083521296, 2.154652869704001272 ) ) ;
#75611=CARTESIAN_POINT ( 'NONE',  ( 1.118424870118275738, -0.04499623084481922664, 1.840855209834332928 ) ) ;
#75614=CARTESIAN_POINT ( 'NONE',  ( 1.927518781310177509, -1.434474475899261581, -1.656937093973806396 ) ) ;
#75615=CARTESIAN_POINT ( 'NONE',  ( 6.983263157960361234, 4.694303448529787204, 2.516403841208918912 ) ) ;
#75616=CARTESIAN_POINT ( 'NONE',  ( 3.362467959171450360, 1.015586399080644187, 2.021831916694483144 ) ) ;
#75618=CARTESIAN_POINT ( 'NONE',  ( 4.575407832915947104, 1.497500392235491029, 1.350737390116145242 ) ) ;
#75624=CARTESIAN_POINT ( 'NONE',  ( 4.463939829769240752, 0.8331255105114807602, 1.561325262609781772 ) ) ;
#75626=CARTESIAN_POINT ( 'NONE',  ( 0.6925746140923200178, -2.090094003047581861, -0.2575201054717362048 ) ) ;
#75629=CARTESIAN_POINT ( 'NONE',  ( 0.7132589462262963753, -1.661971685727476000, -1.056574055910926013 ) ) ;
#75633=CARTESIAN_POINT ( 'NONE',  ( 5.220911918456066836, 1.366450397884883428, -1.189473885788590035 ) ) ;
#75636=CARTESIAN_POINT ( 'NONE',  ( 4.504681594071535677, 1.446009304718363087, -1.186774495104812699 ) ) ;
#75637=CARTESIAN_POINT ( 'NONE',  ( 4.293848342403890683, -1.423947089648310849, -1.503027170334819029 ) ) ;
#75647=CARTESIAN_POINT ( 'NONE',  ( 4.475024536774164119, 1.792854848340214025, 0.7970393728587571447 ) ) ;
#75648=CARTESIAN_POINT ( 'NONE',  ( 1.546249734355091388, 1.863884247081739831, -0.7690006294575403301 ) ) ;
#75650=CARTESIAN_POINT ( 'NONE',  ( 6.639320575229255006, 4.698690022235154196, 2.459427960261594048 ) ) ;
#75651=CARTESIAN_POINT ( 'NONE',  ( 0.8603690976232807319, -1.359099942111790416, 1.285485254608226269 ) ) ;
#75653=CARTESIAN_POINT ( 'NONE',  ( 3.586193004068451540, 1.121915001286919233, 1.671427700405977212 ) ) ;
#75655=CARTESIAN_POINT ( 'NONE',  ( 3.392305424709577188, -0.8603400307676151160, -1.934732246027433433 ) ) ;
#75657=CARTESIAN_POINT ( 'NONE',  ( 4.369627354678314646, -0.3570511267821044332, 2.039192500141631115 ) ) ;
#75659=CARTESIAN_POINT ( 'NONE',  ( 6.580031098407260082, -2.049997751086956921, -0.4092652541880793526 ) ) ;
#75660=CARTESIAN_POINT ( 'NONE',  ( 6.620655732516684822, 7.052296306484477029, 2.671890196246820004 ) ) ;
#75661=CARTESIAN_POINT ( 'NONE',  ( 4.858326754937916547, 0.6996357133068830114, 1.686392194618462570 ) ) ;
#75668=CARTESIAN_POINT ( 'NONE',  ( 6.182274467271688501, 0.9872068455926674702, 1.637624497839342608 ) ) ;
#75677=CARTESIAN_POINT ( 'NONE',  ( 5.396111305808362957, -0.9091601233324579923, -1.799916296964368279 ) ) ;
#75681=CARTESIAN_POINT ( 'NONE',  ( 0.1394461523057136665, 6.947783040739019533, -2.314776707679897516 ) ) ;
#75684=CARTESIAN_POINT ( 'NONE',  ( 2.201947278869041291, 0.7584239558163529127, -1.817761916770490149 ) ) ;
#75685=CARTESIAN_POINT ( 'NONE',  ( 3.409779952838042583, -1.203371721269937744, -1.617806234278630573 ) ) ;
#75687=CARTESIAN_POINT ( 'NONE',  ( 6.727182134110196721, 6.033756510516266935, 2.783943001041962795 ) ) ;
#75688=CARTESIAN_POINT ( 'NONE',  ( 3.591891977137162684, -2.188917585555647527, -0.1077332384093188100 ) ) ;
#75690=CARTESIAN_POINT ( 'NONE',  ( 2.045805558669851365, 0.7393754583576680472, -1.779040955004469904 ) ) ;
#75692=CARTESIAN_POINT ( 'NONE',  ( 0.2333540202161427102, 1.346341334450983140, -2.298657068330804076 ) ) ;
#75698=CARTESIAN_POINT ( 'NONE',  ( 6.480030769895370746, -1.807141314969593848, -0.3518929191878711338 ) ) ;
#75699=CARTESIAN_POINT ( 'NONE',  ( 3.422524054001755633, -0.8179560535927836717, -1.839607883820688405 ) ) ;
#75700=CARTESIAN_POINT ( 'NONE',  ( 4.587492961451061113, 1.418373992658492400, -1.808456645134959073 ) ) ;
#75701=CARTESIAN_POINT ( 'NONE',  ( -0.1288028175206361037, 4.078893953557697571, -2.828657143142800034 ) ) ;
#75702=CARTESIAN_POINT ( 'NONE',  ( 3.361990069819278837, -1.859032935646281581, 0.08664877711485326206 ) ) ;
#75705=CARTESIAN_POINT ( 'NONE',  ( 6.433860211133586304, -1.853236450885078712, 0.4715264990977630077 ) ) ;
#75708=CARTESIAN_POINT ( 'NONE',  ( 5.565992953457829628, -1.325659382304938960, 1.616758296502271097 ) ) ;
#75714=CARTESIAN_POINT ( 'NONE',  ( 6.147054438156498435, -1.453121625630097613, 0.9290195162147057983 ) ) ;
#75716=CARTESIAN_POINT ( 'NONE',  ( 1.283399958720226497, 1.417952419849175305, -0.9979722560638002449 ) ) ;
#75719=CARTESIAN_POINT ( 'NONE',  ( 5.577072259002747501, 2.003115288890752410, 0.8377749483753393900 ) ) ;
#75720=CARTESIAN_POINT ( 'NONE',  ( 4.107882937833263526, -1.820653182827164596, 0.1363937739093170898 ) ) ;
#75721=CARTESIAN_POINT ( 'NONE',  ( 2.395295693335119935, -1.754585731169123752, 0.8775363634117984146 ) ) ;
#75726=CARTESIAN_POINT ( 'NONE',  ( 2.789816089392273213, 2.012775272720100705, -0.6673941125509493810 ) ) ;
#75731=CARTESIAN_POINT ( 'NONE',  ( 0.4267348894952603944, -1.354911996285239617, 1.565345633960464111 ) ) ;
#75734=CARTESIAN_POINT ( 'NONE',  ( 3.334858576441266376, 1.407893888572855801, -1.718160706149525430 ) ) ;
#75736=CARTESIAN_POINT ( 'NONE',  ( 0.7569315055401154568, 2.213468045025353881, -0.6199256774504552370 ) ) ;
#75738=CARTESIAN_POINT ( 'NONE',  ( 6.561391914609854936, 1.711577788671992062, 1.150682440272139617 ) ) ;
#75742=CARTESIAN_POINT ( 'NONE',  ( 6.567912610837368881, -1.126952994821692533, 1.456688911285822119 ) ) ;
#75744=CARTESIAN_POINT ( 'NONE',  ( -0.2104748580754183529, 0.2283854016844401591, -2.137091067173245929 ) ) ;
#75745=CARTESIAN_POINT ( 'NONE',  ( 2.836578922267366742, 0.2088710044844780678, 1.711989638784001677 ) ) ;
#75746=CARTESIAN_POINT ( 'NONE',  ( 1.042204282965590201, 0.8216761606248854655, 1.841732292558920570 ) ) ;
#75747=CARTESIAN_POINT ( 'NONE',  ( 2.444286548701213757, -2.001697433659669567, -1.129998469374261072 ) ) ;
#75749=CARTESIAN_POINT ( 'NONE',  ( 3.216390312923810502, -1.112095606969863759, -1.970117241612897363 ) ) ;
#75750=CARTESIAN_POINT ( 'NONE',  ( 5.233084072137057063, 0.1537158111805384808, 2.100522205955375199 ) ) ;
#75752=CARTESIAN_POINT ( 'NONE',  ( 3.549836697621409964, 1.769921775324476698, 0.002857994197370468913 ) ) ;
#75754=CARTESIAN_POINT ( 'NONE',  ( 6.427265082780700745, -1.493544900618107185, -1.739104490089713462 ) ) ;
#75755=CARTESIAN_POINT ( 'NONE',  ( 5.156134521940135329, -1.331146486249596306, 1.272188372451001026 ) ) ;
#75760=CARTESIAN_POINT ( 'NONE',  ( 4.171962795014371395, -1.262591954434747921, 1.790989659139609946 ) ) ;
#75764=CARTESIAN_POINT ( 'NONE',  ( 5.881320641815353412, -0.05461762546566179682, 2.069818975884097689 ) ) ;
#75765=CARTESIAN_POINT ( 'NONE',  ( -0.1003747550864658999, -1.976661868047492998, 0.3981153667176607902 ) ) ;
#75767=CARTESIAN_POINT ( 'NONE',  ( 3.563037003841040828, -1.699336121007990918, -0.9075540061579747686 ) ) ;
#75770=CARTESIAN_POINT ( 'NONE',  ( 6.416280414004661203, -2.120105685773795212, 0.05337830808049835035 ) ) ;
#75780=CARTESIAN_POINT ( 'NONE',  ( 1.363640982571033611, -0.4799814350611387725, 1.902108589862220311 ) ) ;
#75783=CARTESIAN_POINT ( 'NONE',  ( 5.846142468697441252, -0.8834969228576605715, 1.751761657833034613 ) ) ;
#75786=CARTESIAN_POINT ( 'NONE',  ( 6.420800710400103917, 2.015122584031241004, 0.7829223626853940576 ) ) ;
#75790=CARTESIAN_POINT ( 'NONE',  ( 0.2099203756031532975, -0.7936979409460078738, -1.692237190125941648 ) ) ;
#75791=CARTESIAN_POINT ( 'NONE',  ( 6.327464733921618567, -1.223274778582748246, 1.229020038707399065 ) ) ;
#75793=CARTESIAN_POINT ( 'NONE',  ( 2.806388347806953121, 1.585463108415147149, -1.513251884624075672 ) ) ;
#75794=CARTESIAN_POINT ( 'NONE',  ( 4.419161195688524835, 2.107920515157933661, 0.9393535314214102039 ) ) ;
#75795=CARTESIAN_POINT ( 'NONE',  ( 6.766874334510889710, -1.882258232876810045, -0.8394616043497000746 ) ) ;
#75796=CARTESIAN_POINT ( 'NONE',  ( 2.589705103518041618, -1.936761303218867969, -0.1426656448052856518 ) ) ;
#75799=CARTESIAN_POINT ( 'NONE',  ( 5.379186226027963258, -1.918017450862268714, -0.9047448674902383026 ) ) ;
#75800=CARTESIAN_POINT ( 'NONE',  ( 3.463517678199812266, -1.944071305346905643, -0.5350885120067662148 ) ) ;
#75809=CARTESIAN_POINT ( 'NONE',  ( 5.172756020173422620, -1.939746602593624081, -0.6965250322775017322 ) ) ;
#75814=CARTESIAN_POINT ( 'NONE',  ( 4.301429021398018193, 1.803172560858562701, -0.9099306128727399079 ) ) ;
#75820=CARTESIAN_POINT ( 'NONE',  ( 3.977457805978751093, 1.941116309567689324, -0.6927405623450531014 ) ) ;
#75821=CARTESIAN_POINT ( 'NONE',  ( 3.252577435111691617, 1.966644794889658820, -0.4445022851852917234 ) ) ;
#75829=CARTESIAN_POINT ( 'NONE',  ( 2.548203688163702463, 1.844428314090811538, -0.8144999995377337765 ) ) ;
#75830=CARTESIAN_POINT ( 'NONE',  ( 2.818100271072516261, 1.733748696238574416, 0.6199764264002775027 ) ) ;
#75831=CARTESIAN_POINT ( 'NONE',  ( 0.8917866929778429652, 2.032703844138737725, -1.092514170908296833 ) ) ;
#75833=CARTESIAN_POINT ( 'NONE',  ( 3.638091081701349871, 0.9754702174074175725, -1.929073278114090684 ) ) ;
#75835=CARTESIAN_POINT ( 'NONE',  ( 2.988014862494779322, 2.163403104293510459, 0.7763308700806015317 ) ) ;
#75838=CARTESIAN_POINT ( 'NONE',  ( 1.393192293617943944, 1.414286473764417185, 1.224485199485196629 ) ) ;
#75839=CARTESIAN_POINT ( 'NONE',  ( 6.069206959712960980, 0.1456670527590266107, -1.966150735595481258 ) ) ;
#75843=CARTESIAN_POINT ( 'NONE',  ( 1.067327838873022516, -1.996528553209110379, -0.9406146916221403975 ) ) ;
#75847=CARTESIAN_POINT ( 'NONE',  ( 6.639320575229257670, 3.688898292602959650, 2.617366112374151399 ) ) ;
#75848=CARTESIAN_POINT ( 'NONE',  ( 4.575049868665863606, 0.0009985144121069796600, -1.971640593447765655 ) ) ;
#75849=CARTESIAN_POINT ( 'NONE',  ( 5.760475268203285815, 0.9300522481428794563, 2.112166060234192511 ) ) ;
#75850=CARTESIAN_POINT ( 'NONE',  ( 5.512096448594467901, 1.858919848428818300, -0.09134777953435403719 ) ) ;
#75851=CARTESIAN_POINT ( 'NONE',  ( 3.555586659033848740, 1.623084692090390080, 1.272569074839409398 ) ) ;
#75857=CARTESIAN_POINT ( 'NONE',  ( 4.984931625306495029, 2.076298541577546342, 0.6347802954964998357 ) ) ;
#75859=CARTESIAN_POINT ( 'NONE',  ( 3.825598141381767903, 0.9817388958630569595, -1.557492293685861284 ) ) ;
#75863=CARTESIAN_POINT ( 'NONE',  ( 6.720655732516650716, 2.975630972093906923, 2.379814465338329743 ) ) ;
#75864=CARTESIAN_POINT ( 'NONE',  ( 6.163654587501778970, 1.125051486859941718, 1.880622087419632882 ) ) ;
#75866=CARTESIAN_POINT ( 'NONE',  ( 0.3337811221923889793, -2.067640401758659596, 0.9186946961548744239 ) ) ;
#75872=CARTESIAN_POINT ( 'NONE',  ( 0.9183970251232485005, 1.633131562045697649, 0.6825882272994202582 ) ) ;
#75873=CARTESIAN_POINT ( 'NONE',  ( 5.602202738069384402, -0.9032165795441854383, 1.799149290095316767 ) ) ;
#75875=CARTESIAN_POINT ( 'NONE',  ( 3.803828919190560764, -0.6134138247068477989, 2.014629399117270125 ) ) ;
#75876=CARTESIAN_POINT ( 'NONE',  ( 3.128438982650301625, 0.4684375082077455454, 1.857299403769121060 ) ) ;
#75877=CARTESIAN_POINT ( 'NONE',  ( -0.02244404828160087226, 1.323617703852699057, -2.440988974267483957 ) ) ;
#75878=CARTESIAN_POINT ( 'NONE',  ( 4.562928411757408043, 1.523777916087779571, -1.247912438812292413 ) ) ;
#75879=CARTESIAN_POINT ( 'NONE',  ( 5.625262229866254238, 1.783287769691415781, 0.9483128780355275511 ) ) ;
#75880=CARTESIAN_POINT ( 'NONE',  ( 3.098369316282158614, -0.5415621961667067552, -1.790553177708480215 ) ) ;
#75881=CARTESIAN_POINT ( 'NONE',  ( 5.531808922564334097, -1.099089406413750414, -1.329375763670269883 ) ) ;
#75882=CARTESIAN_POINT ( 'NONE',  ( 0.8965662283535699162, -1.866366896104875162, -0.4163465257057268332 ) ) ;
#75884=CARTESIAN_POINT ( 'NONE',  ( 1.875870136999336246, 2.111227540014638304, -0.6426800678154330759 ) ) ;
#75887=CARTESIAN_POINT ( 'NONE',  ( 6.830524215763060347, -1.208013408316032322, 1.546442907991877558 ) ) ;
#75896=CARTESIAN_POINT ( 'NONE',  ( 1.891162872569674080, 0.2007839719405465906, 2.060584128686280714 ) ) ;
#75901=CARTESIAN_POINT ( 'NONE',  ( 6.252600707356171128, 2.097339953035493476, 0.3115551810550786227 ) ) ;
#75906=CARTESIAN_POINT ( 'NONE',  ( 5.360703810585087048, -0.7282664037663032497, 1.880147357087233129 ) ) ;
#75907=CARTESIAN_POINT ( 'NONE',  ( 4.592943030449060160, 1.669885041223855060, 0.9386680909919845606 ) ) ;
#75909=CARTESIAN_POINT ( 'NONE',  ( 2.929422067023911502, -1.473737196803912797, -1.622193633833472814 ) ) ;
#75912=CARTESIAN_POINT ( 'NONE',  ( 5.115494517658178530, 1.648350763777502559, 1.155591226287083328 ) ) ;
#75913=CARTESIAN_POINT ( 'NONE',  ( 1.757924209179074770, 0.7287868685415777037, -1.768279316124596656 ) ) ;
#75916=CARTESIAN_POINT ( 'NONE',  ( 0.2632962822839111650, 1.880428227362867633, -0.7283992291491693249 ) ) ;
#75918=CARTESIAN_POINT ( 'NONE',  ( 3.228152448572230160, 2.040302950407224536, 0.4557642060307572907 ) ) ;
#75920=CARTESIAN_POINT ( 'NONE',  ( 1.817014216480263622, -0.2154200610367338342, 1.711195096342375210 ) ) ;
#75922=CARTESIAN_POINT ( 'NONE',  ( 6.451439665316073935, -1.893653415279672902, 0.9546920624979161607 ) ) ;
#75928=ORIENTED_EDGE ( 'NONE', *, *, #95054, .T. ) ;
#75931=CARTESIAN_POINT ( 'NONE',  ( 3.246531836744088295, 1.767876921188500150, 0.3942315000180166562 ) ) ;
#75935=CARTESIAN_POINT ( 'NONE',  ( 3.510248027248025426, -1.809562450863181127, -0.08562717191654131699 ) ) ;
#75940=CARTESIAN_POINT ( 'NONE',  ( 4.281604344665800532, -1.781275985052663158, 0.5390932415961935398 ) ) ;
#75941=CARTESIAN_POINT ( 'NONE',  ( 1.968237613432867184, -1.879027187823999245, -0.3716057669084034676 ) ) ;
#75942=CARTESIAN_POINT ( 'NONE',  ( 1.113953379265147925, -0.8168401028521531382, -1.632710947565917170 ) ) ;
#75950=CARTESIAN_POINT ( 'NONE',  ( 5.207841159657320418, 0.6216970817616838119, -1.868779976745947202 ) ) ;
#75953=CARTESIAN_POINT ( 'NONE',  ( 0.2168896333464042925, -0.1002974801882359490, 2.088354908755992945 ) ) ;
#75955=CARTESIAN_POINT ( 'NONE',  ( 5.174797004712035076, -1.813887718507047220, -0.6490126392820031453 ) ) ;
#75957=CARTESIAN_POINT ( 'NONE',  ( 1.834698128333624112, 0.1755570873784827179, 1.817110820650599923 ) ) ;
#75958=CARTESIAN_POINT ( 'NONE',  ( 2.069229996397306426, -2.018448871333050842, -0.8927042923378907258 ) ) ;
#75960=CARTESIAN_POINT ( 'NONE',  ( 0.8262462788446511830, -0.8622288892402606431, -1.707089296137359158 ) ) ;
#75962=CARTESIAN_POINT ( 'NONE',  ( 6.912958093653829295, -1.524444945649571004, 1.246696689375533795 ) ) ;
#75963=CARTESIAN_POINT ( 'NONE',  ( 2.155715342533376155, 0.8324662149039625536, 1.754741561904197056 ) ) ;
#75965=CARTESIAN_POINT ( 'NONE',  ( 0.6146109705059289441, 0.6351056948852469297, -1.913509406280079705 ) ) ;
#75967=CARTESIAN_POINT ( 'NONE',  ( 0.1857038103042158439, -1.139949723551544114, -1.471474936012186596 ) ) ;
#75973=CARTESIAN_POINT ( 'NONE',  ( 2.437293137456029157, -1.626093413141915134, -1.469474007205706645 ) ) ;
#75977=CARTESIAN_POINT ( 'NONE',  ( 2.982817717652554101, -0.1347461720548545627, -1.820777111243766733 ) ) ;
#75983=CARTESIAN_POINT ( 'NONE',  ( 0.5922524703982982031, -1.911778602531236215, -0.2371815352125578036 ) ) ;
#75984=CARTESIAN_POINT ( 'NONE',  ( 5.366048076001885825, -1.952644961629325548, 0.1885061251027941032 ) ) ;
#75989=CARTESIAN_POINT ( 'NONE',  ( 4.880524338131243312, -0.2681524694418158661, -2.175044001020635331 ) ) ;
#75991=CARTESIAN_POINT ( 'NONE',  ( 4.416890754593222113, -1.537527071031305814, 1.386575359339572655 ) ) ;
#75995=CARTESIAN_POINT ( 'NONE',  ( 4.641406123262603600, 0.8788069589312655916, 2.124244668743579201 ) ) ;
#75999=CARTESIAN_POINT ( 'NONE',  ( 0.3402841477759439570, 2.286568017602428338, 0.1625022809590911665 ) ) ;
#76000=CARTESIAN_POINT ( 'NONE',  ( 6.620655732516632419, 1.270823175217004941, 2.040803978124502205 ) ) ;
#76002=CARTESIAN_POINT ( 'NONE',  ( 5.015543440151827959, -1.040391601716946557, -1.639569664018299289 ) ) ;
#76007=CARTESIAN_POINT ( 'NONE',  ( 4.658414424252744546, 1.907665749568526747, 0.1350064596054162680 ) ) ;
#76008=CARTESIAN_POINT ( 'NONE',  ( 6.088827306860007837, -0.2580713809433569650, -1.705207211698676062 ) ) ;
#76009=CARTESIAN_POINT ( 'NONE',  ( 5.243375144629232487, 0.3886363430659240392, -1.978554426619572926 ) ) ;
#76013=CARTESIAN_POINT ( 'NONE',  ( 1.500065138910465334, -0.7538795759346494929, -1.950162888426725250 ) ) ;
#76014=CARTESIAN_POINT ( 'NONE',  ( 6.766889846978989986, -1.619426471845460069, -0.7142080874563813131 ) ) ;
#76015=CARTESIAN_POINT ( 'NONE',  ( 5.344375030997434273, 0.3906003880304632636, -1.978050218768567792 ) ) ;
#76017=CARTESIAN_POINT ( 'NONE',  ( 2.888958383575964017, 1.965592292480751402, -1.179159595035377261 ) ) ;
#76018=CARTESIAN_POINT ( 'NONE',  ( 1.903882329689795094, 1.290680248512179551, -1.167607185883823728 ) ) ;
#76021=CARTESIAN_POINT ( 'NONE',  ( 2.635775109972549490, 0.08874582706053059378, -1.731711113058966633 ) ) ;
#76023=CARTESIAN_POINT ( 'NONE',  ( 1.627181624537884286, 0.1412763417478210271, -1.855766238205541097 ) ) ;
#76024=CARTESIAN_POINT ( 'NONE',  ( 2.805323142837768291, -1.806386208845015995, 1.204286856753070456 ) ) ;
#76025=CARTESIAN_POINT ( 'NONE',  ( 3.520720487665735643, 0.3006478860226591276, 1.993893439002386581 ) ) ;
#76026=CARTESIAN_POINT ( 'NONE',  ( 4.750000000000003553, 2.703060497845378561E-13, 2.052068128417943171 ) ) ;
#76028=CARTESIAN_POINT ( 'NONE',  ( 6.375613808387889492, 1.842787572768100457, -0.5617375553943514399 ) ) ;
#76030=CARTESIAN_POINT ( 'NONE',  ( 3.023905552101690208, -0.4295200811062405699, 2.179336035515607950 ) ) ;
#76032=CARTESIAN_POINT ( 'NONE',  ( -0.2110808730066962846, 5.724502961415374180, -2.391230805320884834 ) ) ;
#76037=CARTESIAN_POINT ( 'NONE',  ( 6.433822955411669930, -2.155103329387221933, 0.5382066023030105395 ) ) ;
#76038=CARTESIAN_POINT ( 'NONE',  ( 4.334394203492665909, -1.131343785558375226, 1.602600411086833931 ) ) ;
#76043=CARTESIAN_POINT ( 'NONE',  ( 6.221994747346401233, -1.249160343739505352, -1.886125069868335613 ) ) ;
#76044=CARTESIAN_POINT ( 'NONE',  ( 2.330602656244503468, -1.270745551583628785, 1.624662076113972065 ) ) ;
#76049=CARTESIAN_POINT ( 'NONE',  ( 3.796049943699483453, -1.868292110373217518, -0.09463876624429126694 ) ) ;
#76050=CARTESIAN_POINT ( 'NONE',  ( 2.461176475124981611, -1.659910965455011267, -0.5019686038148748475 ) ) ;
#76051=CARTESIAN_POINT ( 'NONE',  ( 0.1172542576415449567, -0.1040641125494116137, 2.290134469065004730 ) ) ;
#76052=CARTESIAN_POINT ( 'NONE',  ( 1.536444635327537833, 1.086998388645914027, -1.920427013416255768 ) ) ;
#76053=CARTESIAN_POINT ( 'NONE',  ( 5.384693163835662766, 1.711646917711911353, -0.9173020705802971131 ) ) ;
#76057=CARTESIAN_POINT ( 'NONE',  ( 0.3521856818783953846, 0.1948384997633167970, -2.006960225185448810 ) ) ;
#76058=CARTESIAN_POINT ( 'NONE',  ( -0.03470293633787284449, -1.699275230904277789, 1.268407768021381221 ) ) ;
#76060=CARTESIAN_POINT ( 'NONE',  ( 6.469375277500488686, -1.978045142091336306, -0.3906011616893814709 ) ) ;
#76064=CARTESIAN_POINT ( 'NONE',  ( 4.318856058802469811, 1.670182456744148336, 0.7377305746401884301 ) ) ;
#76065=CARTESIAN_POINT ( 'NONE',  ( 2.309865001130634976, -0.4838574416936823885, 2.152911442350906146 ) ) ;
#76070=CARTESIAN_POINT ( 'NONE',  ( 1.459246395511590189, -1.704040126542965661, 1.084046338683493982 ) ) ;
#76074=CARTESIAN_POINT ( 'NONE',  ( 2.518200207203071805, 0.7905618127436510045, 1.684796146788158699 ) ) ;
#76080=CARTESIAN_POINT ( 'NONE',  ( 4.353998665852670591, 1.825246345946249571, -0.04724550102237072557 ) ) ;
#76084=CARTESIAN_POINT ( 'NONE',  ( 6.696638777208028692, -1.314797947003863543, -1.528504179509587280 ) ) ;
#76085=CARTESIAN_POINT ( 'NONE',  ( 6.246043375366982175, 0.5822610321466625827, 1.746719530172704538 ) ) ;
#76086=CARTESIAN_POINT ( 'NONE',  ( 4.319161277787673114, 2.108828969982502688, 0.9375607936791326980 ) ) ;
#76088=CARTESIAN_POINT ( 'NONE',  ( 0.2103215893997134323, -0.8792329509940269849, -1.862182962916396844 ) ) ;
#76090=CARTESIAN_POINT ( 'NONE',  ( 1.997508135846944421, -1.941589802808607157, 0.04981292379131925518 ) ) ;
#76091=CARTESIAN_POINT ( 'NONE',  ( 5.308124166105086417, -1.975000179191854111, 1.175378216249231222 ) ) ;
#76094=CARTESIAN_POINT ( 'NONE',  ( 5.102362337376947998, -0.6309395149336484154, -1.761181640970375106 ) ) ;
#76096=CARTESIAN_POINT ( 'NONE',  ( 2.636851627972558454, 1.802111047976437508, 0.6404684511054498097 ) ) ;
#76098=CARTESIAN_POINT ( 'NONE',  ( 3.405080638938757343, 1.739790774466195789, -1.357627211771177178 ) ) ;
#76103=CARTESIAN_POINT ( 'NONE',  ( 1.598833994113032730, 1.614015922016404536, -1.131664812120122487 ) ) ;
#76104=CARTESIAN_POINT ( 'NONE',  ( 2.011159220144568938, 1.709348158914993254, -1.550378056569144958 ) ) ;
#76105=CARTESIAN_POINT ( 'NONE',  ( 2.629291921057617554, 0.09916324773191761976, -1.959495597191794225 ) ) ;
#76107=CARTESIAN_POINT ( 'NONE',  ( 6.455934469078565385, -0.7002696157344409089, 1.940163012464599879 ) ) ;
#76109=CARTESIAN_POINT ( 'NONE',  ( 3.942592416894859841, -1.490970858180175940, 1.357867534901323614 ) ) ;
#76112=CARTESIAN_POINT ( 'NONE',  ( 4.505092375653735992, -0.09411930587044713137, 2.014432893821124004 ) ) ;
#76117=CARTESIAN_POINT ( 'NONE',  ( 2.395604216770229833, -1.940863096919882569, 0.9729980962204368700 ) ) ;
#76122=CARTESIAN_POINT ( 'NONE',  ( 2.583089905966722277, 1.711919019956799737, -0.7542334906679578621 ) ) ;
#76123=CARTESIAN_POINT ( 'NONE',  ( 0.1927530690809010350, -0.4471281949963988867, -2.018758496260419921 ) ) ;
#76124=CARTESIAN_POINT ( 'NONE',  ( 0.07775346131142636674, 2.855377671833533970, -2.776861204146412021 ) ) ;
#76127=FACE_OUTER_BOUND ( 'NONE', #10898, .T. ) ;
#76128=CARTESIAN_POINT ( 'NONE',  ( 3.738835060935014276, 1.816739721148411757, 0.5971339541979634458 ) ) ;
#76130=CARTESIAN_POINT ( 'NONE',  ( 4.434285456697817374, 1.735847377751572385, 0.3442416992474469084 ) ) ;
#76131=CARTESIAN_POINT ( 'NONE',  ( 1.963391044528959295, -1.536740334223782867, -1.137898036029337812 ) ) ;
#76134=CARTESIAN_POINT ( 'NONE',  ( 0.1455191377820958532, 1.894478286654190269, -0.2837363430458189062 ) ) ;
#76136=CARTESIAN_POINT ( 'NONE',  ( 1.381394743813993964, -0.05274132383669553892, 2.069866178704109938 ) ) ;
#76138=CARTESIAN_POINT ( 'NONE',  ( 6.297708355432167338, -0.6282832542035889922, 1.762108908958268216 ) ) ;
#76139=CARTESIAN_POINT ( 'NONE',  ( 2.156629195875509719, -1.411784796728832392, 1.157573153174975111 ) ) ;
#76140=CARTESIAN_POINT ( 'NONE',  ( 5.619807753665406302, -2.153844256707802440, 0.4802137346974973409 ) ) ;
#76143=CARTESIAN_POINT ( 'NONE',  ( 2.559094272886554666, 1.658201776010211459, -1.226620081234103266 ) ) ;
#76150=CARTESIAN_POINT ( 'NONE',  ( 4.949704645232674061, 1.531818663031824013, 1.392983054852282132 ) ) ;
#76152=CARTESIAN_POINT ( 'NONE',  ( 2.425270691926323607, -0.002641788883844810656, 2.161773191836775521 ) ) ;
#76154=CARTESIAN_POINT ( 'NONE',  ( 2.666670786633594137, 0.6826474749901580985, 1.900933108274209360 ) ) ;
#76155=CARTESIAN_POINT ( 'NONE',  ( 6.620655732516615544, 0.0004550665019913135447, 2.073887158236031425 ) ) ;
#76160=CARTESIAN_POINT ( 'NONE',  ( 1.253139057289072822, 0.1435168058863903473, -2.011451928166609893 ) ) ;
#76162=CARTESIAN_POINT ( 'NONE',  ( 6.198795224570643470, 1.821041368708445907, 1.219022265761634971 ) ) ;
#76164=CARTESIAN_POINT ( 'NONE',  ( 4.658414424252744546, 1.907665749568526747, 0.1350064596054162680 ) ) ;
#76168=CARTESIAN_POINT ( 'NONE',  ( 3.743767684670766371, 2.000855813463810140, -0.2496267151909299931 ) ) ;
#76170=CARTESIAN_POINT ( 'NONE',  ( 5.227475398614537916, -1.636741361296644603, 0.5442337529403593610 ) ) ;
#76174=CARTESIAN_POINT ( 'NONE',  ( 4.094877388769967652, 1.581529129216452612, -0.9985332613470513374 ) ) ;
#76175=CARTESIAN_POINT ( 'NONE',  ( 0.07536363704235481131, 0.6997989235110781969, -2.226667633679416447 ) ) ;
#76176=CARTESIAN_POINT ( 'NONE',  ( 1.094682738308445202, 2.038987083759949304, 0.3576228084290478115 ) ) ;
#76179=CARTESIAN_POINT ( 'NONE',  ( 6.604213110542080045, -0.7679849629102013520, 1.639316308541746592 ) ) ;
#76182=CARTESIAN_POINT ( 'NONE',  ( 0.7733460811225587594, 0.3524055278083237930, -1.776778109436588204 ) ) ;
#76188=CARTESIAN_POINT ( 'NONE',  ( 0.3616705494772323726, -0.5269360983083425376, 1.889693748445469224 ) ) ;
#76190=CARTESIAN_POINT ( 'NONE',  ( 4.657778235022878022, 1.106396155499450140, 1.563574394034000115 ) ) ;
#76196=CARTESIAN_POINT ( 'NONE',  ( 2.290102563249151402, -0.9248296759884739870, 1.954025333243500695 ) ) ;
#76199=CARTESIAN_POINT ( 'NONE',  ( 0.03560581989598374242, -0.09759080014098624190, 2.118463022953632091 ) ) ;
#76200=CARTESIAN_POINT ( 'NONE',  ( 4.436427218767265757, 1.790408935156896586, 0.3557191534368231434 ) ) ;
#76202=CARTESIAN_POINT ( 'NONE',  ( 1.475783946021753446, 1.170879755915053666, 1.585848323755238320 ) ) ;
#76203=CARTESIAN_POINT ( 'NONE',  ( 3.357576282340120066, -1.451192137084562628, -1.245647637661301044 ) ) ;
#76206=CARTESIAN_POINT ( 'NONE',  ( 4.334397697284593676, -1.135867708366841367, 1.608802569665278348 ) ) ;
#76208=CARTESIAN_POINT ( 'NONE',  ( 5.794467663293456638, 1.585267558806532362, -1.121583357746269050 ) ) ;
#76212=CARTESIAN_POINT ( 'NONE',  ( 6.275647701495586261, 0.3610785225884837746, -2.089460823871174266 ) ) ;
#76214=CARTESIAN_POINT ( 'NONE',  ( 4.178302048780179412, 0.9043031410675538284, 1.684961085834511874 ) ) ;
#76217=CARTESIAN_POINT ( 'NONE',  ( 0.2709337360254741034, -1.439471777561899035, 1.672717458380864608 ) ) ;
#76219=CARTESIAN_POINT ( 'NONE',  ( 5.391275966583902957, -0.05175381893108904618, -2.012593086484148142 ) ) ;
#76221=CARTESIAN_POINT ( 'NONE',  ( 5.725187622324654946, -0.04035785615889506128, 1.825416780793003069 ) ) ;
#76222=CARTESIAN_POINT ( 'NONE',  ( 1.627480586986803868, 0.1543294891723171747, -2.064685722993148342 ) ) ;
#76226=CARTESIAN_POINT ( 'NONE',  ( 6.350466393003619814, 0.5888352225367661230, 1.775644890098279749 ) ) ;
#76238=CARTESIAN_POINT ( 'NONE',  ( 5.203642376314169482, 1.605325691485876671, 0.6564576239363513199 ) ) ;
#76240=CARTESIAN_POINT ( 'NONE',  ( 2.571216573722459486, 1.847313327574741315, 0.9347662400437593000 ) ) ;
#76241=CARTESIAN_POINT ( 'NONE',  ( 3.005573934588702034, -2.039760842771252136, 0.5671949335201897924 ) ) ;
#76244=CARTESIAN_POINT ( 'NONE',  ( 1.692182146996668912, 0.9751594699732427651, -1.711024247558447842 ) ) ;
#76248=CARTESIAN_POINT ( 'NONE',  ( -0.05268457437105152075, -1.747710896673961622, 0.7768168958157274373 ) ) ;
#76249=CARTESIAN_POINT ( 'NONE',  ( 3.996227152750064349, -0.7175114184741685497, -2.177131142417339849 ) ) ;
#76250=CARTESIAN_POINT ( 'NONE',  ( 0.3635304476994546952, 1.806310985241452949, -0.2645042207462811046 ) ) ;
#76255=CARTESIAN_POINT ( 'NONE',  ( 1.353772324478102584, -1.461116690358499337, -1.385217879419877951 ) ) ;
#76256=CARTESIAN_POINT ( 'NONE',  ( 2.694135368495911731, 0.9291169126603683326, -1.727816930623335967 ) ) ;
#76260=CARTESIAN_POINT ( 'NONE',  ( 5.085920031106448747, -2.074780370831377230, -0.2563659892118006489 ) ) ;
#76261=CARTESIAN_POINT ( 'NONE',  ( 3.871743310845751296, 0.9831255770079703193, 1.471438590500689925 ) ) ;
#76263=CARTESIAN_POINT ( 'NONE',  ( 6.492113699461491194, -0.6046859696737926226, -2.211003196133090931 ) ) ;
#76264=CARTESIAN_POINT ( 'NONE',  ( 5.806559702419027857, 1.537982464610265332, 0.8144831216923865691 ) ) ;
#76266=CARTESIAN_POINT ( 'NONE',  ( 6.328761054056312396, 0.8840516187795799397, -2.122072247225449626 ) ) ;
#76268=CARTESIAN_POINT ( 'NONE',  ( 5.026542006541363961, 1.714758565716298477, -0.2553409819617598053 ) ) ;
#76270=CARTESIAN_POINT ( 'NONE',  ( 6.215302479579098538, -1.858902078722439732, -1.121643639950772764 ) ) ;
#76272=CARTESIAN_POINT ( 'NONE',  ( 0.005274918996244109745, -0.09700444455036473512, 2.115223206416060098 ) ) ;
#76273=CARTESIAN_POINT ( 'NONE',  ( 4.812500000000003553, 1.451031289061308183, 1.451031289060921159 ) ) ;
#76275=CARTESIAN_POINT ( 'NONE',  ( 3.838824069632059910, 0.2817418319709265040, 1.905555271966542952 ) ) ;
#76277=CARTESIAN_POINT ( 'NONE',  ( -0.09271296656673803926, -0.4979868145295326953, -2.173146351408902888 ) ) ;
#76282=CARTESIAN_POINT ( 'NONE',  ( 2.877807283724475251, 0.3237236903097116536, -2.197462771414046223 ) ) ;
#76287=CARTESIAN_POINT ( 'NONE',  ( 1.248672897702383988, 1.986100274556975354, -0.3474695496914689818 ) ) ;
#76289=CARTESIAN_POINT ( 'NONE',  ( 5.969198602517502117, 1.817331191306554850, 0.9757160385870704555 ) ) ;
#76295=CARTESIAN_POINT ( 'NONE',  ( 0.1804953903597758258, -0.1286114524143982807, -1.740565225867502397 ) ) ;
#76296=CARTESIAN_POINT ( 'NONE',  ( 5.977189187444425400, -1.726741413813812631, -0.1601111783383553921 ) ) ;
#76297=CARTESIAN_POINT ( 'NONE',  ( 5.847135585344571673, 0.4968686550196474982, -1.668027988745724777 ) ) ;
#76298=CARTESIAN_POINT ( 'NONE',  ( 2.771321709476880280, 2.175846111983824382, -0.7217205603756542409 ) ) ;
#76300=CARTESIAN_POINT ( 'NONE',  ( 2.361056629804247020, 1.805642548105116596, -0.3588866333120652174 ) ) ;
#76304=CARTESIAN_POINT ( 'NONE',  ( 2.660947563312371589, -1.587261545009664765, -0.9017329732442300738 ) ) ;
#76305=CARTESIAN_POINT ( 'NONE',  ( 3.393204081532863459, -0.8197727808607684352, -1.842447475547980495 ) ) ;
#76308=CARTESIAN_POINT ( 'NONE',  ( 5.579168075997259280, -0.04836659121091852614, -2.105573489274599197 ) ) ;
#76310=CARTESIAN_POINT ( 'NONE',  ( 2.295452831283749440, -1.850383948470477602, 0.9288054807428181014 ) ) ;
#76313=CARTESIAN_POINT ( 'NONE',  ( 4.828832153679845973, 1.461785933843419150, -1.536352341152541046 ) ) ;
#76315=CARTESIAN_POINT ( 'NONE',  ( 0.4164666496747080338, 1.329428171303851824, -1.394508830869565230 ) ) ;
#76323=CARTESIAN_POINT ( 'NONE',  ( 6.345950370838200350, -1.386202306585911925, -1.604841549997563455 ) ) ;
#76324=CARTESIAN_POINT ( 'NONE',  ( 2.309725134170067307, -0.4624151122551781179, 2.054391039957529586 ) ) ;
#76327=CARTESIAN_POINT ( 'NONE',  ( 6.772303520102497920, -0.8766781706108403016, -1.641457522745570996 ) ) ;
#76332=CARTESIAN_POINT ( 'NONE',  ( -0.1401555495076401980, -1.643345231473653190, -1.339971704266910812 ) ) ;
#76335=CARTESIAN_POINT ( 'NONE',  ( 1.961309178647975715, 1.629323162926434199, 1.092499269706406428 ) ) ;
#76336=CARTESIAN_POINT ( 'NONE',  ( 1.551884642779034262, 0.6273040060550126862, -2.068667048528524344 ) ) ;
#76340=CARTESIAN_POINT ( 'NONE',  ( 2.730071887686904564, 0.2129287318765031578, 1.727178079207219552 ) ) ;
#76343=CARTESIAN_POINT ( 'NONE',  ( 2.389999771189327937, -0.002812746694069029330, 2.016288306988550438 ) ) ;
#76347=CARTESIAN_POINT ( 'NONE',  ( 1.797671122125501952, -0.6659361598389621495, 1.855707729256075522 ) ) ;
#76348=CARTESIAN_POINT ( 'NONE',  ( 5.801015586618943232, -0.2871438832755985326, -1.890612906794430614 ) ) ;
#76353=CARTESIAN_POINT ( 'NONE',  ( 1.559246255342447984, -1.705015668849844124, 1.082290385971399926 ) ) ;
#76355=CARTESIAN_POINT ( 'NONE',  ( 6.229535257468108433, -2.175718461381468405, 0.7693011637898824473 ) ) ;
#76356=CARTESIAN_POINT ( 'NONE',  ( 5.389097038490845648, 0.1425914310585977562, 1.956722230749983193 ) ) ;
#76357=CARTESIAN_POINT ( 'NONE',  ( 3.168751141962049545, 1.424179589570490512, -1.349414796185027576 ) ) ;
#76359=CARTESIAN_POINT ( 'NONE',  ( 0.7564826839323666174, 1.942540863013635821, -0.5404934282097761944 ) ) ;
#76361=CARTESIAN_POINT ( 'NONE',  ( 1.569685796324036264, 1.464237652897076414, 1.529633472619792656 ) ) ;
#76364=CARTESIAN_POINT ( 'NONE',  ( 1.587592257565925813, -1.832131100469553520, -0.1817911664281982032 ) ) ;
#76367=CARTESIAN_POINT ( 'NONE',  ( 2.672263739372262137, 2.109986773948614225, -0.2121620573234672125 ) ) ;
#76371=CARTESIAN_POINT ( 'NONE',  ( 2.741540247014317533, -1.524689737823584190, -1.386575092742351245 ) ) ;
#76373=CARTESIAN_POINT ( 'NONE',  ( 1.716098596715152746, 1.718394358364897068, 0.6617865747741287219 ) ) ;
#76378=CARTESIAN_POINT ( 'NONE',  ( 0.8564375766340023288, 2.204168734417511821, -0.1118928034387969561 ) ) ;
#76379=CARTESIAN_POINT ( 'NONE',  ( 3.198750403210961490, -0.6533003841502099673, -2.166054703861711506 ) ) ;
#76381=CARTESIAN_POINT ( 'NONE',  ( 2.056637812947777810, 0.3998733141725440698, 1.766706770180977548 ) ) ;
#76382=CARTESIAN_POINT ( 'NONE',  ( 3.397576204589338733, -1.886455135561039942, 0.3326623127566808447 ) ) ;
#76383=CARTESIAN_POINT ( 'NONE',  ( 4.791501694037465953, -1.894250426384593844, 0.8359921707915063394 ) ) ;
#76386=CARTESIAN_POINT ( 'NONE',  ( 2.782053229633123959, -1.014971971657689709, 1.689997848710776740 ) ) ;
#76387=CARTESIAN_POINT ( 'NONE',  ( 6.692047312239829182, -0.8199282357786542574, 1.741332009981966022 ) ) ;
#76388=CARTESIAN_POINT ( 'NONE',  ( 3.889402362484274622, 1.354500474538382626, 1.290456140434749654 ) ) ;
#76389=CARTESIAN_POINT ( 'NONE',  ( 2.543975960257907953, -1.711040505396358657, -1.548661362299937228 ) ) ;
#76391=CARTESIAN_POINT ( 'NONE',  ( 3.297144150320669542, -1.642529969829407577, 0.8749454559845524226 ) ) ;
#76396=CARTESIAN_POINT ( 'NONE',  ( 0.2761803097106649840, 1.214566955493846967, 1.720366990225271842 ) ) ;
#76398=CARTESIAN_POINT ( 'NONE',  ( 6.028642311625867833, 2.081422104948245533, 0.5829617784755269927 ) ) ;
#76399=CARTESIAN_POINT ( 'NONE',  ( 0.1408863878445747453, 1.934039905153326799, 0.5823465565887532280 ) ) ;
#76406=CARTESIAN_POINT ( 'NONE',  ( 4.557827498477605488, 1.164984774316142113, 1.645760986912048640 ) ) ;
#76409=CARTESIAN_POINT ( 'NONE',  ( 6.508665849870632236, 1.605377118863276387, -1.447859449074364591 ) ) ;
#76413=CARTESIAN_POINT ( 'NONE',  ( -0.0005723727212556676321, -1.878494010790388913, 0.3742560964640674892 ) ) ;
#76418=CARTESIAN_POINT ( 'NONE',  ( 1.734533752015484875, 0.1665512568347452815, 1.716820151450085596 ) ) ;
#76422=CARTESIAN_POINT ( 'NONE',  ( 0.6316679966703161453, 0.9168908782757211329, -1.513568585016269452 ) ) ;
#76424=CARTESIAN_POINT ( 'NONE',  ( 4.996905641018499544, 0.3326216897534995387, 1.940969171785451364 ) ) ;
#76425=CARTESIAN_POINT ( 'NONE',  ( 2.438141639825658125, -1.160823251276057011, -1.644512180470799834 ) ) ;
#76427=CARTESIAN_POINT ( 'NONE',  ( 3.979664642534729513, 2.078844338038158934, -0.7408291028327750327 ) ) ;
#76429=CARTESIAN_POINT ( 'NONE',  ( 5.383699271828307431, -2.063871618437407740, 0.6740922461795120224 ) ) ;
#76430=ORIENTED_EDGE ( 'NONE', *, *, #9755, .F. ) ;
#76434=CARTESIAN_POINT ( 'NONE',  ( 2.895306150831237879, -0.1582170333116576511, -2.114654843180157950 ) ) ;
#76435=CARTESIAN_POINT ( 'NONE',  ( 3.128529964930274687, 0.4926631579876328271, 1.955168413974051056 ) ) ;
#76436=CARTESIAN_POINT ( 'NONE',  ( 3.902463391467089426, -1.792703881930355347, -0.2598333579746092692 ) ) ;
#76441=CARTESIAN_POINT ( 'NONE',  ( 0.5845639792326964290, -0.2246964894469481722, -1.857040431621145959 ) ) ;
#76443=CARTESIAN_POINT ( 'NONE',  ( 5.672426548614882158, -1.154804106291613675, 1.414059844683832834 ) ) ;
#76444=CARTESIAN_POINT ( 'NONE',  ( 1.463933648137748733, -1.021544554152100437, 1.620407321708102533 ) ) ;
#76452=CARTESIAN_POINT ( 'NONE',  ( 3.287459871768631636, 0.04819156399121089784, -2.120204644799832394 ) ) ;
#76455=CARTESIAN_POINT ( 'NONE',  ( 4.885985806860754010, -0.9320292603649924512, 1.737142539612034353 ) ) ;
#76456=CARTESIAN_POINT ( 'NONE',  ( 6.293217207623316156, -0.1008467329366956045, -1.909883259500498198 ) ) ;
#76458=CARTESIAN_POINT ( 'NONE',  ( 0.08772780073029294579, -0.5597381814076306528, 2.041856491864118439 ) ) ;
#76460=CARTESIAN_POINT ( 'NONE',  ( 1.082579992370054311, 1.234693400583252609, -1.661741702728709802 ) ) ;
#76461=CARTESIAN_POINT ( 'NONE',  ( 2.642442020880403586, -1.614326438788242557, 1.079121087018119152 ) ) ;
#76464=CARTESIAN_POINT ( 'NONE',  ( 3.750014218873336969, 0.7526759941024010470, 1.950626372838085265 ) ) ;
#76467=CARTESIAN_POINT ( 'NONE',  ( 0.4338566731940462495, -0.9675643781421030543, -1.531218756180543927 ) ) ;
#76469=CARTESIAN_POINT ( 'NONE',  ( 5.531908139154323223, -1.397534428995873546, -1.707979418440738195 ) ) ;
#76471=CARTESIAN_POINT ( 'NONE',  ( 3.083271082906696048, -0.1608111237268796401, -2.200959079826501075 ) ) ;
#76473=CARTESIAN_POINT ( 'NONE',  ( 2.262237773093742188, 1.911903731097279513, 0.04523801603947830152 ) ) ;
#76475=CARTESIAN_POINT ( 'NONE',  ( 5.687960312649480876, -1.310561514506687564, -1.602779375087557190 ) ) ;
#76477=CARTESIAN_POINT ( 'NONE',  ( 2.518638242371186386, 1.412657066830936392, -1.636333507658905173 ) ) ;
#76478=CARTESIAN_POINT ( 'NONE',  ( 4.265290774032561849, 2.125562838249666964, -0.5332280334861272397 ) ) ;
#76488=CARTESIAN_POINT ( 'NONE',  ( 5.700075226665620498, 0.8442301939139056355, -1.890501578402821847 ) ) ;
#76489=CARTESIAN_POINT ( 'NONE',  ( 3.914609504329464418, 1.361597497701543480, -1.363134563274936761 ) ) ;
#76490=CARTESIAN_POINT ( 'NONE',  ( 0.4390776481996219727, -1.704952938511293814, -1.076296438737800454 ) ) ;
#76494=CARTESIAN_POINT ( 'NONE',  ( 4.944182365274345514, -0.9318649803399962073, 1.735062577953277563 ) ) ;
#76495=CARTESIAN_POINT ( 'NONE',  ( 0.1643758432304382178, -1.428106194732338352, 1.662303017507735792 ) ) ;
#76496=CARTESIAN_POINT ( 'NONE',  ( 5.004447790439923160, -0.6182884515001166870, -1.717943145347331280 ) ) ;
#76503=CARTESIAN_POINT ( 'NONE',  ( 2.876309626556411203, -0.1380247437976732383, -1.836149222064882514 ) ) ;
#76504=CARTESIAN_POINT ( 'NONE',  ( 5.906499476128409754, -2.003886227978883383, -0.1931989457738275962 ) ) ;
#76505=CARTESIAN_POINT ( 'NONE',  ( 0.7733716040702149908, -2.287020594544288521, 0.2280439049123609840 ) ) ;
#76506=CARTESIAN_POINT ( 'NONE',  ( 5.910985094894211755, -1.548708053515185812, 1.204094020389692155 ) ) ;
#76510=CARTESIAN_POINT ( 'NONE',  ( 0.5376586404672692998, 1.932363751568724641, -0.7437053376125392079 ) ) ;
#76512=CARTESIAN_POINT ( 'NONE',  ( 1.927394988521138774, -1.368145043076029133, -1.581016005797744262 ) ) ;
#76513=CARTESIAN_POINT ( 'NONE',  ( 6.543818844511720023, 0.6727183027174578056, -1.637219817372371100 ) ) ;
#76516=CARTESIAN_POINT ( 'NONE',  ( 2.296107463031165086, 1.396982486531380463, -1.037807123096459838 ) ) ;
#76521=CARTESIAN_POINT ( 'NONE',  ( 2.297083607218278978, 1.332544580598886252, 1.095227982430951208 ) ) ;
#76522=CARTESIAN_POINT ( 'NONE',  ( 2.841561854484982774, 0.7863008361240211297, -2.045831095052422555 ) ) ;
#76524=CARTESIAN_POINT ( 'NONE',  ( 4.881566871873391555, 2.059980941486462047, -0.7921658822237286346 ) ) ;
#76526=CARTESIAN_POINT ( 'NONE',  ( 2.852568495416502703, -2.164958695077593642, -0.1640175257638913364 ) ) ;
#76527=CARTESIAN_POINT ( 'NONE',  ( 0.9612317138737861422, 0.3586375672061762887, -1.789940867121169843 ) ) ;
#76528=CARTESIAN_POINT ( 'NONE',  ( 3.151669946411875589, 2.064753251683769442, -0.4682690128248386818 ) ) ;
#76529=CARTESIAN_POINT ( 'NONE',  ( 6.539320575229249144, 0.007148032025052972194, 1.896977914940492393 ) ) ;
#76531=CARTESIAN_POINT ( 'NONE',  ( 3.439304851068147428, -1.736875716534720615, -1.496195766483783274 ) ) ;
#76536=CARTESIAN_POINT ( 'NONE',  ( 5.865950696152278709, 0.6470421894613547220, -2.124994868043238672 ) ) ;
#76542=CARTESIAN_POINT ( 'NONE',  ( 3.973279856364997809, -1.994869694282218386, -0.2930714778977619450 ) ) ;
#76544=CARTESIAN_POINT ( 'NONE',  ( 1.709910653088747789, 0.6025335139634242498, -1.972566668331069195 ) ) ;
#76550=CARTESIAN_POINT ( 'NONE',  ( 4.664136352776428573, -1.432711980460563250, 1.658340198327029613 ) ) ;
#76551=CARTESIAN_POINT ( 'NONE',  ( 3.024064729735044921, -1.777011313454954999, 0.9530116517338580451 ) ) ;
#76552=CARTESIAN_POINT ( 'NONE',  ( 2.067674361007607597, -1.131582805410412673, 1.452419944642673100 ) ) ;
#76555=CARTESIAN_POINT ( 'NONE',  ( 6.071303273277399271, 0.1315155018670917386, -1.820917815106848359 ) ) ;
#76557=CARTESIAN_POINT ( 'NONE',  ( 6.245044592044297183, -1.915350782734099200, 1.204081839623271311 ) ) ;
#76559=CARTESIAN_POINT ( 'NONE',  ( 1.629656122859889811, -1.982562362509328047, 0.7109879831135539341 ) ) ;
#76569=CARTESIAN_POINT ( 'NONE',  ( 2.408575119285644384, -2.115224228095522907, -0.1514441693673748146 ) ) ;
#76570=CARTESIAN_POINT ( 'NONE',  ( 2.760263405638745393, 0.7954514732361592788, -2.074294698012415505 ) ) ;
#76571=CARTESIAN_POINT ( 'NONE',  ( 0.5576012004645107822, -1.866542136390366036, -1.177153700605698461 ) ) ;
#76574=CARTESIAN_POINT ( 'NONE',  ( 4.158614545834369736, -0.6132839004606009947, -1.863630207987923004 ) ) ;
#76583=CARTESIAN_POINT ( 'NONE',  ( 3.181995841446764839, 2.068044944583770306, -0.4684364081647199307 ) ) ;
#76585=CARTESIAN_POINT ( 'NONE',  ( 4.522454563201145028, 1.332364063043836033, -1.702191164408660251 ) ) ;
#76586=CARTESIAN_POINT ( 'NONE',  ( 3.597050949361340511, -0.5310884314010614338, 1.763007376093472800 ) ) ;
#76590=CARTESIAN_POINT ( 'NONE',  ( 5.665861931341662938, -1.099307624823061547, 1.349167961392354620 ) ) ;
#76591=CARTESIAN_POINT ( 'NONE',  ( 6.827182134110195477, 7.052946558436035573, 2.509100386683714490 ) ) ;
#76594=CARTESIAN_POINT ( 'NONE',  ( 2.465889518630470789, 2.120156730345585938, -0.4209195040108040797 ) ) ;
#76595=CARTESIAN_POINT ( 'NONE',  ( 5.624374986212743011, 0.3960386850128463920, -1.976653645673176474 ) ) ;
#76597=CARTESIAN_POINT ( 'NONE',  ( 1.903414394802248166, 1.797162532295241366, 1.201017911493490020 ) ) ;
#76598=CARTESIAN_POINT ( 'NONE',  ( 3.216049615590831579, -0.9687177021495720908, -1.716833007709689607 ) ) ;
#76600=CARTESIAN_POINT ( 'NONE',  ( 1.589377644589501148, -0.3404682245478432567, -2.282209529656929803 ) ) ;
#76601=CARTESIAN_POINT ( 'NONE',  ( 4.950698622930713277, -1.642605121802564350, -1.035792469189389386 ) ) ;
#76605=CARTESIAN_POINT ( 'NONE',  ( 0.07775346131144375561, -0.005211914751935430370, -2.288974916015192651 ) ) ;
#76609=CARTESIAN_POINT ( 'NONE',  ( 2.134064618640969524, -1.441378300436758630, -1.671108464803609417 ) ) ;
#76611=CARTESIAN_POINT ( 'NONE',  ( 6.209812062937981381, 0.5727486527220859713, -1.876249287704085722 ) ) ;
#76618=CARTESIAN_POINT ( 'NONE',  ( 5.595603887632320195, -1.841320590885606068, 0.004091980732826016286 ) ) ;
#76626=CARTESIAN_POINT ( 'NONE',  ( 0.3212574623711033639, -0.1015677953285927942, 2.058520922655207031 ) ) ;
#76628=CARTESIAN_POINT ( 'NONE',  ( 2.418200368955259361, 0.7924288909779563239, 1.684046449600750561 ) ) ;
#76629=CARTESIAN_POINT ( 'NONE',  ( 4.265079090171526310, 1.784866007061826298, -0.4516350764028759235 ) ) ;
#76633=CARTESIAN_POINT ( 'NONE',  ( 6.610000000000006537, 2.052567036419289614, 2.306714106643445561 ) ) ;
#76636=CARTESIAN_POINT ( 'NONE',  ( 4.547634279845023109, -1.704780727694398479, -1.401453192282381188 ) ) ;
#76637=CARTESIAN_POINT ( 'NONE',  ( 5.764971491839249396, -2.041691765312734663, -0.9750072289948004123 ) ) ;
#76639=CARTESIAN_POINT ( 'NONE',  ( 6.082253981448354274, 0.9392408507493594794, 1.548964021007705139 ) ) ;
#76640=CARTESIAN_POINT ( 'NONE',  ( 0.1105650446291406575, 1.931126588553159884, 0.5807481968119408977 ) ) ;
#76643=CARTESIAN_POINT ( 'NONE',  ( 5.971340724440282521, -1.642497693792897451, -0.9790476769208908969 ) ) ;
#76646=CARTESIAN_POINT ( 'NONE',  ( 1.041631754505952134, 0.7616270086890539748, -1.708776438048253077 ) ) ;
#76647=CARTESIAN_POINT ( 'NONE',  ( 2.219935720625454412, 0.9462983093676997637, -1.780669029686342331 ) ) ;
#76649=CARTESIAN_POINT ( 'NONE',  ( 4.442079272866404693, 0.9008978453017953969, -1.903793715863113523 ) ) ;
#76654=CARTESIAN_POINT ( 'NONE',  ( 3.445573674754712545, -1.864599547292019155, 0.7769016540176328922 ) ) ;
#76657=CARTESIAN_POINT ( 'NONE',  ( 4.815789973571149574, -2.120931333841672650, 0.4164600335647972162 ) ) ;
#76664=CARTESIAN_POINT ( 'NONE',  ( 2.418641202038225302, 0.9268156738743680290, 1.963535311701142483 ) ) ;
#76667=CARTESIAN_POINT ( 'NONE',  ( 0.5031362391596030381, -1.832460416942282011, 0.1798594046882526221 ) ) ;
#76669=CARTESIAN_POINT ( 'NONE',  ( 2.665787806004877414, 1.174844384069907655, 1.849873475113596566 ) ) ;
#76670=CARTESIAN_POINT ( 'NONE',  ( 6.883263157960350043, 2.968548739964393945, 2.406833999121655854 ) ) ;
#76671=CARTESIAN_POINT ( 'NONE',  ( 2.501149491322187224, 1.817439291034177451, -1.347377658580677817 ) ) ;
#76678=CARTESIAN_POINT ( 'NONE',  ( 4.165142103487808889, 0.2181862141000940336, -1.756177202920036429 ) ) ;
#76680=CARTESIAN_POINT ( 'NONE',  ( 0.5695303461548965052, 0.2060630844733425115, -2.095861547610248454 ) ) ;
#76688=CARTESIAN_POINT ( 'NONE',  ( 3.203821283898714345, -1.868584281295191607, 0.09040415888627445495 ) ) ;
#76689=CARTESIAN_POINT ( 'NONE',  ( 4.909070852169226562, -1.665950775781706028, 1.228889460859562854 ) ) ;
#76696=CARTESIAN_POINT ( 'NONE',  ( 4.369553226407375313, -0.3375162941181614751, 1.932460123137308861 ) ) ;
#76697=CARTESIAN_POINT ( 'NONE',  ( 1.124374798274978104, 0.3960433595797500095, -1.976652716225081097 ) ) ;
#76700=CARTESIAN_POINT ( 'NONE',  ( 1.475632603725419489, 1.109822327618605442, 1.505604422130282227 ) ) ;
#76702=CARTESIAN_POINT ( 'NONE',  ( 3.392840988816598902, -1.941408766427907384, -0.5327130583171105771 ) ) ;
#76704=CARTESIAN_POINT ( 'NONE',  ( 2.935286906334752199, -1.732537268552689635, -1.216715599779298884 ) ) ;
#76705=CARTESIAN_POINT ( 'NONE',  ( 6.825078400183577365, 2.023440267519378999, 2.448151054272352578 ) ) ;
#76706=CARTESIAN_POINT ( 'NONE',  ( 5.266107318980479235, -2.060723932065291031, 0.1993833602659672022 ) ) ;
#76709=CARTESIAN_POINT ( 'NONE',  ( -0.006154234300160406693, -2.090381218474619995, -0.04699178559822854429 ) ) ;
#76711=CARTESIAN_POINT ( 'NONE',  ( 5.227504313999177477, -1.733024862908550290, 0.5741523302658231298 ) ) ;
#76716=CARTESIAN_POINT ( 'NONE',  ( 6.088949818052607377, -0.3178892970779038096, -2.183640257897196513 ) ) ;
#76718=CARTESIAN_POINT ( 'NONE',  ( 6.059226159983991167, -1.612925389857391645, 1.026989893868179404 ) ) ;
#76730=CARTESIAN_POINT ( 'NONE',  ( 0.1399997263885794929, 4.089933038008564559, -2.554595152914000078 ) ) ;
#76733=CARTESIAN_POINT ( 'NONE',  ( 2.149204315396076481, 1.716066119659308331, -0.9661483248721688399 ) ) ;
#76734=CARTESIAN_POINT ( 'NONE',  ( 3.567982607561688280, -0.9913820634350967165, 1.755780237201590488 ) ) ;
#76736=CARTESIAN_POINT ( 'NONE',  ( 6.827182134110199918, 2.946470958711099541, 2.641117900019366527 ) ) ;
#76737=CARTESIAN_POINT ( 'NONE',  ( 3.732539452256115275, 0.3211115598316104935, 2.167677955659273348 ) ) ;
#76738=CARTESIAN_POINT ( 'NONE',  ( 1.676654808981252520, -1.828468026129226542, -0.6065514213326441695 ) ) ;
#76741=CARTESIAN_POINT ( 'NONE',  ( 0.1333542156527582345, 4.089120883327095335, -2.600857804679152174 ) ) ;
#76749=CARTESIAN_POINT ( 'NONE',  ( 5.829618728418341611, 0.9018330327132916269, -1.605192750430362025 ) ) ;
#76750=CARTESIAN_POINT ( 'NONE',  ( 3.334638158648925099, 1.275257586908218110, -1.557663628481553264 ) ) ;
#76751=CARTESIAN_POINT ( 'NONE',  ( 4.060169364306280393, 1.944150891614861543, -1.225672094199470985 ) ) ;
#76752=CARTESIAN_POINT ( 'NONE',  ( -0.1288028175206881731, 1.984098898469729200, -2.687169534535143178 ) ) ;
#76753=CARTESIAN_POINT ( 'NONE',  ( 2.641259143913599949, 1.703662207083409763, -0.7491738860408488909 ) ) ;
#76758=CARTESIAN_POINT ( 'NONE',  ( 4.564062515778636531, -1.364536961465147913, 1.584173057036510013 ) ) ;
#76759=CARTESIAN_POINT ( 'NONE',  ( 3.819104250046548632, -0.1383300533824398659, 1.865606469731183825 ) ) ;
#76765=CARTESIAN_POINT ( 'NONE',  ( 6.041572768212772893, -1.254329016146822351, -1.184272192918204514 ) ) ;
#76767=CARTESIAN_POINT ( 'NONE',  ( 1.019655691060247227, -1.568448733338474455, 0.7400992899176340734 ) ) ;
#76771=CARTESIAN_POINT ( 'NONE',  ( 5.418865745523654631, -1.577555059383651814, 1.491859142196997334 ) ) ;
#76772=CARTESIAN_POINT ( 'NONE',  ( 4.283705427790140519, 1.194290084605063251, 1.380960126487425166 ) ) ;
#76773=CARTESIAN_POINT ( 'NONE',  ( 1.850371385673426294, -1.951817131159512719, -0.1975377159662907445 ) ) ;
#76774=CARTESIAN_POINT ( 'NONE',  ( 6.509000000000050967, 0.001920477310565076989, 2.100274754360692331 ) ) ;
#76778=CARTESIAN_POINT ( 'NONE',  ( 2.701940546545733568, 1.501232083741442125, 1.497845299259781049 ) ) ;
#76779=CARTESIAN_POINT ( 'NONE',  ( 6.827182134110222123, -0.006956174471953178659, 2.188967759425272330 ) ) ;
#76783=CARTESIAN_POINT ( 'NONE',  ( 0.9716355300813659390, -0.3074278181635254348, 2.047203142020392441 ) ) ;
#76786=CARTESIAN_POINT ( 'NONE',  ( 3.141495721539554697, 0.05644213937440466927, 2.220748567232306847 ) ) ;
#76788=CARTESIAN_POINT ( 'NONE',  ( 1.126083094664981799, 0.4549445381971609637, 2.253098081826758303 ) ) ;
#76790=CARTESIAN_POINT ( 'NONE',  ( 6.526245194314398645, 1.055377990298064450, 1.771961156250308145 ) ) ;
#76794=CARTESIAN_POINT ( 'NONE',  ( 0.1333542156527530165, 6.948072531064762636, -2.641009269961028139 ) ) ;
#76795=CARTESIAN_POINT ( 'NONE',  ( 5.987831981441136264, -1.833028718050220940, -0.1737628300680846560 ) ) ;
#76797=CARTESIAN_POINT ( 'NONE',  ( -0.2104748580754183807, 4.084054299358617079, -2.658391380015924010 ) ) ;
#76798=CARTESIAN_POINT ( 'NONE',  ( 2.660839013829336075, -1.499436941970986759, -0.8522202921518050589 ) ) ;
#76799=CARTESIAN_POINT ( 'NONE',  ( 1.569546381206438967, 1.394087592100446971, 1.457234012747665508 ) ) ;
#76800=CARTESIAN_POINT ( 'NONE',  ( 3.358291665479910648, 0.05479990919179249936, -2.298175070600398939 ) ) ;
#76801=CARTESIAN_POINT ( 'NONE',  ( 2.776973401877864234, -2.164208356635976216, -0.6592219059844570683 ) ) ;
#76802=CARTESIAN_POINT ( 'NONE',  ( 4.740906146847382985, 0.3592350385927112200, 2.075039481041524247 ) ) ;
#76804=CARTESIAN_POINT ( 'NONE',  ( 3.233429047156919811, -1.186097956103189910, -1.313638963288694228 ) ) ;
#76807=CARTESIAN_POINT ( 'NONE',  ( -0.02301423135257947214, -0.1624751001964518382, -2.256290569412158220 ) ) ;
#76808=CARTESIAN_POINT ( 'NONE',  ( 4.997927640213790212, -0.6233917918176261619, -1.732523409203725606 ) ) ;
#76813=CARTESIAN_POINT ( 'NONE',  ( 4.312563266315373234, 2.003113633248252867, 0.8892094534625747393 ) ) ;
#76816=CARTESIAN_POINT ( 'NONE',  ( 5.055165704564410944, 1.723227314588217318, -1.147259442322377865 ) ) ;
#76819=CARTESIAN_POINT ( 'NONE',  ( 3.580616652426432012, -1.856930023900615456, -0.5128254122194577658 ) ) ;
#76822=CARTESIAN_POINT ( 'NONE',  ( 0.2115809916233695465, 1.842269378952247738, -1.241004044093022340 ) ) ;
#76831=CARTESIAN_POINT ( 'NONE',  ( 1.574581288703358339, 1.320057194528483135, -1.451483715152704246 ) ) ;
#76835=CARTESIAN_POINT ( 'NONE',  ( 5.617619635959271385, 0.3843197845415853853, -1.923678648292715732 ) ) ;
#76839=CARTESIAN_POINT ( 'NONE',  ( 0.1634265777989383772, -2.022787333623011108, -1.013812598571243617 ) ) ;
#76840=CARTESIAN_POINT ( 'NONE',  ( -0.2106725631050099246, 1.363266585364702577, -2.259529575671606505 ) ) ;
#76843=CARTESIAN_POINT ( 'NONE',  ( 6.854760797074392897, -1.525272977149809694, 1.248552938341955798 ) ) ;
#76844=CARTESIAN_POINT ( 'NONE',  ( 6.415404398373737216, 0.5482957075174756945, 1.644958459601528755 ) ) ;
#76846=CARTESIAN_POINT ( 'NONE',  ( 2.648187065138879692, 0.7411268365287645432, 2.062558662443473523 ) ) ;
#76847=CARTESIAN_POINT ( 'NONE',  ( 4.788248824917088697, -1.092567961935811960, 2.032559802855623321 ) ) ;
#76848=CARTESIAN_POINT ( 'NONE',  ( 5.536423053809180317, 2.029556968340691547, 0.3564751269278207957 ) ) ;
#76849=CARTESIAN_POINT ( 'NONE',  ( 1.675622358955121571, -1.039060084690484942, 1.640409814757173734 ) ) ;
#76852=CARTESIAN_POINT ( 'NONE',  ( 4.763993809689464065, 0.6627061821620899851, -2.014485251161435286 ) ) ;
#76854=CARTESIAN_POINT ( 'NONE',  ( 2.567029916978436077, -1.034165006014248211, 1.730866473406714068 ) ) ;
#76856=CARTESIAN_POINT ( 'NONE',  ( 5.667066814448853407, -1.992748536412903615, -0.9483587796220711574 ) ) ;
#76859=CARTESIAN_POINT ( 'NONE',  ( 0.2229205655521030172, -0.09321834626660817358, 1.823428419517532983 ) ) ;
#76865=CARTESIAN_POINT ( 'NONE',  ( 5.577047029790810129, -0.04816181868504652158, -2.060495320025256483 ) ) ;
#76869=CARTESIAN_POINT ( 'NONE',  ( 4.863928438619278261, 0.6316314618598058983, -1.918449035972718431 ) ) ;
#76875=CARTESIAN_POINT ( 'NONE',  ( 3.784101207196560068, -1.017168810052709205, 1.792309825713923166 ) ) ;
#76876=CARTESIAN_POINT ( 'NONE',  ( 2.391250195717840477, -0.7743161457766101208, -1.862016636315230844 ) ) ;
#76878=CARTESIAN_POINT ( 'NONE',  ( 6.727182134110196721, 6.033756510516266935, 2.783943001041962795 ) ) ;
#76883=CARTESIAN_POINT ( 'NONE',  ( 3.304064382408095302, -1.779354530013575131, 0.9478943420064069869 ) ) ;
#76884=CARTESIAN_POINT ( 'NONE',  ( 2.484105014303281234, -0.3146448974087300288, -1.813890345909507928 ) ) ;
#76885=CARTESIAN_POINT ( 'NONE',  ( 1.243279834139981999, 0.4545127484847265031, 2.262342451343732463 ) ) ;
#76887=CARTESIAN_POINT ( 'NONE',  ( 2.231903258980330484, -1.410129017595105561, -1.638413920015222125 ) ) ;
#76891=CARTESIAN_POINT ( 'NONE',  ( 1.551402291579254022, 0.5461136009352780540, -1.789155053659279071 ) ) ;
#76892=CARTESIAN_POINT ( 'NONE',  ( 5.541858398712612654, 0.7996551022716179569, -1.802186847774432943 ) ) ;
#76896=CARTESIAN_POINT ( 'NONE',  ( 0.8036966383840878914, 1.806304194667744500, 1.267646993260997723 ) ) ;
#76897=CARTESIAN_POINT ( 'NONE',  ( 6.303194806757332458, -1.751150776259063457, 1.104182018118210262 ) ) ;
#76900=CARTESIAN_POINT ( 'NONE',  ( 6.539320575229251808, 2.414832891527439962, 2.584256253838035366 ) ) ;
#76901=CARTESIAN_POINT ( 'NONE',  ( 4.768415704089838947, -1.288333767974993327, 1.492341041399107393 ) ) ;
#76902=CARTESIAN_POINT ( 'NONE',  ( 0.0004480315400831600455, -0.9938866557669153723, 1.873244595478529728 ) ) ;
#76903=CARTESIAN_POINT ( 'NONE',  ( 4.231326342634161186, 0.1110341807785204943, 2.305146914567071548 ) ) ;
#76904=CARTESIAN_POINT ( 'NONE',  ( 2.870046724737782995, -2.040761436538469198, 0.2982335875671269787 ) ) ;
#76911=CARTESIAN_POINT ( 'NONE',  ( 5.195835581519938629, -1.531768914234220347, -1.538983792029069209 ) ) ;
#76913=CARTESIAN_POINT ( 'NONE',  ( 4.405690278861111864, -0.7914791229979671883, -1.662609734262666894 ) ) ;
#76915=CARTESIAN_POINT ( 'NONE',  ( 6.720655732516647163, 0.6055996050860124047, 1.780393570709505546 ) ) ;
#76916=CARTESIAN_POINT ( 'NONE',  ( 5.073855206572205567, -1.217758175834412260, 1.821886007100224969 ) ) ;
#76918=CARTESIAN_POINT ( 'NONE',  ( 0.4919812829822337030, 1.677557865031731765, 1.518126404548009178 ) ) ;
#76924=CARTESIAN_POINT ( 'NONE',  ( 1.340303658288226396, 0.3404796732740902887, 1.736595688552546424 ) ) ;
#76925=CARTESIAN_POINT ( 'NONE',  ( 5.180342516426402533, 0.9943292982247069478, 1.750330089345548679 ) ) ;
#76927=CARTESIAN_POINT ( 'NONE',  ( 4.102637100452250607, -0.6586339671014628250, -2.000395093806975222 ) ) ;
#76928=CARTESIAN_POINT ( 'NONE',  ( 2.864735742032016752, -0.1435939464786405995, -1.910298799178041351 ) ) ;
#76930=CARTESIAN_POINT ( 'NONE',  ( 4.141030287458704606, -0.1905934838449650226, -1.960285098343496291 ) ) ;
#76931=CARTESIAN_POINT ( 'NONE',  ( 5.344012529290226965, -1.284645313656457288, -1.558556736529070674 ) ) ;
#76932=CARTESIAN_POINT ( 'NONE',  ( 2.061206331123175861, 0.3224310286589862629, -1.842498087946140561 ) ) ;
#76933=CARTESIAN_POINT ( 'NONE',  ( 5.566962092400322248, -1.562093814453187735, -0.7318214103424671713 ) ) ;
#76934=CARTESIAN_POINT ( 'NONE',  ( 1.177825114000274898, 1.883588471398514264, -0.3297955356276888184 ) ) ;
#76936=CARTESIAN_POINT ( 'NONE',  ( 1.489210700298746692, -0.3264265768355456010, -2.182489157894373033 ) ) ;
#76940=CARTESIAN_POINT ( 'NONE',  ( 6.232861002365865488, -1.862453515449840724, -0.6167318247369477646 ) ) ;
#76942=CARTESIAN_POINT ( 'NONE',  ( 6.719622092096638966, -1.813896567892055112, 0.4569536213836836169 ) ) ;
#76948=CARTESIAN_POINT ( 'NONE',  ( 1.926316106172959230, 1.062450747350886848, 1.776810178100460824 ) ) ;
#76953=CARTESIAN_POINT ( 'NONE',  ( -0.05793207083453711520, -1.244369569480655136, -1.591280167384064637 ) ) ;
#76958=CARTESIAN_POINT ( 'NONE',  ( 5.975935433960424703, 1.776740614516297390, 0.9528632009266969627 ) ) ;
#76959=CARTESIAN_POINT ( 'NONE',  ( 4.434732071067119641, -1.534896228733380052, 1.146084025706934684 ) ) ;
#76961=CARTESIAN_POINT ( 'NONE',  ( 2.806388347806953121, 1.585463108415147149, -1.513251884624075672 ) ) ;
#76962=CARTESIAN_POINT ( 'NONE',  ( 0.1399997263886003374, 0.002789056014650820314, -1.999853399661279063 ) ) ;
#76964=CARTESIAN_POINT ( 'NONE',  ( 5.343998949255959197, -1.280338926806196431, -1.553582282148850524 ) ) ;
#76965=CARTESIAN_POINT ( 'NONE',  ( 1.705181254219298115, 1.662258477346746588, -0.9455041445245655485 ) ) ;
#76968=CARTESIAN_POINT ( 'NONE',  ( 0.1578276607246929530, 1.163290555716024244, 1.646825313395771762 ) ) ;
#76970=CARTESIAN_POINT ( 'NONE',  ( 3.192999258835881093, 1.649592175042478015, 1.284459162532962440 ) ) ;
#76972=CARTESIAN_POINT ( 'NONE',  ( 1.570901180570225542, 0.1317378181442031559, -1.719804994506502149 ) ) ;
#76973=VERTEX_POINT ( 'NONE', #157104 ) ;
#76974=CARTESIAN_POINT ( 'NONE',  ( 6.433838290133602200, -2.056603270127650429, 0.5165238393732355382 ) ) ;
#76983=CARTESIAN_POINT ( 'NONE',  ( 2.789504176380937395, 1.719411750852325449, -0.5702826837221984801 ) ) ;
#76989=CARTESIAN_POINT ( 'NONE',  ( 3.809066866439265286, 1.528366121442883196, -0.9720638507800370975 ) ) ;
#76990=CARTESIAN_POINT ( 'NONE',  ( 6.539320575229250920, 3.702490941164796379, 2.411252750440337156 ) ) ;
#76993=CARTESIAN_POINT ( 'NONE',  ( 3.736619961808427259, -1.792986960150410036, -0.4983748678565723678 ) ) ;
#76994=CARTESIAN_POINT ( 'NONE',  ( 1.265090914671564759, 1.769361140067410521, -0.7345930670351871195 ) ) ;
#76995=CARTESIAN_POINT ( 'NONE',  ( 1.465546361252961560, 1.799214786004127209, -0.3081908958329632742 ) ) ;
#77003=CARTESIAN_POINT ( 'NONE',  ( 6.262555971378708897, -0.7055598467285629782, -1.838920630280465041 ) ) ;
#77006=CARTESIAN_POINT ( 'NONE',  ( 0.5332922803617061724, -1.479851573012560761, -1.477019686621689143 ) ) ;
#77008=CARTESIAN_POINT ( 'NONE',  ( 5.227533229383872104, -1.829308364520453978, 0.6040709075912870096 ) ) ;
#77010=CARTESIAN_POINT ( 'NONE',  ( 1.061231560844998034, 0.3605832424212577769, -1.789441408372116182 ) ) ;
#77011=CARTESIAN_POINT ( 'NONE',  ( 1.629795212970772456, -2.077151576879713080, 0.7458654493318407352 ) ) ;
#77013=CARTESIAN_POINT ( 'NONE',  ( 0.9317291061951762376, -1.865162313430932750, 0.4216105838140621342 ) ) ;
#77014=CARTESIAN_POINT ( 'NONE',  ( 6.807475516257630588, -1.579661688080177262, -1.175915379947721773 ) ) ;
#77015=CARTESIAN_POINT ( 'NONE',  ( 2.067823894287325714, -1.192992258377950865, 1.532381367046357523 ) ) ;
#77016=CARTESIAN_POINT ( 'NONE',  ( 1.177110994959302825, -0.9039684864705423983, -1.802142742073430171 ) ) ;
#77018=CARTESIAN_POINT ( 'NONE',  ( 6.977413160773116019, -0.1420559494431029579, 1.829748798152310174 ) ) ;
#77024=CARTESIAN_POINT ( 'NONE',  ( 2.015410700679621137, -2.124826835150806392, 0.5361769018528695918 ) ) ;
#77029=CARTESIAN_POINT ( 'NONE',  ( 2.279681363911123970, 1.122676072794186908, 1.439608767588994365 ) ) ;
#77037=CARTESIAN_POINT ( 'NONE',  ( 0.6801461905075457670, -1.071176224578209935, 1.601055298966150842 ) ) ;
#77038=CARTESIAN_POINT ( 'NONE',  ( 5.172687041346638814, 1.355624813549320740, -1.418227474788292364 ) ) ;
#77042=CARTESIAN_POINT ( 'NONE',  ( 5.161759341795384870, 1.079763445194487970, 1.907048802792680631 ) ) ;
#77044=CARTESIAN_POINT ( 'NONE',  ( 3.537997267176114846, 1.309675639058418550, 1.603382541711120268 ) ) ;
#77048=CARTESIAN_POINT ( 'NONE',  ( 3.903220922379626145, -1.182460753651290775, -1.971142157236325243 ) ) ;
#77055=CARTESIAN_POINT ( 'NONE',  ( 4.277243253991915850, 1.269349932698702110, 1.469746654517690487 ) ) ;
#77059=CARTESIAN_POINT ( 'NONE',  ( 5.590081826628392925, 1.144292256163012667, 1.532101299821154949 ) ) ;
#77060=CARTESIAN_POINT ( 'NONE',  ( 5.930603204692192598, 1.663448300781378508, 0.4554771339976750322 ) ) ;
#77061=CARTESIAN_POINT ( 'NONE',  ( 5.120327457147888950, 1.987497208294352280, 0.3399611521368098854 ) ) ;
#77063=CARTESIAN_POINT ( 'NONE',  ( 1.401302286655212948, 1.802556353783949517, -1.272968949304439379 ) ) ;
#77067=CARTESIAN_POINT ( 'NONE',  ( 2.062552408159121775, -1.911915923569502684, -0.8461947581326088041 ) ) ;
#77068=CARTESIAN_POINT ( 'NONE',  ( 6.919227944281516329, -0.1317407762830881124, 1.740281130587753688 ) ) ;
#77069=CARTESIAN_POINT ( 'NONE',  ( 5.836564609439236939, 0.5826586670559866787, -1.930416874340326938 ) ) ;
#77072=CARTESIAN_POINT ( 'NONE',  ( 3.205313226950608385, -0.4470181708258395004, 2.248096707283386841 ) ) ;
#77073=CARTESIAN_POINT ( 'NONE',  ( 1.271012957286155709, 1.034212954684173180, 1.399518829098946204 ) ) ;
#77075=CARTESIAN_POINT ( 'NONE',  ( 3.129257641292593650, 1.918792544363761454, 0.9031103230835100248 ) ) ;
#77077=CARTESIAN_POINT ( 'NONE',  ( 1.018380972650875460, 1.732250818821230443, -0.07729615888975129023 ) ) ;
#77079=CARTESIAN_POINT ( 'NONE',  ( 1.205250485101029723, -1.463924481597483007, -1.148973905474151014 ) ) ;
#77080=CARTESIAN_POINT ( 'NONE',  ( 1.504584854702104124, 2.168655969765376224, 0.1073316571278438991 ) ) ;
#77081=CARTESIAN_POINT ( 'NONE',  ( 2.975796278104340331, -0.8128168404246680634, 1.845627246706407210 ) ) ;
#77082=CARTESIAN_POINT ( 'NONE',  ( 4.593750000000003553, -1.895863743164180493, -0.7852924748297412938 ) ) ;
#77085=CARTESIAN_POINT ( 'NONE',  ( 6.217406027492617504, -0.2333201818524588411, 1.912260165615098595 ) ) ;
#77087=CARTESIAN_POINT ( 'NONE',  ( 3.076664410187186505, 1.002321471918452556, 1.982530577833590879 ) ) ;
#77089=CARTESIAN_POINT ( 'NONE',  ( -0.2108831679771168421, 6.948330828014878335, -2.492181822431015270 ) ) ;
#77093=CARTESIAN_POINT ( 'NONE',  ( 5.195737816846159873, -1.386088135442983260, -1.388664821390848347 ) ) ;
#77097=CARTESIAN_POINT ( 'NONE',  ( 5.782586711780850486, -2.205454299129143703, -0.5038293679325082097 ) ) ;
#77100=CARTESIAN_POINT ( 'NONE',  ( 2.207554788950978786, -1.655329399669298818, -1.230451883716067174 ) ) ;
#77105=CARTESIAN_POINT ( 'NONE',  ( 3.251090012001829788, -1.527204365403836306, -1.079795099579644591 ) ) ;
#77106=CARTESIAN_POINT ( 'NONE',  ( 2.162404540820038967, 1.068076967457934012, 1.366050734290222834 ) ) ;
#77107=CARTESIAN_POINT ( 'NONE',  ( 6.567925981381852907, -1.350348970527824211, 1.726830949945204363 ) ) ;
#77108=CARTESIAN_POINT ( 'NONE',  ( 1.202499378025536636, -2.206952907257493823, 0.001246274542086866404 ) ) ;
#77109=CARTESIAN_POINT ( 'NONE',  ( 4.188458007013862172, -2.137797052781073237, -0.3198388112101158143 ) ) ;
#77110=CARTESIAN_POINT ( 'NONE',  ( 5.261643664715593971, 0.9589319835984220219, 1.688605554185283575 ) ) ;
#77112=CARTESIAN_POINT ( 'NONE',  ( 0.1562501595635738816, -1.895867669153105339, 0.7852924748299968671 ) ) ;
#77113=CARTESIAN_POINT ( 'NONE',  ( -0.06968618116158857567, -1.560424145883563929, -1.276814929289785239 ) ) ;
#77114=CARTESIAN_POINT ( 'NONE',  ( 0.1410940620840978044, 2.031152781523197337, 0.6094965309384676733 ) ) ;
#77117=CARTESIAN_POINT ( 'NONE',  ( 5.924453975591452703, -1.462443569488897754, -1.388487997949397368 ) ) ;
#77121=CARTESIAN_POINT ( 'NONE',  ( 3.510199737632841543, -0.7410081052188906003, -1.668730646197075673 ) ) ;
#77122=CARTESIAN_POINT ( 'NONE',  ( 1.729795059504362076, -2.077734391967264838, 0.7439406459070623256 ) ) ;
#77128=CARTESIAN_POINT ( 'NONE',  ( 0.9319058833903216543, -1.969584188619889487, 0.4467263836498857055 ) ) ;
#77129=CARTESIAN_POINT ( 'NONE',  ( 1.541811043186253061, -1.995513645039903361, 0.7175487213698438227 ) ) ;
#77134=CARTESIAN_POINT ( 'NONE',  ( 3.045584334709343644, 1.312524258565110680, 1.319513337161677846 ) ) ;
#77136=CARTESIAN_POINT ( 'NONE',  ( 1.288190726105652217, -0.9714702286227733241, 1.931199087792371261 ) ) ;
#77137=CARTESIAN_POINT ( 'NONE',  ( 6.604150280000163242, -0.1430408514614608939, 1.983920101186954721 ) ) ;
#77141=CARTESIAN_POINT ( 'NONE',  ( 3.861776535121093090, 1.811678901967550326, -0.2252020330209548171 ) ) ;
#77145=CARTESIAN_POINT ( 'NONE',  ( 6.626327358740755180, 0.3474107405085808953, -1.985797104380654376 ) ) ;
#77146=CARTESIAN_POINT ( 'NONE',  ( 5.367088761235753402, 1.773375748883701419, -0.4946613714205680967 ) ) ;
#77147=CARTESIAN_POINT ( 'NONE',  ( -0.02319159430949797526, 7.629137130509074716, -2.410989586153565067 ) ) ;
#77148=CARTESIAN_POINT ( 'NONE',  ( 4.846439200125199243, 2.301219453760998679, 0.1735292846544200795 ) ) ;
#77150=CARTESIAN_POINT ( 'NONE',  ( 6.731704548537910782, -1.406307105171537009, -1.641701734229366716 ) ) ;
#77151=CARTESIAN_POINT ( 'NONE',  ( 1.804143404396211681, 1.437808690349717589, -1.305647666910898730 ) ) ;
#77152=CARTESIAN_POINT ( 'NONE',  ( 5.237821733363889010, -2.161759915733433068, -0.7809387408506673900 ) ) ;
#77155=CARTESIAN_POINT ( 'NONE',  ( 4.662891624058607576, -1.671085903211678270, -0.8408918736509605196 ) ) ;
#77157=CARTESIAN_POINT ( 'NONE',  ( 2.882959773793275726, -1.768624019741386277, -0.7279546805132871556 ) ) ;
#77160=CARTESIAN_POINT ( 'NONE',  ( 4.002700589841681200, -0.6913439845411989415, -2.095861086919461602 ) ) ;
#77161=CARTESIAN_POINT ( 'NONE',  ( 6.983263157960368339, 4.695310640067480001, 2.508805386165738227 ) ) ;
#77162=CARTESIAN_POINT ( 'NONE',  ( -0.2110808730067326444, 6.948329377029001996, -2.392166167428900536 ) ) ;
#77165=CARTESIAN_POINT ( 'NONE',  ( 1.844934828179781050, -1.667470251784016089, 1.051280099994149841 ) ) ;
#77166=CARTESIAN_POINT ( 'NONE',  ( 1.501454852758288494, 1.885366349659310048, -1.330307493247370410 ) ) ;
#77167=CARTESIAN_POINT ( 'NONE',  ( 2.365611650783586040, -0.4327418640146083462, 1.913375882425945917 ) ) ;
#77169=CARTESIAN_POINT ( 'NONE',  ( 6.192244813941197634, 1.021713635409545073, -1.791695130993501417 ) ) ;
#77176=CARTESIAN_POINT ( 'NONE',  ( 2.272564004159416395, -1.020438428401538200, -1.916272530736246926 ) ) ;
#77180=CARTESIAN_POINT ( 'NONE',  ( 1.932664581101939838, 0.1784410483233467293, 1.861995071071875785 ) ) ;
#77181=CARTESIAN_POINT ( 'NONE',  ( 0.3509462063632540763, -1.656586674793923075, 1.225593781303188967 ) ) ;
#77182=CARTESIAN_POINT ( 'NONE',  ( 0.07755575628181145265, 0.6932613274447991802, -2.271134039238668301 ) ) ;
#77183=CARTESIAN_POINT ( 'NONE',  ( 6.827182134110222123, 7.629137130509070275, 2.410944104600701188 ) ) ;
#77185=CARTESIAN_POINT ( 'NONE',  ( 1.770022778749248182, 1.907080152163560971, -0.1419829583147319274 ) ) ;
#77187=CARTESIAN_POINT ( 'NONE',  ( 4.381574371570028603, 1.156860168461280036, 1.339510341777202074 ) ) ;
#77188=CARTESIAN_POINT ( 'NONE',  ( 1.576665144504853400, -1.351504567317940664, 1.353124384123285617 ) ) ;
#77192=CARTESIAN_POINT ( 'NONE',  ( 6.433208386744649232, -1.541796563146474286, -1.136648034191472645 ) ) ;
#77194=CARTESIAN_POINT ( 'NONE',  ( 0.4497787391488928810, 1.533077660697563793, 1.391591089521776681 ) ) ;
#77197=CARTESIAN_POINT ( 'NONE',  ( 5.541831131927607679, 0.7570117910807551143, -1.710825945835430462 ) ) ;
#77198=CARTESIAN_POINT ( 'NONE',  ( 1.594096589105632011, -1.816728215151931058, -0.1805768397986490248 ) ) ;
#77199=CARTESIAN_POINT ( 'NONE',  ( 5.426482453889071245, 1.317083479513626587, -1.770629405693980640 ) ) ;
#77203=CARTESIAN_POINT ( 'NONE',  ( 2.770046845359328103, -2.040585247751625086, 0.3002346618998888439 ) ) ;
#77205=CARTESIAN_POINT ( 'NONE',  ( 6.610000000000021636, 3.695490760540712127, 2.514297579034238783 ) ) ;
#77210=CARTESIAN_POINT ( 'NONE',  ( 5.758279222819879806, -2.070544812512797428, -0.003756845764937844813 ) ) ;
#77212=CARTESIAN_POINT ( 'NONE',  ( 2.231903258980330484, -1.410129017595105561, -1.638413920015222125 ) ) ;
#77214=CARTESIAN_POINT ( 'NONE',  ( 3.475264548829166689, -1.782285498782819610, -0.9499825727283210952 ) ) ;
#77215=CARTESIAN_POINT ( 'NONE',  ( 6.720655732516654268, 4.688933928088002467, 2.736284108207136079 ) ) ;
#77220=CARTESIAN_POINT ( 'NONE',  ( 1.341030165941111241, -1.731997234073547220, -1.032477317303444053 ) ) ;
#77222=CARTESIAN_POINT ( 'NONE',  ( 6.321842903100938216, 1.263506803105146625, -1.790488031206059150 ) ) ;
#77224=CARTESIAN_POINT ( 'NONE',  ( 4.377155534175989793, -1.710687068321177007, -0.8549628122409487219 ) ) ;
#77228=CARTESIAN_POINT ( 'NONE',  ( 3.374625213368151133, -0.3961236654455925765, -1.976952669325626299 ) ) ;
#77231=CARTESIAN_POINT ( 'NONE',  ( 4.928557879857294211, 1.651178231652555617, 0.4983569138605167814 ) ) ;
#77236=CARTESIAN_POINT ( 'NONE',  ( 4.024554299415397551, 1.775361691451295520, 0.5892213400080713592 ) ) ;
#77238=CARTESIAN_POINT ( 'NONE',  ( 0.6552395816744536194, 1.723207459482085202, -1.147090658606984892 ) ) ;
#77241=CARTESIAN_POINT ( 'NONE',  ( 6.586573151046549945, -1.108064789702201569, 1.433474704228101748 ) ) ;
#77244=CARTESIAN_POINT ( 'NONE',  ( 0.05258934297286410597, 0.3095000349466696110, 1.784779062553583984 ) ) ;
#77247=CARTESIAN_POINT ( 'NONE',  ( 3.029421956395737858, -1.472182739719897215, -1.623467934892895759 ) ) ;
#77249=CARTESIAN_POINT ( 'NONE',  ( 0.5198770262540284293, 1.941052373433370448, -0.2841105942011297736 ) ) ;
#77252=CARTESIAN_POINT ( 'NONE',  ( 4.710494965788769584, 1.834319554003289721, 0.5521488281355608763 ) ) ;
#77262=CARTESIAN_POINT ( 'NONE',  ( 1.446389902895691693, 2.159248346720197276, 0.1057134262518744372 ) ) ;
#77267=CARTESIAN_POINT ( 'NONE',  ( 5.034128509002383289, 0.9373949799435165042, -1.566401400633938179 ) ) ;
#77270=CARTESIAN_POINT ( 'NONE',  ( 1.440630571055816489, 0.3805203625029949799, 1.934124978983255527 ) ) ;
#77271=CARTESIAN_POINT ( 'NONE',  ( 3.638835171272115421, 1.817485770107383436, 0.5952672491930725007 ) ) ;
#77274=CARTESIAN_POINT ( 'NONE',  ( 3.859776292547572929, -0.5741801112500494186, 1.883974994742370068 ) ) ;
#77276=CARTESIAN_POINT ( 'NONE',  ( 5.478056170419292492, -1.895640208600479326, -0.4214399443674861079 ) ) ;
#77280=CARTESIAN_POINT ( 'NONE',  ( 5.871359616481898414, -1.819694913365289768, -1.088597390283413402 ) ) ;
#77282=CARTESIAN_POINT ( 'NONE',  ( 4.441997247558228779, -1.179148908705367482, -1.505365500079666852 ) ) ;
#77289=CARTESIAN_POINT ( 'NONE',  ( 5.672526239869847053, 0.8180066501249063649, 1.839585422649665958 ) ) ;
#77291=CARTESIAN_POINT ( 'NONE',  ( 6.639283661800273961, -1.628176093627232479, 0.8261057939347238310 ) ) ;
#77292=CARTESIAN_POINT ( 'NONE',  ( 1.820844063133007396, -1.465591517063178806, 1.462601037713284535 ) ) ;
#77296=CARTESIAN_POINT ( 'NONE',  ( 6.280143113937574739, -0.9989825818290422044, 1.581392243879369053 ) ) ;
#77305=CARTESIAN_POINT ( 'NONE',  ( 3.885211248783075888, -0.5490618756427265712, -1.644986201639383028 ) ) ;
#77307=CARTESIAN_POINT ( 'NONE',  ( 1.305626334525695986, -1.629615561912756805, -1.276682400165381148 ) ) ;
#77308=CARTESIAN_POINT ( 'NONE',  ( 2.935286906334752199, -1.732537268552689635, -1.216715599779298884 ) ) ;
#77311=CARTESIAN_POINT ( 'NONE',  ( 6.912946559606852226, -1.604190412254998810, 1.308348183162249434 ) ) ;
#77315=CARTESIAN_POINT ( 'NONE',  ( 0.1231139863388103495, 1.664874722635242277, 0.9407772870168448209 ) ) ;
#77316=CARTESIAN_POINT ( 'NONE',  ( 4.031398662939575495, -1.579512745870830237, -1.661420017294244156 ) ) ;
#77317=CARTESIAN_POINT ( 'NONE',  ( 0.1877650043593872553, -0.8638833939697135866, 1.608357707688967242 ) ) ;
#77318=CARTESIAN_POINT ( 'NONE',  ( 3.709155072767254868, 1.612916391665040416, -1.027221078234448859 ) ) ;
#77322=CARTESIAN_POINT ( 'NONE',  ( 2.004154220962415689, -0.8570942286123193199, 1.821751609655430260 ) ) ;
#77323=CARTESIAN_POINT ( 'NONE',  ( 1.815213341579174688, -1.679845371888911698, -1.013028538569618719 ) ) ;
#77327=CARTESIAN_POINT ( 'NONE',  ( 4.910148475136437263, 1.442109633637311372, -1.513870239069979196 ) ) ;
#77328=CARTESIAN_POINT ( 'NONE',  ( 3.449836819150660538, 1.770032027316788437, 0.0008499603425977939660 ) ) ;
#77331=CARTESIAN_POINT ( 'NONE',  ( 6.263675073536269622, 1.173004239817846850, 1.969288764181243989 ) ) ;
#77332=CARTESIAN_POINT ( 'NONE',  ( 5.033026810027643627, -1.234204449110408053, -1.227257546430237989 ) ) ;
#77334=CARTESIAN_POINT ( 'NONE',  ( -0.1104750535120251481, 6.947232870375212421, -2.698533382536407732 ) ) ;
#77335=CARTESIAN_POINT ( 'NONE',  ( 4.639819690880945480, -0.0003889188416681537710, -1.734034292319245552 ) ) ;
#77336=CARTESIAN_POINT ( 'NONE',  ( 5.441899255841128102, 1.454089660041712140, 1.612519925251713060 ) ) ;
#77338=CARTESIAN_POINT ( 'NONE',  ( 6.315638730379727228, -1.320822524126588515, -1.523799118890494020 ) ) ;
#77339=CARTESIAN_POINT ( 'NONE',  ( 5.500000000000004441, -3.262149103155007084E-13, -2.052068128417942283 ) ) ;
#77342=CARTESIAN_POINT ( 'NONE',  ( 3.364200941815390866, 0.8650686769993837233, 1.721291803412771992 ) ) ;
#77344=CARTESIAN_POINT ( 'NONE',  ( 6.468989383178811892, -1.718075365336281246, 1.407709432230166202 ) ) ;
#77346=CARTESIAN_POINT ( 'NONE',  ( -0.1411974294642228400, 2.034035580701949897, -2.316051970441324936 ) ) ;
#77349=CARTESIAN_POINT ( 'NONE',  ( 2.368119171756615238, 0.5893650439614643854, -2.141638343492527685 ) ) ;
#77355=CARTESIAN_POINT ( 'NONE',  ( 0.1939827082095749167, 1.755770691208278889, 0.9913967135185000057 ) ) ;
#77357=CARTESIAN_POINT ( 'NONE',  ( 5.793442459296725744, -1.866233137118753715, 0.8787832743982221251 ) ) ;
#77362=CARTESIAN_POINT ( 'NONE',  ( 0.5437790142346760058, 1.764394620056912055, 0.1386062191098563767 ) ) ;
#77363=CARTESIAN_POINT ( 'NONE',  ( 6.240799290569317925, 1.728800370330787928, -0.1372766232172056844 ) ) ;
#77364=CARTESIAN_POINT ( 'NONE',  ( 5.601031023413125531, -0.4148525734360584138, 1.690157204064596019 ) ) ;
#77365=CARTESIAN_POINT ( 'NONE',  ( 2.577988946098773049, -1.175687941515238588, 1.967785589457039741 ) ) ;
#77367=CARTESIAN_POINT ( 'NONE',  ( 2.431387202150552707, 0.8680758514147070004, -1.623638265414374171 ) ) ;
#77370=CARTESIAN_POINT ( 'NONE',  ( 2.467563089314188662, 1.790814366166630034, -0.3536809140580049471 ) ) ;
#77373=CARTESIAN_POINT ( 'NONE',  ( 4.594815077023072902, -0.4589311638903668111, -2.055181093106945855 ) ) ;
#77376=CARTESIAN_POINT ( 'NONE',  ( 2.031770498437397876, 1.981864486777328294, -0.5989037013024376410 ) ) ;
#77379=CARTESIAN_POINT ( 'NONE',  ( 4.530007735025624704, -2.079396993832134388, 0.4145621898983055109 ) ) ;
#77380=CARTESIAN_POINT ( 'NONE',  ( 0.06489154195065281738, -1.720053269671377949, -0.8678208687467499072 ) ) ;
#77387=CARTESIAN_POINT ( 'NONE',  ( -0.01689291694152022724, -1.444339507245323118, 1.687895485215410885 ) ) ;
#77388=CARTESIAN_POINT ( 'NONE',  ( 1.624194961551369776, -1.169474557214383870, -1.751182684644275289 ) ) ;
#77391=CARTESIAN_POINT ( 'NONE',  ( 5.840631046605349042, -1.815184518647503742, -0.4092948386957768747 ) ) ;
#77397=CARTESIAN_POINT ( 'NONE',  ( -0.1225938595818750754, -1.897163925677572305, -0.9476133185889324961 ) ) ;
#77400=CARTESIAN_POINT ( 'NONE',  ( 2.717183929654675811, -1.705535211757349456, -0.9694657131227711888 ) ) ;
#77401=CARTESIAN_POINT ( 'NONE',  ( 0.8487565004985967443, 0.6285140637429244004, 2.068326486519965979 ) ) ;
#77405=CARTESIAN_POINT ( 'NONE',  ( 3.092811855500672280, 0.9656183884470933565, -1.439801824928796048 ) ) ;
#77406=CARTESIAN_POINT ( 'NONE',  ( 1.956607802488403269, 0.2990611944714368642, -1.714256857270479051 ) ) ;
#77410=CARTESIAN_POINT ( 'NONE',  ( 2.407577179044288584, 0.4389615990625857500, 1.967586618684707522 ) ) ;
#77411=CARTESIAN_POINT ( 'NONE',  ( 6.825078400183552496, 6.035069422732725286, 2.639236294420511442 ) ) ;
#77414=CARTESIAN_POINT ( 'NONE',  ( 1.727351915365995083, -1.857048012799527248, 0.6622322079550806428 ) ) ;
#77416=CARTESIAN_POINT ( 'NONE',  ( 5.238497809344139000, 1.134185964801931679, -1.539638564045166857 ) ) ;
#77421=CARTESIAN_POINT ( 'NONE',  ( 1.014326189163064607, -2.019862491587170350, 0.002270882547714125031 ) ) ;
#77423=CARTESIAN_POINT ( 'NONE',  ( 5.544061457994609476, 0.9416624597364110505, -2.106895457712253616 ) ) ;
#77424=CARTESIAN_POINT ( 'NONE',  ( 6.057081135787192316, 1.604708697955498087, -1.128374156723031430 ) ) ;
#77425=CARTESIAN_POINT ( 'NONE',  ( 3.432423435979839343, -1.172226468724973936, 1.572839002276872566 ) ) ;
#77427=CARTESIAN_POINT ( 'NONE',  ( 0.2467204944939948852, 1.994070950632735428, -0.2986300710981006357 ) ) ;
#77429=CARTESIAN_POINT ( 'NONE',  ( 1.182980447155062453, 1.727502145113229970, -1.224025170244628757 ) ) ;
#77432=CARTESIAN_POINT ( 'NONE',  ( 2.044624030687072214, -1.478315374303545093, -1.097237131862264903 ) ) ;
#77435=CARTESIAN_POINT ( 'NONE',  ( 3.252298345715322281, 0.9499829135306799843, -1.895951488860507128 ) ) ;
#77439=CARTESIAN_POINT ( 'NONE',  ( 2.671226777604285729, 0.1043416919609811144, -2.058284026376159925 ) ) ;
#77441=FACE_OUTER_BOUND ( 'NONE', #109097, .T. ) ;
#77443=CARTESIAN_POINT ( 'NONE',  ( -0.02244404828160086532, 2.859736408857795009, -2.677210243787793598 ) ) ;
#77445=CARTESIAN_POINT ( 'NONE',  ( 0.2763675079364875664, 1.274320874971252460, 1.801605125401319007 ) ) ;
#77446=CARTESIAN_POINT ( 'NONE',  ( 2.653932422735814978, 0.6056841677779849498, -2.179737047031413244 ) ) ;
#77448=CARTESIAN_POINT ( 'NONE',  ( 3.023486134662889402, -0.3489238238089559241, 1.777470660238470224 ) ) ;
#77450=CARTESIAN_POINT ( 'NONE',  ( 3.520622370129117940, 0.2863239327370070697, 1.894091974173327531 ) ) ;
#77451=CARTESIAN_POINT ( 'NONE',  ( 3.736834853878097107, -1.994506513866915576, -0.5549897870569252545 ) ) ;
#77453=CARTESIAN_POINT ( 'NONE',  ( 1.780087957478289074, -1.056366978776434484, 1.664393130878606852 ) ) ;
#77454=CARTESIAN_POINT ( 'NONE',  ( 6.305299685587768543, 1.603216850002240124, 1.067941234924398852 ) ) ;
#77455=CARTESIAN_POINT ( 'NONE',  ( 3.221420234344949840, -1.803205065257794004, 0.4975683872451354683 ) ) ;
#77456=CARTESIAN_POINT ( 'NONE',  ( 2.614278096488438674, -2.282406316997650286, 0.3399710349294912115 ) ) ;
#77458=CARTESIAN_POINT ( 'NONE',  ( 2.506119797010537997, 1.860588423725167306, 0.04906839929019050223 ) ) ;
#77460=CARTESIAN_POINT ( 'NONE',  ( 6.496538660071067284, 2.039668932145132008, 0.3065683105917779705 ) ) ;
#77464=CARTESIAN_POINT ( 'NONE',  ( 0.08283480907551789285, -2.043431366640800384, -0.5094137356045270737 ) ) ;
#77466=CARTESIAN_POINT ( 'NONE',  ( 5.800121417639972243, -2.161773191644947634, -0.006422599366645573467 ) ) ;
#77467=CARTESIAN_POINT ( 'NONE',  ( 6.604167511870285168, -0.8622997358492515696, 1.824817093501039267 ) ) ;
#77474=CARTESIAN_POINT ( 'NONE',  ( -0.2104748580754201293, 5.720428293583295520, -2.697747842008205943 ) ) ;
#77475=CARTESIAN_POINT ( 'NONE',  ( 4.926970384345759513, -1.727065721694167832, 1.040790168839386798 ) ) ;
#77480=CARTESIAN_POINT ( 'NONE',  ( 6.385629968321593353, 1.486944277142748572, 1.569300510047972219 ) ) ;
#77485=CARTESIAN_POINT ( 'NONE',  ( 0.4037314067151754893, -1.025472807287574506, -1.617813098647686632 ) ) ;
#77488=CARTESIAN_POINT ( 'NONE',  ( 2.050978400279603875, -1.384275906022333968, -1.028850351009907849 ) ) ;
#77492=CARTESIAN_POINT ( 'NONE',  ( 1.317257508235271102, -1.728110672573167639, 0.3808341387830004865 ) ) ;
#77493=CARTESIAN_POINT ( 'NONE',  ( 1.682290626080079621, 1.036857497476886936, 1.725414394560653042 ) ) ;
#77495=CARTESIAN_POINT ( 'NONE',  ( 4.102700518754747172, -0.6894086160392081108, -2.096397988278507096 ) ) ;
#77496=CARTESIAN_POINT ( 'NONE',  ( 5.735278773323231327, -0.04571225511484919291, -2.170743740471086980 ) ) ;
#77500=CARTESIAN_POINT ( 'NONE',  ( 2.842561206135377994, 1.176089095116246153, -1.764248410475676820 ) ) ;
#77501=CARTESIAN_POINT ( 'NONE',  ( 3.023064714212614135, -1.777003028299545484, 0.9530295004822467719 ) ) ;
#77502=CARTESIAN_POINT ( 'NONE',  ( 3.164119808340008611, 1.811767227632065325, -0.004774541488360150264 ) ) ;
#77506=CARTESIAN_POINT ( 'NONE',  ( 0.7252172114964609007, -1.777616610744123804, 0.5828384007960025759 ) ) ;
#77508=CARTESIAN_POINT ( 'NONE',  ( 6.516225534515442952, -0.8655890497146904172, -1.607451055071248636 ) ) ;
#77510=CARTESIAN_POINT ( 'NONE',  ( 1.094790513324794601, 1.691201413147478183, 0.8998118624304138891 ) ) ;
#77516=CARTESIAN_POINT ( 'NONE',  ( 5.120075222393803749, -1.153228217640640985, -1.828211184805514700 ) ) ;
#77520=CARTESIAN_POINT ( 'NONE',  ( 3.234745892528373634, 1.342314639517484087, -1.641720766639112039 ) ) ;
#77523=CARTESIAN_POINT ( 'NONE',  ( 4.059811131046401123, 1.956822991617146457, -0.2382644796226577599 ) ) ;
#77524=CARTESIAN_POINT ( 'NONE',  ( 6.416268857797894576, -1.911816439625917852, 0.05404522429636184067 ) ) ;
#77526=CARTESIAN_POINT ( 'NONE',  ( 5.542236361656130761, 0.8606211682868989410, 1.934736125387125361 ) ) ;
#77527=CARTESIAN_POINT ( 'NONE',  ( 0.8716356842100521085, -0.3054578492302991721, 2.047597563663336118 ) ) ;
#77528=CARTESIAN_POINT ( 'NONE',  ( 2.273291157499750526, 1.194718917728957885, 1.530869066462538619 ) ) ;
#77532=CARTESIAN_POINT ( 'NONE',  ( 3.187526948619547884, -0.8467841439671991433, 1.911654264539459191 ) ) ;
#77535=CARTESIAN_POINT ( 'NONE',  ( 0.1350377444619410283, -0.09094779274463302143, 1.809295058508665566 ) ) ;
#77537=CARTESIAN_POINT ( 'NONE',  ( 5.777994779145079640, 1.311685685134782231, 1.774619457157788904 ) ) ;
#77539=CARTESIAN_POINT ( 'NONE',  ( 3.030518406005321186, 1.227118389542979804, -1.833929004854919276 ) ) ;
#77542=CARTESIAN_POINT ( 'NONE',  ( 2.191926089937683564, 1.177725938178806997, 1.506473034612793915 ) ) ;
#77544=CARTESIAN_POINT ( 'NONE',  ( 5.846161131210033446, -0.9342735719010831774, 1.847668428805064655 ) ) ;
#77546=CARTESIAN_POINT ( 'NONE',  ( 3.133815226704575796, -1.450665623810345473, -1.602838778681405785 ) ) ;
#77547=CARTESIAN_POINT ( 'NONE',  ( 4.880524338131243312, -0.2681524694418158661, -2.175044001020635331 ) ) ;
#77549=CARTESIAN_POINT ( 'NONE',  ( -0.02948999725180654480, 0.001137248348246934970, -1.926291057026579434 ) ) ;
#77556=CARTESIAN_POINT ( 'NONE',  ( 0.8267963299631932994, 0.8146243292815741333, -1.844710905833810255 ) ) ;
#77559=CARTESIAN_POINT ( 'NONE',  ( 6.104363016364067640, 2.067617457866403718, 0.1074407263862015016 ) ) ;
#77560=CARTESIAN_POINT ( 'NONE',  ( 4.055238279289786973, -1.602352113334176043, -1.069235405101864878 ) ) ;
#77561=CARTESIAN_POINT ( 'NONE',  ( 6.573823534745116604, -0.9041686956474543901, 1.912245183953432237 ) ) ;
#77566=CARTESIAN_POINT ( 'NONE',  ( 3.678522182247864869, 1.252989934047860965, -1.519404455180313640 ) ) ;
#77567=CARTESIAN_POINT ( 'NONE',  ( 0.5334774086375413393, -1.552487152004313087, -1.546944964277228607 ) ) ;
#77568=CARTESIAN_POINT ( 'NONE',  ( 3.633261591126951018, -1.686358373764598406, 0.7000054678709469735 ) ) ;
#77574=CARTESIAN_POINT ( 'NONE',  ( 1.223879446662301307, 1.774596971308094018, 0.4907264878865265634 ) ) ;
#77575=CARTESIAN_POINT ( 'NONE',  ( 4.658451966079163675, 2.008086622728368464, 0.1439865329972197516 ) ) ;
#77576=CARTESIAN_POINT ( 'NONE',  ( 1.159977488309314797, -0.5597072352675269702, -2.229110579909891143 ) ) ;
#77577=CARTESIAN_POINT ( 'NONE',  ( 5.330891710049517229, -1.845885424482188286, -0.6645199359083459045 ) ) ;
#77581=CARTESIAN_POINT ( 'NONE',  ( 0.3794556558127279988, -0.1030994254981997954, 2.067933115924729837 ) ) ;
#77583=CARTESIAN_POINT ( 'NONE',  ( 1.364907732811880159, 0.1502005422731657047, -2.085395908040136526 ) ) ;
#77584=CARTESIAN_POINT ( 'NONE',  ( 6.578955313817166584, -0.09182192948648319752, -1.767577901409943086 ) ) ;
#77586=CARTESIAN_POINT ( 'NONE',  ( -0.1102773484823885153, 6.947233595868168798, -2.798541112319170576 ) ) ;
#77587=CARTESIAN_POINT ( 'NONE',  ( 1.592878374036447164, -0.5866614404700842833, 1.638733785964431755 ) ) ;
#77590=CARTESIAN_POINT ( 'NONE',  ( 2.103723633838894713, -1.724574586359624906, 0.04069764719066489012 ) ) ;
#77591=CARTESIAN_POINT ( 'NONE',  ( 1.839652601550560096, 0.8350199954420146620, -2.026445374841173930 ) ) ;
#77592=CARTESIAN_POINT ( 'NONE',  ( 0.08792998612136559977, -0.4660014661636499578, 1.670295066556278352 ) ) ;
#77593=CARTESIAN_POINT ( 'NONE',  ( 4.055453297694236348, -1.834216022232620702, -1.226887332174103173 ) ) ;
#77595=CARTESIAN_POINT ( 'NONE',  ( 2.272564004159416395, -1.020438428401538200, -1.916272530736246926 ) ) ;
#77596=CARTESIAN_POINT ( 'NONE',  ( 1.611646134362737959, -1.812087876328593916, 0.2219229778191167957 ) ) ;
#77597=CARTESIAN_POINT ( 'NONE',  ( 2.958335891534333850, -1.257395014299323988, 1.703445231074371291 ) ) ;
#77598=CARTESIAN_POINT ( 'NONE',  ( 6.539320575229274901, 7.053161517996441532, 2.494893549996656912 ) ) ;
#77600=CARTESIAN_POINT ( 'NONE',  ( 3.825942575589100780, 1.225831451615842393, -1.936910307245596652 ) ) ;
#77604=CARTESIAN_POINT ( 'NONE',  ( 5.848318881832833327, 1.097015000334870649, -1.931420017644119635 ) ) ;
#77612=CARTESIAN_POINT ( 'NONE',  ( 4.113907844847329187, 0.1017495355152969322, 2.013985960686740295 ) ) ;
#77614=CARTESIAN_POINT ( 'NONE',  ( 2.289955638094377299, -1.343889277006144356, -1.564782475634781900 ) ) ;
#77619=CARTESIAN_POINT ( 'NONE',  ( 4.734432829848630675, 0.3728853646711489112, 2.159338447334692823 ) ) ;
#77620=CARTESIAN_POINT ( 'NONE',  ( 2.584611472894111195, -0.6298744119781033435, 1.915600275669691488 ) ) ;
#77621=CARTESIAN_POINT ( 'NONE',  ( 2.120424178990498731, 0.001545453418709194504, 1.841430844159386293 ) ) ;
#77624=CARTESIAN_POINT ( 'NONE',  ( 6.739283625173963621, -1.628968703954777553, 0.8242606506234579911 ) ) ;
#77625=CARTESIAN_POINT ( 'NONE',  ( 0.2824055751470951892, 1.906470811695348599, -1.284064767653005257 ) ) ;
#77627=CARTESIAN_POINT ( 'NONE',  ( 5.260715670973223901, -1.642634774727338653, 1.556112085687613611 ) ) ;
#77629=CARTESIAN_POINT ( 'NONE',  ( 1.770285920821415449, 1.083698108115097591, 1.805711900068427411 ) ) ;
#77639=CARTESIAN_POINT ( 'NONE',  ( 1.705496241919310707, 1.842552997918958768, -1.049655202612943095 ) ) ;
#77640=CARTESIAN_POINT ( 'NONE',  ( 2.356001076229676805, -1.649452400593539148, -1.488157709660995920 ) ) ;
#77641=CARTESIAN_POINT ( 'NONE',  ( 0.5927436934281338221, -2.190715567557582677, -0.2661302102612560505 ) ) ;
#77644=CARTESIAN_POINT ( 'NONE',  ( 4.721123852359588646, -1.751549048416237486, -0.8839179009662299080 ) ) ;
#77652=CARTESIAN_POINT ( 'NONE',  ( 3.445663904809421307, -1.957918079443463855, 0.8150281543025169606 ) ) ;
#77654=CARTESIAN_POINT ( 'NONE',  ( 4.786082296487640164, -1.021991182799499409, 1.904868704497929333 ) ) ;
#77655=CARTESIAN_POINT ( 'NONE',  ( 3.913478945735289205, -0.9499487412085620974, -1.577145280185827447 ) ) ;
#77658=CARTESIAN_POINT ( 'NONE',  ( 5.314300430047540935, 1.610136290765556977, 0.6609758457527656894 ) ) ;
#77663=CARTESIAN_POINT ( 'NONE',  ( 3.520547545725543515, 1.372905562624787024, -1.669742455111824286 ) ) ;
#77665=CARTESIAN_POINT ( 'NONE',  ( 5.589220178194088895, 1.203167956798111060, -1.617571559180859486 ) ) ;
#77667=CARTESIAN_POINT ( 'NONE',  ( 2.817419395390472037, -0.2130390993498078311, 2.151187356804876050 ) ) ;
#77668=CARTESIAN_POINT ( 'NONE',  ( 3.585193993258027678, 1.783571249345828003, -0.8399556444593555549 ) ) ;
#77669=CARTESIAN_POINT ( 'NONE',  ( 0.1170720436180875679, -0.1011795954627830590, 2.189343785608413917 ) ) ;
#77670=CARTESIAN_POINT ( 'NONE',  ( 4.335450565170337001, 0.8274041267214229389, -1.757107282799404091 ) ) ;
#77679=CARTESIAN_POINT ( 'NONE',  ( 2.046200460737709559, 0.8445575735530999051, -2.038961412367201298 ) ) ;
#77681=CARTESIAN_POINT ( 'NONE',  ( 6.438335799692933570, -1.052282694883142078, 1.655480336553965648 ) ) ;
#77686=CARTESIAN_POINT ( 'NONE',  ( 5.936183876523434932, 1.091049494364674466, -1.918236432931222257 ) ) ;
#77687=CARTESIAN_POINT ( 'NONE',  ( 5.068220161613846031, -1.734768455660203434, -0.6171159064975312303 ) ) ;
#77695=CARTESIAN_POINT ( 'NONE',  ( 6.151650338133601181, 0.6026783403972060249, -1.970659962842249424 ) ) ;
#77697=CARTESIAN_POINT ( 'NONE',  ( 2.013881029938934919, 1.856366682828480608, -0.1327402387825328822 ) ) ;
#77698=CARTESIAN_POINT ( 'NONE',  ( 3.702549152423353807, 1.581054339307564449, 0.9433870219286569769 ) ) ;
#77705=CARTESIAN_POINT ( 'NONE',  ( 3.791807063958370971, 1.597966631936774684, 1.522356218736670153 ) ) ;
#77706=CARTESIAN_POINT ( 'NONE',  ( 6.151720675889260193, 0.6653518678880927517, -2.162357237652327679 ) ) ;
#77708=CARTESIAN_POINT ( 'NONE',  ( 6.345981700719151242, -1.190820116993321243, -1.365292378351635083 ) ) ;
#77709=CARTESIAN_POINT ( 'NONE',  ( -0.1531117392989979065, -1.803405091603600185, -0.9023890051431044945 ) ) ;
#77711=CARTESIAN_POINT ( 'NONE',  ( 6.262560305340551636, -1.321439916381482060, 1.324322166508178356 ) ) ;
#77712=CARTESIAN_POINT ( 'NONE',  ( 5.813130153884224605, 1.560705751063670377, -1.104717755519408984 ) ) ;
#77714=CARTESIAN_POINT ( 'NONE',  ( 0.8482696660519238874, 0.5391449902514727777, 1.791282564952957124 ) ) ;
#77715=CARTESIAN_POINT ( 'NONE',  ( 0.9718890779336667451, -0.9023411006064323558, 1.803417998987096427 ) ) ;
#77717=CARTESIAN_POINT ( 'NONE',  ( 4.354198888085320185, 2.105621147513780045, -0.05115374888297812700 ) ) ;
#77723=CARTESIAN_POINT ( 'NONE',  ( 3.551039915000217206, 0.3004019028194653829, 1.997212655505080203 ) ) ;
#77727=CARTESIAN_POINT ( 'NONE',  ( 3.058072297120766336, 2.151488047868503894, -0.2085137855245971505 ) ) ;
#77733=CARTESIAN_POINT ( 'NONE',  ( 0.9597157272863182653, 1.774996621215488624, 1.250093255441329543 ) ) ;
#77738=CARTESIAN_POINT ( 'NONE',  ( 2.349409277133751139, 0.5813161652389825518, -2.113004480973964760 ) ) ;
#77739=CARTESIAN_POINT ( 'NONE',  ( 6.983263157960360346, 2.057644363497754814, 2.260506123227977948 ) ) ;
#77740=CARTESIAN_POINT ( 'NONE',  ( 2.342968712349004168, 0.4955985968413346709, 2.207426715909040826 ) ) ;
#77747=CARTESIAN_POINT ( 'NONE',  ( 3.936565515923634795, 0.2574710272360211105, 1.750749954138763442 ) ) ;
#77749=CARTESIAN_POINT ( 'NONE',  ( 0.7980485993467776318, -0.7579980429349441051, 1.964993406121709807 ) ) ;
#77753=CARTESIAN_POINT ( 'NONE',  ( 6.222279831957800766, 1.994873610751911164, 0.2930524845206964879 ) ) ;
#77756=CARTESIAN_POINT ( 'NONE',  ( 3.151090109352538082, -1.528452604574185525, -1.078222621661927061 ) ) ;
#77757=CARTESIAN_POINT ( 'NONE',  ( 4.926661076633905623, -1.356332079400805135, 1.564123780295342492 ) ) ;
#77766=CARTESIAN_POINT ( 'NONE',  ( 4.351973852746993110, -0.7528527933186466292, 1.811862133468461922 ) ) ;
#77768=CARTESIAN_POINT ( 'NONE',  ( 0.8431247865267020858, -1.122328847578180078, 1.674629589540656216 ) ) ;
#77772=CARTESIAN_POINT ( 'NONE',  ( 1.229531971273215341, -1.182229855178434930, -1.449605969065965949 ) ) ;
#77774=CARTESIAN_POINT ( 'NONE',  ( 2.777592571122803555, 0.2913108041502753820, -1.991885045997557224 ) ) ;
#77776=CARTESIAN_POINT ( 'NONE',  ( 2.320046401798322222, 0.9952771033397389555, -1.868693074688542843 ) ) ;
#77778=CARTESIAN_POINT ( 'NONE',  ( 3.473154722801426786, 1.870513717286937494, 0.8877811045280564750 ) ) ;
#77780=CARTESIAN_POINT ( 'NONE',  ( 0.2223640086436579066, 2.001884549173582606, 0.6031067468692548061 ) ) ;
#77782=CARTESIAN_POINT ( 'NONE',  ( 5.649374308873757577, -1.440485763676568443, -1.121356984487072328 ) ) ;
#77789=CARTESIAN_POINT ( 'NONE',  ( 5.127564033545165323, -0.2766344828325461580, 1.892035409188079997 ) ) ;
#77797=ORIENTED_EDGE ( 'NONE', *, *, #78667, .F. ) ;
#77801=FILL_AREA_STYLE_COLOUR ( '', #143836 ) ;
#77805=CARTESIAN_POINT ( 'NONE',  ( 2.606253914610905387, 1.968914028630329272, 0.05319026939461755227 ) ) ;
#77806=CARTESIAN_POINT ( 'NONE',  ( 3.005482631727268039, -1.942536929278560365, 0.5405117225928540714 ) ) ;
#77809=CARTESIAN_POINT ( 'NONE',  ( 6.827182134110222123, 7.629137130509067610, 2.789055895399249252 ) ) ;
#77810=CARTESIAN_POINT ( 'NONE',  ( 3.556733441538503016, -1.932615445784117369, -1.033156731641969195 ) ) ;
#77812=CARTESIAN_POINT ( 'NONE',  ( 2.344641424807081709, 0.4199494819796690814, 1.879913682802894614 ) ) ;
#77814=CARTESIAN_POINT ( 'NONE',  ( 0.1331565106231363538, 2.033293680964400885, -2.362282156872722805 ) ) ;
#77820=VERTEX_POINT ( 'NONE', #149363 ) ;
#77821=CARTESIAN_POINT ( 'NONE',  ( 6.022987620897008121, -1.731432113864934674, 0.6267441317700100933 ) ) ;
#77822=CARTESIAN_POINT ( 'NONE',  ( 1.242838715397933225, 1.940741670474394498, 0.5346661475282618037 ) ) ;
#77823=CARTESIAN_POINT ( 'NONE',  ( 4.640180047935675844, 0.006009439367033602396, -2.298542322207643984 ) ) ;
#77824=CARTESIAN_POINT ( 'NONE',  ( -0.02919842301645457147, 6.946858002156226064, -2.668856405631584217 ) ) ;
#77825=CARTESIAN_POINT ( 'NONE',  ( 2.043593076603223757, 1.278923709890807503, 1.352104710524345554 ) ) ;
#77827=CARTESIAN_POINT ( 'NONE',  ( -0.1290005225502641184, 1.996213967822700663, -2.587563282167547385 ) ) ;
#77828=CARTESIAN_POINT ( 'NONE',  ( 5.133030909251353968, 1.769313487831367659, 0.7262901588861517821 ) ) ;
#77831=CARTESIAN_POINT ( 'NONE',  ( 4.458587642939345841, -1.868375113230103857, -0.9383987773294580892 ) ) ;
#77832=CARTESIAN_POINT ( 'NONE',  ( 3.502682687546424312, 1.475339254275360279, -1.149998991230333223 ) ) ;
#77837=CARTESIAN_POINT ( 'NONE',  ( 6.270102258788001315, 0.8933021238881621029, 1.475393591635131507 ) ) ;
#77839=CARTESIAN_POINT ( 'NONE',  ( 1.300929835083320274, 1.165380355416269609, -1.284392162598305021 ) ) ;
#77842=CARTESIAN_POINT ( 'NONE',  ( 6.051681997923831879, 1.638823605779341053, 1.424080724270002873 ) ) ;
#77843=CARTESIAN_POINT ( 'NONE',  ( 4.406759617291758246, 1.409692282476209924, -1.160130723419292353 ) ) ;
#77844=CARTESIAN_POINT ( 'NONE',  ( 1.832786370036399326, -1.861117592713131819, -0.6203919267877274768 ) ) ;
#77845=CARTESIAN_POINT ( 'NONE',  ( 0.6150561885070615631, 0.1604698007556179251, 2.111222410368835067 ) ) ;
#77849=CARTESIAN_POINT ( 'NONE',  ( 2.842561206135377994, 1.176089095116246153, -1.764248410475676820 ) ) ;
#77854=CARTESIAN_POINT ( 'NONE',  ( 0.2333690889706682703, 0.003390530909083006028, -2.053566628440507635 ) ) ;
#77858=CARTESIAN_POINT ( 'NONE',  ( 3.545754021904829134, -2.051903114543842666, 0.8512574589945339776 ) ) ;
#77860=CARTESIAN_POINT ( 'NONE',  ( 0.5108563537194388271, -2.180326652049785707, 0.7283127579034570642 ) ) ;
#77862=CARTESIAN_POINT ( 'NONE',  ( 5.014538805069497229, 0.7844730879308317029, 1.907755517398136647 ) ) ;
#77866=CARTESIAN_POINT ( 'NONE',  ( 5.144037045698616417, 0.5398437887287730330, 1.760322748975438500 ) ) ;
#77870=CARTESIAN_POINT ( 'NONE',  ( 2.871755265489631448, 0.9208624611983186048, 1.458155879698035395 ) ) ;
#77871=CARTESIAN_POINT ( 'NONE',  ( 1.007046422456716384, -0.04465021774549028655, 2.016188868504041665 ) ) ;
#77873=CARTESIAN_POINT ( 'NONE',  ( 2.848558797923263164, 0.3346648989216906012, -2.274091979294257992 ) ) ;
#77875=CARTESIAN_POINT ( 'NONE',  ( 2.636292518416444075, 1.068738387235500298, -1.994089298797457666 ) ) ;
#77876=CARTESIAN_POINT ( 'NONE',  ( 5.145193760806440864, -1.806914327231067929, 1.081695767794567775 ) ) ;
#77878=CARTESIAN_POINT ( 'NONE',  ( 3.444378845967084324, 0.4270997545614327318, 1.717301222563255791 ) ) ;
#77881=CARTESIAN_POINT ( 'NONE',  ( 5.987847201643853978, -2.280908734910926938, -0.2287418647285797413 ) ) ;
#77882=CARTESIAN_POINT ( 'NONE',  ( 4.083814069670049562, -1.821384084514931612, -0.2681248149544179227 ) ) ;
#77887=CARTESIAN_POINT ( 'NONE',  ( 4.136819237485493517, -1.907179771870757046, 1.079280405373375773 ) ) ;
#77892=CARTESIAN_POINT ( 'NONE',  ( 3.545458749278436184, -1.459459766114965973, -1.257631776117454914 ) ) ;
#77895=CARTESIAN_POINT ( 'NONE',  ( 6.504144398916748671, -0.9053081408615070158, 1.915699539216948688 ) ) ;
#77902=CARTESIAN_POINT ( 'NONE',  ( 0.5023040531197673353, 1.956348610274569744, 0.1481081594910879096 ) ) ;
#77905=CARTESIAN_POINT ( 'NONE',  ( 6.825078400183575589, -0.005632053428735600553, 2.144262460745151255 ) ) ;
#77907=CARTESIAN_POINT ( 'NONE',  ( 5.318788500806308051, -1.422220495204097546, 1.351624447685224162 ) ) ;
#77911=CARTESIAN_POINT ( 'NONE',  ( 5.348557406608104969, 0.6236849695623291057, 2.069784783864880851 ) ) ;
#77912=CARTESIAN_POINT ( 'NONE',  ( -0.2104748580754426390, 2.865278511227668634, -2.591885361450113834 ) ) ;
#77915=CARTESIAN_POINT ( 'NONE',  ( 0.4736314445139556684, 1.071599637473351629, 1.532994764490814177 ) ) ;
#77916=CARTESIAN_POINT ( 'NONE',  ( 5.958250847983307175, 1.314789979124462382, 1.130330842948763514 ) ) ;
#77918=CARTESIAN_POINT ( 'NONE',  ( 3.157961424266928052, 0.9873743524775533409, 1.956624655947765357 ) ) ;
#77919=CARTESIAN_POINT ( 'NONE',  ( 2.872455039471259575, 1.233635154574242554, 1.949979759383664524 ) ) ;
#77920=CARTESIAN_POINT ( 'NONE',  ( 6.046181036401986120, 2.058226046012123334, 0.1054989004632029409 ) ) ;
#77921=CARTESIAN_POINT ( 'NONE',  ( 1.253738886202176106, 0.7867099759248905588, 1.775636482627058088 ) ) ;
#77926=CARTESIAN_POINT ( 'NONE',  ( 4.746395313581045272, 1.087821826000658909, -1.820160695957805608 ) ) ;
#77928=CARTESIAN_POINT ( 'NONE',  ( 2.356092462967720458, 0.09613450340887133572, -2.014232768679749430 ) ) ;
#77930=CARTESIAN_POINT ( 'NONE',  ( 5.561621765989873900, 0.4355406452380207738, -2.163202247768724718 ) ) ;
#77933=CARTESIAN_POINT ( 'NONE',  ( 0.4338677482375961070, 0.9413943332680120291, -1.564114433284753636 ) ) ;
#77939=CARTESIAN_POINT ( 'NONE',  ( 4.118082307656718122, -1.057753326809774963, -1.768578378466668877 ) ) ;
#77944=CARTESIAN_POINT ( 'NONE',  ( 4.248697963213067474, 1.981114831247460017, 0.3918398546494082368 ) ) ;
#77949=CARTESIAN_POINT ( 'NONE',  ( 2.975518139630950021, 1.957357868463033501, -0.6452315760040390202 ) ) ;
#77950=CARTESIAN_POINT ( 'NONE',  ( 2.953750172290267706, -1.864168560446223033, -0.7691209412190866956 ) ) ;
#77956=CARTESIAN_POINT ( 'NONE',  ( 2.882185300971401798, -0.2004049647258976941, 2.006138917898095730 ) ) ;
#77957=CARTESIAN_POINT ( 'NONE',  ( 2.923586578878138109, 1.022379729796508041, -1.530975008504284141 ) ) ;
#77958=CARTESIAN_POINT ( 'NONE',  ( 1.102667438898880192, -2.307868968971817036, 0.004735511273680144059 ) ) ;
#77960=CARTESIAN_POINT ( 'NONE',  ( 2.319794969891198821, -2.097318901067245722, 0.5227781780692899449 ) ) ;
#77962=CARTESIAN_POINT ( 'NONE',  ( 2.636409100479879086, 0.1147267580069409321, -2.295643959171574711 ) ) ;
#77965=CARTESIAN_POINT ( 'NONE',  ( 1.481098450213329976, 1.729700800547562478, -0.7128637423776186255 ) ) ;
#77966=CARTESIAN_POINT ( 'NONE',  ( 5.278184311449350297, -1.095828550124495981, 1.638662057970756925 ) ) ;
#77970=CARTESIAN_POINT ( 'NONE',  ( 0.1884680354247054990, -1.036234488384666586, 1.948478269905975946 ) ) ;
#77971=CARTESIAN_POINT ( 'NONE',  ( 6.812946544903684121, -1.603000239855886466, 1.309962327488790157 ) ) ;
#77975=CARTESIAN_POINT ( 'NONE',  ( 4.487161871577921346, 1.761403164857084702, -0.8856326919300193667 ) ) ;
#77976=CARTESIAN_POINT ( 'NONE',  ( 0.01804983835817890528, -0.5593552815991027494, 2.045460531183339814 ) ) ;
#77978=CARTESIAN_POINT ( 'NONE',  ( 4.653107873243750525, -1.855428480829583338, 1.371977642438865885 ) ) ;
#77979=CARTESIAN_POINT ( 'NONE',  ( 1.709910653088747789, 0.6025335139634242498, -1.972566668331069195 ) ) ;
#77987=CARTESIAN_POINT ( 'NONE',  ( 4.703694880604158968, -1.675542544088706620, -1.380765677988102791 ) ) ;
#77990=CARTESIAN_POINT ( 'NONE',  ( 4.370544011308346910, -0.004580445953385886559, -1.841430844414258861 ) ) ;
#77992=CARTESIAN_POINT ( 'NONE',  ( 6.720655732516649827, 7.053635520514346169, 2.324416633011537225 ) ) ;
#77993=CARTESIAN_POINT ( 'NONE',  ( 5.249643141573060667, 2.189086832579402842, -0.1069518675670885766 ) ) ;
#77995=CARTESIAN_POINT ( 'NONE',  ( 5.840765815766128632, 0.4347934677991367458, 2.220198762108383850 ) ) ;
#78001=CARTESIAN_POINT ( 'NONE',  ( 0.3909914118310651165, 1.306912223127455919, 1.193654972778479539 ) ) ;
#78002=CARTESIAN_POINT ( 'NONE',  ( 5.303390062791992321, 1.774253655011595709, -0.9511161165304935494 ) ) ;
#78004=CARTESIAN_POINT ( 'NONE',  ( 3.891714145839750838, 1.523869777361567479, 1.453819373739003051 ) ) ;
#78005=CARTESIAN_POINT ( 'NONE',  ( 2.179167455442470480, 1.482148263166820801, 1.213602503745815353 ) ) ;
#78007=CARTESIAN_POINT ( 'NONE',  ( 3.473067387030086994, 1.779531822584624834, 0.8443681024216052045 ) ) ;
#78008=CARTESIAN_POINT ( 'NONE',  ( 5.994400513263062891, -1.076938050528394308, 1.708516719617196422 ) ) ;
#78009=CARTESIAN_POINT ( 'NONE',  ( 1.217418975555501826, -1.825842229346545498, 0.4062821374252246764 ) ) ;
#78010=CARTESIAN_POINT ( 'NONE',  ( 5.549328304323321248, -1.363462989569711681, -1.056374310239334591 ) ) ;
#78011=CARTESIAN_POINT ( 'NONE',  ( 1.793074957647671663, -0.09724762972821224261, -1.910064080951429100 ) ) ;
#78013=CARTESIAN_POINT ( 'NONE',  ( 1.348561525465460820, 2.204488851003219896, 0.1053889787279923829 ) ) ;
#78021=CARTESIAN_POINT ( 'NONE',  ( 1.522023487246677798, 2.040062638832959241, -0.3519594530456415793 ) ) ;
#78027=CARTESIAN_POINT ( 'NONE',  ( 6.516280388114966904, -2.120036885061008292, 0.05137064186952475936 ) ) ;
#78033=CARTESIAN_POINT ( 'NONE',  ( 4.763045971468515383, -2.015604388477490350, -0.05228862439247972116 ) ) ;
#78034=CARTESIAN_POINT ( 'NONE',  ( 4.276519664212295346, -0.4255873229474533281, -1.867665486979957157 ) ) ;
#78036=CARTESIAN_POINT ( 'NONE',  ( 2.577880719133851084, -1.123996537731044354, 1.881222605751430521 ) ) ;
#78039=CARTESIAN_POINT ( 'NONE',  ( 5.062748685862976217, 0.5883423404384033883, 1.925289297555386359 ) ) ;
#78043=CARTESIAN_POINT ( 'NONE',  ( 6.292584676692968948, 1.568786179414104032, -1.421969346915842092 ) ) ;
#78045=CARTESIAN_POINT ( 'NONE',  ( 3.632441420962172263, 0.3087965321501208726, 2.067699918487746036 ) ) ;
#78047=CARTESIAN_POINT ( 'NONE',  ( 1.975234724782324980, 1.651647476387863467, -0.4968862749653804589 ) ) ;
#78049=CARTESIAN_POINT ( 'NONE',  ( 4.922192346260839457, -2.110166376318895587, 0.2103620946037400852 ) ) ;
#78058=CARTESIAN_POINT ( 'NONE',  ( 1.945701609745503324, -1.183853311710543199, -1.371160031100856935 ) ) ;
#78064=CARTESIAN_POINT ( 'NONE',  ( 2.279683508022036342, 1.776238746767303978, -0.3545518163566608871 ) ) ;
#78065=CARTESIAN_POINT ( 'NONE',  ( 6.539320575229274901, 7.629137130509072051, 2.496737603865983424 ) ) ;
#78067=CARTESIAN_POINT ( 'NONE',  ( 4.299146511743386689, -1.619905129461503224, 0.9160139579608633786 ) ) ;
#78068=CARTESIAN_POINT ( 'NONE',  ( 1.054133004535224849, -1.214278006866207571, 1.481595424536867656 ) ) ;
#78069=CARTESIAN_POINT ( 'NONE',  ( 0.9557436305893592943, 1.823730570757615022, -0.08488363409227267509 ) ) ;
#78077=CARTESIAN_POINT ( 'NONE',  ( 5.453942691717160507, -0.7125396638749655898, 1.836196350841996949 ) ) ;
#78081=CARTESIAN_POINT ( 'NONE',  ( 0.3750906047784249853, 1.949931092985623726, -0.7544815049443721611 ) ) ;
#78083=CARTESIAN_POINT ( 'NONE',  ( 5.754890659886483739, -1.518548266084504439, 1.185242666505934572 ) ) ;
#78085=CARTESIAN_POINT ( 'NONE',  ( 1.781981981289095796, -0.9795585948506604357, 1.540336029244721461 ) ) ;
#78086=CARTESIAN_POINT ( 'NONE',  ( 2.614145488985010424, -2.182733025630137824, 0.3247920039054427721 ) ) ;
#78088=CARTESIAN_POINT ( 'NONE',  ( 0.1406777020166137260, 1.830675540527426648, 0.5531436448603862521 ) ) ;
#78089=CARTESIAN_POINT ( 'NONE',  ( 0.8187300819318241718, -1.428952508342665517, 1.355707701654704112 ) ) ;
#78090=CARTESIAN_POINT ( 'NONE',  ( 2.823698466604074309, 1.076742338344888639, -1.616048498441272407 ) ) ;
#78091=CARTESIAN_POINT ( 'NONE',  ( 0.3860920070548681804, -0.1017387759476989784, 2.013677428805898728 ) ) ;
#78093=CARTESIAN_POINT ( 'NONE',  ( 5.928513603989616243, -1.181800583780348468, 1.437463819671711995 ) ) ;
#78099=CARTESIAN_POINT ( 'NONE',  ( 1.417800074541092137, -1.221294057239637576, -1.819523406426680090 ) ) ;
#78103=CARTESIAN_POINT ( 'NONE',  ( 3.105874302609371362, -1.823586186413633126, 0.09019715141062728536 ) ) ;
#78109=CARTESIAN_POINT ( 'NONE',  ( 1.102032671262738850, -1.926676517669764443, -0.0008590682252854196007 ) ) ;
#78110=CARTESIAN_POINT ( 'NONE',  ( 5.840667439708360220, -1.913134005453724251, -0.4332900713753874977 ) ) ;
#78113=CARTESIAN_POINT ( 'NONE',  ( 4.810206850810132551, 1.511280187219691928, -1.587364365194674498 ) ) ;
#78115=CARTESIAN_POINT ( 'NONE',  ( 4.557524383921963462, 1.659614545607337677, 1.237363147772299721 ) ) ;
#78119=CARTESIAN_POINT ( 'NONE',  ( 4.149308075173010479, 1.083998706471595463, 2.027078093135482817 ) ) ;
#78124=CARTESIAN_POINT ( 'NONE',  ( 6.620655732516649294, 2.985444497229528427, 2.280274006979409407 ) ) ;
#78126=CARTESIAN_POINT ( 'NONE',  ( 4.013568362537369261, -0.9994162096361800529, -1.664904219174968114 ) ) ;
#78131=CARTESIAN_POINT ( 'NONE',  ( 4.886922752366290368, -1.802716094696995786, -0.6387714794457154399 ) ) ;
#78132=CARTESIAN_POINT ( 'NONE',  ( 0.2331713839410758105, 2.878356536703096324, -2.442089366404568640 ) ) ;
#78133=CARTESIAN_POINT ( 'NONE',  ( 5.825168945638790063, -0.03770542841243298970, 1.724543776939557960 ) ) ;
#78134=CARTESIAN_POINT ( 'NONE',  ( 4.452361426671761713, -1.313546101436880109, 1.530156479064001207 ) ) ;
#78136=CARTESIAN_POINT ( 'NONE',  ( 1.928631425534212074, 1.268998755960360603, -1.805353087401928569 ) ) ;
#78138=CARTESIAN_POINT ( 'NONE',  ( 1.324293675337850695, 2.015212547500934814, 0.5562262626958893730 ) ) ;
#78139=CARTESIAN_POINT ( 'NONE',  ( 0.3382653665467276749, 0.2958422019357190291, 1.744775138515190616 ) ) ;
#78140=CARTESIAN_POINT ( 'NONE',  ( 5.291638762709002464, 1.525045427759319727, -1.319226660814104335 ) ) ;
#78142=CARTESIAN_POINT ( 'NONE',  ( 2.836170770286027043, 2.275064633363361732, 0.2797384389828549978 ) ) ;
#78143=CARTESIAN_POINT ( 'NONE',  ( 0.5677837317836741393, -1.637140195495973671, -0.5907660828440349787 ) ) ;
#78145=CARTESIAN_POINT ( 'NONE',  ( 1.299655142190193402, -1.570548766235444038, 0.7348691985549455907 ) ) ;
#78148=CARTESIAN_POINT ( 'NONE',  ( 1.065148145857688577, 1.644283457976392748, -1.417989991454001730 ) ) ;
#78149=CARTESIAN_POINT ( 'NONE',  ( 2.378138974734815392, -2.011451771401792321, -0.1435188914247695346 ) ) ;
#78150=CARTESIAN_POINT ( 'NONE',  ( 3.656250000000002665, -1.895863743164003523, 0.7852924748301777225 ) ) ;
#78152=CARTESIAN_POINT ( 'NONE',  ( 6.692047312239829182, -0.8199282357786542574, 1.741332009981966022 ) ) ;
#78154=CARTESIAN_POINT ( 'NONE',  ( 3.322728300399055534, -0.9034660432867666069, -2.029577789741637162 ) ) ;
#78160=CARTESIAN_POINT ( 'NONE',  ( 4.880260771415650289, -0.2196809260722985546, -1.726461634439285797 ) ) ;
#78161=CARTESIAN_POINT ( 'NONE',  ( 5.055110333045015558, 1.632132345252810035, -1.088295032039228172 ) ) ;
#78162=EDGE_CURVE ( 'NONE', #65102, #41277, #117020, .T. ) ;
#78166=CARTESIAN_POINT ( 'NONE',  ( 4.376441990627045087, -1.307286168679543614, 1.846302370218126265 ) ) ;
#78168=CARTESIAN_POINT ( 'NONE',  ( 2.383324636069758640, -0.002395321609373335381, 2.062851379284504461 ) ) ;
#78173=CARTESIAN_POINT ( 'NONE',  ( 3.163207368312019430, 0.2779861718534247794, -1.849665920529340646 ) ) ;
#78174=CARTESIAN_POINT ( 'NONE',  ( 2.531537987306311965, -1.440582175967281886, 0.9650062983845784093 ) ) ;
#78175=CARTESIAN_POINT ( 'NONE',  ( 6.532779862045914321, -1.958661757936002612, 0.9833580883553474372 ) ) ;
#78176=CARTESIAN_POINT ( 'NONE',  ( 0.9036964725192305758, 1.805054822729842190, 1.269220749904229839 ) ) ;
#78177=CARTESIAN_POINT ( 'NONE',  ( 4.504844740329728481, 1.672958716126593082, -1.369014088531981255 ) ) ;
#78178=CARTESIAN_POINT ( 'NONE',  ( 4.400292492776470610, 1.500370014523371154, -1.232902440404326727 ) ) ;
#78182=( LENGTH_UNIT ( ) NAMED_UNIT ( * ) SI_UNIT ( .MILLI., .METRE. ) );
#78187=CARTESIAN_POINT ( 'NONE',  ( 5.432267593368638181, -1.591316862017605471, -1.238322901282742805 ) ) ;
#78191=CARTESIAN_POINT ( 'NONE',  ( 2.877373901574116211, 1.733520850877915187, -0.5729475677913041798 ) ) ;
#78192=CARTESIAN_POINT ( 'NONE',  ( 2.134064618640969524, -1.441378300436758630, -1.671108464803609417 ) ) ;
#78196=CARTESIAN_POINT ( 'NONE',  ( 0.5627676185161786249, 0.5905471060306236586, 1.931493850173772397 ) ) ;
#78197=CARTESIAN_POINT ( 'NONE',  ( 1.172698094321134477, 0.8626872041959359194, 1.937259058979395654 ) ) ;
#78201=CARTESIAN_POINT ( 'NONE',  ( 2.272090887488043887, -0.8719313595505603365, -1.644003247725301264 ) ) ;
#78203=CARTESIAN_POINT ( 'NONE',  ( 0.2511322555047851290, -1.735185354305257110, 1.289038484408123963 ) ) ;
#78204=CARTESIAN_POINT ( 'NONE',  ( 6.170546107226446253, 1.392543322632183722, 1.458558933167881211 ) ) ;
#78208=CARTESIAN_POINT ( 'NONE',  ( 3.492628380820805400, -0.3572889717703279788, -1.790209119249221548 ) ) ;
#78214=CARTESIAN_POINT ( 'NONE',  ( 6.643907658006512840, -0.09612306880287316280, -2.013924184692199137 ) ) ;
#78215=CARTESIAN_POINT ( 'NONE',  ( 6.298766309436587996, 1.533505995929709487, 1.018591839899836371 ) ) ;
#78216=CARTESIAN_POINT ( 'NONE',  ( 0.07700591528349547132, 1.369316849116916091, -2.165014180211277228 ) ) ;
#78217=CARTESIAN_POINT ( 'NONE',  ( 4.354349988907435964, 2.307223249097400064, -0.05412331456603951957 ) ) ;
#78219=CARTESIAN_POINT ( 'NONE',  ( 5.852838158510675015, -1.708014377640250991, 1.324763891615586386 ) ) ;
#78221=CARTESIAN_POINT ( 'NONE',  ( 2.577597507962032353, -0.9963960007246205342, 1.666827093504752222 ) ) ;
#78223=CARTESIAN_POINT ( 'NONE',  ( 4.833568131691490244, -1.505864581002622105, 1.736428821378619647 ) ) ;
#78224=CARTESIAN_POINT ( 'NONE',  ( 0.07536363704235826688, -0.001874865094115066300, -2.144269471569634877 ) ) ;
#78226=CARTESIAN_POINT ( 'NONE',  ( 4.908994958506140982, 1.627828031611065152, 0.9215782234750914403 ) ) ;
#78228=CARTESIAN_POINT ( 'NONE',  ( 2.004032382285144021, -0.8144628449315849394, 1.730399521388835460 ) ) ;
#78231=CARTESIAN_POINT ( 'NONE',  ( 4.160898416275903067, -1.636102012888400292, 1.481223685352812680 ) ) ;
#78237=CARTESIAN_POINT ( 'NONE',  ( 1.546097919708361079, 1.968910558940571320, 0.1009371868440200049 ) ) ;
#78238=CARTESIAN_POINT ( 'NONE',  ( 1.659631924955577098, -1.980043282969433882, -1.184870857304116898 ) ) ;
#78239=CARTESIAN_POINT ( 'NONE',  ( 2.453501617077270769, 1.514643136537169310, 1.246875331876770243 ) ) ;
#78241=CARTESIAN_POINT ( 'NONE',  ( 5.049704294756152123, 1.524832160660544611, 1.389060530156678297 ) ) ;
#78248=CARTESIAN_POINT ( 'NONE',  ( 1.850661656762859542, -2.160338676232275823, -0.2159047328044171599 ) ) ;
#78252=CARTESIAN_POINT ( 'NONE',  ( 2.706148147531197701, -0.7121320899835179574, -1.729884524348634933 ) ) ;
#78253=CARTESIAN_POINT ( 'NONE',  ( 6.415313282229532454, -0.2716245656670859820, 2.144420208805633887 ) ) ;
#78254=CARTESIAN_POINT ( 'NONE',  ( 6.670655732516623360, 7.629137130509072051, 2.773739711112707784 ) ) ;
#78255=CARTESIAN_POINT ( 'NONE',  ( 6.827182134110209688, 6.038954451951505042, 2.405852596708078384 ) ) ;
#78257=CARTESIAN_POINT ( 'NONE',  ( 2.648957786072099641, 0.2360777847093403214, 1.897596177352772306 ) ) ;
#78258=CARTESIAN_POINT ( 'NONE',  ( 4.522157790900214636, 1.087963700580677484, -1.395837783952274647 ) ) ;
#78259=CARTESIAN_POINT ( 'NONE',  ( 1.559083858985313542, -1.614856622157490929, 1.023943737511850083 ) ) ;
#78262=CARTESIAN_POINT ( 'NONE',  ( 5.237857731762096236, 1.913213232725724966, -0.09853679971996709419 ) ) ;
#78264=CARTESIAN_POINT ( 'NONE',  ( 6.672316266636414639, -0.9270569987065898632, -1.737699753229291710 ) ) ;
#78266=CARTESIAN_POINT ( 'NONE',  ( 5.418772907935071714, 1.728844841293469159, 0.7149302089985640762 ) ) ;
#78267=CARTESIAN_POINT ( 'NONE',  ( 1.277666653898035021, 1.085793613588705853, 1.467558327050644484 ) ) ;
#78268=CARTESIAN_POINT ( 'NONE',  ( 4.951907052881864502, 0.6945806438464275923, -2.094803410698709900 ) ) ;
#78271=CARTESIAN_POINT ( 'NONE',  ( 2.453648911872767346, 1.593012163857405961, 1.310297011819524293 ) ) ;
#78277=VERTEX_POINT ( 'NONE', #10568 ) ;
#78278=CARTESIAN_POINT ( 'NONE',  ( 5.230950013807261101, -1.948248037745937022, -0.7008574099531189594 ) ) ;
#78280=CARTESIAN_POINT ( 'NONE',  ( 2.671339989782473001, 0.1089736159370843782, -2.158987078831893669 ) ) ;
#78282=CARTESIAN_POINT ( 'NONE',  ( 3.317061382196756281, 1.590690956008104395, -1.244364558649863728 ) ) ;
#78283=CARTESIAN_POINT ( 'NONE',  ( 6.720655732516647163, -0.004400176169771369272, 2.173773060281408931 ) ) ;
#78288=CARTESIAN_POINT ( 'NONE',  ( 1.710173085450257924, 1.157096902994741772, -1.651345047625000007 ) ) ;
#78289=CARTESIAN_POINT ( 'NONE',  ( 6.216381822182692751, 2.044192415450503120, 0.7905562269360305594 ) ) ;
#78292=CARTESIAN_POINT ( 'NONE',  ( 4.851772015791367743, -1.356534033432246211, -1.348250844427544282 ) ) ;
#78294=ADVANCED_FACE ( 'NONE', ( #72361 ), #192801, .T. ) ;
#78297=CARTESIAN_POINT ( 'NONE',  ( 2.864861414439429321, -0.1511590275467006306, -2.010826137130202529 ) ) ;
#78300=CARTESIAN_POINT ( 'NONE',  ( 4.770341545797544214, -1.125046721222152213, 1.307389476665332895 ) ) ;
#78306=CARTESIAN_POINT ( 'NONE',  ( 0.5849358142855851650, 1.980036476162419845, 0.6043757699017646701 ) ) ;
#78309=CARTESIAN_POINT ( 'NONE',  ( 5.338451399618321602, 1.074232541698511900, -1.458426962581545361 ) ) ;
#78312=CARTESIAN_POINT ( 'NONE',  ( 5.865820270629499511, 0.5193939906856791522, -1.735422816724658146 ) ) ;
#78315=CARTESIAN_POINT ( 'NONE',  ( 2.818527994553555516, 2.063739945100159900, 0.7375456357434084786 ) ) ;
#78318=CARTESIAN_POINT ( 'NONE',  ( 0.3792546940144908563, -0.1001052471676349837, 1.959448305358338693 ) ) ;
#78320=CARTESIAN_POINT ( 'NONE',  ( 5.378507874412199463, -0.4701315380702688618, -1.856876755957288516 ) ) ;
#78330=CARTESIAN_POINT ( 'NONE',  ( 1.797963993548271411, -0.7283430984801853025, 2.035426966748521860 ) ) ;
#78333=CARTESIAN_POINT ( 'NONE',  ( 2.045663570152244315, 0.7015605659913305425, -1.685594894050304493 ) ) ;
#78335=CARTESIAN_POINT ( 'NONE',  ( 4.155160913615768337, -1.517764731708035386, -1.014145119915064841 ) ) ;
#78338=CARTESIAN_POINT ( 'NONE',  ( 4.000420421810535032, 1.959860935258441517, 0.1952677912114946512 ) ) ;
#78340=CARTESIAN_POINT ( 'NONE',  ( 5.882362869737407074, -0.2893225776206589384, -1.920288418758001159 ) ) ;
#78344=CARTESIAN_POINT ( 'NONE',  ( 5.906510592826289319, -2.110524776404258507, -0.2060971850248518311 ) ) ;
#78346=CARTESIAN_POINT ( 'NONE',  ( 3.721269560815092525, 1.641568950759502377, 0.9805937191851579193 ) ) ;
#78349=CARTESIAN_POINT ( 'NONE',  ( 0.1127427399064059588, -0.9454589178800475446, -1.991880357201977425 ) ) ;
#78350=CARTESIAN_POINT ( 'NONE',  ( 5.602202738069384402, -0.9032165795441854383, 1.799149290095316767 ) ) ;
#78352=CARTESIAN_POINT ( 'NONE',  ( 5.813091150998386247, 1.612263477354998864, 0.8566026058636074803 ) ) ;
#78353=CARTESIAN_POINT ( 'NONE',  ( 0.8892259839063383353, 0.1505779921940515187, 2.064926437897919964 ) ) ;
#78368=CARTESIAN_POINT ( 'NONE',  ( 3.639074924717408788, 0.6284830325712500443, 1.616442243290783232 ) ) ;
#78370=CARTESIAN_POINT ( 'NONE',  ( 1.252880909328604186, -0.4992908342843911940, -2.009044966204868388 ) ) ;
#78371=CARTESIAN_POINT ( 'NONE',  ( 2.548581339128490608, -1.457745987184940306, 1.535692819318078550 ) ) ;
#78375=CARTESIAN_POINT ( 'NONE',  ( 0.7253723109368491739, 0.1984653623241394993, -1.959446941136263831 ) ) ;
#78380=CARTESIAN_POINT ( 'NONE',  ( 2.519810532312277473, -1.321113963755312870, -1.873090484924363697 ) ) ;
#78381=CARTESIAN_POINT ( 'NONE',  ( 0.9436603434208358232, 0.7422609627109194586, -1.668170528445270140 ) ) ;
#78382=CARTESIAN_POINT ( 'NONE',  ( 3.234525475359388391, 1.209690070866603406, -1.481213593849866950 ) ) ;
#78387=CARTESIAN_POINT ( 'NONE',  ( 2.092043371607322566, 1.241737408274107501, 1.584530653180368009 ) ) ;
#78388=CARTESIAN_POINT ( 'NONE',  ( 1.780054392102415672, -1.085390340960286082, -1.633940563308281968 ) ) ;
#78392=CARTESIAN_POINT ( 'NONE',  ( 4.857415893618338032, 2.067970888898474247, -0.3061586078061846461 ) ) ;
#78393=CARTESIAN_POINT ( 'NONE',  ( 3.537761123354207893, 0.7962651652904990662, -1.580685414113996545 ) ) ;
#78396=CARTESIAN_POINT ( 'NONE',  ( 6.703114550498504798, -0.5130225571751775293, 2.242675272849779411 ) ) ;
#78397=CARTESIAN_POINT ( 'NONE',  ( 4.488070181461626618, -0.3849740463353290010, -1.697036094149968255 ) ) ;
#78400=CARTESIAN_POINT ( 'NONE',  ( 4.622224120573574346, 0.3796314994632241646, -1.691551752166654543 ) ) ;
#78401=CARTESIAN_POINT ( 'NONE',  ( 4.281792510435393773, -2.078899500905183828, 0.6263114880437108400 ) ) ;
#78403=CARTESIAN_POINT ( 'NONE',  ( 0.1283146926199127957, 2.112135570198115708, 0.1490006669643220705 ) ) ;
#78404=CARTESIAN_POINT ( 'NONE',  ( 6.281249999999699796, 0.7852924748228357066, 1.895863743163936022 ) ) ;
#78406=CARTESIAN_POINT ( 'NONE',  ( 3.627879330711426320, -1.146429500678107116, -1.547990911671823566 ) ) ;
#78408=CARTESIAN_POINT ( 'NONE',  ( 0.3818600843802121836, 0.2116341679995105141, -2.211193375792892546 ) ) ;
#78410=CARTESIAN_POINT ( 'NONE',  ( 6.983263157960404754, 7.052265632007776119, 2.644342174942279744 ) ) ;
#78413=CARTESIAN_POINT ( 'NONE',  ( 2.245073739244434208, 2.155446677131687139, 0.5364521487482876161 ) ) ;
#78419=CARTESIAN_POINT ( 'NONE',  ( 0.5631252389872200004, -1.117830369828230808, 1.678006741548984770 ) ) ;
#78421=CARTESIAN_POINT ( 'NONE',  ( 6.057095868330090838, 1.688466812627244185, -1.184547966247089912 ) ) ;
#78426=CARTESIAN_POINT ( 'NONE',  ( 0.4030913312595973408, -0.4806107285681981423, 1.703151836983556988 ) ) ;
#78427=CARTESIAN_POINT ( 'NONE',  ( 6.311143239517568837, 0.9901597221020401740, -1.423469027432751943 ) ) ;
#78428=CARTESIAN_POINT ( 'NONE',  ( 5.161534370633450663, 0.8641669074914829496, 1.510678848428636201 ) ) ;
#78429=CARTESIAN_POINT ( 'NONE',  ( 3.527152830493656577, -2.117552691746289018, 0.8784855890422419433 ) ) ;
#78431=CARTESIAN_POINT ( 'NONE',  ( 1.376629057770164311, 1.701771572936720212, -0.7031625657484343872 ) ) ;
#78433=CARTESIAN_POINT ( 'NONE',  ( 2.010518257881420023, 1.354885872097401078, -1.223726681998098087 ) ) ;
#78434=CARTESIAN_POINT ( 'NONE',  ( 2.901017702322743919, -0.9963018188003970321, -1.753030416019534021 ) ) ;
#78436=CARTESIAN_POINT ( 'NONE',  ( 1.394752248596371702, 1.789971953256053627, -1.264032476404143512 ) ) ;
#78438=CARTESIAN_POINT ( 'NONE',  ( 4.067482540003349634, 0.2598354432931935243, -2.089805856947650309 ) ) ;
#78441=CARTESIAN_POINT ( 'NONE',  ( 1.135311898753359472, -0.04898221611688948623, -2.069941200615910581 ) ) ;
#78444=CARTESIAN_POINT ( 'NONE',  ( 4.617906949270495609, -0.5647423089508787353, 2.043846993246847710 ) ) ;
#78447=CARTESIAN_POINT ( 'NONE',  ( 6.481070005604858686, -0.09514881109910081070, -1.823337098959529001 ) ) ;
#78454=CARTESIAN_POINT ( 'NONE',  ( 6.521762860236213655, -0.4636855090699961712, 2.076960040381255812 ) ) ;
#78455=CARTESIAN_POINT ( 'NONE',  ( 0.8859290024384089968, 1.414438444053778055, 1.560449103131421156 ) ) ;
#78458=CARTESIAN_POINT ( 'NONE',  ( 5.612096381091351560, 1.858897858770152789, -0.08933831184920922042 ) ) ;
#78465=CARTESIAN_POINT ( 'NONE',  ( 2.348037267531626338, -0.8415878996531295231, 1.772339229757218471 ) ) ;
#78466=CARTESIAN_POINT ( 'NONE',  ( 0.7608789386071808103, -1.564954856162886765, 1.491513986042219297 ) ) ;
#78470=CARTESIAN_POINT ( 'NONE',  ( 2.793977985172685141, -1.619072854944574313, 0.6208489642184951141 ) ) ;
#78471=CARTESIAN_POINT ( 'NONE',  ( 2.255425419672125287, 0.7431408456733903378, 1.573829366573131328 ) ) ;
#78475=CARTESIAN_POINT ( 'NONE',  ( 0.8431247865267020858, -1.122328847578180078, 1.674629589540656216 ) ) ;
#78476=CARTESIAN_POINT ( 'NONE',  ( 6.925078400183593885, 7.051837472187183486, 2.742497896504832333 ) ) ;
#78478=CARTESIAN_POINT ( 'NONE',  ( 1.674623549722221716, -1.871433754200592992, -0.6201854899473575600 ) ) ;
#78481=CARTESIAN_POINT ( 'NONE',  ( 6.029550621839829816, -0.2273517531893587407, 1.898748578088353733 ) ) ;
#78486=CARTESIAN_POINT ( 'NONE',  ( 1.401042149647635071, -0.2984598639739938220, -1.997379878556293731 ) ) ;
#78488=CARTESIAN_POINT ( 'NONE',  ( 4.788248824917088697, -1.092567961935811960, 2.032559802855623321 ) ) ;
#78489=CARTESIAN_POINT ( 'NONE',  ( 6.162552467866693640, -0.7048080804108979303, -1.831077584432870609 ) ) ;
#78490=CARTESIAN_POINT ( 'NONE',  ( 3.485159065011545376, 0.04355839926390054490, 1.961427607708134957 ) ) ;
#78494=CARTESIAN_POINT ( 'NONE',  ( 1.710321574826153324, 1.214426542090217609, -1.734289745093554380 ) ) ;
#78497=CARTESIAN_POINT ( 'NONE',  ( 1.306327274835542784, 1.622920506532832929, 0.8694138843568788300 ) ) ;
#78500=CARTESIAN_POINT ( 'NONE',  ( 3.305043459179863419, -0.4174351347619070229, -2.078937965663613774 ) ) ;
#78504=CARTESIAN_POINT ( 'NONE',  ( 3.444654265643578128, 0.4973230594479564060, 1.999757164544394561 ) ) ;
#78506=CARTESIAN_POINT ( 'NONE',  ( 0.1339853816830008371, 0.3136495386693045062, 1.814181566856580607 ) ) ;
#78511=CARTESIAN_POINT ( 'NONE',  ( 0.4697016844467936103, 0.2121168557088908557, -2.196667960996725011 ) ) ;
#78512=CARTESIAN_POINT ( 'NONE',  ( 2.267197333419627370, -2.067742563539621603, -0.9185262150545376869 ) ) ;
#78514=CARTESIAN_POINT ( 'NONE',  ( 2.214858347191206445, 1.452946758456060250, -1.081763258146416939 ) ) ;
#78515=CARTESIAN_POINT ( 'NONE',  ( 2.799894175352398484, -0.9483327596419667271, -1.664474063330185105 ) ) ;
#78516=CARTESIAN_POINT ( 'NONE',  ( 4.686024408448190570, -1.271122505372159539, -1.634150330299996012 ) ) ;
#78518=CARTESIAN_POINT ( 'NONE',  ( 1.516417288619626769, 1.325465413702779482, -1.459542524610158098 ) ) ;
#78519=CARTESIAN_POINT ( 'NONE',  ( 0.2527871956496882122, -1.549381263408876830, 1.144551880545265465 ) ) ;
#78520=CARTESIAN_POINT ( 'NONE',  ( 3.080767038946086611, -0.1360980058115155988, -1.865751385159146070 ) ) ;
#78521=CARTESIAN_POINT ( 'NONE',  ( 1.577271561783103460, -2.192461267746559361, -0.7203256085408450415 ) ) ;
#78523=CARTESIAN_POINT ( 'NONE',  ( 2.717075380476912994, -1.617705633067820559, -0.9199624106535415624 ) ) ;
#78525=CARTESIAN_POINT ( 'NONE',  ( 6.004357462130720080, 2.060136995665005522, 0.1050117271170700056 ) ) ;
#78529=CARTESIAN_POINT ( 'NONE',  ( 5.965875410913440646, 2.075401660611264631, -0.3564754433343624296 ) ) ;
#78531=CARTESIAN_POINT ( 'NONE',  ( 5.835289683280778128, -1.956920075724715602, 0.9183947573421016308 ) ) ;
#78532=CARTESIAN_POINT ( 'NONE',  ( 6.094400524283400067, -1.078572965507901715, 1.707356775630589851 ) ) ;
#78537=CARTESIAN_POINT ( 'NONE',  ( 6.825078400183545391, 0.005516643811322509937, 1.755566376062764222 ) ) ;
#78540=CARTESIAN_POINT ( 'NONE',  ( 4.223842396274177347, 0.8578445224393380641, -1.825075645057252505 ) ) ;
#78545=CARTESIAN_POINT ( 'NONE',  ( 5.629794960336353071, -1.368038101806166029, -1.673757646710342550 ) ) ;
#78551=CARTESIAN_POINT ( 'NONE',  ( 6.398064575937244314, -0.9530261711272209890, -1.777004751544956962 ) ) ;
#78553=CARTESIAN_POINT ( 'NONE',  ( 1.593959923740532414, -1.716304196509855329, -0.1716357895808154899 ) ) ;
#78557=CARTESIAN_POINT ( 'NONE',  ( 0.1804953903597758258, -0.1286114524143982807, -1.740565225867502397 ) ) ;
#78558=CARTESIAN_POINT ( 'NONE',  ( 0.8385398129025347647, 1.197303422201956957, -1.618206657969661011 ) ) ;
#78560=CARTESIAN_POINT ( 'NONE',  ( 3.434799832723956836, 2.152550277175222515, 0.4854691814954179563 ) ) ;
#78561=CARTESIAN_POINT ( 'NONE',  ( 5.067309307786254102, 1.885564733447910646, 1.076134493607887155 ) ) ;
#78565=CARTESIAN_POINT ( 'NONE',  ( 3.580828998445852562, -1.422877522674294681, 1.572404880189558485 ) ) ;
#78566=CARTESIAN_POINT ( 'NONE',  ( 3.181267708840180397, 1.591331833097202608, 1.238305487465785726 ) ) ;
#78567=CARTESIAN_POINT ( 'NONE',  ( 3.111360644411143017, 1.430921235420354654, 1.110905701166440940 ) ) ;
#78571=CARTESIAN_POINT ( 'NONE',  ( 0.2329894512427649056, -1.712236961970284410, 0.7538099095961706686 ) ) ;
#78574=CARTESIAN_POINT ( 'NONE',  ( 1.270553553854154361, -0.2845990055821822629, -1.894349495789057647 ) ) ;
#78580=CARTESIAN_POINT ( 'NONE',  ( 5.102478102407745908, -0.7247817745383768884, -2.036717088958202471 ) ) ;
#78583=CARTESIAN_POINT ( 'NONE',  ( 2.760144723603759065, 0.7592700852765141839, -1.980205354017528840 ) ) ;
#78586=CARTESIAN_POINT ( 'NONE',  ( 4.833256578820930294, -1.803536663746601709, 0.7962986557112069486 ) ) ;
#78587=CARTESIAN_POINT ( 'NONE',  ( 6.504189997394580480, -0.8109953713257547214, 1.730197269205424160 ) ) ;
#78590=CARTESIAN_POINT ( 'NONE',  ( 5.630101985619759830, 2.115003628044552553, 0.1013798475145138156 ) ) ;
#78592=CARTESIAN_POINT ( 'NONE',  ( 6.707475516188797116, -1.580950341439198992, -1.174378316608926331 ) ) ;
#78593=CARTESIAN_POINT ( 'NONE',  ( 2.906119529042447969, 1.406244311732379293, -1.339499261486200465 ) ) ;
#78597=CARTESIAN_POINT ( 'NONE',  ( 2.291069257668688408, 1.616616537889125516, 1.325633359429157831 ) ) ;
#78600=CARTESIAN_POINT ( 'NONE',  ( 0.3635249777022043771, 0.5700983740567664437, -1.719507965497588220 ) ) ;
#78602=CARTESIAN_POINT ( 'NONE',  ( 4.653060005753134831, -1.773635849817876586, 1.313014255023836618 ) ) ;
#78604=CARTESIAN_POINT ( 'NONE',  ( 3.171135245091468491, -2.038329301889611589, -0.8460836234857532778 ) ) ;
#78606=CARTESIAN_POINT ( 'NONE',  ( 1.383307607624170155, 0.1396965592646744470, -1.907218110473147155 ) ) ;
#78608=CARTESIAN_POINT ( 'NONE',  ( 4.000488093070094564, 2.060113009926473726, 0.2059288336104248551 ) ) ;
#78610=CARTESIAN_POINT ( 'NONE',  ( 2.588937169860201504, -0.3686131662095324946, -2.129881858774537395 ) ) ;
#78611=CARTESIAN_POINT ( 'NONE',  ( 5.038714576072483631, -1.879839391954684746, 1.126354835186346603 ) ) ;
#78617=CARTESIAN_POINT ( 'NONE',  ( 0.1939827082095749167, 1.755770691208278889, 0.9913967135185000057 ) ) ;
#78621=CARTESIAN_POINT ( 'NONE',  ( 4.241125740018336643, -0.1978421677554068614, -2.060750949040678570 ) ) ;
#78622=CARTESIAN_POINT ( 'NONE',  ( 3.756402471274498112, 0.6942424141608801724, 1.797233106274237713 ) ) ;
#78623=CARTESIAN_POINT ( 'NONE',  ( 0.4918148228068714989, -2.006445053647107013, 0.2004575690456936732 ) ) ;
#78626=CARTESIAN_POINT ( 'NONE',  ( 3.520317136570957128, 0.8812775084000439296, 1.761307543597267822 ) ) ;
#78627=CARTESIAN_POINT ( 'NONE',  ( 0.6740948890744530297, -1.214310170130480593, 1.824057261183717582 ) ) ;
#78628=CARTESIAN_POINT ( 'NONE',  ( 4.600122369450095228, -1.825375079466069694, -0.04201004182294298950 ) ) ;
#78634=CARTESIAN_POINT ( 'NONE',  ( 1.434833617064284805, -1.334073193498284793, -1.269287082821937362 ) ) ;
#78635=CARTESIAN_POINT ( 'NONE',  ( 4.922139854824453487, -2.003099925734778797, 0.2017396019941309904 ) ) ;
#78636=CARTESIAN_POINT ( 'NONE',  ( 0.3866022076702098076, -0.1098403002397010941, 2.295889243394435564 ) ) ;
#78637=CARTESIAN_POINT ( 'NONE',  ( 5.172687041346638814, 1.355624813549320740, -1.418227474788292364 ) ) ;
#78642=CARTESIAN_POINT ( 'NONE',  ( 1.400065306692158229, -0.7557916345088554477, -1.949536834912476646 ) ) ;
#78643=CARTESIAN_POINT ( 'NONE',  ( 0.4087956859853311142, 1.625333209436867321, 0.9259686016569528277 ) ) ;
#78645=CARTESIAN_POINT ( 'NONE',  ( -0.2102771530458459603, 6.947233595868168798, -2.798738817348767949 ) ) ;
#78646=CARTESIAN_POINT ( 'NONE',  ( 0.4150587399484934603, -0.9287321991380654840, -1.471733822881353015 ) ) ;
#78650=CARTESIAN_POINT ( 'NONE',  ( 2.191662871657253486, -0.7386692205221119245, 1.558845181661876467 ) ) ;
#78651=CARTESIAN_POINT ( 'NONE',  ( 1.365048776756357940, 0.1565470504056795942, -2.186014887712848243 ) ) ;
#78652=CARTESIAN_POINT ( 'NONE',  ( 4.160898416275903067, -1.636102012888400292, 1.481223685352812680 ) ) ;
#78654=CARTESIAN_POINT ( 'NONE',  ( 1.042111193480334430, 1.456518763772189695, 1.610191069602670000 ) ) ;
#78655=CARTESIAN_POINT ( 'NONE',  ( 0.4162703231485806454, 1.261427835099769634, -1.320066674804179385 ) ) ;
#78656=CARTESIAN_POINT ( 'NONE',  ( 2.923186261301851996, -1.865062457072470536, 1.002408848433397726 ) ) ;
#78657=CARTESIAN_POINT ( 'NONE',  ( 6.639320575229252341, 2.457876053485750223, 2.280608551775892501 ) ) ;
#78660=CARTESIAN_POINT ( 'NONE',  ( 3.404133285375851248, -0.9304739769722850662, -2.095221664589861810 ) ) ;
#78665=CARTESIAN_POINT ( 'NONE',  ( 5.953820247260992460, -1.607154219335062528, -1.533616513404257198 ) ) ;
#78667=EDGE_CURVE ( 'NONE', #120459, #175232, #166062, .T. ) ;
#78672=CARTESIAN_POINT ( 'NONE',  ( 3.797500137148449362, 1.423962148579031917, -1.427936706820939872 ) ) ;
#78674=CARTESIAN_POINT ( 'NONE',  ( 2.026308614600486280, 1.056755808076353276, 1.771133502622779243 ) ) ;
#78679=CARTESIAN_POINT ( 'NONE',  ( 5.208995777154565410, -0.3238732214236837992, 2.167259527466679270 ) ) ;
#78680=CARTESIAN_POINT ( 'NONE',  ( 1.916638904718031000, -1.319229391439219246, -1.525043083973671498 ) ) ;
#78681=CARTESIAN_POINT ( 'NONE',  ( 2.647807870277216757, 0.6224553824519338807, 1.732961026760751366 ) ) ;
#78685=CARTESIAN_POINT ( 'NONE',  ( 5.754876975610782708, -1.437719105923901841, 1.124948175183659638 ) ) ;
#78686=CARTESIAN_POINT ( 'NONE',  ( 5.818982467333652764, 0.9914020171761170896, -1.755767668913270407 ) ) ;
#78688=CARTESIAN_POINT ( 'NONE',  ( 5.893528310750998145, 1.708867279757080748, 1.482922863094847443 ) ) ;
#78690=CARTESIAN_POINT ( 'NONE',  ( 0.4871192430246041316, -0.2598372338927424918, -2.089908867234680834 ) ) ;
#78699=CARTESIAN_POINT ( 'NONE',  ( 1.933984528066152953, -2.055706711753771287, 0.5200354980386610038 ) ) ;
#78700=CARTESIAN_POINT ( 'NONE',  ( 3.129344976949835822, 2.009775620968552445, 0.9465212012665072949 ) ) ;
#78704=CARTESIAN_POINT ( 'NONE',  ( 3.824618516750320385, -1.319357783791510697, 1.452116237791359010 ) ) ;
#78711=CARTESIAN_POINT ( 'NONE',  ( 2.092179824929023102, 1.308410154019133076, 1.668721082780571408 ) ) ;
#78713=CARTESIAN_POINT ( 'NONE',  ( 4.803692121107413726, -0.5798474923815257753, 2.082409481564663434 ) ) ;
#78714=CARTESIAN_POINT ( 'NONE',  ( 3.087279721815265443, -0.7436087841871074078, 1.684586988852328160 ) ) ;
#78719=CARTESIAN_POINT ( 'NONE',  ( 5.964775352603689740, 0.1210227373375266924, -1.736196924002187947 ) ) ;
#78722=CARTESIAN_POINT ( 'NONE',  ( 3.502937704049163159, 1.705309618848281472, -1.328393843302433153 ) ) ;
#78723=CARTESIAN_POINT ( 'NONE',  ( 6.169296033003512925, -0.7230314695168098549, -1.882185070641306801 ) ) ;
#78725=CARTESIAN_POINT ( 'NONE',  ( 2.430746436576446179, 2.096607243605509208, 0.5259719050795114148 ) ) ;
#78726=CARTESIAN_POINT ( 'NONE',  ( 3.813711686511447763, -1.942732367404787830, 0.3338136033803756342 ) ) ;
#78728=CARTESIAN_POINT ( 'NONE',  ( 0.1698123575781598782, 1.266975945507025081, 1.788028528876134393 ) ) ;
#78729=CARTESIAN_POINT ( 'NONE',  ( 4.546391927783274056, -1.557747286768229600, 1.159548114344757019 ) ) ;
#78739=CARTESIAN_POINT ( 'NONE',  ( 1.712255133470397261, -2.190042126362458319, 0.2705847154940849153 ) ) ;
#78741=CARTESIAN_POINT ( 'NONE',  ( 6.912952593004609625, -1.518390278170888008, 1.241885805282373134 ) ) ;
#78747=CARTESIAN_POINT ( 'NONE',  ( 5.191278274421009975, -0.6593680717656666967, 1.719199333795925710 ) ) ;
#78751=CARTESIAN_POINT ( 'NONE',  ( 5.783468009189684622, 0.1541500780414573890, -2.115021274163720211 ) ) ;
#78755=CARTESIAN_POINT ( 'NONE',  ( 6.520785525839065677, 1.921145329286999326, 0.7461220883302563944 ) ) ;
#78757=CARTESIAN_POINT ( 'NONE',  ( 1.556854020514925496, 1.524047875013130104, -1.067797667942985917 ) ) ;
#78758=CARTESIAN_POINT ( 'NONE',  ( 3.403688466941825475, -0.7492148395099357261, -1.682118234477212537 ) ) ;
#78762=CARTESIAN_POINT ( 'NONE',  ( 6.610000000000026077, 2.442988107647511065, 2.382821027452782570 ) ) ;
#78764=CARTESIAN_POINT ( 'NONE',  ( 3.352369063006555905, 2.207063162671081713, 4.936380160885933677E-05 ) ) ;
#78765=CARTESIAN_POINT ( 'NONE',  ( 6.345044588916532113, -1.916324442970654962, 1.202328811479462578 ) ) ;
#78767=CARTESIAN_POINT ( 'NONE',  ( 5.467019156909919353, -1.422831870918849217, 1.121200454338074692 ) ) ;
#78768=CARTESIAN_POINT ( 'NONE',  ( 6.051949806467664672, 0.9910487912591151582, 1.639330874965704732 ) ) ;
#78770=CARTESIAN_POINT ( 'NONE',  ( 6.737182200980119440, -1.669782060861616291, 0.8434366901180423426 ) ) ;
#78772=CARTESIAN_POINT ( 'NONE',  ( 6.438360790777991838, 1.751285973423050368, 0.2548140705225035441 ) ) ;
#78773=AXIS2_PLACEMENT_3D ( 'NONE', #84161, #67875, #102548 ) ;
#78775=CARTESIAN_POINT ( 'NONE',  ( 1.657435761918718331, 1.928256795251210631, -0.5899901959932273288 ) ) ;
#78777=CARTESIAN_POINT ( 'NONE',  ( 2.807361190694975139, 1.779531611039061767, 1.126096823879179754 ) ) ;
#78782=CARTESIAN_POINT ( 'NONE',  ( 2.988540512386147707, -1.199814222051265311, 1.624667845120256748 ) ) ;
#78785=CARTESIAN_POINT ( 'NONE',  ( 3.567792053227138105, 2.109782723108716063, -0.4697668898906853796 ) ) ;
#78789=CARTESIAN_POINT ( 'NONE',  ( 0.3093308919281665959, -1.743438469055924145, 1.293836907758689758 ) ) ;
#78793=CARTESIAN_POINT ( 'NONE',  ( 2.050558489324630251, -1.691691439650149897, 1.393213601605561180 ) ) ;
#78794=CARTESIAN_POINT ( 'NONE',  ( 6.883263157960364254, 2.431740398616466070, 2.435552827938294751 ) ) ;
#78795=CARTESIAN_POINT ( 'NONE',  ( 2.923041840916926315, 2.129999922893408559, 0.7632657742467786610 ) ) ;
#78802=CARTESIAN_POINT ( 'NONE',  ( 3.883871017828253613, -0.8741022562178245581, 1.538735937109585672 ) ) ;
#78805=CARTESIAN_POINT ( 'NONE',  ( 0.3410288278610376089, 0.3603064943271740428, 2.074735154451929020 ) ) ;
#78808=CARTESIAN_POINT ( 'NONE',  ( 6.327749939939701918, 0.7691082200134462532, -1.864175038933602924 ) ) ;
#78812=CARTESIAN_POINT ( 'NONE',  ( 3.836663719693265584, 0.2738035037005565053, 1.850374562403465983 ) ) ;
#78813=CARTESIAN_POINT ( 'NONE',  ( 2.887621454190898884, -1.933326653459125355, 0.7409182656877840722 ) ) ;
#78818=CARTESIAN_POINT ( 'NONE',  ( 6.174726448494309849, -2.051094451480539149, -0.6828207641706719455 ) ) ;
#78820=CARTESIAN_POINT ( 'NONE',  ( 3.314850587115983238, -1.487306837207631238, 1.279512770686676681 ) ) ;
#78822=CARTESIAN_POINT ( 'NONE',  ( 0.6673420201736456336, -0.6766069248959758475, -1.899328980164962655 ) ) ;
#78826=CARTESIAN_POINT ( 'NONE',  ( 0.7021627906659900775, -0.6242572379067250488, -1.763460184394528341 ) ) ;
#78828=CARTESIAN_POINT ( 'NONE',  ( 2.795184176893855899, -0.1524655061851394322, -2.007514041822997086 ) ) ;
#78830=CARTESIAN_POINT ( 'NONE',  ( 2.249754300142119856, 2.075745305004289332, -0.4162820868813913999 ) ) ;
#78832=CARTESIAN_POINT ( 'NONE',  ( 4.000488093070094564, 2.060113009926473726, 0.2059288336104248551 ) ) ;
#78834=CARTESIAN_POINT ( 'NONE',  ( -0.07645973585807680495, -1.289725328510348934, -1.646077999003342729 ) ) ;
#78836=CARTESIAN_POINT ( 'NONE',  ( 4.946237996787820279, 1.820793779319082706, 0.1331645236858983172 ) ) ;
#78842=CARTESIAN_POINT ( 'NONE',  ( 6.704147062870869256, -2.206433763861126884, 0.04732420095975712476 ) ) ;
#78844=CARTESIAN_POINT ( 'NONE',  ( 5.567032834676129305, -1.504811603839781631, 1.179860560037985895 ) ) ;
#78853=CARTESIAN_POINT ( 'NONE',  ( 4.569519670753737550, 1.814867081516871261, -0.4525428206468632975 ) ) ;
#78854=CARTESIAN_POINT ( 'NONE',  ( 0.07700591528354748527, 7.629137130509112907, -2.510791685687420838 ) ) ;
#78861=CARTESIAN_POINT ( 'NONE',  ( 1.481237898015239418, -0.05359582033081673746, 1.968903824098491073 ) ) ;
#78862=CARTESIAN_POINT ( 'NONE',  ( 3.023064714212614135, -1.777003028299545484, 0.9530295004822467719 ) ) ;
#78866=CARTESIAN_POINT ( 'NONE',  ( 3.837968455498752096, 2.180838135830205804, 0.2153102754597763235 ) ) ;
#78868=CARTESIAN_POINT ( 'NONE',  ( 1.957912498325198536, 1.921386756000037055, -0.1395382256239047214 ) ) ;
#78870=CARTESIAN_POINT ( 'NONE',  ( 0.1331565106231329398, 0.7299000548664087429, -2.029785554894456556 ) ) ;
#78877=CARTESIAN_POINT ( 'NONE',  ( 5.196754805642953556, 1.508532920973480795, 1.055450849767838317 ) ) ;
#78878=CARTESIAN_POINT ( 'NONE',  ( 1.752591402120354358, 1.991486659738419984, 0.2933061901304565011 ) ) ;
#78879=CARTESIAN_POINT ( 'NONE',  ( 3.831692444270826226, -1.546495240224911250, 1.700404426133800939 ) ) ;
#78880=CARTESIAN_POINT ( 'NONE',  ( -0.1288028175207089898, 5.718623287604398087, -2.868046808693432315 ) ) ;
#78881=CARTESIAN_POINT ( 'NONE',  ( 1.797469275952040979, -1.343413903288761313, -1.288013994602929646 ) ) ;
#78884=CARTESIAN_POINT ( 'NONE',  ( 5.783449990912790106, 0.1341079605299954347, -1.907733270042926810 ) ) ;
#78887=CARTESIAN_POINT ( 'NONE',  ( 4.370703248089922610, -0.001752428395085294443, -2.090933975693793911 ) ) ;
#78888=CARTESIAN_POINT ( 'NONE',  ( 3.590566789841375339, -0.3639703897368729568, -1.834726254853453087 ) ) ;
#78893=CARTESIAN_POINT ( 'NONE',  ( 4.723137274085514647, -0.08022016869785492110, 1.723147214940720762 ) ) ;
#78895=CARTESIAN_POINT ( 'NONE',  ( 0.7560338623246564138, 1.671613681001963281, -0.4610611789691662632 ) ) ;
#78900=CARTESIAN_POINT ( 'NONE',  ( 5.629782814718605977, 2.094415894289668678, -0.5717063696269225614 ) ) ;
#78901=CARTESIAN_POINT ( 'NONE',  ( 4.934128534657983067, 0.9357288403324083292, -1.567518238613223813 ) ) ;
#78902=CARTESIAN_POINT ( 'NONE',  ( 1.182386158793121256, 1.172985831986381955, -1.572276950389992933 ) ) ;
#78903=CARTESIAN_POINT ( 'NONE',  ( 0.3338148283143215767, 0.6594671527525318711, -2.011992694175788188 ) ) ;
#78907=CARTESIAN_POINT ( 'NONE',  ( 2.227333921462580246, 1.895369558270381338, 0.9509248740046101211 ) ) ;
#78912=CARTESIAN_POINT ( 'NONE',  ( 0.8485890540621650047, -2.054197865963180547, -0.2570499307305574299 ) ) ;
#78913=CARTESIAN_POINT ( 'NONE',  ( 6.883263157960404222, 4.689511904294953126, 2.716359706997414136 ) ) ;
#78915=CARTESIAN_POINT ( 'NONE',  ( 2.139591745018020408, 0.003451857093505344976, 2.221473417793240923 ) ) ;
#78917=CARTESIAN_POINT ( 'NONE',  ( 1.108484992968819416, -0.04990477548066223068, 2.298298319747505758 ) ) ;
#78919=CARTESIAN_POINT ( 'NONE',  ( 5.489153638472886954, 0.1464082308396240373, 2.057405090433866324 ) ) ;
#78924=CARTESIAN_POINT ( 'NONE',  ( 5.407694413872749628, -0.8332299576223768378, -1.642021276980778932 ) ) ;
#78928=CARTESIAN_POINT ( 'NONE',  ( 1.641173577361688896, -1.245895879902914727, -1.192971367628747448 ) ) ;
#78929=CARTESIAN_POINT ( 'NONE',  ( 1.604704241733472037, 1.883313803065278513, 0.7212895827233902768 ) ) ;
#78930=CARTESIAN_POINT ( 'NONE',  ( 1.706133075696044221, 2.146806223983906747, 0.8221538945956968769 ) ) ;
#78932=CARTESIAN_POINT ( 'NONE',  ( 2.267197333419627370, -2.067742563539621603, -0.9185262150545376869 ) ) ;
#78933=CARTESIAN_POINT ( 'NONE',  ( 4.283879487498391647, 1.375451533845202245, 1.594966088981208729 ) ) ;
#78935=CARTESIAN_POINT ( 'NONE',  ( 3.620126565017945275, 1.124893713931356842, -1.366185836280229715 ) ) ;
#78938=CARTESIAN_POINT ( 'NONE',  ( 0.02392203315931124008, -1.416205114373503715, -1.803417470570017000 ) ) ;
#78939=CARTESIAN_POINT ( 'NONE',  ( 4.699059028873219468, -0.4882365319774860102, 1.775153104902137624 ) ) ;
#78942=CARTESIAN_POINT ( 'NONE',  ( 4.611385148785618782, -2.149487334021232599, 0.4259423572047504880 ) ) ;
#78950=CARTESIAN_POINT ( 'NONE',  ( 2.842313889931574522, 1.911971217405187495, 0.2356370756458354143 ) ) ;
#78953=CARTESIAN_POINT ( 'NONE',  ( 0.2291713999985908190, 1.525799623841477493, -1.614749986458098974 ) ) ;
#78963=CARTESIAN_POINT ( 'NONE',  ( 2.700428686635591546, 1.471443353139300081, 0.9291617766199999906 ) ) ;
#78966=CARTESIAN_POINT ( 'NONE',  ( 0.4671467121175365000, 1.705069321186868159, 0.9702857188121426502 ) ) ;
#78969=CARTESIAN_POINT ( 'NONE',  ( 6.262596564776618635, -1.532251275270900326, 1.525113613579494709 ) ) ;
#78972=CARTESIAN_POINT ( 'NONE',  ( 5.313408243115379292, -0.3210861823062813314, 2.137610926513198617 ) ) ;
#78973=CARTESIAN_POINT ( 'NONE',  ( -0.2104748580754183529, 0.2283854016844401591, -2.137091067173245929 ) ) ;
#78976=CARTESIAN_POINT ( 'NONE',  ( 6.573508854753547404, 1.887220770608761589, -0.5698601248695351895 ) ) ;
#78977=CARTESIAN_POINT ( 'NONE',  ( 6.186827581914116081, -0.9662774195124073096, -1.439361474112188954 ) ) ;
#78980=CARTESIAN_POINT ( 'NONE',  ( 2.982162443640325566, -2.159563097825706990, -0.3721831821169723775 ) ) ;
#78981=CARTESIAN_POINT ( 'NONE',  ( 3.452467797911736636, 2.307758715189492271, 0.002325993833134780940 ) ) ;
#78982=CARTESIAN_POINT ( 'NONE',  ( 6.169226111886771946, 0.1559856310293654957, -2.054958193847939096 ) ) ;
#78983=CARTESIAN_POINT ( 'NONE',  ( 1.517416608934060385, -1.078585517578967368, -1.614684294522166663 ) ) ;
#78988=CARTESIAN_POINT ( 'NONE',  ( 4.535463010148616192, -0.1012041512906610846, 2.118281909017679432 ) ) ;
#78990=CARTESIAN_POINT ( 'NONE',  ( 2.233046271152541618, 2.016033844848092560, 0.04667593304989729741 ) ) ;
#78992=CARTESIAN_POINT ( 'NONE',  ( 5.157340341976529352, -1.861842412690998039, -1.184373046124863160 ) ) ;
#78998=FACE_OUTER_BOUND ( 'NONE', #79199, .T. ) ;
#79001=CARTESIAN_POINT ( 'NONE',  ( 4.944241404475337553, 2.055231674695843669, 0.1536075889326995458 ) ) ;
#79005=CARTESIAN_POINT ( 'NONE',  ( 3.703775025860293724, 1.464345522003915878, 1.391222453660536873 ) ) ;
#79011=CARTESIAN_POINT ( 'NONE',  ( 2.571226905367568261, 0.1023410288747768487, -2.058482174549924437 ) ) ;
#79012=CARTESIAN_POINT ( 'NONE',  ( 2.672500184003968382, 1.427937546361924381, 1.423961308954827754 ) ) ;
#79018=CARTESIAN_POINT ( 'NONE',  ( 3.216172551982798833, -1.646586737935524125, -1.163091166099708529 ) ) ;
#79019=CARTESIAN_POINT ( 'NONE',  ( 2.782953997937851920, 1.302219384484751830, 1.301801165952347628 ) ) ;
#79020=CARTESIAN_POINT ( 'NONE',  ( 6.164705905600972535, -1.563586322211576674, 1.557672334054376773 ) ) ;
#79022=CARTESIAN_POINT ( 'NONE',  ( 2.249508738127777630, -1.734628566516350778, -1.289557925820798090 ) ) ;
#79025=CARTESIAN_POINT ( 'NONE',  ( 4.171193994350897327, 1.889596262492127199, -0.9554925290978563135 ) ) ;
#79028=CARTESIAN_POINT ( 'NONE',  ( 1.059204734455133412, 0.3686402435371800013, -1.833797362824276078 ) ) ;
#79029=CARTESIAN_POINT ( 'NONE',  ( 5.664905584638975533, -1.781982755157806908, -0.8436340872482649411 ) ) ;
#79033=CARTESIAN_POINT ( 'NONE',  ( 0.9442952520863318044, 0.8911936224933308948, -2.019119535841918278 ) ) ;
#79035=CARTESIAN_POINT ( 'NONE',  ( 5.986797818411375260, 1.994257276370488219, 0.5558945855626205024 ) ) ;
#79038=CARTESIAN_POINT ( 'NONE',  ( 6.639320575229257670, 2.957073754255258535, 2.555924021811271096 ) ) ;
#79039=CARTESIAN_POINT ( 'NONE',  ( 4.891463287051191600, 1.460324016362057886, 1.324601213698357149 ) ) ;
#79040=CARTESIAN_POINT ( 'NONE',  ( 6.398695825915057256, -1.981597308308700844, -0.3899587018172407382 ) ) ;
#79042=CARTESIAN_POINT ( 'NONE',  ( 4.705897867575262516, -0.6186405800616563422, 2.223174812903663256 ) ) ;
#79043=CARTESIAN_POINT ( 'NONE',  ( 2.325117943063298664, -1.883989625962046555, -0.8399396378151212650 ) ) ;
#79050=CARTESIAN_POINT ( 'NONE',  ( 3.965408508876398841, 1.860285638359628235, 1.119340054616506874 ) ) ;
#79052=CARTESIAN_POINT ( 'NONE',  ( 3.667381569930192597, 1.025862638139760419, 1.528780434079744843 ) ) ;
#79054=CARTESIAN_POINT ( 'NONE',  ( 6.620655732516627090, 3.711369741872071693, 2.240970959566997323 ) ) ;
#79055=CARTESIAN_POINT ( 'NONE',  ( 4.950807510372833065, -1.851323926424643274, -1.172527737679923465 ) ) ;
#79056=CARTESIAN_POINT ( 'NONE',  ( 6.104402428500737443, -0.8075561382203682026, -2.113670588390024196 ) ) ;
#79062=CARTESIAN_POINT ( 'NONE',  ( 1.146904862891504173, -1.391901254704702273, -1.093021760518765539 ) ) ;
#79064=CARTESIAN_POINT ( 'NONE',  ( 5.690095194620785612, 1.200872180055783112, 1.615535318972769474 ) ) ;
#79066=CARTESIAN_POINT ( 'NONE',  ( 4.085071245346539648, -0.2040513417298230325, -2.096037468315871788 ) ) ;
#79067=CARTESIAN_POINT ( 'NONE',  ( 1.722145930190256191, 1.895023070986867619, 0.2790570245742740041 ) ) ;
#79069=CARTESIAN_POINT ( 'NONE',  ( 2.664455434096600683, -0.7511504341344789060, -1.820894044046962534 ) ) ;
#79070=CARTESIAN_POINT ( 'NONE',  ( 5.765880396963712684, 0.5824918586248282182, -1.933996001582516611 ) ) ;
#79071=CARTESIAN_POINT ( 'NONE',  ( 1.762360912074714125, -1.325010844092512796, 1.320751239342173200 ) ) ;
#79072=CARTESIAN_POINT ( 'NONE',  ( 2.523818479427087702, 1.924573107942130656, -0.3798230296482503210 ) ) ;
#79073=CARTESIAN_POINT ( 'NONE',  ( 4.916472993244619616, 1.186103633638861288, -1.252587755385982771 ) ) ;
#79074=CARTESIAN_POINT ( 'NONE',  ( 1.230557176020010912, 1.282188879665364656, -1.419081615486268433 ) ) ;
#79076=CARTESIAN_POINT ( 'NONE',  ( 1.331021600797330118, 2.127646391749141941, 0.5858054460900484761 ) ) ;
#79083=CARTESIAN_POINT ( 'NONE',  ( 6.174686067066744499, 1.394736081427111252, -1.530067588329916628 ) ) ;
#79085=CARTESIAN_POINT ( 'NONE',  ( 1.363825363374836286, -0.5049007678423790280, 2.007717453658082629 ) ) ;
#79090=CARTESIAN_POINT ( 'NONE',  ( 4.916704032076687270, -0.7149955815140829340, -1.996424279390257572 ) ) ;
#79096=CARTESIAN_POINT ( 'NONE',  ( 3.866564406427867251, -0.5879305547937460075, 1.928456347981069241 ) ) ;
#79097=CARTESIAN_POINT ( 'NONE',  ( 3.626117945992116898, 1.907004414510531598, 0.1821707851048308124 ) ) ;
#79099=CARTESIAN_POINT ( 'NONE',  ( 2.085717061910817183, -0.9337068281064246911, 1.982830571388309204 ) ) ;
#79102=CARTESIAN_POINT ( 'NONE',  ( 5.414319639144633101, -2.013376227731620283, 0.004290823026709827959 ) ) ;
#79105=CARTESIAN_POINT ( 'NONE',  ( 5.396159345875370938, -0.9528639288615829983, -1.890782970011774422 ) ) ;
#79107=CARTESIAN_POINT ( 'NONE',  ( 3.368770691598612643, 0.04892471221396628434, -2.090337739860036681 ) ) ;
#79109=CARTESIAN_POINT ( 'NONE',  ( 2.150978262527812213, -1.382985381756835608, -1.030390371524889659 ) ) ;
#79111=CARTESIAN_POINT ( 'NONE',  ( 5.572555445586866441, 0.8612648569810870125, 1.938019255899057658 ) ) ;
#79122=CARTESIAN_POINT ( 'NONE',  ( 1.664434086620687703, 0.5685959063129341073, 1.719966406682835958 ) ) ;
#79133=CARTESIAN_POINT ( 'NONE',  ( 3.508111033888267283, 1.861241883637313688, 0.002260837353922766878 ) ) ;
#79135=CARTESIAN_POINT ( 'NONE',  ( 1.352997864604365885, 0.1391545085356447886, -1.910588907247000368 ) ) ;
#79136=CARTESIAN_POINT ( 'NONE',  ( 0.3404811318320751234, 0.3065618842239411501, 1.799498403862239915 ) ) ;
#79142=CARTESIAN_POINT ( 'NONE',  ( 5.664895447484411761, 1.493751497301420761, -1.283663174101207005 ) ) ;
#79145=CARTESIAN_POINT ( 'NONE',  ( 0.5860218096905758234, -2.075098906900944673, -0.2538066186672620628 ) ) ;
#79147=CARTESIAN_POINT ( 'NONE',  ( 5.913098435216375570, 1.699041482274340265, 0.9079036414736068039 ) ) ;
#79149=CARTESIAN_POINT ( 'NONE',  ( 1.026062881544724137, 1.091098483296793820, -1.463488004260153907 ) ) ;
#79150=CARTESIAN_POINT ( 'NONE',  ( 2.666872310945223923, -1.521158656661812714, 1.599105504226288499 ) ) ;
#79152=CARTESIAN_POINT ( 'NONE',  ( 0.2813230411330031044, 0.1852680230450229892, -1.903361379684164412 ) ) ;
#79153=( BOUNDED_CURVE ( )  B_SPLINE_CURVE ( 3, ( #92891, #10532, #76605, #98213 ),
 .UNSPECIFIED., .F., .T. ) 
 B_SPLINE_CURVE_WITH_KNOTS ( ( 4, 4 ),
 ( 0.000000000000000000, 0.4999999999999957812 ),
 .UNSPECIFIED. ) 
 CURVE ( )  GEOMETRIC_REPRESENTATION_ITEM ( )  RATIONAL_B_SPLINE_CURVE ( ( 1.000000000000000222, 0.3333333333333390325, 0.3333333333333334259, 0.9999999999999945599 ) ) 
 REPRESENTATION_ITEM ( '' )  );
#79156=CARTESIAN_POINT ( 'NONE',  ( 0.5550503504515170716, 1.639475800691666985, -1.091118944626153331 ) ) ;
#79157=CARTESIAN_POINT ( 'NONE',  ( 1.839301188190944902, 0.7414227542083090539, -1.795152619562689233 ) ) ;
#79159=CARTESIAN_POINT ( 'NONE',  ( 0.4739822347885510601, 1.752760637641921360, 0.9961516927870717186 ) ) ;
#79161=CARTESIAN_POINT ( 'NONE',  ( 5.014427361338555933, 0.7098351839037967403, 1.720451000603514524 ) ) ;
#79164=CARTESIAN_POINT ( 'NONE',  ( 6.509000000000034092, 7.052765612591089806, 2.598154238703707541 ) ) ;
#79167=CARTESIAN_POINT ( 'NONE',  ( 1.435386855117400717, -1.590506285900999295, -1.507976327226906443 ) ) ;
#79172=CARTESIAN_POINT ( 'NONE',  ( 1.840199252755945425, 1.805614550920462635, 0.2691313018618191055 ) ) ;
#79177=CARTESIAN_POINT ( 'NONE',  ( 6.609000000000015085, -6.653734696158637751E-05, 2.100160721423645960 ) ) ;
#79179=CARTESIAN_POINT ( 'NONE',  ( 1.330555237386946255, 1.856516968354186892, 0.5143259067744552215 ) ) ;
#79180=CARTESIAN_POINT ( 'NONE',  ( 6.104347744599991188, 1.959368324604572775, 0.09974838594294095639 ) ) ;
#79184=CARTESIAN_POINT ( 'NONE',  ( 5.478137895480934105, -2.137967713159651506, -0.4810252310911074525 ) ) ;
#79186=CARTESIAN_POINT ( 'NONE',  ( 4.399325512199628641, -1.803763729973751451, 1.015883459259236954 ) ) ;
#79191=CARTESIAN_POINT ( 'NONE',  ( 4.254688019566841284, 2.229798712500128843, -0.5580973643144919727 ) ) ;
#79198=CARTESIAN_POINT ( 'NONE',  ( 4.189351911999553479, -0.7420460110593477543, 1.794775118790333135 ) ) ;
#79199=EDGE_LOOP ( 'NONE', ( #31296, #85186, #68570, #65761 ) ) ;
#79203=CARTESIAN_POINT ( 'NONE',  ( 5.467032840998240495, -1.503656711810175350, 1.181500457595338505 ) ) ;
#79204=CARTESIAN_POINT ( 'NONE',  ( 6.616207624681263333, -0.8185094323158810248, -1.518158226148608625 ) ) ;
#79205=CARTESIAN_POINT ( 'NONE',  ( 4.979703994296570180, -0.7212954316567052881, 1.883311551353183511 ) ) ;
#79207=CARTESIAN_POINT ( 'NONE',  ( 2.086817400036289794, -2.164668306305051804, -0.4287355390964405211 ) ) ;
#79209=CARTESIAN_POINT ( 'NONE',  ( 1.675843188381221038, -1.117204103763050016, 1.766894365349908069 ) ) ;
#79210=CARTESIAN_POINT ( 'NONE',  ( 0.1448901830083254016, -1.363511527656173339, -1.128195317737596293 ) ) ;
#79211=CARTESIAN_POINT ( 'NONE',  ( 5.942029771888944545, -1.730864577151491890, -1.034168155301495862 ) ) ;
#79213=CARTESIAN_POINT ( 'NONE',  ( 3.591970686985697547, -2.289577047158963374, -0.1132367156824985732 ) ) ;
#79214=CARTESIAN_POINT ( 'NONE',  ( 1.288542162703592231, 1.315766340102142662, 1.139191825253932366 ) ) ;
#79216=CARTESIAN_POINT ( 'NONE',  ( 0.8074296549154248437, -1.491244094015523602, 0.8842416791710568935 ) ) ;
#79220=CARTESIAN_POINT ( 'NONE',  ( 1.873705115703153679, -0.2670016379083521296, 2.154652869704001272 ) ) ;
#79221=CARTESIAN_POINT ( 'NONE',  ( 2.835173002801576914, -1.651343842416473917, -1.157098616274463865 ) ) ;
#79222=CARTESIAN_POINT ( 'NONE',  ( 3.906250000000001776, 1.895863743163997084, -0.7852924748301890467 ) ) ;
#79225=CARTESIAN_POINT ( 'NONE',  ( 6.147092719882727430, -1.626042154682215468, 1.032876571686857536 ) ) ;
#79227=CARTESIAN_POINT ( 'NONE',  ( 3.867602925442710671, -1.848332671738551980, -1.231929692598219050 ) ) ;
#79234=CARTESIAN_POINT ( 'NONE',  ( 5.460439331044164568, -1.576930981450849867, -0.7368137880037448628 ) ) ;
#79235=CARTESIAN_POINT ( 'NONE',  ( 3.736726379466179804, -1.890069333072645241, -0.5255722985574098338 ) ) ;
#79239=CARTESIAN_POINT ( 'NONE',  ( 4.147957446309138874, 0.7671257181886274035, -2.128492778801443830 ) ) ;
#79241=CARTESIAN_POINT ( 'NONE',  ( 1.697793086734213697, -1.492557772401803318, -1.423914585240863673 ) ) ;
#79243=CARTESIAN_POINT ( 'NONE',  ( 2.676973543053912330, -2.164909235287615807, -0.6573374913001366338 ) ) ;
#79246=CARTESIAN_POINT ( 'NONE',  ( 3.374138713240721454, -1.116850685118627728, 1.500355210514233262 ) ) ;
#79247=CARTESIAN_POINT ( 'NONE',  ( 2.179902339641195397, 1.341075392948913425, 1.099452185880249067 ) ) ;
#79249=CARTESIAN_POINT ( 'NONE',  ( -0.1230140872038130023, -0.1644519934839226150, -2.256176000670232717 ) ) ;
#79250=CARTESIAN_POINT ( 'NONE',  ( 6.475599238194152285, 2.210894796874377288, -0.6610463658997690617 ) ) ;
#79251=CARTESIAN_POINT ( 'NONE',  ( 3.432649856329002880, 2.108609624295390006, 0.4754391814798044069 ) ) ;
#79252=CARTESIAN_POINT ( 'NONE',  ( 4.839755972451986743, 1.936857930295164065, 0.1413805851513943446 ) ) ;
#79254=CARTESIAN_POINT ( 'NONE',  ( 6.327412175546781370, -1.761338861328298089, 0.6302073946208713862 ) ) ;
#79261=CARTESIAN_POINT ( 'NONE',  ( 5.520157785563180930, -1.821743191724470634, 0.8647220171385738841 ) ) ;
#79265=CARTESIAN_POINT ( 'NONE',  ( 3.299243935302543118, 1.439784963707075649, 1.122460502641378755 ) ) ;
#79271=CARTESIAN_POINT ( 'NONE',  ( 1.318624316974380317, -0.7310098426952565953, -1.883032709213072975 ) ) ;
#79272=CARTESIAN_POINT ( 'NONE',  ( 1.190261156817543631, 1.266008754425467897, 1.700926646755014593 ) ) ;
#79274=CARTESIAN_POINT ( 'NONE',  ( 1.463465096324652714, -0.4588509492367858766, 1.803342318195770178 ) ) ;
#79277=CARTESIAN_POINT ( 'NONE',  ( 6.702032673877901914, -2.060500267551836018, 0.04777910199381221051 ) ) ;
#79278=CARTESIAN_POINT ( 'NONE',  ( 6.539686446881147752, -1.556848207870220602, 1.281141925495055123 ) ) ;
#79279=EDGE_LOOP ( 'NONE', ( #187538, #64018, #110177, #186572 ) ) ;
#79281=CARTESIAN_POINT ( 'NONE',  ( 3.721172816245840842, -0.1328194893376876962, 1.820914920514608459 ) ) ;
#79285=CARTESIAN_POINT ( 'NONE',  ( 5.888046020683160187, -0.05228737891407529703, 2.015604419750731680 ) ) ;
#79286=CARTESIAN_POINT ( 'NONE',  ( 6.052668933152094866, -1.581501214056714177, -0.9424504099920794076 ) ) ;
#79287=CARTESIAN_POINT ( 'NONE',  ( 0.2333690889706682703, 0.003390530909083006028, -2.053566628440507635 ) ) ;
#79288=CARTESIAN_POINT ( 'NONE',  ( 3.686388391042205726, -1.138424198849327107, 2.007274438705310970 ) ) ;
#79290=CARTESIAN_POINT ( 'NONE',  ( 5.554052124568397808, 2.159397089200214559, -0.09991998142631913771 ) ) ;
#79292=CARTESIAN_POINT ( 'NONE',  ( 1.329522225144257774, 0.9558622346672830394, -1.690450677827403103 ) ) ;
#79295=CARTESIAN_POINT ( 'NONE',  ( 4.148081960540086932, -0.2207414774363871957, -2.287749835899715034 ) ) ;
#79299=CARTESIAN_POINT ( 'NONE',  ( 4.785944050937030347, -0.8815013282119155136, 1.649949660215948688 ) ) ;
#79301=CARTESIAN_POINT ( 'NONE',  ( 1.898553772666348394, -1.876154101037771582, -0.3696338911259658411 ) ) ;
#79304=CARTESIAN_POINT ( 'NONE',  ( 4.477303810882872881, 0.001702072213635372200, -2.207063162522747479 ) ) ;
#79305=CARTESIAN_POINT ( 'NONE',  ( 6.883263157960369583, 7.629137130509070275, 2.546189081643289942 ) ) ;
#79310=CARTESIAN_POINT ( 'NONE',  ( 2.055877211876644406, 1.966332055899377762, -0.1412752051469425008 ) ) ;
#79311=CARTESIAN_POINT ( 'NONE',  ( 0.8335961714901140018, 0.1734020439737720132, 2.301109984577158762 ) ) ;
#79312=CARTESIAN_POINT ( 'NONE',  ( 2.154674626568295892, -0.5202524484802829585, -1.891573884155263396 ) ) ;
#79314=CARTESIAN_POINT ( 'NONE',  ( 5.629752743445687990, 1.989327071453067752, -0.5446528645957140480 ) ) ;
#79321=CARTESIAN_POINT ( 'NONE',  ( 0.6026744816367580748, 2.165159614417012879, 0.1613400170472640283 ) ) ;
#79324=CARTESIAN_POINT ( 'NONE',  ( 2.178771278573924608, -0.08713135167291723160, -1.868625915979430729 ) ) ;
#79327=CARTESIAN_POINT ( 'NONE',  ( 6.573507624224045109, 2.070638407997299257, -0.6205318887850322929 ) ) ;
#79328=CARTESIAN_POINT ( 'NONE',  ( 6.727182134110205602, 7.053355583909074689, 2.409100679957976165 ) ) ;
#79330=CARTESIAN_POINT ( 'NONE',  ( 2.420441844550869526, -0.7335502799032426191, -1.766186906296034698 ) ) ;
#79331=CARTESIAN_POINT ( 'NONE',  ( 4.592510532270950740, -0.3890688374885014067, -1.726373200486588377 ) ) ;
#79332=CARTESIAN_POINT ( 'NONE',  ( 1.770022778749248182, 1.907080152163560971, -0.1419829583147319274 ) ) ;
#79335=CARTESIAN_POINT ( 'NONE',  ( 5.325768798837505535, 0.7719732895165082320, -1.753353820041517741 ) ) ;
#79337=CARTESIAN_POINT ( 'NONE',  ( 6.654754201047359707, -0.5240520113350942699, -1.898494369619908140 ) ) ;
#79339=CARTESIAN_POINT ( 'NONE',  ( 2.443736651115399283, -1.977012053918187906, 0.7674769708189137507 ) ) ;
#79341=CARTESIAN_POINT ( 'NONE',  ( 4.821099876132087125, -0.09137817997613774390, 1.868553921495450965 ) ) ;
#79342=CARTESIAN_POINT ( 'NONE',  ( 1.506192966688112422, -0.6554880476431452774, -1.704135612709246184 ) ) ;
#79344=CARTESIAN_POINT ( 'NONE',  ( 4.319099500008596770, 2.017107695584336557, 0.8957252843501888329 ) ) ;
#79348=CARTESIAN_POINT ( 'NONE',  ( 2.154800422482431532, -0.5477745769525663722, -1.988566864369076592 ) ) ;
#79356=CARTESIAN_POINT ( 'NONE',  ( 4.088381982606685838, 1.110138344689771239, -1.747393465062855533 ) ) ;
#79358=CARTESIAN_POINT ( 'NONE',  ( 2.952577552874091626, 0.7252333659365679530, 2.036452211405047397 ) ) ;
#79360=CARTESIAN_POINT ( 'NONE',  ( 2.807290699014941548, 1.731141667658737449, -1.040073625836896554 ) ) ;
#79361=CARTESIAN_POINT ( 'NONE',  ( 6.620655732516668834, 7.629137130509086262, 2.673739711112704143 ) ) ;
#79366=CARTESIAN_POINT ( 'NONE',  ( 1.446500318503377125, -1.422605717829699801, 1.429450658469958668 ) ) ;
#79367=CARTESIAN_POINT ( 'NONE',  ( 6.181208317857348256, 1.509947553572440704, 1.588605474358975478 ) ) ;
#79369=CARTESIAN_POINT ( 'NONE',  ( 4.271672842113056312, 0.4137096367802223784, -1.866957553337177611 ) ) ;
#79373=CARTESIAN_POINT ( 'NONE',  ( 1.950796209937825321, -1.844718841590715863, -0.8146091914792084054 ) ) ;
#79376=CARTESIAN_POINT ( 'NONE',  ( 5.438411972298594854, 1.699845694858553857, 0.2911611187441583426 ) ) ;
#79377=CARTESIAN_POINT ( 'NONE',  ( -0.1394461523061351904, -0.009327122704730000241, -2.280146446826665230 ) ) ;
#79382=CARTESIAN_POINT ( 'NONE',  ( 1.516557075436252733, 0.8353943144701718726, 1.894387172633307692 ) ) ;
#79384=CARTESIAN_POINT ( 'NONE',  ( 4.670457322363490427, 0.6978976414240989357, 1.671844709466139722 ) ) ;
#79387=CARTESIAN_POINT ( 'NONE',  ( 6.551413666264667590, -1.614568043246225271, 0.8214943993307096681 ) ) ;
#79390=CARTESIAN_POINT ( 'NONE',  ( 3.187623232016934871, -0.8878212517344568067, 2.003729935572157839 ) ) ;
#79393=CARTESIAN_POINT ( 'NONE',  ( 0.6253529088778920775, 0.1960189665039281104, -1.952063659030291998 ) ) ;
#79395=CARTESIAN_POINT ( 'NONE',  ( 4.411684386003834391, -1.181747345438967312, -1.507543049613221386 ) ) ;
#79402=CARTESIAN_POINT ( 'NONE',  ( 1.569428280142046495, 0.1587979871724466974, -2.155937297210829495 ) ) ;
#79405=CARTESIAN_POINT ( 'NONE',  ( 1.922601709848625440, 1.702220721529534853, 0.6601445126475160574 ) ) ;
#79407=CARTESIAN_POINT ( 'NONE',  ( 4.664971680594516279, -1.631047870213175432, -0.8201845326444437978 ) ) ;
#79408=EDGE_CURVE ( 'NONE', #97632, #168104, #130873, .T. ) ;
#79410=CARTESIAN_POINT ( 'NONE',  ( 2.953266587970606150, -1.684550232849800544, 0.9053361341156559439 ) ) ;
#79412=CARTESIAN_POINT ( 'NONE',  ( 3.648844292986920479, -0.3817546106285915619, -1.932013994212372854 ) ) ;
#79414=CARTESIAN_POINT ( 'NONE',  ( 5.970255158568685161, -1.845527328187264615, -0.6049325008806984982 ) ) ;
#79415=ORIENTED_EDGE ( 'NONE', *, *, #149244, .F. ) ;
#79418=CARTESIAN_POINT ( 'NONE',  ( 4.834296457332984076, -1.136628438424293508, -1.790084250976264002 ) ) ;
#79420=CARTESIAN_POINT ( 'NONE',  ( 3.158751774003202950, 0.4669426847015486493, 1.854258104404989060 ) ) ;
#79422=CARTESIAN_POINT ( 'NONE',  ( 6.983263157960368339, 4.695310640067480001, 2.508805386165738227 ) ) ;
#79425=CARTESIAN_POINT ( 'NONE',  ( 5.637363213272434059, -0.04718591601137950980, 2.012692011999743791 ) ) ;
#79427=CARTESIAN_POINT ( 'NONE',  ( 6.164658409365947556, -1.287482145768016339, 1.294691480910937775 ) ) ;
#79428=CARTESIAN_POINT ( 'NONE',  ( 0.5376586404672692998, 1.932363751568724641, -0.7437053376125392079 ) ) ;
#79442=CARTESIAN_POINT ( 'NONE',  ( 1.586871713678970730, 1.994102569620255228, 0.5559867524188369936 ) ) ;
#79443=CARTESIAN_POINT ( 'NONE',  ( 2.249754300142119856, 2.075745305004289332, -0.4162820868813913999 ) ) ;
#79446=CARTESIAN_POINT ( 'NONE',  ( 0.9187298884396404297, -1.430263011927451311, 1.354180262349208075 ) ) ;
#79450=PLANE ( 'NONE',  #194749 ) ;
#79452=CARTESIAN_POINT ( 'NONE',  ( 2.924086828919622238, 1.272802903806929953, -1.906236438263966271 ) ) ;
#79453=CARTESIAN_POINT ( 'NONE',  ( 0.6272434487209905818, -1.734552980249819631, 0.5698080454362154379 ) ) ;
#79454=CARTESIAN_POINT ( 'NONE',  ( 3.814637755342592307, -0.6046605605216844870, -1.814329123173196834 ) ) ;
#79458=CARTESIAN_POINT ( 'NONE',  ( 1.301040509920841526, -0.2996390532185671529, -1.990687865782204469 ) ) ;
#79459=CARTESIAN_POINT ( 'NONE',  ( 1.990992145637654698, 0.1870960246039363450, 1.952785824368876710 ) ) ;
#79463=CARTESIAN_POINT ( 'NONE',  ( 4.699217343460686536, -0.5580910489941055541, 2.014698706189700594 ) ) ;
#79464=CARTESIAN_POINT ( 'NONE',  ( 3.326767387183640956, 0.04228616847017605679, 1.769505212706389941 ) ) ;
#79467=CARTESIAN_POINT ( 'NONE',  ( 0.02373106683711476844, -1.352142385343929387, -1.725327757841053078 ) ) ;
#79468=CARTESIAN_POINT ( 'NONE',  ( 4.031004160980892870, -1.202209430963938619, -1.258585379614601596 ) ) ;
#79471=CARTESIAN_POINT ( 'NONE',  ( 4.323420094722703944, -1.284794005617446278, 1.164475704859231131 ) ) ;
#79472=CARTESIAN_POINT ( 'NONE',  ( 4.422458135217792297, 1.019899284492602698, 1.916704820016806199 ) ) ;
#79474=CARTESIAN_POINT ( 'NONE',  ( 6.087125082597877324, 1.679220375458953862, 1.116214469231976869 ) ) ;
#79475=CARTESIAN_POINT ( 'NONE',  ( 5.531250000000004441, -0.7852924748302730906, -1.895863743163958226 ) ) ;
#79477=CARTESIAN_POINT ( 'NONE',  ( 3.170836325157891267, -1.779339148710285867, -0.7386555552950261339 ) ) ;
#79479=CARTESIAN_POINT ( 'NONE',  ( 0.1006276693296826175, -1.041319732255343355, 1.962097497535258084 ) ) ;
#79481=CARTESIAN_POINT ( 'NONE',  ( 6.883263157960335832, 7.629137130509051623, 2.446189081643288521 ) ) ;
#79485=CARTESIAN_POINT ( 'NONE',  ( 6.689906388054261299, -1.280585065398877731, -1.486383542710855821 ) ) ;
#79489=CARTESIAN_POINT ( 'NONE',  ( 0.07093568767341934533, -0.9480374005119349690, 1.779628194860154222 ) ) ;
#79491=CARTESIAN_POINT ( 'NONE',  ( 5.301261097381549270, -1.770826635688247386, 1.057502194177829979 ) ) ;
#79496=CARTESIAN_POINT ( 'NONE',  ( 6.854772330626868637, -1.445518619047950981, 1.186913843143226233 ) ) ;
#79497=CARTESIAN_POINT ( 'NONE',  ( 5.643113243286411063, 0.7107029072939261560, 1.582047324045066095 ) ) ;
#79498=CARTESIAN_POINT ( 'NONE',  ( 5.565861978284946332, -1.097836388496459037, 1.350534753149737366 ) ) ;
#79501=CARTESIAN_POINT ( 'NONE',  ( 3.175583430956610886, 1.455732557240730696, 1.770799584264992399 ) ) ;
#79503=CARTESIAN_POINT ( 'NONE',  ( 1.411775340717499994, 1.237668241052336970, -1.363247244775968259 ) ) ;
#79506=CARTESIAN_POINT ( 'NONE',  ( 1.799542586263824795, -0.6183211656001773582, 1.717807299235304619 ) ) ;
#79507=CARTESIAN_POINT ( 'NONE',  ( 2.391250195717840477, -0.7743161457766101208, -1.862016636315230844 ) ) ;
#79508=CARTESIAN_POINT ( 'NONE',  ( 1.658417429842372393, -1.548019161032044844, 1.551412955586493947 ) ) ;
#79510=CARTESIAN_POINT ( 'NONE',  ( 4.471769775969771210, 2.043305595564361088, -0.5093722314385378258 ) ) ;
#79514=CARTESIAN_POINT ( 'NONE',  ( 1.047426762419433777, 1.826728496382063582, -0.9743617655595809834 ) ) ;
#79517=CARTESIAN_POINT ( 'NONE',  ( 4.758503674095369007, 2.114844282287762667, 0.1552407789479764155 ) ) ;
#79518=CARTESIAN_POINT ( 'NONE',  ( 6.147073579019600054, -1.539581890156189292, 0.9809480439507823890 ) ) ;
#79519=ADVANCED_FACE ( 'NONE', ( #176615 ), #63131, .F. ) ;
#79526=CARTESIAN_POINT ( 'NONE',  ( 6.205353461901607304, 1.844339991697005798, -1.046509186232460697 ) ) ;
#79527=CARTESIAN_POINT ( 'NONE',  ( 1.184755817749640894, -2.054561091436296838, -0.4616562467647678525 ) ) ;
#79530=CARTESIAN_POINT ( 'NONE',  ( 5.453892037968048001, -0.6717839469763884352, 1.735626407379993186 ) ) ;
#79536=CARTESIAN_POINT ( 'NONE',  ( 2.189831975649577878, -1.279155337443920404, -1.487614327915102841 ) ) ;
#79537=CARTESIAN_POINT ( 'NONE',  ( 0.6026772488060898603, -0.7295331166810551382, -2.035022307366324945 ) ) ;
#79541=CARTESIAN_POINT ( 'NONE',  ( 3.356526315702735186, -0.7047320765170405066, 1.584360681437890550 ) ) ;
#79542=CARTESIAN_POINT ( 'NONE',  ( 2.941039689149751890, 0.6260299441606477222, -1.624016774299047228 ) ) ;
#79545=CARTESIAN_POINT ( 'NONE',  ( 2.776696059289599283, -1.970994871289712069, -0.6015693623636628740 ) ) ;
#79546=CARTESIAN_POINT ( 'NONE',  ( 0.7200771085676247463, -1.701685607325746252, -1.080902626906909747 ) ) ;
#79547=CARTESIAN_POINT ( 'NONE',  ( 6.925078400183575233, 2.022016365062285104, 2.447829694591229899 ) ) ;
#79550=CARTESIAN_POINT ( 'NONE',  ( 1.147272922670502515, -1.552894836003695600, -1.214464739729806730 ) ) ;
#79551=CARTESIAN_POINT ( 'NONE',  ( 6.328373294368253354, -0.9077179077918960948, -1.683272687665722467 ) ) ;
#79556=CARTESIAN_POINT ( 'NONE',  ( 0.7330764811492549438, 1.866981473359119237, 0.7708630573498123084 ) ) ;
#79557=CARTESIAN_POINT ( 'NONE',  ( 4.313705703444643547, -0.3987071732099633503, 2.272742389722400169 ) ) ;
#79558=CARTESIAN_POINT ( 'NONE',  ( 6.004347769543215030, 1.959566550440184907, 0.09775035808561728656 ) ) ;
#79559=CARTESIAN_POINT ( 'NONE',  ( 2.430452978529148655, -1.210835280720125917, 1.543375930141199115 ) ) ;
#79561=CARTESIAN_POINT ( 'NONE',  ( -0.05211191391743182078, -1.802403943428915412, -0.9041556775107385535 ) ) ;
#79563=CARTESIAN_POINT ( 'NONE',  ( 1.288444443960437225, -0.7676182150243222591, -1.973457848717992569 ) ) ;
#79566=CARTESIAN_POINT ( 'NONE',  ( 1.411775340717499994, 1.237668241052336970, -1.363247244775968259 ) ) ;
#79568=CARTESIAN_POINT ( 'NONE',  ( 4.821225769315531373, -1.936335391968559527, -0.9821231961690338741 ) ) ;
#79570=CARTESIAN_POINT ( 'NONE',  ( 2.074623746436579985, 0.9110886696130392481, 1.915067268644244702 ) ) ;
#79574=CARTESIAN_POINT ( 'NONE',  ( 3.725900457647839392, -1.224662966953151688, -1.657274842633131851 ) ) ;
#79577=CARTESIAN_POINT ( 'NONE',  ( 0.1515692981730529243, 0.7036590017722235135, 1.701685288394996665 ) ) ;
#79582=CARTESIAN_POINT ( 'NONE',  ( 2.196875584952286964, -0.6017768564574823564, -2.180865832541518667 ) ) ;
#79584=CARTESIAN_POINT ( 'NONE',  ( 2.900440330899815233, -1.785477387793675597, -0.3053432404436141057 ) ) ;
#79585=CARTESIAN_POINT ( 'NONE',  ( 1.920960065284383678, -1.709437138374754639, 0.8649676252809009869 ) ) ;
#79586=CARTESIAN_POINT ( 'NONE',  ( 3.121598655985452275, 0.3063859900464052100, -2.047459029603612368 ) ) ;
#79588=CARTESIAN_POINT ( 'NONE',  ( 1.533988556244444856, 0.9736202887896376890, -1.714215200822625684 ) ) ;
#79589=CARTESIAN_POINT ( 'NONE',  ( 6.199827818874126706, -0.6464308959919072839, 1.814938386029739892 ) ) ;
#79590=CARTESIAN_POINT ( 'NONE',  ( 2.940157781200231746, 1.856316385841882965, 0.2306766016651334850 ) ) ;
#79592=CARTESIAN_POINT ( 'NONE',  ( 1.383892495861089644, 2.130622466349596511, -0.8869745915042435147 ) ) ;
#79594=CARTESIAN_POINT ( 'NONE',  ( 2.875287963320713569, -0.1852811808005799254, 1.851819283609082323 ) ) ;
#79596=CARTESIAN_POINT ( 'NONE',  ( 5.723111435942265679, -1.863175293877845418, -0.8853075346121098699 ) ) ;
#79600=CARTESIAN_POINT ( 'NONE',  ( 6.299853487814777608, -0.7131585336714525436, 1.981663801677714831 ) ) ;
#79602=CARTESIAN_POINT ( 'NONE',  ( 5.518883860308030798, 1.994880785013030788, 0.8329173350848093627 ) ) ;
#79603=CARTESIAN_POINT ( 'NONE',  ( 6.551426717330563143, -1.803173079755305608, 0.9099084737219197416 ) ) ;
#79607=CARTESIAN_POINT ( 'NONE',  ( 6.925078400183550364, 2.474256779287649088, 2.140290375984225335 ) ) ;
#79610=CARTESIAN_POINT ( 'NONE',  ( 4.171111447311355747, 1.799123655847803205, -0.9110083886025857058 ) ) ;
#79615=CARTESIAN_POINT ( 'NONE',  ( 5.770447993230207295, -1.374857387916775364, 1.668144713590607120 ) ) ;
#79620=CARTESIAN_POINT ( 'NONE',  ( 5.712517600013328867, 1.944077172375497486, 0.5350714256760413789 ) ) ;
#79622=CARTESIAN_POINT ( 'NONE',  ( 1.418105696869888410, 1.160834107949513472, -1.275986549933407543 ) ) ;
#79627=CARTESIAN_POINT ( 'NONE',  ( 6.081297793977560318, 1.728434112010367674, -0.7156336962577531935 ) ) ;
#79628=CARTESIAN_POINT ( 'NONE',  ( 1.242838715397933225, 1.940741670474394498, 0.5346661475282618037 ) ) ;
#79630=CARTESIAN_POINT ( 'NONE',  ( 3.030518406005321186, 1.227118389542980026, -1.833929004854919054 ) ) ;
#79632=CARTESIAN_POINT ( 'NONE',  ( 5.295835511405859286, -1.530271966869084954, -1.540324818649402072 ) ) ;
#79636=CARTESIAN_POINT ( 'NONE',  ( 3.721430941620011534, 1.819509361161365524, 1.088713516244857571 ) ) ;
#79637=CARTESIAN_POINT ( 'NONE',  ( 2.091422941747251851, -0.4390073250180904219, 1.967893905867940996 ) ) ;
#79638=CARTESIAN_POINT ( 'NONE',  ( 1.880848235559588799, -1.657448921354220506, -0.7316143304627804600 ) ) ;
#79646=CARTESIAN_POINT ( 'NONE',  ( 1.569406966088880084, 1.323937531303821968, 1.384834552875470415 ) ) ;
#79653=CARTESIAN_POINT ( 'NONE',  ( 4.821240550277555492, -0.1094919189667045711, 2.159058991224649393 ) ) ;
#79656=CARTESIAN_POINT ( 'NONE',  ( 2.637105894733019262, 1.998242115483703341, 0.7103459930332192140 ) ) ;
#79659=CARTESIAN_POINT ( 'NONE',  ( 3.057844483195955032, 1.962173284599289858, -0.1898399627659839439 ) ) ;
#79660=CARTESIAN_POINT ( 'NONE',  ( 5.220932206144772714, 1.444093599275039885, -1.253800916539760113 ) ) ;
#79663=CARTESIAN_POINT ( 'NONE',  ( 0.2564123431100414074, -2.069877475643782994, -0.05227228806716639753 ) ) ;
#79664=CARTESIAN_POINT ( 'NONE',  ( 2.572129589083424150, -1.858482343604623610, -0.5632287606567585314 ) ) ;
#79669=CARTESIAN_POINT ( 'NONE',  ( 2.168024591681999791, -1.285456077792548335, 1.648657952768191715 ) ) ;
#79672=CARTESIAN_POINT ( 'NONE',  ( 6.393217174440144035, -0.09883813596619006603, -1.909861267343159863 ) ) ;
#79674=CARTESIAN_POINT ( 'NONE',  ( 3.897267319706390065, 1.864829029706360330, -1.179861312946443697 ) ) ;
#79675=CARTESIAN_POINT ( 'NONE',  ( 3.522699392456357881, 1.401646575410384843, -1.704459333586108016 ) ) ;
#79678=CARTESIAN_POINT ( 'NONE',  ( 2.033716200607054159, -1.854476301366870805, 0.4660679227486630438 ) ) ;
#79681=CARTESIAN_POINT ( 'NONE',  ( 4.580570967453869713, 1.276285970795057345, -1.630082184409971324 ) ) ;
#79683=CARTESIAN_POINT ( 'NONE',  ( 3.362350911093567873, 0.9703303321016673033, 1.931748911306984784 ) ) ;
#79684=CARTESIAN_POINT ( 'NONE',  ( 4.933237592207079025, -1.549687834843778811, -1.549900206446311657 ) ) ;
#79691=CARTESIAN_POINT ( 'NONE',  ( 0.5982800022500452952, -0.2930678230431381648, 1.994870242743536304 ) ) ;
#79693=CARTESIAN_POINT ( 'NONE',  ( 4.803616497939601437, -1.596918191575155133, -1.317456641179854726 ) ) ;
#79694=CARTESIAN_POINT ( 'NONE',  ( 2.877471820773948252, 1.829258416151048561, -0.6045268202574998195 ) ) ;
#79695=CARTESIAN_POINT ( 'NONE',  ( 6.169547404874395014, 1.460173559465412829, 1.533355976833279621 ) ) ;
#79698=CARTESIAN_POINT ( 'NONE',  ( 4.522284192717240359, 0.9245163773116799044, 1.738918859443546516 ) ) ;
#79699=CARTESIAN_POINT ( 'NONE',  ( 6.140627040082555332, -1.939752761746313059, 1.221158637518650503 ) ) ;
#79700=CARTESIAN_POINT ( 'NONE',  ( 4.353998665852670591, 1.825246345946249571, -0.04724550102237072557 ) ) ;
#79706=CARTESIAN_POINT ( 'NONE',  ( 1.100829259350871281, -0.4471758257712907247, 1.786007343351428966 ) ) ;
#79707=CARTESIAN_POINT ( 'NONE',  ( 5.660407656431548418, 2.011079132963066840, 0.09461074985974733675 ) ) ;
#79708=CARTESIAN_POINT ( 'NONE',  ( 6.539654151966706408, -1.780142272834178918, 1.453760081647121671 ) ) ;
#79709=CARTESIAN_POINT ( 'NONE',  ( 5.928557400228100960, -1.247251702497784942, 1.514172074262534196 ) ) ;
#79713=CARTESIAN_POINT ( 'NONE',  ( 1.540690653510309538, -1.764467595836321401, 1.121255944808132288 ) ) ;
#79714=CARTESIAN_POINT ( 'NONE',  ( 6.297684251969362101, -0.5920937881782936119, 1.667988322058571393 ) ) ;
#79716=CARTESIAN_POINT ( 'NONE',  ( -0.2102771530458277249, 5.719403664101017526, -2.797728457938574387 ) ) ;
#79717=CARTESIAN_POINT ( 'NONE',  ( 1.153398195617076682, 0.7042877955899041753, 1.591771711926233346 ) ) ;
#79721=CARTESIAN_POINT ( 'NONE',  ( 2.050978400279603875, -1.384275906022333968, -1.028850351009907849 ) ) ;
#79722=CARTESIAN_POINT ( 'NONE',  ( 1.646283778714407342, 0.6915601415973006150, 2.079641132013386517 ) ) ;
#79723=CARTESIAN_POINT ( 'NONE',  ( -0.1229578505166153690, -0.3670672422863025530, -1.699768244568555353 ) ) ;
#79724=CARTESIAN_POINT ( 'NONE',  ( 4.248781725523794073, 0.5872999373685274804, 2.127227798101683387 ) ) ;
#79726=CARTESIAN_POINT ( 'NONE',  ( 1.833130710876787584, -2.060620742141227701, -0.6837463184809766670 ) ) ;
#79727=CARTESIAN_POINT ( 'NONE',  ( 0.3811277156573149583, 1.704729334087114578, -0.6539457117896373406 ) ) ;
#79728=CARTESIAN_POINT ( 'NONE',  ( 2.149754410345839251, 2.075462379332591478, -0.4182697058867020923 ) ) ;
#79731=CARTESIAN_POINT ( 'NONE',  ( 2.244040508683461166, 2.291928982054102004, 0.05232369179298743123 ) ) ;
#79735=CARTESIAN_POINT ( 'NONE',  ( 5.567086426426935297, -1.752359028239593997, 1.364940763008470226 ) ) ;
#79741=CARTESIAN_POINT ( 'NONE',  ( 3.551407868487792552, -1.352154898762620849, 1.496051317864899088 ) ) ;
#79743=CARTESIAN_POINT ( 'NONE',  ( 2.307554651200398599, -1.654038752482372088, -1.231991790176652612 ) ) ;
#79749=CARTESIAN_POINT ( 'NONE',  ( 5.332042502257137606, 2.158596015244533373, 0.3771327725019049670 ) ) ;
#79750=CARTESIAN_POINT ( 'NONE',  ( 2.303361484738715159, 1.314996338066702242, -1.528741580717301263 ) ) ;
#79751=CARTESIAN_POINT ( 'NONE',  ( 2.401689157922583640, -0.7064633820979376866, -1.700523668893457296 ) ) ;
#79753=CARTESIAN_POINT ( 'NONE',  ( 5.526323803393728085, 1.085782926936417425, -1.467421699745217412 ) ) ;
#79754=CARTESIAN_POINT ( 'NONE',  ( 6.117814597332064785, 0.2004318333163370436, 2.006446488866588496 ) ) ;
#79756=CARTESIAN_POINT ( 'NONE',  ( 5.612299388031473768, -1.011774156007083869, -2.023756622241212000 ) ) ;
#79758=CARTESIAN_POINT ( 'NONE',  ( 0.8738170914556376845, 2.029154634757854847, -0.5636997952245518251 ) ) ;
#79770=CARTESIAN_POINT ( 'NONE',  ( 2.004293344102888508, -0.9022931611136343344, 1.919180038594799687 ) ) ;
#79771=CARTESIAN_POINT ( 'NONE',  ( 2.338390812749164827, -1.283062462031187456, -1.813217020134863411 ) ) ;
#79776=CARTESIAN_POINT ( 'NONE',  ( 3.332423539472821439, -1.170687260143790320, 1.574129132985650825 ) ) ;
#79782=CARTESIAN_POINT ( 'NONE',  ( 1.916421503514931679, -2.120014230100770725, 0.05699577502370903326 ) ) ;
#79784=CARTESIAN_POINT ( 'NONE',  ( 4.504844740329728481, 1.672958716126593082, -1.369014088531981255 ) ) ;
#79785=CARTESIAN_POINT ( 'NONE',  ( 2.401689157922583640, -0.7064633820979376866, -1.700523668893457296 ) ) ;
#79788=CARTESIAN_POINT ( 'NONE',  ( 6.316323101372843141, 1.626595589989995982, 0.6193309307870945579 ) ) ;
#79793=CARTESIAN_POINT ( 'NONE',  ( 2.747127081003514881, -1.797865629537301668, 1.199965651887124896 ) ) ;
#79794=CARTESIAN_POINT ( 'NONE',  ( 4.112657547701242144, 0.6818919214185631406, -1.897407125352356339 ) ) ;
#79796=CARTESIAN_POINT ( 'NONE',  ( 2.131903390035182255, -1.411712784473453830, -1.637176306262012826 ) ) ;
#79797=EDGE_CURVE ( 'NONE', #60268, #120459, #190267, .T. ) ;
#79798=CARTESIAN_POINT ( 'NONE',  ( 2.706272882855005335, -0.7510657119417161187, -1.822867458954416708 ) ) ;
#79800=CARTESIAN_POINT ( 'NONE',  ( 4.194824786304445219, 1.561856751782536135, 1.154042840620983057 ) ) ;
#79809=CARTESIAN_POINT ( 'NONE',  ( 1.589210545419886378, -0.3244246349418925535, -2.182665228674217861 ) ) ;
#79811=CARTESIAN_POINT ( 'NONE',  ( 4.768382384511014038, -0.8351381170168621360, -1.775225883709200980 ) ) ;
#79815=CARTESIAN_POINT ( 'NONE',  ( 0.07499057489267992038, 0.7202342490539682673, -2.037914685249627045 ) ) ;
#79816=CARTESIAN_POINT ( 'NONE',  ( 4.083814069670049562, -1.821384084514931612, -0.2681248149544179227 ) ) ;
#79817=ORIENTED_EDGE ( 'NONE', *, *, #120271, .T. ) ;
#79821=CARTESIAN_POINT ( 'NONE',  ( 6.381110825713084189, -1.939362502171553482, -0.8581636585355473246 ) ) ;
#79826=CARTESIAN_POINT ( 'NONE',  ( 6.468051757712944827, 1.055310785928347928, 1.769903775486596054 ) ) ;
#79828=CARTESIAN_POINT ( 'NONE',  ( 1.433807476322545904, 1.104820645310525373, 1.497481488779895731 ) ) ;
#79829=CARTESIAN_POINT ( 'NONE',  ( 3.579498943475650563, -0.9044721095569520086, 1.603693017070174864 ) ) ;
#79835=CARTESIAN_POINT ( 'NONE',  ( 3.123846942790895476, -2.126788776302591888, 0.5888931905130634359 ) ) ;
#79836=CARTESIAN_POINT ( 'NONE',  ( 5.518922325393873507, 2.087324940739025525, 0.8731552084927389767 ) ) ;
#79839=CARTESIAN_POINT ( 'NONE',  ( 6.328355405667826616, -0.8624701743435190249, -1.593140579868371987 ) ) ;
#79840=CARTESIAN_POINT ( 'NONE',  ( 5.805858164762184082, -1.070174230454253639, -1.588719782701804695 ) ) ;
#79842=CARTESIAN_POINT ( 'NONE',  ( 6.684453402082996654, -1.835023323784425564, -0.3624468955198830722 ) ) ;
#79843=CARTESIAN_POINT ( 'NONE',  ( 6.426204213344836269, 0.9576725794440078543, 1.595564698446788388 ) ) ;
#79845=CARTESIAN_POINT ( 'NONE',  ( 6.227411129102443432, -1.664988906758845921, 0.6005623136680103835 ) ) ;
#79846=CARTESIAN_POINT ( 'NONE',  ( 0.8136858238772455287, -1.282993010278702606, -1.555696519147983459 ) ) ;
#79848=CARTESIAN_POINT ( 'NONE',  ( 2.754625382576633807, 0.7102545713932090221, 1.982823988820613170 ) ) ;
#79853=CARTESIAN_POINT ( 'NONE',  ( 3.427994306938833002, -1.989183439576122758, 0.3493681432537446563 ) ) ;
#79856=CARTESIAN_POINT ( 'NONE',  ( 3.638091081701349871, 0.9754702174074175725, -1.929073278114090684 ) ) ;
#79860=CARTESIAN_POINT ( 'NONE',  ( 0.8718042753090318175, -0.3185811321036461363, 2.147578089749022645 ) ) ;
#79864=CARTESIAN_POINT ( 'NONE',  ( 2.419692422129790632, -1.264489869534379141, -1.789777738334753732 ) ) ;
#79866=CARTESIAN_POINT ( 'NONE',  ( 2.536292628665572479, 1.067014414141453704, -1.995120597088717806 ) ) ;
#79873=CARTESIAN_POINT ( 'NONE',  ( 3.286155083303475166, -1.742946490318267205, -0.3057894240724549628 ) ) ;
#79875=CARTESIAN_POINT ( 'NONE',  ( 6.405322867445039314, 1.831175526881479776, 1.231239259074583092 ) ) ;
#79878=CARTESIAN_POINT ( 'NONE',  ( 5.747672784407955149, 1.986098415631059932, -0.3474865836668520336 ) ) ;
#79881=CARTESIAN_POINT ( 'NONE',  ( 4.188257260935820625, -1.850246793840780279, -0.2747695030091561463 ) ) ;
#79882=CARTESIAN_POINT ( 'NONE',  ( 3.274343992483694787, -1.016290647400164282, -1.803532422793553636 ) ) ;
#79887=PRESENTATION_STYLE_ASSIGNMENT (( #193641 ) ) ;
#79890=CARTESIAN_POINT ( 'NONE',  ( 2.963279974173158138, 1.655882904019840840, 1.051842618152734499 ) ) ;
#79891=CARTESIAN_POINT ( 'NONE',  ( 1.071638489536786309, 1.528508772698906837, -1.314793605459969150 ) ) ;
#79895=CARTESIAN_POINT ( 'NONE',  ( 1.405301488743180061, -0.4598193086536165319, 1.813012767170335993 ) ) ;
#79897=CARTESIAN_POINT ( 'NONE',  ( 1.424089148264463089, -1.997494042244374768, 0.2507359931839692191 ) ) ;
#79899=CARTESIAN_POINT ( 'NONE',  ( 2.355205625472241771, 0.1007552864207492405, -2.114937101796029673 ) ) ;
#79901=CARTESIAN_POINT ( 'NONE',  ( 3.402844027952243167, 0.5003511028610057032, 2.008882729757965890 ) ) ;
#79902=B_SPLINE_CURVE_WITH_KNOTS ( 'NONE', 3,
 ( #27960, #208823, #26883, #75650, #172091, #73505, #174243, #207765, #108218, #125548, #142816 ),
 .UNSPECIFIED., .F., .F.,
 ( 4, 1, 1, 1, 1, 1, 1, 1, 4 ),
 ( 0.000000000000000000, 0.2255234228546724728, 0.3973271701647976828, 0.5245128843546777997, 0.6161923999872991331, 0.6815320185768301009, 0.7298552812456317040, 0.7704940248801678271, 1.000000000000000000 ),
 .UNSPECIFIED. ) ;
#79904=CARTESIAN_POINT ( 'NONE',  ( 6.035123006257053113, -1.513425687198214353, -1.442577094899047063 ) ) ;
#79906=CARTESIAN_POINT ( 'NONE',  ( 4.436427218767265757, 1.790408935156896586, 0.3557191534368231434 ) ) ;
#79914=CARTESIAN_POINT ( 'NONE',  ( 5.145129553670328981, 0.1446803459003667691, 1.906877450533929874 ) ) ;
#79921=CARTESIAN_POINT ( 'NONE',  ( 0.7140992756325338364, 1.701125707204935944, 0.7050099338341904165 ) ) ;
#79925=CARTESIAN_POINT ( 'NONE',  ( 4.235518730357812345, -1.288231833625707701, -1.356488508162751128 ) ) ;
#79926=CARTESIAN_POINT ( 'NONE',  ( 0.07700591528349547132, 1.369316849116916091, -2.165014180211277228 ) ) ;
#79932=CARTESIAN_POINT ( 'NONE',  ( 0.7253723109368491739, 0.1984653623241394993, -1.959446941136263831 ) ) ;
#79934=CARTESIAN_POINT ( 'NONE',  ( 2.284780001213771783, 1.617805504991537635, -1.203372706716873575 ) ) ;
#79938=CARTESIAN_POINT ( 'NONE',  ( 2.220887445055406584, 0.001640320231081903845, 2.191629467496846839 ) ) ;
#79950=CARTESIAN_POINT ( 'NONE',  ( 5.319803798718575116, 1.092037692397327620, -1.482314076171886708 ) ) ;
#79951=CARTESIAN_POINT ( 'NONE',  ( 1.787745399045566730, 1.925802014453177557, -0.5863169366013292194 ) ) ;
#79952=CARTESIAN_POINT ( 'NONE',  ( 4.077728334586081083, 1.628699396557086398, -1.621930329367648138 ) ) ;
#79953=CARTESIAN_POINT ( 'NONE',  ( -0.1290005225502918740, 6.946858002156244716, -2.769053915224591211 ) ) ;
#79954=CARTESIAN_POINT ( 'NONE',  ( 1.902945097309636013, -1.575467964945817867, 0.9901336090045903537 ) ) ;
#79956=CARTESIAN_POINT ( 'NONE',  ( 6.983263157960363898, -0.009046620988246927009, 2.153544821522495933 ) ) ;
#79957=CARTESIAN_POINT ( 'NONE',  ( 5.713130151434068438, 1.559639147136464343, -1.106415316399149473 ) ) ;
#79960=CARTESIAN_POINT ( 'NONE',  ( 5.091392180243133225, -0.7513228403347729234, 1.951278057808901512 ) ) ;
#79961=CARTESIAN_POINT ( 'NONE',  ( 3.959713429720784106, 1.856571849420919795, -0.2284545790810637578 ) ) ;
#79963=CARTESIAN_POINT ( 'NONE',  ( 5.548353751603532835, -1.447698842669535413, 1.137588655622793876 ) ) ;
#79966=CARTESIAN_POINT ( 'NONE',  ( 5.215364217145412873, -0.2476331258763775356, 1.706884187403294728 ) ) ;
#79969=CARTESIAN_POINT ( 'NONE',  ( 0.8790820841908916217, -0.4200629052855206491, -1.682323782590444461 ) ) ;
#79972=( NAMED_UNIT ( * ) PLANE_ANGLE_UNIT ( ) SI_UNIT ( $, .RADIAN. ) );
#79973=CARTESIAN_POINT ( 'NONE',  ( 4.469693783504245843, -0.3772167039018388124, 2.137918043537301305 ) ) ;
#79974=CARTESIAN_POINT ( 'NONE',  ( 3.088313589057069208, -1.798746773638896457, -0.3115406389907551810 ) ) ;
#79975=CARTESIAN_POINT ( 'NONE',  ( 0.8835585337332928502, -1.864609544942645414, 0.6100022000963196689 ) ) ;
#79976=CARTESIAN_POINT ( 'NONE',  ( 0.1580148589572556717, 1.223040929162301449, 1.728066982087714809 ) ) ;
#79978=CARTESIAN_POINT ( 'NONE',  ( 6.567932727852480390, -1.414834124515697011, 1.804577934655810401 ) ) ;
#79982=CARTESIAN_POINT ( 'NONE',  ( 2.912858673564645784, -0.6176872867308530468, -2.028511212565413224 ) ) ;
#79986=CARTESIAN_POINT ( 'NONE',  ( 0.3739936534635743270, -2.030981289472892026, 0.4004457479018645460 ) ) ;
#79987=CARTESIAN_POINT ( 'NONE',  ( 6.883263157960341161, 7.051904271082326758, 2.751962465287846271 ) ) ;
#79989=CARTESIAN_POINT ( 'NONE',  ( 2.684490341743519082, 1.190536367853095578, 1.875150363231482098 ) ) ;
#79991=CARTESIAN_POINT ( 'NONE',  ( 1.178858319146030009, 1.745148694481736484, 1.496268366688303653 ) ) ;
#79993=CARTESIAN_POINT ( 'NONE',  ( 5.243062877513432696, -0.2472539590166565604, -2.047610945800168114 ) ) ;
#79997=CARTESIAN_POINT ( 'NONE',  ( 0.2329586101569866563, 0.008238550247445517935, -1.845944905557160398 ) ) ;
#79998=CARTESIAN_POINT ( 'NONE',  ( 5.073706409418358376, -1.018251046719556685, 1.533866337327425278 ) ) ;
#80000=CARTESIAN_POINT ( 'NONE',  ( 1.676317214473854067, -1.636236659294947104, -0.5456935059391133658 ) ) ;
#80001=CARTESIAN_POINT ( 'NONE',  ( 0.7082206942033396624, 1.197301205363930254, -1.622488844446705381 ) ) ;
#80002=CARTESIAN_POINT ( 'NONE',  ( 1.758794133653733827, 2.198278648980501515, -0.6719540409268388581 ) ) ;
#80004=CARTESIAN_POINT ( 'NONE',  ( 2.003560550249494199, 1.880309486893988913, 1.257863985149072938 ) ) ;
#80005=CARTESIAN_POINT ( 'NONE',  ( 4.477239461409222798, 0.0005595100435150377523, -2.106257355078521964 ) ) ;
#80007=CARTESIAN_POINT ( 'NONE',  ( 2.336827959689928846, -1.583187595272864900, 0.7909824253358921364 ) ) ;
#80010=CARTESIAN_POINT ( 'NONE',  ( 5.284854174503876401, 2.022835781599085614, -1.078525118384612735 ) ) ;
#80015=CARTESIAN_POINT ( 'NONE',  ( 6.468989383178811892, -1.718075365336281246, 1.407709432230166202 ) ) ;
#80016=CARTESIAN_POINT ( 'NONE',  ( 5.103566685217446164, -2.181124530238859549, 0.2125310249164805709 ) ) ;
#80019=CARTESIAN_POINT ( 'NONE',  ( 6.633471380297788045, -0.1541069161683609745, 2.086224335282916620 ) ) ;
#80021=CARTESIAN_POINT ( 'NONE',  ( 2.877471820773948252, 1.829258416151048561, -0.6045268202574998195 ) ) ;
#80024=CARTESIAN_POINT ( 'NONE',  ( 5.484674493353773883, -1.343714522216314489, 1.640574901390474460 ) ) ;
#80030=CARTESIAN_POINT ( 'NONE',  ( 5.706567001488551227, 1.626822141722890303, 0.8623401093873286349 ) ) ;
#80034=CARTESIAN_POINT ( 'NONE',  ( 1.944474315927123387, -1.398120440366573680, -1.036317219087657504 ) ) ;
#80038=CARTESIAN_POINT ( 'NONE',  ( 6.684453901184132185, -2.118919246787358102, -0.4271090584619871566 ) ) ;
#80042=CARTESIAN_POINT ( 'NONE',  ( 5.506754051192107369, 1.639644015412666800, -1.408845030788405506 ) ) ;
#80046=CARTESIAN_POINT ( 'NONE',  ( 5.975845355540164938, 1.172130763738386650, 1.584922449839619052 ) ) ;
#80047=CARTESIAN_POINT ( 'NONE',  ( 5.219963594993116018, -1.465640877661518626, -0.9259742478883812300 ) ) ;
#80049=CARTESIAN_POINT ( 'NONE',  ( 1.435386855117400717, -1.590506285900999295, -1.507976327226906443 ) ) ;
#80050=CARTESIAN_POINT ( 'NONE',  ( 3.083396755883772933, -0.1683641986609325514, -2.301487591144059763 ) ) ;
#80051=CARTESIAN_POINT ( 'NONE',  ( 6.151650338133601181, 0.6026783403972060249, -1.970659962842249424 ) ) ;
#80052=CARTESIAN_POINT ( 'NONE',  ( 1.552571996792909248, -1.665377644223103637, -0.9986158231547156428 ) ) ;
#80058=CARTESIAN_POINT ( 'NONE',  ( 4.060867369437678676, 0.5686956411946364476, 2.042824496258560441 ) ) ;
#80060=CARTESIAN_POINT ( 'NONE',  ( 2.320935597664942396, 0.9480396085976348086, -1.779626998253575509 ) ) ;
#80062=CARTESIAN_POINT ( 'NONE',  ( 4.999154358079874960, 1.837129776665728187, -1.222328095618854693 ) ) ;
#80069=CARTESIAN_POINT ( 'NONE',  ( 4.381749043697905854, 1.344797980244310631, 1.561758987969330992 ) ) ;
#80074=CARTESIAN_POINT ( 'NONE',  ( 3.932289538495234549, -1.040048408385336964, -1.731156807262229425 ) ) ;
#80080=CARTESIAN_POINT ( 'NONE',  ( 3.010674446437047624, 1.493694004556917365, -1.420165857245965668 ) ) ;
#80081=CARTESIAN_POINT ( 'NONE',  ( 3.059220373557011818, -1.198860207862334049, 1.621182619130703273 ) ) ;
#80084=CARTESIAN_POINT ( 'NONE',  ( 0.8316833483592298570, 1.813467871694788069, 0.3170515863319539052 ) ) ;
#80085=CARTESIAN_POINT ( 'NONE',  ( 0.1183777584694784279, -2.261842813846013822, 0.4569907027171058456 ) ) ;
#80087=CARTESIAN_POINT ( 'NONE',  ( 2.970174626046932609, 1.153603175066318931, 1.827835936144058371 ) ) ;
#80089=CARTESIAN_POINT ( 'NONE',  ( 4.083301318022297899, 1.702923931485133879, 1.258099284506300153 ) ) ;
#80093=CARTESIAN_POINT ( 'NONE',  ( 1.094370286708164386, -0.4508366001288487412, -1.815394955969009239 ) ) ;
#80094=CARTESIAN_POINT ( 'NONE',  ( 4.575049868665863606, 0.0009985144121069796600, -1.971640593447765655 ) ) ;
#80095=CARTESIAN_POINT ( 'NONE',  ( 5.137907791644652278, 2.014008302827663854, -0.1037760698975112861 ) ) ;
#80099=CARTESIAN_POINT ( 'NONE',  ( 6.217421135136044441, -0.2594034420708571931, 2.089956235961006659 ) ) ;
#80100=CARTESIAN_POINT ( 'NONE',  ( 6.602015318333181781, 0.7961593463888805289, -1.911361562896146671 ) ) ;
#80104=CARTESIAN_POINT ( 'NONE',  ( 5.014510501881845883, 1.360076575639699081, -1.427402630902480762 ) ) ;
#80105=CARTESIAN_POINT ( 'NONE',  ( 6.029558467290160984, -0.2429869472727399504, 2.005020512606956018 ) ) ;
#80107=CARTESIAN_POINT ( 'NONE',  ( 4.442184936073533486, 0.9892916563519343898, -2.085014998049372625 ) ) ;
#80108=CARTESIAN_POINT ( 'NONE',  ( 2.131754086930433001, 1.975065156136386335, -0.5945119761870448771 ) ) ;
#80115=CARTESIAN_POINT ( 'NONE',  ( 4.106061665437168884, 0.7349691374628541940, -2.043110004675054103 ) ) ;
#80118=CARTESIAN_POINT ( 'NONE',  ( 3.386116603743833497, -0.3623624896987759914, -1.805063595765175499 ) ) ;
#80120=CARTESIAN_POINT ( 'NONE',  ( 6.720655732516657821, 4.700665033810172311, 2.388972926809574737 ) ) ;
#80121=CARTESIAN_POINT ( 'NONE',  ( 5.776942576169182608, 2.025397260235710206, -0.8375503648087383457 ) ) ;
#80123=CARTESIAN_POINT ( 'NONE',  ( 6.508658281791896094, 1.681912584842374159, -1.513523023287469016 ) ) ;
#80128=CARTESIAN_POINT ( 'NONE',  ( 6.731742716130249882, -1.158518921844574834, -1.337957499386055682 ) ) ;
#80130=CARTESIAN_POINT ( 'NONE',  ( 4.231111847260408787, 1.841413651135707985, 0.8138496092669408322 ) ) ;
#80132=CARTESIAN_POINT ( 'NONE',  ( 3.223755556863156180, -2.030008631501342808, 0.5602397303039460263 ) ) ;
#80133=CARTESIAN_POINT ( 'NONE',  ( 2.513182649960711945, -1.786459940013595205, 0.6919045257178286779 ) ) ;
#80136=CARTESIAN_POINT ( 'NONE',  ( 3.648844292986920479, -0.3817546106285915619, -1.932013994212372854 ) ) ;
#80138=CARTESIAN_POINT ( 'NONE',  ( 2.201827603038747139, -1.870314503716500099, 0.04339327950253490246 ) ) ;
#80139=CARTESIAN_POINT ( 'NONE',  ( 2.260140581184489239, -1.961506502764579052, 0.04509734162668613960 ) ) ;
#80140=CARTESIAN_POINT ( 'NONE',  ( 3.861678741103656165, 1.711552447172806968, -0.2133835738165473228 ) ) ;
#80141=CARTESIAN_POINT ( 'NONE',  ( 1.160255710619631397, 1.910328232974867868, 0.09094507755665059978 ) ) ;
#80143=CARTESIAN_POINT ( 'NONE',  ( 1.436444770134176485, 1.085300811998829662, -1.921501399296850821 ) ) ;
#80147=CARTESIAN_POINT ( 'NONE',  ( 6.737182200980119440, -1.669782060861616291, 0.8434366901180422316 ) ) ;
#80149=CARTESIAN_POINT ( 'NONE',  ( 6.438344962566215024, -1.112565956905732456, 1.745730973219234317 ) ) ;
#80151=CARTESIAN_POINT ( 'NONE',  ( 1.311079954825690619, -1.633285661836245906, 1.272233187909928454 ) ) ;
#80156=CARTESIAN_POINT ( 'NONE',  ( 5.778019675193696969, 2.089136139637823852, -0.3624112956793351659 ) ) ;
#80162=CARTESIAN_POINT ( 'NONE',  ( 6.742638286788313451, -1.923764577213080029, -0.3838556375530403630 ) ) ;
#80164=CARTESIAN_POINT ( 'NONE',  ( 4.024767406304472495, 2.001204788683898617, -0.2439926020210633206 ) ) ;
#80165=CARTESIAN_POINT ( 'NONE',  ( 3.784325452683900526, -0.6063896298742013080, -1.817255877250848473 ) ) ;
#80167=CARTESIAN_POINT ( 'NONE',  ( 1.980270094416748394, -2.150034404144373301, -0.4237573071887782983 ) ) ;
#80170=CARTESIAN_POINT ( 'NONE',  ( 4.746344407351839045, 1.031357595523854309, -1.728805965807812095 ) ) ;
#80173=CARTESIAN_POINT ( 'NONE',  ( 5.571900387404195243, -0.9513999510230609635, 1.891474119154999745 ) ) ;
#80176=CARTESIAN_POINT ( 'NONE',  ( 1.944979630195432074, -1.681012947115037015, -1.242954243213564292 ) ) ;
#80178=CARTESIAN_POINT ( 'NONE',  ( 1.201696739578085982, -1.724958192343982510, -0.005827584801694830549 ) ) ;
#80189=CARTESIAN_POINT ( 'NONE',  ( 1.998415993447474559, -1.776625121221590220, -0.3526093829155519388 ) ) ;
#80193=CARTESIAN_POINT ( 'NONE',  ( 2.754343952779594318, 1.798010375687082218, 0.2196673718751484539 ) ) ;
#80194=CARTESIAN_POINT ( 'NONE',  ( 6.539320575229249144, 0.007148032025052972194, 1.896977914940492393 ) ) ;
#80198=CARTESIAN_POINT ( 'NONE',  ( 2.752234738034575301, -1.855867026150724186, -0.1399345609422244507 ) ) ;
#80199=CARTESIAN_POINT ( 'NONE',  ( 0.8432031700210621539, 0.3724620109286616576, -1.878856871602401224 ) ) ;
#80200=CARTESIAN_POINT ( 'NONE',  ( 6.827182134110199030, 0.001020705822914885546, 1.910856149448316721 ) ) ;
#80208=CARTESIAN_POINT ( 'NONE',  ( 4.328926673881399623, -1.836050571085739769, -0.7129182788949259830 ) ) ;
#80213=CARTESIAN_POINT ( 'NONE',  ( 6.544889499999918314, -1.757580744090202041, -1.308772488114395616 ) ) ;
#80215=CARTESIAN_POINT ( 'NONE',  ( 5.403319659429405952, 1.574929826682970990, 1.109050863186450853 ) ) ;
#80219=CARTESIAN_POINT ( 'NONE',  ( 2.280145854635793334, 1.358931147977986420, 1.738775483816151768 ) ) ;
#80221=CARTESIAN_POINT ( 'NONE',  ( 0.3867804997886997720, -1.801505969789623629, -0.6421655129100201087 ) ) ;
#80224=CARTESIAN_POINT ( 'NONE',  ( 6.965690641875434075, -0.4316760948062084990, 1.928339623932231239 ) ) ;
#80225=CARTESIAN_POINT ( 'NONE',  ( 1.558044835347382362, -1.372074245553561722, 1.374660786877460072 ) ) ;
#80227=CARTESIAN_POINT ( 'NONE',  ( 0.6497672626537411844, -0.2439889887937417567, -2.001205234435725622 ) ) ;
#80229=CARTESIAN_POINT ( 'NONE',  ( 5.946130789595732935, -0.8379359121385165921, 1.661726607698276181 ) ) ;
#80235=CARTESIAN_POINT ( 'NONE',  ( 1.681448347407452193, 1.514353137444489406, 1.584415833815432162 ) ) ;
#80241=CARTESIAN_POINT ( 'NONE',  ( 1.734698295210383767, 0.1775668987445792879, 1.817036636966688823 ) ) ;
#80245=CARTESIAN_POINT ( 'NONE',  ( 6.609000000000011532, 3.695567819995113634, 2.514302272609474809 ) ) ;
#80247=CARTESIAN_POINT ( 'NONE',  ( 6.234959169399230561, 0.1841439077357870380, 1.816378869960999509 ) ) ;
#80248=CARTESIAN_POINT ( 'NONE',  ( 4.996903459272754588, 0.3314677610860050638, 1.933379042443456486 ) ) ;
#80251=CARTESIAN_POINT ( 'NONE',  ( 5.056268342064010213, -1.587557771011731678, 1.511049258477934032 ) ) ;
#80254=CARTESIAN_POINT ( 'NONE',  ( 4.100488025649267954, 2.059819936833905185, 0.2079151390043249559 ) ) ;
#80258=CARTESIAN_POINT ( 'NONE',  ( 4.571052534358505781, -1.084669189052098082, 2.026668040654127090 ) ) ;
#80262=CARTESIAN_POINT ( 'NONE',  ( 6.620655732516673275, 1.290356161719278028, 1.942653802560645460 ) ) ;
#80264=CARTESIAN_POINT ( 'NONE',  ( 3.538947879116743689, -1.471199320522957876, -1.267674678009507394 ) ) ;
#80267=CARTESIAN_POINT ( 'NONE',  ( 4.922078805074791674, -1.902621863305080430, 0.1933406509087298719 ) ) ;
#80269=CARTESIAN_POINT ( 'NONE',  ( 4.682452625960944026, -1.673401091975829091, -0.4171936932430859168 ) ) ;
#80270=CARTESIAN_POINT ( 'NONE',  ( 4.751185534883737738, 0.1928377863454934504, -2.007255887737584121 ) ) ;
#80271=CARTESIAN_POINT ( 'NONE',  ( 4.905072937705025282, -1.228516145343660826, -1.942733121961652376 ) ) ;
#80273=CARTESIAN_POINT ( 'NONE',  ( 0.3994152196779980346, 1.832435997337564348, -1.229551327501000380 ) ) ;
#80276=CARTESIAN_POINT ( 'NONE',  ( 5.483597806724121781, 1.189268614677735592, 1.310771863001722437 ) ) ;
#80277=CARTESIAN_POINT ( 'NONE',  ( 4.623672751230786027, 0.3474658942751900903, 1.986100912583692812 ) ) ;
#80279=CARTESIAN_POINT ( 'NONE',  ( 1.588225008415785844, -2.281566021618782081, -0.2212011980115625998 ) ) ;
#80280=CARTESIAN_POINT ( 'NONE',  ( 1.394060603838151779, 1.424319145653055507, -0.9997159833949519347 ) ) ;
#80282=CARTESIAN_POINT ( 'NONE',  ( 1.071195256775770543, 1.317505809736085665, -1.127239923523750909 ) ) ;
#80285=CARTESIAN_POINT ( 'NONE',  ( 1.522189222387077656, 2.139176736804601298, -0.3705008953195278454 ) ) ;
#80286=CARTESIAN_POINT ( 'NONE',  ( 2.782435679340321766, -0.5899881929209308540, -1.928257399728677601 ) ) ;
#80289=CARTESIAN_POINT ( 'NONE',  ( 0.2000540296341560831, -1.925883223908849251, -0.05090804828828016798 ) ) ;
#80291=CARTESIAN_POINT ( 'NONE',  ( 2.408681662258719047, -2.215777464676274011, -0.1586666079704464882 ) ) ;
#80299=CARTESIAN_POINT ( 'NONE',  ( 5.618645907585640309, -0.03427301787072359329, 1.740288698465036976 ) ) ;
#80300=CARTESIAN_POINT ( 'NONE',  ( 3.279693232472491893, -1.891448704997201302, 0.5207070127687256633 ) ) ;
#80304=CARTESIAN_POINT ( 'NONE',  ( 4.640055761359395348, 0.9730784542925293712, -2.042606338686814738 ) ) ;
#80305=CARTESIAN_POINT ( 'NONE',  ( 0.9770945003616584579, 1.905102050789074353, 0.7911672170514363334 ) ) ;
#80307=CARTESIAN_POINT ( 'NONE',  ( 2.729655337971720552, -2.111368630554604220, 0.8135341271046038214 ) ) ;
#80310=CARTESIAN_POINT ( 'NONE',  ( 3.426877311086639288, 0.04264493303338459662, 1.870215716092846314 ) ) ;
#80311=CARTESIAN_POINT ( 'NONE',  ( 2.654579492894239223, 0.9294799389642364185, 1.463784073337747849 ) ) ;
#80312=CARTESIAN_POINT ( 'NONE',  ( 6.251546423958431298, 2.185849743821382862, -0.1592787069685035195 ) ) ;
#80313=CARTESIAN_POINT ( 'NONE',  ( 0.1127427399064059588, -0.9454589178800475446, -1.991880357201977425 ) ) ;
#80314=CARTESIAN_POINT ( 'NONE',  ( 4.258765444007106105, -1.603684720688375975, 1.449730421305382544 ) ) ;
#80315=CARTESIAN_POINT ( 'NONE',  ( 4.470608273529505183, -0.001430698596973853159, -1.942124712226586558 ) ) ;
#80322=CARTESIAN_POINT ( 'NONE',  ( 5.906875006520014182, -1.122496024291631755, -1.674889250513518446 ) ) ;
#80326=CARTESIAN_POINT ( 'NONE',  ( 3.193790821891542731, -0.7392406677243367197, 1.669511829839696260 ) ) ;
#80328=CARTESIAN_POINT ( 'NONE',  ( -0.1296875068448125057, 2.889142263448498227, -2.315371602238533555 ) ) ;
#80333=CARTESIAN_POINT ( 'NONE',  ( 6.270176981224262924, 2.014133449145325105, -0.1505704652167982327 ) ) ;
#80334=CARTESIAN_POINT ( 'NONE',  ( 0.9793288802587530872, -1.918618388578940737, -0.9032494106611321794 ) ) ;
#80337=CARTESIAN_POINT ( 'NONE',  ( 2.377597188713850507, -1.806433865756534640, 0.4466691629738496760 ) ) ;
#80340=CARTESIAN_POINT ( 'NONE',  ( 0.1984014031938194922, -2.161264429664040421, -0.05129915172277095536 ) ) ;
#80341=CARTESIAN_POINT ( 'NONE',  ( 6.381482430641396419, -0.5404875331735843336, -1.942542459342583294 ) ) ;
#80346=CARTESIAN_POINT ( 'NONE',  ( 0.07680821025393863577, 2.892152076732486421, -2.299782885777381658 ) ) ;
#80349=CARTESIAN_POINT ( 'NONE',  ( 6.063827332385394620, 1.649827434358666967, -1.158513616066357832 ) ) ;
#80350=CARTESIAN_POINT ( 'NONE',  ( 4.154132678086497776, -1.362845063541193946, 1.238102162693654584 ) ) ;
#80352=CARTESIAN_POINT ( 'NONE',  ( -0.02299388927986567924, 4.093419149701410298, -2.466026074291859160 ) ) ;
#80353=CARTESIAN_POINT ( 'NONE',  ( 3.422812307543467103, 1.464285610008815963, -1.783632237398341536 ) ) ;
#80355=CARTESIAN_POINT ( 'NONE',  ( 5.747404748698970778, -1.700087083557629386, -1.334863535946126722 ) ) ;
#80357=CARTESIAN_POINT ( 'NONE',  ( 1.382261328670054246, -0.2867773604850975544, -1.920668630092968732 ) ) ;
#80362=CARTESIAN_POINT ( 'NONE',  ( 4.552342272275657464, 2.055464322635578878, -1.028527531867760914 ) ) ;
#80366=CARTESIAN_POINT ( 'NONE',  ( 4.487079325084206260, 1.670935625628103605, -0.8411387520786617333 ) ) ;
#80367=CARTESIAN_POINT ( 'NONE',  ( 1.002048865836258518, -0.8573748960705518396, 1.709468765625526521 ) ) ;
#80370=CARTESIAN_POINT ( 'NONE',  ( 2.297764732281985633, 1.706874461811638044, 1.398895601573101111 ) ) ;
#80371=CARTESIAN_POINT ( 'NONE',  ( 0.1399997263886003374, 0.002789056014650820314, -1.999853399661279063 ) ) ;
#80376=CARTESIAN_POINT ( 'NONE',  ( 1.264844077314925652, -1.780367465076490019, -0.8468111885079774304 ) ) ;
#80377=CARTESIAN_POINT ( 'NONE',  ( 0.9566253870459644482, 2.304745586553739400, -0.1165920040033379956 ) ) ;
#80378=CARTESIAN_POINT ( 'NONE',  ( 2.049198471137442912, 1.708465938063120637, -0.9642302061752603404 ) ) ;
#80379=CARTESIAN_POINT ( 'NONE',  ( 5.260619331934998755, -0.6897241169346832734, -1.943984935097947675 ) ) ;
#80386=CARTESIAN_POINT ( 'NONE',  ( 0.3917816989358015034, -1.985425474602352525, 0.8787674391965931697 ) ) ;
#80391=CARTESIAN_POINT ( 'NONE',  ( 2.266681450017640653, -1.708379500633325998, -0.7622673669660309237 ) ) ;
#80392=CARTESIAN_POINT ( 'NONE',  ( 6.274726406708529325, -2.050348626090079840, -0.6846857035173321560 ) ) ;
#80395=CARTESIAN_POINT ( 'NONE',  ( 6.727182134110203826, 2.985950691969770254, 2.264927069331075238 ) ) ;
#80398=CARTESIAN_POINT ( 'NONE',  ( 2.684119430630255820, 1.024705199231435993, 1.614373862881289590 ) ) ;
#80399=CARTESIAN_POINT ( 'NONE',  ( 4.135448415848129500, -1.220878049459400039, -1.281573189658680612 ) ) ;
#80400=CARTESIAN_POINT ( 'NONE',  ( 2.086439996564274146, -1.175226666667992914, 1.508458442701497315 ) ) ;
#80403=CARTESIAN_POINT ( 'NONE',  ( 5.659766488261158024, 1.145116341927857384, 1.535488998638125047 ) ) ;
#80404=CARTESIAN_POINT ( 'NONE',  ( 6.812958078942359386, -1.523254609455872322, 1.248309864861799401 ) ) ;
#80406=CARTESIAN_POINT ( 'NONE',  ( 2.496466685713152334, -1.086271176545396067, 1.821091972856798913 ) ) ;
#80407=CARTESIAN_POINT ( 'NONE',  ( 4.715616592392388284, -1.834479983729628616, 0.3652084810651031743 ) ) ;
#80408=CARTESIAN_POINT ( 'NONE',  ( 0.4865809202317071813, -0.2202831055867389420, -1.812292406919484344 ) ) ;
#80410=CARTESIAN_POINT ( 'NONE',  ( 4.125739685719872263, -2.112183141943014153, 0.6395159525410462065 ) ) ;
#80413=CARTESIAN_POINT ( 'NONE',  ( 2.014201374223419272, 2.057289675485386216, -0.1496214851241447485 ) ) ;
#80421=CARTESIAN_POINT ( 'NONE',  ( 4.510256325466165173, 2.069976601481211542, -0.04757507122059301263 ) ) ;
#80423=CARTESIAN_POINT ( 'NONE',  ( 1.493687833870473547, 1.635750924671933282, 1.413141523588061776 ) ) ;
#80425=CARTESIAN_POINT ( 'NONE',  ( 2.561199701127094830, -1.677907875943387639, 1.123823742627054312 ) ) ;
#80433=CARTESIAN_POINT ( 'NONE',  ( 0.1105650446291406575, 1.931126588553159884, 0.5807481968119408977 ) ) ;
#80434=CARTESIAN_POINT ( 'NONE',  ( 5.021103811603734535, -2.081066139062941023, 0.6872292908843835590 ) ) ;
#80437=CARTESIAN_POINT ( 'NONE',  ( 4.957238921819991262, -1.637161358497842389, 0.9882132959125531357 ) ) ;
#80441=CARTESIAN_POINT ( 'NONE',  ( 2.196888872880573551, 1.802427395782604247, 0.9040921628407010413 ) ) ;
#80444=CARTESIAN_POINT ( 'NONE',  ( 5.016472913109910614, 1.187476848380929928, -1.251119849200056366 ) ) ;
#80454=CARTESIAN_POINT ( 'NONE',  ( 5.373626179778474565, 0.3473841915581803996, -1.777664473148509838 ) ) ;
#80457=CARTESIAN_POINT ( 'NONE',  ( 5.654893700716965732, 0.3597771647365927694, 1.775199357419085411 ) ) ;
#80460=CARTESIAN_POINT ( 'NONE',  ( 3.398540877415173966, 1.727514402264049620, -1.348270469230819391 ) ) ;
#80461=CARTESIAN_POINT ( 'NONE',  ( 0.2913577194270203785, -1.795273245208812485, 0.7915465721433642132 ) ) ;
#80463=CARTESIAN_POINT ( 'NONE',  ( 3.673361179623610084, 1.389826993061950899, 1.318567953439080620 ) ) ;
#80471=CARTESIAN_POINT ( 'NONE',  ( 2.219795081190904629, -2.096929600374438429, 0.5247480557022954351 ) ) ;
#80474=CARTESIAN_POINT ( 'NONE',  ( 1.905030480050071251, 1.515927946353814892, 1.016894063925778635 ) ) ;
#80477=CARTESIAN_POINT ( 'NONE',  ( 3.961776442328440506, 1.811803316853294765, -0.2231971713724384965 ) ) ;
#80480=CARTESIAN_POINT ( 'NONE',  ( 3.314863512866594863, -1.493043793209645864, 1.284631214971102775 ) ) ;
#80482=CARTESIAN_POINT ( 'NONE',  ( 4.722180519508206054, 1.859554500701779745, 0.5601121866093302648 ) ) ;
#80486=CARTESIAN_POINT ( 'NONE',  ( 5.572555445586866441, 0.8612648569810870125, 1.938019255899057658 ) ) ;
#80488=CARTESIAN_POINT ( 'NONE',  ( 2.824755571612533434, 1.383597569638248315, -1.320258682893655999 ) ) ;
#80494=CARTESIAN_POINT ( 'NONE',  ( 4.705731023397805579, 1.493295645070455535, 1.350234862845017592 ) ) ;
#80496=CARTESIAN_POINT ( 'NONE',  ( 5.215394836314163562, -0.2642288504575221464, 1.806346989861665087 ) ) ;
#80497=CARTESIAN_POINT ( 'NONE',  ( 0.4321921490204432281, 1.190796696626210682, 1.693455153822187587 ) ) ;
#80501=CARTESIAN_POINT ( 'NONE',  ( 5.383624799460786647, 1.257121276536907750, 1.385457850027263182 ) ) ;
#80510=CARTESIAN_POINT ( 'NONE',  ( 1.024380955673375393, 1.017105081308821379, 1.803069775380027995 ) ) ;
#80511=CARTESIAN_POINT ( 'NONE',  ( 2.214611691679416072, 2.054518390865597954, 0.5110800211125585690 ) ) ;
#80514=CARTESIAN_POINT ( 'NONE',  ( 0.5320047819624426078, 1.129344350875445935, 1.613283618269464981 ) ) ;
#80519=CARTESIAN_POINT ( 'NONE',  ( 2.361634033267061561, 2.247686861432355077, -0.4490786020208848983 ) ) ;
#80520=CARTESIAN_POINT ( 'NONE',  ( 0.6096330727367264002, -1.817201089070449971, 0.1759225495863714350 ) ) ;
#80521=CARTESIAN_POINT ( 'NONE',  ( 2.724755696555291262, 1.382288352666941389, -1.321784923088549446 ) ) ;
#80525=CARTESIAN_POINT ( 'NONE',  ( 1.248292583380994136, 0.9887404755159521219, -1.753579541237253903 ) ) ;
#80526=CARTESIAN_POINT ( 'NONE',  ( 1.270277045833507312, -0.8771146801004360283, -1.754798696806989078 ) ) ;
#80531=CARTESIAN_POINT ( 'NONE',  ( 3.890639641997388765, 1.766133395052928101, -1.118410975085604608 ) ) ;
#80532=CARTESIAN_POINT ( 'NONE',  ( 2.852158073610413513, 0.5945245674133512459, 1.667141438756434058 ) ) ;
#80535=CARTESIAN_POINT ( 'NONE',  ( 6.527265088719197195, -1.491963682546100900, -1.740339723829595453 ) ) ;
#80536=CARTESIAN_POINT ( 'NONE',  ( 4.329842768969596634, 1.707365525456190358, 0.3361313568818121156 ) ) ;
#80540=CARTESIAN_POINT ( 'NONE',  ( 4.587041898695760622, 1.066698363585473652, -1.366732696162711314 ) ) ;
#80541=CARTESIAN_POINT ( 'NONE',  ( 4.844266001044335468, -1.027726779992131023, 1.912555630771580084 ) ) ;
#80543=CARTESIAN_POINT ( 'NONE',  ( 5.489470343000498076, -0.4852711138302409077, 1.957169415941109047 ) ) ;
#80544=CARTESIAN_POINT ( 'NONE',  ( 5.750000000000004441, 3.273043269275614537E-13, 2.052068128417940951 ) ) ;
#80546=CARTESIAN_POINT ( 'NONE',  ( 3.733351708207183428, -1.780342035418970736, 0.7362343730293962052 ) ) ;
#80548=CARTESIAN_POINT ( 'NONE',  ( 6.258078541936050065, 0.8512804341574469191, -2.052012918514530160 ) ) ;
#80550=CARTESIAN_POINT ( 'NONE',  ( 6.883263157960364254, 2.447565407927353220, 2.329071302269662080 ) ) ;
#80553=CARTESIAN_POINT ( 'NONE',  ( 1.313460851834074905, 1.813262283420258525, -1.282816764689881373 ) ) ;
#80560=CARTESIAN_POINT ( 'NONE',  ( 5.459457826130150515, 1.684308464339222100, 1.190431669587647567 ) ) ;
#80565=CARTESIAN_POINT ( 'NONE',  ( 6.678970768140332304, -0.09217866350584581758, -1.868372134486769420 ) ) ;
#80566=CARTESIAN_POINT ( 'NONE',  ( 5.396976841598324803, -0.7867719702298915374, -1.545497150229415251 ) ) ;
#80567=CARTESIAN_POINT ( 'NONE',  ( 4.018918099032080526, -1.663992213871115178, 0.5101021115980988174 ) ) ;
#80569=CARTESIAN_POINT ( 'NONE',  ( 3.456809812625420975, -2.022294432149398080, -1.079448172897869540 ) ) ;
#80571=CARTESIAN_POINT ( 'NONE',  ( 1.569984571489828173, -1.747861548559765721, -0.5788160320587890650 ) ) ;
#80574=CARTESIAN_POINT ( 'NONE',  ( 1.764397251013736234, -1.293498944356825664, 1.288518760371157201 ) ) ;
#80576=CARTESIAN_POINT ( 'NONE',  ( 2.742814741689561853, 2.006446121045248887, -0.2004354718553730264 ) ) ;
#80577=CARTESIAN_POINT ( 'NONE',  ( 1.095947417326826212, -2.191629467406099430, 0.003159298377679310623 ) ) ;
#80579=CARTESIAN_POINT ( 'NONE',  ( 4.032330418399681093, 1.128390736420165519, -1.777953997047557744 ) ) ;
#80582=CARTESIAN_POINT ( 'NONE',  ( 1.398975865466948632, 0.4019745351953528112, 2.030794141931663521 ) ) ;
#80585=CARTESIAN_POINT ( 'NONE',  ( 3.879626234357834047, 0.2581020070546445888, -2.104639248629774251 ) ) ;
#80588=CARTESIAN_POINT ( 'NONE',  ( 6.076747101522134820, -1.735163100867884500, -0.5679748894881069265 ) ) ;
#80595=CARTESIAN_POINT ( 'NONE',  ( 2.847920605731304011, -1.359688658692468355, -1.493726022120341224 ) ) ;
#80596=CARTESIAN_POINT ( 'NONE',  ( 0.7804679756576750060, -1.169858290841051307, 1.750926281551241415 ) ) ;
#80599=CARTESIAN_POINT ( 'NONE',  ( 5.647250314520869452, 1.642094101250504146, -0.8754911610409812361 ) ) ;
#80607=CARTESIAN_POINT ( 'NONE',  ( 1.838261372102001800, -1.052240823716396267, 1.655630454418555830 ) ) ;
#80608=CARTESIAN_POINT ( 'NONE',  ( 6.807514186891733488, -0.4511856701074740683, 2.018123631040650068 ) ) ;
#80613=CARTESIAN_POINT ( 'NONE',  ( 2.653305042933405300, -0.2923731341353021373, -1.708803492460549744 ) ) ;
#80614=CARTESIAN_POINT ( 'NONE',  ( 1.165484214331854895, -1.106714608479087092, 1.343107696387570549 ) ) ;
#80615=CARTESIAN_POINT ( 'NONE',  ( 6.147156021580305385, -1.953063626952681542, 1.228987080356194195 ) ) ;
#80618=CARTESIAN_POINT ( 'NONE',  ( 2.882161881593125585, -1.062215874558822826, 1.765801728998709352 ) ) ;
#80622=CARTESIAN_POINT ( 'NONE',  ( 1.423203639035979906, 0.8144988626696235690, 1.844428818423976546 ) ) ;
#80623=CARTESIAN_POINT ( 'NONE',  ( 6.825078400183544503, 6.034152930826206962, 2.739236550662868197 ) ) ;
#80625=CARTESIAN_POINT ( 'NONE',  ( 0.7957029915596275371, -0.7116629262611442464, 1.838703523458279143 ) ) ;
#80626=CARTESIAN_POINT ( 'NONE',  ( 4.148624843374196125, 1.876505540506741010, 0.3678670841067502861 ) ) ;
#80631=CARTESIAN_POINT ( 'NONE',  ( 0.6803390939152150763, 0.9973279206440927025, 1.756184504224398202 ) ) ;
#80633=CARTESIAN_POINT ( 'NONE',  ( 4.190657675959572614, -2.281913287836007331, -0.3425691479843806508 ) ) ;
#80634=CARTESIAN_POINT ( 'NONE',  ( 5.441838459065293065, 1.316327937319297758, 1.454900926449454124 ) ) ;
#80635=EDGE_CURVE ( 'NONE', #146910, #126115, #184389, .T. ) ;
#80636=CARTESIAN_POINT ( 'NONE',  ( 1.639427129605858902, 1.814645582613241714, -0.7458448512465406521 ) ) ;
#80638=CARTESIAN_POINT ( 'NONE',  ( -0.03452862918938356951, -1.956592590566148093, -0.4871966601913205186 ) ) ;
#80640=CARTESIAN_POINT ( 'NONE',  ( 1.446650934045516701, -1.493148645901293925, 1.501467539593546840 ) ) ;
#80643=CARTESIAN_POINT ( 'NONE',  ( 1.165666007907351309, -1.169451938622353859, 1.422036577929463030 ) ) ;
#80645=CARTESIAN_POINT ( 'NONE',  ( 4.645498245716852992, 1.942073188235559522, -0.9706016350095565404 ) ) ;
#80647=CARTESIAN_POINT ( 'NONE',  ( 2.144932638433934002, 2.058100890041581810, 0.5106320605416380110 ) ) ;
#80651=CARTESIAN_POINT ( 'NONE',  ( 3.462233735546389468, 0.9232262379769129446, 1.842458217425169131 ) ) ;
#80654=CARTESIAN_POINT ( 'NONE',  ( 0.1691535571452691677, 1.059206136818511501, 1.505872603892892458 ) ) ;
#80656=CARTESIAN_POINT ( 'NONE',  ( -0.02244404828160086532, 2.859736408857795009, -2.677210243787793598 ) ) ;
#80658=CARTESIAN_POINT ( 'NONE',  ( 0.4521680116954321371, 0.6883007682146925488, -2.096869779678663281 ) ) ;
#80659=CARTESIAN_POINT ( 'NONE',  ( 0.9840795919474578657, 1.519885296779641681, 1.676025758627389450 ) ) ;
#80661=CARTESIAN_POINT ( 'NONE',  ( 2.355456482938292240, -1.344675202547132464, -1.214172642412311598 ) ) ;
#80662=CARTESIAN_POINT ( 'NONE',  ( 1.622146050056040512, 1.895417417167859497, 0.2770879218524437415 ) ) ;
#80663=CARTESIAN_POINT ( 'NONE',  ( 3.016144355299533952, 2.060630728401948275, -0.2003171163396169074 ) ) ;
#80665=CARTESIAN_POINT ( 'NONE',  ( 1.235163454902254765, -1.783154728128878652, 0.8411200730164528627 ) ) ;
#80666=CARTESIAN_POINT ( 'NONE',  ( 6.586557377926046897, -1.889895688126231876, -0.3729288831034789364 ) ) ;
#80667=CARTESIAN_POINT ( 'NONE',  ( 3.274138816734498025, -1.115311402298941656, 1.501645261301733481 ) ) ;
#80668=CARTESIAN_POINT ( 'NONE',  ( 0.8038796212130067120, 1.889748380504801650, 1.324265523043531845 ) ) ;
#80670=CARTESIAN_POINT ( 'NONE',  ( 3.015880874418576330, 1.852360388558017545, -0.1794404841957262797 ) ) ;
#80672=CARTESIAN_POINT ( 'NONE',  ( 4.896965771356657449, 0.3494220250804170314, 2.032713711554866354 ) ) ;
#80676=CARTESIAN_POINT ( 'NONE',  ( 6.141652715049399802, -1.522797514780509065, -1.454946885519771582 ) ) ;
#80678=CARTESIAN_POINT ( 'NONE',  ( 6.520800673124607982, 2.014292100380775885, 0.7847517145297827623 ) ) ;
#80679=CARTESIAN_POINT ( 'NONE',  ( 1.083273795380396143, -0.8277460070302902206, 1.644747122058511035 ) ) ;
#80680=CARTESIAN_POINT ( 'NONE',  ( 5.162762804107727810, 0.5884847259931770269, 1.932018068032066438 ) ) ;
#80689=CARTESIAN_POINT ( 'NONE',  ( 3.819546216251490822, -1.394084564108012403, -1.457236891723237449 ) ) ;
#80694=CARTESIAN_POINT ( 'NONE',  ( 6.473507614529132148, 2.070149491355821159, -0.6224772505839873959 ) ) ;
#80699=CARTESIAN_POINT ( 'NONE',  ( 5.150017624212761547, 0.9963180513538304472, 1.753022482293864481 ) ) ;
#80702=CARTESIAN_POINT ( 'NONE',  ( 1.875234852168044641, 1.651158054356154148, -0.4988350824523117844 ) ) ;
#80707=CARTESIAN_POINT ( 'NONE',  ( 0.2448899766094528307, -1.362147681959727574, -1.129672978174221631 ) ) ;
#80708=CARTESIAN_POINT ( 'NONE',  ( 1.295565486743395889, 1.859180707359459284, -0.7724582428273608636 ) ) ;
#80710=CARTESIAN_POINT ( 'NONE',  ( 2.784424029790978139, -1.135345490304447091, 1.892179603154810597 ) ) ;
#80711=CARTESIAN_POINT ( 'NONE',  ( 5.629782814718605977, 2.094415894289668678, -0.5717063696269225614 ) ) ;
#80714=CARTESIAN_POINT ( 'NONE',  ( 3.528090983593739516, -2.088826311502915090, 0.3641918842257965139 ) ) ;
#80715=CARTESIAN_POINT ( 'NONE',  ( 1.423454079394898653, -1.462460055423293825, -1.388472309132340099 ) ) ;
#80716=CARTESIAN_POINT ( 'NONE',  ( 2.548825626188336635, 0.2254045845835982720, 1.797452833117135329 ) ) ;
#80721=CARTESIAN_POINT ( 'NONE',  ( 1.059628844421168559, 1.143981278108822108, 1.536452684808758962 ) ) ;
#80729=CARTESIAN_POINT ( 'NONE',  ( 4.768538688506021472, -1.414568798902924307, 1.634688457493836289 ) ) ;
#80732=CARTESIAN_POINT ( 'NONE',  ( 2.109781586379317897, 1.642293606977158538, 1.341614810521203349 ) ) ;
#80733=DIRECTION ( 'NONE',  ( 1.214306433183764966E-17, 1.000000000000000000, 5.200010849845536803E-32 ) ) ;
#80735=CARTESIAN_POINT ( 'NONE',  ( 3.444560810740458390, 0.4755345817112103246, 1.913044316819292767 ) ) ;
#80736=CARTESIAN_POINT ( 'NONE',  ( 5.871340715825057011, -1.643613990083541143, -0.9773822251149253404 ) ) ;
#80740=CARTESIAN_POINT ( 'NONE',  ( 0.4146172280090759665, 0.7909515328246279342, 1.913518691844050323 ) ) ;
#80741=CARTESIAN_POINT ( 'NONE',  ( 1.816251609031571457, 1.811968324836669142, 0.6989759121980871903 ) ) ;
#80746=CARTESIAN_POINT ( 'NONE',  ( 2.273483640244071680, 1.287084957891961423, 1.647379119656503965 ) ) ;
#80749=CARTESIAN_POINT ( 'NONE',  ( 5.953752735127215701, -1.388294428863137586, -1.315342447896154843 ) ) ;
#80751=CARTESIAN_POINT ( 'NONE',  ( 4.424592250794217030, 1.359014646446855767, -1.738718759629573896 ) ) ;
#80752=CARTESIAN_POINT ( 'NONE',  ( 2.837189949676882428, 0.2689455771197127310, 2.190246129917215789 ) ) ;
#80754=CARTESIAN_POINT ( 'NONE',  ( 1.805181101471531546, 1.663141274854248230, -0.9436981260437929953 ) ) ;
#80757=CARTESIAN_POINT ( 'NONE',  ( 4.193848433072798088, -1.425472641756184489, -1.501718461524886195 ) ) ;
#80760=CARTESIAN_POINT ( 'NONE',  ( 1.674925575805393585, -2.052671086741376882, -0.6780288057936025847 ) ) ;
#80761=CARTESIAN_POINT ( 'NONE',  ( 3.368858348882136422, 0.05182064297618373117, -2.191103300807801801 ) ) ;
#80768=UNCERTAINTY_MEASURE_WITH_UNIT (LENGTH_MEASURE( 1.000000000000000082E-05 ), #78182, 'distance_accuracy_value', 'NONE');
#80769=CARTESIAN_POINT ( 'NONE',  ( 0.1764080092822375156, 1.496053712750060383, 1.352152247781977179 ) ) ;
#80773=CARTESIAN_POINT ( 'NONE',  ( 4.522371119077151391, 0.9712943915625820157, 1.828230030883712498 ) ) ;
#80774=CARTESIAN_POINT ( 'NONE',  ( 2.754421912756400026, 0.6492094756798562072, 1.813941749866236242 ) ) ;
#80775=CARTESIAN_POINT ( 'NONE',  ( 6.187133403942106646, 1.760427041935657799, 1.175965560660442444 ) ) ;
#80778=CARTESIAN_POINT ( 'NONE',  ( 3.942214172571806508, -0.9744538365985645489, 1.711425102584500202 ) ) ;
#80779=CARTESIAN_POINT ( 'NONE',  ( 5.472717818731657857, -0.05164252020756903566, -2.291847404020570966 ) ) ;
#80780=CARTESIAN_POINT ( 'NONE',  ( 4.529811765687052016, -1.125283923072720071, -1.437579299059896343 ) ) ;
#80786=CARTESIAN_POINT ( 'NONE',  ( 4.957293921627444533, -1.724444360862188885, 1.038707789177233831 ) ) ;
#80787=CARTESIAN_POINT ( 'NONE',  ( 6.170549959107765936, 1.581869261771509994, 1.668023173554062266 ) ) ;
#80788=CARTESIAN_POINT ( 'NONE',  ( 5.770351633785986145, -0.8788013674413885923, -1.753946858050984048 ) ) ;
#80793=CARTESIAN_POINT ( 'NONE',  ( 1.136401537022444508, 0.4113854086121961351, 2.049693714879106121 ) ) ;
#80794=CARTESIAN_POINT ( 'NONE',  ( 6.702016551492756768, -1.769339222028827319, 0.04870252428828580893 ) ) ;
#80796=CARTESIAN_POINT ( 'NONE',  ( 6.421825219014824171, 1.115965409679237963, -1.589096094497045142 ) ) ;
#80798=CARTESIAN_POINT ( 'NONE',  ( 0.8369945909703061515, 0.7069334548283608965, -1.590575932886540755 ) ) ;
#80801=CARTESIAN_POINT ( 'NONE',  ( 1.277515311556869593, 1.024738337535425758, 1.387312573235904845 ) ) ;
#80802=CARTESIAN_POINT ( 'NONE',  ( 1.206853476500208133, 1.935082376036290075, 1.028754739392373496 ) ) ;
#80803=CARTESIAN_POINT ( 'NONE',  ( 4.125739685719872263, -2.112183141943014153, 0.6395159525410462065 ) ) ;
#80804=CARTESIAN_POINT ( 'NONE',  ( 1.850661656762859542, -2.160338676232275823, -0.2159047328044171599 ) ) ;
#80806=CARTESIAN_POINT ( 'NONE',  ( 2.483745868283081748, -0.6592627125163934565, 2.012192174959149149 ) ) ;
#80807=CARTESIAN_POINT ( 'NONE',  ( 6.539320575229291777, 2.092415259949731432, 2.107292781797183601 ) ) ;
#80809=CARTESIAN_POINT ( 'NONE',  ( 3.035043143063915760, -2.020573557004992971, 1.082744910948540307 ) ) ;
#80813=CARTESIAN_POINT ( 'NONE',  ( 5.127666992232062348, -0.3272401999867382560, 2.196937980255990741 ) ) ;
#80821=CARTESIAN_POINT ( 'NONE',  ( 3.182267690267494231, 1.591318367894577701, 1.238320962759748234 ) ) ;
#80823=CARTESIAN_POINT ( 'NONE',  ( 1.832955167792608364, -1.957230265441430417, -0.6508311760726466222 ) ) ;
#80829=CARTESIAN_POINT ( 'NONE',  ( 4.611385148785618782, -2.149487334021232599, 0.4259423572047504880 ) ) ;
#80830=CARTESIAN_POINT ( 'NONE',  ( 2.654922836763852878, 1.081066371885472277, 1.701947380796410059 ) ) ;
#80831=CARTESIAN_POINT ( 'NONE',  ( 1.452429406588066740, -1.579491434881035827, -0.9459884711465746943 ) ) ;
#80833=CARTESIAN_POINT ( 'NONE',  ( 5.631824825758743991, -1.159798792365024145, -1.409841961918213427 ) ) ;
#80835=CARTESIAN_POINT ( 'NONE',  ( 6.328750030911493241, 0.7691242348151774433, -1.864167186630163009 ) ) ;
#80837=CARTESIAN_POINT ( 'NONE',  ( 4.434621138646507532, 2.218105251380130483, 0.4453182654360221537 ) ) ;
#80839=CARTESIAN_POINT ( 'NONE',  ( 0.4168064962662480499, 1.450752768847368257, -1.526948433937134197 ) ) ;
#80841=CARTESIAN_POINT ( 'NONE',  ( 4.229010956685672618, -1.930657356216297860, -0.7480826485904977785 ) ) ;
#80850=CARTESIAN_POINT ( 'NONE',  ( 3.182088186068011915, 2.166492470972399165, -0.4902054615175278629 ) ) ;
#80854=CARTESIAN_POINT ( 'NONE',  ( 3.244534624505683418, -1.932379277470747558, -0.3379807920969243873 ) ) ;
#80861=CARTESIAN_POINT ( 'NONE',  ( 2.320699612028754188, -0.8158636990020677882, -1.957571985684476212 ) ) ;
#80863=CARTESIAN_POINT ( 'NONE',  ( 4.170900312159072421, -2.016029151617684256, -0.7805680927704603533 ) ) ;
#80864=CARTESIAN_POINT ( 'NONE',  ( 2.999365392321148960, -1.839032331094083927, 0.09308366406014098593 ) ) ;
#80867=CARTESIAN_POINT ( 'NONE',  ( 5.279165678654878846, 1.172930834070673889, 1.285866470927458094 ) ) ;
#80872=CARTESIAN_POINT ( 'NONE',  ( 2.624079441566569582, -1.243859440641072123, -1.767801033134681843 ) ) ;
#80873=CARTESIAN_POINT ( 'NONE',  ( 4.341172599035714619, -1.163090190446917083, 1.646587424817484324 ) ) ;
#80875=CARTESIAN_POINT ( 'NONE',  ( 1.956163130892615731, 2.155914767609674598, -0.1587918856347721730 ) ) ;
#80876=CARTESIAN_POINT ( 'NONE',  ( 2.723849342626927239, -1.131982996307562273, -1.613792087129195085 ) ) ;
#80877=CARTESIAN_POINT ( 'NONE',  ( 6.509000000000045638, 3.691181720027385094, 2.614238911931165088 ) ) ;
#80878=CARTESIAN_POINT ( 'NONE',  ( 4.106929586529986409, -0.3288250506029398168, 1.913867117139455676 ) ) ;
#80887=CARTESIAN_POINT ( 'NONE',  ( 1.307976841356368602, -0.5351398426680589182, 2.140771676462468687 ) ) ;
#80890=CARTESIAN_POINT ( 'NONE',  ( 5.383633123045536983, -1.864019207510819953, 0.6117972396969260096 ) ) ;
#80893=CARTESIAN_POINT ( 'NONE',  ( 0.07459516483346911864, 0.007201286963446140027, -1.755573347271717211 ) ) ;
#80894=CARTESIAN_POINT ( 'NONE',  ( 4.822110771479974467, 1.762745816080556915, 0.5315184756640098929 ) ) ;
#80899=CARTESIAN_POINT ( 'NONE',  ( 5.554972086574996304, 0.4156608669513594534, 2.079290889414136423 ) ) ;
#80902=CARTESIAN_POINT ( 'NONE',  ( 6.573517591324530507, 1.973370851288195338, -0.5938938365465350477 ) ) ;
#80904=CARTESIAN_POINT ( 'NONE',  ( 0.3263015691194782741, -1.220318288589719913, 1.405194318597773329 ) ) ;
#80905=CARTESIAN_POINT ( 'NONE',  ( 3.649809678215182096, 0.6660801477775115664, 1.716721118343276453 ) ) ;
#80911=CARTESIAN_POINT ( 'NONE',  ( 3.633602750639616019, -2.039237483250630589, 0.8441791899983088765 ) ) ;
#80912=CARTESIAN_POINT ( 'NONE',  ( 5.975896723952917711, 1.340560379189212226, 1.822362705929107429 ) ) ;
#80914=CARTESIAN_POINT ( 'NONE',  ( 5.625234629914776185, 1.601787910378251967, 0.8462062870350762767 ) ) ;
#80915=CARTESIAN_POINT ( 'NONE',  ( 5.454270856000166923, -1.210104932453776039, 1.485173795633880633 ) ) ;
#80917=CARTESIAN_POINT ( 'NONE',  ( 5.823093596695693819, -0.04436734784114480107, 1.870300906237104988 ) ) ;
#80918=CARTESIAN_POINT ( 'NONE',  ( 5.476954007041204164, 1.719599228052148154, 0.7121796456092708283 ) ) ;
#80920=CARTESIAN_POINT ( 'NONE',  ( 0.1275333129481092398, -1.147091320445620566, -1.478225367208672703 ) ) ;
#80921=CARTESIAN_POINT ( 'NONE',  ( 1.305875433988498813, -1.124247956386617009, -1.673852571057245830 ) ) ;
#80923=CARTESIAN_POINT ( 'NONE',  ( 3.000711368280566393, -0.6119465431162304236, -2.015196771704963030 ) ) ;
#80927=CARTESIAN_POINT ( 'NONE',  ( 3.217061457047249551, 1.589534765328611154, -1.246005657720136606 ) ) ;
#80930=CARTESIAN_POINT ( 'NONE',  ( 2.952577552874091626, 0.7252333659365679530, 2.036452211405047397 ) ) ;
#80931=CARTESIAN_POINT ( 'NONE',  ( 6.609999999999971010, 7.629137130509032971, 2.879999999999991456 ) ) ;
#80938=CARTESIAN_POINT ( 'NONE',  ( 0.9959476074029065540, -2.191739723303194332, 0.005169097091584088505 ) ) ;
#80940=CARTESIAN_POINT ( 'NONE',  ( 2.905426592119991991, 1.910755973352752379, 1.211346930818749890 ) ) ;
#80947=CARTESIAN_POINT ( 'NONE',  ( 3.725649928583890436, -1.052200936647734286, -1.422817597083583241 ) ) ;
#80949=CARTESIAN_POINT ( 'NONE',  ( 6.422910180798067969, 2.056742032306459578, 0.8002587082300142152 ) ) ;
#80953=CARTESIAN_POINT ( 'NONE',  ( 4.640250013031629095, 0.7743308749140092040, 1.862011755488258480 ) ) ;
#80955=CARTESIAN_POINT ( 'NONE',  ( 3.362029495745801899, 0.8400119854848132617, 1.671504782411597612 ) ) ;
#80956=CARTESIAN_POINT ( 'NONE',  ( 3.168866831888625946, 1.502704456927813403, -1.424286459396295390 ) ) ;
#80964=CARTESIAN_POINT ( 'NONE',  ( 1.441514601552947417, -1.799640695080907182, 0.6472408003148701905 ) ) ;
#80965=CARTESIAN_POINT ( 'NONE',  ( 2.488659587246494276, 1.902222718079676689, 0.4795239450603656084 ) ) ;
#80966=CARTESIAN_POINT ( 'NONE',  ( 1.212267286723569981, -1.587592435625035270, -1.242539042498117086 ) ) ;
#80970=CARTESIAN_POINT ( 'NONE',  ( 0.1806930697454533219, -0.1309388314422038346, -1.840455529407057256 ) ) ;
#80973=CARTESIAN_POINT ( 'NONE',  ( 2.338141740155843085, -1.162522942608142928, -1.643444077351646326 ) ) ;
#80974=B_SPLINE_CURVE_WITH_KNOTS ( 'NONE', 3,
 ( #199586, #51229, #117353, #183351, #68512, #36027, #102105, #19775, #85857, #119488, #151931, #185475, #3506, #37099, #103178, #169239, #123790, #156211, #155135, #107510, #187613, #24040, #40325, #170297, #41400, #9934, #138895, #57631, #74945, #190807, #39241, #6717, #105333, #188689, #56568, #203847, #189748, #173539, #106430, #38179, #171370, #172453, #22963, #89078, #72795, #7787, #142112, #104251, #204914, #5632, #21885, #26181, #207063, #25113, #58693, #87994, #122726, #124841, #90143, #121646, #73880, #139973, #205995, #42467, #91216, #157277, #92296, #108577, #8866, #174605, #154067, #141056, #158340, #76009, #208125, #59754, #186550, #71713, #137826, #55492, #77061, #162601, #192942, #28322, #31536, #147417, #13127, #128056, #79205, #194012, #93352, #10987, #97611, #126983, #145322, #143191, #159389, #212383, #209182, #60822, #176709, #80270, #81338, #15251, #110709, #163668, #130171, #213442, #46730, #44594, #211323, #94418, #160457, #125914, #112842, #43533, #12065, #146368, #78134, #178858, #144264, #210257, #61895, #191873, #30469, #96554, #45661, #111779, #177785, #64025, #29401, #95493, #161540, #129117, #62948, #196163, #47804, #109656, #14177, #195093, #175658, #27246, #113917, #179913, #185209, #116027, #168976, #165789, #2178, #131221, #84528, #118164, #66112, #151679, #36833, #182012, #16306, #148480, #33643, #135427, #166855, #132255, #82391, #65065, #83456, #101847, #48, #17372, #52038, #167917, #86661, #99717, #198262, #119225, #34704, #184149, #35773, #149536, #197209, #49905, #1122, #32585, #102916, #152728, #20577, #48849, #67184, #114963, #19514, #133321, #180963, #100773, #85591, #3249, #199323, #98662, #50970, #117092, #183092, #18451, #150617, #164717, #68254, #134387, #200390, #69317, #201449, #53092, #88814, #58433, #189494, #202518, #174339, #55236, #171109, #122464, #186281, #22702, #138629, #106167, #90950, #170036, #72532, #41138, #71454, #121383, #124586, #25917, #172194, #6455, #23783, #204653, #37918, #103992, #190546, #5375, #89889, #21622, #87730, #157017, #153802, #56302, #107248, #173269, #92025, #108318, #203584, #42203, #8601, #4310, #139708, #137567, #155940, #187356, #38986, #70381, #205731, #136497, #105071, #24849, #154872, #188422, #206800, #40058, #7526, #54168, #57367, #74685, #73609, #123529, #140786, #120306, #60554, #10729, #109390, #161268, #127794, #178589, #162338, #63755, #78929, #195901, #76799, #179654, #194820, #47536, #129915, #208920, #113650, #44328, #95218, #9670, #177518, #211054, #159128, #30197, #31274, #126714, #175395, #26981, #192674, #142920, #110450, #176451, #93086, #158083, #28063, #46455, #94156, #160195, #145052, #112577, #75746, #11797, #77871, #96286, #143994, #212117, #128838, #141858, #207865, #13921, #209986, #61628, #193749, #45395, #111512, #59489, #125646, #29131, #12854, #80001, #62678, #146107, #191608, #43270, #199063, #99466, #50709, #165525, #64817, #213190, #19262, #52842, #164462, #130963, #151425, #83194, #49642, #149276, #67991, #51794, #118977, #201202, #82132, #135187, #101593, #69067, #18189, #48593, #116835, #81077, #17116, #184956, #2998, #97349, #147163, #196955, #133065, #857, #85344, #16048, #181754, #163406, #84274, #134133, #214226, #114711, #66923, #117913, #65854, #180706, #100525, #182836, #183905, #167661, #14981 ),
 .UNSPECIFIED., .F., .F.,
 ( 4, 1, 1, 1, 1, 1, 1, 1, 1, 1, 1, 1, 1, 1, 1, 1, 1, 1, 1, 1, 1, 1, 1, 1, 1, 1, 1, 1, 1, 1, 1, 1, 1, 1, 1, 1, 1, 1, 1, 1, 1, 1, 1, 1, 1, 1, 1, 1, 1, 1, 1, 1, 1, 1, 1, 1, 1, 1, 1, 1, 1, 1, 1, 1, 1, 1, 1, 1, 1, 1, 1, 1, 1, 1, 1, 1, 1, 1, 1, 1, 1, 1, 1, 1, 1, 1, 1, 1, 1, 1, 1, 1, 1, 1, 1, 1, 1, 1, 1, 1, 1, 1, 1, 1, 1, 1, 1, 1, 1, 1, 1, 1, 1, 1, 1, 1, 1, 1, 1, 1, 1, 1, 1, 1, 1, 1, 1, 1, 1, 1, 1, 1, 1, 1, 1, 1, 1, 1, 1, 1, 1, 1, 1, 1, 1, 1, 1, 1, 1, 1, 1, 1, 1, 1, 1, 1, 1, 1, 1, 1, 1, 1, 1, 1, 1, 1, 1, 1, 1, 1, 1, 1, 1, 1, 1, 1, 1, 1, 1, 1, 1, 1, 1, 1, 1, 1, 1, 1, 1, 1, 1, 1, 1, 1, 1, 1, 1, 1, 1, 1, 1, 1, 1, 1, 1, 1, 1, 1, 1, 1, 1, 1, 1, 1, 1, 1, 1, 1, 1, 1, 1, 1, 1, 1, 1, 1, 1, 1, 1, 1, 1, 1, 1, 1, 1, 1, 1, 1, 1, 1, 1, 1, 1, 1, 1, 1, 1, 1, 1, 1, 1, 1, 1, 1, 1, 1, 1, 1, 1, 1, 1, 1, 1, 1, 1, 1, 1, 1, 1, 1, 1, 1, 1, 1, 1, 1, 1, 1, 1, 1, 1, 1, 1, 1, 1, 1, 1, 1, 1, 1, 1, 1, 1, 1, 1, 1, 1, 1, 1, 1, 1, 1, 1, 1, 1, 1, 1, 1, 1, 1, 1, 1, 1, 1, 1, 1, 1, 1, 1, 1, 1, 1, 1, 1, 1, 1, 1, 1, 1, 1, 1, 1, 1, 1, 1, 1, 1, 1, 1, 1, 1, 1, 1, 1, 1, 1, 1, 1, 1, 1, 1, 1, 1, 1, 1, 1, 1, 1, 1, 1, 1, 1, 1, 1, 1, 1, 1, 1, 1, 1, 1, 1, 1, 1, 1, 1, 1, 1, 1, 1, 1, 1, 1, 1, 4 ),
 ( 0.000000000000000000, 0.002600034503794030130, 0.005208798665460326327, 0.007813183304800875098, 0.01041632952039499814, 0.01302078637366306003, 0.01562487905948694092, 0.01822913957756216313, 0.02083328395591756144, 0.02343739818322774712, 0.02604168118785421884, 0.02864568517727394958, 0.03125004130332968699, 0.03385401862675675722, 0.03645834363201481965, 0.03906241290072134942, 0.04166661303991354287, 0.04427083116291704451, 0.04687488238457573897, 0.04947921467585455341, 0.05208318889621989245, 0.05468754274347345512, 0.05729155431138267807, 0.05989582568988525285, 0.06249996760622017478, 0.06510408932096034551, 0.06770837349117478365, 0.07031237295078232585, 0.07291672927807971161, 0.07552070761765239393, 0.07812503204114096267, 0.08072910085791458468, 0.08333330089851145872, 0.08593751883178461781, 0.08854156980611090078, 0.09114590188302622298, 0.09374987588873062716, 0.09635422952249227124, 0.09895824087764454324, 0.1015625120427016276, 0.1041666537503683765, 0.1067707752516706410, 0.1093750592157429480, 0.1119790584643299974, 0.1145834145867499904, 0.1171873927198607973, 0.1197917169388799108, 0.1223957855539345302, 0.1249999853896588409, 0.1276042031245507580, 0.1302082538950744550, 0.1328125857752754935, 0.1354165595809520839, 0.1380209130188291833, 0.1406249241787864424, 0.1432291951479887082, 0.1458333366646657747, 0.1484374579699756502, 0.1510417417453218114, 0.1536457408005802994, 0.1562500967354857329, 0.1588540746797905134, 0.1614583987117299280, 0.1640624671426803571, 0.1666666667910262079, 0.1692708843450304312, 0.1718749349293641482, 0.1744792666302357464, 0.1770832402535473249, 0.1796875935129024493, 0.1822916044953091785, 0.1848958752860835608, 0.1875000166293293857, 0.1901041377562054102, 0.1927084213602507368, 0.1953124202398235920, 0.1979167760045740521, 0.2005207537777317084, 0.2031250776399721736, 0.2057291459044250093, 0.2083333453828807025, 0.2109375627734847158, 0.2135416131892344249, 0.2161459447281551538, 0.2187499181867580689, 0.2213542712849473904, 0.2239582821074418695, 0.2265625527372090720, 0.2291666939245756707, 0.2317708148905701926, 0.2343750983407339450, 0.2369790970622578097, 0.2395834526742069426, 0.2421874302938704648, 0.2447917540037867212, 0.2473958221193426621, 0.2500000214453905190, 0.2526042386900758108, 0.2552082889548416555, 0.2578126203491843960, 0.2604165936607292231, 0.2630209466151033904, 0.2656249572953180982, 0.2682292277814931625, 0.2708333688305272213, 0.2734374896531870935, 0.2760417729668830367, 0.2786457715479891406, 0.2812501270244852081, 0.2838541045083020076, 0.2864584280832634389, 0.2890624960675178268, 0.2916666952586349781, 0.2942709123748779576, 0.2968749625062547248, 0.2994792937733871119, 0.3020832669555192918, 0.3046876197834237909, 0.3072916303389863768, 0.3098959006989794318, 0.3125000416272227799, 0.3151041623240899980, 0.3177084455187270673, 0.3203124439770417831, 0.3229167993354283839, 0.3255207767010412923, 0.3281251001584127303, 0.3307291680289564662, 0.3333333671026155187, 0.3359375841078879321, 0.3385416341234662174, 0.3411459652807516951, 0.3437499383511121720, 0.3463542910698884647, 0.3489583015184220538, 0.3515625717696388985, 0.3541667125946290073, 0.3567708331832410984, 0.3593751162762241491, 0.3619791146293697692, 0.3645834698869864221, 0.3671874471520340522, 0.3697917705091763874, 0.3723958382835964032, 0.3750000372572658280, 0.3776042541690359799, 0.3802083040864021046, 0.3828126351512001757, 0.3854166081274262856, 0.3880209607544118922, 0.3906249711135359459, 0.3932292412733790488, 0.3958333820126498370, 0.3984375025105409418, 0.4010417855192715542, 0.4036457837848667074, 0.4062501389590495449, 0.4088541161411674008, 0.4114584394154381930, 0.4140625071113177014, 0.4166667060024629166, 0.4192709228381954478, 0.4218749726749327911, 0.4244793036646000717, 0.4270832765643259310, 0.4296876291168554296, 0.4322916394041865784, 0.4348959094900549660, 0.4375000501611374104, 0.4401041705858387276, 0.4427084535277153732, 0.4453124517233759683, 0.4479168068314584583, 0.4505207839482789911, 0.4531251071570330247, 0.4557291747919532399, 0.4583333736180368323, 0.4609375903951940523, 0.4635416401688834398, 0.4661459711007739370, 0.4687499439416310532, 0.4713542964370365795, 0.4739583066701890113, 0.4765625766994796009, 0.4791667173199026797, 0.4817708376889431876, 0.4843751205813623395, 0.4869791187247021202, 0.4895834737840155659, 0.4921874508531692838, 0.4947917740137594000, 0.4973958416052992049, 0.5000000403837819851, 0.5026042571198243714, 0.5052083068480445194, 0.5078126377395105751, 0.5104166105391289010, 0.5130209629947408700, 0.5156249731913270518, 0.5182292431814352618, 0.5208333837687260104, 0.5234375040996330775, 0.5260417869599895990, 0.5286457850686206994, 0.5312501400964950715, 0.5338541171356111503, 0.5364584402653888029, 0.5390625078311259699, 0.5416667065794673608, 0.5442709232918542250, 0.5468749729921829061, 0.5494793038605755298, 0.5520832766365837418, 0.5546876290697317913, 0.5572916392473630243, 0.5598959092156829964, 0.5625000497873680061, 0.5651041700976676685, 0.5677084529433557014, 0.5703124510348895893, 0.5729168060486536929, 0.5755207830753605869, 0.5781251061916765632, 0.5807291737491879768, 0.5833333724848467350, 0.5859375891910368894, 0.5885416388810509325, 0.5911459697437208005, 0.5937499425137473530, 0.5963542949417601768, 0.5989583051180477069, 0.6015625750819736384, 0.6041667156555785567, 0.6067708359627971282, 0.6093751188112106476, 0.6119791169032582356, 0.6145834719202413199, 0.6171874489521673723, 0.6197917720723722379, 0.6223958396392350600, 0.6250000383796699976, 0.6276042550971219214, 0.6302083047943985994, 0.6328126356686964993, 0.6354166084503697354, 0.6380209608905765828, 0.6406249710831318778, 0.6432292410600577437, 0.6458333816531092175, 0.6484375019747732338, 0.6510417848433065480, 0.6536457829534795261, 0.6562501379910111732, 0.6588541150457848383, 0.6614584381872300467, 0.6640625057810221055, 0.6666667045436925898, 0.6692709212898660942, 0.6718749710119833463, 0.6744793019152608426, 0.6770832747262099938, 0.6796876271959411131, 0.6822916374223763070, 0.6848959074296973037, 0.6875000480597228680, 0.6901041684133596421, 0.6927084513194080584, 0.6953124494653194487, 0.6979168045407300180, 0.7005207816359816375, 0.7031251048160196415, 0.7057291724543196532, 0.7083333712566866058, 0.7109375880490425015, 0.7135416378135795989, 0.7161459687631898108, 0.7187499416210458847, 0.7213542941376326345, 0.7239583044155618596, 0.7265625744706748490, 0.7291667151552034820, 0.7317708355583423252, 0.7343751185193033715, 0.7369791167185673064, 0.7395834718491895998, 0.7421874490025512916, 0.7447917722385364314, 0.7473958399389256657, 0.7500000387984516736, 0.7526042556544531026, 0.7552083054789914263, 0.7578126364922896929, 0.7604166094146853627, 0.7630209619954617661, 0.7656249723425013753, 0.7682292424628052174, 0.7708333832193684509, 0.7734375036895410060, 0.7760417867228139865, 0.7786457849930478181, 0.7812501401962168579, 0.7838541174253229604, 0.7864584407346123518, 0.7890625085146746320, 0.7916667074488250577, 0.7942709243859374935, 0.7968749742880611997, 0.7994793053824050810, 0.8020832783869765725, 0.8046876310492792062, 0.8072916414830481058, 0.8098959116859448804, 0.8125000525320774658, 0.8151041730868179291, 0.8177084562098055898, 0.8203124545686294455, 0.8229168098616829186, 0.8255207871841712119, 0.8281251105841250792, 0.8307291784614470043, 0.8333333774876906519, 0.8359375945233833427, 0.8385416445206798075, 0.8411459757134309712, 0.8437499488178175078, 0.8463543015789862789, 0.8489583121171074831, 0.8515625824200027116, 0.8541667233732427311, 0.8567708440300897399, 0.8593751272601987123, 0.8619791257252362726, 0.8645834811255164176, 0.8671874585590289009, 0.8697917820670107991, 0.8723958500591838527, 0.8750000491949933012, 0.8776042663467393812, 0.8802083164568000884, 0.8828126477653241988, 0.8854166209871692228, 0.8880209738645485906, 0.8906249845246493324, 0.8932292549449527552, 0.8958333960228427317, 0.8984375167993386979, 0.9010418001539796107, 0.9036457987428592187, 0.9062501542677121602, 0.9088541318298947180, 0.9114584554632734203, 0.9140625235878931942, 0.9166667228507454634, 0.9192709401360219523, 0.9218749903764450471, 0.9244793218181143191, 0.9270832951750564987, 0.9296876481859919217, 0.9322916589857459524, 0.9348959295408556525, 0.9375000707608250883, 0.9401041916746273319, 0.9427084751713679101, 0.9453124739016935951, 0.9479168295687272483, 0.9505208072738278169, 0.9531251310501845930, 0.9557291993520028450, 0.9583333987332913750, 0.9609376160454207172, 0.9635416666839513589, 0.9661459986354887786, 0.9687499708159389433, 0.9713543235632202677, 0.9739583390673558494, 0.9765626083347638264, 0.9791667417950460361, 0.9817708662416058107, 0.9843751381318576188, 0.9869792129215403387, 0.9895836736503123010, 0.9921868305638316121, 0.9947912020913856068, 0.9973999845648282569, 1.000000000000000000 ),
 .UNSPECIFIED. ) ;
#80976=CARTESIAN_POINT ( 'NONE',  ( 2.232168359954420200, 2.116822148135434567, 0.04868514642705767947 ) ) ;
#80979=CARTESIAN_POINT ( 'NONE',  ( 4.018080225218490398, 2.055083638104511223, -0.2504045000601487492 ) ) ;
#80981=CARTESIAN_POINT ( 'NONE',  ( 5.367163668781920194, 2.014996964747676422, -0.5569773519958736152 ) ) ;
#80983=CARTESIAN_POINT ( 'NONE',  ( 3.768406797884563897, -1.226484811506942441, 1.352366043108324201 ) ) ;
#80988=CARTESIAN_POINT ( 'NONE',  ( 6.739307351729481255, -1.974284904759715298, 0.9861035376414882814 ) ) ;
#80991=CARTESIAN_POINT ( 'NONE',  ( 5.672493831469004100, 0.7790509395085333244, 1.746586765831580124 ) ) ;
#80998=CARTESIAN_POINT ( 'NONE',  ( 0.3976880421775743080, -0.6195963491163229975, -1.733980255833281969 ) ) ;
#81001=CARTESIAN_POINT ( 'NONE',  ( 5.114452126850835612, 1.290914414355217366, -1.353902443742838191 ) ) ;
#81002=CARTESIAN_POINT ( 'NONE',  ( -0.02299388927992032997, 1.367829385570513923, -2.164798317653505944 ) ) ;
#81008=CARTESIAN_POINT ( 'NONE',  ( 1.604289258337993296, 1.966964933800469106, 0.1018061066037061896 ) ) ;
#81009=CARTESIAN_POINT ( 'NONE',  ( 2.478138860811992306, -2.011206848916185397, -0.1455134472309257965 ) ) ;
#81012=CARTESIAN_POINT ( 'NONE',  ( 6.883263157960362477, -0.004191378316371896506, 2.053658919477070910 ) ) ;
#81013=CARTESIAN_POINT ( 'NONE',  ( 3.082162360440068749, -2.159116730143955998, -0.3741398933536920768 ) ) ;
#81023=CARTESIAN_POINT ( 'NONE',  ( 4.405690278861111864, -0.7914791229979671883, -1.662609734262666894 ) ) ;
#81024=CARTESIAN_POINT ( 'NONE',  ( 1.401040355039730345, -0.2976371227399738917, -1.990864243493442709 ) ) ;
#81025=CARTESIAN_POINT ( 'NONE',  ( 3.427438825619326668, 1.030710970775401414, 2.054361689694866211 ) ) ;
#81027=CARTESIAN_POINT ( 'NONE',  ( 1.604125426503384411, 1.858527726531463697, 0.09786615749988146484 ) ) ;
#81031=CARTESIAN_POINT ( 'NONE',  ( 6.170165192347925931, 1.906784905861274693, -0.1475879885542986936 ) ) ;
#81034=CARTESIAN_POINT ( 'NONE',  ( 4.845306142872277455, 0.6545843485197681000, -1.985720288498250774 ) ) ;
#81035=CARTESIAN_POINT ( 'NONE',  ( 3.115926070338378207, -0.9207206926411042325, -1.628290677324291780 ) ) ;
#81038=CARTESIAN_POINT ( 'NONE',  ( 5.636236351835953506, 0.3653394402399374741, 1.804471444190151930 ) ) ;
#81042=CARTESIAN_POINT ( 'NONE',  ( 4.740679804603589176, 0.2991043602584910199, 1.698571524128352994 ) ) ;
#81047=CARTESIAN_POINT ( 'NONE',  ( 5.243124948155760912, -0.2588677773407067617, -2.155501751117256948 ) ) ;
#81048=CARTESIAN_POINT ( 'NONE',  ( 3.211362085483655981, -0.3553965070040401852, 1.790585553824732390 ) ) ;
#81049=CARTESIAN_POINT ( 'NONE',  ( 0.7605091544688712402, -0.6555486260201286441, -1.849146037077718852 ) ) ;
#81051=CARTESIAN_POINT ( 'NONE',  ( 5.717987565503318770, 1.041469840191568963, -1.843387895306993318 ) ) ;
#81052=CARTESIAN_POINT ( 'NONE',  ( 5.882448709439383805, -0.3326909364035086081, -2.268010969791500742 ) ) ;
#81056=CARTESIAN_POINT ( 'NONE',  ( 1.032067064438058068, -2.067986175307830798, 0.4682213744369929098 ) ) ;
#81060=CARTESIAN_POINT ( 'NONE',  ( 6.754729744842355110, -0.5704115468931982846, -2.094772688322795506 ) ) ;
#81061=CARTESIAN_POINT ( 'NONE',  ( 6.983263157960391432, 4.691677264508577139, 2.616375093613742209 ) ) ;
#81063=CARTESIAN_POINT ( 'NONE',  ( 2.385647502782287432, 0.1060323020976374625, -2.218877139873560278 ) ) ;
#81065=CARTESIAN_POINT ( 'NONE',  ( 6.293592298849589817, 1.492257802130890765, -1.356297202127904944 ) ) ;
#81067=CARTESIAN_POINT ( 'NONE',  ( 5.120015017920454881, 2.040880116263335431, -0.2974388374509198685 ) ) ;
#81072=CARTESIAN_POINT ( 'NONE',  ( 0.1331565106231328843, 0.003911343561965873426, -1.946049565259087455 ) ) ;
#81073=CARTESIAN_POINT ( 'NONE',  ( 5.812015183962491172, 1.231757822100377320, -1.368757117762291253 ) ) ;
#81076=CARTESIAN_POINT ( 'NONE',  ( 1.447837905203141373, 1.722567860661971206, 0.08979103728979326293 ) ) ;
#81077=CARTESIAN_POINT ( 'NONE',  ( 0.1808755166769344391, 1.673851406602990366, -1.124249698880399162 ) ) ;
#81079=CARTESIAN_POINT ( 'NONE',  ( 2.671453201960610091, 0.1136055399131811194, -2.259690131287622084 ) ) ;
#81080=CARTESIAN_POINT ( 'NONE',  ( 4.565121803138184831, -1.881030885445551304, -0.9473677958443439406 ) ) ;
#81082=CARTESIAN_POINT ( 'NONE',  ( 2.371989033382770895, -1.092842237840240482, 1.391882982410238556 ) ) ;
#81087=CARTESIAN_POINT ( 'NONE',  ( -0.02240927558793281635, -1.987202795932199839, -0.9927825048469391955 ) ) ;
#81088=CARTESIAN_POINT ( 'NONE',  ( 3.820431320580887302, 2.080737768064028437, 0.6879518193209921417 ) ) ;
#81095=CARTESIAN_POINT ( 'NONE',  ( 6.240501835383900797, 1.219778281852833546, -1.734492557903525523 ) ) ;
#81101=CARTESIAN_POINT ( 'NONE',  ( 6.304252605626877504, 1.359535501544101077, -1.241908024382516018 ) ) ;
#81105=CARTESIAN_POINT ( 'NONE',  ( 2.331276520414362174, 0.8190846186081652824, -1.535621120930601213 ) ) ;
#81110=EDGE_CURVE ( 'NONE', #202176, #87871, #205449, .T. ) ;
#81111=CARTESIAN_POINT ( 'NONE',  ( 6.104392421991035711, -0.7735064434604683736, -2.018760209060527888 ) ) ;
#81115=CARTESIAN_POINT ( 'NONE',  ( 5.893488898593548520, 1.633865717575968324, 1.415524914074948404 ) ) ;
#81119=CARTESIAN_POINT ( 'NONE',  ( 5.694591516259816188, -0.4762896487527890632, -1.912855984147985744 ) ) ;
#81121=CARTESIAN_POINT ( 'NONE',  ( 4.833154173618329885, -1.132187431169606739, 1.313192701189482614 ) ) ;
#81123=CARTESIAN_POINT ( 'NONE',  ( 2.068174269828721101, -1.345378145056834063, 1.729934933326432445 ) ) ;
#81124=CARTESIAN_POINT ( 'NONE',  ( 3.733692867724636599, -2.133222801268436442, 0.8804087197434546930 ) ) ;
#81125=CARTESIAN_POINT ( 'NONE',  ( 4.358703909566331802, -1.529595902882211256, 1.381216288725060082 ) ) ;
#81126=CARTESIAN_POINT ( 'NONE',  ( 1.183423309950997870, -0.8736912582980368436, 1.734375191483277900 ) ) ;
#81130=CARTESIAN_POINT ( 'NONE',  ( 3.832379111121624327, -1.093062754469842579, -1.817066923117337751 ) ) ;
#81132=CARTESIAN_POINT ( 'NONE',  ( 2.584611472894111195, -0.6298744119781033435, 1.915600275669691488 ) ) ;
#81134=CARTESIAN_POINT ( 'NONE',  ( 4.225739626866775289, -2.112672615930260900, 0.6375689414055001336 ) ) ;
#81144=CARTESIAN_POINT ( 'NONE',  ( 4.575106920794588916, 0.002012451770977418796, -2.061077815012714254 ) ) ;
#81148=CARTESIAN_POINT ( 'NONE',  ( 3.141275609595588492, 0.05172059693002092201, 2.019191109193402056 ) ) ;
#81152=CARTESIAN_POINT ( 'NONE',  ( 3.116143102785688068, -1.014332071340098285, -1.793896330205650980 ) ) ;
#81155=FACE_OUTER_BOUND ( 'NONE', #138890, .T. ) ;
#81156=CARTESIAN_POINT ( 'NONE',  ( 1.622747808203903963, -1.734053015003593101, 0.6191010992530541213 ) ) ;
#81159=CARTESIAN_POINT ( 'NONE',  ( 6.235036409211808461, 0.2120174297785166195, 2.196685143856290878 ) ) ;
#81161=CARTESIAN_POINT ( 'NONE',  ( 2.144033130777025065, 0.8294244109963678779, -1.996327601563187670 ) ) ;
#81163=CARTESIAN_POINT ( 'NONE',  ( 1.376185782568883020, -2.007256511855738612, -0.1928315418098166534 ) ) ;
#81164=CARTESIAN_POINT ( 'NONE',  ( 2.443060400399544196, 1.412781429710145975, 1.812861393458516268 ) ) ;
#81167=CARTESIAN_POINT ( 'NONE',  ( 3.994965595081632959, 1.666078911148192843, -1.053691615683423510 ) ) ;
#81169=CARTESIAN_POINT ( 'NONE',  ( 4.768767694835816862, -0.2516295123269947642, -2.000731945836851544 ) ) ;
#81174=CARTESIAN_POINT ( 'NONE',  ( 6.287733905706966553, 1.451067878312240822, 1.526644127000365003 ) ) ;
#81175=CARTESIAN_POINT ( 'NONE',  ( 6.144996677366851401, -0.2998803957653916608, -2.048400609436632269 ) ) ;
#81179=CARTESIAN_POINT ( 'NONE',  ( 6.328379800955010737, -0.9556441952764772596, -1.779432800462784847 ) ) ;
#81181=CARTESIAN_POINT ( 'NONE',  ( 4.178580530314169650, -1.330465218273884087, 1.885386248989364466 ) ) ;
#81183=CARTESIAN_POINT ( 'NONE',  ( 2.448158969691970555, -0.8859891528392377369, 1.862743816677481679 ) ) ;
#81190=CARTESIAN_POINT ( 'NONE',  ( 3.824824921856139870, -1.460638251479762229, 1.606552252625459420 ) ) ;
#81194=CARTESIAN_POINT ( 'NONE',  ( 2.507154105146496725, -1.820902139252629448, 0.2722148935128121394 ) ) ;
#81196=CARTESIAN_POINT ( 'NONE',  ( 5.267185993530860699, 2.112242253262315739, -0.5839428218426812034 ) ) ;
#81198=CARTESIAN_POINT ( 'NONE',  ( 5.805634902324096736, -0.5560928936223124008, 2.193004490925544392 ) ) ;
#81203=CARTESIAN_POINT ( 'NONE',  ( 6.889980056308100842, -0.7542815031014777905, 1.599730008835710482 ) ) ;
#81204=CARTESIAN_POINT ( 'NONE',  ( 3.949861574111676266, -1.389792608731334811, -1.456582260380126392 ) ) ;
#81206=CARTESIAN_POINT ( 'NONE',  ( 3.065558131891146676, 0.3103791954156452371, -2.082839965623133782 ) ) ;
#81207=CARTESIAN_POINT ( 'NONE',  ( 2.003404541029256691, -1.857510701737439929, 0.4675905980212178292 ) ) ;
#81209=CARTESIAN_POINT ( 'NONE',  ( 3.437912432318380507, 1.247599126489881138, 1.524034350268144156 ) ) ;
#81210=CARTESIAN_POINT ( 'NONE',  ( 0.1450994221751950586, -1.442925249786636943, -1.190247126510869613 ) ) ;
#81211=CARTESIAN_POINT ( 'NONE',  ( 0.9066075625437097774, 0.5660373911110065936, 1.878450800843839419 ) ) ;
#81212=CARTESIAN_POINT ( 'NONE',  ( 3.932037377198682737, 0.9205326289291086983, -1.458499330894097668 ) ) ;
#81213=CARTESIAN_POINT ( 'NONE',  ( 0.5098338327763075606, -0.6861045072398126443, 1.785269576063217567 ) ) ;
#81215=CARTESIAN_POINT ( 'NONE',  ( 1.735297346119796691, 0.2185962045802778420, 2.196029071591873993 ) ) ;
#81221=CARTESIAN_POINT ( 'NONE',  ( 6.473496638176248652, -0.2593738453590052617, 2.053908440964563376 ) ) ;
#81222=CARTESIAN_POINT ( 'NONE',  ( 0.8189040078958352842, -1.500748464528355974, 1.426492703164506937 ) ) ;
#81227=CARTESIAN_POINT ( 'NONE',  ( 5.285831659486547984, 2.043504495962459977, -0.5658664308652374686 ) ) ;
#81232=CARTESIAN_POINT ( 'NONE',  ( 6.461383593301071926, 1.630371061775518271, 1.090930979547571456 ) ) ;
#81234=CARTESIAN_POINT ( 'NONE',  ( 4.059922587279920947, 1.704677108394496043, -1.076152822228809480 ) ) ;
#81235=CARTESIAN_POINT ( 'NONE',  ( 3.924928585964591932, -1.664043332733669667, 0.9490909334420574162 ) ) ;
#81237=CARTESIAN_POINT ( 'NONE',  ( 1.224469250947546328, 2.113408192816915943, 0.5798510048089372537 ) ) ;
#81238=CARTESIAN_POINT ( 'NONE',  ( 0.1333692844072316419, 7.629137130509075604, -2.653547345224521514 ) ) ;
#81239=CARTESIAN_POINT ( 'NONE',  ( 2.688565094423268853, -0.3157439183511835945, -1.843535313746543336 ) ) ;
#81243=CARTESIAN_POINT ( 'NONE',  ( 5.185217826725932788, 1.731529828693706641, 1.218147590116857026 ) ) ;
#81247=CARTESIAN_POINT ( 'NONE',  ( 2.120754239039924549, 0.003043923042475667976, 2.090933975095090158 ) ) ;
#81249=CARTESIAN_POINT ( 'NONE',  ( 1.166562959395722077, -1.556812811267356711, -0.7427251802107991407 ) ) ;
#81252=CARTESIAN_POINT ( 'NONE',  ( 6.825078400183569372, -0.002763825414428438751, 2.044262525762723826 ) ) ;
#81260=CARTESIAN_POINT ( 'NONE',  ( 1.330386229028382772, 1.216896677575128205, -1.342046333077246967 ) ) ;
#81264=CARTESIAN_POINT ( 'NONE',  ( 6.539320575229274013, 7.053493080409727334, 2.394893457813539683 ) ) ;
#81269=CARTESIAN_POINT ( 'NONE',  ( 3.051044903872371261, 1.597643715361036998, -0.9542115197753370248 ) ) ;
#81271=CARTESIAN_POINT ( 'NONE',  ( 0.2982578006338062471, 1.320465477219048722, -1.388022668363431356 ) ) ;
#81272=CARTESIAN_POINT ( 'NONE',  ( 6.493193421754636319, 1.675589973874438643, -0.9503142578028888066 ) ) ;
#81281=CARTESIAN_POINT ( 'NONE',  ( 5.190276988288149873, 1.015767153246112775, -1.687157232322311629 ) ) ;
#81282=CARTESIAN_POINT ( 'NONE',  ( 1.805496089173063590, 1.843435535509674317, -1.047849062051922076 ) ) ;
#81286=CARTESIAN_POINT ( 'NONE',  ( 6.228506716250251429, 0.2110190803071687604, 2.181275323772186692 ) ) ;
#81288=CARTESIAN_POINT ( 'NONE',  ( 4.735331810261827812, -1.761409202268785057, 0.7803939243795944281 ) ) ;
#81290=CARTESIAN_POINT ( 'NONE',  ( 0.4108170757193031486, 1.585627777896590151, 0.9046078287104839522 ) ) ;
#81291=CARTESIAN_POINT ( 'NONE',  ( 0.8212658843103730621, 2.040464674744349338, 0.8412164853940640175 ) ) ;
#81297=CARTESIAN_POINT ( 'NONE',  ( 5.840667653085179545, -1.920577060998058583, -0.4351772876184378247 ) ) ;
#81298=CARTESIAN_POINT ( 'NONE',  ( 0.9955321287432462585, -1.942234967994656669, 0.001507142460104027087 ) ) ;
#81299=CARTESIAN_POINT ( 'NONE',  ( 6.608760977740426590, 0.8891218545476579083, -2.119637956729656381 ) ) ;
#81301=CARTESIAN_POINT ( 'NONE',  ( 5.155058861800134729, 1.548501282276077529, -1.031774840880594901 ) ) ;
#81307=CARTESIAN_POINT ( 'NONE',  ( 1.980270094416748394, -2.150034404144373301, -0.4237573071887782983 ) ) ;
#81311=CARTESIAN_POINT ( 'NONE',  ( 1.892912435568369744, 1.589020553905008626, -0.8988452475950716725 ) ) ;
#81314=CARTESIAN_POINT ( 'NONE',  ( 6.509000000000051855, 1.248119779622055336, 2.213941609938009591 ) ) ;
#81316=CARTESIAN_POINT ( 'NONE',  ( 0.4516242601883875274, 0.6054225165459875546, -1.828971364544299538 ) ) ;
#81317=CARTESIAN_POINT ( 'NONE',  ( 4.364078322825436729, -1.956782558839207375, 0.1401112987177987601 ) ) ;
#81320=CARTESIAN_POINT ( 'NONE',  ( 4.124703146219878214, 0.1084699374758208573, 2.189010777610411740 ) ) ;
#81322=CARTESIAN_POINT ( 'NONE',  ( 3.467693386974544545, -0.4085244671708112008, 2.029378838279243258 ) ) ;
#81325=CARTESIAN_POINT ( 'NONE',  ( 3.586856395851648394, -0.6656857563790157251, 2.200217309063193127 ) ) ;
#81329=CARTESIAN_POINT ( 'NONE',  ( 6.720655732516647163, 2.082321177337285167, 2.135279995619132620 ) ) ;
#81331=CARTESIAN_POINT ( 'NONE',  ( 3.398316578678576949, 1.530473418458015100, -1.195227296853792920 ) ) ;
#81335=CARTESIAN_POINT ( 'NONE',  ( 4.465046277278037934, -1.532637281380120564, 1.143568071694904598 ) ) ;
#81337=CARTESIAN_POINT ( 'NONE',  ( 5.649328262929842914, -1.362134112713381029, -1.057878908126141715 ) ) ;
#81338=CARTESIAN_POINT ( 'NONE',  ( 4.733611406029458735, 0.6279933214467496860, -1.916352419866963697 ) ) ;
#81339=CARTESIAN_POINT ( 'NONE',  ( 4.588719013068318198, -0.6136123943910645195, 2.215248572529082693 ) ) ;
#81341=CARTESIAN_POINT ( 'NONE',  ( 0.5927436934281338221, -2.190715567557582677, -0.2661302102612560505 ) ) ;
#81344=CARTESIAN_POINT ( 'NONE',  ( 5.975818619601467319, 1.055637459841787473, 1.420274316496936917 ) ) ;
#81346=CARTESIAN_POINT ( 'NONE',  ( 2.168323659614699750, -1.408312831382242614, 1.808550206204377009 ) ) ;
#81347=CARTESIAN_POINT ( 'NONE',  ( 0.8666887897643248406, 1.678224016273874852, -0.4604494717724941233 ) ) ;
#81348=CARTESIAN_POINT ( 'NONE',  ( 6.369083545433415594, 2.098215621258665564, -0.6323776016037768732 ) ) ;
#81349=CARTESIAN_POINT ( 'NONE',  ( 1.123892771930210754, 0.3453300891937352568, -1.698893503174392139 ) ) ;
#81352=CARTESIAN_POINT ( 'NONE',  ( 1.381551413260760031, -0.05389312200515179035, 2.170675147484208534 ) ) ;
#81353=CARTESIAN_POINT ( 'NONE',  ( 2.606657977298726614, 1.900416011228076130, 0.6748465934659984011 ) ) ;
#81355=CARTESIAN_POINT ( 'NONE',  ( 5.918570133321236604, 1.291915522740747502, -1.429275465086258246 ) ) ;
#81357=CARTESIAN_POINT ( 'NONE',  ( 1.740793075861684303, 1.274151022659695709, -1.819517169034337467 ) ) ;
#81364=CARTESIAN_POINT ( 'NONE',  ( 5.442807971621070884, -1.376865196755885146, -1.064510927867247769 ) ) ;
#81365=CARTESIAN_POINT ( 'NONE',  ( 3.508209890309890167, 1.962046631884439174, 0.002529298861464468473 ) ) ;
#81369=CARTESIAN_POINT ( 'NONE',  ( 5.026804934256954738, 2.162974397647707825, 0.6633081500663459140 ) ) ;
#81370=CARTESIAN_POINT ( 'NONE',  ( 1.152864133210535824, -0.4991712053786099279, -2.001264041248071113 ) ) ;
#81372=CARTESIAN_POINT ( 'NONE',  ( 2.571453329723889958, 0.1116048768269807673, -2.259888279461387040 ) ) ;
#81375=CARTESIAN_POINT ( 'NONE',  ( 2.829206387438303327, -1.746784236434804072, 0.6695917499066756928 ) ) ;
#81376=CARTESIAN_POINT ( 'NONE',  ( 1.459138885926267504, -1.646488293146914472, -0.5446327844310631106 ) ) ;
#81377=CARTESIAN_POINT ( 'NONE',  ( 4.827760788416924242, 1.126602223531171898, -1.879657820484957664 ) ) ;
#81378=CARTESIAN_POINT ( 'NONE',  ( 0.3236265600991515834, -0.1057403636935544400, 2.204373366691187108 ) ) ;
#81379=CARTESIAN_POINT ( 'NONE',  ( 4.241217004700631676, -1.882188537963986219, 1.063020064016991117 ) ) ;
#81380=CARTESIAN_POINT ( 'NONE',  ( 4.242085645372923430, 0.5190250516928176516, 1.871238508296804604 ) ) ;
#81385=CARTESIAN_POINT ( 'NONE',  ( 0.5624999999999944489, -1.451031289061000207, -1.451031289061098795 ) ) ;
#81389=CARTESIAN_POINT ( 'NONE',  ( 5.291638762709002464, 1.525045427759319727, -1.319226660814104335 ) ) ;
#81393=CARTESIAN_POINT ( 'NONE',  ( 3.615676881913011176, -1.798418494116042821, 0.3134422064149794407 ) ) ;
#81401=CARTESIAN_POINT ( 'NONE',  ( 0.2287787457191146345, 1.389782569690813929, -1.465877111898945095 ) ) ;
#81402=CARTESIAN_POINT ( 'NONE',  ( 1.032067064438058068, -2.067986175307830798, 0.4682213744369929098 ) ) ;
#81406=CARTESIAN_POINT ( 'NONE',  ( 6.315316842782157991, -0.2547183123318246256, 2.045024454579154938 ) ) ;
#81407=CARTESIAN_POINT ( 'NONE',  ( 5.608046130584797950, -0.04667949407829304065, 2.016033753796213635 ) ) ;
#81417=CARTESIAN_POINT ( 'NONE',  ( 5.360703810585087048, -0.7282664037663032497, 1.880147357087233129 ) ) ;
#81418=CARTESIAN_POINT ( 'NONE',  ( 5.120983416928425846, -1.747193932927636029, 0.5808180576658967809 ) ) ;
#81420=CARTESIAN_POINT ( 'NONE',  ( 2.790017796326722532, 1.632578265707486098, 1.631241332076227346 ) ) ;
#81422=CARTESIAN_POINT ( 'NONE',  ( 6.274726406708529325, -2.050348626090079840, -0.6846857035173321560 ) ) ;
#81424=CARTESIAN_POINT ( 'NONE',  ( 1.259210993675137225, 1.913035009642606754, -0.3336937221413670551 ) ) ;
#81427=CARTESIAN_POINT ( 'NONE',  ( 4.851052417537679240, -1.089491736270932432, 2.023782222440795753 ) ) ;
#81428=CARTESIAN_POINT ( 'NONE',  ( 0.1753634416057497925, 0.0001173177735149660839, -2.144164757042037017 ) ) ;
#81431=CARTESIAN_POINT ( 'NONE',  ( 3.063207453921251489, 0.2760179531714930246, -1.850060308400132358 ) ) ;
#81434=CARTESIAN_POINT ( 'NONE',  ( 1.757924209179074770, 0.7287868685415777037, -1.768279316124596878 ) ) ;
#81438=CARTESIAN_POINT ( 'NONE',  ( 3.334799921508072806, 2.153101868192684343, 0.4835390122766567433 ) ) ;
#81439=CARTESIAN_POINT ( 'NONE',  ( 6.983263157960380774, 2.077058603031848527, 2.154533585220330227 ) ) ;
#81444=CARTESIAN_POINT ( 'NONE',  ( 0.6671782056521896598, 0.1977593025605048904, -1.961437444221861837 ) ) ;
#81446=CARTESIAN_POINT ( 'NONE',  ( 1.308152564336163115, -0.5581994038030186900, 2.238931160296030232 ) ) ;
#81447=CARTESIAN_POINT ( 'NONE',  ( 1.346068015636435522, -0.8851805579040676886, 1.750911360861057142 ) ) ;
#81448=CARTESIAN_POINT ( 'NONE',  ( 5.612196365462351011, 2.060443358388251323, -0.09580443939274756182 ) ) ;
#81455=CARTESIAN_POINT ( 'NONE',  ( 1.376089442288459752, -2.118726187661602367, 0.4732455120740781673 ) ) ;
#81457=CARTESIAN_POINT ( 'NONE',  ( 6.620655732516645742, 0.007553340620044741646, 1.826407896915737794 ) ) ;
#81460=CARTESIAN_POINT ( 'NONE',  ( 1.264687732342294701, -1.688641954842164283, -0.8049673154429252131 ) ) ;
#81461=CARTESIAN_POINT ( 'NONE',  ( 5.975883356200852425, 1.282301362320131588, 1.740048508431484953 ) ) ;
#81463=CARTESIAN_POINT ( 'NONE',  ( 0.07755575628181145265, 7.629137130509078268, -2.788902932953695846 ) ) ;
#81465=( BOUNDED_SURFACE ( )  B_SPLINE_SURFACE ( 3, 3, ( 
 ( #19182, #49556, #36505, #102585, #33303, #168644, #99388, #17037, #119970, #107992, #124263, #103663, #53839, #205400, #73265, #121055, #57040, #54902, #106914, #3982, #189167, #156685, #38654, #169711, #104734, #88482, #206475, #171852, #21301, #188088, #39719, #86332, #185947, #190222, #87408, #23447, #72190, #187022, #70050, #105826, #123206, #136164, #153472, #40806, #203259, #58104, #152403, #71121, #6122, #8276, #5046, #170780, #74360, #20247, #155608, #41881, #90626, #22370, #172939, #137237, #89557, #7192, #139370, #24516, #140463, #202182, #37579, #154541, #138299, #204314, #55971, #122124, #142589, #59164, #47215, #63441, #42948, #207544, #144733, #12538, #60229, #174021, #91702, #127466, #112258, #13609, #109057, #175074, #208597, #44006, #46144, #78611, #195579, #160945, #110125, #193437, #162020, #79684, #26661, #210744, #77547, #178272, #9352, #126389, #62368, #129591, #111190, #29882, #45081, #158809, #75424, #10405, #95966, #92764, #145797, #192348, #27737, #125322, #177193, #28809, #176137, #93831, #159872, #61304, #211803, #128530, #94893, #143670, #25590, #141536, #11476, #209663, #194499, #157754, #191282, #76478, #198737, #15731, #113330, #81816, #33069, #148951, #97033, #167337, #147899, #51456, #14668, #130647, #146850, #165197, #98094, #67656, #522, #117576, #116505, #196639, #183571, #48279, #35177, #64504, #181440, #163087, #180387, #100195, #2663, #133802, #1595, #66590, #151099, #166261, #49331, #132734, #199812, #50384, #101254, #131684, #16790, #182496, #18923, #197686, #82873, #34124, #17851, #83936, #150026, #212869, #80761, #114392, #85008, #179337, #68736, #32011, #134857, #164146, #200863, #30958, #213915, #65538, #115450, #99147, #40281, #42433, #159353, #58657, #56527, #124810, #52510, #3723, #152153, #59718, #69798, #102324, #109619, #86078, #26145, #36245, #190771, #108539, #174569, #138855, #106391, #204872, #122687, #118643, #188650, #156170, #125877, #173501, #141018, #74910, #207026, #184628, #92259, #158305, #57594, #143154, #168397, #9896, #19994, #75973, #90105, #172414, #24003, #73838, #41365, #189712, #175624, #93317, #43499, #25076, #142076, #7751, #208090, #139934, #205961, #123751, #107476, #91179, #8833, #157238, #191836, #27211, #10950, #77024, #63989, #81307, #179878, #29363, #46692, #129082, #32549, #12028, #130141, #112810, #82355, #110675, #211289, #30435, #95458, #13087, #160422, #44559, #80235, #111742, #209148, #177748, #195053, #96521, #192903, #48813, #31503, #161507, #147384, #176675, #163634, #131188, #79167, #78099, #145283, #62913, #180928, #146334, #210220, #162569, #14142, #60787, #144226, #98626, #61856, #212348, #178823, #196130, #28287, #47770, #97577, #94382, #128023, #15217, #113883, #164687, #126946, #45625, #213410, #197177, #193977, #65032, #114930, #16270, #69280, #37879, #4274, #150580, #36797, #50935, #19478, #167878, #3212, #151643, #101810, #119188, #49866, #85553, #135393, #1084, #54134, #201415, #117059, #33612, #21585, #103955, #17338, #181981, #185173, #53054, #34670, #148445, #66079, #102882, #86626, #202481, #83420, #149501, #183056, #18414, #20542, #168940, #169998, #152693, #84489, #70345, #136462, #120269, #67148, #186244, #52003, #15, #198230, #100740, #132220, #115992, #99683, #165752, #133283, #199290, #166821, #2142, #68219 ),
 ( #134350, #200353, #118129, #184114, #35735, #155900, #187319, #90911, #156976, #106130, #172153, #23745, #189456, #158045, #124550, #8565, #205693, #175361, #203543, #89850, #123492, #122424, #7487, #38947, #137528, #173230, #204614, #87690, #56265, #73569, #41098, #71416, #141823, #58394, #188381, #174301, #55197, #42165, #9631, #139671, #171068, #57328, #107207, #59454, #24810, #88776, #74646, #140751, #153765, #105030, #191570, #154834, #206762, #190508, #40019, #121344, #108280, #25876, #22665, #6418, #91986, #75708, #125611, #5333, #138591, #207825, #43234, #72490, #109351, #163363, #26942, #162294, #130918, #97304, #29094, #129873, #143952, #112533, #46416, #96243, #30155, #194779, #212076, #142880, #178545, #13881, #94118, #147121, #79960, #209947, #126673, #114669, #196911, #110411, #60512, #63715, #146063, #127755, #93049, #159090, #195856, #179609, #81034, #176414, #28021, #61586, #111474, #113605, #47496, #48551, #31230, #177479, #14939, #213147, #64777, #160159, #10688, #145010, #76758, #208882, #193712, #192636, #44289, #11757, #77831, #45355, #95178, #161227, #12814, #78887, #211016, #62639, #128797, #200097, #168682, #86371, #49598, #85297, #84230, #52796, #16003, #806, #151383, #136203, #117869, #118935, #51746, #165478, #82088, #17074, #184915, #115722, #152440, #133019, #34406, #65810, #183860, #35473, #199018, #50665, #116791, #67944, #36539, #2953, #101551, #150318, #53875, #148181, #182788, #1884, #66874, #100478, #131957, #214182, #167620, #83152, #180663, #149232, #166554, #134089, #164419, #20286, #69024, #18142, #102626, #197967, #135141, #4019, #19219, #181713, #201157, #70088, #202221, #32288, #33342, #98354, #99424, #185984, #71156, #9385, #187059, #123238, #171889, #154581, #169749, #73302, #8311, #21337, #121092, #90658, #88519, #91736, #37618, #170819, #105863, #41914, #38692, #204350, #108025, #120008, #40840, #75456, #190256, #122160, #74396, #22410, #205438, #139404, #189203, #106949, #57074, #156720, #87443, #172972, #24551, #104770, #25624, #140497, #6158, #5081, #207577, #141569, #203293, #153512, #206507, #58138, #72227, #103698, #137273, #124297, #174051, #157789, #54940, #138334, #56008, #188127, #39758, #23486, #89593, #155642, #7226, #128564, #145829, #29915, #93867, #111226, #193472, #97064, #76512, #159905, #211834, #175110, #142623, #92798, #177229, #44040, #13641, #94930, #63471, #62401, #208632, #129626, #60265, #195611, #10440, #127501, #109094, #126422, #46176, #163117, #79713, #162051, #160979, #14699, #112290, #209698, #12570, #47248, #78642, #113362, #77583, #28842, #194529, #179367, #143706, #144768, #178306, #210778, #95997, #30989, #158843, #42984, #192386, #80793, #125353, #146883, #110159, #59197, #176171, #191316, #26697, #27771, #11512, #61342, #45116, #197716, #199841, #102351, #1625, #213945, #67684, #212903, #164176, #98125, #2691, #15761, #48309, #52536, #32038, #183598, #196669, #133830, #51483, #117606, #81846, #49358, #147929, #65566, #64536, #131713, #99173, #68763, #116533, #83964, #17879, #150053, #130680, #35205, #101281, #549, #86108, #114420, #167364, #180420, #18952, #33098, #115477, #181469, #16817, #198764, #132761, #118670, #36274, #200890, #182522, #85036, #165225, #151125, #82902, #148975, #66614, #50414, #34152, #166290, #100222, #134883, #184653 ),
 ( #168423, #20019, #135931, #153238, #74133, #3749, #57874, #37351, #187860, #87168, #90388, #140227, #69823, #23213, #24282, #55736, #137001, #139137, #41652, #155373, #4809, #6958, #152179, #103425, #169487, #156457, #21070, #201949, #206248, #185718, #122977, #53605, #73039, #205166, #56807, #70891, #203029, #54670, #120818, #119739, #186795, #38424, #8043, #121891, #89326, #171619, #188936, #104503, #40575, #106681, #154314, #25368, #170547, #172704, #22131, #124036, #88244, #5887, #71960, #138070, #204083, #39487, #190002, #107766, #173792, #105585, #176970, #192127, #28587, #108832, #91468, #159652, #175916, #92547, #44858, #209437, #93607, #10186, #62156, #157530, #160717, #178043, #128314, #126163, #143440, #11249, #129375, #174858, #43792, #29659, #207323, #26437, #125101, #61081, #76260, #45922, #127241, #95745, #94675, #158586, #161796, #142369, #13387, #42724, #77327, #141311, #208378, #78392, #195354, #112042, #194277, #193211, #46986, #144512, #27507, #110962, #79463, #12311, #145580, #60010, #210520, #211577, #63211, #113102, #179108, #9124, #58944, #75200, #191059, #109905, #150879, #83716, #213694, #130432, #118426, #134643, #114175, #64286, #1380, #149806, #131465, #30730, #162862, #198520, #183355, #84791, #180169, #31795, #65316, #115230, #117357, #67441, #52297, #17630, #181220, #50166, #18708, #2442, #97870, #133586, #148735, #34959, #80531, #197466, #199590, #200648, #182277, #101030, #116287, #15505, #146627, #81592, #167121, #163930, #68516, #49110, #98923, #196418, #33902, #99980, #32847, #164976, #16568, #132522, #96813, #51233, #166046, #303, #14441, #212644, #82651, #66374, #48062, #147677, #135691, #19779, #55496, #86929, #184412, #152996, #104255, #5636, #168180, #24043, #155139, #4572, #56571, #85861, #138899, #106434, #202785, #53357, #54435, #38183, #156215, #121650, #185478, #137830, #203851, #36031, #201716, #73884, #37103, #187617, #21889, #70646, #151936, #39245, #72799, #3510, #103183, #6720, #136756, #7791, #102109, #20831, #170301, #172456, #169243, #120577, #90147, #69580, #105337, #139977, #171374, #22967, #89082, #204918, #122730, #119491, #188693, #40329, #186554, #205999, #57635, #87999, #154071, #71717, #13132, #207067, #157281, #94423, #176714, #9938, #123794, #41404, #77067, #61900, #177790, #58697, #124845, #92300, #208129, #210262, #28327, #145327, #110714, #59758, #143196, #111784, #29406, #190811, #160462, #27249, #128061, #173543, #158344, #12070, #79209, #60827, #194017, #209187, #108581, #25117, #174609, #45667, #42471, #95498, #76013, #191877, #8870, #126988, #192947, #142116, #125918, #43537, #10992, #161545, #78138, #44599, #93356, #211328, #91220, #109660, #159393, #175662, #144269, #74949, #141060, #189752, #107514, #26185, #36577, #100520, #117906, #200136, #103735, #83189, #166594, #4057, #181750, #149272, #99462, #183899, #50704, #20324, #101588, #70127, #69061, #851, #136240, #66916, #202261, #17112, #134127, #115760, #133057, #52836, #169786, #86410, #168721, #167656, #21375, #118972, #1925, #19256, #152477, #85338, #53911, #84269, #35510, #135181, #120047, #150355, #151420, #201196, #2993, #184950, #102663, #165519, #49636, #33381, #186021, #37658, #67984, #199058, #51789, #87483, #153549, #62953, #116828, #129122, #195099, #182830, #34445, #18183, #72266 ),
 ( #71195, #56047, #205479, #141605, #138374, #89631, #207613, #5119, #140534, #109134, #75493, #7265, #108063, #122203, #90699, #24592, #74434, #8349, #173011, #190293, #121133, #156761, #206546, #204392, #125389, #58175, #188165, #104811, #92835, #175147, #88558, #38730, #41951, #124335, #105905, #137311, #203327, #174089, #157827, #59231, #154618, #6197, #39798, #155683, #91770, #25661, #26733, #9423, #73342, #191355, #43020, #54980, #171930, #187096, #123280, #170856, #22446, #23524, #139444, #57111, #189241, #40881, #106986, #143742, #208670, #209736, #31025, #27807, #64573, #111262, #12607, #44077, #162088, #13678, #177265, #28881, #94964, #46212, #14737, #195650, #79749, #62437, #32074, #60301, #161012, #194566, #193509, #78679, #110196, #126459, #144806, #96036, #93905, #158879, #210812, #112328, #142660, #212936, #129663, #45150, #97101, #178342, #29951, #10475, #176206, #48346, #11549, #145865, #128600, #211872, #192423, #63511, #47285, #159945, #77619, #113397, #127537, #130715, #76550, #61380, #179405, #80829, #163153, #146918, #196706, #114457, #180457, #118703, #151158, #50450, #101319, #16857, #1663, #84002, #133870, #67719, #150092, #183638, #147967, #199877, #51520, #33133, #200926, #117645, #82938, #65599, #102390, #184691, #49392, #131748, #35244, #167401, #149011, #98162, #15796, #18991, #2727, #52574, #115511, #181504, #587, #198802, #85073, #68800, #164209, #134919, #116568, #36311, #81882, #213979, #66653, #197753, #99213, #165262, #182562, #132799, #34185, #100259, #166326, #17916, #96743, #62081, #127163, #128239, #163857, #160641, #197396, #29584, #145509, #176895, #80460, #146558, #95672, #161725, #13318, #179039, #147604, #114107, #212578, #195283, #164905, #193135, #79390, #113033, #111967, #211507, #28508, #44783, #63144, #14369, #12241, #77247, #129306, #30658, #61006, #131399, #47992, #177970, #15437, #110889, #31722, #213622, #46915, #78315, #162791, #64217, #49038, #130357, #144439, #94598, #180098, #196349, #97797, #143364, #209361, #81526, #65250, #115158, #210442, #194202, #45848, #181153, #32775, #98854, #86111, #135934, #18955, #213947, #180424, #147932, #552, #118673, #17882, #199844, #133833, #51486, #32042, #117609, #85039, #116536, #201952, #98129, #2694, #164180, #151127, #148978, #16820, #81850, #132764, #100225, #34155, #168426, #152182, #102354, #83967, #183601, #66617, #35209, #131716, #114424, #182526, #198767, #115480, #67687, #150056, #166293, #33102, #197719, #101285, #3752, #68766, #134886, #50417, #1628, #167367, #69826, #49360, #200893, #52539, #15765, #181472, #65569, #184657, #99176, #36277, #20022, #165228, #82905, #137005, #206251, #203032, #57877, #4813, #121894, #103428, #120821, #40578, #157533, #8046, #156460, #89329, #91472, #106684, #204086, #6961, #140230, #73042, #41656, #71963, #171622, #56810, #74137, #138073, #23216, #188939, #155376, #139140, #205169, #87172, #37354, #54673, #190005, #119742, #173795, #153240, #122980, #186798, #124039, #107769, #185721, #172708, #25371, #24285, #38427, #90391, #9128, #75203, #70894, #104506, #105588, #170550, #141314, #53609, #169490, #21072, #22134, #88247, #154317, #5891, #55739, #187863, #39490, #60013, #194281, #96816, #161800, #95748, #28591, #30734, #45926, #143444, #160722, #79467, #12315, #195358, #11252, #110966 ),
 ( #62160, #210524, #78396, #178046, #108835, #144516, #112046, #126166, #113107, #29664, #175919, #92550, #80535, #162865, #76263, #26440, #13390, #145584, #93610, #207326, #125105, #128318, #211581, #46990, #142372, #208382, #27510, #77331, #63215, #129379, #179112, #191062, #14445, #159655, #58947, #42727, #192130, #174861, #176974, #158589, #10189, #209441, #43795, #109908, #61086, #127245, #193215, #44862, #94679, #131469, #18711, #15510, #52301, #98926, #307, #31799, #149810, #1384, #164980, #16572, #82655, #33906, #2446, #183359, #67445, #50171, #19783, #48067, #148739, #182281, #181224, #66378, #97874, #196422, #132526, #83720, #81596, #146631, #198524, #99983, #130435, #200651, #117361, #32852, #84795, #114179, #150883, #133590, #147681, #68520, #213698, #134647, #163934, #116291, #180173, #65321, #199594, #36035, #101035, #34964, #166050, #184417, #51237, #17635, #167125, #118430, #102115, #168184, #212648, #64289, #197471, #49114, #115234, #55500, #6724, #121654, #39249, #105341, #119496, #69584, #86934, #7795, #151940, #206003, #185482, #187621, #20835, #24048, #73888, #3514, #171379, #172461, #203855, #70650, #72802, #189756, #89088, #152999, #155142, #85865, #37108, #103186, #90151, #169247, #135695, #139981, #4576, #56575, #201720, #138903, #204922, #106438, #57638, #107518, #122734, #136761, #53362, #202789, #186558, #156219, #22970, #188697, #40332, #123798, #54439, #41409, #173547, #88003, #120581, #38187, #104258, #170304, #21892, #154074, #5641, #71721, #137834, #10996, #159397, #79213, #62957, #13136, #209191, #110718, #125922, #176718, #42475, #25121, #93361, #109664, #26189, #192951, #143201, #27253, #158348, #108585, #28331, #129126, #194021, #210266, #59762, #77072, #60831, #195103, #174613, #191881, #177794, #141064, #92304, #58701, #126992, #9942, #45671, #44603, #145331, #91225, #94427, #111788, #160467, #76017, #12074, #46739, #78142, #142120, #144273, #157285, #190815, #124850, #29411, #208134, #74953, #211332, #43541, #61904, #8874, #128065, #95502, #161549, #112852, #207071, #175666, #64033, #30478, #212391, #65073, #183100, #82398, #49912, #198269, #116033, #96563, #182020, #83463, #180970, #52046, #162610, #67191, #14186, #149543, #213450, #81346, #146377, #197216, #164724, #98669, #18458, #2186, #166863, #148488, #33650, #131228, #99724, #196172, #178867, #32592, #48856, #179921, #132262, #56, #16313, #97619, #47812, #165796, #68262, #133328, #1129, #114970, #66119, #17380, #134394, #113925, #199332, #117099, #80279, #31543, #130179, #50977, #163676, #34711, #100781, #84535, #150625, #15259, #200397, #147426, #122471, #69325, #186288, #167924, #185217, #105079, #7533, #72540, #6463, #153812, #155948, #171117, #54174, #71461, #204660, #137574, #106176, #136505, #21629, #121391, #138638, #202525, #87737, #38994, #5384, #203592, #55244, #151687, #101856, #119234, #40066, #184159, #23790, #3257, #187364, #53101, #56310, #88825, #19523, #22710, #154880, #36841, #89897, #188431, #86669, #135435, #205740, #73616, #201457, #102923, #172202, #139716, #4318, #118172, #35780, #85599, #168984, #20584, #152736, #70388, #120314, #37926, #104000, #170043, #177527, #41146, #12864, #9678, #45405, #29140, #140795, #176458, #175403, #144003, #107256, #92032, #28070, #78938, #208927, #209995, #76807, #42209 ),
 ( #141864, #207874, #159135, #127804, #94164, #126721, #26987, #145060, #173276, #59496, #93094, #158090, #75754, #8609, #24856, #125653, #60562, #206807, #57373, #191615, #10737, #90958, #111521, #160204, #43277, #61637, #157023, #11806, #193758, #109398, #58440, #142927, #192682, #95227, #44335, #124595, #110457, #77881, #123536, #74692, #161277, #190553, #189501, #108326, #174346, #25924, #167404, #102393, #112587, #212126, #184694, #182565, #185758, #62688, #50453, #199880, #135972, #63764, #84005, #201988, #211063, #134923, #103466, #69863, #1666, #168460, #116571, #85076, #18994, #68803, #2731, #151161, #52577, #34188, #96295, #87212, #169528, #80010, #30208, #36314, #118706, #100262, #128847, #194829, #200929, #152219, #53645, #146115, #132802, #166329, #150095, #86148, #20058, #119778, #46464, #21108, #17919, #37391, #178598, #198805, #3788, #117648, #162347, #13930, #67722, #133873, #51523, #183641, #35247, #101322, #138113, #203068, #204124, #25406, #22173, #58983, #105628, #6998, #38467, #156498, #8088, #171657, #23254, #89367, #40617, #9162, #190041, #74176, #56850, #26475, #54711, #155415, #188973, #187900, #73076, #104543, #120862, #139177, #90429, #88288, #153276, #205208, #106721, #137041, #207363, #124077, #39530, #91509, #186835, #107804, #75238, #123022, #154352, #172748, #24323, #125139, #140268, #5930, #206288, #57912, #4853, #170588, #42765, #72002, #41693, #173829, #157569, #55776, #141348, #191097, #121933, #108872, #174896, #70932, #64323, #158627, #143479, #78429, #14480, #159685, #177007, #80569, #92585, #13425, #196457, #162898, #94712, #195395, #209475, #178081, #112079, #161837, #95780, #45958, #63251, #208414, #29698, #79501, #11286, #212682, #47025, #128350, #130467, #145619, #28624, #211615, #179147, #129412, #146668, #111003, #210559, #113140, #30771, #160754, #62194, #96850, #194317, #48100, #114212, #126203, #76298, #93642, #180210, #10224, #142406, #192165, #60048, #27547, #43826, #109942, #175951, #77365, #61117, #127278, #193249, #44896, #12349, #144551, #32885, #35000, #31833, #197506, #131502, #36070, #49149, #81629, #85903, #65355, #2481, #15544, #167159, #101072, #52338, #3551, #53394, #150920, #115266, #97908, #181258, #132558, #102152, #149849, #117398, #51274, #183395, #163968, #18746, #68557, #33944, #119531, #147714, #134684, #213732, #200687, #66413, #148771, #98962, #50206, #17671, #166083, #151977, #69621, #19818, #1418, #84831, #198558, #118466, #165013, #16608, #100019, #116324, #82689, #199628, #67481, #83757, #340, #182315, #184452, #135731, #168218, #201753, #133626, #23004, #105377, #8909, #202822, #5676, #123832, #86967, #54471, #4610, #89122, #170341, #140015, #6760, #189794, #188731, #120615, #41445, #186593, #107553, #136797, #39282, #20868, #38220, #172498, #74989, #206040, #24084, #91259, #169282, #141097, #137870, #173587, #157318, #104293, #90189, #155176, #57674, #153036, #71754, #156252, #207108, #122771, #25157, #204959, #21926, #70684, #88035, #58735, #154107, #185517, #203890, #171416, #55535, #40369, #106471, #121689, #187656, #72835, #138939, #37141, #7831, #73922, #56607, #103223, #26222, #127025, #160500, #159430, #143231, #76051, #174646, #192983, #61937, #59798, #124887, #44637, #12105, #108618, #178899, #95534, #11029, #211366, #92338, #79249, #46773 ),
 ( #14217, #191911, #128095, #176750, #77107, #158380, #78175, #13170, #9973, #125955, #161583, #93393, #96594, #190851, #175697, #110752, #112887, #43575, #209221, #30513, #42512, #45705, #80312, #195137, #28365, #145367, #27287, #210297, #144303, #194053, #111824, #177826, #62991, #142152, #29443, #129160, #109693, #162644, #146412, #60863, #208167, #212425, #94460, #147461, #97651, #34743, #117135, #164761, #64067, #196204, #17413, #2222, #118207, #213482, #65106, #32625, #148521, #150660, #184194, #16351, #132297, #163710, #67227, #133361, #82431, #87, #66152, #165829, #134430, #100816, #199368, #182055, #151724, #179954, #198304, #99762, #98702, #49944, #15292, #113957, #116065, #1163, #131262, #130211, #33685, #83497, #47846, #35817, #166901, #149579, #68297, #31577, #18494, #200433, #51014, #197249, #183138, #84572, #101893, #52080, #48888, #167958, #19564, #81377, #115008, #85638, #181005, #6502, #55281, #37964, #53141, #171155, #106213, #119271, #4358, #188469, #186330, #189536, #69364, #54215, #203629, #139756, #70427, #87778, #205780, #3296, #138678, #107291, #73656, #5423, #172239, #120353, #88863, #22745, #72577, #204697, #154918, #40101, #185256, #56347, #122509, #136543, #123574, #23827, #104037, #102963, #90998, #173313, #86707, #36880, #89932, #155983, #170083, #135473, #201494, #7571, #57408, #41184, #152776, #202563, #21670, #153852, #24892, #169021, #20619, #71502, #137613, #121429, #187399, #39031, #105115, #61674, #60600, #29179, #206846, #191651, #127842, #112626, #94201, #95268, #176495, #141901, #58478, #207911, #161316, #25963, #158126, #160241, #157061, #108361, #42248, #12900, #174385, #124633, #211103, #190591, #193794, #140833, #77918, #11841, #177566, #128888, #178636, #45443, #92068, #8649, #9717, #43316, #78980, #126759, #28106, #144037, #210034, #74728, #111557, #145099, #159172, #30248, #75793, #62727, #59532, #194869, #109434, #125692, #175440, #27025, #142965, #76846, #46503, #93133, #10772, #192719, #208968, #44373, #110496, #113698, #96332, #164509, #180752, #97395, #49688, #214270, #98445, #15031, #179702, #181803, #134174, #50752, #66971, #131010, #148271, #16093, #200182, #31318, #197002, #34496, #212168, #163451, #129960, #65903, #81123, #116881, #132049, #100570, #99513, #147208, #166643, #213233, #18234, #47584, #82177, #146152, #64865, #83239, #51835, #182880, #199107, #198059, #117953, #149324, #32379, #115816, #84318, #33436, #150404, #114755, #165570, #17165, #1971, #902, #133110, #68034, #183948, #162388, #13965, #195948, #80049, #48637, #63802, #101639, #155731, #135232, #71244, #185003, #188211, #23573, #167705, #121178, #122252, #153599, #20374, #22495, #139497, #38776, #151470, #37709, #137360, #70177, #53959, #201245, #85386, #103785, #187147, #36627, #35558, #169836, #203377, #19307, #89682, #6248, #136289, #39851, #3041, #204442, #171981, #120097, #119021, #186075, #21423, #7316, #104858, #102712, #55030, #170902, #69110, #52886, #205525, #168769, #88607, #87532, #202310, #86459, #154662, #138423, #152523, #4108, #72317, #5171, #73394, #56096, #105957, #57160, #123323, #42002, #59283, #111312, #189286, #110246, #78728, #45199, #191403, #77669, #91820, #60347, #208721, #44126, #192472, #142712, #159994, #90748, #126510, #176255, #108110, #95014, #27856, #157877, #74479 ) ),
 .UNSPECIFIED., .T., .F., .T. ) 
 B_SPLINE_SURFACE_WITH_KNOTS ( ( 4, 3, 4 ),
 ( 4, 1, 1, 1, 1, 1, 1, 1, 1, 1, 1, 1, 1, 1, 1, 1, 1, 1, 1, 1, 1, 1, 1, 1, 1, 1, 1, 1, 1, 1, 1, 1, 1, 1, 1, 1, 1, 1, 1, 1, 1, 1, 1, 1, 1, 1, 1, 1, 1, 1, 1, 1, 1, 1, 1, 1, 1, 1, 1, 1, 1, 1, 1, 1, 1, 1, 1, 1, 1, 1, 1, 1, 1, 1, 1, 1, 1, 1, 1, 1, 1, 1, 1, 1, 1, 1, 1, 1, 1, 1, 1, 1, 1, 1, 1, 1, 1, 1, 1, 1, 1, 1, 1, 1, 1, 1, 1, 1, 1, 1, 1, 1, 1, 1, 1, 1, 1, 1, 1, 1, 1, 1, 1, 1, 1, 1, 1, 1, 1, 1, 1, 1, 1, 1, 1, 1, 1, 1, 1, 1, 1, 1, 1, 1, 1, 1, 1, 1, 1, 1, 1, 1, 1, 1, 1, 1, 1, 1, 1, 1, 1, 1, 1, 1, 1, 1, 1, 1, 1, 1, 1, 1, 1, 1, 1, 1, 1, 1, 1, 1, 1, 1, 1, 1, 1, 1, 1, 1, 1, 1, 1, 1, 1, 1, 1, 1, 1, 1, 1, 1, 1, 1, 1, 1, 1, 1, 1, 1, 1, 1, 1, 1, 1, 1, 1, 1, 1, 1, 1, 1, 1, 1, 1, 1, 1, 1, 1, 1, 1, 1, 1, 1, 1, 1, 1, 1, 1, 1, 1, 1, 1, 1, 1, 1, 1, 1, 1, 1, 1, 1, 1, 1, 1, 1, 1, 1, 1, 1, 1, 1, 1, 1, 1, 1, 1, 1, 1, 1, 1, 1, 1, 1, 1, 1, 1, 1, 1, 1, 1, 1, 1, 1, 1, 1, 1, 1, 1, 1, 1, 1, 1, 1, 1, 1, 1, 1, 1, 1, 1, 1, 1, 1, 1, 1, 1, 1, 1, 1, 1, 1, 1, 1, 1, 1, 1, 1, 1, 1, 1, 1, 1, 1, 1, 1, 1, 1, 1, 1, 1, 1, 1, 1, 1, 1, 1, 1, 1, 1, 1, 1, 1, 1, 1, 1, 1, 1, 1, 1, 1, 1, 1, 1, 1, 1, 1, 1, 1, 1, 1, 1, 1, 1, 1, 1, 1, 1, 1, 1, 1, 1, 1, 1, 1, 1, 1, 1, 1, 1, 1, 1, 1, 1, 1, 1, 4 ),
 ( 0.000000000000000000, 0.5000000000000000000, 1.000000000000000000 ),
 ( 0.000000000000000000, 0.002599888508634240914, 0.005208754120092145765, 0.007813069968323356138, 0.01041690100177071650, 0.01302019566086259385, 0.01562517182793091500, 0.01822893254318404960, 0.02083328139698771564, 0.02343764900838959594, 0.02604139750447371365, 0.02864615928571910553, 0.03124958462592061434, 0.03385442086835698666, 0.03645794792899405279, 0.03906256697173399878, 0.04166661757251870907, 0.04427067912273281725, 0.04687528696281444140, 0.04947881815967773017, 0.05208365228821221909, 0.05468707701066444909, 0.05729184299815447134, 0.05989557646906591704, 0.06249996333325048142, 0.06510433798480201595, 0.06770807906337909798, 0.07031283757201339801, 0.07291626355048291819, 0.07552109983967189577, 0.07812462590386089201, 0.08072924387304455940, 0.08333329402460390445, 0.08593735478041557296, 0.08854196204427712547, 0.09114549249794960672, 0.09375032597506528786, 0.09635375006294695510, 0.09895851527076646170, 0.1015622481948881828, 0.1041666342325376776, 0.1067710083972730206, 0.1093747487337090180, 0.1119795066911244419, 0.1145829320296284648, 0.1171877676425944481, 0.1197912931610935483, 0.1223959103579086161, 0.1249999600491941698, 0.1276040200539713398, 0.1302086268569593308, 0.1328121566649932417, 0.1354169895755736042, 0.1380204131161003600, 0.1406251776355303407, 0.1432289101024236955, 0.1458332954032181272, 0.1484376691708411133, 0.1510414088543486633, 0.1536461663508109643, 0.1562495911381983071, 0.1588544261652600487, 0.1614579512270202244, 0.1640625677415503691, 0.1666666170620310916, 0.1692706764052687440, 0.1718752828374313091, 0.1744788120887783289, 0.1770836445231302458, 0.1796870676051354199, 0.1822918315264069888, 0.1848955636252137269, 0.1874999482789682093, 0.1901043217392619777, 0.1927080608589964439, 0.1953128179847096746, 0.1979162423098047296, 0.2005210768412587219, 0.2031246015352002054, 0.2057292174574958665, 0.2083332664966131842, 0.2109373252677763377, 0.2135419314191336626, 0.2161454602027163274, 0.2187502922511180836, 0.2213537149634070833, 0.2239584783767220588, 0.2265622101965570623, 0.2291665942930569411, 0.2317709675357785548, 0.2343747061808670040, 0.2369794630260087243, 0.2395828869776091552, 0.2421877211037245237, 0.2447912455187418734, 0.2473958609388257068, 0.2499999097859964270, 0.2526039680745227334, 0.2552085740350705789, 0.2578121024397855843, 0.2604169341924902348, 0.2630203566238439872, 0.2656251196193780695, 0.2682288512493328225, 0.2708332348783377697, 0.2734376079932215875, 0.2760413462527663842, 0.2786461029074911444, 0.2812495265743710227, 0.2838543603853929120, 0.2864578846103582599, 0.2890624996182282747, 0.2916665483628478883, 0.2942706062581511572, 0.2968752121178640513, 0.2994787402325856385, 0.3020835717798243114, 0.3046869940190023440, 0.3072917566869088346, 0.3098954882160545599, 0.3124998714673014044, 0.3151042445440625506, 0.3177079825071445485, 0.3203127390615869707, 0.3229161625325003282, 0.3255209961186533163, 0.3281245202424198926, 0.3307291349280532256, 0.3333331836594992104, 0.3359372412509727956, 0.3385418470998076690, 0.3411453750133909280, 0.3437502064453764050, 0.3463536285811206206, 0.3489583910115333087, 0.3515621225289245477, 0.3541665054921307454, 0.3567708786204680238, 0.3593746163761498691, 0.3619793729204284771, 0.3645827962841124981, 0.3671876297356038710, 0.3697911538470093351, 0.3723957683003653041, 0.3749998171080005105, 0.3776038744850206963, 0.3802084804129200468, 0.3828120082142042468, 0.3854168396211344327, 0.3880202617421720235, 0.3906250240252089334, 0.3932287556198868494, 0.3958331383847540352, 0.3984375116543538153, 0.4010412492916836102, 0.4036460059159037717, 0.4062494292610819846, 0.4088542626681055392, 0.4114577868559751161, 0.4140624011669984950, 0.4166664501401745602, 0.4192705073921035863, 0.4218751134889988097, 0.4244786412668108966, 0.4270834727388717056, 0.4296868949339185950, 0.4322916571596854274, 0.4348953889206810253, 0.4374997715768980666, 0.4401041450774376140, 0.4427078826854516369, 0.4453126394797092824, 0.4479160628950952239, 0.4505208963478340434, 0.4531244207009840763, 0.4557290349596088697, 0.4583330841876695483, 0.4609371414038593850, 0.4635417477596745495, 0.4661452756028321986, 0.4687501072302013849, 0.4713535295879656695, 0.4739582918465587991, 0.4765620238628961447, 0.4791664065001429718, 0.4817707803212932793, 0.4843745179890200370, 0.4869792750434049911, 0.4895826986177053142, 0.4921875322063354874, 0.4947910568135764908, 0.4973956711097291539, 0.4999997206820134821, 0.5026037779518089943, 0.5052083846564635605, 0.5078119126537786743, 0.5104167445266291070, 0.5130201671358142201, 0.5156249295173244152, 0.5182286618780244103, 0.5208330445859747915, 0.5234374188174044651, 0.5260411566338674128, 0.5286459140384663913, 0.5312493378603841965, 0.5338541716750782040, 0.5364576966252184720, 0.5390623110488209635, 0.5416663610546670338, 0.5442704184674093115, 0.5468750256108222407, 0.5494785538511040013, 0.5520833860596070508, 0.5546868090089153158, 0.5572915716034309019, 0.5598953043975141153, 0.5624996872658396541, 0.5651040619972180767, 0.5677078000514395040, 0.5703125578963399445, 0.5729159820545779436, 0.5755208161855079885, 0.5781243415673570363, 0.5807289562083304268, 0.5833330067370782190, 0.5859370643821081304, 0.5885416720542003821, 0.5911452006262593040, 0.5937500332605881725, 0.5963534566387238556, 0.5989582195363342132, 0.6015619528528246551, 0.6041663359711972880, 0.6067707112921981727, 0.6093744496732020899, 0.6119792080484952601, 0.6145826326317597177, 0.6171874671691013337, 0.6197909930714722293, 0.6223956080197403651, 0.6249996591607356322, 0.6276037171273963766, 0.6302083254180952387, 0.6328118544107458332, 0.6354166875610788301, 0.6380201114567515264, 0.6406248747475506988, 0.6432286086754787080, 0.6458329921335752566, 0.6484373681338796436, 0.6510411069306952792, 0.6536458659264798854, 0.6562492910234830612, 0.6588541260574176661, 0.6614576525691320263, 0.6640622679146246377, 0.6666663197572214594, 0.6692703781348633418, 0.6718749871341050950, 0.6744785166361690898, 0.6770833503926931840, 0.6796867748946214816, 0.6822915386687108397, 0.6848952732971168578, 0.6874996571846213600, 0.6901040339539210589, 0.6927077732555863010, 0.6953125329619718187, 0.6979159586614360755, 0.7005207942821553013, 0.7031243214920454010, 0.7057289373247008779, 0.7083329899582661016, 0.7109370488362486418, 0.7135416586339821121, 0.7161451887342924483, 0.7187500231872065992, 0.7213534483841206324, 0.7239582127316128712, 0.7265619481495508847, 0.7291663325561579256, 0.7317707101841592898, 0.7343744500797240171, 0.7369792105868335774, 0.7395826369774940456, 0.7421874732752028470, 0.7447910012721150608, 0.7473956176818850050, 0.7499996711958007989, 0.7526037306634962842, 0.7552083413496862851, 0.7578118721370898925, 0.7604167073766084917, 0.7630201333572542710, 0.7656248983682768516, 0.7682286346648167230, 0.7708330196802359868, 0.7734373982566630223, 0.7760411388351919904, 0.7786459002331664880, 0.7812493274037752844, 0.7838541644686951582, 0.7864576933414935134, 0.7890623104183455139, 0.7916663649020125870, 0.7942704250488100692, 0.7968750367134410650, 0.7994785682768023038, 0.8020834043931583945, 0.8046868312463003603, 0.8072915970109983963, 0.8098953342752303053, 0.8124997199891885735, 0.8151040996037859365, 0.8177078409543626636, 0.8203126033333638656, 0.8229160313726919806, 0.8255208692950642968, 0.8281243991326340259, 0.8307290169665545454, 0.8333330725093962554, 0.8359371334247044372, 0.8385417461577832077, 0.8411452785859873105, 0.8437501156694361404, 0.8463535434838604932, 0.8489583100924004144, 0.8515620484134380774, 0.8541664349156833369, 0.8567708156582201084, 0.8593745578699503174, 0.8619793213201638604, 0.8645827503170061545, 0.8671875891870957087, 0.8697911200783463581, 0.8723957387593448409, 0.8749997954508100806, 0.8776038572240605351, 0.8802084711156200614, 0.8828120044975765746, 0.8854168426383988155, 0.8880202715029178462, 0.8906250390454908406, 0.8932287785124739532, 0.8958331658927787267, 0.8984375478530519654, 0.9010412910150662480, 0.9036460556267057465, 0.9062494856698833923, 0.9088543255779816255, 0.9114578576118502751, 0.9140624772299625889, 0.9166665351595286726, 0.9192705978801787303, 0.9218752130202838568, 0.9244787474449313036, 0.9270835867334279445, 0.9296870167368762594, 0.9322917853037333558, 0.9348955260058576799, 0.9374999143539141100, 0.9401042976215825409, 0.9427080418234272674, 0.9453128076877782560, 0.9479162388645026027, 0.9505210798953250828, 0.9531246131693177359, 0.9557292338404025367, 0.9583332930514818493, 0.9609373567081632705, 0.9635419734050364449, 0.9661455093234165847, 0.9687503490003109841, 0.9713537788664922124, 0.9739585512809396661, 0.9765622998769101226, 0.9791666815729623830, 0.9817710277688282972, 0.9843747994658795797, 0.9869797739623470401, 0.9895830763955310028, 0.9921869177308453303, 0.9947912343601759133, 0.9974001139318913189, 1.000000000000000000 ),
 .UNSPECIFIED. ) 
 GEOMETRIC_REPRESENTATION_ITEM ( )  RATIONAL_B_SPLINE_SURFACE ( (
 ( 1.000000000000000222, 1.000000000000000222, 1.000000000000000222, 1.000000000000000000, 1.000000000000000000, 1.000000000000000444, 1.000000000000000000, 0.9999999999999997780, 1.000000000000000444, 0.9999999999999997780, 0.9999999999999997780, 1.000000000000000222, 0.9999999999999997780, 0.9999999999999997780, 1.000000000000000444, 0.9999999999999997780, 1.000000000000000222, 1.000000000000000222, 0.9999999999999996669, 1.000000000000000222, 0.9999999999999996669, 1.000000000000000444, 0.9999999999999994449, 1.000000000000000444, 0.9999999999999996669, 1.000000000000000222, 1.000000000000000000, 0.9999999999999997780, 1.000000000000000222, 0.9999999999999997780, 1.000000000000000000, 0.9999999999999997780, 1.000000000000000000, 1.000000000000000222, 0.9999999999999996669, 1.000000000000000000, 0.9999999999999997780, 1.000000000000000000, 1.000000000000000444, 0.9999999999999996669, 1.000000000000000222, 1.000000000000000000, 1.000000000000000222, 1.000000000000000222, 0.9999999999999997780, 0.9999999999999997780, 1.000000000000000222, 0.9999999999999997780, 1.000000000000000222, 0.9999999999999997780, 0.9999999999999997780, 0.9999999999999997780, 1.000000000000000444, 1.000000000000000000, 0.9999999999999997780, 1.000000000000000222, 1.000000000000000000, 1.000000000000000000, 0.9999999999999997780, 1.000000000000000222, 1.000000000000000000, 1.000000000000000000, 1.000000000000000222, 1.000000000000000000, 1.000000000000000000, 1.000000000000000000, 1.000000000000000222, 1.000000000000000000, 0.9999999999999997780, 1.000000000000000444, 1.000000000000000000, 0.9999999999999997780, 1.000000000000000000, 1.000000000000000222, 0.9999999999999997780, 1.000000000000000222, 0.9999999999999996669, 1.000000000000000222, 1.000000000000000000, 1.000000000000000000, 1.000000000000000000, 1.000000000000000222, 0.9999999999999997780, 1.000000000000000000, 1.000000000000000222, 0.9999999999999997780, 1.000000000000000000, 1.000000000000000000, 0.9999999999999996669, 1.000000000000000000, 1.000000000000000000, 1.000000000000000222, 1.000000000000000000, 0.9999999999999997780, 1.000000000000000222, 0.9999999999999996669, 1.000000000000000222, 0.9999999999999997780, 1.000000000000000000, 1.000000000000000000, 1.000000000000000222, 0.9999999999999996669, 1.000000000000000444, 1.000000000000000000, 0.9999999999999997780, 1.000000000000000000, 1.000000000000000000, 1.000000000000000222, 0.9999999999999997780, 1.000000000000000000, 1.000000000000000222, 1.000000000000000444, 1.000000000000000000, 1.000000000000000000, 1.000000000000000444, 1.000000000000000000, 0.9999999999999997780, 1.000000000000000222, 1.000000000000000000, 1.000000000000000000, 1.000000000000000000, 1.000000000000000000, 1.000000000000000000, 1.000000000000000000, 0.9999999999999996669, 1.000000000000000222, 0.9999999999999997780, 1.000000000000000222, 1.000000000000000000, 0.9999999999999997780, 1.000000000000000222, 0.9999999999999997780, 0.9999999999999997780, 0.9999999999999997780, 1.000000000000000000, 1.000000000000000000, 0.9999999999999996669, 1.000000000000000444, 1.000000000000000222, 1.000000000000000000, 1.000000000000000000, 1.000000000000000222, 1.000000000000000222, 1.000000000000000000, 1.000000000000000222, 0.9999999999999996669, 1.000000000000000444, 0.9999999999999997780, 0.9999999999999997780, 1.000000000000000444, 1.000000000000000000, 1.000000000000000222, 0.9999999999999997780, 1.000000000000000222, 1.000000000000000000, 1.000000000000000222, 1.000000000000000000, 1.000000000000000000, 0.9999999999999996669, 1.000000000000000444, 1.000000000000000000, 1.000000000000000222, 0.9999999999999997780, 1.000000000000000000, 1.000000000000000000, 1.000000000000000000, 1.000000000000000000, 0.9999999999999997780, 1.000000000000000000, 1.000000000000000000, 1.000000000000000000, 1.000000000000000222, 1.000000000000000222, 0.9999999999999997780, 1.000000000000000000, 1.000000000000000000, 0.9999999999999997780, 1.000000000000000000, 1.000000000000000000, 1.000000000000000000, 1.000000000000000000, 1.000000000000000444, 0.9999999999999997780, 1.000000000000000222, 0.9999999999999997780, 1.000000000000000000, 1.000000000000000222, 0.9999999999999997780, 1.000000000000000222, 1.000000000000000000, 1.000000000000000000, 1.000000000000000000, 1.000000000000000000, 0.9999999999999997780, 1.000000000000000000, 1.000000000000000000, 1.000000000000000000, 1.000000000000000000, 1.000000000000000000, 1.000000000000000222, 1.000000000000000000, 1.000000000000000222, 0.9999999999999997780, 1.000000000000000222, 0.9999999999999997780, 1.000000000000000222, 1.000000000000000000, 0.9999999999999997780, 1.000000000000000222, 0.9999999999999996669, 1.000000000000000444, 1.000000000000000000, 0.9999999999999996669, 1.000000000000000222, 1.000000000000000000, 1.000000000000000222, 0.9999999999999997780, 1.000000000000000444, 1.000000000000000000, 1.000000000000000000, 0.9999999999999997780, 1.000000000000000222, 1.000000000000000000, 1.000000000000000000, 1.000000000000000000, 1.000000000000000222, 0.9999999999999997780, 1.000000000000000222, 1.000000000000000000, 0.9999999999999997780, 1.000000000000000000, 0.9999999999999997780, 1.000000000000000222, 0.9999999999999996669, 1.000000000000000000, 1.000000000000000000, 1.000000000000000000, 1.000000000000000444, 1.000000000000000222, 1.000000000000000000, 1.000000000000000000, 0.9999999999999997780, 0.9999999999999997780, 1.000000000000000444, 0.9999999999999996669, 1.000000000000000444, 0.9999999999999997780, 0.9999999999999997780, 1.000000000000000222, 0.9999999999999997780, 0.9999999999999996669, 1.000000000000000444, 0.9999999999999997780, 1.000000000000000222, 1.000000000000000222, 1.000000000000000000, 0.9999999999999997780, 1.000000000000000222, 1.000000000000000000, 1.000000000000000222, 1.000000000000000000, 1.000000000000000000, 0.9999999999999997780, 0.9999999999999997780, 1.000000000000000444, 0.9999999999999997780, 0.9999999999999997780, 1.000000000000000222, 0.9999999999999994449, 1.000000000000000222, 0.9999999999999997780, 1.000000000000000000, 0.9999999999999997780, 1.000000000000000000, 1.000000000000000000, 1.000000000000000000, 1.000000000000000000, 1.000000000000000000, 1.000000000000000000, 1.000000000000000000, 1.000000000000000222, 1.000000000000000000, 1.000000000000000000, 1.000000000000000000, 1.000000000000000000, 1.000000000000000000, 1.000000000000000000, 1.000000000000000000, 1.000000000000000222, 1.000000000000000000, 1.000000000000000222, 0.9999999999999997780, 1.000000000000000000, 1.000000000000000444, 1.000000000000000000, 1.000000000000000000, 1.000000000000000000, 1.000000000000000222, 0.9999999999999997780, 1.000000000000000444, 0.9999999999999997780, 1.000000000000000222, 1.000000000000000000, 1.000000000000000000, 1.000000000000000000, 1.000000000000000222, 0.9999999999999994449, 1.000000000000000222, 1.000000000000000000, 1.000000000000000000, 1.000000000000000000, 0.9999999999999997780, 0.9999999999999997780, 1.000000000000000444, 0.9999999999999996669, 1.000000000000000222, 0.9999999999999997780, 1.000000000000000444, 0.9999999999999997780, 1.000000000000000222, 1.000000000000000222, 0.9999999999999996669, 1.000000000000000222, 1.000000000000000000, 1.000000000000000444, 1.000000000000000000, 1.000000000000000000, 1.000000000000000222, 1.000000000000000000, 1.000000000000000000, 0.9999999999999997780, 0.9999999999999997780, 1.000000000000000000, 0.9999999999999997780, 1.000000000000000222, 1.000000000000000222, 1.000000000000000000, 1.000000000000000222, 1.000000000000000222, 1.000000000000000000, 0.9999999999999997780, 0.9999999999999997780, 1.000000000000000222, 0.9999999999999997780, 1.000000000000000222, 1.000000000000000000, 1.000000000000000000, 1.000000000000000000, 0.9999999999999996669, 1.000000000000000222, 0.9999999999999997780, 1.000000000000000000, 0.9999999999999997780, 1.000000000000000222, 0.9999999999999997780, 1.000000000000000444, 0.9999999999999996669, 1.000000000000000222, 1.000000000000000222, 1.000000000000000000, 1.000000000000000000, 0.9999999999999997780, 1.000000000000000222, 0.9999999999999997780, 1.000000000000000222, 0.9999999999999997780, 0.9999999999999997780, 1.000000000000000000, 1.000000000000000000, 1.000000000000000222, 1.000000000000000000, 1.000000000000000444, 0.9999999999999997780, 1.000000000000000222, 0.9999999999999997780, 0.9999999999999997780, 1.000000000000000222, 1.000000000000000000, 0.9999999999999997780, 1.000000000000000000, 1.000000000000000000, 1.000000000000000000, 0.9999999999999997780, 1.000000000000000444, 0.9999999999999997780, 1.000000000000000000, 1.000000000000000000),
 ( 0.3333333333333334259, 0.3333333333333334259, 0.3333333333333333703, 0.3333333333333334259, 0.3333333333333334259, 0.3333333333333334259, 0.3333333333333334259, 0.3333333333333332593, 0.3333333333333335369, 0.3333333333333332593, 0.3333333333333333703, 0.3333333333333334259, 0.3333333333333333703, 0.3333333333333332593, 0.3333333333333334814, 0.3333333333333332593, 0.3333333333333334259, 0.3333333333333334259, 0.3333333333333332593, 0.3333333333333335369, 0.3333333333333332038, 0.3333333333333335369, 0.3333333333333331483, 0.3333333333333334814, 0.3333333333333333148, 0.3333333333333333703, 0.3333333333333333703, 0.3333333333333333148, 0.3333333333333333703, 0.3333333333333333148, 0.3333333333333333703, 0.3333333333333333703, 0.3333333333333333703, 0.3333333333333333703, 0.3333333333333333703, 0.3333333333333333703, 0.3333333333333333148, 0.3333333333333333148, 0.3333333333333334259, 0.3333333333333332593, 0.3333333333333334259, 0.3333333333333333148, 0.3333333333333334259, 0.3333333333333333703, 0.3333333333333333148, 0.3333333333333334259, 0.3333333333333333703, 0.3333333333333333703, 0.3333333333333334259, 0.3333333333333333148, 0.3333333333333333703, 0.3333333333333332593, 0.3333333333333335369, 0.3333333333333333703, 0.3333333333333333148, 0.3333333333333334259, 0.3333333333333333703, 0.3333333333333333703, 0.3333333333333333148, 0.3333333333333333703, 0.3333333333333333703, 0.3333333333333334259, 0.3333333333333334259, 0.3333333333333334259, 0.3333333333333333703, 0.3333333333333333703, 0.3333333333333334259, 0.3333333333333333148, 0.3333333333333333703, 0.3333333333333334259, 0.3333333333333334259, 0.3333333333333332593, 0.3333333333333333703, 0.3333333333333334259, 0.3333333333333333703, 0.3333333333333334259, 0.3333333333333333148, 0.3333333333333334814, 0.3333333333333333148, 0.3333333333333332593, 0.3333333333333334259, 0.3333333333333333703, 0.3333333333333333148, 0.3333333333333333703, 0.3333333333333334259, 0.3333333333333334259, 0.3333333333333333148, 0.3333333333333333703, 0.3333333333333332593, 0.3333333333333333703, 0.3333333333333333703, 0.3333333333333333703, 0.3333333333333333703, 0.3333333333333333148, 0.3333333333333333703, 0.3333333333333333148, 0.3333333333333334259, 0.3333333333333333703, 0.3333333333333334259, 0.3333333333333333148, 0.3333333333333333703, 0.3333333333333333148, 0.3333333333333334259, 0.3333333333333333703, 0.3333333333333333703, 0.3333333333333333703, 0.3333333333333333703, 0.3333333333333333703, 0.3333333333333332593, 0.3333333333333333703, 0.3333333333333333703, 0.3333333333333335369, 0.3333333333333334259, 0.3333333333333333148, 0.3333333333333335369, 0.3333333333333333148, 0.3333333333333333703, 0.3333333333333333703, 0.3333333333333334259, 0.3333333333333333148, 0.3333333333333333703, 0.3333333333333334259, 0.3333333333333334259, 0.3333333333333333703, 0.3333333333333332593, 0.3333333333333334259, 0.3333333333333333703, 0.3333333333333334814, 0.3333333333333333148, 0.3333333333333333703, 0.3333333333333334259, 0.3333333333333333703, 0.3333333333333333148, 0.3333333333333333703, 0.3333333333333333148, 0.3333333333333334259, 0.3333333333333332593, 0.3333333333333334814, 0.3333333333333333703, 0.3333333333333334259, 0.3333333333333333703, 0.3333333333333333703, 0.3333333333333334259, 0.3333333333333333703, 0.3333333333333333703, 0.3333333333333333148, 0.3333333333333335924, 0.3333333333333333148, 0.3333333333333333703, 0.3333333333333334259, 0.3333333333333333148, 0.3333333333333334259, 0.3333333333333333148, 0.3333333333333334259, 0.3333333333333333703, 0.3333333333333334259, 0.3333333333333333703, 0.3333333333333333703, 0.3333333333333333703, 0.3333333333333334259, 0.3333333333333333703, 0.3333333333333334814, 0.3333333333333333148, 0.3333333333333334814, 0.3333333333333333148, 0.3333333333333333703, 0.3333333333333333148, 0.3333333333333333703, 0.3333333333333333703, 0.3333333333333333703, 0.3333333333333333703, 0.3333333333333333703, 0.3333333333333334259, 0.3333333333333333148, 0.3333333333333334259, 0.3333333333333333703, 0.3333333333333333703, 0.3333333333333333703, 0.3333333333333333703, 0.3333333333333333148, 0.3333333333333333703, 0.3333333333333334259, 0.3333333333333333148, 0.3333333333333334259, 0.3333333333333333148, 0.3333333333333333703, 0.3333333333333333703, 0.3333333333333333148, 0.3333333333333333703, 0.3333333333333334259, 0.3333333333333333148, 0.3333333333333334259, 0.3333333333333333703, 0.3333333333333332593, 0.3333333333333334814, 0.3333333333333332593, 0.3333333333333334259, 0.3333333333333333148, 0.3333333333333333703, 0.3333333333333334814, 0.3333333333333333703, 0.3333333333333333703, 0.3333333333333332593, 0.3333333333333334814, 0.3333333333333333148, 0.3333333333333333703, 0.3333333333333334259, 0.3333333333333333148, 0.3333333333333334259, 0.3333333333333333148, 0.3333333333333333703, 0.3333333333333333703, 0.3333333333333332593, 0.3333333333333333703, 0.3333333333333333703, 0.3333333333333334259, 0.3333333333333333148, 0.3333333333333334814, 0.3333333333333333703, 0.3333333333333334259, 0.3333333333333333148, 0.3333333333333334259, 0.3333333333333333703, 0.3333333333333333703, 0.3333333333333333703, 0.3333333333333333703, 0.3333333333333333148, 0.3333333333333334814, 0.3333333333333333703, 0.3333333333333333703, 0.3333333333333333148, 0.3333333333333334259, 0.3333333333333333703, 0.3333333333333332593, 0.3333333333333333703, 0.3333333333333333703, 0.3333333333333333703, 0.3333333333333334259, 0.3333333333333334259, 0.3333333333333333703, 0.3333333333333333703, 0.3333333333333333703, 0.3333333333333333703, 0.3333333333333334259, 0.3333333333333332593, 0.3333333333333335369, 0.3333333333333332038, 0.3333333333333333148, 0.3333333333333333703, 0.3333333333333333148, 0.3333333333333333148, 0.3333333333333334259, 0.3333333333333333703, 0.3333333333333333703, 0.3333333333333333703, 0.3333333333333334259, 0.3333333333333333148, 0.3333333333333334814, 0.3333333333333333703, 0.3333333333333334259, 0.3333333333333333703, 0.3333333333333333703, 0.3333333333333332593, 0.3333333333333333148, 0.3333333333333334814, 0.3333333333333333148, 0.3333333333333332593, 0.3333333333333334259, 0.3333333333333332038, 0.3333333333333334259, 0.3333333333333333148, 0.3333333333333333148, 0.3333333333333334259, 0.3333333333333333703, 0.3333333333333333703, 0.3333333333333333703, 0.3333333333333333703, 0.3333333333333334259, 0.3333333333333333148, 0.3333333333333333148, 0.3333333333333334259, 0.3333333333333333148, 0.3333333333333334259, 0.3333333333333333148, 0.3333333333333333703, 0.3333333333333334259, 0.3333333333333333148, 0.3333333333333334814, 0.3333333333333333148, 0.3333333333333334259, 0.3333333333333334259, 0.3333333333333333148, 0.3333333333333333148, 0.3333333333333335369, 0.3333333333333333148, 0.3333333333333333148, 0.3333333333333333703, 0.3333333333333335369, 0.3333333333333332593, 0.3333333333333335369, 0.3333333333333333148, 0.3333333333333333148, 0.3333333333333334259, 0.3333333333333333148, 0.3333333333333334259, 0.3333333333333333703, 0.3333333333333332593, 0.3333333333333333703, 0.3333333333333333148, 0.3333333333333334259, 0.3333333333333333148, 0.3333333333333334259, 0.3333333333333332593, 0.3333333333333335369, 0.3333333333333332038, 0.3333333333333334259, 0.3333333333333332593, 0.3333333333333335369, 0.3333333333333333148, 0.3333333333333334259, 0.3333333333333334259, 0.3333333333333333148, 0.3333333333333333148, 0.3333333333333334259, 0.3333333333333334814, 0.3333333333333333148, 0.3333333333333333148, 0.3333333333333334259, 0.3333333333333333703, 0.3333333333333334259, 0.3333333333333333148, 0.3333333333333333148, 0.3333333333333333703, 0.3333333333333333703, 0.3333333333333334814, 0.3333333333333333148, 0.3333333333333334259, 0.3333333333333333703, 0.3333333333333334259, 0.3333333333333334259, 0.3333333333333333148, 0.3333333333333333703, 0.3333333333333334259, 0.3333333333333333148, 0.3333333333333334814, 0.3333333333333333703, 0.3333333333333333148, 0.3333333333333333703, 0.3333333333333333148, 0.3333333333333334259, 0.3333333333333333148, 0.3333333333333333703, 0.3333333333333332593, 0.3333333333333334814, 0.3333333333333333703, 0.3333333333333334814, 0.3333333333333333148, 0.3333333333333334259, 0.3333333333333334814, 0.3333333333333333148, 0.3333333333333334259, 0.3333333333333332593, 0.3333333333333334259, 0.3333333333333333703, 0.3333333333333333703, 0.3333333333333333148, 0.3333333333333333148, 0.3333333333333334259, 0.3333333333333333148, 0.3333333333333334814, 0.3333333333333333148, 0.3333333333333335924, 0.3333333333333333148, 0.3333333333333334259, 0.3333333333333333148, 0.3333333333333333703, 0.3333333333333333703, 0.3333333333333334814, 0.3333333333333332593, 0.3333333333333333703, 0.3333333333333333703, 0.3333333333333334259, 0.3333333333333333148, 0.3333333333333334259, 0.3333333333333333703, 0.3333333333333333703, 0.3333333333333333703),
 ( 0.3333333333333334259, 0.3333333333333334259, 0.3333333333333333703, 0.3333333333333334259, 0.3333333333333334259, 0.3333333333333334259, 0.3333333333333334259, 0.3333333333333332593, 0.3333333333333335369, 0.3333333333333332593, 0.3333333333333333703, 0.3333333333333334259, 0.3333333333333333703, 0.3333333333333332593, 0.3333333333333334814, 0.3333333333333332593, 0.3333333333333334259, 0.3333333333333334259, 0.3333333333333332593, 0.3333333333333335369, 0.3333333333333332038, 0.3333333333333335369, 0.3333333333333331483, 0.3333333333333334814, 0.3333333333333333148, 0.3333333333333333703, 0.3333333333333333703, 0.3333333333333333148, 0.3333333333333333703, 0.3333333333333333148, 0.3333333333333333703, 0.3333333333333333703, 0.3333333333333333703, 0.3333333333333333703, 0.3333333333333333703, 0.3333333333333333703, 0.3333333333333333148, 0.3333333333333333148, 0.3333333333333334259, 0.3333333333333332593, 0.3333333333333334259, 0.3333333333333333148, 0.3333333333333334259, 0.3333333333333333703, 0.3333333333333333148, 0.3333333333333334259, 0.3333333333333333703, 0.3333333333333333703, 0.3333333333333334259, 0.3333333333333333148, 0.3333333333333333703, 0.3333333333333332593, 0.3333333333333335369, 0.3333333333333333703, 0.3333333333333333148, 0.3333333333333334259, 0.3333333333333333703, 0.3333333333333333703, 0.3333333333333333148, 0.3333333333333333703, 0.3333333333333333703, 0.3333333333333334259, 0.3333333333333334259, 0.3333333333333334259, 0.3333333333333333703, 0.3333333333333333703, 0.3333333333333334259, 0.3333333333333333148, 0.3333333333333333703, 0.3333333333333334259, 0.3333333333333334259, 0.3333333333333332593, 0.3333333333333333703, 0.3333333333333334259, 0.3333333333333333703, 0.3333333333333334259, 0.3333333333333333148, 0.3333333333333334814, 0.3333333333333333148, 0.3333333333333332593, 0.3333333333333334259, 0.3333333333333333703, 0.3333333333333333148, 0.3333333333333333703, 0.3333333333333334259, 0.3333333333333334259, 0.3333333333333333148, 0.3333333333333333703, 0.3333333333333332593, 0.3333333333333333703, 0.3333333333333333703, 0.3333333333333333703, 0.3333333333333333703, 0.3333333333333333148, 0.3333333333333333703, 0.3333333333333333148, 0.3333333333333334259, 0.3333333333333333703, 0.3333333333333334259, 0.3333333333333333148, 0.3333333333333333703, 0.3333333333333333148, 0.3333333333333334259, 0.3333333333333333703, 0.3333333333333333703, 0.3333333333333333703, 0.3333333333333333703, 0.3333333333333333703, 0.3333333333333332593, 0.3333333333333333703, 0.3333333333333333703, 0.3333333333333335369, 0.3333333333333334259, 0.3333333333333333148, 0.3333333333333335369, 0.3333333333333333148, 0.3333333333333333703, 0.3333333333333333703, 0.3333333333333334259, 0.3333333333333333148, 0.3333333333333333703, 0.3333333333333334259, 0.3333333333333334259, 0.3333333333333333703, 0.3333333333333332593, 0.3333333333333334259, 0.3333333333333333703, 0.3333333333333334814, 0.3333333333333333148, 0.3333333333333333703, 0.3333333333333334259, 0.3333333333333333703, 0.3333333333333333148, 0.3333333333333333703, 0.3333333333333333148, 0.3333333333333334259, 0.3333333333333332593, 0.3333333333333334814, 0.3333333333333333703, 0.3333333333333334259, 0.3333333333333333703, 0.3333333333333333703, 0.3333333333333334259, 0.3333333333333333703, 0.3333333333333333703, 0.3333333333333333148, 0.3333333333333335924, 0.3333333333333333148, 0.3333333333333333703, 0.3333333333333334259, 0.3333333333333333148, 0.3333333333333334259, 0.3333333333333333148, 0.3333333333333334259, 0.3333333333333333703, 0.3333333333333334259, 0.3333333333333333703, 0.3333333333333333703, 0.3333333333333333703, 0.3333333333333334259, 0.3333333333333333703, 0.3333333333333334814, 0.3333333333333333148, 0.3333333333333334814, 0.3333333333333333148, 0.3333333333333333703, 0.3333333333333333148, 0.3333333333333333703, 0.3333333333333333703, 0.3333333333333333703, 0.3333333333333333703, 0.3333333333333333703, 0.3333333333333334259, 0.3333333333333333148, 0.3333333333333334259, 0.3333333333333333703, 0.3333333333333333703, 0.3333333333333333703, 0.3333333333333333703, 0.3333333333333333148, 0.3333333333333333703, 0.3333333333333334259, 0.3333333333333333148, 0.3333333333333334259, 0.3333333333333333148, 0.3333333333333333703, 0.3333333333333333703, 0.3333333333333333148, 0.3333333333333333703, 0.3333333333333334259, 0.3333333333333333148, 0.3333333333333334259, 0.3333333333333333703, 0.3333333333333332593, 0.3333333333333334814, 0.3333333333333332593, 0.3333333333333334259, 0.3333333333333333148, 0.3333333333333333703, 0.3333333333333334814, 0.3333333333333333703, 0.3333333333333333703, 0.3333333333333332593, 0.3333333333333334814, 0.3333333333333333148, 0.3333333333333333703, 0.3333333333333334259, 0.3333333333333333148, 0.3333333333333334259, 0.3333333333333333148, 0.3333333333333333703, 0.3333333333333333703, 0.3333333333333332593, 0.3333333333333333703, 0.3333333333333333703, 0.3333333333333334259, 0.3333333333333333148, 0.3333333333333334814, 0.3333333333333333703, 0.3333333333333334259, 0.3333333333333333148, 0.3333333333333334259, 0.3333333333333333703, 0.3333333333333333703, 0.3333333333333333703, 0.3333333333333333703, 0.3333333333333333148, 0.3333333333333334814, 0.3333333333333333703, 0.3333333333333333703, 0.3333333333333333148, 0.3333333333333334259, 0.3333333333333333703, 0.3333333333333332593, 0.3333333333333333703, 0.3333333333333333703, 0.3333333333333333703, 0.3333333333333334259, 0.3333333333333334259, 0.3333333333333333703, 0.3333333333333333703, 0.3333333333333333703, 0.3333333333333333703, 0.3333333333333334259, 0.3333333333333332593, 0.3333333333333335369, 0.3333333333333332038, 0.3333333333333333148, 0.3333333333333333703, 0.3333333333333333148, 0.3333333333333333148, 0.3333333333333334259, 0.3333333333333333703, 0.3333333333333333703, 0.3333333333333333703, 0.3333333333333334259, 0.3333333333333333148, 0.3333333333333334814, 0.3333333333333333703, 0.3333333333333334259, 0.3333333333333333703, 0.3333333333333333703, 0.3333333333333332593, 0.3333333333333333148, 0.3333333333333334814, 0.3333333333333333148, 0.3333333333333332593, 0.3333333333333334259, 0.3333333333333332038, 0.3333333333333334259, 0.3333333333333333148, 0.3333333333333333148, 0.3333333333333334259, 0.3333333333333333703, 0.3333333333333333703, 0.3333333333333333703, 0.3333333333333333703, 0.3333333333333334259, 0.3333333333333333148, 0.3333333333333333148, 0.3333333333333334259, 0.3333333333333333148, 0.3333333333333334259, 0.3333333333333333148, 0.3333333333333333703, 0.3333333333333334259, 0.3333333333333333148, 0.3333333333333334814, 0.3333333333333333148, 0.3333333333333334259, 0.3333333333333334259, 0.3333333333333333148, 0.3333333333333333148, 0.3333333333333335369, 0.3333333333333333148, 0.3333333333333333148, 0.3333333333333333703, 0.3333333333333335369, 0.3333333333333332593, 0.3333333333333335369, 0.3333333333333333148, 0.3333333333333333148, 0.3333333333333334259, 0.3333333333333333148, 0.3333333333333334259, 0.3333333333333333703, 0.3333333333333332593, 0.3333333333333333703, 0.3333333333333333148, 0.3333333333333334259, 0.3333333333333333148, 0.3333333333333334259, 0.3333333333333332593, 0.3333333333333335369, 0.3333333333333332038, 0.3333333333333334259, 0.3333333333333332593, 0.3333333333333335369, 0.3333333333333333148, 0.3333333333333334259, 0.3333333333333334259, 0.3333333333333333148, 0.3333333333333333148, 0.3333333333333334259, 0.3333333333333334814, 0.3333333333333333148, 0.3333333333333333148, 0.3333333333333334259, 0.3333333333333333703, 0.3333333333333334259, 0.3333333333333333148, 0.3333333333333333148, 0.3333333333333333703, 0.3333333333333333703, 0.3333333333333334814, 0.3333333333333333148, 0.3333333333333334259, 0.3333333333333333703, 0.3333333333333334259, 0.3333333333333334259, 0.3333333333333333148, 0.3333333333333333703, 0.3333333333333334259, 0.3333333333333333148, 0.3333333333333334814, 0.3333333333333333703, 0.3333333333333333148, 0.3333333333333333703, 0.3333333333333333148, 0.3333333333333334259, 0.3333333333333333148, 0.3333333333333333703, 0.3333333333333332593, 0.3333333333333334814, 0.3333333333333333703, 0.3333333333333334814, 0.3333333333333333148, 0.3333333333333334259, 0.3333333333333334814, 0.3333333333333333148, 0.3333333333333334259, 0.3333333333333332593, 0.3333333333333334259, 0.3333333333333333703, 0.3333333333333333703, 0.3333333333333333148, 0.3333333333333333148, 0.3333333333333334259, 0.3333333333333333148, 0.3333333333333334814, 0.3333333333333333148, 0.3333333333333335924, 0.3333333333333333148, 0.3333333333333334259, 0.3333333333333333148, 0.3333333333333333703, 0.3333333333333333703, 0.3333333333333334814, 0.3333333333333332593, 0.3333333333333333703, 0.3333333333333333703, 0.3333333333333334259, 0.3333333333333333148, 0.3333333333333334259, 0.3333333333333333703, 0.3333333333333333703, 0.3333333333333333703),
 ( 1.000000000000000222, 1.000000000000000222, 1.000000000000000222, 1.000000000000000000, 1.000000000000000000, 1.000000000000000444, 1.000000000000000000, 0.9999999999999997780, 1.000000000000000444, 0.9999999999999997780, 0.9999999999999997780, 1.000000000000000222, 0.9999999999999997780, 0.9999999999999997780, 1.000000000000000444, 0.9999999999999997780, 1.000000000000000222, 1.000000000000000222, 0.9999999999999996669, 1.000000000000000222, 0.9999999999999996669, 1.000000000000000444, 0.9999999999999994449, 1.000000000000000444, 0.9999999999999996669, 1.000000000000000222, 1.000000000000000000, 0.9999999999999997780, 1.000000000000000222, 0.9999999999999997780, 1.000000000000000000, 0.9999999999999997780, 1.000000000000000000, 1.000000000000000222, 0.9999999999999996669, 1.000000000000000000, 0.9999999999999997780, 1.000000000000000000, 1.000000000000000444, 0.9999999999999996669, 1.000000000000000222, 1.000000000000000000, 1.000000000000000222, 1.000000000000000222, 0.9999999999999997780, 0.9999999999999997780, 1.000000000000000222, 0.9999999999999997780, 1.000000000000000222, 0.9999999999999997780, 0.9999999999999997780, 0.9999999999999997780, 1.000000000000000444, 1.000000000000000000, 0.9999999999999997780, 1.000000000000000222, 1.000000000000000000, 1.000000000000000000, 0.9999999999999997780, 1.000000000000000222, 1.000000000000000000, 1.000000000000000000, 1.000000000000000222, 1.000000000000000000, 1.000000000000000000, 1.000000000000000000, 1.000000000000000222, 1.000000000000000000, 0.9999999999999997780, 1.000000000000000444, 1.000000000000000000, 0.9999999999999997780, 1.000000000000000000, 1.000000000000000222, 0.9999999999999997780, 1.000000000000000222, 0.9999999999999996669, 1.000000000000000222, 1.000000000000000000, 1.000000000000000000, 1.000000000000000000, 1.000000000000000222, 0.9999999999999997780, 1.000000000000000000, 1.000000000000000222, 0.9999999999999997780, 1.000000000000000000, 1.000000000000000000, 0.9999999999999996669, 1.000000000000000000, 1.000000000000000000, 1.000000000000000222, 1.000000000000000000, 0.9999999999999997780, 1.000000000000000222, 0.9999999999999996669, 1.000000000000000222, 0.9999999999999997780, 1.000000000000000000, 1.000000000000000000, 1.000000000000000222, 0.9999999999999996669, 1.000000000000000444, 1.000000000000000000, 0.9999999999999997780, 1.000000000000000000, 1.000000000000000000, 1.000000000000000222, 0.9999999999999997780, 1.000000000000000000, 1.000000000000000222, 1.000000000000000444, 1.000000000000000000, 1.000000000000000000, 1.000000000000000444, 1.000000000000000000, 0.9999999999999997780, 1.000000000000000222, 1.000000000000000000, 1.000000000000000000, 1.000000000000000000, 1.000000000000000000, 1.000000000000000000, 1.000000000000000000, 0.9999999999999996669, 1.000000000000000222, 0.9999999999999997780, 1.000000000000000222, 1.000000000000000000, 0.9999999999999997780, 1.000000000000000222, 0.9999999999999997780, 0.9999999999999997780, 0.9999999999999997780, 1.000000000000000000, 1.000000000000000000, 0.9999999999999996669, 1.000000000000000444, 1.000000000000000222, 1.000000000000000000, 1.000000000000000000, 1.000000000000000222, 1.000000000000000222, 1.000000000000000000, 1.000000000000000222, 0.9999999999999996669, 1.000000000000000444, 0.9999999999999997780, 0.9999999999999997780, 1.000000000000000444, 1.000000000000000000, 1.000000000000000222, 0.9999999999999997780, 1.000000000000000222, 1.000000000000000000, 1.000000000000000222, 1.000000000000000000, 1.000000000000000000, 0.9999999999999996669, 1.000000000000000444, 1.000000000000000000, 1.000000000000000222, 0.9999999999999997780, 1.000000000000000000, 1.000000000000000000, 1.000000000000000000, 1.000000000000000000, 0.9999999999999997780, 1.000000000000000000, 1.000000000000000000, 1.000000000000000000, 1.000000000000000222, 1.000000000000000222, 0.9999999999999997780, 1.000000000000000000, 1.000000000000000000, 0.9999999999999997780, 1.000000000000000000, 1.000000000000000000, 1.000000000000000000, 1.000000000000000000, 1.000000000000000444, 0.9999999999999997780, 1.000000000000000222, 0.9999999999999997780, 1.000000000000000000, 1.000000000000000222, 0.9999999999999997780, 1.000000000000000222, 1.000000000000000000, 1.000000000000000000, 1.000000000000000000, 1.000000000000000000, 0.9999999999999997780, 1.000000000000000000, 1.000000000000000000, 1.000000000000000000, 1.000000000000000000, 1.000000000000000000, 1.000000000000000222, 1.000000000000000000, 1.000000000000000222, 0.9999999999999997780, 1.000000000000000222, 0.9999999999999997780, 1.000000000000000222, 1.000000000000000000, 0.9999999999999997780, 1.000000000000000222, 0.9999999999999996669, 1.000000000000000444, 1.000000000000000000, 0.9999999999999996669, 1.000000000000000222, 1.000000000000000000, 1.000000000000000222, 0.9999999999999997780, 1.000000000000000444, 1.000000000000000000, 1.000000000000000000, 0.9999999999999997780, 1.000000000000000222, 1.000000000000000000, 1.000000000000000000, 1.000000000000000000, 1.000000000000000222, 0.9999999999999997780, 1.000000000000000222, 1.000000000000000000, 0.9999999999999997780, 1.000000000000000000, 0.9999999999999997780, 1.000000000000000222, 0.9999999999999996669, 1.000000000000000000, 1.000000000000000000, 1.000000000000000000, 1.000000000000000444, 1.000000000000000222, 1.000000000000000000, 1.000000000000000000, 0.9999999999999997780, 0.9999999999999997780, 1.000000000000000444, 0.9999999999999996669, 1.000000000000000444, 0.9999999999999997780, 0.9999999999999997780, 1.000000000000000222, 0.9999999999999997780, 0.9999999999999996669, 1.000000000000000444, 0.9999999999999997780, 1.000000000000000222, 1.000000000000000222, 1.000000000000000000, 0.9999999999999997780, 1.000000000000000222, 1.000000000000000000, 1.000000000000000222, 1.000000000000000000, 1.000000000000000000, 0.9999999999999997780, 0.9999999999999997780, 1.000000000000000444, 0.9999999999999997780, 0.9999999999999997780, 1.000000000000000222, 0.9999999999999994449, 1.000000000000000222, 0.9999999999999997780, 1.000000000000000000, 0.9999999999999997780, 1.000000000000000000, 1.000000000000000000, 1.000000000000000000, 1.000000000000000000, 1.000000000000000000, 1.000000000000000000, 1.000000000000000000, 1.000000000000000222, 1.000000000000000000, 1.000000000000000000, 1.000000000000000000, 1.000000000000000000, 1.000000000000000000, 1.000000000000000000, 1.000000000000000000, 1.000000000000000222, 1.000000000000000000, 1.000000000000000222, 0.9999999999999997780, 1.000000000000000000, 1.000000000000000444, 1.000000000000000000, 1.000000000000000000, 1.000000000000000000, 1.000000000000000222, 0.9999999999999997780, 1.000000000000000444, 0.9999999999999997780, 1.000000000000000222, 1.000000000000000000, 1.000000000000000000, 1.000000000000000000, 1.000000000000000222, 0.9999999999999994449, 1.000000000000000222, 1.000000000000000000, 1.000000000000000000, 1.000000000000000000, 0.9999999999999997780, 0.9999999999999997780, 1.000000000000000444, 0.9999999999999996669, 1.000000000000000222, 0.9999999999999997780, 1.000000000000000444, 0.9999999999999997780, 1.000000000000000222, 1.000000000000000222, 0.9999999999999996669, 1.000000000000000222, 1.000000000000000000, 1.000000000000000444, 1.000000000000000000, 1.000000000000000000, 1.000000000000000222, 1.000000000000000000, 1.000000000000000000, 0.9999999999999997780, 0.9999999999999997780, 1.000000000000000000, 0.9999999999999997780, 1.000000000000000222, 1.000000000000000222, 1.000000000000000000, 1.000000000000000222, 1.000000000000000222, 1.000000000000000000, 0.9999999999999997780, 0.9999999999999997780, 1.000000000000000222, 0.9999999999999997780, 1.000000000000000222, 1.000000000000000000, 1.000000000000000000, 1.000000000000000000, 0.9999999999999996669, 1.000000000000000222, 0.9999999999999997780, 1.000000000000000000, 0.9999999999999997780, 1.000000000000000222, 0.9999999999999997780, 1.000000000000000444, 0.9999999999999996669, 1.000000000000000222, 1.000000000000000222, 1.000000000000000000, 1.000000000000000000, 0.9999999999999997780, 1.000000000000000222, 0.9999999999999997780, 1.000000000000000222, 0.9999999999999997780, 0.9999999999999997780, 1.000000000000000000, 1.000000000000000000, 1.000000000000000222, 1.000000000000000000, 1.000000000000000444, 0.9999999999999997780, 1.000000000000000222, 0.9999999999999997780, 0.9999999999999997780, 1.000000000000000222, 1.000000000000000000, 0.9999999999999997780, 1.000000000000000000, 1.000000000000000000, 1.000000000000000000, 0.9999999999999997780, 1.000000000000000444, 0.9999999999999997780, 1.000000000000000000, 1.000000000000000000),
 ( 0.3333333333333334259, 0.3333333333333334259, 0.3333333333333333703, 0.3333333333333334259, 0.3333333333333334259, 0.3333333333333334259, 0.3333333333333334259, 0.3333333333333332593, 0.3333333333333335369, 0.3333333333333332593, 0.3333333333333333703, 0.3333333333333334259, 0.3333333333333333703, 0.3333333333333332593, 0.3333333333333334814, 0.3333333333333332593, 0.3333333333333334259, 0.3333333333333334259, 0.3333333333333332593, 0.3333333333333335369, 0.3333333333333332038, 0.3333333333333335369, 0.3333333333333331483, 0.3333333333333334814, 0.3333333333333333148, 0.3333333333333333703, 0.3333333333333333703, 0.3333333333333333148, 0.3333333333333333703, 0.3333333333333333148, 0.3333333333333333703, 0.3333333333333333703, 0.3333333333333333703, 0.3333333333333333703, 0.3333333333333333703, 0.3333333333333333703, 0.3333333333333333148, 0.3333333333333333148, 0.3333333333333334259, 0.3333333333333332593, 0.3333333333333334259, 0.3333333333333333148, 0.3333333333333334259, 0.3333333333333333703, 0.3333333333333333148, 0.3333333333333334259, 0.3333333333333333703, 0.3333333333333333703, 0.3333333333333334259, 0.3333333333333333148, 0.3333333333333333703, 0.3333333333333332593, 0.3333333333333335369, 0.3333333333333333703, 0.3333333333333333148, 0.3333333333333334259, 0.3333333333333333703, 0.3333333333333333703, 0.3333333333333333148, 0.3333333333333333703, 0.3333333333333333703, 0.3333333333333334259, 0.3333333333333334259, 0.3333333333333334259, 0.3333333333333333703, 0.3333333333333333703, 0.3333333333333334259, 0.3333333333333333148, 0.3333333333333333703, 0.3333333333333334259, 0.3333333333333334259, 0.3333333333333332593, 0.3333333333333333703, 0.3333333333333334259, 0.3333333333333333703, 0.3333333333333334259, 0.3333333333333333148, 0.3333333333333334814, 0.3333333333333333148, 0.3333333333333332593, 0.3333333333333334259, 0.3333333333333333703, 0.3333333333333333148, 0.3333333333333333703, 0.3333333333333334259, 0.3333333333333334259, 0.3333333333333333148, 0.3333333333333333703, 0.3333333333333332593, 0.3333333333333333703, 0.3333333333333333703, 0.3333333333333333703, 0.3333333333333333703, 0.3333333333333333148, 0.3333333333333333703, 0.3333333333333333148, 0.3333333333333334259, 0.3333333333333333703, 0.3333333333333334259, 0.3333333333333333148, 0.3333333333333333703, 0.3333333333333333148, 0.3333333333333334259, 0.3333333333333333703, 0.3333333333333333703, 0.3333333333333333703, 0.3333333333333333703, 0.3333333333333333703, 0.3333333333333332593, 0.3333333333333333703, 0.3333333333333333703, 0.3333333333333335369, 0.3333333333333334259, 0.3333333333333333148, 0.3333333333333335369, 0.3333333333333333148, 0.3333333333333333703, 0.3333333333333333703, 0.3333333333333334259, 0.3333333333333333148, 0.3333333333333333703, 0.3333333333333334259, 0.3333333333333334259, 0.3333333333333333703, 0.3333333333333332593, 0.3333333333333334259, 0.3333333333333333703, 0.3333333333333334814, 0.3333333333333333148, 0.3333333333333333703, 0.3333333333333334259, 0.3333333333333333703, 0.3333333333333333148, 0.3333333333333333703, 0.3333333333333333148, 0.3333333333333334259, 0.3333333333333332593, 0.3333333333333334814, 0.3333333333333333703, 0.3333333333333334259, 0.3333333333333333703, 0.3333333333333333703, 0.3333333333333334259, 0.3333333333333333703, 0.3333333333333333703, 0.3333333333333333148, 0.3333333333333335924, 0.3333333333333333148, 0.3333333333333333703, 0.3333333333333334259, 0.3333333333333333148, 0.3333333333333334259, 0.3333333333333333148, 0.3333333333333334259, 0.3333333333333333703, 0.3333333333333334259, 0.3333333333333333703, 0.3333333333333333703, 0.3333333333333333703, 0.3333333333333334259, 0.3333333333333333703, 0.3333333333333334814, 0.3333333333333333148, 0.3333333333333334814, 0.3333333333333333148, 0.3333333333333333703, 0.3333333333333333148, 0.3333333333333333703, 0.3333333333333333703, 0.3333333333333333703, 0.3333333333333333703, 0.3333333333333333703, 0.3333333333333334259, 0.3333333333333333148, 0.3333333333333334259, 0.3333333333333333703, 0.3333333333333333703, 0.3333333333333333703, 0.3333333333333333703, 0.3333333333333333148, 0.3333333333333333703, 0.3333333333333334259, 0.3333333333333333148, 0.3333333333333334259, 0.3333333333333333148, 0.3333333333333333703, 0.3333333333333333703, 0.3333333333333333148, 0.3333333333333333703, 0.3333333333333334259, 0.3333333333333333148, 0.3333333333333334259, 0.3333333333333333703, 0.3333333333333332593, 0.3333333333333334814, 0.3333333333333332593, 0.3333333333333334259, 0.3333333333333333148, 0.3333333333333333703, 0.3333333333333334814, 0.3333333333333333703, 0.3333333333333333703, 0.3333333333333332593, 0.3333333333333334814, 0.3333333333333333148, 0.3333333333333333703, 0.3333333333333334259, 0.3333333333333333148, 0.3333333333333334259, 0.3333333333333333148, 0.3333333333333333703, 0.3333333333333333703, 0.3333333333333332593, 0.3333333333333333703, 0.3333333333333333703, 0.3333333333333334259, 0.3333333333333333148, 0.3333333333333334814, 0.3333333333333333703, 0.3333333333333334259, 0.3333333333333333148, 0.3333333333333334259, 0.3333333333333333703, 0.3333333333333333703, 0.3333333333333333703, 0.3333333333333333703, 0.3333333333333333148, 0.3333333333333334814, 0.3333333333333333703, 0.3333333333333333703, 0.3333333333333333148, 0.3333333333333334259, 0.3333333333333333703, 0.3333333333333332593, 0.3333333333333333703, 0.3333333333333333703, 0.3333333333333333703, 0.3333333333333334259, 0.3333333333333334259, 0.3333333333333333703, 0.3333333333333333703, 0.3333333333333333703, 0.3333333333333333703, 0.3333333333333334259, 0.3333333333333332593, 0.3333333333333335369, 0.3333333333333332038, 0.3333333333333333148, 0.3333333333333333703, 0.3333333333333333148, 0.3333333333333333148, 0.3333333333333334259, 0.3333333333333333703, 0.3333333333333333703, 0.3333333333333333703, 0.3333333333333334259, 0.3333333333333333148, 0.3333333333333334814, 0.3333333333333333703, 0.3333333333333334259, 0.3333333333333333703, 0.3333333333333333703, 0.3333333333333332593, 0.3333333333333333148, 0.3333333333333334814, 0.3333333333333333148, 0.3333333333333332593, 0.3333333333333334259, 0.3333333333333332038, 0.3333333333333334259, 0.3333333333333333148, 0.3333333333333333148, 0.3333333333333334259, 0.3333333333333333703, 0.3333333333333333703, 0.3333333333333333703, 0.3333333333333333703, 0.3333333333333334259, 0.3333333333333333148, 0.3333333333333333148, 0.3333333333333334259, 0.3333333333333333148, 0.3333333333333334259, 0.3333333333333333148, 0.3333333333333333703, 0.3333333333333334259, 0.3333333333333333148, 0.3333333333333334814, 0.3333333333333333148, 0.3333333333333334259, 0.3333333333333334259, 0.3333333333333333148, 0.3333333333333333148, 0.3333333333333335369, 0.3333333333333333148, 0.3333333333333333148, 0.3333333333333333703, 0.3333333333333335369, 0.3333333333333332593, 0.3333333333333335369, 0.3333333333333333148, 0.3333333333333333148, 0.3333333333333334259, 0.3333333333333333148, 0.3333333333333334259, 0.3333333333333333703, 0.3333333333333332593, 0.3333333333333333703, 0.3333333333333333148, 0.3333333333333334259, 0.3333333333333333148, 0.3333333333333334259, 0.3333333333333332593, 0.3333333333333335369, 0.3333333333333332038, 0.3333333333333334259, 0.3333333333333332593, 0.3333333333333335369, 0.3333333333333333148, 0.3333333333333334259, 0.3333333333333334259, 0.3333333333333333148, 0.3333333333333333148, 0.3333333333333334259, 0.3333333333333334814, 0.3333333333333333148, 0.3333333333333333148, 0.3333333333333334259, 0.3333333333333333703, 0.3333333333333334259, 0.3333333333333333148, 0.3333333333333333148, 0.3333333333333333703, 0.3333333333333333703, 0.3333333333333334814, 0.3333333333333333148, 0.3333333333333334259, 0.3333333333333333703, 0.3333333333333334259, 0.3333333333333334259, 0.3333333333333333148, 0.3333333333333333703, 0.3333333333333334259, 0.3333333333333333148, 0.3333333333333334814, 0.3333333333333333703, 0.3333333333333333148, 0.3333333333333333703, 0.3333333333333333148, 0.3333333333333334259, 0.3333333333333333148, 0.3333333333333333703, 0.3333333333333332593, 0.3333333333333334814, 0.3333333333333333703, 0.3333333333333334814, 0.3333333333333333148, 0.3333333333333334259, 0.3333333333333334814, 0.3333333333333333148, 0.3333333333333334259, 0.3333333333333332593, 0.3333333333333334259, 0.3333333333333333703, 0.3333333333333333703, 0.3333333333333333148, 0.3333333333333333148, 0.3333333333333334259, 0.3333333333333333148, 0.3333333333333334814, 0.3333333333333333148, 0.3333333333333335924, 0.3333333333333333148, 0.3333333333333334259, 0.3333333333333333148, 0.3333333333333333703, 0.3333333333333333703, 0.3333333333333334814, 0.3333333333333332593, 0.3333333333333333703, 0.3333333333333333703, 0.3333333333333334259, 0.3333333333333333148, 0.3333333333333334259, 0.3333333333333333703, 0.3333333333333333703, 0.3333333333333333703),
 ( 0.3333333333333334259, 0.3333333333333334259, 0.3333333333333333703, 0.3333333333333334259, 0.3333333333333334259, 0.3333333333333334259, 0.3333333333333334259, 0.3333333333333332593, 0.3333333333333335369, 0.3333333333333332593, 0.3333333333333333703, 0.3333333333333334259, 0.3333333333333333703, 0.3333333333333332593, 0.3333333333333334814, 0.3333333333333332593, 0.3333333333333334259, 0.3333333333333334259, 0.3333333333333332593, 0.3333333333333335369, 0.3333333333333332038, 0.3333333333333335369, 0.3333333333333331483, 0.3333333333333334814, 0.3333333333333333148, 0.3333333333333333703, 0.3333333333333333703, 0.3333333333333333148, 0.3333333333333333703, 0.3333333333333333148, 0.3333333333333333703, 0.3333333333333333703, 0.3333333333333333703, 0.3333333333333333703, 0.3333333333333333703, 0.3333333333333333703, 0.3333333333333333148, 0.3333333333333333148, 0.3333333333333334259, 0.3333333333333332593, 0.3333333333333334259, 0.3333333333333333148, 0.3333333333333334259, 0.3333333333333333703, 0.3333333333333333148, 0.3333333333333334259, 0.3333333333333333703, 0.3333333333333333703, 0.3333333333333334259, 0.3333333333333333148, 0.3333333333333333703, 0.3333333333333332593, 0.3333333333333335369, 0.3333333333333333703, 0.3333333333333333148, 0.3333333333333334259, 0.3333333333333333703, 0.3333333333333333703, 0.3333333333333333148, 0.3333333333333333703, 0.3333333333333333703, 0.3333333333333334259, 0.3333333333333334259, 0.3333333333333334259, 0.3333333333333333703, 0.3333333333333333703, 0.3333333333333334259, 0.3333333333333333148, 0.3333333333333333703, 0.3333333333333334259, 0.3333333333333334259, 0.3333333333333332593, 0.3333333333333333703, 0.3333333333333334259, 0.3333333333333333703, 0.3333333333333334259, 0.3333333333333333148, 0.3333333333333334814, 0.3333333333333333148, 0.3333333333333332593, 0.3333333333333334259, 0.3333333333333333703, 0.3333333333333333148, 0.3333333333333333703, 0.3333333333333334259, 0.3333333333333334259, 0.3333333333333333148, 0.3333333333333333703, 0.3333333333333332593, 0.3333333333333333703, 0.3333333333333333703, 0.3333333333333333703, 0.3333333333333333703, 0.3333333333333333148, 0.3333333333333333703, 0.3333333333333333148, 0.3333333333333334259, 0.3333333333333333703, 0.3333333333333334259, 0.3333333333333333148, 0.3333333333333333703, 0.3333333333333333148, 0.3333333333333334259, 0.3333333333333333703, 0.3333333333333333703, 0.3333333333333333703, 0.3333333333333333703, 0.3333333333333333703, 0.3333333333333332593, 0.3333333333333333703, 0.3333333333333333703, 0.3333333333333335369, 0.3333333333333334259, 0.3333333333333333148, 0.3333333333333335369, 0.3333333333333333148, 0.3333333333333333703, 0.3333333333333333703, 0.3333333333333334259, 0.3333333333333333148, 0.3333333333333333703, 0.3333333333333334259, 0.3333333333333334259, 0.3333333333333333703, 0.3333333333333332593, 0.3333333333333334259, 0.3333333333333333703, 0.3333333333333334814, 0.3333333333333333148, 0.3333333333333333703, 0.3333333333333334259, 0.3333333333333333703, 0.3333333333333333148, 0.3333333333333333703, 0.3333333333333333148, 0.3333333333333334259, 0.3333333333333332593, 0.3333333333333334814, 0.3333333333333333703, 0.3333333333333334259, 0.3333333333333333703, 0.3333333333333333703, 0.3333333333333334259, 0.3333333333333333703, 0.3333333333333333703, 0.3333333333333333148, 0.3333333333333335924, 0.3333333333333333148, 0.3333333333333333703, 0.3333333333333334259, 0.3333333333333333148, 0.3333333333333334259, 0.3333333333333333148, 0.3333333333333334259, 0.3333333333333333703, 0.3333333333333334259, 0.3333333333333333703, 0.3333333333333333703, 0.3333333333333333703, 0.3333333333333334259, 0.3333333333333333703, 0.3333333333333334814, 0.3333333333333333148, 0.3333333333333334814, 0.3333333333333333148, 0.3333333333333333703, 0.3333333333333333148, 0.3333333333333333703, 0.3333333333333333703, 0.3333333333333333703, 0.3333333333333333703, 0.3333333333333333703, 0.3333333333333334259, 0.3333333333333333148, 0.3333333333333334259, 0.3333333333333333703, 0.3333333333333333703, 0.3333333333333333703, 0.3333333333333333703, 0.3333333333333333148, 0.3333333333333333703, 0.3333333333333334259, 0.3333333333333333148, 0.3333333333333334259, 0.3333333333333333148, 0.3333333333333333703, 0.3333333333333333703, 0.3333333333333333148, 0.3333333333333333703, 0.3333333333333334259, 0.3333333333333333148, 0.3333333333333334259, 0.3333333333333333703, 0.3333333333333332593, 0.3333333333333334814, 0.3333333333333332593, 0.3333333333333334259, 0.3333333333333333148, 0.3333333333333333703, 0.3333333333333334814, 0.3333333333333333703, 0.3333333333333333703, 0.3333333333333332593, 0.3333333333333334814, 0.3333333333333333148, 0.3333333333333333703, 0.3333333333333334259, 0.3333333333333333148, 0.3333333333333334259, 0.3333333333333333148, 0.3333333333333333703, 0.3333333333333333703, 0.3333333333333332593, 0.3333333333333333703, 0.3333333333333333703, 0.3333333333333334259, 0.3333333333333333148, 0.3333333333333334814, 0.3333333333333333703, 0.3333333333333334259, 0.3333333333333333148, 0.3333333333333334259, 0.3333333333333333703, 0.3333333333333333703, 0.3333333333333333703, 0.3333333333333333703, 0.3333333333333333148, 0.3333333333333334814, 0.3333333333333333703, 0.3333333333333333703, 0.3333333333333333148, 0.3333333333333334259, 0.3333333333333333703, 0.3333333333333332593, 0.3333333333333333703, 0.3333333333333333703, 0.3333333333333333703, 0.3333333333333334259, 0.3333333333333334259, 0.3333333333333333703, 0.3333333333333333703, 0.3333333333333333703, 0.3333333333333333703, 0.3333333333333334259, 0.3333333333333332593, 0.3333333333333335369, 0.3333333333333332038, 0.3333333333333333148, 0.3333333333333333703, 0.3333333333333333148, 0.3333333333333333148, 0.3333333333333334259, 0.3333333333333333703, 0.3333333333333333703, 0.3333333333333333703, 0.3333333333333334259, 0.3333333333333333148, 0.3333333333333334814, 0.3333333333333333703, 0.3333333333333334259, 0.3333333333333333703, 0.3333333333333333703, 0.3333333333333332593, 0.3333333333333333148, 0.3333333333333334814, 0.3333333333333333148, 0.3333333333333332593, 0.3333333333333334259, 0.3333333333333332038, 0.3333333333333334259, 0.3333333333333333148, 0.3333333333333333148, 0.3333333333333334259, 0.3333333333333333703, 0.3333333333333333703, 0.3333333333333333703, 0.3333333333333333703, 0.3333333333333334259, 0.3333333333333333148, 0.3333333333333333148, 0.3333333333333334259, 0.3333333333333333148, 0.3333333333333334259, 0.3333333333333333148, 0.3333333333333333703, 0.3333333333333334259, 0.3333333333333333148, 0.3333333333333334814, 0.3333333333333333148, 0.3333333333333334259, 0.3333333333333334259, 0.3333333333333333148, 0.3333333333333333148, 0.3333333333333335369, 0.3333333333333333148, 0.3333333333333333148, 0.3333333333333333703, 0.3333333333333335369, 0.3333333333333332593, 0.3333333333333335369, 0.3333333333333333148, 0.3333333333333333148, 0.3333333333333334259, 0.3333333333333333148, 0.3333333333333334259, 0.3333333333333333703, 0.3333333333333332593, 0.3333333333333333703, 0.3333333333333333148, 0.3333333333333334259, 0.3333333333333333148, 0.3333333333333334259, 0.3333333333333332593, 0.3333333333333335369, 0.3333333333333332038, 0.3333333333333334259, 0.3333333333333332593, 0.3333333333333335369, 0.3333333333333333148, 0.3333333333333334259, 0.3333333333333334259, 0.3333333333333333148, 0.3333333333333333148, 0.3333333333333334259, 0.3333333333333334814, 0.3333333333333333148, 0.3333333333333333148, 0.3333333333333334259, 0.3333333333333333703, 0.3333333333333334259, 0.3333333333333333148, 0.3333333333333333148, 0.3333333333333333703, 0.3333333333333333703, 0.3333333333333334814, 0.3333333333333333148, 0.3333333333333334259, 0.3333333333333333703, 0.3333333333333334259, 0.3333333333333334259, 0.3333333333333333148, 0.3333333333333333703, 0.3333333333333334259, 0.3333333333333333148, 0.3333333333333334814, 0.3333333333333333703, 0.3333333333333333148, 0.3333333333333333703, 0.3333333333333333148, 0.3333333333333334259, 0.3333333333333333148, 0.3333333333333333703, 0.3333333333333332593, 0.3333333333333334814, 0.3333333333333333703, 0.3333333333333334814, 0.3333333333333333148, 0.3333333333333334259, 0.3333333333333334814, 0.3333333333333333148, 0.3333333333333334259, 0.3333333333333332593, 0.3333333333333334259, 0.3333333333333333703, 0.3333333333333333703, 0.3333333333333333148, 0.3333333333333333148, 0.3333333333333334259, 0.3333333333333333148, 0.3333333333333334814, 0.3333333333333333148, 0.3333333333333335924, 0.3333333333333333148, 0.3333333333333334259, 0.3333333333333333148, 0.3333333333333333703, 0.3333333333333333703, 0.3333333333333334814, 0.3333333333333332593, 0.3333333333333333703, 0.3333333333333333703, 0.3333333333333334259, 0.3333333333333333148, 0.3333333333333334259, 0.3333333333333333703, 0.3333333333333333703, 0.3333333333333333703),
 ( 1.000000000000000222, 1.000000000000000222, 1.000000000000000222, 1.000000000000000000, 1.000000000000000000, 1.000000000000000444, 1.000000000000000000, 0.9999999999999997780, 1.000000000000000444, 0.9999999999999997780, 0.9999999999999997780, 1.000000000000000222, 0.9999999999999997780, 0.9999999999999997780, 1.000000000000000444, 0.9999999999999997780, 1.000000000000000222, 1.000000000000000222, 0.9999999999999996669, 1.000000000000000222, 0.9999999999999996669, 1.000000000000000444, 0.9999999999999994449, 1.000000000000000444, 0.9999999999999996669, 1.000000000000000222, 1.000000000000000000, 0.9999999999999997780, 1.000000000000000222, 0.9999999999999997780, 1.000000000000000000, 0.9999999999999997780, 1.000000000000000000, 1.000000000000000222, 0.9999999999999996669, 1.000000000000000000, 0.9999999999999997780, 1.000000000000000000, 1.000000000000000444, 0.9999999999999996669, 1.000000000000000222, 1.000000000000000000, 1.000000000000000222, 1.000000000000000222, 0.9999999999999997780, 0.9999999999999997780, 1.000000000000000222, 0.9999999999999997780, 1.000000000000000222, 0.9999999999999997780, 0.9999999999999997780, 0.9999999999999997780, 1.000000000000000444, 1.000000000000000000, 0.9999999999999997780, 1.000000000000000222, 1.000000000000000000, 1.000000000000000000, 0.9999999999999997780, 1.000000000000000222, 1.000000000000000000, 1.000000000000000000, 1.000000000000000222, 1.000000000000000000, 1.000000000000000000, 1.000000000000000000, 1.000000000000000222, 1.000000000000000000, 0.9999999999999997780, 1.000000000000000444, 1.000000000000000000, 0.9999999999999997780, 1.000000000000000000, 1.000000000000000222, 0.9999999999999997780, 1.000000000000000222, 0.9999999999999996669, 1.000000000000000222, 1.000000000000000000, 1.000000000000000000, 1.000000000000000000, 1.000000000000000222, 0.9999999999999997780, 1.000000000000000000, 1.000000000000000222, 0.9999999999999997780, 1.000000000000000000, 1.000000000000000000, 0.9999999999999996669, 1.000000000000000000, 1.000000000000000000, 1.000000000000000222, 1.000000000000000000, 0.9999999999999997780, 1.000000000000000222, 0.9999999999999996669, 1.000000000000000222, 0.9999999999999997780, 1.000000000000000000, 1.000000000000000000, 1.000000000000000222, 0.9999999999999996669, 1.000000000000000444, 1.000000000000000000, 0.9999999999999997780, 1.000000000000000000, 1.000000000000000000, 1.000000000000000222, 0.9999999999999997780, 1.000000000000000000, 1.000000000000000222, 1.000000000000000444, 1.000000000000000000, 1.000000000000000000, 1.000000000000000444, 1.000000000000000000, 0.9999999999999997780, 1.000000000000000222, 1.000000000000000000, 1.000000000000000000, 1.000000000000000000, 1.000000000000000000, 1.000000000000000000, 1.000000000000000000, 0.9999999999999996669, 1.000000000000000222, 0.9999999999999997780, 1.000000000000000222, 1.000000000000000000, 0.9999999999999997780, 1.000000000000000222, 0.9999999999999997780, 0.9999999999999997780, 0.9999999999999997780, 1.000000000000000000, 1.000000000000000000, 0.9999999999999996669, 1.000000000000000444, 1.000000000000000222, 1.000000000000000000, 1.000000000000000000, 1.000000000000000222, 1.000000000000000222, 1.000000000000000000, 1.000000000000000222, 0.9999999999999996669, 1.000000000000000444, 0.9999999999999997780, 0.9999999999999997780, 1.000000000000000444, 1.000000000000000000, 1.000000000000000222, 0.9999999999999997780, 1.000000000000000222, 1.000000000000000000, 1.000000000000000222, 1.000000000000000000, 1.000000000000000000, 0.9999999999999996669, 1.000000000000000444, 1.000000000000000000, 1.000000000000000222, 0.9999999999999997780, 1.000000000000000000, 1.000000000000000000, 1.000000000000000000, 1.000000000000000000, 0.9999999999999997780, 1.000000000000000000, 1.000000000000000000, 1.000000000000000000, 1.000000000000000222, 1.000000000000000222, 0.9999999999999997780, 1.000000000000000000, 1.000000000000000000, 0.9999999999999997780, 1.000000000000000000, 1.000000000000000000, 1.000000000000000000, 1.000000000000000000, 1.000000000000000444, 0.9999999999999997780, 1.000000000000000222, 0.9999999999999997780, 1.000000000000000000, 1.000000000000000222, 0.9999999999999997780, 1.000000000000000222, 1.000000000000000000, 1.000000000000000000, 1.000000000000000000, 1.000000000000000000, 0.9999999999999997780, 1.000000000000000000, 1.000000000000000000, 1.000000000000000000, 1.000000000000000000, 1.000000000000000000, 1.000000000000000222, 1.000000000000000000, 1.000000000000000222, 0.9999999999999997780, 1.000000000000000222, 0.9999999999999997780, 1.000000000000000222, 1.000000000000000000, 0.9999999999999997780, 1.000000000000000222, 0.9999999999999996669, 1.000000000000000444, 1.000000000000000000, 0.9999999999999996669, 1.000000000000000222, 1.000000000000000000, 1.000000000000000222, 0.9999999999999997780, 1.000000000000000444, 1.000000000000000000, 1.000000000000000000, 0.9999999999999997780, 1.000000000000000222, 1.000000000000000000, 1.000000000000000000, 1.000000000000000000, 1.000000000000000222, 0.9999999999999997780, 1.000000000000000222, 1.000000000000000000, 0.9999999999999997780, 1.000000000000000000, 0.9999999999999997780, 1.000000000000000222, 0.9999999999999996669, 1.000000000000000000, 1.000000000000000000, 1.000000000000000000, 1.000000000000000444, 1.000000000000000222, 1.000000000000000000, 1.000000000000000000, 0.9999999999999997780, 0.9999999999999997780, 1.000000000000000444, 0.9999999999999996669, 1.000000000000000444, 0.9999999999999997780, 0.9999999999999997780, 1.000000000000000222, 0.9999999999999997780, 0.9999999999999996669, 1.000000000000000444, 0.9999999999999997780, 1.000000000000000222, 1.000000000000000222, 1.000000000000000000, 0.9999999999999997780, 1.000000000000000222, 1.000000000000000000, 1.000000000000000222, 1.000000000000000000, 1.000000000000000000, 0.9999999999999997780, 0.9999999999999997780, 1.000000000000000444, 0.9999999999999997780, 0.9999999999999997780, 1.000000000000000222, 0.9999999999999994449, 1.000000000000000222, 0.9999999999999997780, 1.000000000000000000, 0.9999999999999997780, 1.000000000000000000, 1.000000000000000000, 1.000000000000000000, 1.000000000000000000, 1.000000000000000000, 1.000000000000000000, 1.000000000000000000, 1.000000000000000222, 1.000000000000000000, 1.000000000000000000, 1.000000000000000000, 1.000000000000000000, 1.000000000000000000, 1.000000000000000000, 1.000000000000000000, 1.000000000000000222, 1.000000000000000000, 1.000000000000000222, 0.9999999999999997780, 1.000000000000000000, 1.000000000000000444, 1.000000000000000000, 1.000000000000000000, 1.000000000000000000, 1.000000000000000222, 0.9999999999999997780, 1.000000000000000444, 0.9999999999999997780, 1.000000000000000222, 1.000000000000000000, 1.000000000000000000, 1.000000000000000000, 1.000000000000000222, 0.9999999999999994449, 1.000000000000000222, 1.000000000000000000, 1.000000000000000000, 1.000000000000000000, 0.9999999999999997780, 0.9999999999999997780, 1.000000000000000444, 0.9999999999999996669, 1.000000000000000222, 0.9999999999999997780, 1.000000000000000444, 0.9999999999999997780, 1.000000000000000222, 1.000000000000000222, 0.9999999999999996669, 1.000000000000000222, 1.000000000000000000, 1.000000000000000444, 1.000000000000000000, 1.000000000000000000, 1.000000000000000222, 1.000000000000000000, 1.000000000000000000, 0.9999999999999997780, 0.9999999999999997780, 1.000000000000000000, 0.9999999999999997780, 1.000000000000000222, 1.000000000000000222, 1.000000000000000000, 1.000000000000000222, 1.000000000000000222, 1.000000000000000000, 0.9999999999999997780, 0.9999999999999997780, 1.000000000000000222, 0.9999999999999997780, 1.000000000000000222, 1.000000000000000000, 1.000000000000000000, 1.000000000000000000, 0.9999999999999996669, 1.000000000000000222, 0.9999999999999997780, 1.000000000000000000, 0.9999999999999997780, 1.000000000000000222, 0.9999999999999997780, 1.000000000000000444, 0.9999999999999996669, 1.000000000000000222, 1.000000000000000222, 1.000000000000000000, 1.000000000000000000, 0.9999999999999997780, 1.000000000000000222, 0.9999999999999997780, 1.000000000000000222, 0.9999999999999997780, 0.9999999999999997780, 1.000000000000000000, 1.000000000000000000, 1.000000000000000222, 1.000000000000000000, 1.000000000000000444, 0.9999999999999997780, 1.000000000000000222, 0.9999999999999997780, 0.9999999999999997780, 1.000000000000000222, 1.000000000000000000, 0.9999999999999997780, 1.000000000000000000, 1.000000000000000000, 1.000000000000000000, 0.9999999999999997780, 1.000000000000000444, 0.9999999999999997780, 1.000000000000000000, 1.000000000000000000) ) ) 
 REPRESENTATION_ITEM ( '' )  SURFACE ( )  );
#81466=CARTESIAN_POINT ( 'NONE',  ( 2.596233987490266681, -0.9813665562012074961, 1.641104690102652919 ) ) ;
#81467=CARTESIAN_POINT ( 'NONE',  ( 3.326767387183640956, 0.04228616847017605679, 1.769505212706389941 ) ) ;
#81468=CARTESIAN_POINT ( 'NONE',  ( 1.102048709075389654, -0.8591247869965330519, 1.708478583560539166 ) ) ;
#81470=CARTESIAN_POINT ( 'NONE',  ( 5.571877068885287443, -0.8567909204831600789, 1.713377365699362054 ) ) ;
#81471=CARTESIAN_POINT ( 'NONE',  ( 6.338338845641732888, -1.054863691225367939, 1.663055945198953278 ) ) ;
#81473=CARTESIAN_POINT ( 'NONE',  ( 1.512141599020993432, -0.7094941370262074498, 1.998545949238240027 ) ) ;
#81475=CARTESIAN_POINT ( 'NONE',  ( 5.260568668178753349, -1.354309965608934352, 1.290672426560689035 ) ) ;
#81476=CARTESIAN_POINT ( 'NONE',  ( 0.3986991128735201673, 1.519733473351183362, -1.011397189243423700 ) ) ;
#81478=CARTESIAN_POINT ( 'NONE',  ( 4.776106669258010307, 1.268914099295117781, 1.805409367619143390 ) ) ;
#81481=CARTESIAN_POINT ( 'NONE',  ( 2.066913078360913314, 1.530046405743747506, -1.383527225477628297 ) ) ;
#81488=CARTESIAN_POINT ( 'NONE',  ( 4.334477209444560053, -1.194628513295314942, 1.690740121169509447 ) ) ;
#81490=CARTESIAN_POINT ( 'NONE',  ( 1.845224345143604561, -1.827161268409679407, 1.154667503900350223 ) ) ;
#81492=CARTESIAN_POINT ( 'NONE',  ( 1.910812834059022469, -0.5409473409442880909, -1.945794739053583466 ) ) ;
#81499=CARTESIAN_POINT ( 'NONE',  ( 0.6906390985809904848, 1.523792322931913468, -1.320830384837400118 ) ) ;
#81500=CARTESIAN_POINT ( 'NONE',  ( 5.460537066722415567, -1.980877156148381335, -0.9378266216248376530 ) ) ;
#81502=CARTESIAN_POINT ( 'NONE',  ( 3.041163856788456687, 0.05134138945498378792, 1.911883771832747048 ) ) ;
#81506=CARTESIAN_POINT ( 'NONE',  ( 2.021111450618333194, -1.799914642762674433, 0.9091633978678403949 ) ) ;
#81508=CARTESIAN_POINT ( 'NONE',  ( -0.05846771364293941453, -1.777572824190313261, -1.447063799157372044 ) ) ;
#81510=CARTESIAN_POINT ( 'NONE',  ( 4.155083606764530479, -1.434382041474260516, -0.9574503856549732017 ) ) ;
#81515=CARTESIAN_POINT ( 'NONE',  ( 0.1753634416057497647, 0.2329791690731698173, -2.177930625204091086 ) ) ;
#81518=CARTESIAN_POINT ( 'NONE',  ( 5.584552742667589165, -1.144318741887658586, 1.404276898221923364 ) ) ;
#81523=CARTESIAN_POINT ( 'NONE',  ( 6.270143006926431006, 1.806086713848788161, -0.1406222877055433862 ) ) ;
#81526=CARTESIAN_POINT ( 'NONE',  ( 2.607599380506659514, -2.167453834138896696, 0.3226137089109848421 ) ) ;
#81527=CARTESIAN_POINT ( 'NONE',  ( 6.232830220009587308, -1.767433141015135822, -0.5829711297899267120 ) ) ;
#81529=CARTESIAN_POINT ( 'NONE',  ( 3.743669890235715947, 1.900728030520698830, -0.2378226680747745625 ) ) ;
#81535=CARTESIAN_POINT ( 'NONE',  ( 0.7433210806352362754, -1.853469564684958382, 1.112228649290482263 ) ) ;
#81538=CARTESIAN_POINT ( 'NONE',  ( 0.2877648253245302379, -0.8656086203641421006, 1.607325130595547602 ) ) ;
#81540=CARTESIAN_POINT ( 'NONE',  ( 3.504746488097260748, 1.439749907568649068, -1.122338611188322455 ) ) ;
#81543=CARTESIAN_POINT ( 'NONE',  ( 3.051173608728700248, 1.690664904776484789, -1.010063219348409813 ) ) ;
#81545=CARTESIAN_POINT ( 'NONE',  ( 5.056170473960743372, -1.404048225252243265, 1.341958350743667205 ) ) ;
#81548=CARTESIAN_POINT ( 'NONE',  ( 5.431924468521282634, -2.068440459917933794, 0.4666711972392265650 ) ) ;
#81550=CARTESIAN_POINT ( 'NONE',  ( 3.299369280271017946, 1.727720890571235124, -0.8199460011262191816 ) ) ;
#81554=CARTESIAN_POINT ( 'NONE',  ( 4.477201648280199286, -1.799136850145161892, -0.9032412251695760563 ) ) ;
#81556=CARTESIAN_POINT ( 'NONE',  ( 5.180226163740526246, -1.011166736308216629, 1.519887457628710248 ) ) ;
#81557=CARTESIAN_POINT ( 'NONE',  ( 0.9771079587245214970, 1.912259438035465386, 0.7939916666956441382 ) ) ;
#81561=CARTESIAN_POINT ( 'NONE',  ( 5.366025703835962446, 0.9229158262306772498, 1.627043297953718382 ) ) ;
#81573=CARTESIAN_POINT ( 'NONE',  ( 1.446235060908855008, -0.9343481645287862181, 1.847524432027500385 ) ) ;
#81574=CARTESIAN_POINT ( 'NONE',  ( 2.671616206378808478, 1.499349897650571695, 1.495110359788552223 ) ) ;
#81578=CARTESIAN_POINT ( 'NONE',  ( 0.3562224712859492493, -1.968894089644295686, -0.05400687454796929826 ) ) ;
#81582=DIRECTION ( 'NONE',  ( -1.000000000000000000, 1.014813233446432150E-15, 1.972152263052529514E-31 ) ) ;
#81583=CARTESIAN_POINT ( 'NONE',  ( 3.012002838297692886, -1.130384021687063534, -1.994099915080405294 ) ) ;
#81584=CARTESIAN_POINT ( 'NONE',  ( 0.04711308451243316486, -1.408776630263553375, -1.161003007932148501 ) ) ;
#81585=CARTESIAN_POINT ( 'NONE',  ( 2.601700882821424976, 1.355260107747566334, 1.349524769375435973 ) ) ;
#81587=CARTESIAN_POINT ( 'NONE',  ( 0.3518148739534024960, -1.426620726115679361, -1.420723246562720421 ) ) ;
#81588=CARTESIAN_POINT ( 'NONE',  ( 1.551531708069888715, 1.481957716508151890, 1.285475804911541120 ) ) ;
#81592=CARTESIAN_POINT ( 'NONE',  ( 3.732441334599644556, 0.3067963083541249691, 2.067875747930392638 ) ) ;
#81593=CARTESIAN_POINT ( 'NONE',  ( 2.219294626563913297, -1.717429429511443173, 0.4269959701016200482 ) ) ;
#81596=CARTESIAN_POINT ( 'NONE',  ( 5.402359069383361856, 1.738778441700383315, -1.493778605308769603 ) ) ;
#81597=CARTESIAN_POINT ( 'NONE',  ( 4.822041096100106117, 1.666637052750892911, 0.5010418475075908429 ) ) ;
#81600=CARTESIAN_POINT ( 'NONE',  ( 4.692597494581693063, -1.067344209891357032, -1.366281018423552762 ) ) ;
#81601=CARTESIAN_POINT ( 'NONE',  ( 4.580651514471745678, 1.339088007528920210, -1.708959110978137019 ) ) ;
#81603=CARTESIAN_POINT ( 'NONE',  ( 5.964077395145578109, -1.074666730956087335, 1.706109649615504154 ) ) ;
#81604=CARTESIAN_POINT ( 'NONE',  ( 0.2499999969303341174, 7.552774431159578439E-08, 2.052068128417954274 ) ) ;
#81607=CARTESIAN_POINT ( 'NONE',  ( 3.153258193586833347, -1.574033464040735408, -1.110325110657943481 ) ) ;
#81609=CARTESIAN_POINT ( 'NONE',  ( 6.012022869640524014, -0.7491050530544652863, 2.091446645375413027 ) ) ;
#81611=CARTESIAN_POINT ( 'NONE',  ( 6.883263157960401557, 2.461427291499204362, 2.229941283862615808 ) ) ;
#81614=CARTESIAN_POINT ( 'NONE',  ( 1.208037074693757651, 1.685330760668615646, 1.447128815913247379 ) ) ;
#81621=CARTESIAN_POINT ( 'NONE',  ( 4.791499389596598490, -1.887151845835168817, 0.8330235203531827226 ) ) ;
#81625=CARTESIAN_POINT ( 'NONE',  ( 5.624238404463478780, 1.114819804898508515, -1.501858222471161408 ) ) ;
#81626=CARTESIAN_POINT ( 'NONE',  ( 5.133366751340045830, 0.5111148723837605212, 1.657103328152222055 ) ) ;
#81627=CARTESIAN_POINT ( 'NONE',  ( 4.212277857634297185, 1.593487861523819271, 0.7003764074154511521 ) ) ;
#81629=CARTESIAN_POINT ( 'NONE',  ( 2.331904285594294191, 1.077338530963572127, -2.023425408739158105 ) ) ;
#81631=CARTESIAN_POINT ( 'NONE',  ( 0.7613493127172387132, 0.9053670157611827252, 1.603083849714491027 ) ) ;
#81635=CARTESIAN_POINT ( 'NONE',  ( 1.781981981289095796, -0.9795585948506604357, 1.540336029244721461 ) ) ;
#81636=CARTESIAN_POINT ( 'NONE',  ( 2.426407915648312930, -1.496052118593782065, -1.352154011671408362 ) ) ;
#81637=CARTESIAN_POINT ( 'NONE',  ( 1.640847625397081844, -1.850035366842089024, 1.174371965539475093 ) ) ;
#81640=CARTESIAN_POINT ( 'NONE',  ( 1.188034388246852480, -1.312013912954514971, -1.601590607232979524 ) ) ;
#81643=CARTESIAN_POINT ( 'NONE',  ( 3.528090983593739516, -2.088826311502915090, 0.3641918842257965139 ) ) ;
#81645=CARTESIAN_POINT ( 'NONE',  ( 6.516225534515442952, -0.8655890497146904172, -1.607451055071248636 ) ) ;
#81652=CARTESIAN_POINT ( 'NONE',  ( 3.340107562988120726, -1.206563586372558561, -1.619613960689977761 ) ) ;
#81653=CARTESIAN_POINT ( 'NONE',  ( 1.149603698739794400, -1.659950780972534012, -1.295870271070469260 ) ) ;
#81656=CARTESIAN_POINT ( 'NONE',  ( 5.576953945496859966, 1.718729505308995931, 0.7139912403442708611 ) ) ;
#81662=CARTESIAN_POINT ( 'NONE',  ( 0.3566080023540801336, 0.8287714912002723811, 1.996717379258300840 ) ) ;
#81666=CARTESIAN_POINT ( 'NONE',  ( 2.336848640490073237, -1.070562806433389857, 1.363724479458855443 ) ) ;
#81667=CARTESIAN_POINT ( 'NONE',  ( 1.815945235625218590, 1.623157326234461628, 0.6282625412417954802 ) ) ;
#81668=CARTESIAN_POINT ( 'NONE',  ( 0.1480895125635858234, -1.786911571543071675, -1.459641600669525197 ) ) ;
#81671=CARTESIAN_POINT ( 'NONE',  ( 2.987629706096385895, 1.454891456164056462, 1.459756821352270473 ) ) ;
#81673=CARTESIAN_POINT ( 'NONE',  ( 1.352888501574830205, -0.9090079681693465918, 1.799646022210943386 ) ) ;
#81674=CARTESIAN_POINT ( 'NONE',  ( 6.825078400183574701, 2.043583509370741069, 2.350167621585138367 ) ) ;
#81676=CARTESIAN_POINT ( 'NONE',  ( 1.270321628189803542, -1.252206795699914332, 1.522702518494284396 ) ) ;
#81677=CARTESIAN_POINT ( 'NONE',  ( 4.465046277278037934, -1.532637281380120564, 1.143568071694904598 ) ) ;
#81680=CARTESIAN_POINT ( 'NONE',  ( 6.270183524512255246, 1.130759168108757873, 1.895055401287759178 ) ) ;
#81684=CARTESIAN_POINT ( 'NONE',  ( 0.3463606850301796380, 1.036194208456611809, -1.733443346147050868 ) ) ;
#81688=CARTESIAN_POINT ( 'NONE',  ( 4.665214083390394784, -2.058938813511351551, -1.042142520334616185 ) ) ;
#81689=CARTESIAN_POINT ( 'NONE',  ( 5.266048140081638351, -1.952571265509401854, 0.1905133553196102503 ) ) ;
#81690=CARTESIAN_POINT ( 'NONE',  ( 2.061309051315598051, 1.628117514333087934, 1.094105149622534467 ) ) ;
#81692=CARTESIAN_POINT ( 'NONE',  ( -0.1341500063891595818, -0.1486117279969369209, -1.983907055413631992 ) ) ;
#81694=CARTESIAN_POINT ( 'NONE',  ( 6.509000000000012776, 0.004788705324892602276, 2.000274819378269342 ) ) ;
#81698=CARTESIAN_POINT ( 'NONE',  ( 0.7086343398283838635, -0.2726298849291541870, 1.820711063333625646 ) ) ;
#81700=CARTESIAN_POINT ( 'NONE',  ( 3.713894982949633050, 0.5324762967815239723, -2.104625409411722270 ) ) ;
#81703=CARTESIAN_POINT ( 'NONE',  ( 2.338272602237463360, -1.224740070204191289, -1.730971256048131401 ) ) ;
#81709=CARTESIAN_POINT ( 'NONE',  ( 2.354824746187761164, -1.594966302183076667, 1.304983254080711808 ) ) ;
#81713=CARTESIAN_POINT ( 'NONE',  ( -0.02264175331117677936, 7.629137130509094256, -2.689100833419917347 ) ) ;
#81715=CARTESIAN_POINT ( 'NONE',  ( 5.426388453851806126, -0.8635988772061551355, -1.706256623820540108 ) ) ;
#81717=CARTESIAN_POINT ( 'NONE',  ( 1.722331603166191050, -1.256259422768091216, -1.881381621351454037 ) ) ;
#81719=CARTESIAN_POINT ( 'NONE',  ( 1.406221933027915982, -1.803026290124358555, -0.1754379831288860880 ) ) ;
#81720=CARTESIAN_POINT ( 'NONE',  ( 2.465921856196826134, -0.9807800477944830231, 1.645437157327357180 ) ) ;
#81721=CARTESIAN_POINT ( 'NONE',  ( 3.209495720308676248, -1.691010085789945716, -1.194244797349801157 ) ) ;
#81723=CARTESIAN_POINT ( 'NONE',  ( 1.182427310604698079, -1.922956083944601158, -0.4339701177692931178 ) ) ;
#81724=CARTESIAN_POINT ( 'NONE',  ( 5.760362637647353345, 0.7829873311157690141, 1.760386188003287611 ) ) ;
#81725=CARTESIAN_POINT ( 'NONE',  ( 0.7159568421808035765, -0.3331041906398305441, 2.283425790780469811 ) ) ;
#81729=CARTESIAN_POINT ( 'NONE',  ( 5.195784910611107144, -1.456250996468626768, -1.461061404345398440 ) ) ;
#81733=CARTESIAN_POINT ( 'NONE',  ( 6.774446309029529267, -1.298820955785205955, 1.658247839749617869 ) ) ;
#81737=CARTESIAN_POINT ( 'NONE',  ( 5.325516461952284786, -2.054413220456321909, 0.6725034809518318779 ) ) ;
#81738=CARTESIAN_POINT ( 'NONE',  ( 5.918619479961092722, -0.7289874232782632690, -1.883701229315833059 ) ) ;
#81745=CARTESIAN_POINT ( 'NONE',  ( 3.520720487665735643, 0.3006478860226591276, 1.993893439002386581 ) ) ;
#81750=CARTESIAN_POINT ( 'NONE',  ( 5.137646372127643524, -1.526005641499485810, -1.531359247741073570 ) ) ;
#81755=CARTESIAN_POINT ( 'NONE',  ( 5.237907724141787291, 2.013986247903374327, -0.1017665992488273330 ) ) ;
#81757=CARTESIAN_POINT ( 'NONE',  ( 0.7501351305400367764, 0.4964161116564491660, 1.651887862327553691 ) ) ;
#81762=CARTESIAN_POINT ( 'NONE',  ( 6.292256349370360269, -1.861554482619768525, -0.1834065582871149958 ) ) ;
#81763=CARTESIAN_POINT ( 'NONE',  ( 1.365886254406587064, 0.5821385057369383720, -1.927099543440218499 ) ) ;
#81765=CARTESIAN_POINT ( 'NONE',  ( 3.469938103458301892, 2.153457811087633011, -0.4814610123115290463 ) ) ;
#81770=CARTESIAN_POINT ( 'NONE',  ( 2.491022521637117570, -2.029929026191950481, -0.6131127883793398015 ) ) ;
#81771=CARTESIAN_POINT ( 'NONE',  ( 1.757435634535610136, 1.928746520693159550, -0.5880414618760835266 ) ) ;
#81772=CARTESIAN_POINT ( 'NONE',  ( 2.091809026493749890, 1.116998374171035424, 1.426102431979922702 ) ) ;
#81778=CARTESIAN_POINT ( 'NONE',  ( -0.2353475280464593089, -0.1482846297235005661, -1.883952934485186415 ) ) ;
#81786=CARTESIAN_POINT ( 'NONE',  ( 4.118171802502921253, -1.108985364570359566, -1.855417305202881506 ) ) ;
#81789=CARTESIAN_POINT ( 'NONE',  ( 1.371502371489873751, -1.821557607348308405, -1.085495857948336251 ) ) ;
#81791=CARTESIAN_POINT ( 'NONE',  ( 3.321511454083085457, -1.900871985879136528, 0.5222822307265824193 ) ) ;
#81792=CARTESIAN_POINT ( 'NONE',  ( 5.607647405131535479, 1.452367144367059826, 1.244281684088064166 ) ) ;
#81795=CARTESIAN_POINT ( 'NONE',  ( 6.865690646733241032, -0.4297541067138924697, 1.928966555396218752 ) ) ;
#81796=CARTESIAN_POINT ( 'NONE',  ( 1.886567394283003907, 1.689560458097194795, -0.9572515956587694941 ) ) ;
#81801=CARTESIAN_POINT ( 'NONE',  ( 2.695356974763486679, -0.6552250210129506591, 1.985377264055338209 ) ) ;
#81805=CARTESIAN_POINT ( 'NONE',  ( 5.637344576021464881, -0.04253375892994575719, 1.911971901805488816 ) ) ;
#81807=CARTESIAN_POINT ( 'NONE',  ( 4.776106669258010307, 1.268914099295117781, 1.805409367619143390 ) ) ;
#81809=CARTESIAN_POINT ( 'NONE',  ( 1.659489206604364941, -1.893029981318217647, -1.133929415002648655 ) ) ;
#81810=CARTESIAN_POINT ( 'NONE',  ( 1.119614361207950548, -0.4638517909370845071, 1.855054000551699778 ) ) ;
#81813=CARTESIAN_POINT ( 'NONE',  ( 4.229010956685672618, -1.930657356216297860, -0.7480826485904976675 ) ) ;
#81815=CARTESIAN_POINT ( 'NONE',  ( 1.657319961134783748, -1.854130675604428902, -1.111159678259740602 ) ) ;
#81816=CARTESIAN_POINT ( 'NONE',  ( 4.195009555701286530, 1.760677850468267414, 1.304791629949946019 ) ) ;
#81824=CARTESIAN_POINT ( 'NONE',  ( -0.1224325501351306023, -0.4448023855274513272, -1.973852191825019364 ) ) ;
#81826=CARTESIAN_POINT ( 'NONE',  ( 4.733297664174529906, 0.005294743050891088411, -2.070434559870132585 ) ) ;
#81827=CARTESIAN_POINT ( 'NONE',  ( 6.151990787553828888, 1.088749021807510431, 1.815729776765177661 ) ) ;
#81830=CARTESIAN_POINT ( 'NONE',  ( 3.784006971647640327, -1.169605039944806357, -1.584395421511639812 ) ) ;
#81831=CARTESIAN_POINT ( 'NONE',  ( 5.947306879541199187, 0.6707566017311801243, -2.191947003353618584 ) ) ;
#81832=CARTESIAN_POINT ( 'NONE',  ( 3.756323439517950558, 0.6585720284536450420, 1.702948436616057881 ) ) ;
#81838=CARTESIAN_POINT ( 'NONE',  ( 4.693612458567416823, 1.876924737948972188, -0.7285200738881071336 ) ) ;
#81839=CARTESIAN_POINT ( 'NONE',  ( 6.346320258841911865, 0.3977546830747305528, -2.263887401186816639 ) ) ;
#81840=CARTESIAN_POINT ( 'NONE',  ( 4.768382384511014038, -0.8351381170168621360, -1.775225883709200980 ) ) ;
#81846=CARTESIAN_POINT ( 'NONE',  ( 0.5914941650546343688, -0.7489122546765265565, 1.952206342558031160 ) ) ;
#81847=CARTESIAN_POINT ( 'NONE',  ( 5.700005536890629720, -1.770032025875327042, 0.003423177859356376761 ) ) ;
#81849=CARTESIAN_POINT ( 'NONE',  ( 6.246037776718591061, 0.6113502166280659900, 1.843275756764614082 ) ) ;
#81850=CARTESIAN_POINT ( 'NONE',  ( 2.045129345224237394, -1.761195505111545989, -1.303888621850733509 ) ) ;
#81851=CARTESIAN_POINT ( 'NONE',  ( 1.118268200169919568, -0.04383651085794643132, 1.740047355671838547 ) ) ;
#81853=CARTESIAN_POINT ( 'NONE',  ( 0.2333690889706717397, 6.947499272388762748, -2.648434294982876303 ) ) ;
#81854=CARTESIAN_POINT ( 'NONE',  ( 1.224769985559545304, -0.04580521419573525821, 1.724442238450181186 ) ) ;
#81855=CARTESIAN_POINT ( 'NONE',  ( 1.189316404147572337, 1.662717542896676504, 1.427817766309902314 ) ) ;
#81856=CARTESIAN_POINT ( 'NONE',  ( 3.598431038176507002, -2.204323482753521635, -0.1086902067785888437 ) ) ;
#81857=B_SPLINE_CURVE_WITH_KNOTS ( 'NONE', 3,
 ( #127528, #90689, #207603, #208661, #27798, #75485, #143733, #209726, #11540, #171919, #74425 ),
 .UNSPECIFIED., .F., .F.,
 ( 4, 1, 1, 1, 1, 1, 1, 1, 4 ),
 ( 0.000000000000000000, 0.2254179815473072723, 0.3971144120416517653, 0.5241699701252212629, 0.6156743509408303394, 0.6807935377546089351, 0.7289379548928518471, 0.7696256121123346006, 1.000000000000000000 ),
 .UNSPECIFIED. ) ;
#81858=CARTESIAN_POINT ( 'NONE',  ( 0.9190777403676134716, -1.573854924298900615, 1.495750265368815946 ) ) ;
#81859=CARTESIAN_POINT ( 'NONE',  ( 0.3635304476994546952, 1.806310985241452949, -0.2645042207462811046 ) ) ;
#81860=CARTESIAN_POINT ( 'NONE',  ( 2.220046512049120846, 0.9935532346000598425, -1.869724544471425665 ) ) ;
#81863=CARTESIAN_POINT ( 'NONE',  ( 2.437429393347473994, -1.701094670537067755, -1.536833775788006173 ) ) ;
#81866=CARTESIAN_POINT ( 'NONE',  ( 4.934350062338543452, -1.187533444586796438, -1.877053939226761115 ) ) ;
#81875=CARTESIAN_POINT ( 'NONE',  ( 3.217422812353257555, 1.967887761762876941, 0.4390297752325384995 ) ) ;
#81877=CARTESIAN_POINT ( 'NONE',  ( 0.8485701241471826917, -2.046539366587364572, -0.2563945212397024109 ) ) ;
#81882=CARTESIAN_POINT ( 'NONE',  ( 3.785266741157941262, 1.586943040539133154, 1.511552532079393885 ) ) ;
#81883=CARTESIAN_POINT ( 'NONE',  ( 2.197888892816081796, 1.802417619043535701, 0.9041091288993635677 ) ) ;
#81884=CARTESIAN_POINT ( 'NONE',  ( 1.417261839328866513, -1.023339270300478221, -1.530466495063505628 ) ) ;
#81887=CARTESIAN_POINT ( 'NONE',  ( 4.788025880137685597, -0.8597811773201522456, 1.610451283527076116 ) ) ;
#81888=CARTESIAN_POINT ( 'NONE',  ( 6.100232455412330168, -0.2440331339308223768, 2.001510902166554473 ) ) ;
#81890=CARTESIAN_POINT ( 'NONE',  ( 4.294006694993548479, -0.8693707907260415091, 2.089011835857216948 ) ) ;
#81892=CARTESIAN_POINT ( 'NONE',  ( 1.313257463657933055, 1.858222661572891621, 0.9912184023134795741 ) ) ;
#81894=CARTESIAN_POINT ( 'NONE',  ( 5.178213324540339002, -1.104578422852561914, -1.750899486206449751 ) ) ;
#81902=CARTESIAN_POINT ( 'NONE',  ( 0.4223351350958382544, -2.109807164369668087, 0.2139620856976830743 ) ) ;
#81903=CARTESIAN_POINT ( 'NONE',  ( 2.250487404410873804, 1.042729518208513007, -1.961448655418545739 ) ) ;
#81907=CARTESIAN_POINT ( 'NONE',  ( 3.613678190204441254, 0.4790664972640528152, -1.902336835828049244 ) ) ;
#81914=CARTESIAN_POINT ( 'NONE',  ( 2.566775492539817627, 0.7186216927172992541, 1.995234744298620910 ) ) ;
#81916=CARTESIAN_POINT ( 'NONE',  ( 5.863715402168388380, -0.4781514528688200483, 1.902565108626976809 ) ) ;
#81917=CARTESIAN_POINT ( 'NONE',  ( 3.819328725847204620, -0.1613130240520690706, 2.155748724213396361 ) ) ;
#81918=CARTESIAN_POINT ( 'NONE',  ( 2.471991059931688106, -1.762569054296094340, -0.5325411743367300943 ) ) ;
#81921=CARTESIAN_POINT ( 'NONE',  ( 4.575936575705426890, -1.688975870839603655, -0.4190883748532001629 ) ) ;
#81924=CARTESIAN_POINT ( 'NONE',  ( 6.720655732516647163, 0.005566325962592238996, 1.826293863978686982 ) ) ;
#81926=CARTESIAN_POINT ( 'NONE',  ( 1.657319961134783748, -1.854130675604428902, -1.111159678259740602 ) ) ;
#81927=CARTESIAN_POINT ( 'NONE',  ( 4.692732413458527319, -1.238132498367884082, -1.591073831703953445 ) ) ;
#81929=CARTESIAN_POINT ( 'NONE',  ( 1.674925575805393585, -2.052671086741376882, -0.6780288057936025847 ) ) ;
#81930=CARTESIAN_POINT ( 'NONE',  ( 2.319545460040703500, -1.913138470506670075, 0.4751570986292509846 ) ) ;
#81932=CARTESIAN_POINT ( 'NONE',  ( 3.456523497251274168, -1.714022962016878759, -0.9130526778427237033 ) ) ;
#81944=CARTESIAN_POINT ( 'NONE',  ( 1.026743138268666922, 1.313310656681260680, -1.773271738842125300 ) ) ;
#81946=CARTESIAN_POINT ( 'NONE',  ( 5.489096970993415425, 0.1405823987245969631, 1.956747174436481274 ) ) ;
#81947=CARTESIAN_POINT ( 'NONE',  ( 3.854788253679425125, -1.977088355604763148, -0.7582873983895296321 ) ) ;
#81949=CARTESIAN_POINT ( 'NONE',  ( 0.1745949693968146810, 5.726316517925682525, -2.349368801211670021 ) ) ;
#81950=CARTESIAN_POINT ( 'NONE',  ( 4.452959842461719830, 0.4008590389125502029, -1.796806262838637647 ) ) ;
#81954=CARTESIAN_POINT ( 'NONE',  ( 5.379186226027963258, -1.918017450862268714, -0.9047448674902383026 ) ) ;
#81957=CARTESIAN_POINT ( 'NONE',  ( 6.802032647988246694, -2.060431444914239130, 0.04577141437269586360 ) ) ;
#81959=CARTESIAN_POINT ( 'NONE',  ( 0.9415990247386073486, 1.246032235168346380, 1.382555731526733611 ) ) ;
#81960=CARTESIAN_POINT ( 'NONE',  ( 3.368544699895597461, 0.04196216268675251326, -1.840931771443871101 ) ) ;
#81965=CARTESIAN_POINT ( 'NONE',  ( 3.264504910713565078, 0.9923201075644829672, 1.971275125648555449 ) ) ;
#81966=CARTESIAN_POINT ( 'NONE',  ( 5.167352989974902222, 0.2290589858122368538, -2.250810084452478765 ) ) ;
#81968=CARTESIAN_POINT ( 'NONE',  ( 4.500164564109310206, -0.8477707339301239209, 1.600948808527142386 ) ) ;
#81969=CARTESIAN_POINT ( 'NONE',  ( 5.507027455500737467, -0.04000985115821522470, 1.915467925163343965 ) ) ;
#81971=CARTESIAN_POINT ( 'NONE',  ( 5.735183426005796115, -1.690533149647139410, 0.8011652756413772947 ) ) ;
#81972=CARTESIAN_POINT ( 'NONE',  ( 6.285601362909060796, -1.752004058920811902, 0.6281230767469258014 ) ) ;
#81975=CARTESIAN_POINT ( 'NONE',  ( 6.069200897874186040, 0.1259568369440123015, -1.765440829579780990 ) ) ;
#81976=CARTESIAN_POINT ( 'NONE',  ( 1.692592581891849912, 1.490968054865527304, -1.357870634957742961 ) ) ;
#81978=CARTESIAN_POINT ( 'NONE',  ( 2.561271001754578780, -1.832848164261296597, -1.037248627104673249 ) ) ;
#81983=CARTESIAN_POINT ( 'NONE',  ( 1.758075477673838982, 0.7690763710625804217, -1.867840884567156357 ) ) ;
#81986=CARTESIAN_POINT ( 'NONE',  ( 2.829541668879275829, -2.018026287816252040, 0.7751260729957698548 ) ) ;
#81987=CARTESIAN_POINT ( 'NONE',  ( 6.620655732516645742, 3.706282450693793695, 2.340867613974298767 ) ) ;
#81996=CARTESIAN_POINT ( 'NONE',  ( 1.329895901633147748, 1.076045675571284166, -1.909117696414885934 ) ) ;
#81998=CARTESIAN_POINT ( 'NONE',  ( 0.9368240258568013568, 2.229511284875786536, 0.3842425355367936057 ) ) ;
#82005=CARTESIAN_POINT ( 'NONE',  ( 3.374023350818358580, -1.056766630983814625, 1.419390967538982418 ) ) ;
#82006=CARTESIAN_POINT ( 'NONE',  ( 6.282275147445602670, -1.185768659569720329, 1.860957768143455038 ) ) ;
#82010=CARTESIAN_POINT ( 'NONE',  ( 5.026970340808907700, -1.727993218758390404, 1.039010492973009514 ) ) ;
#82013=CARTESIAN_POINT ( 'NONE',  ( 2.483090063216564669, 1.711211315118581711, -0.7561169667836544761 ) ) ;
#82014=CARTESIAN_POINT ( 'NONE',  ( 2.799741537105740363, -1.531010120401912200, -1.393694001666223814 ) ) ;
#82016=CARTESIAN_POINT ( 'NONE',  ( 1.828231037913151447, -0.9045423626323212396, -1.684975973026317408 ) ) ;
#82021=CARTESIAN_POINT ( 'NONE',  ( 0.9317291061951762376, -1.865162313430932750, 0.4216105838140621342 ) ) ;
#82022=CARTESIAN_POINT ( 'NONE',  ( 2.822649888979886335, -1.354935067541668259, 1.419045635080482093 ) ) ;
#82027=CARTESIAN_POINT ( 'NONE',  ( 6.520779640719153392, 1.838571040693348646, 0.7116797190419403840 ) ) ;
#82029=CARTESIAN_POINT ( 'NONE',  ( 1.599859548348059324, 1.391279381849828800, 1.455310581225319311 ) ) ;
#82031=CARTESIAN_POINT ( 'NONE',  ( 1.669685637109643794, 1.462710821638053105, 1.530943346549427320 ) ) ;
#82033=CARTESIAN_POINT ( 'NONE',  ( 3.613788337741298040, 0.5058112091442801272, -2.007490274132675445 ) ) ;
#82035=CARTESIAN_POINT ( 'NONE',  ( 5.964805764622640005, 0.1547682761293242837, -2.084958343724970131 ) ) ;
#82037=CARTESIAN_POINT ( 'NONE',  ( 3.909063277197013520, 1.565549990038747952, 0.9388121169797561949 ) ) ;
#82042=CARTESIAN_POINT ( 'NONE',  ( 5.104599427727727345, -0.7392731805347592111, -2.079399364341961487 ) ) ;
#82045=CARTESIAN_POINT ( 'NONE',  ( 3.527896108305649037, -1.883508717751972705, 0.3295761852530054159 ) ) ;
#82053=CARTESIAN_POINT ( 'NONE',  ( 0.1867156058280825814, 1.363667594142993877, 1.237386390646778578 ) ) ;
#82058=CARTESIAN_POINT ( 'NONE',  ( 4.639837347815604751, 0.8015432297804045980, -1.690266223530467293 ) ) ;
#82063=CARTESIAN_POINT ( 'NONE',  ( 1.498812192398508270, 0.3789717401675870567, 1.932455098789982895 ) ) ;
#82064=CARTESIAN_POINT ( 'NONE',  ( 2.460564738353550496, -1.930424690641812768, -0.5826366834433827080 ) ) ;
#82069=CARTESIAN_POINT ( 'NONE',  ( 2.695491272475036837, -0.6865090956127660737, 2.081212476921667776 ) ) ;
#82078=CARTESIAN_POINT ( 'NONE',  ( 5.407694413872749628, -0.8332299576223768378, -1.642021276980778932 ) ) ;
#82079=CARTESIAN_POINT ( 'NONE',  ( 1.418609115998151982, -0.7265329536030593616, -1.877579518606347531 ) ) ;
#82081=CARTESIAN_POINT ( 'NONE',  ( 3.444923099841538772, 1.455166840473320233, 1.779090439993118888 ) ) ;
#82082=CARTESIAN_POINT ( 'NONE',  ( 1.410758858885716061, -1.471193852737593843, 1.139540799010074323 ) ) ;
#82085=CARTESIAN_POINT ( 'NONE',  ( 5.801015586618943232, -0.2871438832755985326, -1.890612906794430614 ) ) ;
#82088=CARTESIAN_POINT ( 'NONE',  ( 4.036730150552261698, -1.818196258471163729, 1.032062162679239892 ) ) ;
#82089=CARTESIAN_POINT ( 'NONE',  ( 1.920565142479381038, 1.744437793965779582, 0.6759427408406930571 ) ) ;
#82092=CARTESIAN_POINT ( 'NONE',  ( 5.829618728418341611, 0.9018330327132916269, -1.605192750430362025 ) ) ;
#82095=CARTESIAN_POINT ( 'NONE',  ( 5.109832884134172026, -1.716065896558026216, 0.1740927981267632318 ) ) ;
#82097=( BOUNDED_CURVE ( )  B_SPLINE_CURVE ( 3, ( #142220, #156313, #188797, #72899 ),
 .UNSPECIFIED., .F., .T. ) 
 B_SPLINE_CURVE_WITH_KNOTS ( ( 4, 4 ),
 ( 0.000000000000000000, 0.5000000000000008882 ),
 .UNSPECIFIED. ) 
 CURVE ( )  GEOMETRIC_REPRESENTATION_ITEM ( )  RATIONAL_B_SPLINE_CURVE ( ( 1.000000000000000222, 0.3333333333333322601, 0.3333333333333334259, 1.000000000000001332 ) ) 
 REPRESENTATION_ITEM ( '' )  );
#82098=CARTESIAN_POINT ( 'NONE',  ( 0.4571073982213811893, -1.631979074848688205, -0.5868837268243607408 ) ) ;
#82102=CARTESIAN_POINT ( 'NONE',  ( 5.067309307786254102, 1.885564733447910646, 1.076134493607887155 ) ) ;
#82103=CARTESIAN_POINT ( 'NONE',  ( 3.053144290054691901, -1.492835736363471888, -1.050712463094093385 ) ) ;
#82104=CARTESIAN_POINT ( 'NONE',  ( 0.6198768371072010952, 1.941228818809427104, -0.2821078022595123747 ) ) ;
#82105=CARTESIAN_POINT ( 'NONE',  ( 5.805892041792804825, -1.178307743425134335, -1.758994673012766574 ) ) ;
#82106=CARTESIAN_POINT ( 'NONE',  ( 5.601222333718593127, -0.5599829797399961118, 2.222829207915150374 ) ) ;
#82110=CARTESIAN_POINT ( 'NONE',  ( 1.787894333202539654, 2.028250040683087008, -0.6185522307536188702 ) ) ;
#82114=CARTESIAN_POINT ( 'NONE',  ( 6.702019227905350540, 0.8390156466466727192, -2.002601388009570549 ) ) ;
#82115=CARTESIAN_POINT ( 'NONE',  ( 6.983263157960365675, 7.629137130509066722, 2.753810918356710769 ) ) ;
#82117=CARTESIAN_POINT ( 'NONE',  ( 1.875925780897500950, 0.3759573520328520768, -2.189106109952672519 ) ) ;
#82118=VERTEX_POINT ( 'NONE', #105450 ) ;
#82119=CARTESIAN_POINT ( 'NONE',  ( 5.783827325522512552, 1.646840809264274119, -1.163266671679111353 ) ) ;
#82121=CARTESIAN_POINT ( 'NONE',  ( 5.453991371731997440, -0.7473993133914544895, 1.922551457666883401 ) ) ;
#82127=CARTESIAN_POINT ( 'NONE',  ( 4.950658015114751009, -1.558304906039936988, -0.9804572199803849308 ) ) ;
#82131=CARTESIAN_POINT ( 'NONE',  ( 1.940065037515970037, 1.705369652917272383, 0.2570983470618106170 ) ) ;
#82132=CARTESIAN_POINT ( 'NONE',  ( 0.3039231887648624619, -1.082844287645868375, -1.700959134490941160 ) ) ;
#82133=CARTESIAN_POINT ( 'NONE',  ( 2.163060705912169812, 1.417378650759585357, 1.809622876518288681 ) ) ;
#82135=CARTESIAN_POINT ( 'NONE',  ( 1.581717252844972998, 2.090516975186909487, -0.8654489506779092789 ) ) ;
#82136=CARTESIAN_POINT ( 'NONE',  ( 3.914754834457169874, 1.489469167258972382, -1.489228550157334574 ) ) ;
#82138=CARTESIAN_POINT ( 'NONE',  ( 3.040057762974816224, 1.755912757559551007, 0.2203070401886226548 ) ) ;
#82144=CARTESIAN_POINT ( 'NONE',  ( 4.816739660502834752, -0.7493216981008001820, -2.091313736985983773 ) ) ;
#82145=CARTESIAN_POINT ( 'NONE',  ( 3.785266741157941262, 1.586943040539133154, 1.511552532079393885 ) ) ;
#82150=CARTESIAN_POINT ( 'NONE',  ( 6.890000000000047642, 4.686644152421160392, 2.842524626796953946 ) ) ;
#82152=CARTESIAN_POINT ( 'NONE',  ( 5.678019686890188211, 2.088907387943875982, -0.3644037002746222664 ) ) ;
#82156=CARTESIAN_POINT ( 'NONE',  ( 6.596550757224428629, -0.5713381284546023009, -2.084776384472402100 ) ) ;
#82158=CARTESIAN_POINT ( 'NONE',  ( 6.444863656277017405, -1.483217659742747996, -1.090817886357238198 ) ) ;
#82161=CARTESIAN_POINT ( 'NONE',  ( 1.469815953039468326, -1.652492729624547962, -0.5465173985150991731 ) ) ;
#82166=CARTESIAN_POINT ( 'NONE',  ( 5.963787895669664607, 2.130530397400759668, -0.3648857593604309391 ) ) ;
#82170=CARTESIAN_POINT ( 'NONE',  ( 4.680646922328831394, -2.095996545452833981, -0.5284188670612932626 ) ) ;
#82174=CARTESIAN_POINT ( 'NONE',  ( 5.764905551123544747, -1.781034818069273884, -0.8454043039353341671 ) ) ;
#82175=CARTESIAN_POINT ( 'NONE',  ( 4.710095198716817144, -1.340344737836828282, -1.099787012688882015 ) ) ;
#82177=CARTESIAN_POINT ( 'NONE',  ( 1.892365914234435120, -0.5883382831698009685, -2.111031122750434808 ) ) ;
#82178=CARTESIAN_POINT ( 'NONE',  ( 3.874305460179793048, 1.279221729648010175, 1.920377363040247420 ) ) ;
#82179=CARTESIAN_POINT ( 'NONE',  ( 5.044241359090890775, 2.054987069614383266, 0.1556004420267612098 ) ) ;
#82180=CARTESIAN_POINT ( 'NONE',  ( 0.09355730106928944467, -1.941490229121365374, -0.04880333718709597285 ) ) ;
#82185=CARTESIAN_POINT ( 'NONE',  ( 3.797228045176269440, -0.2112621354826669517, -2.110076569278092062 ) ) ;
#82187=CARTESIAN_POINT ( 'NONE',  ( 1.125625214514534900, 0.3961039030971893471, 1.976955501819408711 ) ) ;
#82189=CARTESIAN_POINT ( 'NONE',  ( 4.067547972739316897, 0.2730280005818259137, -2.189760481282684967 ) ) ;
#82194=CARTESIAN_POINT ( 'NONE',  ( 6.825078400183551608, 0.5660753733540256905, 2.196387875007102419 ) ) ;
#82197=CARTESIAN_POINT ( 'NONE',  ( 4.522374016017603360, 1.269557654445327532, -1.623317902228790910 ) ) ;
#82201=CARTESIAN_POINT ( 'NONE',  ( 3.791669620513484773, 1.900943035724310448, -0.6826196560621737852 ) ) ;
#82205=CARTESIAN_POINT ( 'NONE',  ( 2.659116476608857305, -1.792500920499852546, -1.016832356063899656 ) ) ;
#82209=CARTESIAN_POINT ( 'NONE',  ( -0.2408018239683913930, 0.6935112996086059134, -2.180753846165773169 ) ) ;
#82210=CARTESIAN_POINT ( 'NONE',  ( 1.165666007907351309, -1.169451938622353859, 1.422036577929463030 ) ) ;
#82211=CARTESIAN_POINT ( 'NONE',  ( 0.2765547061623524483, 1.334074794448695034, 1.882843260577294009 ) ) ;
#82213=CARTESIAN_POINT ( 'NONE',  ( 1.722176697685766200, -1.199285583244277253, -1.798187405066300038 ) ) ;
#82215=CARTESIAN_POINT ( 'NONE',  ( 2.378138974734815392, -2.011451771401792321, -0.1435188914247695346 ) ) ;
#82217=CARTESIAN_POINT ( 'NONE',  ( 1.757567914286566335, -2.287329856776819881, -0.2253975434684113155 ) ) ;
#82219=CARTESIAN_POINT ( 'NONE',  ( 0.3384655940862451029, 0.3152513238553408814, 1.843739016257638141 ) ) ;
#82221=CARTESIAN_POINT ( 'NONE',  ( 4.627780688875618331, -1.211982541104269062, -1.554853849032981072 ) ) ;
#82222=CARTESIAN_POINT ( 'NONE',  ( 4.188685576152741064, 1.555700494002542067, -1.282988152656767911 ) ) ;
#82226=CARTESIAN_POINT ( 'NONE',  ( 6.094376849853386346, -2.095768364502542003, -0.2079484218287275255 ) ) ;
#82227=CARTESIAN_POINT ( 'NONE',  ( 5.266107318980479235, -2.060723932065291031, 0.1993833602659672022 ) ) ;
#82230=CARTESIAN_POINT ( 'NONE',  ( 6.539320575229223387, 6.036367980355456631, 2.598156967962389263 ) ) ;
#82231=CARTESIAN_POINT ( 'NONE',  ( 5.765880396963712684, 0.5824918586248282182, -1.933996001582516611 ) ) ;
#82233=CARTESIAN_POINT ( 'NONE',  ( 3.071242857908276669, -2.132312958082840826, -0.8828933859421483898 ) ) ;
#82234=CARTESIAN_POINT ( 'NONE',  ( 1.411062195701995980, -1.628543573593312921, 1.265665014175233916 ) ) ;
#82241=CARTESIAN_POINT ( 'NONE',  ( 4.035715546050927749, 2.045666111725014780, -0.7279006231073074096 ) ) ;
#82245=CARTESIAN_POINT ( 'NONE',  ( 2.718100415690410721, 1.734538518968967935, 0.6181264464550640936 ) ) ;
#82247=CARTESIAN_POINT ( 'NONE',  ( 3.808297599986898430, 1.548825491099754315, -1.550762550882843094 ) ) ;
#82249=CARTESIAN_POINT ( 'NONE',  ( 5.981380223923965289, 2.093118249296622491, -0.8594570314751952544 ) ) ;
#82254=CARTESIAN_POINT ( 'NONE',  ( 0.07459516483346910476, 0.007201286963451345932, -1.755573347271717655 ) ) ;
#82255=CARTESIAN_POINT ( 'NONE',  ( 3.686192936682455734, 1.120187844794858556, 1.672449120617898410 ) ) ;
#82257=CARTESIAN_POINT ( 'NONE',  ( 2.678859613419749763, -2.014854250346362008, -0.6126693332187698182 ) ) ;
#82258=CARTESIAN_POINT ( 'NONE',  ( 1.669406806874464300, 1.322410700044797327, 1.386144426805105523 ) ) ;
#82260=CARTESIAN_POINT ( 'NONE',  ( 3.174220446822792141, -0.9683065041741106826, -1.714983525329449421 ) ) ;
#82261=CARTESIAN_POINT ( 'NONE',  ( 4.816668504955663899, -0.6845142050268312461, -1.900371106210005712 ) ) ;
#82262=CARTESIAN_POINT ( 'NONE',  ( 0.1099206271272800961, -0.7955684105149689600, -1.691499381818922343 ) ) ;
#82263=CARTESIAN_POINT ( 'NONE',  ( 0.6429252097494702056, -0.2364460082661112295, -1.947484529462916836 ) ) ;
#82264=CARTESIAN_POINT ( 'NONE',  ( 0.3692113334803036606, -1.616751421056546789, -1.021125667832627260 ) ) ;
#82268=CARTESIAN_POINT ( 'NONE',  ( 6.455916552660014851, 1.865467424361374249, -0.1398750677365916961 ) ) ;
#82271=CARTESIAN_POINT ( 'NONE',  ( 6.280147189154119403, -1.145143509460907039, -1.724508502191648862 ) ) ;
#82272=CARTESIAN_POINT ( 'NONE',  ( 0.5200892513525963157, 2.048054262204841880, -0.3022008342252607838 ) ) ;
#82277=CARTESIAN_POINT ( 'NONE',  ( 5.092489908381383934, -1.177591669451777179, 1.763244422785560150 ) ) ;
#82282=CARTESIAN_POINT ( 'NONE',  ( 6.707479306934847507, -1.574971382793718178, -1.169550641929931079 ) ) ;
#82284=CARTESIAN_POINT ( 'NONE',  ( 4.481795959180916888, 1.842165523724150544, 0.8196470798618460396 ) ) ;
#82285=CARTESIAN_POINT ( 'NONE',  ( 3.204202018521628226, 1.211454676919420326, -1.484069150048252350 ) ) ;
#82287=CARTESIAN_POINT ( 'NONE',  ( 1.945129482973105839, -1.762486321751283835, -1.302348873264857820 ) ) ;
#82290=CARTESIAN_POINT ( 'NONE',  ( 3.303821147848403861, -1.868562489643767144, 0.08839296284299941187 ) ) ;
#82295=CARTESIAN_POINT ( 'NONE',  ( 5.817987567751313982, 1.043164272916985214, -1.842315021624504778 ) ) ;
#82298=CARTESIAN_POINT ( 'NONE',  ( 2.331682703721962291, 0.9828498176551370147, -1.845303212725694975 ) ) ;
#82300=CARTESIAN_POINT ( 'NONE',  ( 0.9731894095723004900, 1.663878915475509812, -0.4539961392346722469 ) ) ;
#82309=CARTESIAN_POINT ( 'NONE',  ( 1.752323211514599688, 1.791785093909546323, 0.2653131528348381396 ) ) ;
#82321=CARTESIAN_POINT ( 'NONE',  ( 3.279601929513912939, -1.794223665640673593, 0.4940275889762090200 ) ) ;
#82322=CARTESIAN_POINT ( 'NONE',  ( -0.0005723727212556676321, -1.878494010790388913, 0.3742560964640674892 ) ) ;
#82323=CARTESIAN_POINT ( 'NONE',  ( 6.211935731971203190, -1.911736917912661537, 0.2365620046330171311 ) ) ;
#82330=CARTESIAN_POINT ( 'NONE',  ( 4.153143631030720151, 1.666095859335927187, -1.049822023992821984 ) ) ;
#82331=CARTESIAN_POINT ( 'NONE',  ( 1.541811043186253061, -1.995513645039903361, 0.7175487213698439337 ) ) ;
#82335=CARTESIAN_POINT ( 'NONE',  ( 5.384801694919699067, 1.933943663793664225, -1.030698541907522081 ) ) ;
#82337=CARTESIAN_POINT ( 'NONE',  ( 3.944294614955777600, 1.917013643722576433, 0.1899554498810165082 ) ) ;
#82339=CARTESIAN_POINT ( 'NONE',  ( 0.1471128783409255958, -1.407412912164500263, -1.162481699956314785 ) ) ;
#82340=CARTESIAN_POINT ( 'NONE',  ( 1.366164030173491195, 2.173753390890633685, -0.3800739277931909355 ) ) ;
#82345=CARTESIAN_POINT ( 'NONE',  ( 6.631706394207740551, 1.885626601332585306, -0.5685293109318545479 ) ) ;
#82346=CARTESIAN_POINT ( 'NONE',  ( 2.050241756059832721, -1.499988152044306133, 1.233518166440790598 ) ) ;
#82347=CARTESIAN_POINT ( 'NONE',  ( 6.591202130252849400, 1.331619970128885777, -1.873199602832905430 ) ) ;
#82349=CARTESIAN_POINT ( 'NONE',  ( 4.610102165239228889, 1.860615736367857265, -0.04253844368732987574 ) ) ;
#82352=CARTESIAN_POINT ( 'NONE',  ( 6.509000000000020769, 1.267728212239338736, 2.115804336118334295 ) ) ;
#82355=CARTESIAN_POINT ( 'NONE',  ( 1.822082775007987543, 1.258534617508931586, -1.793986466278547853 ) ) ;
#82360=CARTESIAN_POINT ( 'NONE',  ( 2.139018802738294589, -1.631172329757241801, 0.8201644002571031322 ) ) ;
#82363=CARTESIAN_POINT ( 'NONE',  ( 3.744493841719060967, 1.720499418279351822, -0.2165549783500023973 ) ) ;
#82365=CARTESIAN_POINT ( 'NONE',  ( 6.609000000000053276, 0.5717736360873815205, 2.152148306911850995 ) ) ;
#82367=CARTESIAN_POINT ( 'NONE',  ( 6.692070433991195166, -0.7751425012093198230, 1.651373049820707317 ) ) ;
#82368=CARTESIAN_POINT ( 'NONE',  ( 4.153139481255548660, 1.659551801668930793, -1.045809187271130591 ) ) ;
#82372=CARTESIAN_POINT ( 'NONE',  ( 5.338584462458719315, 1.262900380722062454, -1.703257760751579530 ) ) ;
#82375=CARTESIAN_POINT ( 'NONE',  ( 2.975506508543227291, -0.2074491501150333705, 2.059866449969804503 ) ) ;
#82379=CARTESIAN_POINT ( 'NONE',  ( 3.094664012895144367, -0.4461126415513679833, 2.254854857015383462 ) ) ;
#82383=CARTESIAN_POINT ( 'NONE',  ( 6.720655732516650716, 2.467238681591706673, 2.210725262702870175 ) ) ;
#82388=CARTESIAN_POINT ( 'NONE',  ( 3.902528505893249733, -1.892296425594198750, -0.2755589300712790735 ) ) ;
#82390=CARTESIAN_POINT ( 'NONE',  ( 5.157137038817142916, -1.458691705945897032, -0.9200343150467110709 ) ) ;
#82391=CARTESIAN_POINT ( 'NONE',  ( 3.678922940808615483, 1.700962499606586853, -1.082838980105811366 ) ) ;
#82392=CARTESIAN_POINT ( 'NONE',  ( 5.449893634413335519, -2.076765696135183248, -0.9856196477224605790 ) ) ;
#82394=CARTESIAN_POINT ( 'NONE',  ( 0.2412292383832773390, 0.3817025157030576321, 2.173470055567463088 ) ) ;
#82396=CARTESIAN_POINT ( 'NONE',  ( 5.694547528447587048, -0.4312477495709844399, -1.716266690248748672 ) ) ;
#82398=CARTESIAN_POINT ( 'NONE',  ( 2.414399183035727425, 1.495821068830467615, -1.737032439462746325 ) ) ;
#82399=CARTESIAN_POINT ( 'NONE',  ( 6.615202361034350886, -1.784545987531281019, 0.4526050685512914007 ) ) ;
#82405=CARTESIAN_POINT ( 'NONE',  ( 0.3972422249299937258, 0.3718246657071262451, 2.138946393809169511 ) ) ;
#82406=CARTESIAN_POINT ( 'NONE',  ( 2.852750215419812108, -1.865046845876184189, -0.7672916333427428626 ) ) ;
#82408=CARTESIAN_POINT ( 'NONE',  ( 5.461526653864938297, 0.3736970969714300539, -1.889748759083320406 ) ) ;
#82410=CARTESIAN_POINT ( 'NONE',  ( 2.039591900818237491, 0.005460781979979567602, 2.221583674558536892 ) ) ;
#82417=CARTESIAN_POINT ( 'NONE',  ( 4.933026880143430049, -1.235701381803285148, -1.225916536586797667 ) ) ;
#82418=CARTESIAN_POINT ( 'NONE',  ( 3.420314466093795414, 0.8798059112791326575, 1.753580237611163994 ) ) ;
#82422=CARTESIAN_POINT ( 'NONE',  ( 5.061948053633171796, 2.238818834584723749, -0.3250485201948364877 ) ) ;
#82423=CARTESIAN_POINT ( 'NONE',  ( 0.9595213787957155294, 1.685235279958563037, 1.189114231603551675 ) ) ;
#82426=CARTESIAN_POINT ( 'NONE',  ( 2.378104638162964246, 1.391771292293322082, 1.783738300129237508 ) ) ;
#82429=CARTESIAN_POINT ( 'NONE',  ( 2.934663490303309530, 0.2251962677765201870, 1.856852477824536329 ) ) ;
#82430=CARTESIAN_POINT ( 'NONE',  ( 1.722904486866124962, 1.715286564835089456, 0.2538950934896730405 ) ) ;
#82431=CARTESIAN_POINT ( 'NONE',  ( 5.513277522340928272, -2.138352208816508782, 0.4792397250529822905 ) ) ;
#82432=CARTESIAN_POINT ( 'NONE',  ( 6.405331179067034419, 1.913585160600343782, 1.289386977092843889 ) ) ;
#82433=CARTESIAN_POINT ( 'NONE',  ( 1.745067373267340960, -1.741593738584124695, 1.101550882630119244 ) ) ;
#82434=CARTESIAN_POINT ( 'NONE',  ( 4.048723784538146298, -1.615201170136868924, -1.077811959465636571 ) ) ;
#82436=CARTESIAN_POINT ( 'NONE',  ( 6.837182164354378422, -1.670574593475544489, 0.8415915117672703172 ) ) ;
#82437=CARTESIAN_POINT ( 'NONE',  ( 1.437500000000001110, 1.451031289061064156, -1.451031289061176288 ) ) ;
#82439=CARTESIAN_POINT ( 'NONE',  ( 6.485703859413265882, 1.880147802650249611, 0.7282652505391642439 ) ) ;
#82441=CARTESIAN_POINT ( 'NONE',  ( 4.887342357109405455, -0.6819942819097268849, -1.897698409216505233 ) ) ;
#82445=CARTESIAN_POINT ( 'NONE',  ( 2.613660848560446226, -1.805822647967849193, 0.2677728182119283318 ) ) ;
#82453=B_SPLINE_CURVE_WITH_KNOTS ( 'NONE', 3,
 ( #32469, #16188, #62833, #211208, #33530, #178740, #145202, #63902, #64953, #128994, #147302, #182975, #199205, #83333, #15133, #131104, #197093, #146254, #17257, #130058, #47684, #95373, #163549, #179798, #96439, #50852, #46608, #14063, #180845, #148365, #81221, #48733, #80149, #31417, #67065, #97493, #212268, #198150, #161424, #114846, #99601, #82271, #214364, #133202, #65994, #132144, #149418, #79083, #49782, #116978, #13007, #38868, #101731, #37800, #104953, #70268, #169924, #72413, #86549, #184036, #121267, #187242, #85479, #56187, #166739, #36718, #134268, #118051, #22592, #103875, #120190, #35652, #2063, #122347, #102805, #54054, #185092, #152614, #135321, #69202, #21509, #100662, #52975, #186166, #201336, #84413, #68135, #20464, #136383, #18332, #170993, #168861, #137452, #151565, #4198, #150503, #119112, #55121, #200275, #202401, #204538, #51926, #87618, #153690, #88698, #154757, #5259, #19398, #71335, #6341, #203466, #138514, #3132, #34592, #167801, #107131, #192561, #205615, #77757, #76689, #176340, #156900, #110337, #27946, #106052, #8488, #143879, #140674, #208808, #94042, #160081, #57255, #92974, #39945, #7409, #209872, #126598, #61511, #157970, #125536, #43163, #89778, #60439, #123415, #23668, #74572, #9561, #155825, #25803, #188303, #172076, #11683, #108206, #91912, #75637, #24736, #44216, #206689, #58318, #175285, #73491, #124475, #189379, #139591, #41022, #173154, #59380, #26871, #174228, #141745, #90837, #190432, #42091, #207753, #191496, #142804, #109276, #159019, #10613, #729, #46344, #197891, #163284, #48478, #165400, #179538, #62567, #214108, #111399, #30081, #130844, #128731, #131882, #194703, #196838, #144937, #33265, #148105, #114595, #180586, #115641, #129800, #147048, #63643, #31158, #13811, #162224, #32209, #96173, #99348, #213070, #95103, #79882, #29018, #210942, #98283, #97230, #14867, #80956, #64701, #161151, #195780, #193636, #145992, #65735, #12739, #212004, #83072, #127676, #47417, #164342, #16996, #113532, #15930, #78813, #45278, #149149, #112461, #177403, #82014, #178471, #49520, #181637, #74052, #84150, #173712, #172627, #57797, #38345, #5808, #88166, #105507, #91389, #139064, #104422, #25289, #166469, #132934, #100402, #170470, #54596, #18062, #157449, #7960, #66795, #39412, #6883, #205091, #34327, #182708, #156376, #150236, #116708, #22056, #171539, #1806, #121814, #198941, #50585, #123957, #204011, #23132, #67864, #137993, #55658, #154236, #140143, #136926, #187782, #71884, #202954, #120744, #186718, #89249, #155300, #122900, #72962, #56732, #188859, #40496, #189925, #90307, #206167, #106600, #24204, #41570, #107684, #58861, #42642, #209351, #110880, #75119, #79382, #11160, #111957, #126080, #159564, #141229, #43704, #29575, #125019, #143355, #94589, #207238, #27423, #128230, #211499, #95665, #127153, #208292, #210432, #195273, #176886, #60999, #59925, #192041, #76176, #142282, #13309, #26350, #113023, #62073, #193125, #109822, #145501, #63134, #190975, #175833, #179031, #93522, #161717, #129298, #46907, #92466, #194193, #108751, #174775, #30649, #96733, #9044, #44773, #77238, #28497, #160631, #12232, #78306, #158503, #10102, #144430, #45837, #177960, #47982, #97786, #163848, #17549, #167038, #116211, #35955, #16489, #82570, #32766, #149721, #162783, #64207, #164896, #198443, #99904 ),
 .UNSPECIFIED., .F., .F.,
 ( 4, 1, 1, 1, 1, 1, 1, 1, 1, 1, 1, 1, 1, 1, 1, 1, 1, 1, 1, 1, 1, 1, 1, 1, 1, 1, 1, 1, 1, 1, 1, 1, 1, 1, 1, 1, 1, 1, 1, 1, 1, 1, 1, 1, 1, 1, 1, 1, 1, 1, 1, 1, 1, 1, 1, 1, 1, 1, 1, 1, 1, 1, 1, 1, 1, 1, 1, 1, 1, 1, 1, 1, 1, 1, 1, 1, 1, 1, 1, 1, 1, 1, 1, 1, 1, 1, 1, 1, 1, 1, 1, 1, 1, 1, 1, 1, 1, 1, 1, 1, 1, 1, 1, 1, 1, 1, 1, 1, 1, 1, 1, 1, 1, 1, 1, 1, 1, 1, 1, 1, 1, 1, 1, 1, 1, 1, 1, 1, 1, 1, 1, 1, 1, 1, 1, 1, 1, 1, 1, 1, 1, 1, 1, 1, 1, 1, 1, 1, 1, 1, 1, 1, 1, 1, 1, 1, 1, 1, 1, 1, 1, 1, 1, 1, 1, 1, 1, 1, 1, 1, 1, 1, 1, 1, 1, 1, 1, 1, 1, 1, 1, 1, 1, 1, 1, 1, 1, 1, 1, 1, 1, 1, 1, 1, 1, 1, 1, 1, 1, 1, 1, 1, 1, 1, 1, 1, 1, 1, 1, 1, 1, 1, 1, 1, 1, 1, 1, 1, 1, 1, 1, 1, 1, 1, 1, 1, 1, 1, 1, 1, 1, 1, 1, 1, 1, 1, 1, 1, 1, 1, 1, 1, 1, 1, 1, 1, 1, 1, 1, 1, 1, 1, 1, 1, 1, 1, 1, 1, 1, 1, 1, 1, 1, 1, 1, 1, 1, 1, 1, 1, 1, 1, 1, 1, 1, 1, 1, 1, 1, 1, 1, 1, 1, 1, 1, 1, 1, 1, 1, 1, 1, 1, 1, 1, 1, 1, 1, 1, 1, 1, 1, 1, 1, 1, 1, 1, 1, 1, 1, 1, 1, 1, 1, 1, 1, 1, 1, 1, 1, 1, 1, 1, 1, 1, 1, 1, 1, 1, 1, 1, 1, 1, 1, 1, 1, 1, 1, 1, 1, 1, 1, 1, 1, 1, 1, 1, 1, 1, 1, 1, 1, 1, 1, 1, 1, 1, 1, 1, 1, 1, 1, 1, 1, 1, 1, 1, 1, 1, 1, 1, 1, 1, 1, 1, 1, 1, 1, 1, 1, 1, 1, 1, 1, 1, 4 ),
 ( 0.000000000000000000, 0.002599974731368114196, 0.005208790931971673047, 0.007813145979665977320, 0.01041652777592116073, 0.01302061325022423749, 0.01562498222773845216, 0.01822909327250534645, 0.02083329118620782031, 0.02343750764584028035, 0.02604160881127103033, 0.02864587273906003470, 0.03124992668191499748, 0.03385418289307650513, 0.03645825757725845717, 0.03906249379052053466, 0.04166666320740203266, 0.04427081823557592333, 0.04687506849204003262, 0.04947913642841410276, 0.05208339700068515682, 0.05468745344639398126, 0.05729170333903113588, 0.05989581325979084075, 0.06250002080062810883, 0.06510424464624173235, 0.06770834408375023261, 0.07031260355790951155, 0.07291665769283758869, 0.07552091454841564078, 0.07812498837240108851, 0.08072922377910608793, 0.08333339284475561881, 0.08593754734057650058, 0.08854179710653446722, 0.09114586450482109470, 0.09375012458370637902, 0.09635418052565795921, 0.09895842987840544613, 0.1015625393267825388, 0.1041667463075427041, 0.1067709697059155277, 0.1093750686050062593, 0.1119793276133541904, 0.1145833812402851093, 0.1171876375884709082, 0.1197917109360151500, 0.1223959458003068407, 0.1250001144218755300, 0.1276042683764700425, 0.1302085177025434359, 0.1328125845892443313, 0.1354168441945610146, 0.1380208996559441903, 0.1406251484930516882, 0.1432292574929059925, 0.1458334639374244401, 0.1484376869122458475, 0.1510417852965526830, 0.1536460438630466996, 0.1562500970055218374, 0.1588543528702505148, 0.1614584257649260002, 0.1640626601106844606, 0.1666668283118819260, 0.1692709817489688462, 0.1718752306590244638, 0.1744792970577103974, 0.1770835562133957763, 0.1796876112177483997, 0.1822918595631332073, 0.1848959681380851483, 0.1875001740701665309, 0.1901043966452301559, 0.1927084945383780445, 0.1953127526869259389, 0.1979168053684795814, 0.2005210607736844508, 0.2031251332390507092, 0.2057293670901427229, 0.2083335348946688259, 0.2109376878379560227, 0.2135419363558502259, 0.2161460022900811573, 0.2187502610200618980, 0.2213543155909112325, 0.2239585634684796434, 0.2265626716421396125, 0.2291668770855771753, 0.2317710992846666596, 0.2343751967102698508, 0.2369794544647692847, 0.2395835067089256143, 0.2421877616785296505, 0.2447918337381362330, 0.2473960671184182170, 0.2500002345499632850, 0.2526043870231480248, 0.2552086351727278490, 0.2578127006660536624, 0.2604169589942467167, 0.2630210131551104502, 0.2656252605887587936, 0.2682293683847277177, 0.2708335733633049913, 0.2734377952101950116, 0.2760418921918580404, 0.2786461495761977103, 0.2812502014064713896, 0.2838544559643880194, 0.2864585276417753179, 0.2890627605750938911, 0.2916669276573394809, 0.2942710796841097043, 0.2968753274892133587, 0.2994793925651746958, 0.3020836505154881335, 0.3046877042898750165, 0.3072919513034905736, 0.3098960587453611915, 0.3125002632828523530, 0.3151044848013095923, 0.3177085813626279731, 0.3203128384006882490, 0.3229168898405855304, 0.3255211440107198539, 0.3281252153294201834, 0.3307294478396133885, 0.3333336145962333963, 0.3359377662002681064, 0.3385420136847264727, 0.3411460783668558427, 0.3437503359631899347, 0.3463543893746011126, 0.3489586359920627823, 0.3515627431034201722, 0.3541669472235909888, 0.3567711684373747749, 0.3593752646019360286, 0.3619795213175900916, 0.3645835723906095116, 0.3671878261968588575, 0.3697918971803975663, 0.3723961292912953969, 0.3750002957459567798, 0.3776044469509276524, 0.3802086941385645069, 0.3828127584503868142, 0.3854170157166348365, 0.3880210687885642384, 0.3906253150337437030, 0.3932294218381663375, 0.3958336255647753599, 0.3984378464976386924, 0.4010419422890235119, 0.4036461987061379930, 0.4062502494357712601, 0.4088545029020263510, 0.4114585735739221262, 0.4140628053093475813, 0.4166669714857112461, 0.4192711223152827404, 0.4218753692299160307, 0.4244794331949501842, 0.4270836901549991405, 0.4296877429109347002, 0.4322919888076972583, 0.4348960953287579478, 0.4375002986855570652, 0.4401045193612476147, 0.4427086148030301427, 0.4453128709454660106, 0.4479169213551993378, 0.4505211745053449013, 0.4531252448891109341, 0.4557294762728811288, 0.4583336421946030970, 0.4609377926724337327, 0.4635420393378766879, 0.4661461029796354349, 0.4687503596573671660, 0.4713544121207915438, 0.4739586576929967765, 0.4765627639542633909, 0.4791669669649988861, 0.4817711874072597711, 0.4843752825230089321, 0.4869795384146229367, 0.4895835885279371524, 0.4921878413858530310, 0.4947919115049980165, 0.4973961425609249032, 0.5000003082516567554, 0.5026044584014001115, 0.5052087048414615200, 0.5078127681834534446, 0.5104170246027455171, 0.5130210767971369323, 0.5156253220686399796, 0.5182294280936764475, 0.5208336307820899957, 0.5234378510146604491, 0.5260419458279406157, 0.5286462014925853437, 0.5312502513329574461, 0.5338545039225196520, 0.5364585738005485105, 0.5390628045524396006, 0.5416669700358295314, 0.5442711198811350792, 0.5468753661196208427, 0.5494794291853500878, 0.5520836853700766822, 0.5546877373189100791, 0.5572919823135623618, 0.5598960881259297251, 0.5625002905157588939, 0.5651045105623757614, 0.5677086050967478092, 0.5703128605582734600, 0.5729169101491768945, 0.5755211624942581095, 0.5781252321546730411, 0.5807294626263322934, 0.5833336279260263879, 0.5859377774905402125, 0.5885420235512536236, 0.5911460863642216124, 0.5937503423382545220, 0.5963543940650019026, 0.5989586388066517886, 0.6015627444299086468, 0.6041669465448881171, 0.6067711664292861906, 0.6093752607083083861, 0.6119795159905627724, 0.6145835653554690969, 0.6171878174799397820, 0.6197918869462408775, 0.6223961171614702526, 0.6250002823011129305, 0.6276044316084782304, 0.6302086775152213605, 0.6328127400989277396, 0.6354169958861367595, 0.6380210474142689048, 0.6406252919267632073, 0.6432293973844667168, 0.6458335992483292820, 0.6484378189942425763, 0.6510419130414711875, 0.6536461681683013447, 0.6562502173306804520, 0.6588544692584096252, 0.6614585385540960871, 0.6640627685366956579, 0.6666669335399304508, 0.6692710826137896474, 0.6718753283903641238, 0.6744793907683068745, 0.6770836463925611337, 0.6796876977455479363, 0.6822919420527318035, 0.6848960473684391204, 0.6875002490049163528, 0.6901044686360783276, 0.6927085624750688453, 0.6953128174703216979, 0.6979168664536427036, 0.7005211182084990496, 0.7031251873570698585, 0.7057294171308388098, 0.7083335820213095824, 0.7109377308853042088, 0.7135419765555117699, 0.7161460387511890957, 0.7187502942363581671, 0.7213543454376690756, 0.7239585895633880996, 0.7265626947606567132, 0.7291668961934797411, 0.7317711157336249661, 0.7343752093879328813, 0.7369794642754557978, 0.7395835131031885945, 0.7421877647090413532, 0.7447918337339959338, 0.7473960633227341166, 0.7500002281240860658, 0.7526043768018576552, 0.7552086223895014827, 0.7578126844264116979, 0.7604169397963658206, 0.7630209908694718379, 0.7656252348375721661, 0.7682293399399604539, 0.7708335411928610714, 0.7734377606657260040, 0.7760418541589074737, 0.7786461089625497101, 0.7812501576581653007, 0.7838544091388848223, 0.7864584780637244865, 0.7890627074912324179, 0.7916668722271122949, 0.7942710207423038238, 0.7968752662711893198, 0.7994793281728324041, 0.8020835834514440377, 0.8046876344198176101, 0.8072918782541467220, 0.8098959832852158369, 0.8125001843819276148, 0.8151044038112509327, 0.8177084971668638902, 0.8203127519104773668, 0.8229168004974481976, 0.8255210518769072747, 0.8281251207251358881, 0.8307293500152160837, 0.8333335147092740813, 0.8359376630855301915, 0.8385419085794658667, 0.8411459703693440204, 0.8437502255804886220, 0.8463542764676049712, 0.8489585201920134550, 0.8515626251753276588, 0.8541668261395859441, 0.8567710455491102106, 0.8593751387907155870, 0.8619793934981552219, 0.8645834419999574028, 0.8671876933020320477, 0.8697917620971562513, 0.8723959912736143352, 0.8750001559495040881, 0.8776043042104727521, 0.8802085496932706699, 0.8828126113948897569, 0.8854168665624462253, 0.8880209173917842369, 0.8906251610301256783, 0.8932292659892527853, 0.8958334668447968108, 0.8984376862582688084, 0.9010417794094305322, 0.9036460341045560174, 0.9062500825446693220, 0.9088543337932389887, 0.9114584025587700866, 0.9140626316454156797, 0.9166667963267953745, 0.9192709444961273402, 0.9218751899916067805, 0.9244792516284782158, 0.9270835067763207871, 0.9296875575713596795, 0.9322918011475309630, 0.9348959061060417852, 0.9375001068764983181, 0.9401043263176916964, 0.9427084194022110619, 0.9453126741091559815, 0.9479167225106870376, 0.9505209737258253355, 0.9531250424882484751, 0.9557292715345466760, 0.9583334362123939743, 0.9609375841976093291, 0.9635418299546441023, 0.9661458919105455623, 0.9687501459642621215, 0.9713541960184646218, 0.9739584433044384815, 0.9765625494917742344, 0.9791667425299969141, 0.9817709508269629737, 0.9843750450459556323, 0.9869794226472197174, 0.9895834977571079660, 0.9921868632736227100, 0.9947912224625704569, 0.9974000159472320437, 1.000000000000000000 ),
 .UNSPECIFIED. ) ;
#82455=CARTESIAN_POINT ( 'NONE',  ( 0.0002682147194760230472, -0.9481790448457677600, 1.783359508359374512 ) ) ;
#82456=CARTESIAN_POINT ( 'NONE',  ( 0.1883438084668061507, 1.224518555304452416, 1.730999496979759300 ) ) ;
#82457=EDGE_LOOP ( 'NONE', ( #33681, #191866, #26945, #205378 ) ) ;
#82460=CARTESIAN_POINT ( 'NONE',  ( 6.104382415481349966, -0.7394567487006579176, -1.923849829731038019 ) ) ;
#82461=CARTESIAN_POINT ( 'NONE',  ( 4.570935502227962743, -0.9480417383296577682, 1.779625852769653127 ) ) ;
#82470=CARTESIAN_POINT ( 'NONE',  ( 5.220077296912079667, -1.701688162634030999, -1.080898591909580597 ) ) ;
#82471=CARTESIAN_POINT ( 'NONE',  ( 4.382634408885896171, 1.643497958660003144, -0.8300281608688080404 ) ) ;
#82473=CARTESIAN_POINT ( 'NONE',  ( 3.334905300413065543, 2.251431139208215804, 0.5058342958955232005 ) ) ;
#82475=CARTESIAN_POINT ( 'NONE',  ( 5.624359561864977763, 1.292596479719224645, -1.732379065785584871 ) ) ;
#82477=CARTESIAN_POINT ( 'NONE',  ( 1.434995430731567101, -1.407912642168735573, -1.337921467293776923 ) ) ;
#82479=CARTESIAN_POINT ( 'NONE',  ( 4.938965133657190698, 1.317805461337580697, 1.882938791714399374 ) ) ;
#82482=CARTESIAN_POINT ( 'NONE',  ( 3.731198135974967300, -1.728734619261709904, 0.7151963084984153118 ) ) ;
#82485=CARTESIAN_POINT ( 'NONE',  ( 1.283307755816986528, 0.1377011610334301639, -1.907463248872851569 ) ) ;
#82488=CARTESIAN_POINT ( 'NONE',  ( 2.702037527177497012, -0.6914408288211832954, 2.095836555436859872 ) ) ;
#82489=CARTESIAN_POINT ( 'NONE',  ( 6.883263157960371359, 7.052674735402435502, 2.544342468817725855 ) ) ;
#82494=CARTESIAN_POINT ( 'NONE',  ( 0.6144489392437714192, 1.362578290646492718, -1.424861684082868063 ) ) ;
#82495=CARTESIAN_POINT ( 'NONE',  ( 6.721333375000203780, -0.1674226297891309168, 2.271100132491596479 ) ) ;
#82496=CARTESIAN_POINT ( 'NONE',  ( 1.592165322863370980, 0.9698756732311950568, -1.705302290208744687 ) ) ;
#82497=CARTESIAN_POINT ( 'NONE',  ( 5.155161738035724639, 1.717805270433828246, -1.141362358335789251 ) ) ;
#82504=CARTESIAN_POINT ( 'NONE',  ( 0.6378409936122396706, 2.026330576540099404, -0.7799181171992456418 ) ) ;
#82509=CARTESIAN_POINT ( 'NONE',  ( 1.581098268704693055, 1.730367963306264301, -0.7109649657882493035 ) ) ;
#82510=CARTESIAN_POINT ( 'NONE',  ( 5.624359561864977763, 1.292596479719224645, -1.732379065785584871 ) ) ;
#82515=CARTESIAN_POINT ( 'NONE',  ( 1.102048709075389876, -0.8591247869965330519, 1.708478583560539166 ) ) ;
#82516=CARTESIAN_POINT ( 'NONE',  ( 2.781836775232096048, -0.9115585761545975663, 1.516887842838773759 ) ) ;
#82517=CARTESIAN_POINT ( 'NONE',  ( 0.2758376730330712734, 1.891454726169951250, -0.2806862973558504892 ) ) ;
#82519=CARTESIAN_POINT ( 'NONE',  ( 5.097249261280999200, -0.2764669589378037085, 1.895409748447648202 ) ) ;
#82520=CARTESIAN_POINT ( 'NONE',  ( 6.883263157960362477, -0.001323150302089473379, 1.953658984494692330 ) ) ;
#82523=CARTESIAN_POINT ( 'NONE',  ( 1.143014088299774578, 2.045220145331683614, 0.5602274146137007360 ) ) ;
#82525=CARTESIAN_POINT ( 'NONE',  ( 3.625732356982212412, -1.113523340526129335, -1.502988901547596567 ) ) ;
#82526=CARTESIAN_POINT ( 'NONE',  ( 0.6447967512687136082, -1.567379569643694515, 0.9359695128687425258 ) ) ;
#82528=CARTESIAN_POINT ( 'NONE',  ( 4.565167970240332274, -1.970479184476851886, -0.9938812724585781577 ) ) ;
#82532=CARTESIAN_POINT ( 'NONE',  ( 2.137244103193221889, -0.09901990427806567352, -2.060404765751827405 ) ) ;
#82539=CARTESIAN_POINT ( 'NONE',  ( 4.422371208857902580, 0.9731212702417373350, 1.827393648576709717 ) ) ;
#82541=CARTESIAN_POINT ( 'NONE',  ( 2.020999711022552159, 2.016103727727487804, 0.7800470891412072394 ) ) ;
#82543=CARTESIAN_POINT ( 'NONE',  ( 2.315108654539797861, 1.620709295712051246, -1.204917113890991320 ) ) ;
#82549=CARTESIAN_POINT ( 'NONE',  ( 6.883263157960362477, -0.004191378316371896506, 2.053658919477070910 ) ) ;
#82550=CARTESIAN_POINT ( 'NONE',  ( 0.4621254960020632074, -1.116205757145168231, 1.679226196708947239 ) ) ;
#82551=CARTESIAN_POINT ( 'NONE',  ( 6.539320575229274901, 4.692178491785949923, 2.665866134390063813 ) ) ;
#82552=CARTESIAN_POINT ( 'NONE',  ( 5.232042516939362287, 2.159042084939459816, 0.3751777721049884273 ) ) ;
#82554=CARTESIAN_POINT ( 'NONE',  ( 3.322422747544371280, -0.7792853099402965444, -1.746611395919236642 ) ) ;
#82558=CARTESIAN_POINT ( 'NONE',  ( 1.985954055300429566, -2.015913623055834325, 0.05231662700833779323 ) ) ;
#82561=CARTESIAN_POINT ( 'NONE',  ( 0.1699995558098127968, 1.326729642492694872, 1.869266897796989291 ) ) ;
#82563=CARTESIAN_POINT ( 'NONE',  ( 3.979312383816283383, 1.623897443016858011, -0.5815980338331677713 ) ) ;
#82564=CARTESIAN_POINT ( 'NONE',  ( 0.1405533004714799583, 4.081756738537394291, -2.834601852798774413 ) ) ;
#82566=CARTESIAN_POINT ( 'NONE',  ( 0.3736316133628529434, 1.073300769168658686, 1.531925686032776124 ) ) ;
#82568=CARTESIAN_POINT ( 'NONE',  ( 0.1751657365761703222, 0.2353161675953834020, -2.077853038718394885 ) ) ;
#82570=CARTESIAN_POINT ( 'NONE',  ( 0.3388458784313007066, -2.007247006727829852, -0.5063607812752639603 ) ) ;
#82572=CARTESIAN_POINT ( 'NONE',  ( 5.549399115596888699, -1.634990982212698230, 0.7802194360074166113 ) ) ;
#82576=CARTESIAN_POINT ( 'NONE',  ( 5.549399115596888699, -1.634990982212698230, 0.7802194360074166113 ) ) ;
#82582=CARTESIAN_POINT ( 'NONE',  ( 6.637149568644561626, -0.09269223384644230401, -1.858852300295941395 ) ) ;
#82584=CARTESIAN_POINT ( 'NONE',  ( 3.690956203553748427, 1.644769065816154008, 0.9816995294186120491 ) ) ;
#82590=CARTESIAN_POINT ( 'NONE',  ( 5.735599800244862045, 0.6120854273203913953, -2.026975329707622731 ) ) ;
#82591=CARTESIAN_POINT ( 'NONE',  ( 0.4444780689869810564, 2.156031605563761833, 0.1575401717312311101 ) ) ;
#82595=CARTESIAN_POINT ( 'NONE',  ( 0.9557436305893592943, 1.823730570757615022, -0.08488363409227267509 ) ) ;
#82597=CARTESIAN_POINT ( 'NONE',  ( 3.117977517195897441, -0.8984765085307615529, -1.589086709143338272 ) ) ;
#82599=CARTESIAN_POINT ( 'NONE',  ( 2.795058504854182946, -0.1448928079688660830, -1.906987441340234568 ) ) ;
#82601=CARTESIAN_POINT ( 'NONE',  ( 2.892966452247947906, 0.2382023302623069438, 1.955005545544076240 ) ) ;
#82602=CARTESIAN_POINT ( 'NONE',  ( 4.704598389810739079, 1.691404259434112767, 0.9541841752371772456 ) ) ;
#82605=CARTESIAN_POINT ( 'NONE',  ( 5.220985865760717992, 1.604251394084664550, -1.386888226476624242 ) ) ;
#82607=CARTESIAN_POINT ( 'NONE',  ( 2.719282321824310511, 1.616554633311767297, 1.021241153818429614 ) ) ;
#82612=CARTESIAN_POINT ( 'NONE',  ( 4.336591701909254581, 1.236597081578957757, -1.588450131361287987 ) ) ;
#82614=CARTESIAN_POINT ( 'NONE',  ( 4.652862234063231739, -1.464609733205827879, 1.089778014065109657 ) ) ;
#82615=CARTESIAN_POINT ( 'NONE',  ( 0.4146172280090759665, 0.7909515328246279342, 1.913518691844050323 ) ) ;
#82619=CARTESIAN_POINT ( 'NONE',  ( 5.330866702616011921, 0.1386157390740362649, 1.865562100978317206 ) ) ;
#82629=CARTESIAN_POINT ( 'NONE',  ( 0.3739936534635743270, -2.030981289472892026, 0.4004457479018645460 ) ) ;
#82630=CARTESIAN_POINT ( 'NONE',  ( 1.775175926465226039, 1.840253878465339055, -1.046873989079605050 ) ) ;
#82634=CARTESIAN_POINT ( 'NONE',  ( 6.244996659533327943, -0.2978818936431072983, -2.048576297084458098 ) ) ;
#82639=CARTESIAN_POINT ( 'NONE',  ( 3.047136720273002641, -1.874302040764055599, -1.319397901421492714 ) ) ;
#82640=CARTESIAN_POINT ( 'NONE',  ( 0.08226035653636187828, -1.769965142718381124, -0.4472663993063328847 ) ) ;
#82641=CARTESIAN_POINT ( 'NONE',  ( -0.1409997244346088141, -0.002808977843308038680, -2.000147647483838220 ) ) ;
#82642=CARTESIAN_POINT ( 'NONE',  ( 2.707167837304753633, 1.638089068140319071, -0.9866689735503200165 ) ) ;
#82646=CARTESIAN_POINT ( 'NONE',  ( 0.2111898618733127897, 1.671471951565723035, -1.121848769376234234 ) ) ;
#82647=CARTESIAN_POINT ( 'NONE',  ( 1.182386158793121256, 1.172985831986381955, -1.572276950389992933 ) ) ;
#82648=CARTESIAN_POINT ( 'NONE',  ( 0.2335667940002684739, 0.001055507091213010252, -2.153566573614831281 ) ) ;
#82651=CARTESIAN_POINT ( 'NONE',  ( 3.398458197991469643, 1.647775209707361466, -1.286576258924768235 ) ) ;
#82652=CARTESIAN_POINT ( 'NONE',  ( 2.430210232679584248, 1.715968397599322737, 0.4327865170333042300 ) ) ;
#82655=CARTESIAN_POINT ( 'NONE',  ( 5.683585447934278001, -1.035311694948486183, 2.045203486727443121 ) ) ;
#82656=CARTESIAN_POINT ( 'NONE',  ( 3.978220273661048356, -0.1731065449946489199, -1.731690827559639878 ) ) ;
#82659=CARTESIAN_POINT ( 'NONE',  ( 2.969770354771487320, 1.463018481607085475, 0.9301108516524180247 ) ) ;
#82660=CARTESIAN_POINT ( 'NONE',  ( 5.195835581519938629, -1.531768914234220347, -1.538983792029069209 ) ) ;
#82662=CARTESIAN_POINT ( 'NONE',  ( 6.104703911763087909, 1.883310800321544409, 0.7212973825745233603 ) ) ;
#82663=CARTESIAN_POINT ( 'NONE',  ( 6.656247777566118629, -1.895918425136842833, 0.7852924748303453661 ) ) ;
#82665=CARTESIAN_POINT ( 'NONE',  ( 1.729391032145210394, -1.814785505609041838, 0.6465514451386763506 ) ) ;
#82667=CARTESIAN_POINT ( 'NONE',  ( 5.519863322019965324, -0.5397129975505778887, 2.154757917147765323 ) ) ;
#82669=CARTESIAN_POINT ( 'NONE',  ( 6.883263157960368694, 4.693146704925188040, 2.608790034323371643 ) ) ;
#82673=CARTESIAN_POINT ( 'NONE',  ( 1.911064425300706526, -0.5960121562160587416, -2.139774337300159424 ) ) ;
#82674=CARTESIAN_POINT ( 'NONE',  ( 6.391066755906244623, 0.1909826923555627554, 1.952524381009380861 ) ) ;
#82680=CARTESIAN_POINT ( 'NONE',  ( 4.229007335028351910, -1.923526752047514110, -0.7451934795693700986 ) ) ;
#82685=CARTESIAN_POINT ( 'NONE',  ( 5.712129104542990277, -0.8404194184173617854, -1.671158263034502767 ) ) ;
#82686=CARTESIAN_POINT ( 'NONE',  ( 4.641094080744356809, 0.6698209448141523303, 1.599790421982680400 ) ) ;
#82687=CARTESIAN_POINT ( 'NONE',  ( 4.159493969870859509, 0.8249727819007621754, 1.532509256507504025 ) ) ;
#82689=CARTESIAN_POINT ( 'NONE',  ( 1.523386150502318737, -2.156637510313658801, 0.7774349738483375960 ) ) ;
#82691=CARTESIAN_POINT ( 'NONE',  ( 5.196857871947656804, 1.709930586799845553, 1.202785367055765775 ) ) ;
#82692=CARTESIAN_POINT ( 'NONE',  ( 0.8492453639068753279, 1.839163117542693904, -0.08803940487626948919 ) ) ;
#82695=CARTESIAN_POINT ( 'NONE',  ( 1.740861508391436274, 2.010826320759526720, -0.1511413081683593562 ) ) ;
#82700=CARTESIAN_POINT ( 'NONE',  ( 1.346235217667652417, -0.9325981557438846048, 1.848514419461377845 ) ) ;
#82703=CARTESIAN_POINT ( 'NONE',  ( 3.071057173463411338, -1.604308532545582366, 1.386676294644908936 ) ) ;
#82705=CARTESIAN_POINT ( 'NONE',  ( 5.373610676068619973, 1.758448663713826132, -0.4906839848310071139 ) ) ;
#82714=CARTESIAN_POINT ( 'NONE',  ( 3.445573674754712545, -1.864599547292019155, 0.7769016540176328922 ) ) ;
#82715=CARTESIAN_POINT ( 'NONE',  ( 6.686557766011572923, -2.162873314485185272, -0.4371622687903350957 ) ) ;
#82718=CARTESIAN_POINT ( 'NONE',  ( 4.733164070488131259, 0.002922519798398153738, -1.861131630917359336 ) ) ;
#82724=CARTESIAN_POINT ( 'NONE',  ( 0.1280963075596490419, -1.331634228802502928, -1.703589906866372017 ) ) ;
#82728=CARTESIAN_POINT ( 'NONE',  ( 1.791952614948258304, -1.634470817638247642, 0.5789770405969245637 ) ) ;
#82729=CARTESIAN_POINT ( 'NONE',  ( 1.394060603838151779, 1.424319145653055507, -0.9997159833949519347 ) ) ;
#82731=CARTESIAN_POINT ( 'NONE',  ( 6.393248246410252911, 2.011339380631727458, -1.131280203180404342 ) ) ;
#82734=CARTESIAN_POINT ( 'NONE',  ( 2.108734400483037952, 1.529077776457531401, -1.381789073784354560 ) ) ;
#82736=COLOUR_RGB ( '', 0.40784314, 0.44705882, 0.49803922) ;
#82738=CARTESIAN_POINT ( 'NONE',  ( 1.669295836627190610, -0.7230268306642473330, -1.882186858670406693 ) ) ;
#82741=CARTESIAN_POINT ( 'NONE',  ( 0.5496082175940236736, 0.6205544711120424273, -1.871312427623121000 ) ) ;
#82742=CARTESIAN_POINT ( 'NONE',  ( 5.062724140118719518, 0.5608846916410530348, 1.828269531156314853 ) ) ;
#82744=CARTESIAN_POINT ( 'NONE',  ( 6.674453038267287752, -1.361800985140369402, 1.737325302230605883 ) ) ;
#82748=CARTESIAN_POINT ( 'NONE',  ( 0.1002680356884171620, -0.9499045104094726577, 1.782327323349098602 ) ) ;
#82750=CARTESIAN_POINT ( 'NONE',  ( 4.805897800482852311, -0.6205396350037055697, 2.222522205952178975 ) ) ;
#82751=CARTESIAN_POINT ( 'NONE',  ( 5.019951445752288244, 1.940773837913706057, -0.2859759768028962146 ) ) ;
#82752=CARTESIAN_POINT ( 'NONE',  ( 1.551531708069888715, 1.481957716508151890, 1.285475804911541120 ) ) ;
#82756=CARTESIAN_POINT ( 'NONE',  ( 0.4974488191052604535, -0.3042024069639309158, 2.095249342460514086 ) ) ;
#82759=CARTESIAN_POINT ( 'NONE',  ( 0.8844010234979463592, 1.624802019249080853, -0.8659260420235401767 ) ) ;
#82761=CARTESIAN_POINT ( 'NONE',  ( 4.434556658511819016, -1.254960995779637045, 1.771429847731820661 ) ) ;
#82763=CARTESIAN_POINT ( 'NONE',  ( 1.371502371489873751, -1.821557607348308405, -1.085495857948336251 ) ) ;
#82767=CARTESIAN_POINT ( 'NONE',  ( 2.636070936407476584, 0.9742463255392861399, -1.815968889038493073 ) ) ;
#82773=CARTESIAN_POINT ( 'NONE',  ( 4.758414378865199801, 1.907420806491459064, 0.1369992607160031295 ) ) ;
#82777=CARTESIAN_POINT ( 'NONE',  ( 1.810245590833154283, -2.245401999695510575, 0.2761584955175334644 ) ) ;
#82779=CARTESIAN_POINT ( 'NONE',  ( 1.001899194773261170, -0.8131845483106721062, 1.618847804792804324 ) ) ;
#82780=CARTESIAN_POINT ( 'NONE',  ( 1.569406966088880084, 1.323937531303821968, 1.384834552875470415 ) ) ;
#82781=CARTESIAN_POINT ( 'NONE',  ( 3.561042923925850978, 1.633862107263984065, -1.271492733312264090 ) ) ;
#82783=CARTESIAN_POINT ( 'NONE',  ( 0.8660190917160478508, 0.9698478150794390684, 1.716334202883246229 ) ) ;
#82784=CARTESIAN_POINT ( 'NONE',  ( 6.006463946069247939, -0.6956954824784820079, -1.796673741800159707 ) ) ;
#82786=CARTESIAN_POINT ( 'NONE',  ( 1.260874316716424470, 0.9392902264234997967, 2.108064829403846208 ) ) ;
#82789=CARTESIAN_POINT ( 'NONE',  ( 4.914538883754228316, 0.7863694667932183968, 1.907089347224044884 ) ) ;
#82792=CARTESIAN_POINT ( 'NONE',  ( 6.229533133763371922, -1.984190613765562494, 0.7061325270490863559 ) ) ;
#82795=CARTESIAN_POINT ( 'NONE',  ( 4.780646861661003832, -2.095393720161139228, -0.5303334973314683953 ) ) ;
#82796=CARTESIAN_POINT ( 'NONE',  ( 5.022131231807676066, -2.009760515157756444, 0.1999713455246488469 ) ) ;
#82803=CARTESIAN_POINT ( 'NONE',  ( 3.485564796978508184, -0.5807542032013839339, 1.931124776463407189 ) ) ;
#82808=CARTESIAN_POINT ( 'NONE',  ( 5.102478102407745908, -0.7247817745383768884, -2.036717088958202471 ) ) ;
#82812=CARTESIAN_POINT ( 'NONE',  ( 5.624625116526842383, 0.3961212581503182339, 1.976953148079656719 ) ) ;
#82815=CARTESIAN_POINT ( 'NONE',  ( 0.5742808809356505506, -1.622453496466894407, -0.5859570326207633739 ) ) ;
#82821=CARTESIAN_POINT ( 'NONE',  ( 6.889956934492897034, -0.7990643998789861424, 1.689675875712663755 ) ) ;
#82822=CARTESIAN_POINT ( 'NONE',  ( 0.3111896917125516748, 1.672494819392616128, -1.120119447130196288 ) ) ;
#82823=CARTESIAN_POINT ( 'NONE',  ( 6.539320575229250920, 2.072231551265828475, 2.205269387046896679 ) ) ;
#82827=CARTESIAN_POINT ( 'NONE',  ( 2.403126630736720948, -0.3650820022202577175, -2.088671427859823293 ) ) ;
#82828=CARTESIAN_POINT ( 'NONE',  ( 1.950796209937825321, -1.844718841590715863, -0.8146091914792084054 ) ) ;
#82829=CARTESIAN_POINT ( 'NONE',  ( 2.109342631017618874, 1.402271653390272377, 1.146968571259598058 ) ) ;
#82831=CARTESIAN_POINT ( 'NONE',  ( 6.350466702034289312, 0.6732396885240909956, 2.054270918568662729 ) ) ;
#82836=CARTESIAN_POINT ( 'NONE',  ( 0.7080363470168028472, 1.138615994813133359, -1.540489816406021673 ) ) ;
#82842=CARTESIAN_POINT ( 'NONE',  ( 4.364260218091946975, 1.016419123106377276, 1.907829002176252953 ) ) ;
#82846=CARTESIAN_POINT ( 'NONE',  ( 1.933984528066152953, -2.055706711753771287, 0.5200354980386610038 ) ) ;
#82848=CARTESIAN_POINT ( 'NONE',  ( 3.725814648419359720, -1.171505211990100159, -1.585385422309880887 ) ) ;
#82849=CARTESIAN_POINT ( 'NONE',  ( 5.713130151434068438, 1.559639147136464343, -1.106415316399149473 ) ) ;
#82852=CARTESIAN_POINT ( 'NONE',  ( 5.600048008112708864, 0.7998006467024108002, -1.800045223161725660 ) ) ;
#82853=CARTESIAN_POINT ( 'NONE',  ( 1.921723552510564259, 1.118073055411296313, -1.587613466820477992 ) ) ;
#82858=CARTESIAN_POINT ( 'NONE',  ( 2.431682593473180276, 0.9845738105917539729, -1.844271946693208708 ) ) ;
#82862=CARTESIAN_POINT ( 'NONE',  ( 6.551426578739074635, -1.705833205818767295, 0.8644478841580638395 ) ) ;
#82864=CARTESIAN_POINT ( 'NONE',  ( 4.916741810085081710, 1.523553907054091328, -1.596827639139485777 ) ) ;
#82865=CARTESIAN_POINT ( 'NONE',  ( 1.466163881440044836, 2.173982691173735216, -0.3780781022180225159 ) ) ;
#82867=CARTESIAN_POINT ( 'NONE',  ( 0.5395309102857149819, -1.815710607404594557, 0.6001554849531522962 ) ) ;
#82869=CARTESIAN_POINT ( 'NONE',  ( 3.719242722441223226, -1.824546119899137731, -0.9785211796824041519 ) ) ;
#82872=CARTESIAN_POINT ( 'NONE',  ( 1.587033755777764510, -0.3173376132806354222, -2.138153673666403964 ) ) ;
#82873=CARTESIAN_POINT ( 'NONE',  ( 3.474349307649237328, -2.112600797985896950, -0.5827812199917583591 ) ) ;
#82880=CARTESIAN_POINT ( 'NONE',  ( 5.766190679352209969, 1.598854145598350929, -0.6720813200297001133 ) ) ;
#82882=CARTESIAN_POINT ( 'NONE',  ( 4.293848342403890683, -1.423947089648310849, -1.503027170334819029 ) ) ;
#82883=CARTESIAN_POINT ( 'NONE',  ( 5.835599761872579450, 0.6139674163637841575, -2.026275392342128612 ) ) ;
#82887=CARTESIAN_POINT ( 'NONE',  ( 3.221498965751792731, 0.2935017643310656177, -1.947342446911073610 ) ) ;
#82888=CARTESIAN_POINT ( 'NONE',  ( 6.474598600699414064, -0.1057723710937721190, -2.289958182497778161 ) ) ;
#82889=CARTESIAN_POINT ( 'NONE',  ( 2.736711336054332921, 0.2235625380298221498, 1.811883384933578256 ) ) ;
#82897=CARTESIAN_POINT ( 'NONE',  ( 3.674091251731440355, 1.997487462777279621, -0.2507888908306437625 ) ) ;
#82898=CARTESIAN_POINT ( 'NONE',  ( 4.293769791895286403, -1.349757117914761384, -1.423854091114319598 ) ) ;
#82902=CARTESIAN_POINT ( 'NONE',  ( -0.006154234300160406693, -2.090381218474619995, -0.04699178559822854429 ) ) ;
#82903=CARTESIAN_POINT ( 'NONE',  ( 6.051566426668148146, 0.5099629880620482059, -1.694758430261036564 ) ) ;
#82905=CARTESIAN_POINT ( 'NONE',  ( 1.342011898504836820, 2.189069585219292957, 0.1046993245200772138 ) ) ;
#82906=CARTESIAN_POINT ( 'NONE',  ( 0.8193799409778947940, 1.038239828973979373, -1.396697621350863505 ) ) ;
#82909=CARTESIAN_POINT ( 'NONE',  ( 1.048929499675733235, -1.357256335890437926, -1.064349854222715885 ) ) ;
#82910=CARTESIAN_POINT ( 'NONE',  ( 1.072081722297711259, 1.739511735661619429, -1.502347287396257114 ) ) ;
#82911=CARTESIAN_POINT ( 'NONE',  ( 0.2928600448571066495, 1.818678932476354149, -1.222557900829209121 ) ) ;
#82912=CARTESIAN_POINT ( 'NONE',  ( 2.614145488985010424, -2.182733025630137824, 0.3247920039054427721 ) ) ;
#82913=CARTESIAN_POINT ( 'NONE',  ( 1.604584692665763423, 2.168457688117795712, 0.1093331725631509210 ) ) ;
#82915=CARTESIAN_POINT ( 'NONE',  ( 1.833370464255643206, -1.703966518588348578, -1.256690760101538240 ) ) ;
#82916=CARTESIAN_POINT ( 'NONE',  ( 6.727182134110236689, 0.5535242275785922095, 2.340336476220133743 ) ) ;
#82917=CARTESIAN_POINT ( 'NONE',  ( 5.649420354817641154, -1.518837414639911065, -1.184835060848010713 ) ) ;
#82919=CARTESIAN_POINT ( 'NONE',  ( 2.261634143469380742, 2.247403939606710477, -0.4510662058269006569 ) ) ;
#82923=CARTESIAN_POINT ( 'NONE',  ( 4.811300260135710438, 1.847242992945047568, -1.233362022257722845 ) ) ;
#82930=ORIENTED_EDGE ( 'NONE', *, *, #155535, .T. ) ;
#82931=CARTESIAN_POINT ( 'NONE',  ( 2.936172824561166905, -1.650081981912490336, -1.158688413653415239 ) ) ;
#82933=CARTESIAN_POINT ( 'NONE',  ( 1.586864402838471522, 1.986712475098152408, 0.5538950855334312529 ) ) ;
#82934=CARTESIAN_POINT ( 'NONE',  ( 6.883263157960400669, 0.001763689368145522022, 1.846037217754382009 ) ) ;
#82938=CARTESIAN_POINT ( 'NONE',  ( 4.207102436150745639, -0.3756362130699179014, 2.158856393654845274 ) ) ;
#82939=CARTESIAN_POINT ( 'NONE',  ( 1.670546294658280084, 1.392546765991018454, 1.458555661489918442 ) ) ;
#82940=CARTESIAN_POINT ( 'NONE',  ( 1.012948470060770934, -1.796336717620912626, 0.4034172393945419377 ) ) ;
#82941=CARTESIAN_POINT ( 'NONE',  ( 4.136529068399773301, -1.600833271991594531, 0.9093273525555561898 ) ) ;
#82944=CARTESIAN_POINT ( 'NONE',  ( 5.315394819225006451, -0.2661953434012730435, 1.805952802178517613 ) ) ;
#82945=CARTESIAN_POINT ( 'NONE',  ( 5.959611329766300258, -1.915599147091971544, -0.6298778581111733610 ) ) ;
#82947=CARTESIAN_POINT ( 'NONE',  ( 4.206154751832458238, -2.256696944984788011, 0.1629611055770207317 ) ) ;
#82949=CARTESIAN_POINT ( 'NONE',  ( 0.3289212212809545788, 2.016005455721520345, 0.6092940615431781115 ) ) ;
#82951=CARTESIAN_POINT ( 'NONE',  ( 5.213363469605923228, -1.747142239327776903, -1.110534646669825376 ) ) ;
#82960=CARTESIAN_POINT ( 'NONE',  ( 1.125412309253082332, 1.872817075645373697, 0.9946839901537674056 ) ) ;
#82961=CARTESIAN_POINT ( 'NONE',  ( 1.916566064170255324, -2.220770990188126959, 0.06023022952456217466 ) ) ;
#82966=CARTESIAN_POINT ( 'NONE',  ( 3.420314466093795414, 0.8798059112791326575, 1.753580237611163994 ) ) ;
#82972=CARTESIAN_POINT ( 'NONE',  ( 2.707414796094851361, 1.816601298730673220, -1.093838055662835096 ) ) ;
#82974=CARTESIAN_POINT ( 'NONE',  ( 4.123457186961496213, 0.2424046295769199388, -1.946780420294342617 ) ) ;
#82975=CARTESIAN_POINT ( 'NONE',  ( 3.221700144506876917, -2.083771231579465866, 0.5749860669421112958 ) ) ;
#82976=CARTESIAN_POINT ( 'NONE',  ( 2.577489280727011334, -0.9446877197298313433, 1.580272903027237552 ) ) ;
#82979=CARTESIAN_POINT ( 'NONE',  ( 4.417713501739753745, 1.067903927642421591, -1.374066674465204363 ) ) ;
#82983=CARTESIAN_POINT ( 'NONE',  ( 1.903414394802248166, 1.797162532295241366, 1.201017911493490020 ) ) ;
#82984=CARTESIAN_POINT ( 'NONE',  ( 4.903672622533055581, 0.3418847601762939337, 1.986741992616162245 ) ) ;
#82986=CARTESIAN_POINT ( 'NONE',  ( 1.270647086845246188, -1.370953960119488668, 1.671340013135722558 ) ) ;
#82987=CARTESIAN_POINT ( 'NONE',  ( 3.942224353883512222, 1.961846943226858597, 0.1946112770482635312 ) ) ;
#82988=CARTESIAN_POINT ( 'NONE',  ( 2.477749938138404051, 1.209727786519874559, 1.556487202666415604 ) ) ;
#82990=CARTESIAN_POINT ( 'NONE',  ( 3.685046248344743258, 1.408799512439436352, 1.336988689110546913 ) ) ;
#82998=CARTESIAN_POINT ( 'NONE',  ( 1.641937377912294771, -1.598774535768614280, -1.521335986861327427 ) ) ;
#83000=CARTESIAN_POINT ( 'NONE',  ( 5.330891710049517229, -1.845885424482188286, -0.6645199359083459045 ) ) ;
#83002=CARTESIAN_POINT ( 'NONE',  ( 3.696581757058306383, 1.494387559712303526, -1.500228622805776624 ) ) ;
#83004=CARTESIAN_POINT ( 'NONE',  ( 0.07459516483345089710, 7.629137130509094256, -2.355503875070711572 ) ) ;
#83006=CARTESIAN_POINT ( 'NONE',  ( 3.837712106225504183, 1.832433245109680531, 0.1787696065849928018 ) ) ;
#83010=CARTESIAN_POINT ( 'NONE',  ( 5.010073305087408002, -0.7609581946756528437, 1.979555329295646260 ) ) ;
#83015=CARTESIAN_POINT ( 'NONE',  ( 5.395800779767854216, -0.7457615368846971515, 1.921284171288279996 ) ) ;
#83017=CARTESIAN_POINT ( 'NONE',  ( 0.9767415019392856612, 1.717539547389279830, 0.7171521658363362306 ) ) ;
#83018=CARTESIAN_POINT ( 'NONE',  ( 1.997363575765517485, -1.840834563946552649, 0.04656924640939614363 ) ) ;
#83022=CARTESIAN_POINT ( 'NONE',  ( 2.368051099418837069, 2.164043333312406503, -0.4318774905316472013 ) ) ;
#83023=CARTESIAN_POINT ( 'NONE',  ( 5.149841461411730492, 0.7164311094934887603, -2.146032026599023812 ) ) ;
#83025=CARTESIAN_POINT ( 'NONE',  ( 4.957183922012514898, -1.549878356133486124, 0.9377188026478706639 ) ) ;
#83026=CARTESIAN_POINT ( 'NONE',  ( 4.997249278368244951, -0.2745004324337502744, 1.895803710022869959 ) ) ;
#83029=STYLED_ITEM ( 'NONE', ( #29630 ), #162104 ) ;
#83030=CARTESIAN_POINT ( 'NONE',  ( 5.032044620589739559, 0.9611010790777809731, -1.604743002217932313 ) ) ;
#83032=CARTESIAN_POINT ( 'NONE',  ( 4.668306603206507255, -0.7948602423475581435, -1.682893250223691517 ) ) ;
#83034=CARTESIAN_POINT ( 'NONE',  ( 6.104346055523492964, -0.6409971714030155976, -1.649885601521252410 ) ) ;
#83035=CARTESIAN_POINT ( 'NONE',  ( -0.2409995289980038091, -0.004801160710915519658, -2.000252362011435636 ) ) ;
#83037=CARTESIAN_POINT ( 'NONE',  ( 2.701903229428818776, -0.6601559168808753819, 2.000001591751764618 ) ) ;
#83042=CARTESIAN_POINT ( 'NONE',  ( 2.373312353838610722, -1.759458965525468210, -0.9916931515873882441 ) ) ;
#83045=ORIENTED_EDGE ( 'NONE', *, *, #103113, .T. ) ;
#83046=CARTESIAN_POINT ( 'NONE',  ( 2.038557401052975671, 2.137775048120754029, 0.3193135401893046899 ) ) ;
#83047=CARTESIAN_POINT ( 'NONE',  ( 6.890000000000008562, 1.260399741928097672, 2.114076522472335462 ) ) ;
#83054=CARTESIAN_POINT ( 'NONE',  ( 1.048660896456204528, -1.724490848714568259, 1.352309724062021878 ) ) ;
#83056=CARTESIAN_POINT ( 'NONE',  ( 1.675094374204841419, -2.148779999652763895, -0.7084808733194192243 ) ) ;
#83063=CARTESIAN_POINT ( 'NONE',  ( 3.022431051408695613, 1.665045927894950095, 0.5999815234925524043 ) ) ;
#83065=CARTESIAN_POINT ( 'NONE',  ( 6.176841753231244958, -2.093540797633717254, -0.6980159708611932690 ) ) ;
#83068=CARTESIAN_POINT ( 'NONE',  ( 4.868767636308747093, -0.2496254991312534810, -2.000855965115163837 ) ) ;
#83069=CARTESIAN_POINT ( 'NONE',  ( 4.939644399817936460, -1.717766137778716118, 0.5755910463909068575 ) ) ;
#83071=CARTESIAN_POINT ( 'NONE',  ( 2.852262661058731386, 0.6285613048715790185, 1.762029509812724992 ) ) ;
#83072=CARTESIAN_POINT ( 'NONE',  ( 3.010663864534826928, 0.6931938328994196041, 1.950912564768356505 ) ) ;
#83074=CARTESIAN_POINT ( 'NONE',  ( 2.338023529656753752, -1.104205016203146705, -1.561194055274425452 ) ) ;
#83079=CARTESIAN_POINT ( 'NONE',  ( 1.371198541116287917, -1.641758494746584418, -0.9804709962101464393 ) ) ;
#83081=CARTESIAN_POINT ( 'NONE',  ( 2.523818479427087702, 1.924573107942130656, -0.3798230296482503210 ) ) ;
#83085=CARTESIAN_POINT ( 'NONE',  ( 5.607717026683647354, 1.607092460389969446, 1.383685132418293495 ) ) ;
#83088=CARTESIAN_POINT ( 'NONE',  ( 6.485619883616900339, 1.357675630217811014, 1.429558606944077326 ) ) ;
#83090=CARTESIAN_POINT ( 'NONE',  ( 2.267839937129061401, 0.5327387516648759425, -1.941401684534331817 ) ) ;
#83092=CARTESIAN_POINT ( 'NONE',  ( 1.616979318382205433, 0.2114564432566454211, 2.106663336370690143 ) ) ;
#83094=CARTESIAN_POINT ( 'NONE',  ( 2.998552181135270001, 2.054425100943928051, 0.2560010573490826835 ) ) ;
#83098=CARTESIAN_POINT ( 'NONE',  ( 5.701146808890831252, -0.5089937999912234057, 2.027600676370949095 ) ) ;
#83100=CARTESIAN_POINT ( 'NONE',  ( 3.926616521958687045, 1.733384925006593136, 0.5729815612169064654 ) ) ;
#83103=CARTESIAN_POINT ( 'NONE',  ( 6.890000000000008562, 2.965158640989657535, 2.452917560796506802 ) ) ;
#83105=CARTESIAN_POINT ( 'NONE',  ( 5.280388062626482970, -1.229865305990836877, 1.832093573602276759 ) ) ;
#83109=CARTESIAN_POINT ( 'NONE',  ( 4.055252259792781366, -1.662250449027093735, 0.9452659147194606426 ) ) ;
#83116=CARTESIAN_POINT ( 'NONE',  ( -0.05938221139379848412, -1.422385081007140117, -1.168950373246782526 ) ) ;
#83120=CARTESIAN_POINT ( 'NONE',  ( 4.991395955090764502, 1.385047395102714685, 1.257364466828891914 ) ) ;
#83125=CARTESIAN_POINT ( 'NONE',  ( 1.569134323820881027, 1.734487354001874371, 0.9329377246683704383 ) ) ;
#83126=CARTESIAN_POINT ( 'NONE',  ( 2.671500097371417137, 1.427951006967288272, 1.423949442620517702 ) ) ;
#83131=CARTESIAN_POINT ( 'NONE',  ( 2.783357461837578484, 1.550338952211056220, 1.549093164327268068 ) ) ;
#83132=CARTESIAN_POINT ( 'NONE',  ( 6.639320575229281651, -0.0007625845807879281287, 2.103388539994067497 ) ) ;
#83142=CARTESIAN_POINT ( 'NONE',  ( 4.599059095968327071, -0.4863373063577690059, 1.775805238918099382 ) ) ;
#83143=CARTESIAN_POINT ( 'NONE',  ( 0.1881394758670457412, 1.160778376788082378, 1.644543748126830796 ) ) ;
#83144=CARTESIAN_POINT ( 'NONE',  ( 2.794613785990595733, -2.145299970026095071, 0.8252070097543462435 ) ) ;
#83146=CARTESIAN_POINT ( 'NONE',  ( 0.8657744530725123289, -1.852701964455932604, 0.1747518070307155780 ) ) ;
#83149=CARTESIAN_POINT ( 'NONE',  ( 4.834190613173367623, -1.027981871586785889, -1.612434056610718480 ) ) ;
#83152=CARTESIAN_POINT ( 'NONE',  ( 3.562131390660903563, -1.402593093800925894, 1.550658987340556294 ) ) ;
#83153=CARTESIAN_POINT ( 'NONE',  ( 2.694054421766533203, -1.865511834602461949, -0.1395888279770511053 ) ) ;
#83156=CARTESIAN_POINT ( 'NONE',  ( 5.706567001488551227, 1.626822141722890303, 0.8623401093873286349 ) ) ;
#83159=CARTESIAN_POINT ( 'NONE',  ( 5.092313435308955860, -1.712476623254995278, -0.2059198849207622417 ) ) ;
#83161=CARTESIAN_POINT ( 'NONE',  ( 0.5801786448705691379, -0.6264061342569470225, 1.617264071341844245 ) ) ;
#83162=CARTESIAN_POINT ( 'NONE',  ( 6.516270054225981490, -1.036149114087565382, -1.948532232987249424 ) ) ;
#83164=CARTESIAN_POINT ( 'NONE',  ( 4.698188964201695406, 0.9341788774818636787, -1.959971951513925781 ) ) ;
#83165=CARTESIAN_POINT ( 'NONE',  ( 2.894927146036041510, 1.565677646668685696, -0.9388022922067614795 ) ) ;
#83166=CARTESIAN_POINT ( 'NONE',  ( 0.9187138386215136787, -1.424830647414500051, 1.348730089142296418 ) ) ;
#83167=CARTESIAN_POINT ( 'NONE',  ( 5.348860635491798909, -1.915306066586830669, -0.9028416433708542632 ) ) ;
#83169=CARTESIAN_POINT ( 'NONE',  ( 6.198803536200695241, 1.903451089567553822, 1.277169966706873883 ) ) ;
#83173=CARTESIAN_POINT ( 'NONE',  ( 1.946092837771850492, -1.387361170020007695, -1.603719225630481970 ) ) ;
#83176=CARTESIAN_POINT ( 'NONE',  ( 6.209878556409044847, 0.6379485578581347571, -2.075210184031409888 ) ) ;
#83177=CARTESIAN_POINT ( 'NONE',  ( 6.883263157960367806, 2.959656548886806071, 2.506466465954690914 ) ) ;
#83179=CARTESIAN_POINT ( 'NONE',  ( 2.596574818557799258, -1.139633321999042659, 1.906535983277869661 ) ) ;
#83181=CARTESIAN_POINT ( 'NONE',  ( 6.276017556857773627, 1.753032240926259311, -0.9962986157117934560 ) ) ;
#83183=CARTESIAN_POINT ( 'NONE',  ( 4.188373618524662056, 1.107674127198258196, -1.739744320567500280 ) ) ;
#83188=CARTESIAN_POINT ( 'NONE',  ( 0.1331565106231363538, 0.2470099659030860484, -1.980838409567912572 ) ) ;
#83189=CARTESIAN_POINT ( 'NONE',  ( 0.9903105584966699348, -0.5097506344743455431, -2.027405242695742515 ) ) ;
#83190=CARTESIAN_POINT ( 'NONE',  ( 4.827609030688454261, 0.9420861819694618111, -1.581835861328761528 ) ) ;
#83193=CARTESIAN_POINT ( 'NONE',  ( 1.711479192339813382, -1.712302428074402583, 0.2063632002643790431 ) ) ;
#83194=CARTESIAN_POINT ( 'NONE',  ( 0.4269707148552639997, -1.727061408318403712, 1.040797348915108111 ) ) ;
#83195=CARTESIAN_POINT ( 'NONE',  ( 1.460084154473238138, -2.184713004772549372, -0.7151137612169417013 ) ) ;
#83197=CARTESIAN_POINT ( 'NONE',  ( 1.282923566313122210, -2.207321063319432231, -0.4954982646878171582 ) ) ;
#83198=CARTESIAN_POINT ( 'NONE',  ( 4.072956574305106159, -1.964985935830084740, -0.7583447493727160094 ) ) ;
#83203=CARTESIAN_POINT ( 'NONE',  ( 5.718750000000003553, -0.7852924748296825630, 1.895863743164203141 ) ) ;
#83207=CARTESIAN_POINT ( 'NONE',  ( 4.641020947978182321, 2.126209183204033959, 0.6434571820467527292 ) ) ;
#83208=CARTESIAN_POINT ( 'NONE',  ( 3.187623232016934871, -0.8878212517344568067, 2.003729935572157395 ) ) ;
#83211=CARTESIAN_POINT ( 'NONE',  ( 5.567072742743464531, -1.671543079161823542, 1.304629437388994395 ) ) ;
#83214=CARTESIAN_POINT ( 'NONE',  ( 6.889999999999967706, 0.005249217920031550542, 1.719840535937327664 ) ) ;
#83216=CARTESIAN_POINT ( 'NONE',  ( 5.396778611113259849, -2.069399493756381769, -0.4625044129713885011 ) ) ;
#83220=CARTESIAN_POINT ( 'NONE',  ( 6.315313271410192719, -0.2696487299426887363, 2.144762774094311375 ) ) ;
#83224=CARTESIAN_POINT ( 'NONE',  ( 0.9072687458823289752, -0.7809752019604562223, -1.555474206689683836 ) ) ;
#83229=CARTESIAN_POINT ( 'NONE',  ( 4.856408821558930278, 0.8241108818672329139, 1.998647875481096126 ) ) ;
#83232=CARTESIAN_POINT ( 'NONE',  ( 4.856408821558930278, 0.8241108818672329139, 1.998647875481096126 ) ) ;
#83236=CARTESIAN_POINT ( 'NONE',  ( 5.430923302262330665, 0.1424395525144121211, 1.966244542718327715 ) ) ;
#83237=CARTESIAN_POINT ( 'NONE',  ( 5.202368031388965974, -1.227288160380139548, -1.225006654371106452 ) ) ;
#83239=CARTESIAN_POINT ( 'NONE',  ( 1.839652601550560096, 0.8350199954420146620, -2.026445374841173930 ) ) ;
#83240=CARTESIAN_POINT ( 'NONE',  ( 2.450585703787050651, 2.307050653106942573, 0.05676454813420374335 ) ) ;
#83241=CARTESIAN_POINT ( 'NONE',  ( 5.255176862235733992, -1.738700696582769378, -1.105936373271217521 ) ) ;
#83242=CARTESIAN_POINT ( 'NONE',  ( 0.5330192132981932396, -1.372706249750287322, -1.373872859839823990 ) ) ;
#83246=CARTESIAN_POINT ( 'NONE',  ( 4.377262645480927361, -1.895543854172193399, -0.9507902649282941043 ) ) ;
#83248=CARTESIAN_POINT ( 'NONE',  ( 1.389296306420295224, -0.7283806465635984662, -1.880434191983325398 ) ) ;
#83250=EDGE_CURVE ( 'NONE', #53136, #71735, #159915, .T. ) ;
#83251=CARTESIAN_POINT ( 'NONE',  ( 4.630015379333586978, -1.354682855507854278, -1.741961856448564383 ) ) ;
#83259=CARTESIAN_POINT ( 'NONE',  ( 3.661055773700711224, -1.816817347422092555, -0.9728634070030485193 ) ) ;
#83262=CARTESIAN_POINT ( 'NONE',  ( 3.949871522956601932, -1.394395303408175080, -1.461305941245706119 ) ) ;
#83265=CARTESIAN_POINT ( 'NONE',  ( 1.569287236123186213, 0.1524497474049029966, -2.055318472165644117 ) ) ;
#83268=CARTESIAN_POINT ( 'NONE',  ( -0.2411972340276230808, 7.629137130509075604, -2.500476664557866435 ) ) ;
#83269=CARTESIAN_POINT ( 'NONE',  ( 1.605144257462550517, -1.827384369528777031, 0.2241066044648756805 ) ) ;
#83270=CARTESIAN_POINT ( 'NONE',  ( 0.3996046210705077595, 1.915144275937111340, -1.287252092841030260 ) ) ;
#83272=CARTESIAN_POINT ( 'NONE',  ( 1.036653925908154639, 2.129443126370239803, 0.3705773954724436159 ) ) ;
#83274=CARTESIAN_POINT ( 'NONE',  ( 1.710173085450257924, 1.157096902994741772, -1.651345047625000007 ) ) ;
#83275=ADVANCED_FACE ( 'NONE', ( #108438 ), #146021, .T. ) ;
#83276=CARTESIAN_POINT ( 'NONE',  ( 1.863111423135884293, -0.7740270289045609875, 2.164224664766948525 ) ) ;
#83281=CARTESIAN_POINT ( 'NONE',  ( 4.346526858336821952, 0.5246154692373095063, 1.900329053005628044 ) ) ;
#83282=CARTESIAN_POINT ( 'NONE',  ( 4.065638850954083061, 1.320825628876612479, 1.523796413913918846 ) ) ;
#83286=CARTESIAN_POINT ( 'NONE',  ( 6.164693330894345458, -1.490570670011469812, 1.488127047250583201 ) ) ;
#83287=CARTESIAN_POINT ( 'NONE',  ( 5.424307079040114665, 1.017280057988108499, 1.803113764695261523 ) ) ;
#83291=CARTESIAN_POINT ( 'NONE',  ( 4.886975862609196142, -1.903224527948672584, -0.6766701927056159027 ) ) ;
#83293=CARTESIAN_POINT ( 'NONE',  ( 3.914918041407587257, 1.633027907263858491, -1.630791690553441420 ) ) ;
#83294=CARTESIAN_POINT ( 'NONE',  ( 0.7606827552629210620, -0.6912373536034731591, -1.943445369992405025 ) ) ;
#83302=CARTESIAN_POINT ( 'NONE',  ( 2.875608777474625732, -0.2152533142569280078, 2.160498500671267585 ) ) ;
#83304=CARTESIAN_POINT ( 'NONE',  ( 3.333393596924072444, 0.8250370302015205271, -1.646115572170883112 ) ) ;
#83306=CARTESIAN_POINT ( 'NONE',  ( 4.071962858106247474, -1.261020321617589479, 1.792237525612811355 ) ) ;
#83308=CARTESIAN_POINT ( 'NONE',  ( 4.504895162230450723, 1.751659092587343869, -1.432031112679124085 ) ) ;
#83314=CARTESIAN_POINT ( 'NONE',  ( 6.116413106003639300, 1.187136285548880066, -1.312641305385914947 ) ) ;
#83315=CARTESIAN_POINT ( 'NONE',  ( 4.283843839860628222, 1.952122219449687668, -0.4911893120533029622 ) ) ;
#83317=CARTESIAN_POINT ( 'NONE',  ( 3.417109911095609132, 1.903178947333901583, 0.9019662245143298396 ) ) ;
#83318=CARTESIAN_POINT ( 'NONE',  ( 0.9662486314009374189, -1.869180826568194398, -0.4184218257623931181 ) ) ;
#83321=CARTESIAN_POINT ( 'NONE',  ( 1.609744333363828384, 0.5749553099084430130, -1.883740962975283706 ) ) ;
#83322=CARTESIAN_POINT ( 'NONE',  ( 4.746356070053968423, 1.034628734442550879, -1.734499354260822468 ) ) ;
#83323=CARTESIAN_POINT ( 'NONE',  ( 0.3384655940862451029, 0.3152513238553408814, 1.843739016257638141 ) ) ;
#83324=CARTESIAN_POINT ( 'NONE',  ( 0.9417639971489067952, 1.314929008279978495, 1.456166070238865018 ) ) ;
#83325=CARTESIAN_POINT ( 'NONE',  ( 0.1758378621803426134, 1.891278220088285833, -0.2826890867150752551 ) ) ;
#83330=CARTESIAN_POINT ( 'NONE',  ( 5.735183426005796115, -1.690533149647139410, 0.8011652756413772947 ) ) ;
#83333=CARTESIAN_POINT ( 'NONE',  ( 6.772334134356085222, -0.9704686269969391432, -1.828672837219179392 ) ) ;
#83335=CARTESIAN_POINT ( 'NONE',  ( 0.9067890187421032699, 0.5993529260880943177, 1.981728858978973218 ) ) ;
#83344=CARTESIAN_POINT ( 'NONE',  ( 5.916451087343006954, 0.7937011933104149985, 1.794315766958521241 ) ) ;
#83346=CARTESIAN_POINT ( 'NONE',  ( 2.864611068004913275, -0.6351033500862738324, 1.913510180259501592 ) ) ;
#83348=CARTESIAN_POINT ( 'NONE',  ( 3.977677156295666538, -0.7278633372749753194, 1.772268029184346227 ) ) ;
#83350=CARTESIAN_POINT ( 'NONE',  ( 1.294752383181968503, 1.788903229852260246, -1.265732775075766092 ) ) ;
#83351=CARTESIAN_POINT ( 'NONE',  ( 0.2333690889706717397, 7.629137130509078268, -2.653349640194931247 ) ) ;
#83352=CARTESIAN_POINT ( 'NONE',  ( 3.057714436724996876, 1.861869414292870006, -0.1796979844640861634 ) ) ;
#83356=CARTESIAN_POINT ( 'NONE',  ( 4.921547094770428288, -1.498112151610554665, -1.496348102564814209 ) ) ;
#83358=CARTESIAN_POINT ( 'NONE',  ( 6.637176860265922684, -0.09746846054551477900, -2.068182370504913159 ) ) ;
#83359=CARTESIAN_POINT ( 'NONE',  ( 2.735971011012145127, 2.075282486531265569, 0.2531079119270570610 ) ) ;
#83360=CARTESIAN_POINT ( 'NONE',  ( 6.620655732516651071, 1.241313378043694238, 2.288056600130850882 ) ) ;
#83361=CARTESIAN_POINT ( 'NONE',  ( 0.4985095413094174921, 1.438046592433483761, -0.9519660005063760311 ) ) ;
#83364=CARTESIAN_POINT ( 'NONE',  ( 6.925078400183531713, -0.004750840071900481326, 2.044148492825673014 ) ) ;
#83372=CARTESIAN_POINT ( 'NONE',  ( 0.7678511737040129015, 1.809490520450097284, -0.08760732307166485544 ) ) ;
#83380=CARTESIAN_POINT ( 'NONE',  ( -0.2409995289980224054, 7.629137130509101361, -2.600476469121244527 ) ) ;
#83384=CARTESIAN_POINT ( 'NONE',  ( 2.594024687173156263, 0.8801344893799438740, -1.639794913454610148 ) ) ;
#83385=CARTESIAN_POINT ( 'NONE',  ( 0.1224727961543301408, 0.3280879897031144798, 1.887133295268013766 ) ) ;
#83386=CARTESIAN_POINT ( 'NONE',  ( 0.09436191691250192526, -0.3928898508825870439, -1.789253991261535726 ) ) ;
#83392=CARTESIAN_POINT ( 'NONE',  ( 4.873860229706322933, -1.932217566332248282, 0.3801659098390720581 ) ) ;
#83393=CARTESIAN_POINT ( 'NONE',  ( 1.155114678095255254, 0.4172207117813032662, 2.078868179971034902 ) ) ;
#83399=CARTESIAN_POINT ( 'NONE',  ( 5.806613533822880591, 1.931179984464112653, 1.035834350304319695 ) ) ;
#83401=CARTESIAN_POINT ( 'NONE',  ( 4.295867091898570855, -0.7379356464434319030, 1.779637345161827922 ) ) ;
#83403=CARTESIAN_POINT ( 'NONE',  ( 0.2877648253245302934, -0.8656086203641421006, 1.607325130595547602 ) ) ;
#83404=CARTESIAN_POINT ( 'NONE',  ( 1.577102763248950046, -2.096353118739826993, -0.6898709473643764856 ) ) ;
#83409=CARTESIAN_POINT ( 'NONE',  ( 5.735196696812420392, -0.04448252213613138051, -1.969098798407813433 ) ) ;
#83410=CARTESIAN_POINT ( 'NONE',  ( 1.593202639421680278, -0.6524502387153191529, 1.829324111618094717 ) ) ;
#83411=CARTESIAN_POINT ( 'NONE',  ( 6.784486029815019137, -2.232095771774603055, 0.5478248251382932255 ) ) ;
#83413=CARTESIAN_POINT ( 'NONE',  ( 4.680409711739222267, 1.147293496411544433, -1.465074471950976953 ) ) ;
#83420=CARTESIAN_POINT ( 'NONE',  ( 0.3104468679729632807, 1.506874830639578056, -1.591553791636945991 ) ) ;
#83425=CARTESIAN_POINT ( 'NONE',  ( 1.172165686010542274, -1.159919637379997814, 1.409874495853599141 ) ) ;
#83427=CARTESIAN_POINT ( 'NONE',  ( 3.199597886960439119, 1.569373658825726769, 0.7380672391785416675 ) ) ;
#83429=CARTESIAN_POINT ( 'NONE',  ( 6.509000000000032315, 0.5738235599486035676, 2.152438501345500743 ) ) ;
#83430=CARTESIAN_POINT ( 'NONE',  ( 0.1331565106231571705, 6.948071080078889850, -2.540993614958915181 ) ) ;
#83431=CARTESIAN_POINT ( 'NONE',  ( 0.2231027806867662000, -0.09612335957175778545, 1.924217376148322334 ) ) ;
#83432=CARTESIAN_POINT ( 'NONE',  ( 4.768382384511014038, -0.8351381170168621360, -1.775225883709200980 ) ) ;
#83435=CARTESIAN_POINT ( 'NONE',  ( 4.319064098534145302, 1.638436671179326787, -1.346072318137331969 ) ) ;
#83441=CARTESIAN_POINT ( 'NONE',  ( 2.588806720547200513, 2.007000696110202043, 0.5072723548179418618 ) ) ;
#83445=CARTESIAN_POINT ( 'NONE',  ( 2.848558797923263164, 0.3346648989216906012, -2.274091979294257992 ) ) ;
#83453=CARTESIAN_POINT ( 'NONE',  ( 3.814637755342592307, -0.6046605605216844870, -1.814329123173196834 ) ) ;
#83455=CARTESIAN_POINT ( 'NONE',  ( 5.579022813628022881, -0.04626586813367798007, -1.724316369773688962 ) ) ;
#83456=CARTESIAN_POINT ( 'NONE',  ( 3.643767777461913493, 2.000731686840724333, -0.2516315899964287617 ) ) ;
#83457=CARTESIAN_POINT ( 'NONE',  ( 4.852278370791485607, 0.2271405875100707961, -2.287421213010778942 ) ) ;
#83459=CARTESIAN_POINT ( 'NONE',  ( 0.2060869173217265982, -0.5842117877600698783, 2.128085570573131413 ) ) ;
#83461=CARTESIAN_POINT ( 'NONE',  ( 6.415310830085463323, -0.2139434178000785558, 1.756706237510232915 ) ) ;
#83463=CARTESIAN_POINT ( 'NONE',  ( 2.308868829589076022, 2.048438961056008090, 1.028902946192054912 ) ) ;
#83464=CARTESIAN_POINT ( 'NONE',  ( 0.5150585655138568697, -0.9269755740852363424, -1.472709990541859693 ) ) ;
#83467=CARTESIAN_POINT ( 'NONE',  ( 6.632779825423476439, -1.959453823303359377, 0.9815127000676395763 ) ) ;
#83470=CARTESIAN_POINT ( 'NONE',  ( 6.619590326553026038, 0.3579758704960536719, -2.039031579972025554 ) ) ;
#83471=CARTESIAN_POINT ( 'NONE',  ( 0.8840003597419334724, -2.016708404047353742, 0.004841148455551891328 ) ) ;
#83473=CARTESIAN_POINT ( 'NONE',  ( 5.303319688262892129, 1.576177044413902717, 1.107479782286522996 ) ) ;
#83475=CARTESIAN_POINT ( 'NONE',  ( 2.654761906407083760, 2.205155901917950967, 0.2675573109941364880 ) ) ;
#83481=CARTESIAN_POINT ( 'NONE',  ( 4.177133728293176418, 1.140962030703307928, 1.314357115670391707 ) ) ;
#83483=CARTESIAN_POINT ( 'NONE',  ( 3.455471728117681440, 1.544996161402897528, 1.208956721487665087 ) ) ;
#83488=CARTESIAN_POINT ( 'NONE',  ( 0.7485702846574161518, -2.046882729015482738, -0.2544144183350918742 ) ) ;
#83491=CARTESIAN_POINT ( 'NONE',  ( 4.821500071095637274, -1.429446227384461032, -1.422610148874188463 ) ) ;
#83492=CARTESIAN_POINT ( 'NONE',  ( 1.727766546026089145, -2.130035881452702728, 0.7632205929882311946 ) ) ;
#83495=CARTESIAN_POINT ( 'NONE',  ( 2.319419987651088810, -1.815478447740950685, 0.4500915571382518854 ) ) ;
#83496=CARTESIAN_POINT ( 'NONE',  ( 1.863478119473166439, -0.08537559288352389308, -1.732189446134152266 ) ) ;
#83497=CARTESIAN_POINT ( 'NONE',  ( 5.144143540903125533, 0.6357783856077160456, 2.097287126430439130 ) ) ;
#83498=CARTESIAN_POINT ( 'NONE',  ( 6.528381088282158906, 1.336169653064466889, -1.881230508112927025 ) ) ;
#83499=CARTESIAN_POINT ( 'NONE',  ( 0.9189065912094130928, 1.903898908998642447, 0.7894373168981814182 ) ) ;
#83500=CARTESIAN_POINT ( 'NONE',  ( 3.222533412629301708, 0.04844597582449915174, 1.941506634493498362 ) ) ;
#83502=CARTESIAN_POINT ( 'NONE',  ( 6.134044790494318278, 0.9221746925026914621, -1.627378824227587062 ) ) ;
#83503=CARTESIAN_POINT ( 'NONE',  ( 1.312500000000000888, 1.451031289061174734, 1.451031289061067486 ) ) ;
#83505=CARTESIAN_POINT ( 'NONE',  ( 6.626327358740755180, 0.3474107405085808953, -1.985797104380654376 ) ) ;
#83508=CARTESIAN_POINT ( 'NONE',  ( 4.764296165657141202, 1.880435471729305030, -0.7283773170061805802 ) ) ;
#83512=CARTESIAN_POINT ( 'NONE',  ( 2.349991895876184511, 1.825291697999480434, 0.04531359951509549705 ) ) ;
#83521=CARTESIAN_POINT ( 'NONE',  ( -0.03488881496042146174, -1.619560933857542073, 1.206636643155176714 ) ) ;
#83522=CARTESIAN_POINT ( 'NONE',  ( 0.3816889160728508812, 0.2035859187828891470, -2.110680546376259681 ) ) ;
#83526=CARTESIAN_POINT ( 'NONE',  ( 5.981337812661591258, 1.905142945929317211, -0.7864339424841911841 ) ) ;
#83527=CARTESIAN_POINT ( 'NONE',  ( 5.555314621531947772, -1.277044735018734833, 1.560499014526220307 ) ) ;
#83531=CARTESIAN_POINT ( 'NONE',  ( -0.2108831679771168421, 6.948330828014878335, -2.492181822431015270 ) ) ;
#83532=CIRCLE ( 'NONE', #131970, 0.04999999999999937828 ) ;
#83537=CARTESIAN_POINT ( 'NONE',  ( 5.290388671387995956, -1.915306256023459053, 0.6297802918850338161 ) ) ;
#83538=CARTESIAN_POINT ( 'NONE',  ( 4.962772036422566480, 0.1772586797372834311, -1.832584332494808121 ) ) ;
#83541=CARTESIAN_POINT ( 'NONE',  ( 3.827072092044791596, 2.190881801378454785, 0.7251257774964211533 ) ) ;
#83543=CARTESIAN_POINT ( 'NONE',  ( 4.288457955665158750, -2.137403104576699242, -0.3218062170811594735 ) ) ;
#83545=CARTESIAN_POINT ( 'NONE',  ( 6.515202330376022921, -1.784155196879381622, 0.4545711315065634195 ) ) ;
#83550=CARTESIAN_POINT ( 'NONE',  ( 3.871829239884491791, 1.038646522470688671, 1.555605274479121114 ) ) ;
#83551=CARTESIAN_POINT ( 'NONE',  ( 1.177825114000274898, 1.883588471398514264, -0.3297955356276888184 ) ) ;
#83554=CARTESIAN_POINT ( 'NONE',  ( 3.317197348578094562, 1.995112415077514356, 0.9436014139095407760 ) ) ;
#83560=CARTESIAN_POINT ( 'NONE',  ( 0.5089730629182923627, 1.712948150172272976, 0.9756560103859630573 ) ) ;
#83561=CARTESIAN_POINT ( 'NONE',  ( 0.4644773334415828736, 2.281836724062924038, -0.3429670027690605583 ) ) ;
#83562=CARTESIAN_POINT ( 'NONE',  ( 1.557006721180295150, 1.605793932651664813, -1.126831546849601740 ) ) ;
#83563=CARTESIAN_POINT ( 'NONE',  ( 4.627816428071820809, 2.001945081875619259, -0.4960309448565465851 ) ) ;
#83572=CARTESIAN_POINT ( 'NONE',  ( 0.4269466478069834925, -1.418992435970769739, 1.643201522047117669 ) ) ;
#83578=CARTESIAN_POINT ( 'NONE',  ( 1.299835797595794151, -1.870726058509405210, -0.005653028302576856845 ) ) ;
#83579=CARTESIAN_POINT ( 'NONE',  ( 5.764953170560049855, -1.951456690425241947, -0.9300186209130756332 ) ) ;
#83584=CARTESIAN_POINT ( 'NONE',  ( 0.8910925258837493201, -0.04752833427993513604, -1.911862225341356858 ) ) ;
#83585=CARTESIAN_POINT ( 'NONE',  ( 2.922431196026415101, 1.665835785064853969, 0.5981315555363684311 ) ) ;
#83586=CARTESIAN_POINT ( 'NONE',  ( 0.8031952904608251620, 1.686239601473665140, -0.9019194118903075541 ) ) ;
#83588=CARTESIAN_POINT ( 'NONE',  ( 4.464398116780900594, -1.859039872360370937, -0.4615888831297955686 ) ) ;
#83590=CARTESIAN_POINT ( 'NONE',  ( 5.617622257330707747, 0.3859593044726419286, -1.931177630036359005 ) ) ;
#83591=CARTESIAN_POINT ( 'NONE',  ( 0.8266187642571948269, -0.9586779626098644869, -1.891633453305548773 ) ) ;
#83593=CARTESIAN_POINT ( 'NONE',  ( 3.555401268124198655, 0.4554524271490404952, -1.814226883376020671 ) ) ;
#83594=CARTESIAN_POINT ( 'NONE',  ( 0.9436603434208358232, 0.7422609627109194586, -1.668170528445270140 ) ) ;
#83596=CARTESIAN_POINT ( 'NONE',  ( 3.369938178094655346, 2.153121441420174698, -0.4834393813165636100 ) ) ;
#83599=CARTESIAN_POINT ( 'NONE',  ( 1.557159421845564218, 1.687539990290163772, -1.185865425756290392 ) ) ;
#83607=CARTESIAN_POINT ( 'NONE',  ( 4.791501694037465953, -1.894250426384593844, 0.8359921707915063394 ) ) ;
#83609=CARTESIAN_POINT ( 'NONE',  ( 1.247603677004164746, -1.703183937513498281, -1.330886036463780009 ) ) ;
#83611=CARTESIAN_POINT ( 'NONE',  ( 2.227218753574769838, 1.805135905798272100, 0.9059672028350268524 ) ) ;
#83616=CARTESIAN_POINT ( 'NONE',  ( 6.520861224751243412, 2.010896128390584625, -0.1455136175190149816 ) ) ;
#83617=CARTESIAN_POINT ( 'NONE',  ( 0.6730650033222317363, 1.776164188848127878, -0.9548607967814757291 ) ) ;
#83618=CARTESIAN_POINT ( 'NONE',  ( 6.639320575229251453, 6.034321252505787214, 2.798156424428144717 ) ) ;
#83619=CARTESIAN_POINT ( 'NONE',  ( 4.933237592207079025, -1.549687834843778811, -1.549900206446311657 ) ) ;
#83621=CARTESIAN_POINT ( 'NONE',  ( 3.726736447152957599, 1.348887845406310682, -1.355897031963343213 ) ) ;
#83625=CARTESIAN_POINT ( 'NONE',  ( 2.056267757160272325, -1.238304521155994209, 1.591332585091954854 ) ) ;
#83627=CARTESIAN_POINT ( 'NONE',  ( 0.3809655214361170050, -0.2885804254640594868, -2.274098033663536356 ) ) ;
#83629=CARTESIAN_POINT ( 'NONE',  ( 3.698037441923990087, -1.722821800119245683, -0.08474311298608917797 ) ) ;
#83634=CARTESIAN_POINT ( 'NONE',  ( 0.8187140321147531319, -1.423520202335259999, 1.350257566363553208 ) ) ;
#83635=CARTESIAN_POINT ( 'NONE',  ( 0.1753634416057497647, 4.084635187426246539, -2.698744815386323381 ) ) ;
#83637=CARTESIAN_POINT ( 'NONE',  ( 3.580526426040127941, -1.214262702978758712, 1.344428254631929276 ) ) ;
#83640=FACE_OUTER_BOUND ( 'NONE', #2509, .T. ) ;
#83641=CARTESIAN_POINT ( 'NONE',  ( 4.775916358578648158, 1.790991888885495431, -0.2707881515907252234 ) ) ;
#83646=CARTESIAN_POINT ( 'NONE',  ( 6.180112001919068732, -1.034620502799053599, -1.546732508075428392 ) ) ;
#83648=CARTESIAN_POINT ( 'NONE',  ( 4.077677060472849391, -0.7296757366501721576, 1.771397967703478793 ) ) ;
#83654=CARTESIAN_POINT ( 'NONE',  ( 5.823477710672365859, -1.535350753823118586, -1.458276433397849514 ) ) ;
#83655=CARTESIAN_POINT ( 'NONE',  ( 1.006953172832128374, 1.636353683469338183, -1.412668763314451903 ) ) ;
#83658=CARTESIAN_POINT ( 'NONE',  ( 1.166719304534512558, -1.648536928579244165, -0.7845717211837843763 ) ) ;
#83660=CARTESIAN_POINT ( 'NONE',  ( 3.381694320706640333, 1.157239582903809128, 1.411935816614327655 ) ) ;
#83663=CARTESIAN_POINT ( 'NONE',  ( 2.312896453495900673, -1.524290774635113088, 1.247285826271822939 ) ) ;
#83664=CARTESIAN_POINT ( 'NONE',  ( 4.458499667006603495, -1.736235857128598070, -0.8702183630341918663 ) ) ;
#83667=CARTESIAN_POINT ( 'NONE',  ( 5.801066647469003357, -0.3129311994157328303, -2.097281602037828208 ) ) ;
#83670=CARTESIAN_POINT ( 'NONE',  ( 3.053266463924544372, -1.685387242695039811, 0.9035085923766730254 ) ) ;
#83677=CARTESIAN_POINT ( 'NONE',  ( 4.529811765687052016, -1.125283923072720071, -1.437579299059896343 ) ) ;
#83678=CARTESIAN_POINT ( 'NONE',  ( 6.087125082597877324, 1.679220375458953862, 1.116214469231976869 ) ) ;
#83684=CARTESIAN_POINT ( 'NONE',  ( 5.998880656844745474, 1.528293836345222312, -1.078463600801618405 ) ) ;
#83694=CARTESIAN_POINT ( 'NONE',  ( 6.455955546751245500, -0.7393474466994474081, 2.041418194955111787 ) ) ;
#83695=EDGE_CURVE ( 'NONE', #35846, #82118, #51711, .T. ) ;
#83696=CARTESIAN_POINT ( 'NONE',  ( 1.687271568794300070, 1.762372639767064042, 1.173053760763353104 ) ) ;
#83699=CARTESIAN_POINT ( 'NONE',  ( 5.752806990244247132, -0.4974732019265226679, -2.009498513695342936 ) ) ;
#83700=CARTESIAN_POINT ( 'NONE',  ( 1.188719773494644860, 1.394467456127197025, 1.202481090285527632 ) ) ;
#83704=CARTESIAN_POINT ( 'NONE',  ( 1.096115288130569798, -2.292435215939184534, 0.004638672314880368241 ) ) ;
#83707=CARTESIAN_POINT ( 'NONE',  ( 2.443496805918866865, -1.782974011999260977, 0.6919810379762069141 ) ) ;
#83710=CARTESIAN_POINT ( 'NONE',  ( 0.9670423206251937964, -1.584547017232017518, 1.241716394148101088 ) ) ;
#83711=CARTESIAN_POINT ( 'NONE',  ( 0.7253527386562284018, 0.1980078388067410544, -1.951770168129369543 ) ) ;
#83716=CARTESIAN_POINT ( 'NONE',  ( 4.435544174077206137, 0.8940267830384877046, -1.889970096008020128 ) ) ;
#83717=CARTESIAN_POINT ( 'NONE',  ( 2.570886989259568267, 0.08925172825972882418, -1.767725737713058631 ) ) ;
#83720=CARTESIAN_POINT ( 'NONE',  ( 5.419995920891611085, 1.369053228189264670, -1.838397148955115412 ) ) ;
#83721=CARTESIAN_POINT ( 'NONE',  ( 3.152039231231161587, -1.317153252834550425, 1.137565551706197775 ) ) ;
#83725=CARTESIAN_POINT ( 'NONE',  ( 3.251044507966997177, -1.707695807076513805, -0.2988343314351063484 ) ) ;
#83726=CARTESIAN_POINT ( 'NONE',  ( 3.209609721163650509, -1.773450621654437009, -1.252290679139915319 ) ) ;
#83728=CARTESIAN_POINT ( 'NONE',  ( 5.155482549980198392, 1.942097955248718533, -0.5424665614216088727 ) ) ;
#83729=CARTESIAN_POINT ( 'NONE',  ( 6.739650031034449817, -0.2601230917362121753, 2.000000000000034639 ) ) ;
#83731=CARTESIAN_POINT ( 'NONE',  ( 2.204012588094861780, -1.926017964255047010, 0.04517517324725479899 ) ) ;
#83733=CARTESIAN_POINT ( 'NONE',  ( 5.256174644204150148, 0.8999736644031709476, -2.031094499404682008 ) ) ;
#83735=CARTESIAN_POINT ( 'NONE',  ( -0.2106854629474881058, 5.722459385925042774, -2.591190942950042597 ) ) ;
#83740=CARTESIAN_POINT ( 'NONE',  ( 1.700152687198818402, 1.534743396142525640, 1.606060300191413548 ) ) ;
#83741=CARTESIAN_POINT ( 'NONE',  ( 6.426224708462171087, 1.007414738832881573, 1.683299376423300853 ) ) ;
#83743=CARTESIAN_POINT ( 'NONE',  ( 6.907534427287327361, -0.5096537312613695914, 2.212693016512882416 ) ) ;
#83747=CARTESIAN_POINT ( 'NONE',  ( -0.1048463755018592264, -0.8645036352170620830, -1.819965476435807306 ) ) ;
#83748=CARTESIAN_POINT ( 'NONE',  ( 4.650865732144216835, -0.4487226328800034691, -2.013136760839563166 ) ) ;
#83753=CARTESIAN_POINT ( 'NONE',  ( 5.466025653875023593, 0.9211120992074215419, 1.627924866423650530 ) ) ;
#83754=CARTESIAN_POINT ( 'NONE',  ( 4.570818470097482766, -0.8114142876072638622, 1.532583664885181607 ) ) ;
#83755=CARTESIAN_POINT ( 'NONE',  ( 4.458407330353141518, -1.557363759602323761, -0.7771466779550126880 ) ) ;
#83757=CARTESIAN_POINT ( 'NONE',  ( 1.470720204089857930, -2.178542539925924171, -0.7136519110988813752 ) ) ;
#83759=CARTESIAN_POINT ( 'NONE',  ( 5.161704669080129371, 1.031500688015974054, 1.818515148517543034 ) ) ;
#83760=CARTESIAN_POINT ( 'NONE',  ( 0.1988192939417210425, -0.4940924592915455493, 1.773541111592655373 ) ) ;
#83762=CARTESIAN_POINT ( 'NONE',  ( 2.074842474778653134, -0.8596299393073093542, 1.824119475507138821 ) ) ;
#83763=CARTESIAN_POINT ( 'NONE',  ( 0.3577192552456122665, 2.167005522336755696, -0.3256184645209562190 ) ) ;
#83768=CARTESIAN_POINT ( 'NONE',  ( 3.281995766809755466, 2.068381274212594878, -0.4664580258975092875 ) ) ;
#83770=CARTESIAN_POINT ( 'NONE',  ( 5.795480788678070816, 1.385457615097264394, 1.189071861804301466 ) ) ;
#83776=CARTESIAN_POINT ( 'NONE',  ( 2.935811755974365500, -1.945362344549756539, 0.5428778075214285570 ) ) ;
#83777=CARTESIAN_POINT ( 'NONE',  ( 0.2355646933672841947, -1.925288835042149760, 0.8538303211676525617 ) ) ;
#83780=CARTESIAN_POINT ( 'NONE',  ( 3.625696855625531345, 1.816486592755601315, -0.4036080491761192546 ) ) ;
#83785=CARTESIAN_POINT ( 'NONE',  ( 6.631718597260928050, -1.344210725561691300, -1.562263648894322898 ) ) ;
#83789=CARTESIAN_POINT ( 'NONE',  ( 1.387607149621207236, -0.04906231267952190778, 1.733339852973712292 ) ) ;
#83790=CARTESIAN_POINT ( 'NONE',  ( 1.464397578914914400, 0.1305661322733233098, -1.735479185401978208 ) ) ;
#83791=CARTESIAN_POINT ( 'NONE',  ( 6.252564486485036710, 0.7173172151448119482, 2.193443857502775263 ) ) ;
#83794=CARTESIAN_POINT ( 'NONE',  ( 1.563821040897996895, 2.030780823367520416, -0.3493207144565529942 ) ) ;
#83797=CARTESIAN_POINT ( 'NONE',  ( 6.327535152267887320, -1.632159162827769405, 1.618470562452605455 ) ) ;
#83800=CARTESIAN_POINT ( 'NONE',  ( 0.4968692282744023303, 1.640418903650592508, -1.093199247851096789 ) ) ;
#83801=CARTESIAN_POINT ( 'NONE',  ( 4.623256175466385010, 1.666654777633369555, 0.9376445158523971646 ) ) ;
#83803=CARTESIAN_POINT ( 'NONE',  ( 6.445939570963194143, 0.8488519614954292969, -2.037301952897092594 ) ) ;
#83808=CARTESIAN_POINT ( 'NONE',  ( 0.2057307448365216507, 1.498047248056989522, 1.354806506954453482 ) ) ;
#83809=CARTESIAN_POINT ( 'NONE',  ( 3.417284581939382448, 2.085149140145211799, 0.9887805580795704374 ) ) ;
#83810=CARTESIAN_POINT ( 'NONE',  ( 5.301206097546149465, -1.683542251207278628, 1.007010407901312465 ) ) ;
#83811=CARTESIAN_POINT ( 'NONE',  ( 1.762477828903946442, -0.7011357286515782494, -1.832381215946830011 ) ) ;
#83815=CARTESIAN_POINT ( 'NONE',  ( 0.5325983862809284819, 0.6208049431430485710, 2.024263306480874380 ) ) ;
#83818=CARTESIAN_POINT ( 'NONE',  ( 0.2867153840934756337, 1.362228626754984573, 1.238794746348782505 ) ) ;
#83819=CARTESIAN_POINT ( 'NONE',  ( 4.663029205760478746, 1.682383395889605282, -1.372325453836314768 ) ) ;
#83821=CARTESIAN_POINT ( 'NONE',  ( 2.109781586379317897, 1.642293606977158538, 1.341614810521203349 ) ) ;
#83826=CARTESIAN_POINT ( 'NONE',  ( 2.126313425470290674, 1.189129703756890644, -1.682874868902742405 ) ) ;
#83830=CARTESIAN_POINT ( 'NONE',  ( -0.02264175331115856477, -0.002534049983802035520, -2.089079740194145440 ) ) ;
#83833=CARTESIAN_POINT ( 'NONE',  ( 4.195896582043898704, 1.251535281948525036, 1.445917311372606262 ) ) ;
#83836=CARTESIAN_POINT ( 'NONE',  ( 1.107111304455286049, 1.712943910497457756, -1.478075018494163118 ) ) ;
#83839=CARTESIAN_POINT ( 'NONE',  ( 1.283166710957379220, 0.1313358247177751625, -1.806845861898898953 ) ) ;
#83840=EDGE_CURVE ( 'NONE', #11451, #146910, #41375, .T. ) ;
#83841=CARTESIAN_POINT ( 'NONE',  ( 2.518635572904056374, 0.2389622604833125386, 1.900711705027556153 ) ) ;
#83842=CARTESIAN_POINT ( 'NONE',  ( 2.875506610227479332, -0.2054619808779626633, 2.060159609288146232 ) ) ;
#83844=CARTESIAN_POINT ( 'NONE',  ( 0.5496082175940236736, 0.6205544711120424273, -1.871312427623121000 ) ) ;
#83845=CARTESIAN_POINT ( 'NONE',  ( 4.986905038743431717, -0.2377927182869009337, -1.911709049817163164 ) ) ;
#83846=CARTESIAN_POINT ( 'NONE',  ( 0.5226545517994193313, -1.239659060731788998, -1.946298918093934960 ) ) ;
#83849=CARTESIAN_POINT ( 'NONE',  ( 4.844214494511547286, -0.9753611933653669741, 1.817521503207474076 ) ) ;
#83853=CARTESIAN_POINT ( 'NONE',  ( 5.210040546657988436, -2.096114648464560748, 0.2032773619186321323 ) ) ;
#83856=CARTESIAN_POINT ( 'NONE',  ( 1.258521197368984268, -2.171350058325251187, -0.0004004535333074903960 ) ) ;
#83858=CARTESIAN_POINT ( 'NONE',  ( 5.009125465012424172, 1.878017946038791575, 1.070212309444783294 ) ) ;
#83859=CARTESIAN_POINT ( 'NONE',  ( 5.654946514622759324, 0.3960909877551482827, 1.980269227310478275 ) ) ;
#83865=CARTESIAN_POINT ( 'NONE',  ( 3.942592416894859841, -1.490970858180175940, 1.357867534901323614 ) ) ;
#83870=CARTESIAN_POINT ( 'NONE',  ( 4.627887939457571598, -1.327398817707679868, -1.706084338546076662 ) ) ;
#83874=CARTESIAN_POINT ( 'NONE',  ( 5.694935465533643715, 1.779635825068434984, 0.9480254120717497290 ) ) ;
#83876=CARTESIAN_POINT ( 'NONE',  ( 0.8204219880046401681, 1.592052673282555286, 0.6642659308724234712 ) ) ;
#83882=CARTESIAN_POINT ( 'NONE',  ( 6.010993879215096314, 1.649516084216671397, 0.8821100558755521348 ) ) ;
#83883=CARTESIAN_POINT ( 'NONE',  ( 0.1002437576986033446, -0.9471954198254585178, 1.776316830230479260 ) ) ;
#83887=CARTESIAN_POINT ( 'NONE',  ( 1.752743329737327826, 2.097873456429504735, 0.3079802404963859486 ) ) ;
#83888=CARTESIAN_POINT ( 'NONE',  ( 1.282827611874960416, 1.646826022920354848, -1.163289555428485667 ) ) ;
#83889=CARTESIAN_POINT ( 'NONE',  ( 2.777393361597128685, 0.2615887081860277519, -1.792441719956331170 ) ) ;
#83891=CARTESIAN_POINT ( 'NONE',  ( 6.772347375734490527, -1.334533509509854943, 1.701269717329929820 ) ) ;
#83895=CARTESIAN_POINT ( 'NONE',  ( 0.7959256443332961561, -0.8641892358523853845, -1.709830222631677943 ) ) ;
#83903=CARTESIAN_POINT ( 'NONE',  ( 3.977527890101069996, 2.036293384626610248, -0.7259696361804208742 ) ) ;
#83906=CARTESIAN_POINT ( 'NONE',  ( 2.039458538997685366, 0.004855507148140979744, 2.120778211687989856 ) ) ;
#83907=CARTESIAN_POINT ( 'NONE',  ( 6.668987789458199700, -1.670617902683011025, -0.7365018021969899076 ) ) ;
#83908=CARTESIAN_POINT ( 'NONE',  ( 2.794160851653566535, -1.965818266918018864, -0.1488234875552247316 ) ) ;
#83909=CARTESIAN_POINT ( 'NONE',  ( 5.431871263539022721, -1.864374737420209760, 0.4251265778823994368 ) ) ;
#83912=CARTESIAN_POINT ( 'NONE',  ( 5.916450756658795385, 0.7966118609284984498, 1.801439653064011548 ) ) ;
#83913=CARTESIAN_POINT ( 'NONE',  ( 1.007640649619114148, -0.8727987561519714443, -1.734835989144311919 ) ) ;
#83922=CARTESIAN_POINT ( 'NONE',  ( 6.094389051209717856, -1.018956457145767436, 1.618003106988876283 ) ) ;
#83924=CARTESIAN_POINT ( 'NONE',  ( 3.739080281021702312, 0.3231575147602770426, 2.182976880621155136 ) ) ;
#83926=CARTESIAN_POINT ( 'NONE',  ( 2.134064618640969524, -1.441378300436758630, -1.671108464803609417 ) ) ;
#83928=CARTESIAN_POINT ( 'NONE',  ( 0.5043727151736315806, -1.897847990334254886, -0.2338014693106793551 ) ) ;
#83931=CARTESIAN_POINT ( 'NONE',  ( 3.543477799061961253, 1.872898848466747479, -0.8826743078152868849 ) ) ;
#83935=CARTESIAN_POINT ( 'NONE',  ( 1.762795743007524063, -1.528684080660724920, 1.528680807790387286 ) ) ;
#83936=CARTESIAN_POINT ( 'NONE',  ( 3.421585747727782678, -1.306972202059282218, -1.759028276249123168 ) ) ;
#83942=CARTESIAN_POINT ( 'NONE',  ( 6.416678112323896954, -1.140949303232444478, -1.306061676789990855 ) ) ;
#83944=CARTESIAN_POINT ( 'NONE',  ( 3.696198088285786998, 0.9351842759567146057, -1.847102243037239910 ) ) ;
#83945=CARTESIAN_POINT ( 'NONE',  ( 5.853141746508254251, 0.1553614259057617408, -2.111562834372962438 ) ) ;
#83948=CARTESIAN_POINT ( 'NONE',  ( 2.869919493663297683, -1.948696178941822899, 0.2840860843679354764 ) ) ;
#83949=CARTESIAN_POINT ( 'NONE',  ( 1.177825114000274898, 1.883588471398514264, -0.3297955356276888184 ) ) ;
#83950=CARTESIAN_POINT ( 'NONE',  ( 6.456980045808101032, 0.3985590825250818203, -2.257207781175464056 ) ) ;
#83951=CARTESIAN_POINT ( 'NONE',  ( 3.404746562951190381, 1.438594061741470753, -1.123979961188771304 ) ) ;
#83958=CARTESIAN_POINT ( 'NONE',  ( 4.412362193956616885, -2.012844744014946841, -0.04520991500436136873 ) ) ;
#83960=CARTESIAN_POINT ( 'NONE',  ( 4.100408672059585591, 1.951911038179511726, 0.1965976633130430695 ) ) ;
#83963=CARTESIAN_POINT ( 'NONE',  ( 0.1753634416057497647, 4.084635187426246539, -2.698744815386323381 ) ) ;
#83964=CARTESIAN_POINT ( 'NONE',  ( 0.4332924875789189167, -1.481350984940564830, -1.475676199967065338 ) ) ;
#83965=CARTESIAN_POINT ( 'NONE',  ( 5.260532772634206822, -1.280100971201453497, 1.222426461919926322 ) ) ;
#83967=CARTESIAN_POINT ( 'NONE',  ( 1.922082643403967506, 1.260107670313360240, -1.792737600334909365 ) ) ;
#83968=CARTESIAN_POINT ( 'NONE',  ( 0.04591871184063747030, -1.399829139283098822, 1.033961902999945170 ) ) ;
#83970=CARTESIAN_POINT ( 'NONE',  ( 0.1333692844072559280, 6.947498546895843674, -2.648624074793118233 ) ) ;
#83971=CARTESIAN_POINT ( 'NONE',  ( 0.3809451599157384627, 1.611386624718774918, -0.6158283211408090985 ) ) ;
#83972=CARTESIAN_POINT ( 'NONE',  ( 1.142455020822298106, -0.05817821010643645790, -2.297781139197229372 ) ) ;
#83974=CARTESIAN_POINT ( 'NONE',  ( 0.7674258922165803076, 2.110627382301712540, -0.5898035449652739848 ) ) ;
#83975=CARTESIAN_POINT ( 'NONE',  ( 6.397740202767369766, 0.1737558121157663782, 1.725068634017632885 ) ) ;
#83976=CARTESIAN_POINT ( 'NONE',  ( 2.754729969050898841, 0.7443088323898851000, 2.077706851784946185 ) ) ;
#83978=CARTESIAN_POINT ( 'NONE',  ( 0.5148107762544695820, 0.8296010825015688317, 2.006500992472683098 ) ) ;
#83979=CARTESIAN_POINT ( 'NONE',  ( 1.973964399615803389, -0.9004667817871301327, 1.916432390954267984 ) ) ;
#83981=CARTESIAN_POINT ( 'NONE',  ( 5.368162667233546514, 0.9496366811117643580, 1.675975028240711540 ) ) ;
#83983=CARTESIAN_POINT ( 'NONE',  ( 2.121020962670455923, 0.004254578539099414594, 2.292545472008022056 ) ) ;
#83987=CARTESIAN_POINT ( 'NONE',  ( 4.512477240926440203, -2.220771887297602110, -0.05487108470654011860 ) ) ;
#83995=CARTESIAN_POINT ( 'NONE',  ( 3.322888845334175389, 0.9041102021897020613, -1.802417075407992897 ) ) ;
#83997=CARTESIAN_POINT ( 'NONE',  ( 0.8837254586576195337, -1.959797800638187093, 0.6432524670345032280 ) ) ;
#84002=CARTESIAN_POINT ( 'NONE',  ( 4.400438482046089561, 1.694813852089768869, -1.389250428430639950 ) ) ;
#84003=CARTESIAN_POINT ( 'NONE',  ( 1.547500230860882287, -1.423960469535384465, 1.427938386157491246 ) ) ;
#84004=CARTESIAN_POINT ( 'NONE',  ( 0.8020088176248600931, 1.394402496181508466, -1.202495849378336423 ) ) ;
#84005=CARTESIAN_POINT ( 'NONE',  ( 5.618756969397510126, -0.05950314066365805510, 2.291748599322357194 ) ) ;
#84006=CARTESIAN_POINT ( 'NONE',  ( 3.995923475689294513, -0.5793754966058572986, -1.747668199984537152 ) ) ;
#84008=CARTESIAN_POINT ( 'NONE',  ( 4.049673113991675955, 0.6152068410551281286, -1.718917501701062278 ) ) ;
#84009=CARTESIAN_POINT ( 'NONE',  ( 4.922500090287251773, -1.427935867408920645, -1.423962988533589158 ) ) ;
#84011=CARTESIAN_POINT ( 'NONE',  ( 4.592800228568824750, -0.4914316458759260264, -2.208360408168393629 ) ) ;
#84013=CARTESIAN_POINT ( 'NONE',  ( -0.02264175331115856477, -0.002534049983802035520, -2.089079740194145440 ) ) ;
#84015=CARTESIAN_POINT ( 'NONE',  ( 4.809070886388271404, -1.664838503569150419, 1.230558894880565246 ) ) ;
#84020=CARTESIAN_POINT ( 'NONE',  ( 2.262220261732431403, 0.8237980678013016034, 1.741618625116077235 ) ) ;
#84023=CARTESIAN_POINT ( 'NONE',  ( 6.895365913452266682, -1.760736289220961481, 0.8823945077177670626 ) ) ;
#84027=CARTESIAN_POINT ( 'NONE',  ( 0.5453776912951785460, 0.1620316879334358084, 2.114494688702214020 ) ) ;
#84028=CARTESIAN_POINT ( 'NONE',  ( 1.406790049154776234, -2.211310019597735987, -0.2114152780076440363 ) ) ;
#84030=CARTESIAN_POINT ( 'NONE',  ( 3.329229500047115042, 0.04992189587533709533, 2.105534426424925165 ) ) ;
#84033=CARTESIAN_POINT ( 'NONE',  ( 0.4493573998385214652, 1.374985906440568506, 1.254353302672887693 ) ) ;
#84040=CARTESIAN_POINT ( 'NONE',  ( 1.019968326173793960, -0.5097545255977399270, 2.058319881341897695 ) ) ;
#84043=CARTESIAN_POINT ( 'NONE',  ( 4.791432466842788784, -1.794507165602466037, 0.7932701521168731285 ) ) ;
#84044=CARTESIAN_POINT ( 'NONE',  ( 3.713887418366210280, -2.130098009959373151, 0.3673708613747132534 ) ) ;
#84045=CARTESIAN_POINT ( 'NONE',  ( 1.399689850468607277, -0.6632477835330424787, -1.717811453623831808 ) ) ;
#84049=CARTESIAN_POINT ( 'NONE',  ( 5.103314706128504241, -1.731452751257630096, 0.1754873227253881951 ) ) ;
#84053=CARTESIAN_POINT ( 'NONE',  ( 2.184651956524386041, -2.119909832212972578, -0.4221607449544013679 ) ) ;
#84055=CARTESIAN_POINT ( 'NONE',  ( 3.813827237909522605, -1.649828814528127907, 1.158511658058670957 ) ) ;
#84057=CARTESIAN_POINT ( 'NONE',  ( 1.499129196564863209, 1.767075381950654611, -1.244890797856931686 ) ) ;
#84059=CARTESIAN_POINT ( 'NONE',  ( 3.748864756286158340, -1.612500686720008236, 1.134000162313458793 ) ) ;
#84060=CARTESIAN_POINT ( 'NONE',  ( 3.720204347993858462, 1.845125290474887159, 0.6061553137183937068 ) ) ;
#84071=CARTESIAN_POINT ( 'NONE',  ( 6.821333373144921275, -0.1693730316576994299, 2.270769535942236406 ) ) ;
#84074=CARTESIAN_POINT ( 'NONE',  ( 5.049637047142223167, 1.450995767963231264, 1.320413740667214508 ) ) ;
#84075=CARTESIAN_POINT ( 'NONE',  ( 1.336564801266389990, 0.5826540126645517459, -1.930418273149013153 ) ) ;
#84077=CARTESIAN_POINT ( 'NONE',  ( 2.975892561826110505, -0.8538584053617600533, 1.937700190512989362 ) ) ;
#84081=CARTESIAN_POINT ( 'NONE',  ( 4.523293815724619193, -1.134750198001058585, -1.449786353205910538 ) ) ;
#84086=CARTESIAN_POINT ( 'NONE',  ( 5.256147377898004791, 0.8573370980917979223, -1.939729252509444279 ) ) ;
#84090=CARTESIAN_POINT ( 'NONE',  ( 5.958293153512181917, 0.8310434803317863217, 1.885964484847465705 ) ) ;
#84092=CARTESIAN_POINT ( 'NONE',  ( 1.082201983675265655, 1.112762242526295298, -1.491567265455741476 ) ) ;
#84093=CARTESIAN_POINT ( 'NONE',  ( 2.366542893654680402, 0.08848056876738576160, -1.839231530397527736 ) ) ;
#84098=CARTESIAN_POINT ( 'NONE',  ( 2.420803835572300500, 1.440536793087299205, -1.671967039616916617 ) ) ;
#84099=CARTESIAN_POINT ( 'NONE',  ( 5.009165025557245521, 1.964990322317389015, 1.121224042300600576 ) ) ;
#84101=CARTESIAN_POINT ( 'NONE',  ( 4.201270403262004294, 1.615401881959299235, -0.8201500932763347018 ) ) ;
#84102=CARTESIAN_POINT ( 'NONE',  ( 5.225768846659354594, 0.7701814094057590765, -1.754262016157917881 ) ) ;
#84104=CARTESIAN_POINT ( 'NONE',  ( 3.889495165534775811, 1.427134975246695969, 1.360358076685687978 ) ) ;
#84105=CARTESIAN_POINT ( 'NONE',  ( 5.471519871388384360, 1.802534880541529994, -0.5000026934619330454 ) ) ;
#84106=CARTESIAN_POINT ( 'NONE',  ( 5.107777090148794663, 0.5842497386982176133, -1.767012650282340003 ) ) ;
#84107=CARTESIAN_POINT ( 'NONE',  ( 5.752768645092715794, -1.392961553103783112, 1.091694246300749738 ) ) ;
#84109=CARTESIAN_POINT ( 'NONE',  ( 1.348413808652969337, 2.103741849630758054, 0.1016320799899407962 ) ) ;
#84114=CARTESIAN_POINT ( 'NONE',  ( 3.621431001533811589, 1.820626359085864454, 1.087046460333654485 ) ) ;
#84116=CARTESIAN_POINT ( 'NONE',  ( 2.092062652781300880, 1.246029564253118282, 1.589516146451919631 ) ) ;
#84122=CARTESIAN_POINT ( 'NONE',  ( 1.810078809455554438, -2.145489296895970011, 0.2626290421628638128 ) ) ;
#84123=CARTESIAN_POINT ( 'NONE',  ( 6.890000000000012115, 1.205492346117660762, 2.388860368086835884 ) ) ;
#84130=CARTESIAN_POINT ( 'NONE',  ( 0.7498831369015904746, 2.188782640433343474, -0.1130235578899463078 ) ) ;
#84132=CARTESIAN_POINT ( 'NONE',  ( 1.323510708689378479, -0.05371019744930016770, 2.262043349595239228 ) ) ;
#84140=CARTESIAN_POINT ( 'NONE',  ( 2.741159958678766717, -1.308340514575502045, -1.191892431489706805 ) ) ;
#84142=CARTESIAN_POINT ( 'NONE',  ( 6.141676493652540536, -1.594220855400224401, -1.526124331276897950 ) ) ;
#84146=CARTESIAN_POINT ( 'NONE',  ( 5.466422796518627614, -1.967893101392578448, -0.4390109167287381542 ) ) ;
#84147=CARTESIAN_POINT ( 'NONE',  ( 4.957183922012514898, -1.549878356133486124, 0.9377188026478706639 ) ) ;
#84149=CARTESIAN_POINT ( 'NONE',  ( 2.957714569337116739, 1.861795396119047208, -0.1817069356538636715 ) ) ;
#84150=CARTESIAN_POINT ( 'NONE',  ( 2.711853232431875593, 0.5564382603544040240, -1.993978196652478996 ) ) ;
#84152=CARTESIAN_POINT ( 'NONE',  ( 1.986440140746603911, -1.173720106059353396, 1.509789020923378189 ) ) ;
#84158=CARTESIAN_POINT ( 'NONE',  ( 0.1406777020166137260, 1.830675540527426648, 0.5531436448603862521 ) ) ;
#84160=CARTESIAN_POINT ( 'NONE',  ( 1.890992312513404716, 0.1891058464698439912, 1.952711869325058691 ) ) ;
#84161=CARTESIAN_POINT ( 'NONE',  ( 6.670655732516623360, 7.629137130509072051, 2.773739711112707784 ) ) ;
#84163=CARTESIAN_POINT ( 'NONE',  ( 4.974906307097914926, -1.534222593358970821, 1.464151343314526343 ) ) ;
#84166=CARTESIAN_POINT ( 'NONE',  ( 6.555938671473301227, 1.966215360770405818, -0.1428278144062731236 ) ) ;
#84168=CARTESIAN_POINT ( 'NONE',  ( 1.494390954318410625, -1.073482900754536784, 1.702939308294330489 ) ) ;
#84170=CARTESIAN_POINT ( 'NONE',  ( 1.247838713208373029, 2.085211562554165621, -0.3660346322543471809 ) ) ;
#84172=CARTESIAN_POINT ( 'NONE',  ( 2.857943571468853250, -0.6518772230660694333, 1.965110387975615991 ) ) ;
#84176=CARTESIAN_POINT ( 'NONE',  ( 5.349593081218750434, 2.088290806564324420, -0.1017214290881287009 ) ) ;
#84178=CARTESIAN_POINT ( 'NONE',  ( 4.260648785556298890, -1.352668379831567069, 1.226179085325199258 ) ) ;
#84179=CARTESIAN_POINT ( 'NONE',  ( 2.437905218827548737, -1.044187398466125627, -1.480012136316358085 ) ) ;
#84184=CARTESIAN_POINT ( 'NONE',  ( 5.350674426004140116, 0.6359874849255695572, 2.113150234885258438 ) ) ;
#84187=CARTESIAN_POINT ( 'NONE',  ( 4.301352856729808494, 1.706663192164651122, -0.8627939227693476321 ) ) ;
#84194=CARTESIAN_POINT ( 'NONE',  ( -0.1296875068448159751, 0.001480089298542403009, -1.826395826379861864 ) ) ;
#84196=CARTESIAN_POINT ( 'NONE',  ( 3.672993792711932048, 0.04889617625786558258, -1.870083761627352237 ) ) ;
#84203=CARTESIAN_POINT ( 'NONE',  ( 0.6198874644624132735, 1.948816017023939251, -0.2832832528399802374 ) ) ;
#84204=CARTESIAN_POINT ( 'NONE',  ( 1.739861462675455828, 2.010826045486389102, -0.1511602461454417123 ) ) ;
#84209=CARTESIAN_POINT ( 'NONE',  ( 2.660326705311684581, -1.510451929809487170, 1.587989696798755013 ) ) ;
#84210=CARTESIAN_POINT ( 'NONE',  ( 6.551389018236878137, -1.469694460105780864, -1.082916835497591102 ) ) ;
#84218=CARTESIAN_POINT ( 'NONE',  ( 4.282634502089007533, 1.642705626968201216, -0.8318752211165170163 ) ) ;
#84219=CARTESIAN_POINT ( 'NONE',  ( 0.2760392706695756759, 1.990868297383071139, -0.2976099395228733457 ) ) ;
#84220=CARTESIAN_POINT ( 'NONE',  ( 3.286738001609066817, -2.216000729425780413, 0.6097190577039524051 ) ) ;
#84222=CARTESIAN_POINT ( 'NONE',  ( 0.5845111633032008536, 1.778450750175617712, 0.5478710867917855332 ) ) ;
#84226=CARTESIAN_POINT ( 'NONE',  ( 4.974826827724895928, -1.381046924789817831, 1.323090558688621909 ) ) ;
#84230=CARTESIAN_POINT ( 'NONE',  ( 4.212501570603551571, 1.912301062189927015, 0.8455808105151915166 ) ) ;
#84231=CARTESIAN_POINT ( 'NONE',  ( 2.377632874612686020, 1.149002834218125102, 1.476114537088555112 ) ) ;
#84234=CARTESIAN_POINT ( 'NONE',  ( 5.671403949121008203, 1.101820082107987098, 1.475039313902235305 ) ) ;
#84238=CARTESIAN_POINT ( 'NONE',  ( 4.318794280271901265, 1.578467719028648686, 0.6958846415187101009 ) ) ;
#84240=CARTESIAN_POINT ( 'NONE',  ( 6.252570086353132162, 0.6882034672392455255, 2.096894461246688213 ) ) ;
#84241=CARTESIAN_POINT ( 'NONE',  ( 6.983263157960386103, 3.689421308571324776, 2.567857239638075217 ) ) ;
#84244=CARTESIAN_POINT ( 'NONE',  ( 5.172805277531332457, 1.502137693623846193, -1.567733665727601089 ) ) ;
#84245=CARTESIAN_POINT ( 'NONE',  ( 2.824607995650964209, 1.719152210223941823, 0.6149139946348627372 ) ) ;
#84247=CARTESIAN_POINT ( 'NONE',  ( 5.401600794869550803, -2.065136407520694828, 0.4665587172485561318 ) ) ;
#84249=CARTESIAN_POINT ( 'NONE',  ( 5.724266765471021756, 2.208406811287708660, 0.6146092054917261516 ) ) ;
#84252=CARTESIAN_POINT ( 'NONE',  ( 1.137531110418067204, -0.04838959064331486287, 2.120096749846810624 ) ) ;
#84257=CARTESIAN_POINT ( 'NONE',  ( 6.877770952621925282, -2.108145516380425910, 0.5186976372570563099 ) ) ;
#84258=CARTESIAN_POINT ( 'NONE',  ( 6.883263157960369583, 7.629137130509070275, 2.653810918356712900 ) ) ;
#84260=CARTESIAN_POINT ( 'NONE',  ( 1.401376347886007068, -0.3305552470432049916, -2.196467622588905932 ) ) ;
#84262=CARTESIAN_POINT ( 'NONE',  ( 5.959611329766300258, -1.915599147091971544, -0.6298778581111733610 ) ) ;
#84264=CARTESIAN_POINT ( 'NONE',  ( 4.082923458916259740, 1.956979318386397715, 0.6515942777399350572 ) ) ;
#84269=CARTESIAN_POINT ( 'NONE',  ( 0.4278232814946582585, 1.072867435734598196, -1.794206126505201837 ) ) ;
#84270=CARTESIAN_POINT ( 'NONE',  ( 4.131482539099665452, 0.5404898895830790861, 1.942541833525657680 ) ) ;
#84271=CARTESIAN_POINT ( 'NONE',  ( 4.862772069579198941, 0.1752732939881325724, -1.832877676746891726 ) ) ;
#84273=CARTESIAN_POINT ( 'NONE',  ( 1.113767329461469835, -0.7700024601069790364, -1.543427451845545084 ) ) ;
#84274=CARTESIAN_POINT ( 'NONE',  ( -0.04763828917917976857, -1.313539345393003321, 1.530161206715647149 ) ) ;
#84275=CARTESIAN_POINT ( 'NONE',  ( 1.055823836731560439, -1.452736638576918038, 1.781478128903237756 ) ) ;
#84277=CARTESIAN_POINT ( 'NONE',  ( 0.9137757228094539608, -0.3311857980235459742, 2.237941903941061739 ) ) ;
#84278=CARTESIAN_POINT ( 'NONE',  ( 2.490967578435684615, -0.3607690000238995554, -2.074772605841824991 ) ) ;
#84282=CARTESIAN_POINT ( 'NONE',  ( 5.562500000000004441, -1.451031289061337937, -1.451031289060889851 ) ) ;
#84287=CARTESIAN_POINT ( 'NONE',  ( 4.623389083599304783, 1.933371432498669273, 1.093773624979002879 ) ) ;
#84288=CARTESIAN_POINT ( 'NONE',  ( 3.767680093253112705, 1.217039798425190167, 1.822233383357040104 ) ) ;
#84293=CARTESIAN_POINT ( 'NONE',  ( 6.890000000000037872, 2.400824642991986391, 2.659875214078717853 ) ) ;
#84295=CARTESIAN_POINT ( 'NONE',  ( 6.205353461901607304, 1.844339991697005798, -1.046509186232460697 ) ) ;
#84299=CARTESIAN_POINT ( 'NONE',  ( 6.157120911006636277, -1.851533521339579380, -1.115484332758958974 ) ) ;
#84302=CARTESIAN_POINT ( 'NONE',  ( 6.110883706712432861, -0.2185277653131960651, 1.828168259763853998 ) ) ;
#84305=CARTESIAN_POINT ( 'NONE',  ( 0.8369945909703061515, 0.7069334548283608965, -1.590575932886540755 ) ) ;
#84309=CARTESIAN_POINT ( 'NONE',  ( 5.348557406608104969, 0.6236849695623291057, 2.069784783864880851 ) ) ;
#84313=CARTESIAN_POINT ( 'NONE',  ( 4.381803836707322652, 1.409801062080328959, 1.638821348427916602 ) ) ;
#84315=CARTESIAN_POINT ( 'NONE',  ( 6.397732417105159719, -0.6663202349154914161, 1.855440513692607540 ) ) ;
#84316=CARTESIAN_POINT ( 'NONE',  ( 4.639819690880945480, -0.0003889188416681537710, -1.734034292319245552 ) ) ;
#84318=CARTESIAN_POINT ( 'NONE',  ( 1.681448347407452193, 1.514353137444489406, 1.584415833815432162 ) ) ;
#84319=CARTESIAN_POINT ( 'NONE',  ( 1.852963337694241819, 0.7249817717532834882, 2.190821962643316301 ) ) ;
#84320=CARTESIAN_POINT ( 'NONE',  ( 4.657529158609388986, 0.4554517582456064084, -2.009643979410648651 ) ) ;
#84321=CARTESIAN_POINT ( 'NONE',  ( 0.04082682177056726897, -1.500436592000290670, -1.232479804542076618 ) ) ;
#84327=CARTESIAN_POINT ( 'NONE',  ( 1.160779977835691312, 1.203355533934968635, 1.617816888933524710 ) ) ;
#84329=CARTESIAN_POINT ( 'NONE',  ( 4.173040645679537697, -2.057929556117383374, -0.7971749352265260491 ) ) ;
#84331=CARTESIAN_POINT ( 'NONE',  ( 1.938117168453708627, -1.000761817645494212, 1.568762535561243121 ) ) ;
#84336=CARTESIAN_POINT ( 'NONE',  ( 6.925078400183526384, 2.431821113958906544, 2.425929786733098226 ) ) ;
#84339=CARTESIAN_POINT ( 'NONE',  ( 3.204032760728621643, -2.058606879712703286, 0.09948017704831073338 ) ) ;
#84342=CARTESIAN_POINT ( 'NONE',  ( 2.297526485177129540, 1.845687725436034432, -0.8205148536439119678 ) ) ;
#84345=CARTESIAN_POINT ( 'NONE',  ( 1.446242185974885963, 2.058501543756698915, 0.1019544441857832273 ) ) ;
#84350=CARTESIAN_POINT ( 'NONE',  ( -0.2408018239684408812, 2.868499929943384874, -2.588695376639174484 ) ) ;
#84351=CARTESIAN_POINT ( 'NONE',  ( 0.6734667703603390843, -1.024904740748554532, 1.529287851792550335 ) ) ;
#84352=CARTESIAN_POINT ( 'NONE',  ( 5.268293329372571776, 1.085216321637239023, 1.921556908365213312 ) ) ;
#84354=CARTESIAN_POINT ( 'NONE',  ( 1.669428131952359839, 0.1607934374257547205, -2.155692497560882437 ) ) ;
#84356=CARTESIAN_POINT ( 'NONE',  ( 1.991423064788412800, -0.4370762659771566527, 1.968445590580846893 ) ) ;
#84360=CARTESIAN_POINT ( 'NONE',  ( 4.135589226209329006, -1.358636868218986216, -1.428786634662780219 ) ) ;
#84361=CARTESIAN_POINT ( 'NONE',  ( 3.749232653202066778, 0.2420323627391370025, -2.001857840249580800 ) ) ;
#84365=CARTESIAN_POINT ( 'NONE',  ( 5.110040610736272804, -2.096041292509024156, 0.2052846074404850174 ) ) ;
#84369=CARTESIAN_POINT ( 'NONE',  ( 5.529760519541640384, 1.996289034380031913, -0.5486624943154896350 ) ) ;
#84373=CARTESIAN_POINT ( 'NONE',  ( 5.590105174118587428, 1.206514928144377441, 1.619649990711173215 ) ) ;
#84376=CARTESIAN_POINT ( 'NONE',  ( 1.077094301713815039, 1.904230998939509867, 0.7929820198450258095 ) ) ;
#84384=CARTESIAN_POINT ( 'NONE',  ( 3.068971866484587530, 1.574395709666128296, -1.495330859492151943 ) ) ;
#84387=CARTESIAN_POINT ( 'NONE',  ( 2.524749765808989466, -1.717266272480859834, 0.6646640004178904215 ) ) ;
#84389=CARTESIAN_POINT ( 'NONE',  ( 4.230150181147958044, 2.149441460308566754, 0.4267382380854707336 ) ) ;
#84391=CARTESIAN_POINT ( 'NONE',  ( 4.997079013686112958, 1.883918014071528146, -1.252661935414706162 ) ) ;
#84397=CARTESIAN_POINT ( 'NONE',  ( 0.09216213259799833912, -0.3764253007602496592, -1.735191564994809976 ) ) ;
#84398=CARTESIAN_POINT ( 'NONE',  ( 4.389318492827157137, -0.002256833108382152835, -2.013265972533995640 ) ) ;
#84400=CARTESIAN_POINT ( 'NONE',  ( 3.329229500047115042, 0.04992189587533709533, 2.105534426424925165 ) ) ;
#84401=CARTESIAN_POINT ( 'NONE',  ( 1.247507242870619981, 1.886983585358002813, -0.3289482045247971165 ) ) ;
#84404=CARTESIAN_POINT ( 'NONE',  ( 1.961320326556061922, 1.635743983707088622, 1.096704005335534138 ) ) ;
#84405=CARTESIAN_POINT ( 'NONE',  ( 0.7427767429722329506, -1.606530860214189893, 0.9580933318182258684 ) ) ;
#84406=CARTESIAN_POINT ( 'NONE',  ( 0.5374593765826127800, 1.831924746014142791, -0.7026076897959919743 ) ) ;
#84407=CARTESIAN_POINT ( 'NONE',  ( 6.433875545303581411, -1.754733077360526972, 0.4498553729834730008 ) ) ;
#84411=CARTESIAN_POINT ( 'NONE',  ( 6.016445890116215445, 1.255022122864515310, -1.387330985440645037 ) ) ;
#84413=CARTESIAN_POINT ( 'NONE',  ( 5.506714918851105089, 0.5956099481174789156, 1.982760374633622424 ) ) ;
#84417=CARTESIAN_POINT ( 'NONE',  ( 0.1685321339487330372, -0.8835925182541467526, -1.870455940253319183 ) ) ;
#84424=CARTESIAN_POINT ( 'NONE',  ( 5.371523934717264304, -0.2895824386080196322, 1.940264742196501802 ) ) ;
#84426=CARTESIAN_POINT ( 'NONE',  ( 3.444685325028495004, 1.276847194542466646, 1.560261755768836744 ) ) ;
#84427=CARTESIAN_POINT ( 'NONE',  ( 2.518635572904056374, 0.2389622604833125386, 1.900711705027556153 ) ) ;
#84429=CARTESIAN_POINT ( 'NONE',  ( 0.5916818631664169104, -0.7834642122952638621, 2.046923429677327100 ) ) ;
#84430=CARTESIAN_POINT ( 'NONE',  ( 0.2333690889706717397, 6.947499272388762748, -2.648434294982876303 ) ) ;
#84431=CARTESIAN_POINT ( 'NONE',  ( 2.917106759524803472, -0.1871779394605546654, 1.861177454839262113 ) ) ;
#84435=CARTESIAN_POINT ( 'NONE',  ( 4.675474996081856460, 1.569897879423647336, 1.420792320860002178 ) ) ;
#84437=CARTESIAN_POINT ( 'NONE',  ( 5.687960312649480876, -1.310561514506687564, -1.602779375087557412 ) ) ;
#84438=CARTESIAN_POINT ( 'NONE',  ( 2.243796185194739223, 2.090353954619321275, 0.04827919579214814960 ) ) ;
#84440=CARTESIAN_POINT ( 'NONE',  ( 1.008351294761783423, 1.310062561100222123, -1.121974927168223335 ) ) ;
#84449=CARTESIAN_POINT ( 'NONE',  ( 1.013979471798792886, -1.811656969585205612, -0.0007847632289004204901 ) ) ;
#84458=CARTESIAN_POINT ( 'NONE',  ( 0.6322731411384452382, 0.5572298914768618605, 1.832739050869176101 ) ) ;
#84459=CARTESIAN_POINT ( 'NONE',  ( 0.2059360158346480729, 1.574223368660916611, 1.420867075595611650 ) ) ;
#84465=CARTESIAN_POINT ( 'NONE',  ( 4.065260974683176265, 1.686948271169801616, 1.016115061114295504 ) ) ;
#84466=CARTESIAN_POINT ( 'NONE',  ( 1.014494059972574691, -2.120667955011676487, 0.003750198165439199392 ) ) ;
#84470=CARTESIAN_POINT ( 'NONE',  ( 6.158177532299373702, -1.552315630085840947, 1.547116483708823598 ) ) ;
#84472=CARTESIAN_POINT ( 'NONE',  ( 4.577124784165859772, 0.0005310917307651402686, -1.926566264685470875 ) ) ;
#84474=CARTESIAN_POINT ( 'NONE',  ( -0.1411974294641839822, -0.0004739540254219998553, -1.900147702309517239 ) ) ;
#84475=CARTESIAN_POINT ( 'NONE',  ( 0.7509353727821498348, 0.6442623716619542140, 2.110749664216593047 ) ) ;
#84477=CARTESIAN_POINT ( 'NONE',  ( -0.1108833634137010304, 7.629137130509073828, -2.496956624467902675 ) ) ;
#84480=CARTESIAN_POINT ( 'NONE',  ( 6.121921657745279077, 1.940899573806122325, -0.3330216297181831653 ) ) ;
#84481=CARTESIAN_POINT ( 'NONE',  ( 0.2923913620977801053, 1.614019350141202569, -1.079779171115168523 ) ) ;
#84482=CARTESIAN_POINT ( 'NONE',  ( 6.520923251934013898, 2.292922446452568597, -0.1593734864932250250 ) ) ;
#84484=CARTESIAN_POINT ( 'NONE',  ( 4.504654980070036174, 0.4933668235826896287, 1.794306199697106363 ) ) ;
#84489=CARTESIAN_POINT ( 'NONE',  ( 0.1698123575781598782, 1.266975945507025081, 1.788028528876134393 ) ) ;
#84495=CARTESIAN_POINT ( 'NONE',  ( 0.5041868517345666767, -0.6120625888205477594, -1.720162557568189809 ) ) ;
#84497=CARTESIAN_POINT ( 'NONE',  ( 3.551122959743778562, -1.161752147869070884, 1.287673551650715842 ) ) ;
#84501=CARTESIAN_POINT ( 'NONE',  ( 0.3637320452541660254, 1.905723972499345997, -0.2814332051396683521 ) ) ;
#84502=CARTESIAN_POINT ( 'NONE',  ( 4.047668389856577065, 1.417901948909123799, 1.355967163993692992 ) ) ;
#84506=CARTESIAN_POINT ( 'NONE',  ( 4.916704032076687270, -0.7149955815140829340, -1.996424279390257572 ) ) ;
#84512=CARTESIAN_POINT ( 'NONE',  ( 2.641538584800803502, 1.894577224340647792, -0.8349662684224223863 ) ) ;
#84514=CIRCLE ( 'NONE', #164157, 0.04999999999999970440 ) ;
#84515=CARTESIAN_POINT ( 'NONE',  ( 4.037882060770150439, -2.125535223720369071, 0.6451317522137323124 ) ) ;
#84517=CARTESIAN_POINT ( 'NONE',  ( 2.620138118368781743, 0.2850873451692262361, 2.280912332010568644 ) ) ;
#84523=ORIENTED_EDGE ( 'NONE', *, *, #176754, .T. ) ;
#84525=CARTESIAN_POINT ( 'NONE',  ( 4.324404969281474109, -0.8226261416362996570, -1.726585468271451651 ) ) ;
#84527=CARTESIAN_POINT ( 'NONE',  ( 4.840679758638335883, 0.2971110944181546976, 1.698800604571904849 ) ) ;
#84528=CARTESIAN_POINT ( 'NONE',  ( 3.889861467948488638, -2.010801299972611478, 0.1531677096566556318 ) ) ;
#84529=CARTESIAN_POINT ( 'NONE',  ( 5.660817213934862480, 1.366460917787317930, 1.848312285176759717 ) ) ;
#84531=CARTESIAN_POINT ( 'NONE',  ( 0.1884680354247054990, -1.036234488384666586, 1.948478269905975946 ) ) ;
#84533=CARTESIAN_POINT ( 'NONE',  ( 5.712081065023381754, -0.7967057657092267986, -1.580296573674238259 ) ) ;
#84535=CARTESIAN_POINT ( 'NONE',  ( 1.465189672511356900, 0.1648890142370383061, -2.286389102023842490 ) ) ;
#84536=CARTESIAN_POINT ( 'NONE',  ( 0.4798830478778244868, -0.2081801751476043960, -1.727770289196085329 ) ) ;
#84542=CARTESIAN_POINT ( 'NONE',  ( 0.5905675304203241716, 1.115885162268255293, -1.862360684160404123 ) ) ;
#84543=CARTESIAN_POINT ( 'NONE',  ( 1.288296401830712368, -0.7303101666344159471, -1.879802715551846859 ) ) ;
#84545=CARTESIAN_POINT ( 'NONE',  ( 5.039640240021522999, -1.363685002003648616, -1.361047059521299785 ) ) ;
#84548=CARTESIAN_POINT ( 'NONE',  ( 2.584490447655915624, 1.192291587189574065, 1.874175285706691341 ) ) ;
#84556=CARTESIAN_POINT ( 'NONE',  ( 4.141972075035261547, 0.4693275899197508760, 1.675879475284934195 ) ) ;
#84557=CARTESIAN_POINT ( 'NONE',  ( 2.189831975649577878, -1.279155337443920404, -1.487614327915102619 ) ) ;
#84561=CARTESIAN_POINT ( 'NONE',  ( 1.082570677935968062, 1.230128212588364356, -1.655568962787755005 ) ) ;
#84566=CARTESIAN_POINT ( 'NONE',  ( 1.024742985469536016, 1.345695571256789513, -1.818664117639690714 ) ) ;
#84570=CARTESIAN_POINT ( 'NONE',  ( 2.530351333283612281, 1.813318468827030072, 0.4585936022679508728 ) ) ;
#84571=CARTESIAN_POINT ( 'NONE',  ( 1.547078507373225165, -1.226440487959565173, 1.226290910655163380 ) ) ;
#84572=CARTESIAN_POINT ( 'NONE',  ( 4.933237592207079025, -1.549687834843778811, -1.549900206446311657 ) ) ;
#84573=CARTESIAN_POINT ( 'NONE',  ( 5.210162647842351724, -2.297074225899544242, 0.2200332968223562558 ) ) ;
#84574=CARTESIAN_POINT ( 'NONE',  ( 1.797801859905317823, -0.6954313725856995365, 1.940136720205553278 ) ) ;
#84575=CARTESIAN_POINT ( 'NONE',  ( 3.064326467805338350, -1.794528509343394473, -0.7426413790867588682 ) ) ;
#84578=CARTESIAN_POINT ( 'NONE',  ( 6.239502018287079288, -1.354773164471131164, -1.289998633004642237 ) ) ;
#84579=CARTESIAN_POINT ( 'NONE',  ( 1.656250000000001554, -1.895863743164051485, 0.7852924748300756930 ) ) ;
#84581=CARTESIAN_POINT ( 'NONE',  ( 0.1570416503036062006, -0.3615154868755916517, -1.700924732364687220 ) ) ;
#84585=CARTESIAN_POINT ( 'NONE',  ( 4.113907844847329187, 0.1017495355152969322, 2.013985960686740295 ) ) ;
#84589=CARTESIAN_POINT ( 'NONE',  ( 2.314841291766779108, 1.630546960418734148, 0.8213866120303781049 ) ) ;
#84597=CARTESIAN_POINT ( 'NONE',  ( 0.4572932007271997001, -1.730182198833930318, 1.041906760498239271 ) ) ;
#84598=CARTESIAN_POINT ( 'NONE',  ( 0.4168467196605326053, -0.7183999135813922132, -1.995210048009891102 ) ) ;
#84602=CARTESIAN_POINT ( 'NONE',  ( 5.524313221898556669, 1.229557446212639071, -1.653754484787550494 ) ) ;
#84603=CARTESIAN_POINT ( 'NONE',  ( 5.186172726741035355, 1.650080556555008293, 1.158690440749516881 ) ) ;
#84606=CARTESIAN_POINT ( 'NONE',  ( -0.2108831679770960255, 0.2438762813419328990, -1.931650693707862132 ) ) ;
#84610=CARTESIAN_POINT ( 'NONE',  ( 5.413435409655408925, 0.5825687168248098180, 1.930121546480124461 ) ) ;
#84611=CARTESIAN_POINT ( 'NONE',  ( 4.435397664686764330, 0.7849604969769330420, -1.665558179074405620 ) ) ;
#84612=CARTESIAN_POINT ( 'NONE',  ( 0.07661050522431847587, 7.629137130509112907, -2.310792076560589603 ) ) ;
#84613=CARTESIAN_POINT ( 'NONE',  ( 2.174872218848258765, -1.417835807431093276, 1.820694940605925849 ) ) ;
#84615=CARTESIAN_POINT ( 'NONE',  ( 5.132170659515546518, 1.116069247042193124, -1.851066442873222639 ) ) ;
#84617=CARTESIAN_POINT ( 'NONE',  ( 0.2220789341932476180, 1.858810982918417620, 0.5625763381651854855 ) ) ;
#84621=CARTESIAN_POINT ( 'NONE',  ( 3.713615009860570915, -1.843089489661839053, 0.3189824552965599969 ) ) ;
#84622=CARTESIAN_POINT ( 'NONE',  ( 0.7910927259777954523, -0.04954035392716604758, -1.911929172785244102 ) ) ;
#84625=CARTESIAN_POINT ( 'NONE',  ( 2.719571217284349363, -0.2154062111461417517, 2.196339928330424129 ) ) ;
#84632=CARTESIAN_POINT ( 'NONE',  ( 1.036326318785439016, 1.941456103877332140, 0.3412654001589945918 ) ) ;
#84633=CARTESIAN_POINT ( 'NONE',  ( 0.1304780226794301778, -1.424241760892838382, -1.816604428824322159 ) ) ;
#84634=CARTESIAN_POINT ( 'NONE',  ( 1.064813361795993618, 1.487921858168140377, -1.278797858372302088 ) ) ;
#84635=CARTESIAN_POINT ( 'NONE',  ( 3.854389151762872778, -2.059979072249884080, -0.1062074158154867054 ) ) ;
#84643=CARTESIAN_POINT ( 'NONE',  ( 6.478989045741552211, 2.023467559352111866, 0.7875856005067942700 ) ) ;
#84645=CARTESIAN_POINT ( 'NONE',  ( 6.198766299729112639, 1.534709720371667308, 1.016988835930050739 ) ) ;
#84650=CARTESIAN_POINT ( 'NONE',  ( 1.686563950722594685, -0.2693046698774223535, -1.850923959389898288 ) ) ;
#84655=CARTESIAN_POINT ( 'NONE',  ( 1.049298088506251947, -1.728493729547800895, 0.8183166869351959916 ) ) ;
#84657=CARTESIAN_POINT ( 'NONE',  ( 3.291635156611854462, -0.7182737719314927771, 1.617730789815795545 ) ) ;
#84658=CARTESIAN_POINT ( 'NONE',  ( 0.2231138172586397683, 1.663799575440491285, 0.9424754157791456199 ) ) ;
#84660=CARTESIAN_POINT ( 'NONE',  ( 4.358935675595962955, -0.003970376728411328937, -1.915793142021319007 ) ) ;
#84661=CARTESIAN_POINT ( 'NONE',  ( -0.1409997244345879974, 6.947781918643359589, -2.595319453918026653 ) ) ;
#84662=CARTESIAN_POINT ( 'NONE',  ( 5.582459562482231519, 1.174703874196600495, -1.580708309230594688 ) ) ;
#84663=CARTESIAN_POINT ( 'NONE',  ( 0.6156802735862785259, 1.737094954450137285, 1.216079458918501333 ) ) ;
#84665=CARTESIAN_POINT ( 'NONE',  ( 3.731198135974967300, -1.728734619261709904, 0.7151963084984153118 ) ) ;
#84666=CARTESIAN_POINT ( 'NONE',  ( 0.8381832108898427114, 1.798179982845280467, 0.3147962740308178353 ) ) ;
#84668=CARTESIAN_POINT ( 'NONE',  ( 3.211752199052122503, -0.4303563718574507369, 2.164345902561148005 ) ) ;
#84671=CARTESIAN_POINT ( 'NONE',  ( 0.5552253240413919100, 1.715889405040219584, -1.144428160675447614 ) ) ;
#84677=EDGE_CURVE ( 'NONE', #110107, #46524, #190582, .T. ) ;
#84678=CARTESIAN_POINT ( 'NONE',  ( 0.1753634416057497925, 0.0001173177735149660839, -2.144164757042037017 ) ) ;
#84680=CARTESIAN_POINT ( 'NONE',  ( 3.613788337741298040, 0.5058112091442801272, -2.007490274132675445 ) ) ;
#84683=CARTESIAN_POINT ( 'NONE',  ( 1.440939128517594758, 0.4201678954103040819, 2.120193794684998245 ) ) ;
#84685=CARTESIAN_POINT ( 'NONE',  ( 1.822921661270057836, 1.494980448624585234, -1.358156064218164927 ) ) ;
#84691=CARTESIAN_POINT ( 'NONE',  ( 0.7082206942033396624, 1.197301205363930254, -1.622488844446705381 ) ) ;
#84692=CARTESIAN_POINT ( 'NONE',  ( 4.898067072109578035, -0.7382639882421681010, -2.063579870930781546 ) ) ;
#84695=CARTESIAN_POINT ( 'NONE',  ( 3.797043250571481732, -0.1924442655423033721, -1.902711443722324258 ) ) ;
#84699=CARTESIAN_POINT ( 'NONE',  ( 0.7906389332529573100, 1.525030349845598820, -1.319245847334844735 ) ) ;
#84701=CARTESIAN_POINT ( 'NONE',  ( 0.9257723888009254942, -1.459437212925698502, -1.767766894381626486 ) ) ;
#84703=CARTESIAN_POINT ( 'NONE',  ( 3.662884335446520367, -1.521034750653621481, -0.8131990640867832187 ) ) ;
#84707=CARTESIAN_POINT ( 'NONE',  ( 1.152704166800899932, -0.4732522875653189520, -1.903817266927515961 ) ) ;
#84710=CARTESIAN_POINT ( 'NONE',  ( 0.07556134207192893859, 0.6772206542668850471, -2.324809334106460845 ) ) ;
#84714=CARTESIAN_POINT ( 'NONE',  ( 3.492628052329676880, -1.746589362535276191, -0.4802254367691183856 ) ) ;
#84717=CARTESIAN_POINT ( 'NONE',  ( 4.951724851890283219, -1.284874556838147219, -1.277195305962516292 ) ) ;
#84719=SURFACE_STYLE_USAGE ( .BOTH. , #167048 ) ;
#84721=CARTESIAN_POINT ( 'NONE',  ( 6.355886303346764521, -0.6260325832568144344, 1.752714347800623518 ) ) ;
#84723=CARTESIAN_POINT ( 'NONE',  ( 3.321808155663192874, 0.8583493116562285197, -1.712590381118280991 ) ) ;
#84731=CARTESIAN_POINT ( 'NONE',  ( 0.6026772488060898603, -0.7295331166810550272, -2.035022307366324945 ) ) ;
#84735=CARTESIAN_POINT ( 'NONE',  ( 0.7623938366894518204, -1.325735992016435105, 1.255310662410371370 ) ) ;
#84737=CARTESIAN_POINT ( 'NONE',  ( 3.575057022766346293, 0.04566639709948847742, -1.825179878808772305 ) ) ;
#84739=CARTESIAN_POINT ( 'NONE',  ( 2.197387184563174944, 1.746976956643018442, -0.7784620831182070821 ) ) ;
#84741=CARTESIAN_POINT ( 'NONE',  ( 3.244544899158372520, -1.939951241085198896, -0.3392403660903812734 ) ) ;
#84742=CARTESIAN_POINT ( 'NONE',  ( 5.390160969041248862, -0.4756269310413098750, -1.882793909387857179 ) ) ;
#84745=CARTESIAN_POINT ( 'NONE',  ( 4.254221937059123881, 0.9039275175388861161, -1.918405034562712830 ) ) ;
#84755=CARTESIAN_POINT ( 'NONE',  ( 5.549374350267230582, -1.441814640532925074, -1.119852386600270533 ) ) ;
#84760=CARTESIAN_POINT ( 'NONE',  ( 5.770339134078734666, -1.185559297855027561, 1.446973003893243348 ) ) ;
#84762=CARTESIAN_POINT ( 'NONE',  ( 3.475144788579834110, 0.04656949993332368254, -1.926097043150078791 ) ) ;
#84771=CARTESIAN_POINT ( 'NONE',  ( 0.7732552308061869661, 1.865071980587120315, -1.002124039132473055 ) ) ;
#84774=CARTESIAN_POINT ( 'NONE',  ( 5.893440691016273547, -1.874049447596724427, 0.8799615681738190975 ) ) ;
#84775=CARTESIAN_POINT ( 'NONE',  ( 1.663359199420410883, 0.9473472845980964729, 1.578708189602283873 ) ) ;
#84780=CARTESIAN_POINT ( 'NONE',  ( 2.010137459244505820, -1.083026110817113086, -2.020279618534262855 ) ) ;
#84781=CARTESIAN_POINT ( 'NONE',  ( -0.01727558406095473439, -0.1313277740116538805, -1.795991579427682838 ) ) ;
#84785=CARTESIAN_POINT ( 'NONE',  ( 0.6682274066662279299, 2.010706302723582972, -0.1030755154480169355 ) ) ;
#84786=CARTESIAN_POINT ( 'NONE',  ( 1.375751926856683127, -1.915142299924106339, 0.4244507266663796741 ) ) ;
#84791=CARTESIAN_POINT ( 'NONE',  ( 4.189459526602421491, -0.8002100119003925371, 1.931633446273020693 ) ) ;
#84792=CARTESIAN_POINT ( 'NONE',  ( 2.729092984789914578, -1.652188407247729529, 0.6350153418272014294 ) ) ;
#84795=CARTESIAN_POINT ( 'NONE',  ( 5.261813964552005451, 1.126222290254262015, 1.996463630829442337 ) ) ;
#84796=CARTESIAN_POINT ( 'NONE',  ( 3.345385115808647392, 1.740516467222261499, -0.001323508237265763176 ) ) ;
#84799=CARTESIAN_POINT ( 'NONE',  ( 3.795997188448175130, -1.602592684597732298, 0.6622489764130984335 ) ) ;
#84800=CARTESIAN_POINT ( 'NONE',  ( 4.035715546050927749, 2.045666111725014780, -0.7279006231073074096 ) ) ;
#84802=CARTESIAN_POINT ( 'NONE',  ( 4.680875185974167074, 1.673856063443099895, -1.124242729735332347 ) ) ;
#84803=CARTESIAN_POINT ( 'NONE',  ( 1.218750000000000888, -0.7852924748299231483, 1.895863743164115656 ) ) ;
#84805=CARTESIAN_POINT ( 'NONE',  ( 1.782126058915745936, -1.032679515686143024, 1.626040290554785717 ) ) ;
#84807=CARTESIAN_POINT ( 'NONE',  ( 5.801095770108652516, -0.3255204119565913157, -2.197341616521626406 ) ) ;
#84809=CARTESIAN_POINT ( 'NONE',  ( 6.883263157960391787, -0.001104538646235289417, 1.946037152736757925 ) ) ;
#84814=CARTESIAN_POINT ( 'NONE',  ( 0.7334294796089964041, 2.054545164755026576, 0.8448789909778311458 ) ) ;
#84815=CARTESIAN_POINT ( 'NONE',  ( 6.127397123722368555, 0.1457569626216181913, -1.956525209266091192 ) ) ;
#84818=CARTESIAN_POINT ( 'NONE',  ( 6.415309710857563630, -0.2865549832780675543, 2.244158528320794765 ) ) ;
#84822=CARTESIAN_POINT ( 'NONE',  ( 4.176276986610152342, -1.057847390704643509, -1.770619276543743625 ) ) ;
#84827=CARTESIAN_POINT ( 'NONE',  ( 6.292256349370360269, -1.861554482619768525, -0.1834065582871149958 ) ) ;
#84828=CARTESIAN_POINT ( 'NONE',  ( 4.605968593894432139, -0.07825817699743177480, 1.732511586087708499 ) ) ;
#84829=CARTESIAN_POINT ( 'NONE',  ( 4.194663043249587275, 1.400965740628885126, 1.032472458625796286 ) ) ;
#84831=CARTESIAN_POINT ( 'NONE',  ( 1.646416196899816997, 0.7239943723881783200, 2.175097950400638691 ) ) ;
#84833=CARTESIAN_POINT ( 'NONE',  ( 5.495677747024089399, -2.090933975967598446, 0.001106539467419370270 ) ) ;
#84834=CARTESIAN_POINT ( 'NONE',  ( 0.3218710511002781383, 1.760991339961643920, 0.5373333866721883290 ) ) ;
#84836=CARTESIAN_POINT ( 'NONE',  ( 2.039685609654022347, -1.556907966322677472, 1.281362143053674130 ) ) ;
#84842=CARTESIAN_POINT ( 'NONE',  ( 2.789816089392273213, 2.012775272720100705, -0.6673941125509493810 ) ) ;
#84844=CARTESIAN_POINT ( 'NONE',  ( 5.690036971771410101, -0.8169618954828453683, 1.632782195682795257 ) ) ;
#84850=CARTESIAN_POINT ( 'NONE',  ( 3.357680014348028763, -1.532128950806666445, -1.316242992507418386 ) ) ;
#84851=CARTESIAN_POINT ( 'NONE',  ( 6.387735258934439386, 1.517164627179751646, 1.602757196154185770 ) ) ;
#84853=CARTESIAN_POINT ( 'NONE',  ( 3.660865129197692358, 1.469539745679597553, -1.141665872729610287 ) ) ;
#84863=CARTESIAN_POINT ( 'NONE',  ( 1.493026163575939425, 1.669116110853157808, 0.4689669769783275100 ) ) ;
#84864=CARTESIAN_POINT ( 'NONE',  ( 1.798380396644788659, 1.445777515557338688, 0.9684012028719732879 ) ) ;
#84865=CARTESIAN_POINT ( 'NONE',  ( 6.586558022634583232, -2.261718397432868066, -0.4576183726279075548 ) ) ;
#84868=CARTESIAN_POINT ( 'NONE',  ( 1.071639231386111391, 1.986785141929363618, -0.5470796107636519690 ) ) ;
#84869=CARTESIAN_POINT ( 'NONE',  ( 0.5618747747782488755, 1.677749815653075460, -1.117659098820653174 ) ) ;
#84872=CARTESIAN_POINT ( 'NONE',  ( 6.825078400183573812, 0.002648415797040087893, 1.855566311045192540 ) ) ;
#84873=CARTESIAN_POINT ( 'NONE',  ( 4.869353489999923568, -1.618680692612521455, -1.018082601613921723 ) ) ;
#84875=CARTESIAN_POINT ( 'NONE',  ( 5.883472226557855400, 2.040502603023553796, -0.8411249186189362348 ) ) ;
#84882=CARTESIAN_POINT ( 'NONE',  ( 6.393239817247728496, -0.1034752114322245314, -2.118097640427937911 ) ) ;
#84883=CARTESIAN_POINT ( 'NONE',  ( 3.540313787445231508, 1.039887675495542618, -2.060077152250729071 ) ) ;
#84884=CARTESIAN_POINT ( 'NONE',  ( 5.230891786122516152, -1.846674803186045821, -0.6626716404555529349 ) ) ;
#84885=CARTESIAN_POINT ( 'NONE',  ( 0.9011314981347726683, -1.685442764318560771, 1.003610994683441948 ) ) ;
#84889=CARTESIAN_POINT ( 'NONE',  ( 0.4271636869729276698, -1.812546591343185298, 1.094284096637233583 ) ) ;
#84893=CARTESIAN_POINT ( 'NONE',  ( 2.835037514343414777, -2.076374246603398532, -0.6340929010987955694 ) ) ;
#84895=CARTESIAN_POINT ( 'NONE',  ( 0.7914572142167939361, -0.05789999323873443182, -2.119991495365561640 ) ) ;
#84901=CARTESIAN_POINT ( 'NONE',  ( 1.792332366127664223, -2.050593157767267805, -0.2048568651325937962 ) ) ;
#84905=CARTESIAN_POINT ( 'NONE',  ( 0.07755575628183573877, -0.002876890934064984650, -2.188974970840869005 ) ) ;
#84907=CARTESIAN_POINT ( 'NONE',  ( 4.565046243057500952, -1.533749416048999947, 1.141898535029245432 ) ) ;
#84909=CARTESIAN_POINT ( 'NONE',  ( 1.054439146255849780, 2.259743442402757818, -0.1116689827955052033 ) ) ;
#84911=CARTESIAN_POINT ( 'NONE',  ( 1.476514701902143623, -1.279619142688562805, 1.282606640394849951 ) ) ;
#84912=CARTESIAN_POINT ( 'NONE',  ( 0.3564614995229599681, -1.804831555932787657, -0.6427613734035338977 ) ) ;
#84913=CARTESIAN_POINT ( 'NONE',  ( 1.539598694730393680, 1.913698299121506352, -0.7905179490511196061 ) ) ;
#84915=CARTESIAN_POINT ( 'NONE',  ( 0.9714808946714141857, 1.900638238906343425, -0.5234924991099793035 ) ) ;
#84916=CARTESIAN_POINT ( 'NONE',  ( 5.883413297016587329, 1.779079706761811153, -0.7395700111451685155 ) ) ;
#84917=CARTESIAN_POINT ( 'NONE',  ( 6.604147088760183415, -2.206502607372296421, 0.04933187264975073122 ) ) ;
#84920=CARTESIAN_POINT ( 'NONE',  ( 3.736832797123919025, -1.987151705994869344, -0.5527697292582544053 ) ) ;
#84927=CARTESIAN_POINT ( 'NONE',  ( 5.544006925699364707, 0.8563935509715396854, -1.924162301928746821 ) ) ;
#84929=CARTESIAN_POINT ( 'NONE',  ( 1.240952474410524031, -2.118199589774888647, -0.4760015480929754017 ) ) ;
#84931=CARTESIAN_POINT ( 'NONE',  ( 4.815789973571149574, -2.120931333841672650, 0.4164600335647972162 ) ) ;
#84932=CARTESIAN_POINT ( 'NONE',  ( 5.672522982350666432, 0.8204337683548768023, 1.845723718880077469 ) ) ;
#84933=DIRECTION ( 'NONE',  ( 1.214306433183764966E-17, 1.000000000000000000, 5.200010849845536803E-32 ) ) ;
#84938=CARTESIAN_POINT ( 'NONE',  ( 3.134000194803722383, 2.016708403948695771, -0.004836970814638129855 ) ) ;
#84942=CARTESIAN_POINT ( 'NONE',  ( 4.838837662799537753, 0.3661284547709364734, 2.130314178654398205 ) ) ;
#84947=CARTESIAN_POINT ( 'NONE',  ( 4.939077454563308933, -1.704950310733845065, -1.076300583479961048 ) ) ;
#84949=CARTESIAN_POINT ( 'NONE',  ( 0.3458015845922198239, 1.719860733928044949, 0.1322621976239789499 ) ) ;
#84954=CARTESIAN_POINT ( 'NONE',  ( 5.255093269098372488, -1.579555527043162488, -1.001684657140684775 ) ) ;
#84955=CARTESIAN_POINT ( 'NONE',  ( 6.117445361114795865, 1.676175193246462802, 1.114809878595341308 ) ) ;
#84961=CARTESIAN_POINT ( 'NONE',  ( 2.104293207771616991, -0.9040658786637757460, 1.918231223523607865 ) ) ;
#84962=CARTESIAN_POINT ( 'NONE',  ( 0.4215001937674204280, -1.427952733550428288, -1.423947716221201976 ) ) ;
#84963=CARTESIAN_POINT ( 'NONE',  ( 1.476514701902143623, -1.279619142688562805, 1.282606640394849951 ) ) ;
#84965=CARTESIAN_POINT ( 'NONE',  ( 6.385629968321593353, 1.486944277142748794, 1.569300510047972219 ) ) ;
#84969=CARTESIAN_POINT ( 'NONE',  ( 0.2334084307264666924, 0.5983727300521198833, -1.819970363327483076 ) ) ;
#84976=CARTESIAN_POINT ( 'NONE',  ( 3.924826023212550030, 2.051882857192890430, 0.6804245187241527715 ) ) ;
#84979=CARTESIAN_POINT ( 'NONE',  ( 1.898838059644195386, -2.080654286433290867, -0.4088066060855889972 ) ) ;
#84980=CARTESIAN_POINT ( 'NONE',  ( 6.405291383686445350, 1.519602032305459316, 1.011395407323860907 ) ) ;
#84981=CARTESIAN_POINT ( 'NONE',  ( 1.633988421434044325, 0.9753176276560069358, -1.713140426071022349 ) ) ;
#84982=CARTESIAN_POINT ( 'NONE',  ( 4.851772015791367743, -1.356534033432246211, -1.348250844427544282 ) ) ;
#84985=CARTESIAN_POINT ( 'NONE',  ( 6.408657466097477773, 0.6165391127177908270, 1.870651749748206916 ) ) ;
#84986=CARTESIAN_POINT ( 'NONE',  ( 1.218581363712217591, -0.04816221259190026777, 1.941509521754792855 ) ) ;
#84993=CARTESIAN_POINT ( 'NONE',  ( 4.793567869993575314, 1.782951692925707654, -0.6917526515820491273 ) ) ;
#84995=CARTESIAN_POINT ( 'NONE',  ( 3.791807063958370971, 1.597966631936774684, 1.522356218736670153 ) ) ;
#84996=CARTESIAN_POINT ( 'NONE',  ( 2.380145745526092593, 1.357289424207007489, 1.739932290444376584 ) ) ;
#84998=CARTESIAN_POINT ( 'NONE',  ( 0.6977377480232997975, 1.284608138224270002, 1.416691289136004395 ) ) ;
#85002=CARTESIAN_POINT ( 'NONE',  ( 3.016144355299533952, 2.060630728401948275, -0.2003171163396169074 ) ) ;
#85007=CARTESIAN_POINT ( 'NONE',  ( 2.079201547314021070, -0.1057080177612122196, -2.159229931372666389 ) ) ;
#85008=CARTESIAN_POINT ( 'NONE',  ( 3.333693798916517625, 0.9835563995168915552, -1.958507884819527867 ) ) ;
#85016=CARTESIAN_POINT ( 'NONE',  ( 5.449791032962750137, -1.571470184986222263, -0.7336466892688772168 ) ) ;
#85018=CARTESIAN_POINT ( 'NONE',  ( 3.397389602098393802, -1.828008730618407851, 0.9717071122367711977 ) ) ;
#85019=CARTESIAN_POINT ( 'NONE',  ( 4.991875679739185223, -2.106924267290931851, 0.2088435281543659927 ) ) ;
#85022=CARTESIAN_POINT ( 'NONE',  ( 2.553506168856953806, 1.519147476331883517, 1.253303911792477132 ) ) ;
#85023=CARTESIAN_POINT ( 'NONE',  ( 0.3164790345465406385, -0.6463921985436006379, -1.799943259716822341 ) ) ;
#85024=CARTESIAN_POINT ( 'NONE',  ( 4.927800006241752406, 1.181458742244513971, -1.964204249851936090 ) ) ;
#85025=CARTESIAN_POINT ( 'NONE',  ( 2.578497204056416248, -1.747032809129964281, -0.5301130021647950663 ) ) ;
#85031=CARTESIAN_POINT ( 'NONE',  ( 3.761980314931902214, 0.6741652524458006113, -1.897120442666611506 ) ) ;
#85032=CARTESIAN_POINT ( 'NONE',  ( 4.381663332995835880, -1.878531202089319674, 0.5654445158327011667 ) ) ;
#85035=CARTESIAN_POINT ( 'NONE',  ( 0.07536363704235479744, 6.947016338497881804, -2.739277465201896078 ) ) ;
#85036=CARTESIAN_POINT ( 'NONE',  ( 0.04657986452102218927, -1.676603903080859492, 1.248863468804935151 ) ) ;
#85037=CARTESIAN_POINT ( 'NONE',  ( 5.893352214189693683, 1.342564598491655437, 1.153274331617970550 ) ) ;
#85039=CARTESIAN_POINT ( 'NONE',  ( 2.203317661949526052, -0.4785072280911427667, 2.138412878249687399 ) ) ;
#85040=CARTESIAN_POINT ( 'NONE',  ( 0.2568327444973814155, 1.721937519821172602, -0.2522849218079876721 ) ) ;
#85042=CARTESIAN_POINT ( 'NONE',  ( 0.1335669894368813060, 0.6916768264315333870, -2.234939561487662818 ) ) ;
#85043=CARTESIAN_POINT ( 'NONE',  ( 0.2578720826223569462, 0.6548769427211723615, 1.595941719785697988 ) ) ;
#85044=CARTESIAN_POINT ( 'NONE',  ( 0.8612291682562907003, -0.8250023432496387255, 2.145356560901264142 ) ) ;
#85045=CARTESIAN_POINT ( 'NONE',  ( 0.2225716830646235489, 2.098996182288978218, 0.6302611576235671587 ) ) ;
#85046=CARTESIAN_POINT ( 'NONE',  ( 6.591143254762334536, 0.9945565086073978600, -1.419977980273220863 ) ) ;
#85047=CARTESIAN_POINT ( 'NONE',  ( 3.387540773601561916, 1.995160029947869340, -0.9435142334218297178 ) ) ;
#85048=CARTESIAN_POINT ( 'NONE',  ( 6.584450689261575285, 1.255587272919860942, -1.771131291935989616 ) ) ;
#85050=CARTESIAN_POINT ( 'NONE',  ( 1.042374724401398334, 0.8638241406289723923, 1.933313940807819487 ) ) ;
#85051=CARTESIAN_POINT ( 'NONE',  ( 6.727182134110200273, 0.5640974741700152117, 2.241195997201197443 ) ) ;
#85052=CARTESIAN_POINT ( 'NONE',  ( 5.034167752753979208, 0.9906028322895725768, -1.652054708979720399 ) ) ;
#85055=CARTESIAN_POINT ( 'NONE',  ( 1.382826565882399272, -0.3421621995536459626, -2.266597836251768250 ) ) ;
#85059=CARTESIAN_POINT ( 'NONE',  ( 5.338630837375411886, 1.324400161455315805, -1.783172940106398485 ) ) ;
#85065=CARTESIAN_POINT ( 'NONE',  ( 2.865861461037176205, -0.1511401116795624278, -2.010826411938296143 ) ) ;
#85067=CARTESIAN_POINT ( 'NONE',  ( 1.323174825800084609, -1.862915942116917689, -0.8856262590048938899 ) ) ;
#85073=CARTESIAN_POINT ( 'NONE',  ( 3.890727776643727598, 1.851661642969665067, -1.171806376371389957 ) ) ;
#85074=CARTESIAN_POINT ( 'NONE',  ( 1.266250242576156815, 1.862016182229693673, -0.7743172429433076154 ) ) ;
#85075=CARTESIAN_POINT ( 'NONE',  ( 1.259045258496578557, 1.813921241667546758, -0.3151448728593714277 ) ) ;
#85076=CARTESIAN_POINT ( 'NONE',  ( 5.460555387939631800, -2.071112900911156185, -0.9828140750258400615 ) ) ;
#85077=CARTESIAN_POINT ( 'NONE',  ( 2.870863542623874221, 1.748142402769039760, -0.5779331317549916136 ) ) ;
#85080=CARTESIAN_POINT ( 'NONE',  ( 3.733261478165556646, -1.687024869733319221, 0.6981082995600741414 ) ) ;
#85081=CARTESIAN_POINT ( 'NONE',  ( 5.203750078570229753, 1.864167652161516031, 0.7691231355932278690 ) ) ;
#85083=CARTESIAN_POINT ( 'NONE',  ( 4.364347144703619286, 1.063191675971109307, 1.997143021516068595 ) ) ;
#85085=CARTESIAN_POINT ( 'NONE',  ( 6.370163019944321547, 1.079249059096079044, 1.808242165975785909 ) ) ;
#85087=CARTESIAN_POINT ( 'NONE',  ( 3.631357695093720750, 0.05367941694835526995, -2.069842578854002468 ) ) ;
#85092=CARTESIAN_POINT ( 'NONE',  ( 1.629391185616009707, -1.814203104720218951, 0.6484763462606003559 ) ) ;
#85094=CARTESIAN_POINT ( 'NONE',  ( 6.825064197248748243, -1.799304382776808930, -0.8012231885662893793 ) ) ;
#85098=CARTESIAN_POINT ( 'NONE',  ( 1.301376502765494658, -0.3325571857498362260, -2.196291469625763160 ) ) ;
#85099=CARTESIAN_POINT ( 'NONE',  ( 3.628042789974804450, -1.253006538321174146, -1.692492853607285630 ) ) ;
#85102=CARTESIAN_POINT ( 'NONE',  ( 0.1857038103042158439, -1.139949723551544114, -1.471474936012186596 ) ) ;
#85107=CARTESIAN_POINT ( 'NONE',  ( 1.740644586495963431, 1.216819214799185866, -1.736574482785017359 ) ) ;
#85110=CARTESIAN_POINT ( 'NONE',  ( 4.105873170248697690, 0.6631157982108953908, -1.846516426336957784 ) ) ;
#85111=CARTESIAN_POINT ( 'NONE',  ( 3.151412294154242844, -1.766339975446712174, -1.245920677233211871 ) ) ;
#85112=CARTESIAN_POINT ( 'NONE',  ( 1.909461114401575843, -0.8690924446688346183, -1.623246667998109682 ) ) ;
#85115=CARTESIAN_POINT ( 'NONE',  ( 4.769343782054527026, 1.005586498893149772, 1.420189556619367410 ) ) ;
#85119=CARTESIAN_POINT ( 'NONE',  ( 1.885829143180400624, 1.490600019384461072, 1.565824011241300440 ) ) ;
#85121=CARTESIAN_POINT ( 'NONE',  ( 3.532577226125938274, 1.967586357134976094, -0.4389627639644277934 ) ) ;
#85123=CARTESIAN_POINT ( 'NONE',  ( 0.7960496800812133511, -0.7770375076890515542, 2.017388685454111652 ) ) ;
#85124=CARTESIAN_POINT ( 'NONE',  ( 3.133621081638960693, -1.322844378366348606, -1.461937730511401190 ) ) ;
#85127=CARTESIAN_POINT ( 'NONE',  ( 3.772937862106290563, 1.827633595424851043, -0.6570963203050876889 ) ) ;
#85132=CARTESIAN_POINT ( 'NONE',  ( -0.1106856583840696712, 2.878213433396461962, -2.485464591233726317 ) ) ;
#85137=CARTESIAN_POINT ( 'NONE',  ( 6.827182134110238110, -0.009824402486291110986, 2.288967694407697984 ) ) ;
#85139=CARTESIAN_POINT ( 'NONE',  ( 4.381663332995835880, -1.878531202089319674, 0.5654445158327011667 ) ) ;
#85140=CARTESIAN_POINT ( 'NONE',  ( 1.354138928560550070, 0.1455316553338575625, -2.011204400906742240 ) ) ;
#85142=CARTESIAN_POINT ( 'NONE',  ( 3.573546900796530146, 1.536558363836796337, 1.457006447099787882 ) ) ;
#85144=CARTESIAN_POINT ( 'NONE',  ( 0.07459516483343266169, 4.098104556601829707, -2.310507343083552989 ) ) ;
#85146=CARTESIAN_POINT ( 'NONE',  ( 3.187279605439637287, -0.7454021820463945236, 1.683677988101241141 ) ) ;
#85153=CARTESIAN_POINT ( 'NONE',  ( 4.728832233812888752, 1.460412846248357210, -1.537820402542383169 ) ) ;
#85155=CARTESIAN_POINT ( 'NONE',  ( 6.925078400183544147, 0.003529629153843987736, 1.755452343125717851 ) ) ;
#85157=CARTESIAN_POINT ( 'NONE',  ( 5.606733736089553055, 1.563247385715782700, -1.342922781998987736 ) ) ;
#85158=CARTESIAN_POINT ( 'NONE',  ( 0.3790724793553065797, -0.09720884262147008736, 1.858658634516747510 ) ) ;
#85159=CARTESIAN_POINT ( 'NONE',  ( 2.806014743833367131, 1.331929863061011465, -1.271513748034671654 ) ) ;
#85164=CARTESIAN_POINT ( 'NONE',  ( 2.403190426070573871, 1.771669130372434564, -1.315670724662293178 ) ) ;
#85165=CARTESIAN_POINT ( 'NONE',  ( 5.255258077898470326, -1.907309223944063437, -1.216589440439620695 ) ) ;
#85167=CARTESIAN_POINT ( 'NONE',  ( 5.185751641416406876, 1.743707907788614619, -0.4909320375018846883 ) ) ;
#85168=CARTESIAN_POINT ( 'NONE',  ( 4.487445792895001340, -0.5051273088985311910, 1.847880739403139572 ) ) ;
#85170=CARTESIAN_POINT ( 'NONE',  ( 4.188322375386017704, -1.949839058108787437, -0.2904977467932718382 ) ) ;
#85171=CARTESIAN_POINT ( 'NONE',  ( 5.225416543158964977, -1.776039340814106637, 0.5876355328483380269 ) ) ;
#85172=CARTESIAN_POINT ( 'NONE',  ( 4.281604344665800532, -1.781275985052663158, 0.5390932415961935398 ) ) ;
#85174=CARTESIAN_POINT ( 'NONE',  ( 0.1281391398850126040, 2.011452084832816123, 0.1435147193784985509 ) ) ;
#85176=CARTESIAN_POINT ( 'NONE',  ( 1.225372267635124635, -0.04993704651819717150, 2.105648344105083947 ) ) ;
#85180=CARTESIAN_POINT ( 'NONE',  ( 2.918346969001627045, -2.117983955170518851, 0.1081942149789016649 ) ) ;
#85182=CARTESIAN_POINT ( 'NONE',  ( 1.388932113579334660, -1.919223592974130588, -0.6296790815572687050 ) ) ;
#85186=ORIENTED_EDGE ( 'NONE', *, *, #116226, .F. ) ;
#85187=CARTESIAN_POINT ( 'NONE',  ( 1.933122032479916985, 0.2097677157741582865, 2.151362962771664833 ) ) ;
#85188=CARTESIAN_POINT ( 'NONE',  ( 6.609999999999985221, 3.681232580627872952, 2.794007784547379192 ) ) ;
#85193=CARTESIAN_POINT ( 'NONE',  ( -0.1296875068448137269, 7.629137130509075604, -2.426516348560475045 ) ) ;
#85195=CARTESIAN_POINT ( 'NONE',  ( 1.242012060539962492, 2.189267750446591609, 0.1026977899005257211 ) ) ;
#85197=CARTESIAN_POINT ( 'NONE',  ( 1.341102801589135529, 0.4431706325995210527, 2.218532444564396577 ) ) ;
#85205=CARTESIAN_POINT ( 'NONE',  ( 3.773808747373870620, 0.9599976342714054978, 1.432812656881277791 ) ) ;
#85207=CARTESIAN_POINT ( 'NONE',  ( 2.301682877085888368, -1.769492147959438322, 0.03813942612425345879 ) ) ;
#85208=CARTESIAN_POINT ( 'NONE',  ( 5.174942826180319422, -2.076333920960464763, -0.7478091396579674699 ) ) ;
#85211=CARTESIAN_POINT ( 'NONE',  ( 5.220327442464319567, 1.987051044970666647, 0.3419161450798278157 ) ) ;
#85212=CARTESIAN_POINT ( 'NONE',  ( 4.675916410682629198, 1.790815896176844335, -0.2727875059450618478 ) ) ;
#85214=CARTESIAN_POINT ( 'NONE',  ( 2.694054421766532759, -1.865511834602461505, -0.1395888279770511053 ) ) ;
#85216=CARTESIAN_POINT ( 'NONE',  ( 6.604126001430527637, -1.825160783932573860, 0.05055279568313279792 ) ) ;
#85217=CARTESIAN_POINT ( 'NONE',  ( 2.267699027020404490, 0.5063876334258295975, -1.844086191983687062 ) ) ;
#85221=CARTESIAN_POINT ( 'NONE',  ( 0.05278957052760185897, 0.3289079202175131389, 1.883742972368242174 ) ) ;
#85223=CARTESIAN_POINT ( 'NONE',  ( 1.521847698614446687, 1.933392594956625521, -0.3320675068423510345 ) ) ;
#85226=CARTESIAN_POINT ( 'NONE',  ( 5.625269520628737752, 1.871107552910089122, 0.9978724776121964402 ) ) ;
#85229=CARTESIAN_POINT ( 'NONE',  ( 5.149669460738499183, 0.6209446730581876794, -1.871051946789156650 ) ) ;
#85231=CARTESIAN_POINT ( 'NONE',  ( 0.7736903856863480700, 0.3886292558455446411, -1.975178614941161870 ) ) ;
#85232=EDGE_LOOP ( 'NONE', ( #211927, #174416, #156561, #105896 ) ) ;
#85234=CARTESIAN_POINT ( 'NONE',  ( 0.5447201963149818082, -1.530340168762192254, 1.463345158046714056 ) ) ;
#85236=CARTESIAN_POINT ( 'NONE',  ( 3.033707436314789785, 1.966763487489433970, -0.6469820378900912328 ) ) ;
#85240=CARTESIAN_POINT ( 'NONE',  ( 4.699217343460686536, -0.5580910489941055541, 2.014698706189700594 ) ) ;
#85242=CARTESIAN_POINT ( 'NONE',  ( 3.504746488097260748, 1.439749907568649068, -1.122338611188322455 ) ) ;
#85243=CARTESIAN_POINT ( 'NONE',  ( 2.543383136322028282, -1.689629589678593558, 0.6535807426650240837 ) ) ;
#85247=CARTESIAN_POINT ( 'NONE',  ( 4.999154358079874960, 1.837129776665728187, -1.222328095618854693 ) ) ;
#85251=CARTESIAN_POINT ( 'NONE',  ( 3.809155001108742056, 1.613891119516493999, -1.025466636117925212 ) ) ;
#85254=CARTESIAN_POINT ( 'NONE',  ( 6.883263157960362477, -0.004191378316371896506, 2.053658919477070910 ) ) ;
#85262=EDGE_CURVE ( 'NONE', #53136, #150774, #178153, .T. ) ;
#85263=CARTESIAN_POINT ( 'NONE',  ( 3.391731324245280010, -0.7611128710301139355, 1.708892184765831157 ) ) ;
#85269=CARTESIAN_POINT ( 'NONE',  ( 0.05278957052760185897, 0.3289079202175131389, 1.883742972368242174 ) ) ;
#85271=CARTESIAN_POINT ( 'NONE',  ( 0.6550501802922055195, 1.640498656168420943, -1.089389633329050033 ) ) ;
#85272=CARTESIAN_POINT ( 'NONE',  ( 1.353138909097661768, 0.1455122274086443901, -2.011206940682720212 ) ) ;
#85276=CARTESIAN_POINT ( 'NONE',  ( 1.394752248596371702, 1.789971953256053627, -1.264032476404143512 ) ) ;
#85277=CARTESIAN_POINT ( 'NONE',  ( 6.692070433991195166, -0.7751425012093198230, 1.651373049820707317 ) ) ;
#85285=CARTESIAN_POINT ( 'NONE',  ( 3.491602800004707241, -1.839307750763185645, -0.08696504193297231733 ) ) ;
#85286=CARTESIAN_POINT ( 'NONE',  ( 0.8736902326584498057, 0.3905749221770152269, -1.974679160882378826 ) ) ;
#85287=CARTESIAN_POINT ( 'NONE',  ( 2.196985159075715011, -1.500492831465898513, -1.741107174271120384 ) ) ;
#85289=CARTESIAN_POINT ( 'NONE',  ( 0.7778919621034340315, -0.9889961724188134351, -1.576189065804904477 ) ) ;
#85293=CARTESIAN_POINT ( 'NONE',  ( 4.341997288149157086, -1.180789491531178292, -1.504210074635865757 ) ) ;
#85297=CARTESIAN_POINT ( 'NONE',  ( 4.230081496780574213, 2.050754116127400106, 0.4060544076584340356 ) ) ;
#85298=CARTESIAN_POINT ( 'NONE',  ( 2.342468781959532453, 0.4075140148256419792, 1.825566309089213579 ) ) ;
#85301=CARTESIAN_POINT ( 'NONE',  ( 3.298151293307958642, 1.369808456162135091, -1.073517941977668588 ) ) ;
#85305=CARTESIAN_POINT ( 'NONE',  ( 3.984733165684080092, -0.1715787546078418324, -1.716317334075837975 ) ) ;
#85307=CARTESIAN_POINT ( 'NONE',  ( 3.790727848299980440, 1.850687065220711469, -1.173560875862532660 ) ) ;
#85308=CARTESIAN_POINT ( 'NONE',  ( 6.721333373144884327, -0.1645177889858795151, 2.170883633896856679 ) ) ;
#85312=CARTESIAN_POINT ( 'NONE',  ( 3.467796559821629820, -0.4283512159202977343, 2.128237193570106101 ) ) ;
#85313=CARTESIAN_POINT ( 'NONE',  ( 2.262075381241589245, 0.7800679334904643270, 1.650788133108482825 ) ) ;
#85315=CARTESIAN_POINT ( 'NONE',  ( 6.157425464982741126, 2.025529447029483343, -0.6166105444416707382 ) ) ;
#85318=CARTESIAN_POINT ( 'NONE',  ( 5.847306917912500346, 0.6688746937079934618, -2.192647164702413498 ) ) ;
#85321=CARTESIAN_POINT ( 'NONE',  ( 1.295735140135088281, 1.957893036122235531, -0.8148005001323217478 ) ) ;
#85327=CARTESIAN_POINT ( 'NONE',  ( 1.190412498926897600, 1.327076764020938882, 1.781161496267854361 ) ) ;
#85329=CARTESIAN_POINT ( 'NONE',  ( 5.906875006520014182, -1.122496024291631755, -1.674889250513518446 ) ) ;
#85331=CARTESIAN_POINT ( 'NONE',  ( 3.889554661416291026, -1.907601829641421887, 0.7848441205193229520 ) ) ;
#85333=CARTESIAN_POINT ( 'NONE',  ( -0.2409995289980038091, 6.947781193150415646, -2.595509233728268583 ) ) ;
#85337=CARTESIAN_POINT ( 'NONE',  ( 0.1329588055935760349, 7.629137130509077380, -2.445925914280167923 ) ) ;
#85338=CARTESIAN_POINT ( 'NONE',  ( 0.4629771330677232011, 0.2027323353172970355, -2.080777175944429125 ) ) ;
#85339=CARTESIAN_POINT ( 'NONE',  ( 5.238907797441370029, 2.013986022392059816, -0.1017483359899013229 ) ) ;
#85340=CARTESIAN_POINT ( 'NONE',  ( 4.845164456061270997, 0.5726227986864868003, -1.750029900461601340 ) ) ;
#85343=CARTESIAN_POINT ( 'NONE',  ( 1.201696739578085982, -1.724958192343982510, -0.005827584801694830549 ) ) ;
#85344=CARTESIAN_POINT ( 'NONE',  ( 0.02267320670834571672, 0.3494893071277604402, 1.985867805234131644 ) ) ;
#85345=CARTESIAN_POINT ( 'NONE',  ( 1.143681411288837824, 0.9377895679426456743, 2.098875006570381618 ) ) ;
#85347=CARTESIAN_POINT ( 'NONE',  ( 1.089599759544016999, 1.994953948513054742, -1.067007742874733545 ) ) ;
#85348=CARTESIAN_POINT ( 'NONE',  ( 3.369845833479632180, 2.054674681345913800, -0.4616683548303905926 ) ) ;
#85352=CARTESIAN_POINT ( 'NONE',  ( 0.000000000000000000, 0.000000000000000000, -1.999999999999999556 ) ) ;
#85357=CARTESIAN_POINT ( 'NONE',  ( 5.431947826915617838, -2.167270271666811077, 0.4867340719418070671 ) ) ;
#85358=CARTESIAN_POINT ( 'NONE',  ( 3.011879173929287390, -1.080601074572758558, -1.906429682232862577 ) ) ;
#85361=CARTESIAN_POINT ( 'NONE',  ( 5.600043156098196917, 0.7966083592686534764, -1.793046234938546757 ) ) ;
#85363=CARTESIAN_POINT ( 'NONE',  ( 6.610000000000014531, 2.942932264094192174, 2.732153830519419291 ) ) ;
#85366=CARTESIAN_POINT ( 'NONE',  ( 4.640951271726033056, 2.030106984047326701, 0.6129599860185754867 ) ) ;
#85370=CARTESIAN_POINT ( 'NONE',  ( 6.614160618316515361, -1.014195557614630205, -1.909021090911746654 ) ) ;
#85372=CARTESIAN_POINT ( 'NONE',  ( 5.003375819710620398, -1.831856422778654681, 0.1858995714831001289 ) ) ;
#85375=CARTESIAN_POINT ( 'NONE',  ( 1.381927130872797838, -0.2546507840628647878, -1.721584071012570050 ) ) ;
#85379=CARTESIAN_POINT ( 'NONE',  ( 5.524359596833869013, 1.291058806671550485, -1.733668313432787933 ) ) ;
#85382=CARTESIAN_POINT ( 'NONE',  ( 4.504844740329728481, 1.672958716126593082, -1.369014088531981255 ) ) ;
#85384=CARTESIAN_POINT ( 'NONE',  ( 4.745367521161733215, -1.522072814771213922, -1.252777155790285590 ) ) ;
#85385=CARTESIAN_POINT ( 'NONE',  ( 3.567500862290486019, 1.367785175758473581, -1.065411925293987760 ) ) ;
#85386=CARTESIAN_POINT ( 'NONE',  ( 1.013517375116283592, -2.137022957946862700, 0.4851717564131745597 ) ) ;
#85387=CARTESIAN_POINT ( 'NONE',  ( 2.485774399949276070, 2.109797628256422364, -0.9350972159218959856 ) ) ;
#85388=CARTESIAN_POINT ( 'NONE',  ( 4.991509756128800213, 1.524171611017493655, 1.387147876433484806 ) ) ;
#85389=CARTESIAN_POINT ( 'NONE',  ( 6.374560617330069512, -0.09999853314933374038, -1.939619642457596660 ) ) ;
#85393=CARTESIAN_POINT ( 'NONE',  ( 1.002577532868035526, -1.966644254196001196, 0.4445047019146358691 ) ) ;
#85395=CARTESIAN_POINT ( 'NONE',  ( 3.803933094734159415, -0.6430795383850876901, 2.110982628114480786 ) ) ;
#85397=CARTESIAN_POINT ( 'NONE',  ( 1.270090995528074362, -0.8302864195119415980, -1.665510012463662148 ) ) ;
#85402=CARTESIAN_POINT ( 'NONE',  ( 6.825078400183575589, -0.005632053428735600553, 2.144262460745151255 ) ) ;
#85404=CARTESIAN_POINT ( 'NONE',  ( 6.193280126971262511, -0.6156851667328180344, 1.735278506779000640 ) ) ;
#85406=CARTESIAN_POINT ( 'NONE',  ( 2.887629844759795450, 1.456389637235107948, 1.458414562493230759 ) ) ;
#85409=CARTESIAN_POINT ( 'NONE',  ( 2.227218753574769838, 1.805135905798272100, 0.9059672028350268524 ) ) ;
#85413=CARTESIAN_POINT ( 'NONE',  ( 2.289980725320222010, -0.8822103741390595610, 1.862666789336121509 ) ) ;
#85417=CARTESIAN_POINT ( 'NONE',  ( -0.2409995289980246258, 7.629137130509076492, -2.600476469121239198 ) ) ;
#85418=CARTESIAN_POINT ( 'NONE',  ( 5.250674450588199704, 0.6379336648693231249, 2.112661011922472021 ) ) ;
#85420=CARTESIAN_POINT ( 'NONE',  ( 1.124558466181435179, 1.288545020775376804, -1.735378439385642180 ) ) ;
#85422=CARTESIAN_POINT ( 'NONE',  ( 2.413296319342159713, -1.879803466158457059, 0.7303082167480907660 ) ) ;
#85423=CARTESIAN_POINT ( 'NONE',  ( 2.249760294480507294, -2.253934603285558502, -0.4491563171437322199 ) ) ;
#85425=CARTESIAN_POINT ( 'NONE',  ( 0.4263524580605422276, 1.788790299270696993, 0.5473224044415525569 ) ) ;
#85427=CARTESIAN_POINT ( 'NONE',  ( 1.938157646728836614, 1.849873822469105145, 0.2772664081076986475 ) ) ;
#85429=CARTESIAN_POINT ( 'NONE',  ( 3.116422982138194353, 1.968445132739887748, 0.4370783100892047801 ) ) ;
#85433=CARTESIAN_POINT ( 'NONE',  ( 5.303390785913836503, 1.721067984382893545, 1.213575365270858075 ) ) ;
#85437=CARTESIAN_POINT ( 'NONE',  ( 5.748308766347858700, 0.9917722086787251756, -1.759414076857076514 ) ) ;
#85439=CARTESIAN_POINT ( 'NONE',  ( 0.3563950589157930393, -2.062029646941070382, -0.05432448973826872057 ) ) ;
#85447=CARTESIAN_POINT ( 'NONE',  ( 3.174467775116470936, -1.067885509202262773, -1.890316989176257234 ) ) ;
#85450=CARTESIAN_POINT ( 'NONE',  ( 1.698526806778306586, 1.531337151408303621, 1.022036240780115346 ) ) ;
#85452=CARTESIAN_POINT ( 'NONE',  ( 4.177398808104064720, 1.432170664236757540, 1.658919600136643524 ) ) ;
#85453=CARTESIAN_POINT ( 'NONE',  ( 6.883263157960367806, 2.959656548886806071, 2.506466465954690914 ) ) ;
#85454=CARTESIAN_POINT ( 'NONE',  ( 5.225545412997908201, -2.150153479602398221, 0.7043797957921889008 ) ) ;
#85461=CARTESIAN_POINT ( 'NONE',  ( 5.993352163831329626, 1.341162022463908032, 1.154712335393495160 ) ) ;
#85463=CARTESIAN_POINT ( 'NONE',  ( 2.046058472223175162, 0.8067420340923843192, -1.945513702063914163 ) ) ;
#85466=CARTESIAN_POINT ( 'NONE',  ( 1.521857752106166695, 1.940948540861246352, -0.3334180107718246466 ) ) ;
#85467=CARTESIAN_POINT ( 'NONE',  ( 0.09234973940512071489, -0.4041859633337717694, -1.833079292876439670 ) ) ;
#85468=CARTESIAN_POINT ( 'NONE',  ( 0.8011316787140990714, -1.684513426579350659, 1.005393624328714264 ) ) ;
#85469=CARTESIAN_POINT ( 'NONE',  ( 0.2285749388857594433, 1.317234250586714284, -1.386657971642536014 ) ) ;
#85475=CARTESIAN_POINT ( 'NONE',  ( 6.368025811218641863, 0.9635043244729593059, 1.603280169136585220 ) ) ;
#85479=CARTESIAN_POINT ( 'NONE',  ( 5.911005882915713272, -1.635593682349820499, 1.269112435710928688 ) ) ;
#85489=CARTESIAN_POINT ( 'NONE',  ( 5.529730448059603454, 1.891198321494348633, -0.5216162335564683561 ) ) ;
#85491=CARTESIAN_POINT ( 'NONE',  ( 3.602888598310006074, 0.9090057795711030675, -1.799647124144133858 ) ) ;
#85492=CARTESIAN_POINT ( 'NONE',  ( 2.237376970375870577, 0.5068087052534899772, -1.847417656071285608 ) ) ;
#85494=CARTESIAN_POINT ( 'NONE',  ( 0.4510473619779230003, -1.854578567552306767, -1.167393260480112493 ) ) ;
#85496=CARTESIAN_POINT ( 'NONE',  ( 2.758895227446885645, -1.625506345271657604, -0.9254698705311248386 ) ) ;
#85500=CARTESIAN_POINT ( 'NONE',  ( 4.183301248788100501, 1.701634275673917784, 1.259637755991403374 ) ) ;
#85502=CARTESIAN_POINT ( 'NONE',  ( 6.478973898625433492, 1.930320082341809629, 0.7489585856828018251 ) ) ;
#85503=CARTESIAN_POINT ( 'NONE',  ( 0.8024204784428441428, 1.580594792060415088, -1.368634514759473397 ) ) ;
#85504=CARTESIAN_POINT ( 'NONE',  ( 6.720655732516649827, 4.686306134629722564, 2.836255308917837947 ) ) ;
#85505=CARTESIAN_POINT ( 'NONE',  ( 6.792070425361753649, -0.7769146798779454910, 1.650438213995283565 ) ) ;
#85510=SURFACE_STYLE_USAGE ( .BOTH. , #115943 ) ;
#85514=CARTESIAN_POINT ( 'NONE',  ( 0.04710954650594124937, -1.657193159602200927, 0.7319819781744562048 ) ) ;
#85522=CARTESIAN_POINT ( 'NONE',  ( 5.712517600013328867, 1.944077172375497486, 0.5350714256760413789 ) ) ;
#85523=CARTESIAN_POINT ( 'NONE',  ( 0.5574859923395922845, -1.816599148028580579, 1.093606109393664427 ) ) ;
#85524=CARTESIAN_POINT ( 'NONE',  ( -0.1394461523060883668, 1.988389203256015536, -2.694605331112149393 ) ) ;
#85528=CARTESIAN_POINT ( 'NONE',  ( 3.344544815957225747, -1.939504806627976752, -0.3411970713738179395 ) ) ;
#85529=CARTESIAN_POINT ( 'NONE',  ( 0.9266185682500321930, -0.9568284065921551784, -1.892426592148554132 ) ) ;
#85533=CARTESIAN_POINT ( 'NONE',  ( 5.648420989521034663, -1.729380818958951460, 1.345873388983606533 ) ) ;
#85535=CARTESIAN_POINT ( 'NONE',  ( 4.647439542507147081, -1.488915335790324201, -1.222320866314072774 ) ) ;
#85537=CARTESIAN_POINT ( 'NONE',  ( -0.1296875068448125057, 2.889142263448498227, -2.315371602238533555 ) ) ;
#85538=CARTESIAN_POINT ( 'NONE',  ( 1.137671262558290763, -1.993743905544292927, 0.9465009238469669350 ) ) ;
#85543=CARTESIAN_POINT ( 'NONE',  ( 5.858249334120006147, -1.969629310164786373, -0.003746551262697600092 ) ) ;
#85544=CARTESIAN_POINT ( 'NONE',  ( 0.3978616433950994957, -0.6552777965449173569, -1.828281909955962181 ) ) ;
#85546=CARTESIAN_POINT ( 'NONE',  ( 6.872461156203343080, -0.5239007177601956444, 2.246970456009795836 ) ) ;
#85548=CARTESIAN_POINT ( 'NONE',  ( 4.082723863713003887, 1.765846151219726101, 0.5873946967244033646 ) ) ;
#85553=CARTESIAN_POINT ( 'NONE',  ( 0.6443834720083198020, 0.6415979653194536780, 2.095529601600601755 ) ) ;
#85558=CARTESIAN_POINT ( 'NONE',  ( 0.9612317138737861422, 0.3586375672061762887, -1.789940867121169843 ) ) ;
#85561=CARTESIAN_POINT ( 'NONE',  ( 2.513978358999646723, -1.617321061556979300, 0.6262005117416250544 ) ) ;
#85563=CARTESIAN_POINT ( 'NONE',  ( 6.509000000000010111, 6.037005099786168394, 2.594901386363585694 ) ) ;
#85565=CARTESIAN_POINT ( 'NONE',  ( 5.584540971669589737, -1.782103179330214449, -0.3958202769075992444 ) ) ;
#85566=CARTESIAN_POINT ( 'NONE',  ( 3.133595828963112950, 1.864314371477162169, -0.6108997337519045390 ) ) ;
#85570=CARTESIAN_POINT ( 'NONE',  ( 4.565154201998150363, -1.702539431995837349, 1.263830167178958463 ) ) ;
#85574=CARTESIAN_POINT ( 'NONE',  ( 2.799741537105740363, -1.531010120401912200, -1.393694001666223814 ) ) ;
#85575=CARTESIAN_POINT ( 'NONE',  ( 6.827182134110198142, 0.003888933837258023996, 1.810856214465889069 ) ) ;
#85577=CARTESIAN_POINT ( 'NONE',  ( 4.635507155980078231, -0.1095829440264598081, 2.218699120425669413 ) ) ;
#85579=CARTESIAN_POINT ( 'NONE',  ( 2.374040334453372925, -0.3969776081079456898, -2.264039395722910353 ) ) ;
#85585=CARTESIAN_POINT ( 'NONE',  ( 6.720655732516647163, 0.005566325962592238996, 1.826293863978686982 ) ) ;
#85588=CARTESIAN_POINT ( 'NONE',  ( 4.218947473185084007, 1.474887410857337100, -1.217315437338606365 ) ) ;
#85590=CARTESIAN_POINT ( 'NONE',  ( 3.557352906045672114, 0.4196458916515317661, -1.672789571874600645 ) ) ;
#85591=CARTESIAN_POINT ( 'NONE',  ( 3.151577601795185757, 1.966304690962265234, -0.4465026806126579095 ) ) ;
#85592=CARTESIAN_POINT ( 'NONE',  ( 3.534061846033216714, -1.878541635090751560, 1.324563465849286859 ) ) ;
#85594=CARTESIAN_POINT ( 'NONE',  ( 6.428360055892773595, 1.214212339677790409, -1.720619796903441578 ) ) ;
#85597=CARTESIAN_POINT ( 'NONE',  ( 4.463939829769240752, 0.8331255105114807602, 1.561325262609781772 ) ) ;
#85599=CARTESIAN_POINT ( 'NONE',  ( 0.4106429779945898195, 1.576260533944493503, -1.664518642746879662 ) ) ;
#85600=CARTESIAN_POINT ( 'NONE',  ( 6.562460610575872266, -1.685528226061007162, -0.7412392050258274079 ) ) ;
#85607=CARTESIAN_POINT ( 'NONE',  ( 0.2566020104313873618, -2.170709068928804886, -0.05254486697847670501 ) ) ;
#85608=CARTESIAN_POINT ( 'NONE',  ( 1.147673126774436225, 1.985868168208399842, -0.3494872464938902357 ) ) ;
#85611=CARTESIAN_POINT ( 'NONE',  ( 5.953728026056397837, 0.5566793334266966209, -1.844321365346488273 ) ) ;
#85613=CARTESIAN_POINT ( 'NONE',  ( 1.160717840558170622, 2.219164385786871030, 0.1022553982447590853 ) ) ;
#85622=CARTESIAN_POINT ( 'NONE',  ( 4.827569786946327213, 0.8888792617508225469, -1.496182039812316678 ) ) ;
#85624=CARTESIAN_POINT ( 'NONE',  ( 2.014041202081144011, 1.956828179156915315, -0.1411808619533050091 ) ) ;
#85629=CARTESIAN_POINT ( 'NONE',  ( 6.391066755906244623, 0.1909826923555627554, 1.952524381009380861 ) ) ;
#85632=CARTESIAN_POINT ( 'NONE',  ( 5.313685493615880162, -1.282986534165726944, -1.555701818360885280 ) ) ;
#85633=CARTESIAN_POINT ( 'NONE',  ( 1.235668275047563380, -2.044475609799735416, 0.9693208282701860634 ) ) ;
#85636=CARTESIAN_POINT ( 'NONE',  ( 2.038157526861613889, 1.849479306444936411, 0.2792354855166642724 ) ) ;
#85637=CARTESIAN_POINT ( 'NONE',  ( 1.142726939315736656, 0.7017603364856840331, 1.586018014115580188 ) ) ;
#85638=CARTESIAN_POINT ( 'NONE',  ( 4.792620198997869174, 1.822056328612733145, -1.217503271791681163 ) ) ;
#85639=CARTESIAN_POINT ( 'NONE',  ( 5.913149109437923379, 2.031366086520134395, 1.094794683655570644 ) ) ;
#85640=CARTESIAN_POINT ( 'NONE',  ( 1.094684877246233201, -0.5000429121475665761, -1.999180680717755898 ) ) ;
#85641=CARTESIAN_POINT ( 'NONE',  ( 3.451055654028605701, 0.4708835965685866376, -1.883881102318455847 ) ) ;
#85644=CARTESIAN_POINT ( 'NONE',  ( 5.501189692264965458, 1.528658022856645315, 1.077728667985423661 ) ) ;
#85646=CARTESIAN_POINT ( 'NONE',  ( 0.4031117941524774984, 0.2875473383168804520, 1.709643368666772467 ) ) ;
#85648=CARTESIAN_POINT ( 'NONE',  ( 4.799454022740247794, 1.388487131293577592, -1.462444391756134943 ) ) ;
#85651=CARTESIAN_POINT ( 'NONE',  ( 2.666400811807769777, -1.259032629953384719, 1.322343945743660543 ) ) ;
#85661=CARTESIAN_POINT ( 'NONE',  ( 5.830724911194343996, 1.354916080449189764, -1.497948107757952174 ) ) ;
#85662=CARTESIAN_POINT ( 'NONE',  ( 6.445936322256165418, -1.448296609194921647, -1.684281199878513657 ) ) ;
#85666=CARTESIAN_POINT ( 'NONE',  ( 5.102442524761234388, -0.6923759778164092493, -1.941246359495584883 ) ) ;
#85667=CARTESIAN_POINT ( 'NONE',  ( 4.940077362011475515, -1.704937458037486531, -1.076318853994034930 ) ) ;
#85675=CARTESIAN_POINT ( 'NONE',  ( 5.079453798366286854, 1.392331892589277142, -1.458333960840517696 ) ) ;
#85676=CARTESIAN_POINT ( 'NONE',  ( 4.118977087773854961, -1.761250088754966692, 0.5364436722887636622 ) ) ;
#85678=CARTESIAN_POINT ( 'NONE',  ( 1.928779914882609914, 1.326332282235458848, -1.888294200376864573 ) ) ;
#85680=CARTESIAN_POINT ( 'NONE',  ( 4.516967039858135635, 1.974289957696921949, 0.8805908171375662619 ) ) ;
#85682=CARTESIAN_POINT ( 'NONE',  ( 0.3451281418221859854, 0.6079892978090885025, -1.844522312511005957 ) ) ;
#85683=CARTESIAN_POINT ( 'NONE',  ( 2.747280062631300535, 0.2910806042949847239, -1.995268371848608835 ) ) ;
#85686=CARTESIAN_POINT ( 'NONE',  ( 3.151090109352538082, -1.528452604574185525, -1.078222621661927061 ) ) ;
#85687=CARTESIAN_POINT ( 'NONE',  ( 0.4914017305483203701, 1.457842971892213235, 1.327161884117057600 ) ) ;
#85690=CARTESIAN_POINT ( 'NONE',  ( 2.227434312139275896, 0.001603268854937638837, 2.207063162490217056 ) ) ;
#85695=CARTESIAN_POINT ( 'NONE',  ( 6.737195113697223903, -1.761045485681483669, 0.8863934713586976155 ) ) ;
#85696=CARTESIAN_POINT ( 'NONE',  ( 6.252564486485036710, 0.7173172151448119482, 2.193443857502775263 ) ) ;
#85697=CARTESIAN_POINT ( 'NONE',  ( 0.8890225878602634468, 0.1407106197201784259, 1.956863499422318631 ) ) ;
#85698=CARTESIAN_POINT ( 'NONE',  ( 3.907127581704954888, -1.689070986467123836, 1.183507789072274496 ) ) ;
#85706=CARTESIAN_POINT ( 'NONE',  ( 6.461400869420954152, 1.801464151850284301, 1.211653227174382952 ) ) ;
#85709=CARTESIAN_POINT ( 'NONE',  ( 6.515202330376022921, -1.784155196879381622, 0.4545711315065634195 ) ) ;
#85712=CARTESIAN_POINT ( 'NONE',  ( 0.8252170375972631700, -1.778153878779257901, 0.5809004490327505099 ) ) ;
#85718=CARTESIAN_POINT ( 'NONE',  ( 1.154776974461441341, 0.3738248154092556064, 1.875208037630435864 ) ) ;
#85719=CARTESIAN_POINT ( 'NONE',  ( 3.432247180620687566, 1.726460203109028591, 0.3886401920838201685 ) ) ;
#85721=CARTESIAN_POINT ( 'NONE',  ( 1.189939518123926510, 1.139724415472416652, 1.535358521287055300 ) ) ;
#85723=CARTESIAN_POINT ( 'NONE',  ( 4.077677060472849391, -0.7296757366501721576, 1.771397967703478793 ) ) ;
#85726=CARTESIAN_POINT ( 'NONE',  ( 5.863713558449636487, -0.4802757262234845226, 1.909948281557447114 ) ) ;
#85727=CARTESIAN_POINT ( 'NONE',  ( 0.8617730121942971389, -1.675286201960282995, -1.300076073212981242 ) ) ;
#85730=CARTESIAN_POINT ( 'NONE',  ( 4.100366707588389836, -0.5864361863821172527, -1.776433678864146382 ) ) ;
#85731=CARTESIAN_POINT ( 'NONE',  ( 5.848237035817564156, 1.723274176396558888, 0.07769637638467204177 ) ) ;
#85733=CARTESIAN_POINT ( 'NONE',  ( 3.844505992619148937, 2.196175933995975438, 0.2170506636963928093 ) ) ;
#85736=CARTESIAN_POINT ( 'NONE',  ( 1.275913394178169957, -2.012872700982801355, 0.4499014461352250360 ) ) ;
#85738=EDGE_CURVE ( 'NONE', #36822, #15524, #211136, .T. ) ;
#85747=CARTESIAN_POINT ( 'NONE',  ( 3.139188941651628539, -0.1496422021231707811, -2.064996656166856237 ) ) ;
#85751=CARTESIAN_POINT ( 'NONE',  ( 1.418624149192078576, -0.7290977765982089576, -1.883658722702468591 ) ) ;
#85754=CARTESIAN_POINT ( 'NONE',  ( 0.07479286986305544449, 2.888457405263197941, -2.344396930208477947 ) ) ;
#85756=CARTESIAN_POINT ( 'NONE',  ( 6.309922681198771421, -1.704675833164914778, 1.076154833852351000 ) ) ;
#85757=CARTESIAN_POINT ( 'NONE',  ( 6.245329893291753365, 0.3200292219377436354, -1.888624904781693870 ) ) ;
#85758=CARTESIAN_POINT ( 'NONE',  ( 6.639320575229230137, 7.629137130509035636, 2.603262396134010892 ) ) ;
#85759=CARTESIAN_POINT ( 'NONE',  ( 4.282901435897610298, 1.957309562236182021, -0.9860176978964061423 ) ) ;
#85761=CARTESIAN_POINT ( 'NONE',  ( 3.937688585161042809, -1.828529804631402023, 0.5600222464785462595 ) ) ;
#85765=CARTESIAN_POINT ( 'NONE',  ( 0.5621253344089729431, -1.117812357707391069, 1.678020072846800659 ) ) ;
#85767=CARTESIAN_POINT ( 'NONE',  ( 6.567925981381852907, -1.350348970527824211, 1.726830949945204363 ) ) ;
#85769=CARTESIAN_POINT ( 'NONE',  ( 4.383650571098846704, 1.127723038421009738, 1.305118705121767420 ) ) ;
#85775=CARTESIAN_POINT ( 'NONE',  ( 0.7835587076311965049, -1.864072139945194717, 0.6119401183290391621 ) ) ;
#85778=CARTESIAN_POINT ( 'NONE',  ( 0.07536363704237906969, 4.084105538841027894, -2.698926661290324880 ) ) ;
#85783=CARTESIAN_POINT ( 'NONE',  ( 4.301270310059371660, 1.616194109774160559, -0.8183029847002845081 ) ) ;
#85787=CARTESIAN_POINT ( 'NONE',  ( 5.180233172056982305, 0.8977705535664436409, 1.573279850597033347 ) ) ;
#85792=CARTESIAN_POINT ( 'NONE',  ( 6.725070007137362360, -1.702231675683645973, -0.7527390810756880990 ) ) ;
#85794=CARTESIAN_POINT ( 'NONE',  ( 2.618635445852790511, 0.2369565241663183774, 1.900835938982778472 ) ) ;
#85801=CARTESIAN_POINT ( 'NONE',  ( 0.8136072859011161951, -0.3160970183575459447, 2.138355382504661506 ) ) ;
#85804=CARTESIAN_POINT ( 'NONE',  ( 1.342497868159111984, 0.3520595052693386018, 1.791136884925909056 ) ) ;
#85806=CARTESIAN_POINT ( 'NONE',  ( 2.414841169274529520, 1.629557050654990791, 0.8231356554938076275 ) ) ;
#85809=CARTESIAN_POINT ( 'NONE',  ( 2.039183100597967258, 0.003605121848727563250, 1.912571728241836633 ) ) ;
#85810=CARTESIAN_POINT ( 'NONE',  ( 3.191813391966125124, -1.320872291013975630, -1.461159636213595459 ) ) ;
#85811=CARTESIAN_POINT ( 'NONE',  ( 3.913568440338021315, -1.001196544591560933, -1.663976088286099886 ) ) ;
#85814=CARTESIAN_POINT ( 'NONE',  ( 4.728832233812888752, 1.460412846248357210, -1.537820402542383169 ) ) ;
#85822=CARTESIAN_POINT ( 'NONE',  ( 4.406759617291758246, 1.409692282476209924, -1.160130723419292353 ) ) ;
#85828=CARTESIAN_POINT ( 'NONE',  ( 5.049604242677837362, 0.5861553263475408615, -1.776501995420045832 ) ) ;
#85830=CARTESIAN_POINT ( 'NONE',  ( 3.404829243095872648, 1.518349439661485389, -1.185654278882039669 ) ) ;
#85831=CARTESIAN_POINT ( 'NONE',  ( 6.860214158839045950, -1.961385418603446062, 0.04497666117601883257 ) ) ;
#85839=CARTESIAN_POINT ( 'NONE',  ( 1.353279953590967644, 0.1518699462816820722, -2.111824974118434728 ) ) ;
#85842=CARTESIAN_POINT ( 'NONE',  ( 6.280147189154119403, -1.145143509460907039, -1.724508502191648862 ) ) ;
#85843=CARTESIAN_POINT ( 'NONE',  ( 0.4679805871025365382, -1.733519288248483559, -0.6209854868195128219 ) ) ;
#85845=CARTESIAN_POINT ( 'NONE',  ( 6.012345284929816458, -2.165844811509042511, 0.7704031996330994447 ) ) ;
#85848=CARTESIAN_POINT ( 'NONE',  ( 1.342159615362942704, 2.289816521768207380, 0.1084569774388414870 ) ) ;
#85852=CARTESIAN_POINT ( 'NONE',  ( 6.105412738798914773, -1.926975682693391700, 0.2402159021005992046 ) ) ;
#85856=CARTESIAN_POINT ( 'NONE',  ( 0.8439947366445134103, -1.280256340399921200, -1.553649900018534202 ) ) ;
#85857=CARTESIAN_POINT ( 'NONE',  ( 6.385953923436008317, -2.015982004707029596, 0.05432014494890363698 ) ) ;
#85861=CARTESIAN_POINT ( 'NONE',  ( 3.099644000116580589, -2.088226275799191622, 0.1030096337034935861 ) ) ;
#85862=CARTESIAN_POINT ( 'NONE',  ( 1.428175943150990390, 1.704372189200783705, 0.4766478552604267449 ) ) ;
#85865=CARTESIAN_POINT ( 'NONE',  ( 4.295090358266894448, 1.839821235612853600, 1.367129665020486273 ) ) ;
#85866=CARTESIAN_POINT ( 'NONE',  ( 3.204748380415303188, -0.3384778632026878564, 1.706898776778777993 ) ) ;
#85869=CARTESIAN_POINT ( 'NONE',  ( 3.584998556975723005, 1.101681934899124915, -1.338793912720330770 ) ) ;
#85870=CARTESIAN_POINT ( 'NONE',  ( 4.070888617658403597, 1.538033944094893579, -1.532718761138168517 ) ) ;
#85872=CARTESIAN_POINT ( 'NONE',  ( 4.100796195634116792, 1.845626398921360822, 0.8128187495666516771 ) ) ;
#85873=CARTESIAN_POINT ( 'NONE',  ( 3.406250000000002220, 1.895863743164009740, -0.7852924748301655100 ) ) ;
#85876=CARTESIAN_POINT ( 'NONE',  ( 1.676654808981252520, -1.828468026129226542, -0.6065514213326441695 ) ) ;
#85879=CARTESIAN_POINT ( 'NONE',  ( 5.906509255234578148, -2.210603606603298132, -0.2184946463264207661 ) ) ;
#85881=CARTESIAN_POINT ( 'NONE',  ( -0.1108833634137009749, 4.092508091048022933, -2.451885048449681914 ) ) ;
#85886=CARTESIAN_POINT ( 'NONE',  ( 0.3291711827644402399, 1.527175228150777331, -1.613279532339807476 ) ) ;
#85887=CARTESIAN_POINT ( 'NONE',  ( 6.180128940399614912, -1.088687182605744042, -1.631870318916525120 ) ) ;
#85890=CARTESIAN_POINT ( 'NONE',  ( 0.2280961430754513408, -1.329988288769240024, -1.704746276402234528 ) ) ;
#85895=CARTESIAN_POINT ( 'NONE',  ( 4.053227687556320014, 1.744102858319864113, -1.100964799198749455 ) ) ;
#85900=CARTESIAN_POINT ( 'NONE',  ( 5.589076619078012342, 1.650032040524500143, -0.8810306647013477210 ) ) ;
#85901=CARTESIAN_POINT ( 'NONE',  ( 4.219182763733449804, 1.701723821253621427, 0.3326838626578206282 ) ) ;
#85902=CARTESIAN_POINT ( 'NONE',  ( 2.805909833680774845, 1.258924587927259253, -1.202001966437598268 ) ) ;
#85903=CARTESIAN_POINT ( 'NONE',  ( 2.314399336204819857, 1.494381390340574489, -1.738437040929841082 ) ) ;
#85905=CARTESIAN_POINT ( 'NONE',  ( 6.216366674833015971, 1.951045902775162322, 0.7519257042096252341 ) ) ;
#85906=CARTESIAN_POINT ( 'NONE',  ( 6.720655732516681802, 0.002698097948229584257, 1.926293798961112858 ) ) ;
#85908=CARTESIAN_POINT ( 'NONE',  ( 1.916638904718031000, -1.319229391439219246, -1.525043083973671498 ) ) ;
#85909=CARTESIAN_POINT ( 'NONE',  ( 0.02373106683711476844, -1.352142385343929387, -1.725327757841052856 ) ) ;
#85913=CARTESIAN_POINT ( 'NONE',  ( 2.473420802178166067, -1.846219560914775570, -1.042883725575906029 ) ) ;
#85915=CARTESIAN_POINT ( 'NONE',  ( 5.145057536039753465, -1.563975785779356587, 0.9416349707431559413 ) ) ;
#85923=CARTESIAN_POINT ( 'NONE',  ( 1.670181813679386007, 2.014099715005359670, -0.1526998803580876252 ) ) ;
#85924=CARTESIAN_POINT ( 'NONE',  ( 0.2882880397960294605, -0.9922573751702695732, 1.857558580286112981 ) ) ;
#85926=CARTESIAN_POINT ( 'NONE',  ( 4.346440162718026912, -1.840208154270198015, -0.2762933559420696072 ) ) ;
#85933=CARTESIAN_POINT ( 'NONE',  ( 5.602125774977974260, -1.825872481414937853, 0.004271240736861136277 ) ) ;
#85937=CARTESIAN_POINT ( 'NONE',  ( 1.405166929871915604, 0.3316955492517637549, 1.701605581617445129 ) ) ;
#85938=CARTESIAN_POINT ( 'NONE',  ( 0.3568325553494673397, 1.722114113718915984, -0.2502821355834724537 ) ) ;
#85939=CARTESIAN_POINT ( 'NONE',  ( 6.094374174207308315, -2.295927367373576722, -0.2327322904458818675 ) ) ;
#85942=CARTESIAN_POINT ( 'NONE',  ( 1.634131612217240681, 1.018193428692963698, -1.791617596397138801 ) ) ;
#85944=CARTESIAN_POINT ( 'NONE',  ( 0.4915642615439493879, 1.928455281639355867, 0.5879340682083398217 ) ) ;
#85947=CARTESIAN_POINT ( 'NONE',  ( 0.09253734621218495660, -0.4319466259074012937, -1.930967020758065589 ) ) ;
#85948=CARTESIAN_POINT ( 'NONE',  ( 3.902528505893249733, -1.892296425594198750, -0.2755589300712790735 ) ) ;
#85950=CARTESIAN_POINT ( 'NONE',  ( 5.602238545945851023, -2.207063162045197924, -0.003355105161521875021 ) ) ;
#85955=CARTESIAN_POINT ( 'NONE',  ( 0.01237536129615121258, -2.019283296508204817, -0.04721428876065454638 ) ) ;
#85956=CARTESIAN_POINT ( 'NONE',  ( 3.100898361104642120, -0.6683016296473989204, -2.208703637169514788 ) ) ;
#85957=CARTESIAN_POINT ( 'NONE',  ( 4.404711838702720428, 0.5211615849865286476, 1.891323523724611766 ) ) ;
#85958=CARTESIAN_POINT ( 'NONE',  ( 0.4440980561614649158, -0.9299495107331550159, 1.727370323332158897 ) ) ;
#85961=CARTESIAN_POINT ( 'NONE',  ( 6.368375356916068597, -1.978549699825098429, -0.3886382054163611821 ) ) ;
#85963=CARTESIAN_POINT ( 'NONE',  ( -0.02968770228140016343, 0.003472272166151618711, -1.826291111852257343 ) ) ;
#85965=CARTESIAN_POINT ( 'NONE',  ( 3.098652014986380543, 2.154143853245940043, 0.2703130112568508103 ) ) ;
#85967=CARTESIAN_POINT ( 'NONE',  ( 0.5629301599625028407, 0.6213668382478373386, 2.027498709647377773 ) ) ;
#85973=CARTESIAN_POINT ( 'NONE',  ( 1.704443381354688203, -0.7389896827423731995, -1.923919429860524888 ) ) ;
#85979=CARTESIAN_POINT ( 'NONE',  ( 4.424404876070213710, -0.8207606565990737124, -1.727334472114170794 ) ) ;
#85982=CARTESIAN_POINT ( 'NONE',  ( 1.441375510584298913, -1.705046834049932292, 0.6123784311264174329 ) ) ;
#85984=CARTESIAN_POINT ( 'NONE',  ( 0.8486862992652006721, -1.733348825135153648, -0.8160025691017428473 ) ) ;
#85986=CARTESIAN_POINT ( 'NONE',  ( 2.031770498437397876, 1.981864486777328294, -0.5989037013024376410 ) ) ;
#85989=CARTESIAN_POINT ( 'NONE',  ( 0.9187500235564357576, 1.820693165844145867, 0.7566030219750378150 ) ) ;
#85990=CARTESIAN_POINT ( 'NONE',  ( 5.373632986646971865, 1.856140760046654403, -0.5156676092323666527 ) ) ;
#85991=CARTESIAN_POINT ( 'NONE',  ( 6.498651167236064730, -0.5841124237929047336, -2.128106146270396071 ) ) ;
#85994=CARTESIAN_POINT ( 'NONE',  ( 3.666515279890161239, -0.8333913613888814798, -1.886988505759807921 ) ) ;
#85999=CARTESIAN_POINT ( 'NONE',  ( 5.350649881110917327, 0.6085095821539068250, 2.016136239840255140 ) ) ;
#86001=CARTESIAN_POINT ( 'NONE',  ( 6.883263157960362477, -0.004191378316371896506, 2.053658919477070910 ) ) ;
#86003=CARTESIAN_POINT ( 'NONE',  ( 4.411504763889100289, -0.3743020017868465832, 2.128795073437335095 ) ) ;
#86004=CARTESIAN_POINT ( 'NONE',  ( 4.389322685995568740, -0.002182162029157329840, -2.019862493239577894 ) ) ;
#86011=CARTESIAN_POINT ( 'NONE',  ( 2.958220528980558761, -1.197304571117228100, 1.622486353517027968 ) ) ;
#86019=CARTESIAN_POINT ( 'NONE',  ( 4.534779904478015489, -1.617806963314952773, 1.203370736114671269 ) ) ;
#86021=CARTESIAN_POINT ( 'NONE',  ( 1.048929499675733235, -1.357256335890437926, -1.064349854222715885 ) ) ;
#86026=CARTESIAN_POINT ( 'NONE',  ( 5.729731410239141454, -1.186140735684092284, -1.446405967604667886 ) ) ;
#86027=CARTESIAN_POINT ( 'NONE',  ( -0.09313581672419719848, -0.4459848746838651623, -1.970588110806646753 ) ) ;
#86032=CARTESIAN_POINT ( 'NONE',  ( 0.3511856949766634095, 0.1948183440376727305, -2.006963311255556714 ) ) ;
#86038=CARTESIAN_POINT ( 'NONE',  ( 0.2861690844194793026, -0.6482510287857257136, -1.802810126718904504 ) ) ;
#86041=DIRECTION ( 'NONE',  ( -1.000000000000000000, 1.014813233446432150E-15, 1.972152263052529514E-31 ) ) ;
#86046=CARTESIAN_POINT ( 'NONE',  ( 4.083022661009271914, -0.2092679848491978134, -2.151539631373246220 ) ) ;
#86049=CARTESIAN_POINT ( 'NONE',  ( 1.160570123509139906, 2.118417766304943495, 0.09849428607798524360 ) ) ;
#86050=CARTESIAN_POINT ( 'NONE',  ( 6.821331453475777629, -0.1281762050449504198, 1.796388512460028286 ) ) ;
#86052=CARTESIAN_POINT ( 'NONE',  ( 2.671113287583181339, 0.1005484070672260644, -1.968930098583418387 ) ) ;
#86053=CARTESIAN_POINT ( 'NONE',  ( 4.869353489999923568, -1.618680692612521455, -1.018082601613921723 ) ) ;
#86056=CARTESIAN_POINT ( 'NONE',  ( 5.775830853014204180, -1.921903692836058886, 0.4298591908668251138 ) ) ;
#86057=CARTESIAN_POINT ( 'NONE',  ( 0.8142755762143333298, 1.794035260217427874, 0.7438321904150380082 ) ) ;
#86063=CARTESIAN_POINT ( 'NONE',  ( 5.426388453851806126, -0.8635988772061551355, -1.706256623820540108 ) ) ;
#86065=CARTESIAN_POINT ( 'NONE',  ( 3.158999515626020216, -1.670948785577108797, 1.441709373268922123 ) ) ;
#86066=CARTESIAN_POINT ( 'NONE',  ( 1.606762454812577179, -0.7948807482080816333, -2.058825234118460745 ) ) ;
#86069=CARTESIAN_POINT ( 'NONE',  ( 0.3285747216504387724, 1.318609938922534530, -1.385187620709791512 ) ) ;
#86070=CARTESIAN_POINT ( 'NONE',  ( 0.07661050522435490506, 0.2583762315121455599, -1.746200777818290195 ) ) ;
#86073=CARTESIAN_POINT ( 'NONE',  ( 2.910663983731573090, 0.6951178490613962868, 1.950330170896700022 ) ) ;
#86077=CARTESIAN_POINT ( 'NONE',  ( 0.2862814217290919894, -1.017545141758866789, 1.907252267444502269 ) ) ;
#86078=CARTESIAN_POINT ( 'NONE',  ( 2.894263506066748093, -0.6386881658498286818, -2.096408367471907841 ) ) ;
#86085=CARTESIAN_POINT ( 'NONE',  ( 6.293613488329289574, 1.277945636399902440, -1.172455961997687535 ) ) ;
#86087=CARTESIAN_POINT ( 'NONE',  ( 3.414952709633051864, -1.570776679111930640, 1.348709175982481856 ) ) ;
#86088=CARTESIAN_POINT ( 'NONE',  ( 4.165693581912960575, 1.384238758890417031, 1.602101081018918904 ) ) ;
#86091=CARTESIAN_POINT ( 'NONE',  ( 3.168761922233914952, 1.429703897159577464, -1.354768240434875759 ) ) ;
#86092=CARTESIAN_POINT ( 'NONE',  ( 1.212987991671743204, 1.561712320281399835, -1.103468303573502673 ) ) ;
#86093=CARTESIAN_POINT ( 'NONE',  ( 4.734495095973747070, 0.3888400998970488187, 2.258902165976091059 ) ) ;
#86094=CARTESIAN_POINT ( 'NONE',  ( 3.422296110638739286, 1.157362003623555236, -1.411967061744797469 ) ) ;
#86102=CARTESIAN_POINT ( 'NONE',  ( 4.289318580081720178, -0.004264002974461738975, -2.013376228308662252 ) ) ;
#86103=CARTESIAN_POINT ( 'NONE',  ( 3.203904402660478379, 0.7104733393662396868, -1.828749470067204896 ) ) ;
#86106=CARTESIAN_POINT ( 'NONE',  ( 0.1755611466353291517, 1.991966693188641280, -2.657903234774192658 ) ) ;
#86108=CARTESIAN_POINT ( 'NONE',  ( 0.3102505407175432661, 1.438864707272140775, -1.517118456267575022 ) ) ;
#86109=CARTESIAN_POINT ( 'NONE',  ( 5.664868940362820737, -1.601528614980719967, -0.7536287887903775351 ) ) ;
#86111=CARTESIAN_POINT ( 'NONE',  ( 2.449409141518565480, 0.5832169002529237201, -2.112351429719904861 ) ) ;
#86112=CARTESIAN_POINT ( 'NONE',  ( 6.351467175048743918, 1.735110083250133162, -0.1355937802150069815 ) ) ;
#86115=CARTESIAN_POINT ( 'NONE',  ( 0.1333692844072802142, 0.2389375359408679178, -2.087895146362698906 ) ) ;
#86116=CARTESIAN_POINT ( 'NONE',  ( 0.7852881911578631913, 1.155166132482473351, 1.281103752909551030 ) ) ;
#86117=CARTESIAN_POINT ( 'NONE',  ( 0.8377433530848135135, 0.8832496248250313320, -2.005872107257236969 ) ) ;
#86118=CARTESIAN_POINT ( 'NONE',  ( 2.965657822035951963, 0.3232568108629539361, -2.182957019552448141 ) ) ;
#86119=CARTESIAN_POINT ( 'NONE',  ( 0.6202906599508707375, 2.147645164210740365, -0.3171128231679083975 ) ) ;
#86121=CARTESIAN_POINT ( 'NONE',  ( 1.481820193039787403, -0.7077492718140475647, 1.995708955693164199 ) ) ;
#86122=CARTESIAN_POINT ( 'NONE',  ( 6.727182134110200273, -0.004969159814478123736, 2.189081792362323586 ) ) ;
#86123=CARTESIAN_POINT ( 'NONE',  ( 5.684577344524033293, -1.879503395548718148, -0.4217397607521166103 ) ) ;
#86124=EDGE_LOOP ( 'NONE', ( #58512, #25110, #168751, #10752 ) ) ;
#86126=CARTESIAN_POINT ( 'NONE',  ( 1.365189820700737577, 0.1628935585381158235, -2.286633867385555519 ) ) ;
#86130=CARTESIAN_POINT ( 'NONE',  ( 3.475417139410865275, -1.959577385150832907, -1.046020024706290297 ) ) ;
#86137=CARTESIAN_POINT ( 'NONE',  ( 1.635388916632842360, 0.6352005984417673501, 1.913803229121699534 ) ) ;
#86139=CARTESIAN_POINT ( 'NONE',  ( 0.6728087625662204641, 1.424998530877854552, -1.491364779339200641 ) ) ;
#86142=CARTESIAN_POINT ( 'NONE',  ( -0.006632162239710717895, -1.840811702136424088, -0.04651623371411393176 ) ) ;
#86145=CARTESIAN_POINT ( 'NONE',  ( 2.618099050500310998, 1.159573672392331112, -1.336980558935680241 ) ) ;
#86146=CARTESIAN_POINT ( 'NONE',  ( 1.652970434142877920, 1.038994816082598804, 1.728001345923817267 ) ) ;
#86147=CARTESIAN_POINT ( 'NONE',  ( 6.497592319816168249, -1.739837010378456617, 0.05289828334312414448 ) ) ;
#86148=CARTESIAN_POINT ( 'NONE',  ( 5.038769576086907342, -1.967128976631225434, 1.176836258767649745 ) ) ;
#86149=CARTESIAN_POINT ( 'NONE',  ( 3.380630241506640932, 1.664009615612583204, -0.7882418170854917916 ) ) ;
#86151=CARTESIAN_POINT ( 'NONE',  ( 4.243042751400435186, -1.588269943899191183, 0.8999137264355041577 ) ) ;
#86152=CARTESIAN_POINT ( 'NONE',  ( 4.711564657724523819, 1.930417226389494090, 0.5826574956761670920 ) ) ;
#86154=CARTESIAN_POINT ( 'NONE',  ( 3.485499699327331502, 2.046305154993263375, -0.9654624412855338234 ) ) ;
#86156=CARTESIAN_POINT ( 'NONE',  ( 6.821333371289608927, -0.1635999628400324479, 2.070553102365073173 ) ) ;
#86158=CARTESIAN_POINT ( 'NONE',  ( 3.965334771736851671, 1.774175476309115984, 1.066894043611272824 ) ) ;
#86163=CARTESIAN_POINT ( 'NONE',  ( 2.051278105266049590, -1.547248087829168339, -1.147608674410576901 ) ) ;
#86166=CARTESIAN_POINT ( 'NONE',  ( 0.2210688645036896216, -1.757681936009440893, -0.8888059845142733950 ) ) ;
#86171=CARTESIAN_POINT ( 'NONE',  ( 0.6334296782557496952, 2.055416226174343386, 0.8430641771750585489 ) ) ;
#86172=CARTESIAN_POINT ( 'NONE',  ( 3.557739748072580088, 0.5135893094758836597, -2.042235538380641202 ) ) ;
#86175=CARTESIAN_POINT ( 'NONE',  ( 1.029495724655055344, 1.794938190532389788, -0.4914328765713778524 ) ) ;
#86181=CARTESIAN_POINT ( 'NONE',  ( 1.441811196653530747, -1.994930912159533332, 0.7194735443712959588 ) ) ;
#86184=CARTESIAN_POINT ( 'NONE',  ( 4.264078424595136418, -1.956757550135434620, 0.1421211968542570592 ) ) ;
#86185=CARTESIAN_POINT ( 'NONE',  ( 2.870174731959000525, 1.155358403710282866, 1.826860881501219280 ) ) ;
#86186=CARTESIAN_POINT ( 'NONE',  ( 2.208333698829296310, 1.645431377724184463, 0.8263914577605266931 ) ) ;
#86188=CARTESIAN_POINT ( 'NONE',  ( 4.962738864268898098, 0.1657098081031352088, -1.732421123976911836 ) ) ;
#86192=CARTESIAN_POINT ( 'NONE',  ( 2.237400686453533183, -1.931180590798301955, 0.9714560045831142077 ) ) ;
#86193=CARTESIAN_POINT ( 'NONE',  ( 2.899767358622063806, 0.2439914025648345919, 2.001204936777578602 ) ) ;
#86195=CARTESIAN_POINT ( 'NONE',  ( 1.727627455807039691, -2.035446057602477321, 0.7283451284763039490 ) ) ;
#86196=CARTESIAN_POINT ( 'NONE',  ( 3.977382581243666504, 1.856787152588537548, -0.6629638669850937971 ) ) ;
#86197=CARTESIAN_POINT ( 'NONE',  ( 6.509000000000033204, 1.287336644856639456, 2.017667062298739822 ) ) ;
#86198=CARTESIAN_POINT ( 'NONE',  ( 3.632312094575868677, 0.2880498525525148623, 1.920478541846024179 ) ) ;
#86202=CARTESIAN_POINT ( 'NONE',  ( -0.1110810684432622653, 5.724789179085956192, -2.391029204513066553 ) ) ;
#86208=CARTESIAN_POINT ( 'NONE',  ( 0.1127427399064059588, -0.9454589178800475446, -1.991880357201977425 ) ) ;
#86210=CARTESIAN_POINT ( 'NONE',  ( 3.801568999928582659, -1.482573837031101016, -1.284759613706359271 ) ) ;
#86212=CARTESIAN_POINT ( 'NONE',  ( 1.266250242576156815, 1.862016182229693673, -0.7743172429433077264 ) ) ;
#86214=CARTESIAN_POINT ( 'NONE',  ( 3.011064194431464003, 0.05668958241028876355, 2.116758953476727267 ) ) ;
#86218=CARTESIAN_POINT ( 'NONE',  ( 2.712652182946372559, -0.1802803596865458491, 1.832282175343015407 ) ) ;
#86222=CARTESIAN_POINT ( 'NONE',  ( 4.201511661969238531, 1.892856375164463367, -0.9562558712687405649 ) ) ;
#86225=CARTESIAN_POINT ( 'NONE',  ( 5.096976104305405819, 1.715636550957209794, -1.141348886549067077 ) ) ;
#86226=AXIS2_PLACEMENT_3D ( 'NONE', #46035, #178159, #147792 ) ;
#86228=CARTESIAN_POINT ( 'NONE',  ( 2.419273308677453826, -1.061688697878185206, -1.504126257600538974 ) ) ;
#86233=CARTESIAN_POINT ( 'NONE',  ( 2.719571217284349363, -0.2154062111461417517, 2.196339928330424129 ) ) ;
#86234=CARTESIAN_POINT ( 'NONE',  ( 4.710415318105323657, -0.9616676431317521256, -2.047968690232481848 ) ) ;
#86236=CARTESIAN_POINT ( 'NONE',  ( 5.203285271772914555, 1.593979872821064570, -0.8609055379997750945 ) ) ;
#86237=CARTESIAN_POINT ( 'NONE',  ( 4.522610612662866458, 0.3335214923718023416, 1.886305606834618231 ) ) ;
#86240=CARTESIAN_POINT ( 'NONE',  ( 3.414874914781691473, 1.781649806626634858, 0.8443359948157087569 ) ) ;
#86241=CARTESIAN_POINT ( 'NONE',  ( 5.506679003988666388, 1.415762158562785533, -1.222804595763474333 ) ) ;
#86243=CARTESIAN_POINT ( 'NONE',  ( 5.283604245000163679, -1.767202373759840572, 0.5838029059755837080 ) ) ;
#86245=CARTESIAN_POINT ( 'NONE',  ( 0.6554828803995507158, 1.942095732595986890, -0.5424746339172461518 ) ) ;
#86247=CARTESIAN_POINT ( 'NONE',  ( 1.875742097524640384, 2.014971663898405652, -0.6126918839576761533 ) ) ;
#86251=CARTESIAN_POINT ( 'NONE',  ( 2.971057270251746818, -1.603071526910588629, 1.388259434452358665 ) ) ;
#86253=CARTESIAN_POINT ( 'NONE',  ( 0.9494800659552645739, -1.824215446917340389, 0.8674010940010259407 ) ) ;
#86258=CARTESIAN_POINT ( 'NONE',  ( 1.985828983967323325, 1.489073237690191176, 1.567133960648490199 ) ) ;
#86262=CARTESIAN_POINT ( 'NONE',  ( 6.639320575229281651, -0.0007625845807879281287, 2.103388539994067497 ) ) ;
#86266=CARTESIAN_POINT ( 'NONE',  ( 0.4159077360078728969, -1.177411712353953588, -1.848246096435968600 ) ) ;
#86268=CARTESIAN_POINT ( 'NONE',  ( 1.253188901120566134, -1.782426524439745030, 1.393456103103172250 ) ) ;
#86276=CARTESIAN_POINT ( 'NONE',  ( 4.547283022377748729, -1.335744037758682667, -1.091317429222604884 ) ) ;
#86278=CARTESIAN_POINT ( 'NONE',  ( 1.756752346989236768, -1.514669478205426190, -0.9150583790542564655 ) ) ;
#86279=CARTESIAN_POINT ( 'NONE',  ( 2.719391910328097683, 1.701792079550172421, 1.075097526896612088 ) ) ;
#86280=CARTESIAN_POINT ( 'NONE',  ( 5.614374367772542840, -0.9875226594672004143, -1.973556357105679115 ) ) ;
#86283=CARTESIAN_POINT ( 'NONE',  ( 3.955335691828856692, -1.755346444749112722, 0.9990557238469994772 ) ) ;
#86285=CARTESIAN_POINT ( 'NONE',  ( 5.127636373287420390, -0.3106611864900839515, 2.097473367668806876 ) ) ;
#86286=CARTESIAN_POINT ( 'NONE',  ( 4.411732571322396268, -1.242743209197882059, -1.587826168943158089 ) ) ;
#86287=CARTESIAN_POINT ( 'NONE',  ( 4.429823666617582312, -1.775263289385048848, 0.3600210208860327721 ) ) ;
#86289=ORIENTED_EDGE ( 'NONE', *, *, #136321, .F. ) ;
#86290=CARTESIAN_POINT ( 'NONE',  ( 2.201827603038747139, -1.870314503716500099, 0.04339327950253490246 ) ) ;
#86292=CARTESIAN_POINT ( 'NONE',  ( 1.740342883905017013, 1.098329146349947827, -1.565357986077076990 ) ) ;
#86296=B_SPLINE_CURVE_WITH_KNOTS ( 'NONE', 3,
 ( #188150, #39781, #111245, #143725, #62420, #63492, #61363, #131730, #144790, #94949 ),
 .UNSPECIFIED., .F., .F.,
 ( 4, 1, 1, 1, 1, 1, 1, 4 ),
 ( 0.000000000000000000, 0.09090790722575105287, 0.1825853934691276381, 0.2551728700554835028, 0.3603391217242263855, 0.5205903519787860034, 0.7335386666926504429, 0.9999999999999998890 ),
 .UNSPECIFIED. ) ;
#86298=CARTESIAN_POINT ( 'NONE',  ( 0.08795244648929222142, 1.102731429460445334, 1.562230693318837238 ) ) ;
#86300=CARTESIAN_POINT ( 'NONE',  ( 1.187862215860764126, -1.241893603568875903, -1.518774446641702580 ) ) ;
#86303=CARTESIAN_POINT ( 'NONE',  ( 3.691739789689612472, 1.995538565534977549, -0.7177698711837015022 ) ) ;
#86305=CARTESIAN_POINT ( 'NONE',  ( 5.255133876903111734, -1.663856106090171538, -1.057019077474026680 ) ) ;
#86308=CARTESIAN_POINT ( 'NONE',  ( 1.634521315757204940, 0.6676430208681031209, 2.009258352967583150 ) ) ;
#86310=CARTESIAN_POINT ( 'NONE',  ( 2.348173244826061268, -0.8873571809006628452, 1.870714752860686447 ) ) ;
#86314=CARTESIAN_POINT ( 'NONE',  ( 5.156232390734752258, -1.514662699498746878, 1.441270160984737370 ) ) ;
#86316=CARTESIAN_POINT ( 'NONE',  ( 2.942213871598580166, 1.811567870905493205, 0.2252638538085757203 ) ) ;
#86317=CARTESIAN_POINT ( 'NONE',  ( 1.348006360704995910, 0.8929448326314154416, -1.575985355173844527 ) ) ;
#86319=CARTESIAN_POINT ( 'NONE',  ( 6.691986956589398794, -0.9478133180038283978, 1.990996264204819122 ) ) ;
#86322=CARTESIAN_POINT ( 'NONE',  ( 5.139771110516938357, -1.557344429106276573, -1.563758303505815794 ) ) ;
#86325=CARTESIAN_POINT ( 'NONE',  ( 4.389254143344611947, -0.003399479254035177832, -1.912461472815998320 ) ) ;
#86329=CARTESIAN_POINT ( 'NONE',  ( 6.549288556030709252, 1.803345607721940524, -1.016871928424131877 ) ) ;
#86332=CARTESIAN_POINT ( 'NONE',  ( 6.093348126157794198, -0.7399906200981146709, 2.062998119606203939 ) ) ;
#86337=CARTESIAN_POINT ( 'NONE',  ( 3.971829172498120286, 1.036919360001643531, 1.556626693588740062 ) ) ;
#86343=CARTESIAN_POINT ( 'NONE',  ( 0.6374758831957715310, 1.839649526063956042, -0.7036667969960698210 ) ) ;
#86345=CARTESIAN_POINT ( 'NONE',  ( 1.581657880887325174, -0.6766953518495041342, 1.899626397962331126 ) ) ;
#86349=CARTESIAN_POINT ( 'NONE',  ( 1.728746526384251858, 0.2170652002222578369, 2.180672313318913869 ) ) ;
#86350=CARTESIAN_POINT ( 'NONE',  ( 6.410779360540267646, 1.349177972556347971, -1.230185023894624141 ) ) ;
#86357=CARTESIAN_POINT ( 'NONE',  ( 4.124425300631988200, 0.09459923933386081563, 1.838956108544815171 ) ) ;
#86358=CARTESIAN_POINT ( 'NONE',  ( 0.9791529934419791470, -1.820790759202662423, -0.8588917989246074303 ) ) ;
#86359=CARTESIAN_POINT ( 'NONE',  ( 1.669710354559012622, -0.8274895997400324443, -2.144421126502197517 ) ) ;
#86361=CARTESIAN_POINT ( 'NONE',  ( 1.375590602687895458, -1.817075280682054927, 0.4009801126106312674 ) ) ;
#86365=CARTESIAN_POINT ( 'NONE',  ( 4.025576834063953946, -0.3218090080209669024, 1.884953445776993863 ) ) ;
#86371=CARTESIAN_POINT ( 'NONE',  ( 4.265234282975380431, 2.027484720304991495, -0.5098422324811486828 ) ) ;
#86372=CARTESIAN_POINT ( 'NONE',  ( 2.412791964582483129, 1.669947582624079274, 0.8431454209596804805 ) ) ;
#86375=CARTESIAN_POINT ( 'NONE',  ( 3.139928233896288390, 0.4259470162499751633, 1.687361108405739385 ) ) ;
#86380=CARTESIAN_POINT ( 'NONE',  ( 3.615580125028591052, -1.699004861347377604, 0.2966152939984505466 ) ) ;
#86381=CARTESIAN_POINT ( 'NONE',  ( 3.527062600443749307, -2.024233912922444478, 0.8403589366152917073 ) ) ;
#86382=CARTESIAN_POINT ( 'NONE',  ( 5.936183876523434932, 1.091049494364674466, -1.918236432931222257 ) ) ;
#86383=CARTESIAN_POINT ( 'NONE',  ( 6.983263157960362122, 2.430545403621493072, 2.435370848939223620 ) ) ;
#86384=CARTESIAN_POINT ( 'NONE',  ( 3.362351297888244606, -2.168775535925556053, 0.1018362995675748534 ) ) ;
#86385=CARTESIAN_POINT ( 'NONE',  ( 1.805030607383810715, 1.517133602069477893, 1.015288170653723343 ) ) ;
#86387=CARTESIAN_POINT ( 'NONE',  ( 4.909417703775454278, -2.009542366629351484, 0.6670832617777838758 ) ) ;
#86389=CARTESIAN_POINT ( 'NONE',  ( 4.810265146351084375, 1.581823803905563430, -1.659390399702101337 ) ) ;
#86391=CARTESIAN_POINT ( 'NONE',  ( 6.720655732516641834, 2.102516797890502165, 2.037305422295607293 ) ) ;
#86393=CARTESIAN_POINT ( 'NONE',  ( 0.7859742890132662696, 2.042544534415400737, -0.5693509180391894686 ) ) ;
#86401=ORIENTED_EDGE ( 'NONE', *, *, #45059, .T. ) ;
#86402=CARTESIAN_POINT ( 'NONE',  ( 5.379529795981254914, -0.4926393568372189335, -1.955173248319847845 ) ) ;
#86404=CARTESIAN_POINT ( 'NONE',  ( 4.329007229187351591, -1.922695762783795947, -0.7470244877981512266 ) ) ;
#86406=CARTESIAN_POINT ( 'NONE',  ( -0.2408018239684096284, 1.329574536483958846, -2.350731018214331947 ) ) ;
#86410=CARTESIAN_POINT ( 'NONE',  ( 0.6036074345479571779, -2.080388865039545454, 0.2067186989125231189 ) ) ;
#86411=CARTESIAN_POINT ( 'NONE',  ( 5.186172726741035355, 1.650080556555008293, 1.158690440749516881 ) ) ;
#86412=CARTESIAN_POINT ( 'NONE',  ( 4.265079090171526310, 1.784866007061826298, -0.4516350764028759235 ) ) ;
#86414=CARTESIAN_POINT ( 'NONE',  ( 1.096240241049123210, -0.4132495022837120446, -1.674402075930980338 ) ) ;
#86415=FACE_OUTER_BOUND ( 'NONE', #29119, .T. ) ;
#86416=CARTESIAN_POINT ( 'NONE',  ( 0.7569315055401154568, 2.213468045025353881, -0.6199256774504552370 ) ) ;
#86418=CARTESIAN_POINT ( 'NONE',  ( 1.687200700035433876, -0.3313812920804170559, -2.237873883018532073 ) ) ;
#86419=CARTESIAN_POINT ( 'NONE',  ( 2.596425589483622787, -2.100489730888196238, -0.1540555546653120389 ) ) ;
#86424=( LENGTH_UNIT ( ) NAMED_UNIT ( * ) SI_UNIT ( .MILLI., .METRE. ) );
#86429=CARTESIAN_POINT ( 'NONE',  ( 5.590131909697702461, 1.323030080273413844, 1.784280720909060758 ) ) ;
#86430=CARTESIAN_POINT ( 'NONE',  ( 1.904481915951491189, 1.622449043516610123, -1.473309109067892697 ) ) ;
#86433=CARTESIAN_POINT ( 'NONE',  ( 5.828557447170540584, -1.245780601409246957, 1.515539014345569147 ) ) ;
#86437=CARTESIAN_POINT ( 'NONE',  ( 4.096021571020786567, 1.387573888390711385, 1.603661410755026440 ) ) ;
#86441=CARTESIAN_POINT ( 'NONE',  ( 6.543834100630380846, 0.8322713294773576020, -1.995267709627518427 ) ) ;
#86443=CARTESIAN_POINT ( 'NONE',  ( 4.915489835137424102, -0.9894786724786635013, -1.552603174752004600 ) ) ;
#86446=CARTESIAN_POINT ( 'NONE',  ( 1.135833342500572440, 0.3383711564543417927, 1.707032442944929729 ) ) ;
#86451=CARTESIAN_POINT ( 'NONE',  ( 5.278265135069068137, -1.204163492603943064, 1.795060720813673738 ) ) ;
#86455=CARTESIAN_POINT ( 'NONE',  ( 4.223607183596161718, -2.069420184152844566, 0.6248923283326962563 ) ) ;
#86457=CARTESIAN_POINT ( 'NONE',  ( 5.237557467868056094, -1.392094792763297617, -1.396070155715684269 ) ) ;
#86458=CARTESIAN_POINT ( 'NONE',  ( 3.497127502780640107, 1.691016411901521854, 0.3820211100199251697 ) ) ;
#86459=CARTESIAN_POINT ( 'NONE',  ( 0.4686481397476391364, -2.065551408369214137, -0.7328327568804984260 ) ) ;
#86460=CARTESIAN_POINT ( 'NONE',  ( 1.888135564707097425, 1.592107727680527329, 1.670599446388189913 ) ) ;
#86461=CARTESIAN_POINT ( 'NONE',  ( 4.042301887969748542, 2.050516515953205055, 0.2056252831919377910 ) ) ;
#86462=CARTESIAN_POINT ( 'NONE',  ( 0.1111347575282967681, -1.904682588250571573, 0.3777756254830581528 ) ) ;
#86468=CARTESIAN_POINT ( 'NONE',  ( 2.872332416675418276, 1.179501869419818494, 1.864919306664609921 ) ) ;
#86470=CARTESIAN_POINT ( 'NONE',  ( 0.3735836145450521228, -1.826584228078181660, 0.3550381321636967846 ) ) ;
#86471=CARTESIAN_POINT ( 'NONE',  ( -0.1290005225502676156, 1.324981729379502537, -2.425680704180297464 ) ) ;
#86475=CARTESIAN_POINT ( 'NONE',  ( 6.825078400183551608, 0.5660753733540256905, 2.196387875007102419 ) ) ;
#86476=CARTESIAN_POINT ( 'NONE',  ( 6.492148756324659153, -0.4961259030743305209, -1.772972609911625419 ) ) ;
#86478=CARTESIAN_POINT ( 'NONE',  ( 3.186453599190769648, -2.030135695866011503, -0.3537577654625714274 ) ) ;
#86481=CARTESIAN_POINT ( 'NONE',  ( 2.526040989133854886, -1.997384215488164694, 0.2984307725432763236 ) ) ;
#86483=CARTESIAN_POINT ( 'NONE',  ( 2.026313557074521210, 1.187556641299570614, -1.684123726253353492 ) ) ;
#86489=CARTESIAN_POINT ( 'NONE',  ( 5.936183876523434932, 1.091049494364674466, -1.918236432931222257 ) ) ;
#86490=CARTESIAN_POINT ( 'NONE',  ( 1.985828983967323325, 1.489073237690191176, 1.567133960648490199 ) ) ;
#86492=CARTESIAN_POINT ( 'NONE',  ( 1.305875433988498813, -1.124247956386617009, -1.673852571057245830 ) ) ;
#86493=CARTESIAN_POINT ( 'NONE',  ( 2.320019640604139788, -1.777541238149564107, 1.457059784348129217 ) ) ;
#86497=CARTESIAN_POINT ( 'NONE',  ( 2.096370420935515178, -0.4963513585865795275, -1.803540123670114736 ) ) ;
#86498=CARTESIAN_POINT ( 'NONE',  ( 3.696500153570709379, 1.422608671726926177, -1.429447704489300364 ) ) ;
#86502=CARTESIAN_POINT ( 'NONE',  ( 5.039724086851991913, -1.488677873513370331, -1.490019843855681536 ) ) ;
#86507=CARTESIAN_POINT ( 'NONE',  ( 5.783464979101770709, 0.1443126057797445849, -2.014664192723765623 ) ) ;
#86510=CARTESIAN_POINT ( 'NONE',  ( 0.3739784900498700493, -2.023488180542520887, 0.3987778971655773219 ) ) ;
#86517=CARTESIAN_POINT ( 'NONE',  ( 2.910768570555821277, 0.7291657262279130913, 2.045214924614814578 ) ) ;
#86520=CARTESIAN_POINT ( 'NONE',  ( 2.366542893654680402, 0.08848056876738576160, -1.839231530397527736 ) ) ;
#86522=CARTESIAN_POINT ( 'NONE',  ( 4.564136437409766600, -1.431273618155091576, 1.659743667367798103 ) ) ;
#86523=CARTESIAN_POINT ( 'NONE',  ( 6.883263157960391787, 1.253787318140922480, 2.167784446185747171 ) ) ;
#86524=CARTESIAN_POINT ( 'NONE',  ( 4.452213415057678425, 2.262087339288323840, -0.05152095106783493444 ) ) ;
#86532=CARTESIAN_POINT ( 'NONE',  ( 5.096827573163183800, 1.471272477087566699, -0.9831756853606200552 ) ) ;
#86534=CARTESIAN_POINT ( 'NONE',  ( 1.940588816512535120, 2.082954711654343427, 0.3096100588686269695 ) ) ;
#86538=CARTESIAN_POINT ( 'NONE',  ( 2.523828315609038864, 1.932092998399935091, -0.3813574256018251729 ) ) ;
#86541=CARTESIAN_POINT ( 'NONE',  ( 5.941655795435678122, -1.702662506596404279, 0.6190658298997688824 ) ) ;
#86546=CARTESIAN_POINT ( 'NONE',  ( 5.436355746168001879, 1.843147576875401983, 0.3187000444574567548 ) ) ;
#86549=CARTESIAN_POINT ( 'NONE',  ( 5.981320602565292077, -0.05662044862421274083, 2.069665677200482445 ) ) ;
#86561=CARTESIAN_POINT ( 'NONE',  ( 5.406682003534418079, 0.5678430586343993225, 1.877905798087247335 ) ) ;
#86563=CARTESIAN_POINT ( 'NONE',  ( 3.304064382408095302, -1.779354530013575131, 0.9478943420064069869 ) ) ;
#86564=CARTESIAN_POINT ( 'NONE',  ( 2.184663254350202255, 1.535933850207292783, -1.144682215256398239 ) ) ;
#86566=CARTESIAN_POINT ( 'NONE',  ( 0.09952931447375359952, -0.5783855404800625211, 2.113812074898171023 ) ) ;
#86568=CARTESIAN_POINT ( 'NONE',  ( 2.301827437220682171, -1.870247568056710774, 0.04138213060620592881 ) ) ;
#86572=CARTESIAN_POINT ( 'NONE',  ( 4.112992273575425628, 0.1058706520744826102, 2.114715381611050660 ) ) ;
#86574=CARTESIAN_POINT ( 'NONE',  ( 5.617656447048144486, 0.4075009240860455462, -2.029694874052537568 ) ) ;
#86575=CARTESIAN_POINT ( 'NONE',  ( 0.9254645587078378366, -1.329342062510083355, -1.613690532076578199 ) ) ;
#86577=CARTESIAN_POINT ( 'NONE',  ( 6.211906940382025510, -1.811394037990306627, 0.2264786762415857968 ) ) ;
#86585=CARTESIAN_POINT ( 'NONE',  ( 0.6096459265214678735, -0.6533943968328138618, 1.689718745909152053 ) ) ;
#86587=( BOUNDED_CURVE ( )  B_SPLINE_CURVE ( 3, ( #146174, #160262, #213259, #28128 ),
 .UNSPECIFIED., .F., .T. ) 
 B_SPLINE_CURVE_WITH_KNOTS ( ( 4, 4 ),
 ( 0.4999999999999970579, 1.000000000000000000 ),
 .UNSPECIFIED. ) 
 CURVE ( )  GEOMETRIC_REPRESENTATION_ITEM ( )  RATIONAL_B_SPLINE_CURVE ( ( 1.000000000000003997, 0.3333333333333334259, 0.3333333333333294846, 1.000000000000000222 ) ) 
 REPRESENTATION_ITEM ( '' )  );
#86593=AXIS2_PLACEMENT_3D ( 'NONE', #14669, #209665, #93833 ) ;
#86594=CARTESIAN_POINT ( 'NONE',  ( 6.257435441360899908, 1.928747933193178721, -0.5880367767025842518 ) ) ;
#86595=CARTESIAN_POINT ( 'NONE',  ( 0.3113914200543760336, 1.760583737686383321, -1.181573663439142052 ) ) ;
#86597=CARTESIAN_POINT ( 'NONE',  ( 0.1405533004714279999, 2.862415582289945526, -2.767767315042678700 ) ) ;
#86601=CARTESIAN_POINT ( 'NONE',  ( 3.696117419531047776, 0.8894436365228419739, -1.757264023730123581 ) ) ;
#86602=CARTESIAN_POINT ( 'NONE',  ( 4.376577478760902196, -0.4445230835841383898, -1.966641233467445016 ) ) ;
#86606=CARTESIAN_POINT ( 'NONE',  ( 5.226606370275341362, 0.1587857941063846590, 2.185760735149797185 ) ) ;
#86607=CARTESIAN_POINT ( 'NONE',  ( 2.959893420002459585, 1.917249785004307316, -0.1873479421724104088 ) ) ;
#86609=CARTESIAN_POINT ( 'NONE',  ( -0.02948999725178608200, 2.884818527723536530, -2.415019744152223868 ) ) ;
#86614=CARTESIAN_POINT ( 'NONE',  ( 4.803538196489102852, -1.519661447750167982, -1.252675939642827529 ) ) ;
#86615=CARTESIAN_POINT ( 'NONE',  ( 0.3627036604622800864, 0.1893831815216796277, -1.932784825206189661 ) ) ;
#86616=CARTESIAN_POINT ( 'NONE',  ( 3.721343298090164620, 1.727675083452884897, 1.033047338021097383 ) ) ;
#86617=CARTESIAN_POINT ( 'NONE',  ( 5.712396407272276377, -1.806953704233695612, -1.420304717212710122 ) ) ;
#86619=CARTESIAN_POINT ( 'NONE',  ( 3.942128412476927135, -0.9204884114761485714, 1.617296529409748773 ) ) ;
#86626=CARTESIAN_POINT ( 'NONE',  ( 0.3456114054924685486, 0.6817542107791437767, -2.082909237240769151 ) ) ;
#86631=CARTESIAN_POINT ( 'NONE',  ( 0.1877650043593872553, -0.8638833939697135866, 1.608357707688967242 ) ) ;
#86634=CARTESIAN_POINT ( 'NONE',  ( 2.760114697247218807, 1.645750434341390900, -0.5467383172713826678 ) ) ;
#86637=CARTESIAN_POINT ( 'NONE',  ( 5.496661139185262002, -0.4475443406098400523, -1.769863040007889410 ) ) ;
#86638=CARTESIAN_POINT ( 'NONE',  ( 2.817183829107517745, -1.704460984269994039, -0.9711623693852902139 ) ) ;
#86642=CARTESIAN_POINT ( 'NONE',  ( 4.776102292387626846, 2.097323840013893381, -0.3118266106481304423 ) ) ;
#86645=CARTESIAN_POINT ( 'NONE',  ( 1.393514648303464165, -1.873246724434135313, 0.8816542684770898308 ) ) ;
#86648=CARTESIAN_POINT ( 'NONE',  ( 5.127666992232062348, -0.3272401999867382560, 2.196937980255990741 ) ) ;
#86650=CARTESIAN_POINT ( 'NONE',  ( 2.989241104188970155, -2.295904969233518500, 0.1156830036863568528 ) ) ;
#86658=CARTESIAN_POINT ( 'NONE',  ( 3.392734571251673881, -1.844325299564765652, -0.5055192353106837677 ) ) ;
#86660=CARTESIAN_POINT ( 'NONE',  ( 3.821100691872282518, -0.1266977344972844144, 1.720184112200423332 ) ) ;
#86661=CARTESIAN_POINT ( 'NONE',  ( 3.538296236868877731, 0.7303062672313584969, 1.879804216660937666 ) ) ;
#86662=CARTESIAN_POINT ( 'NONE',  ( 4.026267332373588914, -1.999701941076356349, 1.133592428816285080 ) ) ;
#86664=CARTESIAN_POINT ( 'NONE',  ( 6.305314546112477103, 1.749969596565099650, 1.171488565500600654 ) ) ;
#86667=CARTESIAN_POINT ( 'NONE',  ( 4.323360031453548302, -1.693909316728856806, 0.5125324126216290743 ) ) ;
#86669=CARTESIAN_POINT ( 'NONE',  ( 0.6040055286682350921, -2.280654241543427663, 0.2304348961432670095 ) ) ;
#86671=CARTESIAN_POINT ( 'NONE',  ( 0.005214030526056419486, -0.7400075616556491820, -1.574097848898856622 ) ) ;
#86673=CARTESIAN_POINT ( 'NONE',  ( 5.244143516318892750, 0.6338322011035132375, 2.097776330851252258 ) ) ;
#86677=CARTESIAN_POINT ( 'NONE',  ( 0.6257148180217129152, 0.2125798311119214690, -2.160765367999056608 ) ) ;
#86678=CARTESIAN_POINT ( 'NONE',  ( 1.112517963266421939, 1.944731545904467396, 0.5331650539944567946 ) ) ;
#86680=CARTESIAN_POINT ( 'NONE',  ( 4.441968003317652958, 0.8225352836801721468, -1.742211325687251788 ) ) ;
#86682=CARTESIAN_POINT ( 'NONE',  ( 1.652877544743835969, 2.198119390704804665, 0.3199964322739051736 ) ) ;
#86688=DIRECTION ( 'NONE',  ( -0.9999980456341538426, 0.000000000000000000, -0.001977050295958626691 ) ) ;
#86690=CARTESIAN_POINT ( 'NONE',  ( 4.757210230733205591, 1.720523950154304371, -0.2617468875206073742 ) ) ;
#86691=CARTESIAN_POINT ( 'NONE',  ( 2.101936620064443151, 0.7537240185569763495, -1.811501260397870405 ) ) ;
#86697=CARTESIAN_POINT ( 'NONE',  ( 0.2212323960570794501, -1.841704181501323312, -0.9290775759197547057 ) ) ;
#86701=CARTESIAN_POINT ( 'NONE',  ( 0.9016947886714383742, 1.851236229948808543, 1.300475659685183416 ) ) ;
#86705=CARTESIAN_POINT ( 'NONE',  ( 1.475632603725419489, 1.109822327618605442, 1.505604422130282227 ) ) ;
#86706=CARTESIAN_POINT ( 'NONE',  ( 0.6153164582703105623, 0.1250789957258427176, 1.729716150945133535 ) ) ;
#86707=CARTESIAN_POINT ( 'NONE',  ( 4.036819321710017228, -1.906298169312226953, 1.081085072550565407 ) ) ;
#86708=CARTESIAN_POINT ( 'NONE',  ( 5.842881032528668861, 0.4426140756379555730, 2.264596805331307472 ) ) ;
#86709=CARTESIAN_POINT ( 'NONE',  ( 0.7782833776110262836, -1.145455985629862505, 1.713024904945841254 ) ) ;
#86710=CARTESIAN_POINT ( 'NONE',  ( 3.046748965309022505, -1.587984067068026528, -1.117546226756223726 ) ) ;
#86712=CARTESIAN_POINT ( 'NONE',  ( 5.764887228985436707, -1.690807747980655584, -0.8004016547063924625 ) ) ;
#86716=CARTESIAN_POINT ( 'NONE',  ( 4.922500090287251773, -1.427935867408920645, -1.423962988533589158 ) ) ;
#86720=CARTESIAN_POINT ( 'NONE',  ( 1.576486190600217663, -1.733098801405801304, -0.5742540608338757568 ) ) ;
#86729=CARTESIAN_POINT ( 'NONE',  ( 5.514321518048907578, -2.019862493962302441, 0.002152582845403941403 ) ) ;
#86730=CARTESIAN_POINT ( 'NONE',  ( 6.481102860290734569, -2.029466250747449685, -0.9033904549611364576 ) ) ;
#86735=CARTESIAN_POINT ( 'NONE',  ( 5.366112562010656895, 1.013659120426290361, 1.794278544449072088 ) ) ;
#86736=CARTESIAN_POINT ( 'NONE',  ( 4.061172775696818782, -1.158689426361030561, 1.650081270007992318 ) ) ;
#86744=CARTESIAN_POINT ( 'NONE',  ( 4.323592178502837058, -1.495822217463145476, 1.351947993609707632 ) ) ;
#86745=CARTESIAN_POINT ( 'NONE',  ( 3.714658492009088153, -0.1339090230784936997, 1.836323816731308067 ) ) ;
#86747=CARTESIAN_POINT ( 'NONE',  ( 1.629934303081633340, -2.171740791250169611, 0.7807429155501348639 ) ) ;
#86750=CARTESIAN_POINT ( 'NONE',  ( 4.956408742875526130, 0.8222144862577386304, 1.999314050312686053 ) ) ;
#86751=CARTESIAN_POINT ( 'NONE',  ( 3.397672961473942266, -1.985868886743065609, 0.3494831190506141883 ) ) ;
#86753=CARTESIAN_POINT ( 'NONE',  ( 0.2923913620977801053, 1.614019350141202569, -1.079779171115168523 ) ) ;
#86758=CARTESIAN_POINT ( 'NONE',  ( 2.289737743334671283, -0.8020533187339595749, 1.690132462187944107 ) ) ;
#86759=CARTESIAN_POINT ( 'NONE',  ( 0.5265599218138971027, 1.885207356905926668, 0.5763402985480212681 ) ) ;
#86762=CARTESIAN_POINT ( 'NONE',  ( 1.155211076828046579, -1.737760091701185505, 1.360235214042208263 ) ) ;
#86768=CARTESIAN_POINT ( 'NONE',  ( 5.963742398600946792, 1.942370021616221409, -0.3365726279523760800 ) ) ;
#86769=CARTESIAN_POINT ( 'NONE',  ( 6.604155123031994812, -2.307348207032692944, 0.04906353339812623282 ) ) ;
#86770=CARTESIAN_POINT ( 'NONE',  ( 6.566864649055507819, 1.378042638564499489, -1.251022615016267103 ) ) ;
#86772=CARTESIAN_POINT ( 'NONE',  ( 3.924720150778399752, -1.388762634255924500, 1.525101558930273660 ) ) ;
#86775=ORIENTED_EDGE ( 'NONE', *, *, #5273, .T. ) ;
#86780=CARTESIAN_POINT ( 'NONE',  ( 6.742638747055813120, -2.127943412135436585, -0.4303581323979056017 ) ) ;
#86782=CARTESIAN_POINT ( 'NONE',  ( 4.862772069579198941, 0.1752732939881325724, -1.832877676746891726 ) ) ;
#86785=CARTESIAN_POINT ( 'NONE',  ( 0.7021627906659901885, -0.6242572379067250488, -1.763460184394528341 ) ) ;
#86789=CARTESIAN_POINT ( 'NONE',  ( 0.6625817696367036769, 0.5554855734208345996, 1.829800363923417716 ) ) ;
#86791=CARTESIAN_POINT ( 'NONE',  ( 1.480939207288126669, 1.637052324538622816, -0.6731226676765161843 ) ) ;
#86793=CARTESIAN_POINT ( 'NONE',  ( 6.551439491213440824, -1.797098368391306655, 0.9074013689854224518 ) ) ;
#86795=CARTESIAN_POINT ( 'NONE',  ( 4.763251566037994600, 1.785832754541897049, -0.6935334960865118248 ) ) ;
#86798=CARTESIAN_POINT ( 'NONE',  ( 4.932068866601894364, 1.132370341068598796, 1.611282302955379553 ) ) ;
#86799=CARTESIAN_POINT ( 'NONE',  ( 6.345964425358009642, -1.322526734765665513, -1.526637064097993157 ) ) ;
#86801=CARTESIAN_POINT ( 'NONE',  ( 4.328871119428026049, 0.09166491666120352155, 1.868520897946590598 ) ) ;
#86802=CARTESIAN_POINT ( 'NONE',  ( 5.707552393076498198, -0.4128270653469527374, 1.674615006835003639 ) ) ;
#86804=CARTESIAN_POINT ( 'NONE',  ( 3.580891165198408110, -2.126768340858419926, -0.5889919780145411732 ) ) ;
#86807=CARTESIAN_POINT ( 'NONE',  ( 0.7661727470247855498, -2.052889565338772204, 0.2005107248105562623 ) ) ;
#86814=CARTESIAN_POINT ( 'NONE',  ( 3.279797552538410876, -1.996039814156633785, 0.5495672325947635883 ) ) ;
#86818=CARTESIAN_POINT ( 'NONE',  ( 1.207682226051248753, 1.530763495831432452, 1.317637323925124671 ) ) ;
#86822=CARTESIAN_POINT ( 'NONE',  ( 0.07499057489267992038, 0.7202342490539682673, -2.037914685249627045 ) ) ;
#86824=CARTESIAN_POINT ( 'NONE',  ( 6.169296033003512925, -0.7230314695168098549, -1.882185070641306801 ) ) ;
#86825=CARTESIAN_POINT ( 'NONE',  ( 5.348823992091742419, -1.734843432642660721, -0.8128511771108116735 ) ) ;
#86827=CARTESIAN_POINT ( 'NONE',  ( 4.054362073078698891, -1.623213109359676443, 1.472610181411205144 ) ) ;
#86829=CARTESIAN_POINT ( 'NONE',  ( 1.951281838316549777, -1.706683157587106425, 0.8630329916254892986 ) ) ;
#86833=CARTESIAN_POINT ( 'NONE',  ( 1.370720498019749378, -0.2986500928384462350, -1.994069080148860973 ) ) ;
#86835=CARTESIAN_POINT ( 'NONE',  ( 6.515165533258342023, -2.126321577054360201, 0.5302794918828001025 ) ) ;
#86837=CARTESIAN_POINT ( 'NONE',  ( 3.469487465715580310, 1.682841854137674398, -0.3771888234031828824 ) ) ;
#86839=CARTESIAN_POINT ( 'NONE',  ( -0.1405533004718676759, 6.947778977978678050, -2.315285900534403307 ) ) ;
#86843=CARTESIAN_POINT ( 'NONE',  ( 1.521847698614446687, 1.933392594956625521, -0.3320675068423510345 ) ) ;
#86846=CARTESIAN_POINT ( 'NONE',  ( 0.07536363704233395300, 5.720741966631408104, -2.738263776839637398 ) ) ;
#86851=CARTESIAN_POINT ( 'NONE',  ( 3.387185712204858312, 0.04143215291275677975, -1.811162278692766581 ) ) ;
#86855=CARTESIAN_POINT ( 'NONE',  ( 4.652869415276386533, 0.3145016728411016982, 1.783790502623605834 ) ) ;
#86857=( NAMED_UNIT ( * ) PLANE_ANGLE_UNIT ( ) SI_UNIT ( $, .RADIAN. ) );
#86859=CARTESIAN_POINT ( 'NONE',  ( 5.652756593210860103, -0.4525561148686143009, -1.805067620203390177 ) ) ;
#86861=CARTESIAN_POINT ( 'NONE',  ( 2.706530202829552145, 1.804627309565815185, 0.6429686382581675241 ) ) ;
#86870=CARTESIAN_POINT ( 'NONE',  ( 1.816468492311611893, 1.951142502984483107, 0.7513475392508098816 ) ) ;
#86872=CARTESIAN_POINT ( 'NONE',  ( 6.827182134110199030, 0.001020705822914885546, 1.910856149448316721 ) ) ;
#86874=CARTESIAN_POINT ( 'NONE',  ( 2.274178591966895091, -1.125271047149905890, 1.437439779654096750 ) ) ;
#86876=CARTESIAN_POINT ( 'NONE',  ( 2.338023529656753752, -1.104205016203146705, -1.561194055274425452 ) ) ;
#86877=CARTESIAN_POINT ( 'NONE',  ( 1.978894816976022097, 1.836590731562221412, 0.7118427970769640734 ) ) ;
#86878=CARTESIAN_POINT ( 'NONE',  ( 3.685046248344743258, 1.408799512439436352, 1.336988689110546913 ) ) ;
#86883=CARTESIAN_POINT ( 'NONE',  ( 4.693665235656380830, 1.977662049654808740, -0.7657889336421249693 ) ) ;
#86892=CARTESIAN_POINT ( 'NONE',  ( 3.826616632296374831, 1.734130841282412128, 0.5711148077138239465 ) ) ;
#86897=CARTESIAN_POINT ( 'NONE',  ( 4.785944050937030347, -0.8815013282119155136, 1.649949660215948688 ) ) ;
#86899=CARTESIAN_POINT ( 'NONE',  ( 1.998540859798603408, -0.5134167636005394497, -1.856760371892735906 ) ) ;
#86907=CARTESIAN_POINT ( 'NONE',  ( 1.441172756004579947, -1.817888344413360668, -1.085095524780084864 ) ) ;
#86910=CARTESIAN_POINT ( 'NONE',  ( 5.911005882915712384, -1.635593682349820721, 1.269112435710928688 ) ) ;
#86911=CARTESIAN_POINT ( 'NONE',  ( 0.5382993156314471728, -1.579489783069366604, 0.9460463261394758128 ) ) ;
#86913=CARTESIAN_POINT ( 'NONE',  ( 6.574781987728091970, -0.9847942639734930115, 2.074158207377621910 ) ) ;
#86917=CARTESIAN_POINT ( 'NONE',  ( 1.131297326486919497, -2.070297854115164871, 0.9843215409001818683 ) ) ;
#86920=CARTESIAN_POINT ( 'NONE',  ( 6.316353394666050391, 1.812894500769960837, 0.6965700268309078513 ) ) ;
#86924=CARTESIAN_POINT ( 'NONE',  ( 5.994389040191065554, -1.017321598621454548, 1.619163160827830517 ) ) ;
#86929=CARTESIAN_POINT ( 'NONE',  ( 3.275413508211636238, 1.326730841477074208, 1.615706224610208519 ) ) ;
#86930=CARTESIAN_POINT ( 'NONE',  ( 1.551229123295729373, 0.5181449431543529993, -1.692289574110398931 ) ) ;
#86934=CARTESIAN_POINT ( 'NONE',  ( 4.629038687585553369, -2.096899809942855075, 0.9264041093646653291 ) ) ;
#86935=CARTESIAN_POINT ( 'NONE',  ( 3.468456934111513235, 0.04105959252117792613, -1.740014521098575351 ) ) ;
#86938=CARTESIAN_POINT ( 'NONE',  ( 3.022450238936627009, 1.725798670860735351, -0.1664453034943418896 ) ) ;
#86939=CARTESIAN_POINT ( 'NONE',  ( 3.578747896202236323, 1.379726198893852729, -1.676393335895840497 ) ) ;
#86941=CARTESIAN_POINT ( 'NONE',  ( 4.628138809701114020, 2.011451458044950069, 0.1435230606586651581 ) ) ;
#86942=CARTESIAN_POINT ( 'NONE',  ( 2.031250000000000888, -0.7852924748300881275, -1.895863743164043491 ) ) ;
#86944=CARTESIAN_POINT ( 'NONE',  ( 2.573164103464478991, 0.09656903795818297387, -1.924097065980167942 ) ) ;
#86946=CARTESIAN_POINT ( 'NONE',  ( 5.062811918942510481, 0.6453760322048059939, 2.125560002649288460 ) ) ;
#86953=CARTESIAN_POINT ( 'NONE',  ( 1.155278206730834256, 0.4382352071879510036, 2.177490050429623736 ) ) ;
#86954=CARTESIAN_POINT ( 'NONE',  ( 5.793401095800717826, -1.774274828963496198, 0.8374297333502839225 ) ) ;
#86958=CARTESIAN_POINT ( 'NONE',  ( 6.661402789601885033, 0.3967159107356016401, -2.227235065690711835 ) ) ;
#86960=CARTESIAN_POINT ( 'NONE',  ( 2.893094712532847890, 0.2500570216604477980, 2.047387263510790145 ) ) ;
#86964=CARTESIAN_POINT ( 'NONE',  ( 5.184763189090160651, -0.2277032997176874074, -1.856539885857370953 ) ) ;
#86965=CARTESIAN_POINT ( 'NONE',  ( 3.603937110245566178, -0.1228517400825197836, 1.729840182746833266 ) ) ;
#86966=CARTESIAN_POINT ( 'NONE',  ( 3.755166387800693339, 1.726757624646685807, -0.2173075579294906912 ) ) ;
#86967=CARTESIAN_POINT ( 'NONE',  ( 1.224644656679523713, 2.210950556192964989, 0.6053773189644614527 ) ) ;
#86969=CARTESIAN_POINT ( 'NONE',  ( 5.021074897447791230, -1.984789774362485604, 0.6572858584967393725 ) ) ;
#86970=CARTESIAN_POINT ( 'NONE',  ( 6.703083108286362446, -0.4264415456523527603, 1.901745634116110084 ) ) ;
#86972=CARTESIAN_POINT ( 'NONE',  ( 1.283827520628720187, 1.646837967535810021, -1.163270716046126196 ) ) ;
#86973=CARTESIAN_POINT ( 'NONE',  ( 0.1819133275808570704, -1.029140439971199417, 1.934768540691175431 ) ) ;
#86977=CARTESIAN_POINT ( 'NONE',  ( 2.631617588254760776, -0.2053842346896698201, 2.110501108333342035 ) ) ;
#86979=CARTESIAN_POINT ( 'NONE',  ( 4.951681858558426796, 0.5695450498939165218, -1.734646904759745700 ) ) ;
#86984=CARTESIAN_POINT ( 'NONE',  ( 2.584245202030683419, 1.084020786718616680, 1.704056320703779992 ) ) ;
#86985=CARTESIAN_POINT ( 'NONE',  ( 0.08314155087942810829, -0.1569203414564980525, -2.071771216027401774 ) ) ;
#86987=CARTESIAN_POINT ( 'NONE',  ( 4.328838875689292820, -1.735142615721802395, -0.6730405439913983434 ) ) ;
#86992=CARTESIAN_POINT ( 'NONE',  ( 5.426323838365306074, 1.084245000580752238, -1.468710674947353967 ) ) ;
#86996=CARTESIAN_POINT ( 'NONE',  ( 1.633743589071215974, 0.1333172958793479579, -1.728787957231948447 ) ) ;
#86997=CARTESIAN_POINT ( 'NONE',  ( 0.09317796543232242934, -1.739829294281483474, -0.04824335600969902743 ) ) ;
#86998=CARTESIAN_POINT ( 'NONE',  ( 5.602268381685036935, -2.307868969066428022, -0.005371834822459965395 ) ) ;
#87001=CARTESIAN_POINT ( 'NONE',  ( 1.950533276942335137, 0.6436621796281314367, 1.957774297735858759 ) ) ;
#87003=CARTESIAN_POINT ( 'NONE',  ( 6.714253291261501388, -1.839887274036870357, -1.377324995421406628 ) ) ;
#87007=CARTESIAN_POINT ( 'NONE',  ( 6.473518811298506925, 1.789458955665638618, -0.5451884755478533240 ) ) ;
#87008=CARTESIAN_POINT ( 'NONE',  ( 3.322422747544371280, -0.7792853099402965444, -1.746611395919236642 ) ) ;
#87010=CARTESIAN_POINT ( 'NONE',  ( 4.600333186373093852, -2.206333364838486411, -0.05604163552313382035 ) ) ;
#87015=CARTESIAN_POINT ( 'NONE',  ( 6.094406630213895504, -1.134638919006492275, 1.791192486788994120 ) ) ;
#87017=CARTESIAN_POINT ( 'NONE',  ( 3.733692867724636599, -2.133222801268436442, 0.8804087197434546930 ) ) ;
#87018=CARTESIAN_POINT ( 'NONE',  ( 3.437899435096212208, 1.242623406730450908, 1.518177208742684803 ) ) ;
#87021=CARTESIAN_POINT ( 'NONE',  ( 0.3562053913853078790, -1.961198556353323186, -0.05404869553313899899 ) ) ;
#87025=CARTESIAN_POINT ( 'NONE',  ( 5.665250009225348826, 1.861346387706263261, -0.7762253298396750711 ) ) ;
#87028=CARTESIAN_POINT ( 'NONE',  ( 3.081114545232612301, 2.042771114613873173, 0.7355539269583191153 ) ) ;
#87030=CARTESIAN_POINT ( 'NONE',  ( 0.4223351350958382544, -2.109807164369668087, 0.2139620856976830743 ) ) ;
#87035=CARTESIAN_POINT ( 'NONE',  ( 1.247419646546283234, -1.622699693697586820, -1.270148745232473564 ) ) ;
#87043=CARTESIAN_POINT ( 'NONE',  ( 4.283787348595206268, 1.854039900284172315, -0.4678174759695231666 ) ) ;
#87046=CARTESIAN_POINT ( 'NONE',  ( 0.2811518721992244951, 0.1772043297433387177, -1.802849762578159876 ) ) ;
#87048=CARTESIAN_POINT ( 'NONE',  ( 0.9892949506953198080, -0.4622125203353181222, 1.859009271263431184 ) ) ;
#87049=CARTESIAN_POINT ( 'NONE',  ( 1.697802635435996743, -1.498143435978617877, -1.429203828351800487 ) ) ;
#87052=CARTESIAN_POINT ( 'NONE',  ( 0.08089089327990153788, -0.1352431037574420292, -1.940231264204687722 ) ) ;
#87053=CARTESIAN_POINT ( 'NONE',  ( 3.088313589057069208, -1.798746773638896457, -0.3115406389907551810 ) ) ;
#87054=CARTESIAN_POINT ( 'NONE',  ( 0.1183777584694784279, -2.261842813846013822, 0.4569907027171058456 ) ) ;
#87057=CARTESIAN_POINT ( 'NONE',  ( 4.475086314992714698, 1.884572246790953365, 0.8388810360253369236 ) ) ;
#87062=CARTESIAN_POINT ( 'NONE',  ( 5.420966337283807945, 1.944620675078809757, 0.8088979906116978702 ) ) ;
#87064=CARTESIAN_POINT ( 'NONE',  ( 5.969205681473694902, 1.824102622056431811, 0.9793482939001868504 ) ) ;
#87066=CARTESIAN_POINT ( 'NONE',  ( 4.270900206319126369, -2.015198044118733822, -0.7823990653590962019 ) ) ;
#87067=CARTESIAN_POINT ( 'NONE',  ( 4.740881522827352867, 1.933304458870839238, 0.5843455605825734755 ) ) ;
#87069=EDGE_CURVE ( 'NONE', #71735, #21539, #167775, .T. ) ;
#87074=CARTESIAN_POINT ( 'NONE',  ( 2.044158018538293042, 0.8666093899718421145, 1.820985203412978093 ) ) ;
#87082=CARTESIAN_POINT ( 'NONE',  ( 4.552361342037492875, -1.314984614574012944, 1.528753174698034067 ) ) ;
#87085=CARTESIAN_POINT ( 'NONE',  ( 6.821331452548096586, -0.1252896706360993595, 1.696280295671446448 ) ) ;
#87090=CARTESIAN_POINT ( 'NONE',  ( 5.325416506339426981, -1.776575524504429016, 0.5857008802128694791 ) ) ;
#87091=CARTESIAN_POINT ( 'NONE',  ( 0.2232913631893228001, 1.752491241892171647, 0.9904617665423065542 ) ) ;
#87096=CARTESIAN_POINT ( 'NONE',  ( 0.9136856707930467447, -1.281379520587552889, -1.556895127150646374 ) ) ;
#87097=CARTESIAN_POINT ( 'NONE',  ( 0.9842725786804270571, -1.148342222048874595, 1.401147620581437048 ) ) ;
#87103=CARTESIAN_POINT ( 'NONE',  ( 5.923430108280006934, -1.391030039757386039, -1.317302766908773126 ) ) ;
#87111=CARTESIAN_POINT ( 'NONE',  ( 3.168983506954273999, -1.996715753333128118, -0.8287754370841573515 ) ) ;
#87114=CARTESIAN_POINT ( 'NONE',  ( 0.9496594531581278309, -1.914679731917130479, 0.9119059213342149972 ) ) ;
#87115=CARTESIAN_POINT ( 'NONE',  ( 5.842758758449526191, 0.3585452818064547853, 1.789846783968067845 ) ) ;
#87116=CARTESIAN_POINT ( 'NONE',  ( 1.915242260480106706, -0.2453889982298693984, 1.955985308386765542 ) ) ;
#87117=CARTESIAN_POINT ( 'NONE',  ( 4.254103502353132171, 0.8128351696983120434, -1.731171583500931366 ) ) ;
#87118=ORIENTED_EDGE ( 'NONE', *, *, #159948, .T. ) ;
#87120=CARTESIAN_POINT ( 'NONE',  ( 6.285607346219458158, -1.855037422363578381, 0.6622139934589140742 ) ) ;
#87122=CARTESIAN_POINT ( 'NONE',  ( 0.1111347575282967681, -1.904682588250571573, 0.3777756254830581528 ) ) ;
#87129=CARTESIAN_POINT ( 'NONE',  ( 5.268181577278353345, 1.909906527651853425, -0.09793718704654422180 ) ) ;
#87131=CARTESIAN_POINT ( 'NONE',  ( 0.3060867131535296992, -0.5861141839358529060, 2.127432003918772629 ) ) ;
#87134=CARTESIAN_POINT ( 'NONE',  ( -0.1108833634136767443, 0.0002062650063822807356, -1.896853557917008271 ) ) ;
#87138=CARTESIAN_POINT ( 'NONE',  ( 2.594261239525695206, 0.9781076984213372683, -1.824767828009652204 ) ) ;
#87142=CARTESIAN_POINT ( 'NONE',  ( 0.2335756976950612018, -1.975703151049061024, 0.8776370805363906680 ) ) ;
#87146=CARTESIAN_POINT ( 'NONE',  ( 6.825078400183553384, 0.5907600490881077526, 1.908621492364571903 ) ) ;
#87148=CARTESIAN_POINT ( 'NONE',  ( 5.836466137708809399, 0.4949425091341461136, -1.662031903658898413 ) ) ;
#87151=CARTESIAN_POINT ( 'NONE',  ( 3.537997267176114846, 1.309675639058418550, 1.603382541711120268 ) ) ;
#87152=CARTESIAN_POINT ( 'NONE',  ( 4.851218673320928154, 0.2063579389092398131, -2.107127644889031703 ) ) ;
#87155=CARTESIAN_POINT ( 'NONE',  ( 2.448051270322794348, -0.8465065455745772738, 1.778409512993859076 ) ) ;
#87156=CARTESIAN_POINT ( 'NONE',  ( 1.230557176020010912, 1.282188879665364656, -1.419081615486268433 ) ) ;
#87157=CARTESIAN_POINT ( 'NONE',  ( 4.470831859796895458, 0.002540009476469616122, -2.292435214262526166 ) ) ;
#87158=CARTESIAN_POINT ( 'NONE',  ( 2.156629195875509719, -1.411784796728832170, 1.157573153174975111 ) ) ;
#87162=EDGE_CURVE ( 'NONE', #68014, #120459, #79902, .T. ) ;
#87163=CARTESIAN_POINT ( 'NONE',  ( 3.885024706246028803, -1.880017414580990032, -0.7205730073996403640 ) ) ;
#87164=CARTESIAN_POINT ( 'NONE',  ( 3.467582345443523728, -0.3871886708083654427, 1.922995549214156608 ) ) ;
#87167=FACE_OUTER_BOUND ( 'NONE', #31605, .T. ) ;
#87168=CARTESIAN_POINT ( 'NONE',  ( 6.580031098407260082, -2.049997751086956921, -0.4092652541880793526 ) ) ;
#87169=CARTESIAN_POINT ( 'NONE',  ( 4.100303288188038131, -0.5556836211836749806, -1.680424235071773742 ) ) ;
#87172=CARTESIAN_POINT ( 'NONE',  ( 0.7971425760184660536, 1.793611693402120455, 1.258865353619270433 ) ) ;
#87173=CARTESIAN_POINT ( 'NONE',  ( -0.006821830062568761018, -1.739981233400577088, -0.04623622425214619219 ) ) ;
#87177=CARTESIAN_POINT ( 'NONE',  ( 0.1331715793776418189, 1.377430125279802686, -2.211494238769554865 ) ) ;
#87178=CARTESIAN_POINT ( 'NONE',  ( 0.8964060800229460835, 0.1715710081350088068, 2.292006659179766537 ) ) ;
#87179=CARTESIAN_POINT ( 'NONE',  ( 0.4334776158547505864, -1.553986563932317377, -1.545601477622601472 ) ) ;
#87180=CARTESIAN_POINT ( 'NONE',  ( 6.538463365017005202, 1.657764536579940495, -0.5080105315169358704 ) ) ;
#87181=CARTESIAN_POINT ( 'NONE',  ( 3.141465813989018141, -1.946189201368169641, 1.040519825639886431 ) ) ;
#87183=CARTESIAN_POINT ( 'NONE',  ( 0.4093307213487142326, -1.744552795675001100, 1.292164652415381365 ) ) ;
#87185=CARTESIAN_POINT ( 'NONE',  ( 1.640021805331920213, 2.111262888970814267, -0.1616085204505824935 ) ) ;
#87186=CARTESIAN_POINT ( 'NONE',  ( 3.406250000000002220, 1.895863743164009740, -0.7852924748301655100 ) ) ;
#87187=CARTESIAN_POINT ( 'NONE',  ( 6.727182134110203826, 2.399899341769623273, 2.668786705202597531 ) ) ;
#87188=CARTESIAN_POINT ( 'NONE',  ( 5.526370178063710448, 1.147270165450631207, -1.547347761420419188 ) ) ;
#87190=CARTESIAN_POINT ( 'NONE',  ( 1.576131469712481303, -1.221787821332357860, 1.939473486982680628 ) ) ;
#87195=CARTESIAN_POINT ( 'NONE',  ( 3.457896741714714395, -1.683011943829109791, -1.449823692882054482 ) ) ;
#87201=CARTESIAN_POINT ( 'NONE',  ( 1.811172873341511336, 1.158687402475454098, -1.650082692374904125 ) ) ;
#87203=CARTESIAN_POINT ( 'NONE',  ( 0.2392226684038156193, -0.1392734953599965297, -2.030321344557210139 ) ) ;
#87206=CARTESIAN_POINT ( 'NONE',  ( 6.233937787808796038, 1.722893207988238862, 0.2456954999437432341 ) ) ;
#87209=CARTESIAN_POINT ( 'NONE',  ( 0.8425835904034431056, -1.521979116790536768, 0.9028166612478020214 ) ) ;
#87210=CARTESIAN_POINT ( 'NONE',  ( 1.283827520628720187, 1.646837967535810021, -1.163270716046126196 ) ) ;
#87211=CARTESIAN_POINT ( 'NONE',  ( 0.06366010765614799061, -1.203631707120488947, 1.393476991864414760 ) ) ;
#87212=CARTESIAN_POINT ( 'NONE',  ( 5.319995955860258974, 1.367515572929053791, -1.839686415443070100 ) ) ;
#87213=CARTESIAN_POINT ( 'NONE',  ( 3.697050842446505392, -0.5329721798031424873, 1.762307204009383454 ) ) ;
#87217=CARTESIAN_POINT ( 'NONE',  ( 4.137589658204786858, -1.258905094989383189, -1.322318538811013688 ) ) ;
#87218=CARTESIAN_POINT ( 'NONE',  ( 4.975232503164924935, -2.001511053420693020, -0.2440319332882301961 ) ) ;
#87220=CARTESIAN_POINT ( 'NONE',  ( 4.012777769421401963, 1.602246665114055002, -1.597678914196493771 ) ) ;
#87222=CARTESIAN_POINT ( 'NONE',  ( 6.176810970088661534, -1.998525488361714508, -0.6642400113570454678 ) ) ;
#87224=CARTESIAN_POINT ( 'NONE',  ( 3.262232429473245432, -2.068111870375147987, 0.09887451149894616043 ) ) ;
#87227=CARTESIAN_POINT ( 'NONE',  ( 6.147156607449644206, 0.2074554230099104890, 2.110329589018632657 ) ) ;
#87230=CARTESIAN_POINT ( 'NONE',  ( 1.646969920108354524, -1.627708819445686572, 1.030247865989121880 ) ) ;
#87232=CARTESIAN_POINT ( 'NONE',  ( 6.526221542235329132, 1.009325857860805087, 1.690966299934024031 ) ) ;
#87237=CARTESIAN_POINT ( 'NONE',  ( 0.07096481000732741962, 0.8580841460674984988, 2.049194762706497031 ) ) ;
#87238=CARTESIAN_POINT ( 'NONE',  ( 3.100711275163593239, -0.6099987009138232441, -2.015686496682663087 ) ) ;
#87241=CARTESIAN_POINT ( 'NONE',  ( 0.8888279104573212352, 0.1313983060258062385, 1.856467483602406432 ) ) ;
#87247=CARTESIAN_POINT ( 'NONE',  ( 0.7562902151678205787, 0.8540304730459827853, -1.941197329821432227 ) ) ;
#87250=CARTESIAN_POINT ( 'NONE',  ( 5.002378505967388200, 1.956489882415031190, 0.1462272935644214900 ) ) ;
#87251=CARTESIAN_POINT ( 'NONE',  ( 2.430746436576446179, 2.096607243605509208, 0.5259719050795114148 ) ) ;
#87252=CARTESIAN_POINT ( 'NONE',  ( 1.645803748337611783, 0.5784278848013635344, 1.748079663633335334 ) ) ;
#87256=CARTESIAN_POINT ( 'NONE',  ( 3.556370828957751140, -1.535720284108733624, -0.8187001993567950553 ) ) ;
#87260=CARTESIAN_POINT ( 'NONE',  ( 0.2159880523044250267, -2.119658899406823505, 0.4233941889316418239 ) ) ;
#87261=CARTESIAN_POINT ( 'NONE',  ( 3.936874915731437774, 1.117662071392529377, 1.677747830363854664 ) ) ;
#87263=CARTESIAN_POINT ( 'NONE',  ( 0.4972265960483426284, 1.796464302094663346, -1.202062886709959422 ) ) ;
#87264=CARTESIAN_POINT ( 'NONE',  ( 3.450034532000289200, 1.971640592831106709, 0.001386944525654659321 ) ) ;
#87265=CARTESIAN_POINT ( 'NONE',  ( 6.609000000000005315, 2.959011640422835487, 2.552823073452652913 ) ) ;
#87266=CARTESIAN_POINT ( 'NONE',  ( 2.085399755688497336, -0.8285669363069894100, 1.756555673176816157 ) ) ;
#87275=CARTESIAN_POINT ( 'NONE',  ( 6.528381088282158906, 1.336169653064466889, -1.881230508112927025 ) ) ;
#87276=CARTESIAN_POINT ( 'NONE',  ( 6.742638286788313451, -1.923764577213080029, -0.3838556375530403630 ) ) ;
#87278=CARTESIAN_POINT ( 'NONE',  ( 3.907043859180459933, -1.606318986283063799, 1.125903821926607318 ) ) ;
#87280=CARTESIAN_POINT ( 'NONE',  ( 1.652970434142877920, 1.038994816082598804, 1.728001345923817267 ) ) ;
#87282=CARTESIAN_POINT ( 'NONE',  ( 2.782529222840863348, -0.6191273052778034636, -2.024769726974411377 ) ) ;
#87286=CARTESIAN_POINT ( 'NONE',  ( 3.292734131499192252, 1.452021927685825275, 1.131891246899892289 ) ) ;
#87290=CARTESIAN_POINT ( 'NONE',  ( 4.236665939827915395, 1.302216991916404387, -1.673619383358643908 ) ) ;
#87293=CARTESIAN_POINT ( 'NONE',  ( 5.272755944101470860, -1.938957023840400362, -0.6983732565980956819 ) ) ;
#87295=CARTESIAN_POINT ( 'NONE',  ( 2.999365392321148516, -1.839032331094083927, 0.09308366406014097205 ) ) ;
#87301=CARTESIAN_POINT ( 'NONE',  ( 2.245003380770736801, 0.4850519687749441644, 2.152760086278446394 ) ) ;
#87302=CARTESIAN_POINT ( 'NONE',  ( 3.778848203065594102, -2.179170165155080774, -0.6077416658978853636 ) ) ;
#87304=CARTESIAN_POINT ( 'NONE',  ( 3.832113882524991411, -0.9361971883012323303, -1.550792431135393334 ) ) ;
#87305=CARTESIAN_POINT ( 'NONE',  ( 4.188635153834672664, 1.476993813991718918, -1.219978962091677221 ) ) ;
#87307=CARTESIAN_POINT ( 'NONE',  ( 3.977382581243666504, 1.856787152588537548, -0.6629638669850937971 ) ) ;
#87308=CARTESIAN_POINT ( 'NONE',  ( 0.9735099972556484627, 1.857407184102148001, -0.5107058244425541904 ) ) ;
#87309=CARTESIAN_POINT ( 'NONE',  ( 4.522238337509359773, 1.150754656758418593, -1.474723989322044959 ) ) ;
#87310=CARTESIAN_POINT ( 'NONE',  ( 3.176728247877279365, -1.374524503021319344, 1.853549100471873823 ) ) ;
#87311=CARTESIAN_POINT ( 'NONE',  ( 4.369486748645814878, -0.3193033414996570007, 1.833288415851072273 ) ) ;
#87315=CARTESIAN_POINT ( 'NONE',  ( 0.3918150239524306189, -2.006371095615328226, 0.2024682584410575914 ) ) ;
#87317=CARTESIAN_POINT ( 'NONE',  ( 1.541775746491366395, -1.526411702840410722, -1.451317155924846336 ) ) ;
#87320=CARTESIAN_POINT ( 'NONE',  ( 6.591117433763723277, 1.884315261875910474, -1.059023293578951863 ) ) ;
#87321=CARTESIAN_POINT ( 'NONE',  ( 3.515986968957810266, -0.6120941298391362473, 2.030368431519948391 ) ) ;
#87323=CARTESIAN_POINT ( 'NONE',  ( 1.283469775389501910, 0.1441914389909859651, -2.014673257830889685 ) ) ;
#87328=EDGE_LOOP ( 'NONE', ( #198472, #130908, #145681, #196524 ) ) ;
#87329=CARTESIAN_POINT ( 'NONE',  ( 1.651884467337715989, 0.6291892518628816600, -2.067965918892029631 ) ) ;
#87330=CARTESIAN_POINT ( 'NONE',  ( 6.609999999999971010, 7.629137130509032971, 2.319999999999996287 ) ) ;
#87335=CARTESIAN_POINT ( 'NONE',  ( 5.507046092540283766, -0.04465857163906890998, 2.016188657829049991 ) ) ;
#87338=CARTESIAN_POINT ( 'NONE',  ( 0.3280006606478855224, 1.121390616443746602, -1.882787531365101685 ) ) ;
#87340=CARTESIAN_POINT ( 'NONE',  ( 6.807524309086420367, -0.4794501827766698421, 2.115671360755105646 ) ) ;
#87343=CARTESIAN_POINT ( 'NONE',  ( 4.346888830327386266, -1.803415170841724979, -0.9023466997552240798 ) ) ;
#87349=CARTESIAN_POINT ( 'NONE',  ( 3.650762458506318087, -1.408968171862119423, 0.9946885059901353632 ) ) ;
#87351=CARTESIAN_POINT ( 'NONE',  ( 1.897346677678591442, -0.6019946308016431713, 1.664328231202655273 ) ) ;
#87353=CARTESIAN_POINT ( 'NONE',  ( 5.456176519787153012, 2.204477245749701719, -0.1032804940204190558 ) ) ;
#87355=CARTESIAN_POINT ( 'NONE',  ( 4.535418805095452477, -0.09482428102505417733, 2.017666594091566346 ) ) ;
#87357=CARTESIAN_POINT ( 'NONE',  ( 3.949941927655271190, -1.463281269271698770, -1.534908012577620440 ) ) ;
#87358=CARTESIAN_POINT ( 'NONE',  ( 3.937125189161301719, -1.678018027730580286, -1.117815418662113203 ) ) ;
#87362=CARTESIAN_POINT ( 'NONE',  ( 0.9713206009373563932, 1.803875226702996049, -0.4951341686536685494 ) ) ;
#87365=CARTESIAN_POINT ( 'NONE',  ( 5.707607943424125807, 1.375951858612366019, 1.178334608346263579 ) ) ;
#87372=CARTESIAN_POINT ( 'NONE',  ( 1.908577322519442454, 0.6123880975643315461, 1.863924812142327525 ) ) ;
#87375=CARTESIAN_POINT ( 'NONE',  ( 3.849942018323779358, -1.464806807754112539, -1.533599281611098597 ) ) ;
#87376=CARTESIAN_POINT ( 'NONE',  ( -0.02948999725180690215, 0.001137248348246927814, -1.926291057026579656 ) ) ;
#87379=CARTESIAN_POINT ( 'NONE',  ( 6.046159394557358624, 1.968988722785993462, 0.09938198387684710200 ) ) ;
#87381=CARTESIAN_POINT ( 'NONE',  ( 1.177990849177086075, 1.982702329297232113, -0.3483419944294365300 ) ) ;
#87383=CARTESIAN_POINT ( 'NONE',  ( 0.7907972306774737614, 1.600388572762038830, -1.386229290198564001 ) ) ;
#87385=CARTESIAN_POINT ( 'NONE',  ( 2.717306809760032138, -1.800131872397674471, -1.022606600864908399 ) ) ;
#87389=ORIENTED_EDGE ( 'NONE', *, *, #87162, .T. ) ;
#87390=CARTESIAN_POINT ( 'NONE',  ( 5.033190428309433528, -1.478027449723118725, -1.478843810762977995 ) ) ;
#87392=CARTESIAN_POINT ( 'NONE',  ( 2.748829393344632166, -1.518919317350690967, 1.012417160375630898 ) ) ;
#87393=CARTESIAN_POINT ( 'NONE',  ( 1.998415993447474559, -1.776625121221590220, -0.3526093829155519388 ) ) ;
#87395=CARTESIAN_POINT ( 'NONE',  ( 6.568967528192747984, -2.015767819289843388, -0.8987472251835016968 ) ) ;
#87397=CARTESIAN_POINT ( 'NONE',  ( 4.506973327934083784, 1.708129512224244806, -1.397202154207459524 ) ) ;
#87401=CARTESIAN_POINT ( 'NONE',  ( 3.334525359879161766, 1.211162569113528598, -1.479845612687477496 ) ) ;
#87405=CARTESIAN_POINT ( 'NONE',  ( 6.877413708759195998, -0.1538780216673047430, 2.036608477593480959 ) ) ;
#87408=CARTESIAN_POINT ( 'NONE',  ( 6.040607902356621928, -1.852314659301615096, 1.170993205287726990 ) ) ;
#87414=CARTESIAN_POINT ( 'NONE',  ( 3.145614842782416432, 0.6765965015090926737, -1.744060075730607950 ) ) ;
#87419=CARTESIAN_POINT ( 'NONE',  ( 0.5144232481557647896, 0.7485027850700550767, 1.821871385004094845 ) ) ;
#87420=CARTESIAN_POINT ( 'NONE',  ( 1.616814774554303780, 0.2004563524992293566, 2.006445175307514095 ) ) ;
#87423=CARTESIAN_POINT ( 'NONE',  ( -0.07900062026858570285, 7.629137130509076492, -2.773896239169175271 ) ) ;
#87424=CARTESIAN_POINT ( 'NONE',  ( 1.904481915951491189, 1.622449043516610123, -1.473309109067892697 ) ) ;
#87425=CARTESIAN_POINT ( 'NONE',  ( 6.498675964634617941, -0.4922777150685350156, -1.758009983081544991 ) ) ;
#87432=CARTESIAN_POINT ( 'NONE',  ( 3.737712173649463399, 1.832726675769575486, 0.1767833568970395008 ) ) ;
#87433=CARTESIAN_POINT ( 'NONE',  ( 0.3111896917125516748, 1.672494819392616128, -1.120119447130196288 ) ) ;
#87434=CARTESIAN_POINT ( 'NONE',  ( 2.249760294480507294, -2.253934603285558502, -0.4491563171437322199 ) ) ;
#87436=CARTESIAN_POINT ( 'NONE',  ( 6.526224699197019419, 1.005635830909179074, 1.684226478273798788 ) ) ;
#87439=CARTESIAN_POINT ( 'NONE',  ( 4.746305163667582150, 0.9781546018433548983, -1.643150005489722787 ) ) ;
#87443=CARTESIAN_POINT ( 'NONE',  ( 2.560199545759346496, -1.439800679921798165, 1.516228354532923372 ) ) ;
#87444=CARTESIAN_POINT ( 'NONE',  ( 1.182252951876180180, -1.824241171369020531, -0.4133900166373091767 ) ) ;
#87445=CARTESIAN_POINT ( 'NONE',  ( 2.196638537759632470, -1.314794530490107638, -1.528507974810841219 ) ) ;
#87449=CARTESIAN_POINT ( 'NONE',  ( 2.858654643706417975, 0.2527927160936989659, -1.721832920378673748 ) ) ;
#87454=CARTESIAN_POINT ( 'NONE',  ( 4.459404883141235842, 0.3742951803532655330, -1.683599696842478677 ) ) ;
#87455=CARTESIAN_POINT ( 'NONE',  ( 3.685266855566126321, 1.588411730319793769, 1.510178839762461811 ) ) ;
#87457=CARTESIAN_POINT ( 'NONE',  ( 3.959984535978885667, -0.6353779353734061441, 2.075986281735443750 ) ) ;
#87458=CARTESIAN_POINT ( 'NONE',  ( 1.646812808029130215, -1.543121136568927243, 0.9753659028155501343 ) ) ;
#87459=CARTESIAN_POINT ( 'NONE',  ( 0.3034670832338138835, -1.512625156342655819, -1.248876549296701333 ) ) ;
#87460=CARTESIAN_POINT ( 'NONE',  ( 3.995394017595743641, -0.3581701549109669869, 2.086669383214428297 ) ) ;
#87462=CARTESIAN_POINT ( 'NONE',  ( 5.126663105998436443, 0.1666055143465100530, 2.286395203598155845 ) ) ;
#87464=CARTESIAN_POINT ( 'NONE',  ( 6.620655732516649294, 0.5971256128398574337, 1.879834161342401666 ) ) ;
#87467=CARTESIAN_POINT ( 'NONE',  ( 0.3289748556246673838, 1.459166701075472750, -1.538843095060193233 ) ) ;
#87475=CARTESIAN_POINT ( 'NONE',  ( 5.397111353752316987, -0.9091427841607623295, -1.799923777076550824 ) ) ;
#87477=CARTESIAN_POINT ( 'NONE',  ( 4.241124981676721362, -0.1973008666005781619, -2.053083420615212429 ) ) ;
#87479=CARTESIAN_POINT ( 'NONE',  ( -0.1408020194049964258, 1.331054986036240173, -2.350941690117592575 ) ) ;
#87483=CARTESIAN_POINT ( 'NONE',  ( 0.1114262914704557683, -2.049844763593706265, 0.4100319678014376912 ) ) ;
#87484=CARTESIAN_POINT ( 'NONE',  ( 4.764296165657141202, 1.880435471729305030, -0.7283773170061805802 ) ) ;
#87485=CARTESIAN_POINT ( 'NONE',  ( 3.386116603743833497, -0.3623624896987759914, -1.805063595765175499 ) ) ;
#87488=CARTESIAN_POINT ( 'NONE',  ( 0.2172357734837098431, -1.693002290532450882, 0.3285655886510214230 ) ) ;
#87490=DIRECTION ( 'NONE',  ( 1.214306433183764966E-17, 1.000000000000000000, 5.200009205990155575E-32 ) ) ;
#87491=CARTESIAN_POINT ( 'NONE',  ( 0.5987520574620349700, -0.3298207119002970478, 2.274815185769126114 ) ) ;
#87493=CARTESIAN_POINT ( 'NONE',  ( 0.2458944382301266607, -1.750094391731635168, -1.433289930825008218 ) ) ;
#87494=CARTESIAN_POINT ( 'NONE',  ( 3.422586708326117666, 1.336063110485498973, -1.628023012543792447 ) ) ;
#87498=CARTESIAN_POINT ( 'NONE',  ( 6.500000003069670740, 7.552736074387352678E-08, -2.052068128417939175 ) ) ;
#87505=CARTESIAN_POINT ( 'NONE',  ( 3.463320643641348173, -1.814240386431978713, 1.281607931980492054 ) ) ;
#87506=CARTESIAN_POINT ( 'NONE',  ( 2.888834398507355239, 1.879202789969806497, -1.127179367409691935 ) ) ;
#87509=CARTESIAN_POINT ( 'NONE',  ( 5.582460749670235423, 1.169929261559121247, -1.574690175210855747 ) ) ;
#87511=CARTESIAN_POINT ( 'NONE',  ( 6.610000000000003872, 7.053606217926155608, 2.318153411789238838 ) ) ;
#87513=CARTESIAN_POINT ( 'NONE',  ( 4.939744792934912532, -2.012803497507458683, 0.6676120485993168874 ) ) ;
#87515=ORIENTED_EDGE ( 'NONE', *, *, #16285, .T. ) ;
#87517=CARTESIAN_POINT ( 'NONE',  ( 5.629794960336353071, -1.368038101806166029, -1.673757646710342550 ) ) ;
#87519=CARTESIAN_POINT ( 'NONE',  ( 5.460457653299121361, -1.667157065227730106, -0.7818181906407914994 ) ) ;
#87522=CARTESIAN_POINT ( 'NONE',  ( 0.09860955243249854008, -0.4675299588126168859, 1.676413046982327515 ) ) ;
#87526=CARTESIAN_POINT ( 'NONE',  ( 4.293933718354110418, -0.8299404887524584051, 1.996233173270183681 ) ) ;
#87529=CARTESIAN_POINT ( 'NONE',  ( 3.766626874709140704, -1.453462046928340579, 1.600284095077113333 ) ) ;
#87530=CARTESIAN_POINT ( 'NONE',  ( 4.622318808457460015, 1.215050846432633946, -1.552280729921464708 ) ) ;
#87531=CARTESIAN_POINT ( 'NONE',  ( 4.200348813226637112, -1.195399808894830773, -1.256130793262473455 ) ) ;
#87532=CARTESIAN_POINT ( 'NONE',  ( 0.5038066827526345159, -2.180447833630628107, 0.2205874978757973448 ) ) ;
#87533=CARTESIAN_POINT ( 'NONE',  ( 1.905729856612170758, 1.919199136376721793, 1.280985070478329435 ) ) ;
#87534=CARTESIAN_POINT ( 'NONE',  ( 4.130192093715317370, 1.105610312200686174, -1.738907380658259560 ) ) ;
#87535=CARTESIAN_POINT ( 'NONE',  ( 5.407742453289367646, -0.8769457196468108950, -1.732881886176732777 ) ) ;
#87540=CARTESIAN_POINT ( 'NONE',  ( 3.680891063843365174, -2.126115503207156809, -0.5908918699835326027 ) ) ;
#87543=CARTESIAN_POINT ( 'NONE',  ( 0.2388273096324589895, -0.1346187373043924163, -1.830540737478093982 ) ) ;
#87544=CARTESIAN_POINT ( 'NONE',  ( -0.02900071798685523866, 4.082342745036794618, -2.728474045032194262 ) ) ;
#87548=CARTESIAN_POINT ( 'NONE',  ( 6.925078400183519278, 1.259550266093687920, 2.159391284976417857 ) ) ;
#87551=CARTESIAN_POINT ( 'NONE',  ( 3.309499033229778231, -0.4035708669713148899, 2.020805850887919863 ) ) ;
#87554=CARTESIAN_POINT ( 'NONE',  ( 0.07680821025393690105, 0.005952109439256307241, -1.810863387344714193 ) ) ;
#87557=CARTESIAN_POINT ( 'NONE',  ( 1.534131747024346737, 1.016495879925772616, -1.792692027746685346 ) ) ;
#87562=CARTESIAN_POINT ( 'NONE',  ( -0.2409995289980003397, 2.873648158547074338, -2.488896373646624749 ) ) ;
#87563=CARTESIAN_POINT ( 'NONE',  ( 5.602238545945851023, -2.207063162045197924, -0.003355105161521875021 ) ) ;
#87564=CARTESIAN_POINT ( 'NONE',  ( 6.626273523942327159, 1.310778252226969975, -1.843845376178480322 ) ) ;
#87566=CARTESIAN_POINT ( 'NONE',  ( 0.2863426850727782136, -0.6839425765656822476, -1.897108587135355684 ) ) ;
#87567=CARTESIAN_POINT ( 'NONE',  ( 1.511505665106587459, 2.295766583369537095, 0.1122837871174054425 ) ) ;
#87571=CARTESIAN_POINT ( 'NONE',  ( 2.307302758404996545, -0.4121581357655336175, 1.824517092411604979 ) ) ;
#87572=CARTESIAN_POINT ( 'NONE',  ( 3.221888912838869690, 0.9023448338944944913, -1.803416113280359445 ) ) ;
#87574=CARTESIAN_POINT ( 'NONE',  ( 6.639320575229281651, -0.0007625845807879281287, 2.103388539994067497 ) ) ;
#87576=CARTESIAN_POINT ( 'NONE',  ( 5.426436078920066741, 1.255580583125959437, -1.690716914145540040 ) ) ;
#87581=CARTESIAN_POINT ( 'NONE',  ( 4.394789018838915595, -1.960137222954833502, -0.4867870608649630393 ) ) ;
#87583=CARTESIAN_POINT ( 'NONE',  ( 0.9364711893796459075, -1.149011738537804250, 1.712694122252313100 ) ) ;
#87585=CARTESIAN_POINT ( 'NONE',  ( 5.448557382023540896, 0.6217387762853660016, 2.070273951448368788 ) ) ;
#87589=CARTESIAN_POINT ( 'NONE',  ( -0.1108833634136767443, 0.0002062650063822807356, -1.896853557917008271 ) ) ;
#87591=CARTESIAN_POINT ( 'NONE',  ( 3.121698260611803999, 0.3212384671735257213, -2.147181447086630612 ) ) ;
#87594=CARTESIAN_POINT ( 'NONE',  ( 2.102840161960460197, -0.4018910908503615653, 1.796694178532439956 ) ) ;
#87597=CARTESIAN_POINT ( 'NONE',  ( 3.456733517523991051, -1.933646301634945885, -1.031433503814835007 ) ) ;
#87598=CARTESIAN_POINT ( 'NONE',  ( 6.983263157960368339, 1.232032666090671302, 2.265420076015733031 ) ) ;
#87599=CARTESIAN_POINT ( 'NONE',  ( 4.329186484417943959, 0.1072846252610352574, 2.260086081085868948 ) ) ;
#87606=CARTESIAN_POINT ( 'NONE',  ( 5.694547528447587048, -0.4312477495709844399, -1.716266690248748672 ) ) ;
#87608=CARTESIAN_POINT ( 'NONE',  ( 1.606614413041591360, -0.7575671727712609549, -1.965171518483445068 ) ) ;
#87610=CARTESIAN_POINT ( 'NONE',  ( 1.908593538011025492, 0.6150006609981206740, 1.871157805954210440 ) ) ;
#87612=CARTESIAN_POINT ( 'NONE',  ( 0.3265133270617843197, -1.284392789319420913, 1.483054880892266114 ) ) ;
#87613=CARTESIAN_POINT ( 'NONE',  ( 5.748286673958676651, 0.8850744635948673000, -1.580567631948928797 ) ) ;
#87617=CARTESIAN_POINT ( 'NONE',  ( 4.768341783539651324, -1.221614081569386112, 1.416756073533788518 ) ) ;
#87618=CARTESIAN_POINT ( 'NONE',  ( 5.207906454484914072, 0.6546344234062730916, -1.964071172066352400 ) ) ;
#87629=CARTESIAN_POINT ( 'NONE',  ( 4.826587731031282580, -1.282962940432516907, 1.484285152025546672 ) ) ;
#87631=CARTESIAN_POINT ( 'NONE',  ( 2.917342117414220670, 0.6766092434087739305, 1.899328150365031664 ) ) ;
#87632=CARTESIAN_POINT ( 'NONE',  ( 2.641684811942858424, 1.906066497734011378, -0.1923337340370822046 ) ) ;
#87635=CARTESIAN_POINT ( 'NONE',  ( 0.5740950506661415265, -1.212703583203307511, 1.825263377225619266 ) ) ;
#87637=CARTESIAN_POINT ( 'NONE',  ( 2.618241971997347317, 1.224968108320439342, -1.413705424714882586 ) ) ;
#87639=CARTESIAN_POINT ( 'NONE',  ( 4.060795210881157580, 0.5408870827437872730, 1.939095388008914345 ) ) ;
#87642=CARTESIAN_POINT ( 'NONE',  ( 4.991875679739185223, -2.106924267290931851, 0.2088435281543659927 ) ) ;
#87645=CARTESIAN_POINT ( 'NONE',  ( 6.215297738502283842, -1.773692237561547147, -1.067698627785176768 ) ) ;
#87646=CARTESIAN_POINT ( 'NONE',  ( 1.347338520094189862, 0.6037249722931283813, -2.001697839036377324 ) ) ;
#87648=CARTESIAN_POINT ( 'NONE',  ( 6.704125975539116489, -1.825092170400946845, 0.04854515157103055090 ) ) ;
#87651=AXIS2_PLACEMENT_3D ( 'NONE', #159662, #178055, #110977 ) ;
#87656=CARTESIAN_POINT ( 'NONE',  ( 0.08225775502835978858, -1.185065876811146834, 1.370160863432666076 ) ) ;
#87663=CARTESIAN_POINT ( 'NONE',  ( 6.345327396762703742, 0.3419173589993273477, -1.987050850726256979 ) ) ;
#87664=CARTESIAN_POINT ( 'NONE',  ( 0.1707708301344288415, 0.8156354886642532831, 1.957547177562010354 ) ) ;
#87668=CARTESIAN_POINT ( 'NONE',  ( 3.485164662121999601, 0.04367138265829079852, 1.969119211374547707 ) ) ;
#87669=CARTESIAN_POINT ( 'NONE',  ( 4.482046101484723266, -2.016035353076811809, -0.04666016718203602753 ) ) ;
#87672=CARTESIAN_POINT ( 'NONE',  ( 5.332042502257137606, 2.158596015244533373, 0.3771327725019049670 ) ) ;
#87674=CARTESIAN_POINT ( 'NONE',  ( 2.661056112795460837, -1.675086148048400503, -0.9512456543366625272 ) ) ;
#87676=CARTESIAN_POINT ( 'NONE',  ( -0.1298852118744100725, 0.003815113116375101580, -1.726395881205537330 ) ) ;
#87677=CARTESIAN_POINT ( 'NONE',  ( 0.3466626200071438735, 2.201290530325435757, 0.1579762268871589825 ) ) ;
#87680=CARTESIAN_POINT ( 'NONE',  ( 4.750814831274846384, -0.4274863908861815665, -1.922328355476431216 ) ) ;
#87681=CARTESIAN_POINT ( 'NONE',  ( 0.06387186515662347797, -1.267698835582967476, 1.471343342715900615 ) ) ;
#87682=CARTESIAN_POINT ( 'NONE',  ( 3.844392992367959838, 1.075074360472785928, -1.701806764060603161 ) ) ;
#87683=CARTESIAN_POINT ( 'NONE',  ( 5.167441833834662823, -0.7673274391166631236, -2.166651051963175423 ) ) ;
#87684=CARTESIAN_POINT ( 'NONE',  ( 3.203785720953303606, 0.6742969627455961401, -1.734658892920079243 ) ) ;
#87690=CARTESIAN_POINT ( 'NONE',  ( 6.163634092203726489, 1.075319730316869560, 1.792882302630414593 ) ) ;
#87695=CARTESIAN_POINT ( 'NONE',  ( 0.7854531640391904102, 1.224056292049885419, 1.354719642434290439 ) ) ;
#87698=CARTESIAN_POINT ( 'NONE',  ( 2.302961303058923992, 1.131868135402936737, -1.313931383173136513 ) ) ;
#87703=CARTESIAN_POINT ( 'NONE',  ( 6.977413708759169886, -0.1587332643391472231, 2.136494379638858909 ) ) ;
#87705=CARTESIAN_POINT ( 'NONE',  ( 5.865807274569020180, 1.797851641234180509, -0.3166982042408575948 ) ) ;
#87706=CARTESIAN_POINT ( 'NONE',  ( 3.520314338623427020, 0.8779579967637550775, 1.754372790864023646 ) ) ;
#87711=CARTESIAN_POINT ( 'NONE',  ( 4.055424778641623540, -1.844328037693225397, 1.046277804987456372 ) ) ;
#87712=CARTESIAN_POINT ( 'NONE',  ( 6.827182134110222123, 4.687887262399931920, 2.751577338787388083 ) ) ;
#87715=CARTESIAN_POINT ( 'NONE',  ( 2.272408084759574454, -0.9721198248324285363, -1.827787434591138238 ) ) ;
#87717=CARTESIAN_POINT ( 'NONE',  ( 5.057398377711723292, -1.905748072847958108, 1.140992067822230505 ) ) ;
#87719=CARTESIAN_POINT ( 'NONE',  ( 1.934640009471942035, -1.849324232932574530, -1.365145410983016117 ) ) ;
#87727=CARTESIAN_POINT ( 'NONE',  ( 2.636851627972558454, 1.802111047976437508, 0.6404684511054498097 ) ) ;
#87729=CARTESIAN_POINT ( 'NONE',  ( 4.471539400256457242, 1.672567520934200136, -0.4206060815013599741 ) ) ;
#87730=CARTESIAN_POINT ( 'NONE',  ( 2.342982756445275427, -1.756855002775299379, -0.9896843009072552322 ) ) ;
#87731=CARTESIAN_POINT ( 'NONE',  ( 4.166792231569245608, 1.501215554499458982, 1.740835934941728169 ) ) ;
#87732=CARTESIAN_POINT ( 'NONE',  ( 3.356942810317259163, -1.715728140842260441, 1.474839417774987060 ) ) ;
#87733=CARTESIAN_POINT ( 'NONE',  ( 5.848290838822029158, 2.103586024953810085, 0.1047431163101186502 ) ) ;
#87735=CARTESIAN_POINT ( 'NONE',  ( 4.411239408862893008, -0.3036837672792407905, 1.743313046103856179 ) ) ;
#87737=CARTESIAN_POINT ( 'NONE',  ( 0.9906304909971673789, -0.5616109214932778482, -2.222291424677411698 ) ) ;
#87738=CARTESIAN_POINT ( 'NONE',  ( 6.193280126971262511, -0.6156851667328180344, 1.735278506779000640 ) ) ;
#87740=CARTESIAN_POINT ( 'NONE',  ( 5.666036703420031628, -1.392593631063457682, 1.692088878451535106 ) ) ;
#87744=CARTESIAN_POINT ( 'NONE',  ( 5.547352688424546763, 1.827615396715172258, -0.9727077141251788683 ) ) ;
#87745=CARTESIAN_POINT ( 'NONE',  ( 1.622280145275534435, 1.995268681201247452, 0.2910785328335343536 ) ) ;
#87747=CARTESIAN_POINT ( 'NONE',  ( 4.037660154168158932, -1.329308714249255452, -1.394617731102282709 ) ) ;
#87749=CARTESIAN_POINT ( 'NONE',  ( 1.547463978342083157, 0.2240547868478468541, 2.210115929984892258 ) ) ;
#87758=DIRECTION ( 'NONE',  ( 2.949029909160572061E-17, 1.000000000000000000, -8.673600428462541149E-15 ) ) ;
#87759=CARTESIAN_POINT ( 'NONE',  ( 4.581465296696157097, -0.8148697087324536792, 1.537882137665383064 ) ) ;
#87760=CARTESIAN_POINT ( 'NONE',  ( 2.066782613880484565, 1.455849762852476248, -1.315278764014264912 ) ) ;
#87765=CARTESIAN_POINT ( 'NONE',  ( 6.707479306934847507, -1.574971382793718178, -1.169550641929931079 ) ) ;
#87768=CARTESIAN_POINT ( 'NONE',  ( 5.243375144629232487, 0.3886363430659239837, -1.978554426619572926 ) ) ;
#87769=CARTESIAN_POINT ( 'NONE',  ( 1.657462679512666348, -1.941143012291703940, -1.162103002166763988 ) ) ;
#87774=CARTESIAN_POINT ( 'NONE',  ( 1.422894040683621464, -0.05142188859055819850, 1.870020055627517497 ) ) ;
#87775=CARTESIAN_POINT ( 'NONE',  ( 0.4922575064417636925, -1.726078246012904938, 0.1672019070194027679 ) ) ;
#87778=CARTESIAN_POINT ( 'NONE',  ( 4.476244563333130699, -2.125884358948509689, -0.5320566845071761364 ) ) ;
#87779=CARTESIAN_POINT ( 'NONE',  ( 6.036188935239226616, 1.144513723677667461, -2.003705632283636184 ) ) ;
#87780=CARTESIAN_POINT ( 'NONE',  ( 0.07516593201271813685, 0.0004601587237540622779, -2.044269526395313452 ) ) ;
#87781=CARTESIAN_POINT ( 'NONE',  ( 2.941277052067638120, 0.6983745205926906729, -1.812199837690719129 ) ) ;
#87787=CARTESIAN_POINT ( 'NONE',  ( 3.059220373557011818, -1.198860207862334049, 1.621182619130703051 ) ) ;
#87791=CARTESIAN_POINT ( 'NONE',  ( 1.154616158753757338, -1.440623569337009968, 1.121372061650728558 ) ) ;
#87797=CARTESIAN_POINT ( 'NONE',  ( 0.2511322555047851290, -1.735185354305257110, 1.289038484408123963 ) ) ;
#87803=CARTESIAN_POINT ( 'NONE',  ( 5.391273274344085209, -0.05166147132495273880, -2.019192591660509351 ) ) ;
#87804=CARTESIAN_POINT ( 'NONE',  ( 5.883471028171038952, 0.1659795297097066691, -2.215133764073994982 ) ) ;
#87808=CARTESIAN_POINT ( 'NONE',  ( 5.612203307022772591, -0.9243832361092527705, -1.842014774801424615 ) ) ;
#87809=CARTESIAN_POINT ( 'NONE',  ( 3.639296212489909532, 0.7283784247123015199, 1.880435045658496618 ) ) ;
#87817=CARTESIAN_POINT ( 'NONE',  ( 3.655624903986275154, -0.3905385215352343287, -1.977747697055858955 ) ) ;
#87818=CARTESIAN_POINT ( 'NONE',  ( 3.187279605439637287, -0.7454021820463945236, 1.683677988101241141 ) ) ;
#87820=CARTESIAN_POINT ( 'NONE',  ( 2.227567673948157800, 0.002208658356158287820, 2.307868969919598889 ) ) ;
#87822=CARTESIAN_POINT ( 'NONE',  ( 3.374459016379764087, -1.290570702369205014, 1.733878788530068160 ) ) ;
#87824=CARTESIAN_POINT ( 'NONE',  ( 6.620655732516645742, 0.007553340620044741646, 1.826407896915737794 ) ) ;
#87825=CARTESIAN_POINT ( 'NONE',  ( 2.712125330650519750, 1.116209241849321465, -1.679223868463100011 ) ) ;
#87827=CARTESIAN_POINT ( 'NONE',  ( 3.005512134316370432, 2.280722703800378337, 0.2841129622813722277 ) ) ;
#87830=CARTESIAN_POINT ( 'NONE',  ( 2.360033908006432757, 0.7977434165707707470, 1.692156362554583460 ) ) ;
#87831=CARTESIAN_POINT ( 'NONE',  ( 0.5617156953909893113, 1.950523934018918659, -0.2849811346736507156 ) ) ;
#87834=CARTESIAN_POINT ( 'NONE',  ( 2.157103830005083100, -1.704838622333640030, 1.401371054633032909 ) ) ;
#87840=CARTESIAN_POINT ( 'NONE',  ( 6.420779677996255153, 1.839401344301737184, 0.7098503129845078474 ) ) ;
#87841=CARTESIAN_POINT ( 'NONE',  ( 6.164718480307596060, -1.636601974411681981, 1.627217620858178337 ) ) ;
#87842=CARTESIAN_POINT ( 'NONE',  ( 6.877413160773132361, -0.1400689347856296230, 1.829862831089356545 ) ) ;
#87843=CARTESIAN_POINT ( 'NONE',  ( 3.661030488878083577, 1.629037084659604728, -1.265030972029494993 ) ) ;
#87850=CARTESIAN_POINT ( 'NONE',  ( 6.180164126497881938, -1.200935631872475540, -1.808625420649534021 ) ) ;
#87851=CARTESIAN_POINT ( 'NONE',  ( 6.639320575229252341, 0.005161017367553630275, 1.896863882003448021 ) ) ;
#87852=CARTESIAN_POINT ( 'NONE',  ( 5.214338956685347526, 1.703448749313410282, 0.6994016148276983591 ) ) ;
#87855=CARTESIAN_POINT ( 'NONE',  ( 6.532779862045914321, -1.958661757936002612, 0.9833580883553474372 ) ) ;
#87856=CARTESIAN_POINT ( 'NONE',  ( 0.7197278698120104234, -0.9953326032119573785, -1.583558375183778288 ) ) ;
#87861=CARTESIAN_POINT ( 'NONE',  ( 1.990718100289643244, 1.541686266772484437, -0.8690610084590517648 ) ) ;
#87862=CARTESIAN_POINT ( 'NONE',  ( 0.1527893875182678718, 0.3269112364552365091, 1.883972597190447518 ) ) ;
#87864=CARTESIAN_POINT ( 'NONE',  ( 4.042530882030176187, -1.416877165883747125, 1.289359272694647451 ) ) ;
#87866=CARTESIAN_POINT ( 'NONE',  ( 5.828554260932977904, -1.250890888562717684, 1.521285551415082482 ) ) ;
#87867=CARTESIAN_POINT ( 'NONE',  ( 0.01804983835817890528, -0.5593552815991027494, 2.045460531183339814 ) ) ;
#87869=CARTESIAN_POINT ( 'NONE',  ( 2.307302758404996545, -0.4121581357655336175, 1.824517092411604979 ) ) ;
#87870=CARTESIAN_POINT ( 'NONE',  ( 6.287718881003963034, 1.195215413365672275, 1.243919913892058693 ) ) ;
#87871=VERTEX_POINT ( 'NONE', #117805 ) ;
#87872=CARTESIAN_POINT ( 'NONE',  ( 3.176612885197922953, -1.314426786483071208, 1.772596291930063739 ) ) ;
#87875=CARTESIAN_POINT ( 'NONE',  ( 1.205618545266523567, -1.624909386276121692, -1.270427818644123796 ) ) ;
#87882=CARTESIAN_POINT ( 'NONE',  ( 2.998552181135270001, 2.054425100943928051, 0.2560010573490826835 ) ) ;
#87886=CARTESIAN_POINT ( 'NONE',  ( 0.9264325174072656210, -0.9100096784926974269, -1.803132658094412477 ) ) ;
#87890=CARTESIAN_POINT ( 'NONE',  ( 0.1749903794560644099, 4.092791488633133135, -2.510332109122221045 ) ) ;
#87892=CARTESIAN_POINT ( 'NONE',  ( 6.151720201709268920, -0.2930281871833945173, -1.994563951915592881 ) ) ;
#87893=CARTESIAN_POINT ( 'NONE',  ( 5.542171544414384421, 0.7827158775690710169, 1.748735243013665785 ) ) ;
#87894=CARTESIAN_POINT ( 'NONE',  ( 6.539320575229276677, 2.966918982532817051, 2.456386401752636672 ) ) ;
#87895=CARTESIAN_POINT ( 'NONE',  ( 3.843468145482429321, 0.7371271433744167600, -2.064019554291535830 ) ) ;
#87897=CARTESIAN_POINT ( 'NONE',  ( 2.724755696555291262, 1.382288352666941389, -1.321784923088549446 ) ) ;
#87901=CARTESIAN_POINT ( 'NONE',  ( 1.142204091441896718, 0.8197918422115093584, 1.842440257734210274 ) ) ;
#87903=CARTESIAN_POINT ( 'NONE',  ( 6.040607902356621928, -1.852314659301615096, 1.170993205287726990 ) ) ;
#87905=CARTESIAN_POINT ( 'NONE',  ( 2.520142033498268486, 1.128878695625197492, -1.304093658461308980 ) ) ;
#87907=CARTESIAN_POINT ( 'NONE',  ( -0.1405533004718312329, 2.055874972810427526, -2.136773944524199109 ) ) ;
#87910=CARTESIAN_POINT ( 'NONE',  ( 0.8362905744919849615, -1.092891352686057527, 1.629061181365853539 ) ) ;
#87916=CARTESIAN_POINT ( 'NONE',  ( 4.424329001689049079, -0.7786147893445326540, -1.635752125832173220 ) ) ;
#87920=CARTESIAN_POINT ( 'NONE',  ( 5.162699569786796339, 0.5314807639728249544, 1.731738579618222973 ) ) ;
#87924=CARTESIAN_POINT ( 'NONE',  ( 5.072628826387419743, 1.283713728693743894, -1.347665127999774448 ) ) ;
#87926=B_SPLINE_CURVE_WITH_KNOTS ( 'NONE', 3,
 ( #8409, #173073, #187161, #24654, #206610, #42016, #108125, #174152, #91835, #9485, #75558 ),
 .UNSPECIFIED., .F., .F.,
 ( 4, 1, 1, 1, 1, 1, 1, 1, 4 ),
 ( 0.000000000000000000, 0.2256777920876190668, 0.3978457394851813711, 0.5256768607792676740, 0.6183602023682204241, 0.6850295134299612121, 0.7345374503969632762, 0.7752450576501028756, 1.000000000000000000 ),
 .UNSPECIFIED. ) ;
#87927=CARTESIAN_POINT ( 'NONE',  ( 3.075699878008768096, -0.7735687425090407299, 1.752645402151173926 ) ) ;
#87932=CARTESIAN_POINT ( 'NONE',  ( 6.925078400183575233, 4.688909937558557672, 2.706876980850602354 ) ) ;
#87937=CARTESIAN_POINT ( 'NONE',  ( 1.043050037176814326, -1.649054093272810606, -1.284947313888247900 ) ) ;
#87939=CARTESIAN_POINT ( 'NONE',  ( 6.528350403681292491, 1.108413491673976736, -1.575378176345716419 ) ) ;
#87941=CARTESIAN_POINT ( 'NONE',  ( 2.028078973712159172, 1.053637016394028292, -1.490636434207486483 ) ) ;
#87943=CARTESIAN_POINT ( 'NONE',  ( 1.845825534506392085, -1.251752223804462272, -1.445855903880132631 ) ) ;
#87944=CARTESIAN_POINT ( 'NONE',  ( 1.873436276770530595, -0.2440693053713405281, 1.954313301998261920 ) ) ;
#87945=CARTESIAN_POINT ( 'NONE',  ( 4.001460698126992455, -1.936627024540507946, 0.1462448094460607750 ) ) ;
#87950=CARTESIAN_POINT ( 'NONE',  ( 3.885109016898561585, -1.979880364965879380, -0.7601140796509860964 ) ) ;
#87958=CARTESIAN_POINT ( 'NONE',  ( 3.562960707638890501, -1.610701098693729350, -0.8595150645765645692 ) ) ;
#87962=CARTESIAN_POINT ( 'NONE',  ( 6.589320575229281829, 7.629137130509070275, 2.703262396134015866 ) ) ;
#87963=CARTESIAN_POINT ( 'NONE',  ( 4.750782166719051069, -1.502237938222051650, 1.114538048626475986 ) ) ;
#87965=CARTESIAN_POINT ( 'NONE',  ( 1.664548039484465614, -1.362698257634049614, 1.362033803609383531 ) ) ;
#87966=CARTESIAN_POINT ( 'NONE',  ( 6.719590461409528537, 0.3385411321301828869, -1.932175811092277096 ) ) ;
#87973=CARTESIAN_POINT ( 'NONE',  ( 0.7907972306774737614, 1.600388572762038830, -1.386229290198564001 ) ) ;
#87976=CARTESIAN_POINT ( 'NONE',  ( 5.190316231837919680, 1.068962568377257671, -1.772817291931286787 ) ) ;
#87977=CARTESIAN_POINT ( 'NONE',  ( 0.6261898170028465938, 0.1349980957352381883, 1.836376839866371569 ) ) ;
#87979=EDGE_LOOP ( 'NONE', ( #208335, #53174 ) ) ;
#87980=CARTESIAN_POINT ( 'NONE',  ( 5.713622356042774797, 2.214598200325838206, 0.6159738146167788031 ) ) ;
#87983=CARTESIAN_POINT ( 'NONE',  ( 1.324644486801781040, 2.210297274253099520, 0.6072788910070088253 ) ) ;
#87986=CARTESIAN_POINT ( 'NONE',  ( 5.630791504788829727, -1.754662785997921359, 0.8323459256341717571 ) ) ;
#87993=CARTESIAN_POINT ( 'NONE',  ( 5.924064563541377559, -1.897137492723115049, 0.2407653536913647030 ) ) ;
#87994=CARTESIAN_POINT ( 'NONE',  ( 5.559779856078610472, 1.205038519190555268, 1.616695979245158066 ) ) ;
#87999=CARTESIAN_POINT ( 'NONE',  ( 2.255913092623571092, 0.8947350874906587759, 1.889642235345281307 ) ) ;
#88000=CARTESIAN_POINT ( 'NONE',  ( 1.727073733189425031, -1.667858853059518420, 0.5925122568580538651 ) ) ;
#88003=CARTESIAN_POINT ( 'NONE',  ( 3.802894434091105946, 1.965436290923015639, 1.179407150283459105 ) ) ;
#88004=CARTESIAN_POINT ( 'NONE',  ( 2.905909708737213659, 1.260233761464889302, -1.200475698291984861 ) ) ;
#88007=CARTESIAN_POINT ( 'NONE',  ( 2.582960874182936628, 1.135899660060729399, -1.309998962497432196 ) ) ;
#88008=CARTESIAN_POINT ( 'NONE',  ( 3.631445352573436480, 0.05657863903951602241, -2.170607583040237820 ) ) ;
#88010=CARTESIAN_POINT ( 'NONE',  ( 4.522672878804367969, 0.3494810548456111499, 1.985869246038343583 ) ) ;
#88011=CARTESIAN_POINT ( 'NONE',  ( 2.437500000000002220, 1.451031289061020857, -1.451031289061217366 ) ) ;
#88013=CARTESIAN_POINT ( 'NONE',  ( 1.254767684091241620, -1.520462189517374219, 1.182783339890740359 ) ) ;
#88015=CARTESIAN_POINT ( 'NONE',  ( 4.430067838210618447, -2.178247905445731103, 0.4349904863075284567 ) ) ;
#88017=CARTESIAN_POINT ( 'NONE',  ( -0.1108833634137010304, 7.629137130509073828, -2.496956624467902675 ) ) ;
#88021=CARTESIAN_POINT ( 'NONE',  ( 0.8916360836422586589, -0.05999620363036740206, -2.220659203727569420 ) ) ;
#88022=CARTESIAN_POINT ( 'NONE',  ( 5.810985101215744741, -1.547553103248515027, 1.205733875218002238 ) ) ;
#88025=CARTESIAN_POINT ( 'NONE',  ( 6.555986116969920730, 2.257040928323080564, -0.1566935481548906162 ) ) ;
#88027=CARTESIAN_POINT ( 'NONE',  ( 3.543474241949475356, 1.865888119384132127, -0.8795106731672995837 ) ) ;
#88032=CARTESIAN_POINT ( 'NONE',  ( 5.307814152003552444, -1.861618091082300808, 0.1822119596564600597 ) ) ;
#88033=CARTESIAN_POINT ( 'NONE',  ( 3.937908632975633871, -1.444535402496229137, -0.9590898762639500363 ) ) ;
#88034=CARTESIAN_POINT ( 'NONE',  ( 3.403587037673636129, -0.7086591031593177936, -1.589830453666951415 ) ) ;
#88035=CARTESIAN_POINT ( 'NONE',  ( 0.5215107003284430442, -2.174349661526672417, 0.7262685697029276355 ) ) ;
#88037=CARTESIAN_POINT ( 'NONE',  ( 5.126549769544753055, 0.1549841644245806838, 2.085076985156742779 ) ) ;
#88038=CARTESIAN_POINT ( 'NONE',  ( 6.714805131850001274, -0.1305238817815305985, 1.911932681171425896 ) ) ;
#88042=CARTESIAN_POINT ( 'NONE',  ( 0.6334356698059575574, 0.5880228326464317368, 1.928751028484784413 ) ) ;
#88043=CARTESIAN_POINT ( 'NONE',  ( 0.9672155168029163974, -1.668165459610539081, 1.309123814877902969 ) ) ;
#88044=CARTESIAN_POINT ( 'NONE',  ( 6.925078400183534377, -0.01048729610059368801, 2.244148362790527873 ) ) ;
#88048=CARTESIAN_POINT ( 'NONE',  ( 2.174623584685225541, 0.9092215167782154994, 1.915816808323366871 ) ) ;
#88050=CARTESIAN_POINT ( 'NONE',  ( 4.494645072041675071, -0.4025399330690944133, -1.780595394402582077 ) ) ;
#88056=CARTESIAN_POINT ( 'NONE',  ( 2.513930914015961804, -0.6297079463782135900, 1.919214091249999088 ) ) ;
#88057=CARTESIAN_POINT ( 'NONE',  ( 5.192482782645277517, -2.189556457885518892, -0.2746672974567528347 ) ) ;
#88059=CARTESIAN_POINT ( 'NONE',  ( 3.731172809088632025, 0.04972793443442201367, -1.860468898575567520 ) ) ;
#88066=CARTESIAN_POINT ( 'NONE',  ( 4.635264976507449397, -1.668059998867366778, 0.7425182445051290436 ) ) ;
#88070=CARTESIAN_POINT ( 'NONE',  ( 0.4909827745146425060, 1.656533638411663345, 0.5119339833263967243 ) ) ;
#88071=CARTESIAN_POINT ( 'NONE',  ( 6.650350966976619205, -1.419654684173769166, 1.172063944840713523 ) ) ;
#88072=CARTESIAN_POINT ( 'NONE',  ( 5.672612835131308984, -1.468196381517340665, 1.780430754307258390 ) ) ;
#88074=CARTESIAN_POINT ( 'NONE',  ( 1.124374118904346798, 1.229854006068244132, -1.653384075620732307 ) ) ;
#88076=CARTESIAN_POINT ( 'NONE',  ( 0.5794536021234627521, 1.392335491182377316, -1.458330535474762213 ) ) ;
#88080=CARTESIAN_POINT ( 'NONE',  ( 5.823093596695693819, -0.04436734784114480107, 1.870300906237104988 ) ) ;
#88082=CARTESIAN_POINT ( 'NONE',  ( 3.375170810042011915, -1.688748480992762868, -0.8973671847329609541 ) ) ;
#88085=CARTESIAN_POINT ( 'NONE',  ( 5.162800556355915838, -1.600310254184673431, 1.519886962452212664 ) ) ;
#88090=CARTESIAN_POINT ( 'NONE',  ( 5.848313825214911610, 1.045240856298999432, -1.844880668361434939 ) ) ;
#88091=CARTESIAN_POINT ( 'NONE',  ( 3.083396755883772933, -0.1683641986609325514, -2.301487591144059763 ) ) ;
#88092=CARTESIAN_POINT ( 'NONE',  ( 4.035565188342554954, 1.848088059160474694, -0.6588067414724924076 ) ) ;
#88094=CARTESIAN_POINT ( 'NONE',  ( 1.041763817972749750, 1.313373124611896703, 1.457441342770829262 ) ) ;
#88098=CARTESIAN_POINT ( 'NONE',  ( 6.051970301643104122, 1.040788372175960541, 1.727066800951609249 ) ) ;
#88101=CARTESIAN_POINT ( 'NONE',  ( 0.3218710511002781383, 1.760991339961643920, 0.5373333866721883290 ) ) ;
#88103=CARTESIAN_POINT ( 'NONE',  ( 2.588947950494639993, 2.104950400290429791, 0.5311738530254602741 ) ) ;
#88105=CARTESIAN_POINT ( 'NONE',  ( 0.3344391967911933272, -1.139684030083350841, -1.788147294700337397 ) ) ;
#88111=CARTESIAN_POINT ( 'NONE',  ( 0.4212572661226633985, -0.1035701926632242170, 2.058322702938982562 ) ) ;
#88117=CARTESIAN_POINT ( 'NONE',  ( 3.053266463924544372, -1.685387242695039811, 0.9035085923766730254 ) ) ;
#88118=CARTESIAN_POINT ( 'NONE',  ( 5.506658716161647149, 1.338116961444441921, -1.158480101542769036 ) ) ;
#88121=CARTESIAN_POINT ( 'NONE',  ( 0.4042039562905282435, -1.797914468929398879, -0.2212116797051487393 ) ) ;
#88123=CARTESIAN_POINT ( 'NONE',  ( 0.7432033230480495911, 0.3705163548812146490, -1.879356322977752347 ) ) ;
#88124=CARTESIAN_POINT ( 'NONE',  ( 2.400909748719297188, 0.4512941399696759337, 2.020426262116347349 ) ) ;
#88126=CARTESIAN_POINT ( 'NONE',  ( 6.702024585102262400, -1.870183347854617040, 0.04844413084104796929 ) ) ;
#88127=CARTESIAN_POINT ( 'NONE',  ( 2.877373901574116211, 1.733520850877915187, -0.5729475677913041798 ) ) ;
#88128=CARTESIAN_POINT ( 'NONE',  ( 6.727182134110200273, -0.004969159814478123736, 2.189081792362323586 ) ) ;
#88131=CARTESIAN_POINT ( 'NONE',  ( 3.859879052112312969, -0.6014189565349871147, 1.973034901002912678 ) ) ;
#88136=CARTESIAN_POINT ( 'NONE',  ( 0.7202740732663616141, -1.155732025818452913, -1.826486478054230256 ) ) ;
#88137=CARTESIAN_POINT ( 'NONE',  ( 6.725056259267968350, -1.891221747171191403, -0.8428681758992571105 ) ) ;
#88139=CARTESIAN_POINT ( 'NONE',  ( 3.936934155531632396, 0.3128429973590241553, 2.138701728237289768 ) ) ;
#88140=CARTESIAN_POINT ( 'NONE',  ( 4.442060220718175856, -1.244341337028841421, -1.590709041654225553 ) ) ;
#88148=CARTESIAN_POINT ( 'NONE',  ( 2.483611571103708116, -0.6279893487078171965, 1.916353726171161620 ) ) ;
#88151=CARTESIAN_POINT ( 'NONE',  ( 6.670655732516623360, 7.629137130509072051, 2.773739711112707784 ) ) ;
#88152=CARTESIAN_POINT ( 'NONE',  ( 5.414289803398987466, -1.912571729023364364, 0.006307610287324683096 ) ) ;
#88156=CARTESIAN_POINT ( 'NONE',  ( 4.833611329963474645, 0.6298591494234163646, -1.915606498650752831 ) ) ;
#88159=CARTESIAN_POINT ( 'NONE',  ( 6.229511965242640059, -1.622199917339474329, 0.5863599495292673991 ) ) ;
#88163=CARTESIAN_POINT ( 'NONE',  ( 5.008994926481016741, 1.626754543590884561, 0.9232732976792232815 ) ) ;
#88164=CARTESIAN_POINT ( 'NONE',  ( 6.047140908842845164, 0.2017661761196144488, 2.003097277516131758 ) ) ;
#88166=CARTESIAN_POINT ( 'NONE',  ( 2.606376076552410659, 2.069701014239883730, 0.05521581806712527740 ) ) ;
#88170=CARTESIAN_POINT ( 'NONE',  ( 0.4566579290818244541, -1.899626807963299635, -0.6766942018802262204 ) ) ;
#88178=CARTESIAN_POINT ( 'NONE',  ( 6.345329912860430355, 0.3219833572893218698, -1.888178885089139669 ) ) ;
#88186=CARTESIAN_POINT ( 'NONE',  ( 2.588937169860201504, -0.3686131662095324391, -2.129881858774537395 ) ) ;
#88189=CARTESIAN_POINT ( 'NONE',  ( 0.7387272492362946252, 1.258454933865692293, -1.706699550108881080 ) ) ;
#88190=CARTESIAN_POINT ( 'NONE',  ( 5.948246703923279810, 1.823645139926059144, 0.08696428134234018836 ) ) ;
#88191=CARTESIAN_POINT ( 'NONE',  ( 2.706272882855005335, -0.7510657119417161187, -1.822867458954416708 ) ) ;
#88192=CARTESIAN_POINT ( 'NONE',  ( 4.236511230858605259, 1.172298487584079396, -1.510895503047122945 ) ) ;
#88194=CARTESIAN_POINT ( 'NONE',  ( 4.510180775305682843, 1.969176117969779982, -0.04608634298608124680 ) ) ;
#88195=CARTESIAN_POINT ( 'NONE',  ( 0.9021669503554888836, 1.471007182523446311, -1.267884427665219471 ) ) ;
#88202=CARTESIAN_POINT ( 'NONE',  ( 5.567032834676129305, -1.504811603839781631, 1.179860560037985895 ) ) ;
#88205=CARTESIAN_POINT ( 'NONE',  ( 1.079469989902905214, -0.05558308599296066244, -2.206230565744627281 ) ) ;
#88208=CARTESIAN_POINT ( 'NONE',  ( 6.305343602688459725, 1.750316497599126331, -0.9943532346578187742 ) ) ;
#88209=CARTESIAN_POINT ( 'NONE',  ( -0.02338929933905566777, 0.2563879980532010605, -1.746150209723141167 ) ) ;
#88212=CARTESIAN_POINT ( 'NONE',  ( 2.664580169416390643, -0.7900844611210651180, -1.913877855911281012 ) ) ;
#88216=CARTESIAN_POINT ( 'NONE',  ( 0.9015118058452382677, 1.767791302423503685, 1.243857928393626633 ) ) ;
#88221=CARTESIAN_POINT ( 'NONE',  ( 6.825078400183593352, 2.989295776279639938, 2.209688085509611710 ) ) ;
#88224=CARTESIAN_POINT ( 'NONE',  ( 4.289544331642456854, 1.336530783054422189, -1.104934575851760137 ) ) ;
#88226=CARTESIAN_POINT ( 'NONE',  ( 2.448173108494243078, -0.8891298726186761536, 1.869765896676472083 ) ) ;
#88227=CARTESIAN_POINT ( 'NONE',  ( 4.446934944069580453, -1.891868754433777555, -0.9506184929228760350 ) ) ;
#88231=CARTESIAN_POINT ( 'NONE',  ( 1.604289258337993296, 1.966964933800469106, 0.1018061066037061896 ) ) ;
#88232=CARTESIAN_POINT ( 'NONE',  ( 1.353610510645312237, -1.387278792934818705, -1.316581319992945920 ) ) ;
#88233=CARTESIAN_POINT ( 'NONE',  ( 5.138769532551322072, -1.968056315684912683, 1.175056510511104158 ) ) ;
#88234=CARTESIAN_POINT ( 'NONE',  ( 1.787459277025660542, 1.258035843444211155, 1.323286951131589895 ) ) ;
#88239=CARTESIAN_POINT ( 'NONE',  ( 3.006110871101048687, -0.8120814715368419590, 1.842311383860009588 ) ) ;
#88240=CARTESIAN_POINT ( 'NONE',  ( 3.116010788575247936, 1.952738871351952232, -0.1875660449981580158 ) ) ;
#88243=CARTESIAN_POINT ( 'NONE',  ( 0.07516593201269992919, 2.015085533825950126, -2.458757630349134082 ) ) ;
#88244=CARTESIAN_POINT ( 'NONE',  ( 5.753879374300719718, 0.8463200818398952663, 1.911864941374420201 ) ) ;
#88245=CARTESIAN_POINT ( 'NONE',  ( 4.346413238989558003, 0.4729554063761501892, 1.705410949051559877 ) ) ;
#88247=CARTESIAN_POINT ( 'NONE',  ( 0.3049557181189038180, 1.908793570626087455, 1.076422248949958638 ) ) ;
#88248=CARTESIAN_POINT ( 'NONE',  ( 6.439394946090388316, 0.6587646163928980725, -1.611052209844960670 ) ) ;
#88250=CARTESIAN_POINT ( 'NONE',  ( 0.1333692844072559003, 5.722267537706915874, -2.647605121726896105 ) ) ;
#88251=CARTESIAN_POINT ( 'NONE',  ( 6.592461167385279097, -0.5184713896582182624, 2.248443398875634269 ) ) ;
#88254=CARTESIAN_POINT ( 'NONE',  ( 6.450542193449531503, 1.198949306261879455, 1.252755643323471668 ) ) ;
#88255=CARTESIAN_POINT ( 'NONE',  ( 1.506762622594171930, -0.7967928049063888185, -2.058199171410409978 ) ) ;
#88256=CARTESIAN_POINT ( 'NONE',  ( 0.7081837076810155729, 0.6824709381345904768, -2.061040276042750641 ) ) ;
#88258=CARTESIAN_POINT ( 'NONE',  ( 0.8665975061730617490, -2.067159395656243515, -0.4576585243742418152 ) ) ;
#88259=CARTESIAN_POINT ( 'NONE',  ( 2.562500000000001332, -1.451031289061222251, -1.451031289061014196 ) ) ;
#88262=CARTESIAN_POINT ( 'NONE',  ( 4.770489386553291133, -1.258480429039417592, 1.458564191902473661 ) ) ;
#88264=CARTESIAN_POINT ( 'NONE',  ( 1.751946580633024331, 2.285858364093972028, -0.1737669427509143383 ) ) ;
#88268=CARTESIAN_POINT ( 'NONE',  ( 4.125785508553894587, -0.3794599818576475658, 2.188496638732019495 ) ) ;
#88276=CARTESIAN_POINT ( 'NONE',  ( 1.318982659667154334, 0.9913977828604101372, -1.755770081111128977 ) ) ;
#88278=CARTESIAN_POINT ( 'NONE',  ( 6.584441931359013900, 1.190761153509769521, -1.684076666428784064 ) ) ;
#88281=CARTESIAN_POINT ( 'NONE',  ( 6.444851825500396814, -1.403812859381381895, -1.028626497576446086 ) ) ;
#88285=CARTESIAN_POINT ( 'NONE',  ( 1.440303513825416992, 0.3384911870211620988, 1.736878781881325384 ) ) ;
#88286=CARTESIAN_POINT ( 'NONE',  ( 6.609999999999995879, 0.01081285896096205283, 1.720159828161060833 ) ) ;
#88287=CARTESIAN_POINT ( 'NONE',  ( 6.286628787680052177, 1.509496725765889114, -0.8662470760552234417 ) ) ;
#88288=CARTESIAN_POINT ( 'NONE',  ( 4.195090427499806651, 1.841111018879896477, 1.365591311898015192 ) ) ;
#88289=CARTESIAN_POINT ( 'NONE',  ( 3.345483972246702020, 1.841320589717788447, -0.001054884335952021917 ) ) ;
#88294=CARTESIAN_POINT ( 'NONE',  ( 4.366094929315432083, 0.8608494910617261464, 1.609850404305966265 ) ) ;
#88295=CARTESIAN_POINT ( 'NONE',  ( 5.027970288326706338, -1.728003250605243180, 1.038991650911202713 ) ) ;
#88297=CARTESIAN_POINT ( 'NONE',  ( 3.186655532321683637, -2.228779239134215384, -0.3884498486929898742 ) ) ;
#88299=CARTESIAN_POINT ( 'NONE',  ( 6.792010069470917344, -0.9048057162561828903, 1.900113248071538585 ) ) ;
#88301=CARTESIAN_POINT ( 'NONE',  ( 3.807136610393092813, -1.694265131726957252, 1.189645435975445809 ) ) ;
#88304=CARTESIAN_POINT ( 'NONE',  ( 6.235037545507011281, 1.978399733989940401, 0.7636319146847592165 ) ) ;
#88306=CARTESIAN_POINT ( 'NONE',  ( 2.033698780422585006, -1.258094322230184581, -1.459052628860134648 ) ) ;
#88308=CARTESIAN_POINT ( 'NONE',  ( 0.3089591345776849241, -1.584006439100977603, 1.170298647042963935 ) ) ;
#88313=CARTESIAN_POINT ( 'NONE',  ( 0.03578803411239706023, -0.1004787818888741302, 2.219253419324648036 ) ) ;
#88314=CARTESIAN_POINT ( 'NONE',  ( 1.852698501422584298, 0.6601115537133980249, 1.999908888789264649 ) ) ;
#88317=CARTESIAN_POINT ( 'NONE',  ( 0.3966288646398182238, 0.3121968076400126746, 1.834509442227350462 ) ) ;
#88319=CARTESIAN_POINT ( 'NONE',  ( 0.07700591528353981086, 0.003617085621422309362, -1.910863332519038726 ) ) ;
#88322=CARTESIAN_POINT ( 'NONE',  ( 0.7035762090183244055, 1.867434778015097940, -1.004864118554361863 ) ) ;
#88325=CARTESIAN_POINT ( 'NONE',  ( 2.875390130891414042, -0.1950805366632331617, 1.952157403750237163 ) ) ;
#88326=CARTESIAN_POINT ( 'NONE',  ( 2.114359756454447847, -1.018641858927371135, -1.906637348776268004 ) ) ;
#88327=CARTESIAN_POINT ( 'NONE',  ( 2.102840161960460197, -0.4018910908503615653, 1.796694178532439956 ) ) ;
#88330=CARTESIAN_POINT ( 'NONE',  ( 3.239928156850964580, 0.4239778953066320466, 1.687749859276384878 ) ) ;
#88333=CARTESIAN_POINT ( 'NONE',  ( 1.042116488573753497, 0.8753402851892390091, -1.976733581976031218 ) ) ;
#88334=CARTESIAN_POINT ( 'NONE',  ( 2.917342117414220670, 0.6766092434087739305, 1.899328150365031664 ) ) ;
#88337=CARTESIAN_POINT ( 'NONE',  ( 0.07536363704235826688, -0.001874865094115066300, -2.144269471569634877 ) ) ;
#88338=CARTESIAN_POINT ( 'NONE',  ( 1.762511527598693784, -1.395553132451602174, 1.392767733363926119 ) ) ;
#88341=CARTESIAN_POINT ( 'NONE',  ( 2.190873381757904692, 1.502741926987064325, 1.230217333823523163 ) ) ;
#88345=CARTESIAN_POINT ( 'NONE',  ( -0.2106854629474881058, 5.722459385925042774, -2.591190942950042597 ) ) ;
#88350=CARTESIAN_POINT ( 'NONE',  ( 6.440458288041322810, 2.281167638128688946, 0.3475669597150666257 ) ) ;
#88352=CARTESIAN_POINT ( 'NONE',  ( 4.662917994108885189, 1.519075486231920458, -1.241376779329693258 ) ) ;
#88354=CARTESIAN_POINT ( 'NONE',  ( 1.459611520199757706, -1.915600648959712382, -0.6298732728240025169 ) ) ;
#88356=CARTESIAN_POINT ( 'NONE',  ( 2.589187231636483233, 1.791351791295469731, 1.128514814827277002 ) ) ;
#88360=CARTESIAN_POINT ( 'NONE',  ( 2.765369989423609454, 0.9851603262180377296, 1.555203531693909680 ) ) ;
#88364=CARTESIAN_POINT ( 'NONE',  ( 4.306960158517386894, -0.4675538901007176285, -2.068242682749166672 ) ) ;
#88365=CARTESIAN_POINT ( 'NONE',  ( 0.1109373197970727615, -1.806229982939497658, 0.3559056038356380736 ) ) ;
#88368=CARTESIAN_POINT ( 'NONE',  ( 4.411438286107774331, -0.3560947707623678959, 2.029623144953551339 ) ) ;
#88370=CARTESIAN_POINT ( 'NONE',  ( 1.223879446662301307, 1.774596971308094018, 0.4907264878865265634 ) ) ;
#88374=CARTESIAN_POINT ( 'NONE',  ( 0.9970219447392356660, -0.5395372827587068265, -2.139793933917451874 ) ) ;
#88375=CARTESIAN_POINT ( 'NONE',  ( 3.444836229973327946, 0.5457880569446837971, 2.195490905318697283 ) ) ;
#88377=CARTESIAN_POINT ( 'NONE',  ( 3.181707836761258790, 1.766318828868058910, -0.4016052188219875752 ) ) ;
#88378=CARTESIAN_POINT ( 'NONE',  ( 4.381993024020896854, -1.915445973796879864, -0.04088167158281148100 ) ) ;
#88379=CARTESIAN_POINT ( 'NONE',  ( 5.547352688424546763, 1.827615396715172258, -0.9727077141251788683 ) ) ;
#88381=CARTESIAN_POINT ( 'NONE',  ( 3.643400374902918681, -1.492087795311855425, -1.288628176122036839 ) ) ;
#88382=CARTESIAN_POINT ( 'NONE',  ( 1.342661396784496697, 0.3730742192328758144, 1.889760217127177455 ) ) ;
#88383=CARTESIAN_POINT ( 'NONE',  ( 3.414787578387419309, 1.690673485743508619, 0.8009127983473337542 ) ) ;
#88384=CARTESIAN_POINT ( 'NONE',  ( 3.756711156304150201, 0.8293906405268698379, 2.153668854807685662 ) ) ;
#88385=CARTESIAN_POINT ( 'NONE',  ( 4.053051418270800177, 1.573051355563404252, -0.9941624863331417483 ) ) ;
#88390=CARTESIAN_POINT ( 'NONE',  ( 1.436301726765435438, 1.036571610867568216, -1.833232669937171266 ) ) ;
#88396=CARTESIAN_POINT ( 'NONE',  ( 3.058948843759463188, 0.5191580478346514704, 2.055925682384197373 ) ) ;
#88398=CARTESIAN_POINT ( 'NONE',  ( 1.265885189609064376, 0.5823756177252036315, -1.934031124627869414 ) ) ;
#88402=ORIENTED_EDGE ( 'NONE', *, *, #47626, .T. ) ;
#88403=CARTESIAN_POINT ( 'NONE',  ( 0.7554163591718568993, -1.825703804718967316, -1.157005318491082901 ) ) ;
#88407=CARTESIAN_POINT ( 'NONE',  ( 6.539320575229233157, 0.001224430076711413356, 2.103502572931112091 ) ) ;
#88409=CARTESIAN_POINT ( 'NONE',  ( 5.858611323429600226, -1.916351766245901977, -0.6279953093112633500 ) ) ;
#88411=CARTESIAN_POINT ( 'NONE',  ( -0.1232117409455633916, -0.1621322592461546530, -2.156395338765437764 ) ) ;
#88413=CARTESIAN_POINT ( 'NONE',  ( 0.5325469457231490900, 1.160272198634606955, -1.942242498246045113 ) ) ;
#88416=CARTESIAN_POINT ( 'NONE',  ( 4.329314735043091389, -1.561880650076686861, -1.275557594027726394 ) ) ;
#88418=CARTESIAN_POINT ( 'NONE',  ( 0.7553224350208649351, 1.845776580612036533, -0.5121453728616427448 ) ) ;
#88423=CARTESIAN_POINT ( 'NONE',  ( 3.088212622510533301, -1.699425283745788162, -0.2941843989033367524 ) ) ;
#88425=CARTESIAN_POINT ( 'NONE',  ( 2.266550661271060640, -1.615954428537921483, -0.7220204016161780869 ) ) ;
#88427=CARTESIAN_POINT ( 'NONE',  ( 5.122202071631626552, -1.176711583861598243, -1.866687997650509079 ) ) ;
#88430=CARTESIAN_POINT ( 'NONE',  ( 4.131121313247118287, 1.848376352210901574, 0.8146727144991843250 ) ) ;
#88432=CARTESIAN_POINT ( 'NONE',  ( 4.723349490952149843, 1.845327050471495367, 1.044454997443218236 ) ) ;
#88433=CARTESIAN_POINT ( 'NONE',  ( 3.989861366179075830, -2.010826228832915508, 0.1511578083489423796 ) ) ;
#88434=CARTESIAN_POINT ( 'NONE',  ( 4.113381391103660967, 1.458659968308340993, 1.074121561303176264 ) ) ;
#88439=CARTESIAN_POINT ( 'NONE',  ( 1.481098450213329754, 1.729700800547562478, -0.7128637423776187365 ) ) ;
#88442=CARTESIAN_POINT ( 'NONE',  ( 6.498695496729308907, -1.778006411731817060, -0.3456425897902185018 ) ) ;
#88448=CARTESIAN_POINT ( 'NONE',  ( -0.1581436608063293003, -1.178060542814472367, -1.506996232563104554 ) ) ;
#88453=CARTESIAN_POINT ( 'NONE',  ( 4.254221937059123881, 0.9039275175388860051, -1.918405034562712608 ) ) ;
#88454=CARTESIAN_POINT ( 'NONE',  ( -0.02968770228140015649, 0.7448490463385792903, -1.910291535987144629 ) ) ;
#88456=CARTESIAN_POINT ( 'NONE',  ( 5.606699263565281477, 1.494642942781895023, -1.285547057225975509 ) ) ;
#88458=CARTESIAN_POINT ( 'NONE',  ( 0.5627444733627232631, 0.5882401669465211480, 1.925320163072720359 ) ) ;
#88459=VERTEX_POINT ( 'NONE', #183026 ) ;
#88460=CARTESIAN_POINT ( 'NONE',  ( 6.298082486376491929, -1.000091913425070311, -1.866304853008766917 ) ) ;
#88462=CARTESIAN_POINT ( 'NONE',  ( 1.943885480841448965, 1.426152643941134501, 1.501071833787496645 ) ) ;
#88463=ORIENTED_EDGE ( 'NONE', *, *, #124624, .F. ) ;
#88467=CARTESIAN_POINT ( 'NONE',  ( 4.541018360983569480, -1.615799657739678263, -1.326631217474142366 ) ) ;
#88469=CARTESIAN_POINT ( 'NONE',  ( 3.434410497111122673, 1.780829521046650932, 0.4009754434649847044 ) ) ;
#88470=CARTESIAN_POINT ( 'NONE',  ( 1.400706157114139261, -0.2655193030335687987, -1.791778796870816759 ) ) ;
#88474=CARTESIAN_POINT ( 'NONE',  ( 4.788207028248289809, -1.043783763870303360, 1.944324211313207318 ) ) ;
#88477=CARTESIAN_POINT ( 'NONE',  ( 2.543496672408153358, -1.783599581865771500, 0.6900697577220117340 ) ) ;
#88478=( BOUNDED_SURFACE ( )  B_SPLINE_SURFACE ( 3, 3, ( 
 ( #130328, #162763, #196317, #170197, #73767, #20727, #201606, #168076, #203742, #21781 ),
 ( #187513, #53255, #86822, #119385, #3411, #52192, #70536, #88972, #69477, #4464 ),
 ( #136655, #185373, #40214, #155027, #138787, #35928, #87890, #39144, #152886, #118318 ),
 ( #36993, #120468, #103077, #169132, #202680, #153963, #7683, #184304, #105225, #102006 ),
 ( #6612, #19674, #204807, #186440, #54329, #38077, #72692, #104149, #5530, #71610 ),
 ( #137723, #56458, #55387, #121542, #171265, #22859, #122620, #23936, #188581, #106323 ),
 ( #135585, #172346, #90040, #156098, #139863, #85754, #151835, #26076, #111673, #174498 ) ),
 .UNSPECIFIED., .T., .F., .T. ) 
 B_SPLINE_SURFACE_WITH_KNOTS ( ( 4, 3, 4 ),
 ( 4, 1, 1, 1, 1, 1, 1, 4 ),
 ( 0.000000000000000000, 0.5000000000000000000, 1.000000000000000000 ),
 ( 0.000000000000000000, 0.09790276019723312406, 0.1918320694002237370, 0.2608036337010187777, 0.3626611837559554630, 0.5214803378330250538, 0.7337833476510040587, 1.000000000000000000 ),
 .UNSPECIFIED. ) 
 GEOMETRIC_REPRESENTATION_ITEM ( )  RATIONAL_B_SPLINE_SURFACE ( (
 ( 1.000000000000000444, 1.000000000000000444, 1.000000000000000000, 1.000000000000000444, 1.000000000000000222, 1.000000000000000222, 1.000000000000000444, 1.000000000000000000, 1.000000000000000222, 1.000000000000000222),
 ( 0.3333333333333334814, 0.3333333333333334814, 0.3333333333333334814, 0.3333333333333334259, 0.3333333333333333703, 0.3333333333333334259, 0.3333333333333335369, 0.3333333333333333703, 0.3333333333333334259, 0.3333333333333334259),
 ( 0.3333333333333334814, 0.3333333333333334814, 0.3333333333333334814, 0.3333333333333334259, 0.3333333333333333703, 0.3333333333333334259, 0.3333333333333335369, 0.3333333333333333703, 0.3333333333333334259, 0.3333333333333334259),
 ( 1.000000000000000444, 1.000000000000000444, 1.000000000000000000, 1.000000000000000444, 1.000000000000000222, 1.000000000000000222, 1.000000000000000444, 1.000000000000000000, 1.000000000000000222, 1.000000000000000222),
 ( 0.3333333333333334814, 0.3333333333333334814, 0.3333333333333334814, 0.3333333333333334259, 0.3333333333333333703, 0.3333333333333334259, 0.3333333333333335369, 0.3333333333333333703, 0.3333333333333334259, 0.3333333333333334259),
 ( 0.3333333333333334814, 0.3333333333333334814, 0.3333333333333334814, 0.3333333333333334259, 0.3333333333333333703, 0.3333333333333334259, 0.3333333333333335369, 0.3333333333333333703, 0.3333333333333334259, 0.3333333333333334259),
 ( 1.000000000000000444, 1.000000000000000444, 1.000000000000000000, 1.000000000000000444, 1.000000000000000222, 1.000000000000000222, 1.000000000000000444, 1.000000000000000000, 1.000000000000000222, 1.000000000000000222) ) ) 
 REPRESENTATION_ITEM ( '' )  SURFACE ( )  );
#88482=CARTESIAN_POINT ( 'NONE',  ( 6.198795224570643470, 1.821041368708445907, 1.219022265761634971 ) ) ;
#88488=CARTESIAN_POINT ( 'NONE',  ( 3.321420150926617687, -1.803644938814071175, 0.4956094624995326381 ) ) ;
#88493=CARTESIAN_POINT ( 'NONE',  ( 6.420769920452011448, -1.468259139554881409, 1.459777494992514857 ) ) ;
#88494=CARTESIAN_POINT ( 'NONE',  ( 1.212517793387542842, 1.944078472882956987, 0.5350667013180390175 ) ) ;
#88498=CARTESIAN_POINT ( 'NONE',  ( 1.166276502169643070, -1.387892208999995436, 1.695937554688830451 ) ) ;
#88499=CARTESIAN_POINT ( 'NONE',  ( 5.514214477338499343, -0.8245889995748826307, -1.628937154514856767 ) ) ;
#88508=CARTESIAN_POINT ( 'NONE',  ( 4.089279031174639201, -0.7008038172400687937, 1.702867937621636463 ) ) ;
#88509=CARTESIAN_POINT ( 'NONE',  ( 6.398696026112846269, -1.975200287401058130, -0.3884956089365321774 ) ) ;
#88510=CARTESIAN_POINT ( 'NONE',  ( 1.529136539685072238, 2.264261833246409505, -0.3938019620175516322 ) ) ;
#88512=CARTESIAN_POINT ( 'NONE',  ( 6.977413161700751765, -0.1449424838519241254, 1.929857014940839832 ) ) ;
#88515=CARTESIAN_POINT ( 'NONE',  ( 3.884940529579200774, -1.786240503712609895, -0.6835825222790415934 ) ) ;
#88519=CARTESIAN_POINT ( 'NONE',  ( 2.946908815893133138, -1.710673590971498292, -1.201729372296795662 ) ) ;
#88520=CARTESIAN_POINT ( 'NONE',  ( 1.340467186903429253, 0.3614942610149494695, 1.835218787103513050 ) ) ;
#88521=CARTESIAN_POINT ( 'NONE',  ( 1.950545848857932807, 1.388271641964162084, 1.462223312268404074 ) ) ;
#88524=CARTESIAN_POINT ( 'NONE',  ( 3.579424886596099586, -0.8542006638617373193, 1.516299650553302181 ) ) ;
#88528=CARTESIAN_POINT ( 'NONE',  ( 3.967213729759576868, 0.2084270747255561884, -1.712163910207653128 ) ) ;
#88529=CARTESIAN_POINT ( 'NONE',  ( 4.265290774032561849, 2.125562838249666964, -0.5332280334861272397 ) ) ;
#88530=CARTESIAN_POINT ( 'NONE',  ( 5.268293329372571776, 1.085216321637239023, 1.921556908365213312 ) ) ;
#88532=CARTESIAN_POINT ( 'NONE',  ( 3.608415011292832819, 2.171239808225163159, 0.005094884836047069293 ) ) ;
#88533=CARTESIAN_POINT ( 'NONE',  ( 2.596107596775329540, -1.820790993511243849, -0.1344670722737417168 ) ) ;
#88535=CARTESIAN_POINT ( 'NONE',  ( 4.206348283080693307, 1.299600563804912623, -1.671539989125019332 ) ) ;
#88538=CARTESIAN_POINT ( 'NONE',  ( 4.968466765020612463, -2.157917790226408172, -0.7739415147586664601 ) ) ;
#88540=CARTESIAN_POINT ( 'NONE',  ( 6.720655732516647163, 0.5950723047917580999, 1.879543361893110109 ) ) ;
#88542=CARTESIAN_POINT ( 'NONE',  ( 0.8035760164417544704, 1.868272328500224289, -1.003034915376184388 ) ) ;
#88546=CARTESIAN_POINT ( 'NONE',  ( 6.883263157960363365, 3.690127339433949327, 2.567897385111846731 ) ) ;
#88549=CARTESIAN_POINT ( 'NONE',  ( 5.537732479266092689, -1.587839044716709669, 1.242724925242834066 ) ) ;
#88551=CARTESIAN_POINT ( 'NONE',  ( 3.045816552677531597, 1.455321998776702319, 1.461834479831431555 ) ) ;
#88553=CARTESIAN_POINT ( 'NONE',  ( -0.1408020194050146334, 2.009929383927198998, -2.515281701100045009 ) ) ;
#88558=CARTESIAN_POINT ( 'NONE',  ( 6.210891007176935652, -0.2719346519345893776, 2.174439262769362280 ) ) ;
#88559=CARTESIAN_POINT ( 'NONE',  ( 3.287732575140737801, 1.587837554856496691, -1.242726844152845178 ) ) ;
#88560=CARTESIAN_POINT ( 'NONE',  ( 3.509164994824386596, -1.813400730843343966, 0.3181347684400454012 ) ) ;
#88564=CARTESIAN_POINT ( 'NONE',  ( 0.1820471141361617307, -1.670984272841398832, -0.4269972090983116253 ) ) ;
#88566=CARTESIAN_POINT ( 'NONE',  ( 0.5285108043569552994, -1.967359331218739626, 1.188758619093014168 ) ) ;
#88568=CARTESIAN_POINT ( 'NONE',  ( 6.420815857685610695, 2.108269355124866351, 0.8215519888849237562 ) ) ;
#88569=CARTESIAN_POINT ( 'NONE',  ( 3.194068465612946994, -0.8531780664592978347, 1.925702383005133855 ) ) ;
#88578=CARTESIAN_POINT ( 'NONE',  ( 3.955514033904330873, -1.931546270572735979, 1.097109147590840550 ) ) ;
#88579=CARTESIAN_POINT ( 'NONE',  ( 2.361504994916805877, 2.148894721571582789, -0.4289216190115978100 ) ) ;
#88582=CARTESIAN_POINT ( 'NONE',  ( 5.090269282739749102, 1.010147525469132557, -1.681691772506640481 ) ) ;
#88587=CARTESIAN_POINT ( 'NONE',  ( 5.097945154717048233, 1.425953928781589886, 1.569717048080176314 ) ) ;
#88590=CARTESIAN_POINT ( 'NONE',  ( 5.840740251263128791, 0.4172088472891195554, 2.120894824392767664 ) ) ;
#88592=CARTESIAN_POINT ( 'NONE',  ( 4.739718475747470627, 1.836682745182907972, 0.1304020654292817605 ) ) ;
#88595=CARTESIAN_POINT ( 'NONE',  ( 0.06344835015564037617, -1.139564578658038618, 1.315610641012928239 ) ) ;
#88596=FACE_OUTER_BOUND ( 'NONE', #193997, .T. ) ;
#88599=CARTESIAN_POINT ( 'NONE',  ( 4.346650381253648554, 0.5737703434565506466, 2.084106190491950006 ) ) ;
#88603=CARTESIAN_POINT ( 'NONE',  ( 3.081113354808207916, -0.1575343947536785305, -2.156009052512488200 ) ) ;
#88604=CARTESIAN_POINT ( 'NONE',  ( 4.675049781410951510, 0.003005680196035282782, -1.971530341645504780 ) ) ;
#88605=CARTESIAN_POINT ( 'NONE',  ( 3.690549081386824248, -1.031632686913460883, -1.393354295182136715 ) ) ;
#88607=CARTESIAN_POINT ( 'NONE',  ( 0.5213437761196970666, -2.079166062760181788, 0.6930039600180630810 ) ) ;
#88608=CARTESIAN_POINT ( 'NONE',  ( 1.448709080243043124, 2.305037702096077723, 0.1111474144101440020 ) ) ;
#88609=CARTESIAN_POINT ( 'NONE',  ( 3.901680821178232339, -0.6019389665811913925, 1.970883251864594454 ) ) ;
#88610=CARTESIAN_POINT ( 'NONE',  ( 5.847205921155025798, 0.5594960185140216424, -1.859740419532672773 ) ) ;
#88617=CARTESIAN_POINT ( 'NONE',  ( 3.329339556154627289, 0.05228039400686017302, 2.206313527657398854 ) ) ;
#88620=CARTESIAN_POINT ( 'NONE',  ( 0.5493571781046421298, 1.373546829346812714, 1.255761559867879962 ) ) ;
#88621=CARTESIAN_POINT ( 'NONE',  ( -0.02880301295724378360, 1.300294777490899056, -2.522425657339548266 ) ) ;
#88625=CARTESIAN_POINT ( 'NONE',  ( 6.925078400183552141, 7.052169149086129352, 2.642497803771151954 ) ) ;
#88626=CARTESIAN_POINT ( 'NONE',  ( 6.685540632719009224, -0.7820230359689305244, 1.665195522482863399 ) ) ;
#88628=CARTESIAN_POINT ( 'NONE',  ( 2.219669609025213930, -1.999274383190910775, 0.4996674803129513842 ) ) ;
#88633=CARTESIAN_POINT ( 'NONE',  ( 0.9364841293936125854, 2.030268333626069843, 0.3529954148920669277 ) ) ;
#88635=CARTESIAN_POINT ( 'NONE',  ( 4.950658015114751009, -1.558304906039936988, -0.9804572199803849308 ) ) ;
#88640=CARTESIAN_POINT ( 'NONE',  ( 5.742855475442601332, 0.4270144693867898300, 2.165010647329483895 ) ) ;
#88641=CARTESIAN_POINT ( 'NONE',  ( 0.8608787451157871029, -1.566265403972837866, 1.489986575276234460 ) ) ;
#88643=CARTESIAN_POINT ( 'NONE',  ( 0.3516297456669579269, -1.353986107606550471, -1.350798769753497552 ) ) ;
#88644=CARTESIAN_POINT ( 'NONE',  ( 0.6027503803631119039, 1.865048444749048739, 0.7672877736318934883 ) ) ;
#88647=CARTESIAN_POINT ( 'NONE',  ( 6.481121912432155519, -1.750430003815309998, -0.7703581994758443852 ) ) ;
#88649=CARTESIAN_POINT ( 'NONE',  ( 1.428351348257720588, 1.801920623737063520, 0.5021531274154652502 ) ) ;
#88650=CARTESIAN_POINT ( 'NONE',  ( 2.835173002801576914, -1.651343842416473917, -1.157098616274463865 ) ) ;
#88654=CARTESIAN_POINT ( 'NONE',  ( 4.846364118386396136, 2.100373345016784743, 0.1556085008114059531 ) ) ;
#88659=CARTESIAN_POINT ( 'NONE',  ( 4.219013726799848207, 1.558537513506755845, -1.284668789120123833 ) ) ;
#88661=CARTESIAN_POINT ( 'NONE',  ( 6.461391904901197414, 1.712781507706350848, 1.149079448644703350 ) ) ;
#88663=CARTESIAN_POINT ( 'NONE',  ( 5.009125465012424172, 1.878017946038791575, 1.070212309444783294 ) ) ;
#88670=CARTESIAN_POINT ( 'NONE',  ( 1.908858375081338377, 0.6798548000985217277, 2.062075944584631504 ) ) ;
#88672=CARTESIAN_POINT ( 'NONE',  ( 1.927068723821170559, -1.203646435588998420, -1.393412863611859454 ) ) ;
#88675=CARTESIAN_POINT ( 'NONE',  ( 2.806388347806953121, 1.585463108415147149, -1.513251884624075672 ) ) ;
#88677=CARTESIAN_POINT ( 'NONE',  ( 3.397619368019880959, 1.782376118940771637, 1.393485768503288202 ) ) ;
#88683=CARTESIAN_POINT ( 'NONE',  ( 5.290226454957744018, -1.756441682966399132, -0.2160651130965525468 ) ) ;
#88685=CARTESIAN_POINT ( 'NONE',  ( 2.133940825901488481, -1.375048162780323935, -1.595187971101755364 ) ) ;
#88688=CARTESIAN_POINT ( 'NONE',  ( 1.258185455790395979, -1.969739565659900160, -0.003359478883382254876 ) ) ;
#88691=CARTESIAN_POINT ( 'NONE',  ( 5.554893708145399067, 0.3617622393776204204, 1.774916939089685730 ) ) ;
#88697=CARTESIAN_POINT ( 'NONE',  ( 4.311305935566238645, -0.3199438451688824125, 1.842931056080451935 ) ) ;
#88698=CARTESIAN_POINT ( 'NONE',  ( 5.172746982222708567, 1.431596967658786745, -1.495705434250683918 ) ) ;
#88709=CARTESIAN_POINT ( 'NONE',  ( 4.580490334204036174, 1.208584658811951762, -1.545285769342201965 ) ) ;
#88711=CARTESIAN_POINT ( 'NONE',  ( 2.038435264984053585, 1.930122609968443204, -0.5825652091262025767 ) ) ;
#88714=CARTESIAN_POINT ( 'NONE',  ( 0.3280006606478855224, 1.121390616443746602, -1.882787531365101685 ) ) ;
#88716=CARTESIAN_POINT ( 'NONE',  ( 1.967826412060974084, 0.9573937279930484490, 1.606809688844474726 ) ) ;
#88718=CARTESIAN_POINT ( 'NONE',  ( 4.623295736497193609, 1.753618999902604614, 0.9886709913553303197 ) ) ;
#88721=CARTESIAN_POINT ( 'NONE',  ( 3.269268187362909028, 1.912946029434154038, -0.9076713616091285353 ) ) ;
#88724=CARTESIAN_POINT ( 'NONE',  ( 5.160626937512653001, -0.6942339714755951796, -1.950645400549338104 ) ) ;
#88725=CARTESIAN_POINT ( 'NONE',  ( 1.540690653510309538, -1.764467595836321401, 1.121255944808132288 ) ) ;
#88726=CARTESIAN_POINT ( 'NONE',  ( 6.720655732516679137, 3.688991442244013097, 2.587785764416630219 ) ) ;
#88727=CARTESIAN_POINT ( 'NONE',  ( 6.405291383686446238, 1.519602032305459538, 1.011395407323860907 ) ) ;
#88735=CARTESIAN_POINT ( 'NONE',  ( 5.936178161767468708, -1.066166440211462563, -1.587280745415058814 ) ) ;
#88743=CARTESIAN_POINT ( 'NONE',  ( 5.782827418265350516, 1.646828846085298448, -1.163285542026312847 ) ) ;
#88744=CARTESIAN_POINT ( 'NONE',  ( -0.02259406399240069044, -1.896172633340575064, -0.9493637518730789759 ) ) ;
#88749=CARTESIAN_POINT ( 'NONE',  ( 3.608217298448283206, 1.969629311412910866, 0.004557946788486669405 ) ) ;
#88750=CARTESIAN_POINT ( 'NONE',  ( 4.077750037130567939, -0.7691059624741981571, 1.864175985064358665 ) ) ;
#88752=CARTESIAN_POINT ( 'NONE',  ( 6.727182134110178069, 2.947419669445831669, 2.641212418657997496 ) ) ;
#88754=CARTESIAN_POINT ( 'NONE',  ( 4.681673494351117348, -1.034495392153191418, 1.931897795048514554 ) ) ;
#88756=CARTESIAN_POINT ( 'NONE',  ( 2.784106279807782247, -0.9919383200396988398, 1.651252367177785230 ) ) ;
#88758=CARTESIAN_POINT ( 'NONE',  ( -0.02988540731099428513, 6.948706544289728448, -2.321349141872154132 ) ) ;
#88759=CARTESIAN_POINT ( 'NONE',  ( 0.1005910224048736229, -2.206496634663042133, -0.04943112074598519229 ) ) ;
#88766=CARTESIAN_POINT ( 'NONE',  ( -0.09434409087969403140, -0.8304652339055562660, -1.753633067539569490 ) ) ;
#88767=CARTESIAN_POINT ( 'NONE',  ( 3.070950286465543577, -1.523008450377001832, 1.316504112208529920 ) ) ;
#88768=CARTESIAN_POINT ( 'NONE',  ( 5.220190998831037987, -1.937735447606624639, -1.235822935930783517 ) ) ;
#88770=CARTESIAN_POINT ( 'NONE',  ( 3.449909520549806707, -0.7582208578979282576, 1.699682486939468440 ) ) ;
#88773=CARTESIAN_POINT ( 'NONE',  ( 6.258066496116281741, 0.7254575739856858885, -1.769658340881982816 ) ) ;
#88776=CARTESIAN_POINT ( 'NONE',  ( 5.847236579984706140, 0.6061975457797988964, -2.000951093856804253 ) ) ;
#88781=CARTESIAN_POINT ( 'NONE',  ( 0.06470675514189982991, -1.629034059718449834, -0.8243793580787887043 ) ) ;
#88783=CARTESIAN_POINT ( 'NONE',  ( 2.988574679986736093, -1.732066829584472556, 0.08781845822969887305 ) ) ;
#88788=CARTESIAN_POINT ( 'NONE',  ( 0.5146170122050791607, 0.7890519337857507809, 1.914186188738425942 ) ) ;
#88789=CARTESIAN_POINT ( 'NONE',  ( 5.426323838365306074, 1.084245000580752238, -1.468710674947353967 ) ) ;
#88790=CARTESIAN_POINT ( 'NONE',  ( 3.168751141962049989, 1.424179589570490512, -1.349414796185027576 ) ) ;
#88794=CARTESIAN_POINT ( 'NONE',  ( 4.002672028760116518, -2.097606743168555443, -0.3097674545872729501 ) ) ;
#88797=CARTESIAN_POINT ( 'NONE',  ( 2.008725816923035978, 0.6454906730102347723, 1.967154155859623055 ) ) ;
#88798=CARTESIAN_POINT ( 'NONE',  ( 6.827182134110199030, 7.629137130509070275, 2.410944104600701188 ) ) ;
#88800=CARTESIAN_POINT ( 'NONE',  ( 4.213700991847090016, 1.784230803775087137, 1.322971166850190450 ) ) ;
#88802=CARTESIAN_POINT ( 'NONE',  ( 2.127932615311285414, 0.5078372532463393263, 2.241765503411979221 ) ) ;
#88804=CARTESIAN_POINT ( 'NONE',  ( 6.578975509608026684, 1.922407110116808981, 0.7477742492353837145 ) ) ;
#88809=CARTESIAN_POINT ( 'NONE',  ( 6.304252605626877504, 1.359535501544101077, -1.241908024382516240 ) ) ;
#88811=CARTESIAN_POINT ( 'NONE',  ( 3.252119977711815491, 0.8557668478980616777, -1.710280963351323846 ) ) ;
#88812=CARTESIAN_POINT ( 'NONE',  ( -0.1106727585416019261, 7.629137130509112907, -2.603481208547548054 ) ) ;
#88813=CARTESIAN_POINT ( 'NONE',  ( 4.330854930063167352, 0.08572247821646634958, 1.722753318990229099 ) ) ;
#88814=CARTESIAN_POINT ( 'NONE',  ( 2.870327622459168726, -1.987497926849005836, -0.3399570244180456502 ) ) ;
#88816=CARTESIAN_POINT ( 'NONE',  ( 3.604340556743702795, -0.1682163741436558391, 2.292568252494499692 ) ) ;
#88817=CARTESIAN_POINT ( 'NONE',  ( 3.901889172025752472, -0.6612649319669267056, 2.163591406342895596 ) ) ;
#88818=CARTESIAN_POINT ( 'NONE',  ( 6.727182134110234024, -0.002100931800118072384, 2.089081857379895268 ) ) ;
#88820=VERTEX_POINT ( 'NONE', #37846 ) ;
#88821=CARTESIAN_POINT ( 'NONE',  ( 4.868267778354250730, -1.156333057219432581, 1.339767963349105528 ) ) ;
#88825=CARTESIAN_POINT ( 'NONE',  ( 0.7270408775228944798, 0.1741418271693234987, 2.285704298519490862 ) ) ;
#88826=CARTESIAN_POINT ( 'NONE',  ( 5.841722611436679813, 1.839261846420519930, 0.08593139445873398952 ) ) ;
#88828=CARTESIAN_POINT ( 'NONE',  ( 6.035146784841348477, -1.584849238314169240, -1.513754250258770639 ) ) ;
#88832=CARTESIAN_POINT ( 'NONE',  ( 6.303194806757332458, -1.751150776259063457, 1.104182018118210262 ) ) ;
#88833=CARTESIAN_POINT ( 'NONE',  ( 0.07540816263147330500, 1.497505997221737273, 1.350731191893522976 ) ) ;
#88835=CARTESIAN_POINT ( 'NONE',  ( 3.773980605468800320, 1.071039916736727937, 1.601146377209327731 ) ) ;
#88837=CARTESIAN_POINT ( 'NONE',  ( 1.336510806674645391, -1.239524924825789132, -1.843257696707498061 ) ) ;
#88847=CARTESIAN_POINT ( 'NONE',  ( 2.418345249890076154, 0.8361516037145629854, 1.774881043358336630 ) ) ;
#88852=CARTESIAN_POINT ( 'NONE',  ( 6.443807124430430910, 1.351966286592180211, 1.421895456074427688 ) ) ;
#88856=CARTESIAN_POINT ( 'NONE',  ( 0.4271420986578051138, 2.166143833277152542, 0.6532491227348672380 ) ) ;
#88858=ORIENTED_EDGE ( 'NONE', *, *, #141701, .T. ) ;
#88860=CARTESIAN_POINT ( 'NONE',  ( 1.440467042440606749, 0.3595057747620767907, 1.835501880432292010 ) ) ;
#88861=CARTESIAN_POINT ( 'NONE',  ( 0.2109833617158912156, 1.658496975328831891, 0.5066527762955413960 ) ) ;
#88863=CARTESIAN_POINT ( 'NONE',  ( 4.318054327947466575, 1.347776305887092185, -1.728067674571641898 ) ) ;
#88864=CARTESIAN_POINT ( 'NONE',  ( 5.245303717312764569, -1.982421492789496753, 1.180877550764187545 ) ) ;
#88865=CARTESIAN_POINT ( 'NONE',  ( 0.3388364525104338165, 0.3516977924403408284, 2.030485180972623205 ) ) ;
#88866=CARTESIAN_POINT ( 'NONE',  ( 2.607286591753724014, -1.920749920159558810, 0.2854125566163211447 ) ) ;
#88871=CARTESIAN_POINT ( 'NONE',  ( 3.551407868487792552, -1.352154898762620849, 1.496051317864899088 ) ) ;
#88875=CARTESIAN_POINT ( 'NONE',  ( 0.6096330727367264002, -1.817201089070449971, 0.1759225495863714350 ) ) ;
#88881=CARTESIAN_POINT ( 'NONE',  ( 5.647358743468454456, -1.623080139260910437, -1.269863021155111849 ) ) ;
#88886=CARTESIAN_POINT ( 'NONE',  ( 5.918619479961092722, -0.7289874232782632690, -1.883701229315833059 ) ) ;
#88887=CARTESIAN_POINT ( 'NONE',  ( 5.707756388377941192, 1.680692789272177468, 1.452518960167401341 ) ) ;
#88891=CARTESIAN_POINT ( 'NONE',  ( 5.840714686760185792, 0.3996242267790580116, 2.021590886677153254 ) ) ;
#88892=CARTESIAN_POINT ( 'NONE',  ( 4.307267641921147749, 1.238321930042911578, -1.591317616567271775 ) ) ;
#88899=CARTESIAN_POINT ( 'NONE',  ( 3.936874915731437774, 1.117662071392529377, 1.677747830363854664 ) ) ;
#88900=CARTESIAN_POINT ( 'NONE',  ( 3.697050842446505392, -0.5329721798031424873, 1.762307204009383454 ) ) ;
#88902=CARTESIAN_POINT ( 'NONE',  ( 2.385774557197326562, 2.109090111016972191, -0.9369807928535575092 ) ) ;
#88904=CARTESIAN_POINT ( 'NONE',  ( 3.427187520701843404, 0.04928524951339217919, 2.161187641841005647 ) ) ;
#88905=CARTESIAN_POINT ( 'NONE',  ( 3.327361509216096191, -1.530157842762596143, -1.313544516083162028 ) ) ;
#88908=CARTESIAN_POINT ( 'NONE',  ( 3.655889646864494580, -0.4445778678274399098, -2.254845314064676032 ) ) ;
#88910=CARTESIAN_POINT ( 'NONE',  ( 2.518242125168220102, 1.223528130051700025, -1.415109699333151561 ) ) ;
#88911=CARTESIAN_POINT ( 'NONE',  ( 6.350460794227542394, 0.6179267841925452087, 1.872200446973372179 ) ) ;
#88915=CARTESIAN_POINT ( 'NONE',  ( 1.454063653991678473, 0.6380318336138122159, -2.112638918738508398 ) ) ;
#88921=CARTESIAN_POINT ( 'NONE',  ( 6.157099186568592231, -1.690597638883487797, -1.013973547023840460 ) ) ;
#88922=CARTESIAN_POINT ( 'NONE',  ( 5.303480822065511191, 1.883932040028640786, 1.332532017187069817 ) ) ;
#88923=CARTESIAN_POINT ( 'NONE',  ( 0.7484013653801385724, -1.946605496936428370, -0.2438083268051088881 ) ) ;
#88924=CARTESIAN_POINT ( 'NONE',  ( 2.782143433959896051, -1.183836405090990640, -1.688839807681275174 ) ) ;
#88930=CARTESIAN_POINT ( 'NONE',  ( 0.3214382364499007161, -1.938747691508705184, -0.9774007134471692781 ) ) ;
#88933=CARTESIAN_POINT ( 'NONE',  ( 4.669393045487420402, 1.064170941109745305, 1.502380130741477693 ) ) ;
#88935=CARTESIAN_POINT ( 'NONE',  ( 6.620655732516620873, 0.004685112605665174221, 1.926407831898164558 ) ) ;
#88936=CARTESIAN_POINT ( 'NONE',  ( 6.620655732516649294, -0.005281389526671945688, 2.273887028200880511 ) ) ;
#88938=CARTESIAN_POINT ( 'NONE',  ( 0.9137757228094539608, -0.3311857980235459742, 2.237941903941061739 ) ) ;
#88942=CARTESIAN_POINT ( 'NONE',  ( 0.02974158317493520720, -1.875378228685410376, 0.3729384364157954379 ) ) ;
#88943=CARTESIAN_POINT ( 'NONE',  ( 1.533702468213002712, 0.8761213712049474855, -1.537698828099523629 ) ) ;
#88944=CARTESIAN_POINT ( 'NONE',  ( 6.481113961022470171, -1.841437297342415791, -0.8137991234780891370 ) ) ;
#88946=CARTESIAN_POINT ( 'NONE',  ( 3.374530662324583652, -0.3768237823980990497, -1.877989258545700535 ) ) ;
#88948=CARTESIAN_POINT ( 'NONE',  ( 4.809023018811155126, -1.583041700261601958, 1.171600654023413624 ) ) ;
#88949=CARTESIAN_POINT ( 'NONE',  ( 0.3344391967911933272, -1.139684030083350841, -1.788147294700337397 ) ) ;
#88951=CARTESIAN_POINT ( 'NONE',  ( 3.080767038946086611, -0.1360980058115155988, -1.865751385159146070 ) ) ;
#88952=CARTESIAN_POINT ( 'NONE',  ( 5.865779507164840645, 1.698138087647281358, -0.3015940010741220978 ) ) ;
#88954=CARTESIAN_POINT ( 'NONE',  ( 2.420803835572300500, 1.440536793087299205, -1.671967039616916617 ) ) ;
#88958=CARTESIAN_POINT ( 'NONE',  ( 0.9067701044400799937, 0.5968461685175918685, 1.974459182335401186 ) ) ;
#88965=CARTESIAN_POINT ( 'NONE',  ( 2.629418614236479712, 0.1040367438073786233, -2.067886086930009970 ) ) ;
#88969=CARTESIAN_POINT ( 'NONE',  ( 1.260422244424246108, 2.017472913078500518, 0.09673469748067325957 ) ) ;
#88972=CARTESIAN_POINT ( 'NONE',  ( 0.07499057489262526965, 5.723988098492513998, -2.549530206576706259 ) ) ;
#88974=CARTESIAN_POINT ( 'NONE',  ( 4.956407584168041502, 1.492027487219639514, 1.356091576722208369 ) ) ;
#88975=CARTESIAN_POINT ( 'NONE',  ( 5.788286065124909285, -0.6962570634414954052, -1.784894364769493924 ) ) ;
#88977=CARTESIAN_POINT ( 'NONE',  ( 4.247736854543925133, 2.191053489037126045, -0.05455935714590579022 ) ) ;
#88980=CARTESIAN_POINT ( 'NONE',  ( 2.021601768330282045, -0.4154675118966509317, 1.866563793090275203 ) ) ;
#88985=CARTESIAN_POINT ( 'NONE',  ( 1.001577623981730891, -1.966640429010723112, 0.4445266750975271353 ) ) ;
#88987=CARTESIAN_POINT ( 'NONE',  ( 5.899973326018037589, -0.7874313895239596350, -2.045375389432432467 ) ) ;
#88989=CARTESIAN_POINT ( 'NONE',  ( 2.660839013829336075, -1.499436941970986759, -0.8522202921518050589 ) ) ;
#88991=CARTESIAN_POINT ( 'NONE',  ( 6.082307721193076944, 1.091511717630256673, 1.817998432235830908 ) ) ;
#88995=CARTESIAN_POINT ( 'NONE',  ( 0.2386218892466463737, -1.902018210125755004, -0.4804332253167050149 ) ) ;
#89002=CARTESIAN_POINT ( 'NONE',  ( 3.193826918316445163, 1.151326796633693084, 1.398496967315324246 ) ) ;
#89007=CARTESIAN_POINT ( 'NONE',  ( 4.301270310059371660, 1.616194109774160559, -0.8183029847002845081 ) ) ;
#89011=CARTESIAN_POINT ( 'NONE',  ( 5.353892109531869004, -0.6699537489362316078, 1.736457084658560079 ) ) ;
#89013=CARTESIAN_POINT ( 'NONE',  ( 2.231924035814872642, 1.915248681264541508, 0.04463030589317053265 ) ) ;
#89023=CARTESIAN_POINT ( 'NONE',  ( 1.851626064562774010, 2.084957031469181654, -0.1549042654368226746 ) ) ;
#89025=CARTESIAN_POINT ( 'NONE',  ( 6.159198499077391808, -1.652456008184695735, -0.9899348748576908275 ) ) ;
#89027=CARTESIAN_POINT ( 'NONE',  ( 2.151128115021032627, -1.464471472660273665, -1.089769533225225073 ) ) ;
#89029=CARTESIAN_POINT ( 'NONE',  ( 0.7559434568639655794, 0.7726834774516875282, -1.749509110286852742 ) ) ;
#89030=CARTESIAN_POINT ( 'NONE',  ( 2.084365741702984387, 1.136530121079984301, -1.608336531363078414 ) ) ;
#89031=CARTESIAN_POINT ( 'NONE',  ( 3.614730616327064716, -0.1400294986239834782, 1.937054734790619293 ) ) ;
#89035=CARTESIAN_POINT ( 'NONE',  ( 0.1505322013598429098, -0.3980627942141829467, -1.824191605747552014 ) ) ;
#89044=CARTESIAN_POINT ( 'NONE',  ( 3.949673224339702138, 0.6133576713117370183, -1.719707012317383432 ) ) ;
#89045=CARTESIAN_POINT ( 'NONE',  ( 5.946499988598237252, -1.422611626450220434, 1.429444749906971790 ) ) ;
#89050=CARTESIAN_POINT ( 'NONE',  ( 5.102362337376947998, -0.6309395149336484154, -1.761181640970375106 ) ) ;
#89052=CARTESIAN_POINT ( 'NONE',  ( 1.682126184939515934, -1.031041751839639087, 1.627202258603721363 ) ) ;
#89053=CARTESIAN_POINT ( 'NONE',  ( 6.455910365318025868, -0.6640748382394038307, 1.846044136633723243 ) ) ;
#89059=CARTESIAN_POINT ( 'NONE',  ( 0.1228732512454956405, 0.3668972607131052999, 2.085061435120295847 ) ) ;
#89062=CARTESIAN_POINT ( 'NONE',  ( 4.698136132249701724, 0.8899761679339033282, -1.869364561350304488 ) ) ;
#89063=CARTESIAN_POINT ( 'NONE',  ( 0.3800845246329161431, -0.2246070939678334044, -1.827447590993152682 ) ) ;
#89065=CARTESIAN_POINT ( 'NONE',  ( 5.151170688231202277, 1.131463054214848940, 2.000911673594136797 ) ) ;
#89069=CARTESIAN_POINT ( 'NONE',  ( 0.6742756655733075366, -1.268823270132292791, 1.908895542103898890 ) ) ;
#89073=CARTESIAN_POINT ( 'NONE',  ( 5.033120997586177481, -1.374529083251808892, -1.372050024763036280 ) ) ;
#89077=CARTESIAN_POINT ( 'NONE',  ( 6.135011676971934058, 1.786887936952135991, 0.6819008164158719687 ) ) ;
#89078=CARTESIAN_POINT ( 'NONE',  ( 5.770720322323381168, -0.3006437417610394736, -1.993894057904864514 ) ) ;
#89082=CARTESIAN_POINT ( 'NONE',  ( 2.414113337891873101, 1.364997783657854846, -1.583610807417460631 ) ) ;
#89083=CARTESIAN_POINT ( 'NONE',  ( 1.656752475421595872, -1.515787608549432175, -0.9133899773908128461 ) ) ;
#89085=CARTESIAN_POINT ( 'NONE',  ( 6.610000000000006537, 0.002781820520842553934, 2.000159646111852929 ) ) ;
#89088=CARTESIAN_POINT ( 'NONE',  ( 4.347812307665041232, 2.291787294364412642, -0.05403505903618135986 ) ) ;
#89089=CARTESIAN_POINT ( 'NONE',  ( 1.798380396644788659, 1.445777515557338688, 0.9684012028719732879 ) ) ;
#89092=CARTESIAN_POINT ( 'NONE',  ( 2.547823072707461112, 1.587006686370129316, -0.6987220570618419835 ) ) ;
#89094=CARTESIAN_POINT ( 'NONE',  ( 1.679899622522099012, -1.030144609347281026, -1.549723197825584764 ) ) ;
#89096=CARTESIAN_POINT ( 'NONE',  ( 2.436178610684522461, 1.334241001675811500, 1.712780914784496122 ) ) ;
#89098=CARTESIAN_POINT ( 'NONE',  ( 4.259000112335223243, -0.004834882008357410665, -2.016708403958865414 ) ) ;
#89099=CARTESIAN_POINT ( 'NONE',  ( 3.343750000000002220, 1.895863743164157178, 0.7852924748298092394 ) ) ;
#89101=CARTESIAN_POINT ( 'NONE',  ( 0.5516240470409677910, 0.6072917441693607143, -1.828224634575502883 ) ) ;
#89103=CARTESIAN_POINT ( 'NONE',  ( 4.658541260611516854, 2.215511418189203496, 0.1622135575486300108 ) ) ;
#89108=CARTESIAN_POINT ( 'NONE',  ( 0.4346306299643958315, -1.193539479193185038, -1.873246666896864143 ) ) ;
#89109=CARTESIAN_POINT ( 'NONE',  ( 5.248475795274027078, -1.946838731704622072, -0.2419367024937419397 ) ) ;
#89112=CARTESIAN_POINT ( 'NONE',  ( 6.239586896912570069, -1.632293121298231675, -1.566800261409779349 ) ) ;
#89114=CARTESIAN_POINT ( 'NONE',  ( 2.998538507119326901, 2.046783137066817027, 0.2552134970664684532 ) ) ;
#89119=CARTESIAN_POINT ( 'NONE',  ( 4.921099816907485547, -0.09337705715995943401, 1.868355541605345671 ) ) ;
#89120=CARTESIAN_POINT ( 'NONE',  ( 3.463219708433932009, -1.672243815576504700, -0.4589255088537134153 ) ) ;
#89121=CARTESIAN_POINT ( 'NONE',  ( 3.667295640872432649, 0.9703414817801876424, 1.444613691174992720 ) ) ;
#89122=CARTESIAN_POINT ( 'NONE',  ( 1.171857018789014271, 1.370485515009724820, 1.837452469633732210 ) ) ;
#89124=CARTESIAN_POINT ( 'NONE',  ( 4.493745196466782943, -2.090321524099489903, -0.04957026750533782833 ) ) ;
#89125=CARTESIAN_POINT ( 'NONE',  ( 5.331954954513311584, 1.913531179151845674, 0.3301462080481341599 ) ) ;
#89128=CARTESIAN_POINT ( 'NONE',  ( 0.8092204703840089053, 1.198858234535697065, -1.621184076614573533 ) ) ;
#89129=CARTESIAN_POINT ( 'NONE',  ( 0.4926326669930108371, -1.172979896111199904, 1.766458537607276114 ) ) ;
#89134=CARTESIAN_POINT ( 'NONE',  ( 2.244932509249154329, 2.057497683098849617, 0.5125483897536405875 ) ) ;
#89136=CARTESIAN_POINT ( 'NONE',  ( 4.072732355924274295, -1.704239406772959153, -0.6552279023967976235 ) ) ;
#89142=CARTESIAN_POINT ( 'NONE',  ( 2.074478865019005802, 0.8673736069498124701, 1.824228476594942583 ) ) ;
#89143=CARTESIAN_POINT ( 'NONE',  ( 5.649526978565787338, -1.736373965863503122, -1.361823127433124725 ) ) ;
#89145=CARTESIAN_POINT ( 'NONE',  ( 3.274093294390582276, -0.9130387472845059582, -1.621452132119176159 ) ) ;
#89151=CARTESIAN_POINT ( 'NONE',  ( 5.197797600609998625, -0.6536857159176562293, 1.704833070275885598 ) ) ;
#89156=CARTESIAN_POINT ( 'NONE',  ( 0.7195771044254402060, -1.460395948178545344, -0.9342476737749583204 ) ) ;
#89157=CARTESIAN_POINT ( 'NONE',  ( 0.3041415704291222100, 1.511679331021776207, 0.8621369596173468208 ) ) ;
#89158=CARTESIAN_POINT ( 'NONE',  ( 5.778008146871475681, 1.369946362297723264, 1.856932335381543897 ) ) ;
#89160=CARTESIAN_POINT ( 'NONE',  ( 0.6673476085290538373, 0.2044725723429566266, -2.050631486922994906 ) ) ;
#89162=CARTESIAN_POINT ( 'NONE',  ( 5.167441833834662823, -0.7673274391166631236, -2.166651051963175423 ) ) ;
#89165=CARTESIAN_POINT ( 'NONE',  ( 5.840666405660361882, 0.3664468388623157158, 1.834233659845653897 ) ) ;
#89168=CARTESIAN_POINT ( 'NONE',  ( 3.480628297764537304, -1.280852673386581264, 1.420289963180096260 ) ) ;
#89170=CARTESIAN_POINT ( 'NONE',  ( 5.584669497696876483, -2.152379054646291756, -0.4867646435422824935 ) ) ;
#89171=CARTESIAN_POINT ( 'NONE',  ( 5.050072346573388771, 1.046394516673061270, 1.840669678815173960 ) ) ;
#89176=CARTESIAN_POINT ( 'NONE',  ( 5.479186192515411946, -1.917069751554843160, -0.9065152316691318379 ) ) ;
#89177=CARTESIAN_POINT ( 'NONE',  ( 2.327567518148494941, 0.0001997265634129384874, 2.307758715027211416 ) ) ;
#89178=CARTESIAN_POINT ( 'NONE',  ( 3.455471728117681440, 1.544996161402897528, 1.208956721487665087 ) ) ;
#89180=CARTESIAN_POINT ( 'NONE',  ( 1.305434336737832490, -1.543085766649286317, -1.211208057394968618 ) ) ;
#89184=CARTESIAN_POINT ( 'NONE',  ( 5.507046092540283766, -0.04465857163906890998, 2.016188657829049991 ) ) ;
#89188=CARTESIAN_POINT ( 'NONE',  ( 3.362351297888244606, -2.168775535925556053, 0.1018362995675748534 ) ) ;
#89190=CARTESIAN_POINT ( 'NONE',  ( 0.3520121086563637314, -1.504009422257305495, -1.495223887398588358 ) ) ;
#89195=CARTESIAN_POINT ( 'NONE',  ( 0.8255485222598609729, -1.957653584835903349, 0.6440290526678188465 ) ) ;
#89200=CARTESIAN_POINT ( 'NONE',  ( 2.965378323150099416, -1.564627974442783120, -1.099164922500090347 ) ) ;
#89201=CARTESIAN_POINT ( 'NONE',  ( 5.295665003108637414, -0.6346038033320391403, 1.652335088206556613 ) ) ;
#89204=CARTESIAN_POINT ( 'NONE',  ( 0.08776524826303951088, 1.042983370315919478, 1.480986741271082430 ) ) ;
#89206=CARTESIAN_POINT ( 'NONE',  ( 0.9014164429375628451, -1.868237418080781254, 0.4230343950424199084 ) ) ;
#89207=CARTESIAN_POINT ( 'NONE',  ( 2.506376218629560171, 2.069854378281150709, 0.05321039126485183068 ) ) ;
#89210=CARTESIAN_POINT ( 'NONE',  ( 6.174654088403855212, -1.776896415251895789, -0.5849557326117056366 ) ) ;
#89211=CARTESIAN_POINT ( 'NONE',  ( 2.420285107995377327, 1.192830232448302441, -1.382225081888274643 ) ) ;
#89212=CARTESIAN_POINT ( 'NONE',  ( 6.094375512030342001, -2.195847865938059140, -0.2203403561373064590 ) ) ;
#89216=CARTESIAN_POINT ( 'NONE',  ( 3.631348232279749233, 0.05352869315983609100, -2.062151203995182147 ) ) ;
#89221=CARTESIAN_POINT ( 'NONE',  ( 6.144996677366851401, -0.2998803957653916608, -2.048400609436632269 ) ) ;
#89223=CARTESIAN_POINT ( 'NONE',  ( 3.813887338145681927, -2.130327034543195275, 0.3653767458386343314 ) ) ;
#89224=CARTESIAN_POINT ( 'NONE',  ( 3.756514258062096712, 2.010158954970509892, 0.1956256540626959695 ) ) ;
#89232=CARTESIAN_POINT ( 'NONE',  ( 2.712125330650519750, 1.116209241849321465, -1.679223868463100011 ) ) ;
#89236=CARTESIAN_POINT ( 'NONE',  ( 5.590081826628392925, 1.144292256163012667, 1.532101299821154949 ) ) ;
#89240=CARTESIAN_POINT ( 'NONE',  ( 4.042592340535226647, -1.492244431823461115, 1.356313616978216618 ) ) ;
#89243=CARTESIAN_POINT ( 'NONE',  ( 6.317413179709785886, -0.2053877530918957195, 1.712446389806308256 ) ) ;
#89247=CARTESIAN_POINT ( 'NONE',  ( 4.376139848268215893, -1.078761963904120602, 1.527931137620001989 ) ) ;
#89249=CARTESIAN_POINT ( 'NONE',  ( 1.850524992189076290, -2.059912964915584954, -0.2069831422613493399 ) ) ;
#89253=CARTESIAN_POINT ( 'NONE',  ( 0.3336115229473045618, 0.6298545048411038350, -1.915608025624820909 ) ) ;
#89255=CARTESIAN_POINT ( 'NONE',  ( 0.8260602286952464235, -0.8153974433127196830, -1.617802387155008681 ) ) ;
#89257=CIRCLE ( 'NONE', #172281, 0.04999999999999969746 ) ;
#89262=CARTESIAN_POINT ( 'NONE',  ( 6.327746003090493510, 0.7280626223893000848, -1.772066133663487530 ) ) ;
#89269=CARTESIAN_POINT ( 'NONE',  ( 3.309602206082487008, -0.4233974974612622066, 2.119663826602156131 ) ) ;
#89273=CARTESIAN_POINT ( 'NONE',  ( 1.019968326173793960, -0.5097545255977400380, 2.058319881341897695 ) ) ;
#89274=CARTESIAN_POINT ( 'NONE',  ( 5.772426501671442445, -1.156275361458743545, 1.412693073426966039 ) ) ;
#89276=CARTESIAN_POINT ( 'NONE',  ( 2.618384893494442256, 1.290362544248652599, -1.490430290494165755 ) ) ;
#89277=CARTESIAN_POINT ( 'NONE',  ( 4.341997288149157086, -1.180789491531178292, -1.504210074635865757 ) ) ;
#89280=CARTESIAN_POINT ( 'NONE',  ( 5.178159682156908694, -1.051918566972683600, -1.664904379343169705 ) ) ;
#89281=CARTESIAN_POINT ( 'NONE',  ( 0.7088029311262042942, -0.2857661853880436031, 1.920690660100693226 ) ) ;
#89288=CARTESIAN_POINT ( 'NONE',  ( 0.6576010401811819284, -1.865379905010958517, -1.178792301215730642 ) ) ;
#89290=CARTESIAN_POINT ( 'NONE',  ( -0.07574839183086683192, -0.8175154495408327726, -1.727131953450977253 ) ) ;
#89291=CARTESIAN_POINT ( 'NONE',  ( 0.07661050522430808141, 2.897279719329011627, -2.199986835335824953 ) ) ;
#89293=CARTESIAN_POINT ( 'NONE',  ( 5.717982508692024624, 0.9896897593998502662, -1.756851901128737348 ) ) ;
#89294=CARTESIAN_POINT ( 'NONE',  ( 1.943885480841448965, 1.426152643941134501, 1.501071833787496645 ) ) ;
#89297=CARTESIAN_POINT ( 'NONE',  ( 0.3390366800232989530, 0.3710982241871863541, 2.129449491308422537 ) ) ;
#89303=CARTESIAN_POINT ( 'NONE',  ( 6.825078400183572036, 7.053423702906556514, 2.353807037893948628 ) ) ;
#89305=CARTESIAN_POINT ( 'NONE',  ( 4.588316246536889409, -0.4565669943805070186, 1.672893389497135841 ) ) ;
#89309=CARTESIAN_POINT ( 'NONE',  ( 2.553653463975919635, 1.597511423921485818, 1.316731848974454833 ) ) ;
#89310=CARTESIAN_POINT ( 'NONE',  ( 4.833676624637527119, 0.6627930923091308602, -2.010898772050497829 ) ) ;
#89313=CARTESIAN_POINT ( 'NONE',  ( 1.481237898015239418, -0.05359582033081673746, 1.968903824098491073 ) ) ;
#89316=CARTESIAN_POINT ( 'NONE',  ( 4.523529124507605914, -1.408076564469705527, -1.808723714663774240 ) ) ;
#89317=CARTESIAN_POINT ( 'NONE',  ( 1.295219883412350503, 1.381147610352757127, 1.194082977437810333 ) ) ;
#89321=CARTESIAN_POINT ( 'NONE',  ( 2.672137747239998529, 2.003105221038860684, -0.2016864653290161569 ) ) ;
#89322=CARTESIAN_POINT ( 'NONE',  ( 3.414850490325722632, -1.488543670003231068, 1.277929504599809585 ) ) ;
#89326=CARTESIAN_POINT ( 'NONE',  ( 5.964805764622640005, 0.1547682761293242837, -2.084958343724970131 ) ) ;
#89327=CARTESIAN_POINT ( 'NONE',  ( 4.293650081035056409, -0.6766669130573493840, 1.635584247362771304 ) ) ;
#89329=CARTESIAN_POINT ( 'NONE',  ( 1.113517231965298837, -2.137359700923711081, 0.4831916906855234228 ) ) ;
#89330=CARTESIAN_POINT ( 'NONE',  ( 5.542807930227759527, -1.375536301258666105, -1.066015508636003251 ) ) ;
#89333=CARTESIAN_POINT ( 'NONE',  ( 6.276074014454348315, 2.002121775873589637, -1.129333029253890341 ) ) ;
#89335=CARTESIAN_POINT ( 'NONE',  ( 6.098968314571592053, 0.8511620794300640558, -1.510462927660038090 ) ) ;
#89336=CARTESIAN_POINT ( 'NONE',  ( 1.717678464306471309, -0.2677704892378242607, 2.190511422692428045 ) ) ;
#89338=CARTESIAN_POINT ( 'NONE',  ( 5.424361751532248199, 1.065549429306617446, 1.891644033573415040 ) ) ;
#89340=CARTESIAN_POINT ( 'NONE',  ( 0.9193374879241524855, -1.911445915896703207, 0.9111208566532496000 ) ) ;
#89341=CARTESIAN_POINT ( 'NONE',  ( 4.125000000000001776, -2.052068128417945392, 2.349217982248014418E-13 ) ) ;
#89342=CARTESIAN_POINT ( 'NONE',  ( 6.827182134110167055, 4.690515317746113411, 2.651606140002475076 ) ) ;
#89343=CARTESIAN_POINT ( 'NONE',  ( 4.647439542507147081, -1.488915335790324201, -1.222320866314072774 ) ) ;
#89344=CARTESIAN_POINT ( 'NONE',  ( 1.559560479473407701, -1.874198601735496794, 1.192037787016706485 ) ) ;
#89350=CARTESIAN_POINT ( 'NONE',  ( 3.528187740469524769, -2.188240134182100949, 0.3810097408954765119 ) ) ;
#89355=ORIENTED_EDGE ( 'NONE', *, *, #52718, .T. ) ;
#89356=CARTESIAN_POINT ( 'NONE',  ( 2.197888892816081796, 1.802417619043535701, 0.9041091288993635677 ) ) ;
#89358=CARTESIAN_POINT ( 'NONE',  ( 0.3563950589157930393, -2.062029646941070382, -0.05432448973826872057 ) ) ;
#89361=CARTESIAN_POINT ( 'NONE',  ( 0.2394788589213901198, 1.836227513651207177, 0.1364553164684492448 ) ) ;
#89364=CARTESIAN_POINT ( 'NONE',  ( 1.739140684745379195, -1.277452191371928558, -1.225025713498065549 ) ) ;
#89365=CARTESIAN_POINT ( 'NONE',  ( 0.5982800022500452952, -0.2930678230431381648, 1.994870242743536304 ) ) ;
#89366=CARTESIAN_POINT ( 'NONE',  ( 6.392160974223673797, -0.4739405955596608933, -1.674609590779071455 ) ) ;
#89367=CARTESIAN_POINT ( 'NONE',  ( 4.476316811684385222, -2.223409025971525121, -0.5576598666321966880 ) ) ;
#89368=CARTESIAN_POINT ( 'NONE',  ( 3.609164914601064922, -1.813629950718143702, 0.3161406477080672128 ) ) ;
#89370=CARTESIAN_POINT ( 'NONE',  ( 2.625780896952558674, -1.049238153381076177, -1.493741879923994542 ) ) ;
#89371=CARTESIAN_POINT ( 'NONE',  ( 3.692029868468839737, 1.730865839653324079, 1.034166058993556181 ) ) ;
#89373=CARTESIAN_POINT ( 'NONE',  ( 3.503020383517113423, 1.785049946035693891, -1.390086647613536952 ) ) ;
#89375=CARTESIAN_POINT ( 'NONE',  ( 5.245193717270952405, -1.807841653007141947, 1.079916013355223248 ) ) ;
#89377=CARTESIAN_POINT ( 'NONE',  ( 3.684089399883890614, -1.230936008959164996, -1.664559344884769088 ) ) ;
#89380=CARTESIAN_POINT ( 'NONE',  ( 5.848313825214911610, 1.045240856298999432, -1.844880668361434939 ) ) ;
#89383=CARTESIAN_POINT ( 'NONE',  ( 1.242661541247750856, 0.3750627104036097781, 1.889477121596821352 ) ) ;
#89391=CARTESIAN_POINT ( 'NONE',  ( 1.037687956146810198, -0.04753379745526563338, 2.221059295257783006 ) ) ;
#89392=CARTESIAN_POINT ( 'NONE',  ( 2.046058472223175162, 0.8067420340923843192, -1.945513702063914163 ) ) ;
#89395=CARTESIAN_POINT ( 'NONE',  ( 5.963677626732073023, -0.4536248188283693583, 1.804646041804882195 ) ) ;
#89400=CARTESIAN_POINT ( 'NONE',  ( 0.4574861729177078229, -1.815669959853306370, 1.095388807130371900 ) ) ;
#89403=CARTESIAN_POINT ( 'NONE',  ( 3.244534624505683418, -1.932379277470747558, -0.3379807920969243873 ) ) ;
#89404=CARTESIAN_POINT ( 'NONE',  ( 1.639762333045853726, -1.565812861550972324, -1.490595759849028035 ) ) ;
#89405=CARTESIAN_POINT ( 'NONE',  ( 0.9602180038516641147, -1.664555262390180257, -0.7873027242753791732 ) ) ;
#89408=CARTESIAN_POINT ( 'NONE',  ( 3.099246252510225119, -1.738326302361908882, 0.08608614090572026811 ) ) ;
#89412=CARTESIAN_POINT ( 'NONE',  ( 0.9717996764858798375, 2.083101276202529384, -0.5774176476955604764 ) ) ;
#89414=CARTESIAN_POINT ( 'NONE',  ( 2.425157474508771838, 0.8594973679685766754, 1.823840639232063854 ) ) ;
#89417=CARTESIAN_POINT ( 'NONE',  ( 2.325019196037684477, -0.001775356835979901692, 1.971640592446997298 ) ) ;
#89418=CARTESIAN_POINT ( 'NONE',  ( 6.509000000000039421, 2.968845098214093703, 2.453284407971462411 ) ) ;
#89427=CARTESIAN_POINT ( 'NONE',  ( 5.842881032528668861, 0.4426140756379555730, 2.264596805331307472 ) ) ;
#89428=CARTESIAN_POINT ( 'NONE',  ( 6.707479306934847507, -1.574971382793718178, -1.169550641929931079 ) ) ;
#89429=CARTESIAN_POINT ( 'NONE',  ( 4.328923052438288899, -1.828919189252835142, -0.7100325158947774495 ) ) ;
#89431=CARTESIAN_POINT ( 'NONE',  ( 0.2291389764034670318, 2.011204493129043591, 0.1455304468792120720 ) ) ;
#89432=VERTEX_POINT ( 'NONE', #24781 ) ;
#89433=CARTESIAN_POINT ( 'NONE',  ( 2.466138310383278132, -1.084178177903678320, 1.818555153620523779 ) ) ;
#89436=CARTESIAN_POINT ( 'NONE',  ( 2.870863542623874221, 1.748142402769039760, -0.5779331317549916136 ) ) ;
#89439=MANIFOLD_SOLID_BREP ( 'Sweep1[7]', #202089 ) ;
#89440=CARTESIAN_POINT ( 'NONE',  ( 4.096021571020786567, 1.387573888390711385, 1.603661410755026440 ) ) ;
#89441=CARTESIAN_POINT ( 'NONE',  ( 6.714805131850001274, -0.1305238817815305985, 1.911932681171425896 ) ) ;
#89446=CARTESIAN_POINT ( 'NONE',  ( 4.059881558241601240, 2.045671965140416937, -0.2483333800566180083 ) ) ;
#89448=CARTESIAN_POINT ( 'NONE',  ( 1.206327419354651820, 1.623952629372883427, 0.8676893986077349741 ) ) ;
#89454=CARTESIAN_POINT ( 'NONE',  ( 1.629795212970772456, -2.077151576879713080, 0.7458654493318407352 ) ) ;
#89455=CARTESIAN_POINT ( 'NONE',  ( 3.937032273161138463, 0.3271595461276222139, 2.238503835787652996 ) ) ;
#89457=CARTESIAN_POINT ( 'NONE',  ( 3.779414081507098011, 0.2159278537227064809, -1.798573134706340504 ) ) ;
#89458=CARTESIAN_POINT ( 'NONE',  ( 4.768704397049558175, -0.2406929234074564883, -1.900496090682921579 ) ) ;
#89459=CARTESIAN_POINT ( 'NONE',  ( 5.564915762860970894, 1.570151797963925455, -1.349580972669261580 ) ) ;
#89461=CARTESIAN_POINT ( 'NONE',  ( 2.905103271286565647, 1.664600965932877319, 1.056039161509576108 ) ) ;
#89462=CARTESIAN_POINT ( 'NONE',  ( 0.9207747878037384481, 1.778742719161881203, 0.7400954639872597829 ) ) ;
#89463=CARTESIAN_POINT ( 'NONE',  ( 3.871829239884491791, 1.038646522470688671, 1.555605274479121114 ) ) ;
#89464=CARTESIAN_POINT ( 'NONE',  ( 2.930630293717914725, 1.281480123180640529, -1.919000982882083095 ) ) ;
#89465=CARTESIAN_POINT ( 'NONE',  ( 4.088223475482699598, 0.9968510564385362205, -1.571365414726686227 ) ) ;
#89471=CARTESIAN_POINT ( 'NONE',  ( 1.084755975048516285, -2.055113062490296016, -0.4597243831155339300 ) ) ;
#89475=CARTESIAN_POINT ( 'NONE',  ( 1.916421503514931679, -2.120014230100770725, 0.05699577502370903326 ) ) ;
#89477=CARTESIAN_POINT ( 'NONE',  ( 0.5451830133551841540, 0.1527301869948919366, 2.014097447171578903 ) ) ;
#89483=CARTESIAN_POINT ( 'NONE',  ( 0.6675187767142229944, 0.2125181155594977611, -2.151144519195991922 ) ) ;
#89484=CARTESIAN_POINT ( 'NONE',  ( 6.610000000000030518, 1.266345627986571021, 2.115470293623383569 ) ) ;
#89486=CARTESIAN_POINT ( 'NONE',  ( 6.925078400183550364, 2.979478345347879031, 2.309228228758605450 ) ) ;
#89489=CARTESIAN_POINT ( 'NONE',  ( 5.348842313791752900, -1.825074749614737701, -0.8578464102408298597 ) ) ;
#89491=CARTESIAN_POINT ( 'NONE',  ( 0.04676574305502099321, -1.756316032869180921, 1.310637071781264984 ) ) ;
#89494=CARTESIAN_POINT ( 'NONE',  ( 6.596550757224428629, -0.5713381284546023009, -2.084776384472402100 ) ) ;
#89498=CARTESIAN_POINT ( 'NONE',  ( 1.036581048048822673, -1.509151586612084373, 1.179680973199858318 ) ) ;
#89501=CARTESIAN_POINT ( 'NONE',  ( 2.455304126353729188, 0.4608866456157869607, -1.662088558372651903 ) ) ;
#89504=CARTESIAN_POINT ( 'NONE',  ( 2.407162768383603435, -0.3926560375935496672, 1.725441652247063251 ) ) ;
#89506=CARTESIAN_POINT ( 'NONE',  ( 5.210101597250164751, -2.196594437182074255, 0.2116553293704941940 ) ) ;
#89508=CARTESIAN_POINT ( 'NONE',  ( 4.166274539359494433, 2.019258995967411430, -0.05370046678233526827 ) ) ;
#89510=CARTESIAN_POINT ( 'NONE',  ( 4.424552244980545446, -0.9075887007226298708, -1.916591080935086788 ) ) ;
#89511=CARTESIAN_POINT ( 'NONE',  ( 4.482046101484723266, -2.016035353076811809, -0.04666016718203602753 ) ) ;
#89512=CARTESIAN_POINT ( 'NONE',  ( 3.990334445075129466, -1.038098595406260705, 1.484453480236499923 ) ) ;
#89516=CARTESIAN_POINT ( 'NONE',  ( 1.938157646728836614, 1.849873822469105145, 0.2772664081076986475 ) ) ;
#89518=CARTESIAN_POINT ( 'NONE',  ( 5.988875474321468495, -1.722281623382706073, -0.5616633497566495548 ) ) ;
#89528=CARTESIAN_POINT ( 'NONE',  ( 3.955424862866574021, -1.843446357660895041, 1.048082435718917571 ) ) ;
#89529=CARTESIAN_POINT ( 'NONE',  ( -0.1294898018152304819, 0.2484418290887774605, -1.961697698124951650 ) ) ;
#89531=CARTESIAN_POINT ( 'NONE',  ( 5.307875201598577064, -1.962095876955988638, 0.1906144227653387424 ) ) ;
#89533=CARTESIAN_POINT ( 'NONE',  ( 1.160403428290600392, 2.011073784072180182, 0.09471770850632241223 ) ) ;
#89535=CARTESIAN_POINT ( 'NONE',  ( 6.403513597085680686, -2.053302684608013795, 0.5162988180226235624 ) ) ;
#89537=CARTESIAN_POINT ( 'NONE',  ( 1.117730493923989599, 0.4056601665377962407, -2.030061024271647252 ) ) ;
#89541=CARTESIAN_POINT ( 'NONE',  ( 3.802746959959231177, 1.793210335683467216, 1.074525653306056316 ) ) ;
#89544=CARTESIAN_POINT ( 'NONE',  ( 3.205874166558682514, -1.823564452915670042, 0.08818595847179949709 ) ) ;
#89545=CARTESIAN_POINT ( 'NONE',  ( 1.963241191952873388, -1.455257657876586341, -1.078514734469406600 ) ) ;
#89547=CARTESIAN_POINT ( 'NONE',  ( 6.059228469117068805, -1.890744221452178353, -1.137928576693452820 ) ) ;
#89548=AXIS2_PLACEMENT_3D ( 'NONE', #60093, #126252, #39575 ) ;
#89549=CARTESIAN_POINT ( 'NONE',  ( 3.997267248050282884, 1.865803599355109421, -1.178106810156675843 ) ) ;
#89553=CARTESIAN_POINT ( 'NONE',  ( 3.299369280271017946, 1.727720890571235124, -0.8199460011262191816 ) ) ;
#89555=CARTESIAN_POINT ( 'NONE',  ( 6.109843426155950219, 0.6047356833836557977, -1.980059631771100781 ) ) ;
#89557=CARTESIAN_POINT ( 'NONE',  ( 5.583573808894983337, -0.9862700065477579825, 1.957137920222583372 ) ) ;
#89569=CARTESIAN_POINT ( 'NONE',  ( 5.348515126027270306, -2.053966340784090239, -0.2589089449258550890 ) ) ;
#89570=CARTESIAN_POINT ( 'NONE',  ( 4.125552361149776637, -1.843237290211484192, 0.5602470265201089372 ) ) ;
#89571=CARTESIAN_POINT ( 'NONE',  ( 1.599232692168949699, -0.2440074622011619843, 2.001515180871694888 ) ) ;
#89575=CARTESIAN_POINT ( 'NONE',  ( 1.043234067691005684, -1.729537258485489115, -1.345685951901639532 ) ) ;
#89576=CARTESIAN_POINT ( 'NONE',  ( 5.127504350819418910, -1.732488751877172772, 0.5760870007271365889 ) ) ;
#89583=CARTESIAN_POINT ( 'NONE',  ( 2.489598673502769977, -1.836455140896048999, -0.1334285330320400531 ) ) ;
#89584=CARTESIAN_POINT ( 'NONE',  ( 6.469000937953021335, -1.553436082622870140, 1.280157488742767136 ) ) ;
#89585=CARTESIAN_POINT ( 'NONE',  ( 2.161834534229470695, -0.6120774379556602751, -2.215351195248612459 ) ) ;
#89586=CARTESIAN_POINT ( 'NONE',  ( 6.860214158839045950, -1.961385418603446062, 0.04497666117601883257 ) ) ;
#89589=CARTESIAN_POINT ( 'NONE',  ( 2.918110517850933672, -1.910018876965378309, 0.09814724848770939314 ) ) ;
#89591=CARTESIAN_POINT ( 'NONE',  ( 0.2564123431100414074, -2.069877475643782994, -0.05227228806716639753 ) ) ;
#89593=CARTESIAN_POINT ( 'NONE',  ( 2.103177918021365223, -0.4551342947399418248, 2.040444103505714146 ) ) ;
#89594=CARTESIAN_POINT ( 'NONE',  ( 1.234984068473435892, -1.692697435815498919, 0.7966027930108383615 ) ) ;
#89595=CARTESIAN_POINT ( 'NONE',  ( 1.968124833515383809, 1.674630251985644414, 1.122327857054454814 ) ) ;
#89598=CARTESIAN_POINT ( 'NONE',  ( 2.964111632446063016, -1.609175542312387908, -0.6635834015607346981 ) ) ;
#89602=CARTESIAN_POINT ( 'NONE',  ( 3.299128894759464359, 1.360359547890070964, 1.060362228049552158 ) ) ;
#89603=CARTESIAN_POINT ( 'NONE',  ( 2.683357600500847262, 1.551837136583393839, 1.547750905674146971 ) ) ;
#89604=CARTESIAN_POINT ( 'NONE',  ( 5.479209177496175087, -0.05098606815037013545, -2.206463706674952618 ) ) ;
#89607=CARTESIAN_POINT ( 'NONE',  ( 3.872083141701920805, -2.139866411213369624, 0.3658599195538684290 ) ) ;
#89608=CARTESIAN_POINT ( 'NONE',  ( 2.525780997283606499, -1.050937884436175418, -1.492673824175783093 ) ) ;
#89609=CARTESIAN_POINT ( 'NONE',  ( 4.452435347768154195, -1.380274204828018991, 1.605734313660161172 ) ) ;
#89610=CARTESIAN_POINT ( 'NONE',  ( 6.639320575229274546, 6.037277963978410433, 2.591643891269063360 ) ) ;
#89612=CARTESIAN_POINT ( 'NONE',  ( 5.179329019713509119, 1.537796090523161796, 1.700180828611449035 ) ) ;
#89616=CARTESIAN_POINT ( 'NONE',  ( 0.2586463447097427926, 2.115114616003030079, 0.1516365082330217162 ) ) ;
#89623=CARTESIAN_POINT ( 'NONE',  ( 5.344375030997434273, 0.3906003880304632636, -1.978050218768567792 ) ) ;
#89625=CARTESIAN_POINT ( 'NONE',  ( 3.010651042449908221, 0.6904807078514271224, 1.943715162320960088 ) ) ;
#89627=CARTESIAN_POINT ( 'NONE',  ( -0.2411972340276360705, 6.947779742164541972, -2.495493578726155182 ) ) ;
#89631=CARTESIAN_POINT ( 'NONE',  ( 6.650331627364351128, -1.696677047125955795, 1.386650686450926484 ) ) ;
#89632=CARTESIAN_POINT ( 'NONE',  ( 3.041638857185970046, -1.525043868314728934, 1.319228477497782714 ) ) ;
#89633=CARTESIAN_POINT ( 'NONE',  ( 2.893917256732419396, -0.5369380550670297403, -1.761199466696103499 ) ) ;
#89636=CARTESIAN_POINT ( 'NONE',  ( 6.124025070245508573, -1.016541136310184390, -1.516163765885633286 ) ) ;
#89638=CARTESIAN_POINT ( 'NONE',  ( 6.491137613139088991, 1.972399245366265985, -1.108330356262598126 ) ) ;
#89639=CARTESIAN_POINT ( 'NONE',  ( 1.348413808652969337, 2.103741849630758054, 0.1016320799899407962 ) ) ;
#89648=CARTESIAN_POINT ( 'NONE',  ( 3.920361760358490599, -2.215291009692350599, 0.1660125995653055075 ) ) ;
#89649=CARTESIAN_POINT ( 'NONE',  ( 2.396645607016957502, 1.759237466006560391, -1.306522788049699457 ) ) ;
#89651=CARTESIAN_POINT ( 'NONE',  ( 6.883263157960367806, 0.5819222519044697783, 1.998722019247618276 ) ) ;
#89654=CARTESIAN_POINT ( 'NONE',  ( 5.529730448059603454, 1.891198321494348633, -0.5216162335564683561 ) ) ;
#89657=CARTESIAN_POINT ( 'NONE',  ( 6.610000000000030518, 2.992693383986976041, 2.174209315121559349 ) ) ;
#89659=CARTESIAN_POINT ( 'NONE',  ( 5.150683391976684788, 2.089615912265533559, 0.3601871064465370087 ) ) ;
#89662=CARTESIAN_POINT ( 'NONE',  ( 5.928642344448160628, 2.082074431819755045, 0.5810635428650026135 ) ) ;
#89664=CARTESIAN_POINT ( 'NONE',  ( 5.126429434416579056, 0.1410513515392505246, 1.835921608166577013 ) ) ;
#89668=CARTESIAN_POINT ( 'NONE',  ( 0.5205769134342881355, -1.653362465512813184, 0.5437448749807861637 ) ) ;
#89669=CARTESIAN_POINT ( 'NONE',  ( 6.727182134110237577, 2.455520393281558356, 2.294684051055717600 ) ) ;
#89673=CARTESIAN_POINT ( 'NONE',  ( 4.223607183596161718, -2.069420184152844566, 0.6248923283326962563 ) ) ;
#89676=CARTESIAN_POINT ( 'NONE',  ( 6.884150277402729223, -0.1485532345978715640, 1.983297619905934006 ) ) ;
#89678=CARTESIAN_POINT ( 'NONE',  ( 4.065412822539622439, 0.2671453805177248508, -2.145074402785766665 ) ) ;
#89680=CARTESIAN_POINT ( 'NONE',  ( 4.921144022694462272, -0.09977086410491335655, 1.968969177566483042 ) ) ;
#89681=CARTESIAN_POINT ( 'NONE',  ( 3.391645568799035892, 0.04004947218742663240, 1.733546134666413607 ) ) ;
#89682=CARTESIAN_POINT ( 'NONE',  ( 0.8729168595149154886, -0.05911722906676297740, -2.190938979806676734 ) ) ;
#89683=CARTESIAN_POINT ( 'NONE',  ( 1.132322824279883955, -1.466084937595305560, -1.782028031347275832 ) ) ;
#89684=CARTESIAN_POINT ( 'NONE',  ( 3.409498948718358680, -0.4055148060846422431, 2.020306737620365389 ) ) ;
#89685=CARTESIAN_POINT ( 'NONE',  ( 5.706574293107399498, 1.714631337756479912, 0.9119185223999854983 ) ) ;
#89691=CARTESIAN_POINT ( 'NONE',  ( 2.960231987352707428, 2.196266598062237563, -0.2149427413448631863 ) ) ;
#89693=VERTEX_POINT ( 'NONE', #130889 ) ;
#89694=CARTESIAN_POINT ( 'NONE',  ( 0.7251815698985024650, 0.1899481183357653036, -1.851258252060000498 ) ) ;
#89696=CARTESIAN_POINT ( 'NONE',  ( -0.1291982275798625457, 2.008329037175633491, -2.487957029800022202 ) ) ;
#89701=CARTESIAN_POINT ( 'NONE',  ( 6.544863656343847147, -1.481929198830441052, -1.092355128777318107 ) ) ;
#89703=CARTESIAN_POINT ( 'NONE',  ( 2.377870294028866294, 1.267006343609432761, 1.625331576946090539 ) ) ;
#89708=CARTESIAN_POINT ( 'NONE',  ( 0.9540633210794751129, 2.058568143186993105, -0.1002533246910724124 ) ) ;
#89712=CARTESIAN_POINT ( 'NONE',  ( 5.267088776126935379, 1.772936381825638952, -0.4966186330585887210 ) ) ;
#89715=CARTESIAN_POINT ( 'NONE',  ( 4.653060005753134831, -1.773635849817876586, 1.313014255023836618 ) ) ;
#89716=CARTESIAN_POINT ( 'NONE',  ( 0.2984011986874868794, -2.161112683670802337, -0.05330630956579958390 ) ) ;
#89719=CARTESIAN_POINT ( 'NONE',  ( 0.01762790050853849447, -0.5081247445114078776, 1.843608005305336528 ) ) ;
#89721=CARTESIAN_POINT ( 'NONE',  ( 0.8488426437929346147, -1.825078332268307513, -0.8578388575243289793 ) ) ;
#89723=CARTESIAN_POINT ( 'NONE',  ( 1.300659708833833861, -2.077133573725042037, 0.9841232947556498578 ) ) ;
#89724=STYLED_ITEM ( 'NONE', ( #191580 ), #158197 ) ;
#89726=CARTESIAN_POINT ( 'NONE',  ( 6.633470332280523074, -0.1331818211787652029, 1.881796397474523541 ) ) ;
#89728=CARTESIAN_POINT ( 'NONE',  ( 1.305301652190330675, -0.4579020413679709689, 1.813615928118620380 ) ) ;
#89729=CARTESIAN_POINT ( 'NONE',  ( 2.676970549635893537, 1.727063564601112100, -1.040793759654296213 ) ) ;
#89733=CARTESIAN_POINT ( 'NONE',  ( 3.949915024511057471, 0.7098439763573929362, -1.982976504383345162 ) ) ;
#89737=CARTESIAN_POINT ( 'NONE',  ( 4.166274539359494433, 2.019258995967411430, -0.05370046678233526827 ) ) ;
#89739=CARTESIAN_POINT ( 'NONE',  ( 6.232891784722141892, -1.957473889884550289, -0.6504925196839649315 ) ) ;
#89742=CARTESIAN_POINT ( 'NONE',  ( 4.850933092205481856, -1.739298515662604405, 1.283314429840809234 ) ) ;
#89748=CARTESIAN_POINT ( 'NONE',  ( 2.119799831544411095, 0.3726140298815834861, -2.138824928699584405 ) ) ;
#89751=CARTESIAN_POINT ( 'NONE',  ( 1.294213439101927321, 1.504999338701202394, -1.060447551955064016 ) ) ;
#89753=CARTESIAN_POINT ( 'NONE',  ( 2.683357600500847262, 1.551837136583393839, 1.547750905674146971 ) ) ;
#89755=CARTESIAN_POINT ( 'NONE',  ( 3.837032359523879332, 0.3291597691741187104, 2.238327980419333674 ) ) ;
#89756=B_SPLINE_CURVE_WITH_KNOTS ( 'NONE', 3,
 ( #84678, #30617, #129269, #15394, #100919, #115116, #180059, #181112, #133471, #98811 ),
 .UNSPECIFIED., .F., .F.,
 ( 4, 1, 1, 1, 1, 1, 1, 4 ),
 ( 0.000000000000000000, 0.09183773654504942541, 0.1838067853904964410, 0.2558923657893393822, 0.3606054339151033017, 0.5206678126786191685, 0.7335446035554463728, 1.000000000000000000 ),
 .UNSPECIFIED. ) ;
#89763=CARTESIAN_POINT ( 'NONE',  ( 5.184699891622216228, -0.2167559868061739725, -1.756304918635148704 ) ) ;
#89764=( BOUNDED_SURFACE ( )  B_SPLINE_SURFACE ( 3, 3, ( 
 ( #4684, #172571, #139014, #122846, #24153, #73995, #90256, #156324, #57745, #123903, #108694 ),
 ( #189872, #41514, #107627, #173659, #25232, #91335, #58809, #124963, #174722, #26295, #70758 ),
 ( #136871, #202896, #54541, #38291, #104369, #29519, #27370, #129244, #208242, #14301, #59873 ),
 ( #77183, #176831, #78255, #44717, #144379, #63076, #95612, #195217, #112967, #12183, #30593 ),
 ( #50816, #178979, #43652, #45786, #143305, #159509, #67033, #13256, #10050, #127100, #128174 ),
 ( #93470, #109769, #46853, #209296, #133170, #11108, #193065, #161661, #60944, #96679, #116942 ),
 ( #145445, #79328, #211443, #162729, #110823, #80395, #126024, #146490, #191986, #175776, #28445 ) ),
 .UNSPECIFIED., .T., .F., .T. ) 
 B_SPLINE_SURFACE_WITH_KNOTS ( ( 4, 3, 4 ),
 ( 4, 1, 1, 1, 1, 1, 1, 1, 4 ),
 ( 0.000000000000000000, 0.5000000000000000000, 1.000000000000000000 ),
 ( 0.000000000000000000, 0.2254101072112788262, 0.3970395454107691902, 0.5239558410346354389, 0.6152342776129972046, 0.6800502191696807808, 0.7279184599320936977, 0.7685697607527866015, 1.000000000000000000 ),
 .UNSPECIFIED. ) 
 GEOMETRIC_REPRESENTATION_ITEM ( )  RATIONAL_B_SPLINE_SURFACE ( (
 ( 1.000000000000000000, 1.000000000000000000, 1.000000000000000222, 1.000000000000000222, 0.9999999999999996669, 1.000000000000000222, 0.9999999999999994449, 1.000000000000000222, 0.9999999999999992228, 1.000000000000000000, 1.000000000000000000),
 ( 0.3333333333333333703, 0.3333333333333333703, 0.3333333333333334259, 0.3333333333333333703, 0.3333333333333333148, 0.3333333333333334814, 0.3333333333333332593, 0.3333333333333334259, 0.3333333333333330928, 0.3333333333333333703, 0.3333333333333333703),
 ( 0.3333333333333333703, 0.3333333333333333703, 0.3333333333333334259, 0.3333333333333333703, 0.3333333333333333148, 0.3333333333333334814, 0.3333333333333332593, 0.3333333333333334259, 0.3333333333333330928, 0.3333333333333333703, 0.3333333333333333703),
 ( 1.000000000000000000, 1.000000000000000000, 1.000000000000000222, 1.000000000000000222, 0.9999999999999996669, 1.000000000000000222, 0.9999999999999994449, 1.000000000000000222, 0.9999999999999992228, 1.000000000000000000, 1.000000000000000000),
 ( 0.3333333333333333703, 0.3333333333333333703, 0.3333333333333334259, 0.3333333333333333703, 0.3333333333333333148, 0.3333333333333334814, 0.3333333333333332593, 0.3333333333333334259, 0.3333333333333330928, 0.3333333333333333703, 0.3333333333333333703),
 ( 0.3333333333333333703, 0.3333333333333333703, 0.3333333333333334259, 0.3333333333333333703, 0.3333333333333333148, 0.3333333333333334814, 0.3333333333333332593, 0.3333333333333334259, 0.3333333333333330928, 0.3333333333333333703, 0.3333333333333333703),
 ( 1.000000000000000000, 1.000000000000000000, 1.000000000000000222, 1.000000000000000222, 0.9999999999999996669, 1.000000000000000222, 0.9999999999999994449, 1.000000000000000222, 0.9999999999999992228, 1.000000000000000000, 1.000000000000000000) ) ) 
 REPRESENTATION_ITEM ( '' )  SURFACE ( )  );
#89767=CARTESIAN_POINT ( 'NONE',  ( 1.799976324648028481, -0.7102278526811952597, 1.982709249334560164 ) ) ;
#89770=CARTESIAN_POINT ( 'NONE',  ( 0.7835775553649370062, -1.871284325210004429, 0.6146160330302401498 ) ) ;
#89773=CARTESIAN_POINT ( 'NONE',  ( 6.205303291940151844, 1.571521137685438108, -0.9011181087926769528 ) ) ;
#89776=CARTESIAN_POINT ( 'NONE',  ( 4.803500792215161574, -0.4985019455652460740, 1.802925825644098534 ) ) ;
#89778=CARTESIAN_POINT ( 'NONE',  ( 4.522371119077151391, 0.9712943915625820157, 1.828230030883712498 ) ) ;
#89789=CARTESIAN_POINT ( 'NONE',  ( 3.437899435096212208, 1.242623406730450908, 1.518177208742684803 ) ) ;
#89792=CARTESIAN_POINT ( 'NONE',  ( 2.583361055862750000, 1.319027862724517330, -1.524809160041600498 ) ) ;
#89793=CARTESIAN_POINT ( 'NONE',  ( -0.1108833634137010582, 5.723767666350643601, -2.491012016648496363 ) ) ;
#89795=CARTESIAN_POINT ( 'NONE',  ( 2.161206213664386144, 0.3243885794495802721, -1.842051381961368639 ) ) ;
#89797=CARTESIAN_POINT ( 'NONE',  ( 3.621343358005862267, 1.728792273982106220, 1.031380397273339078 ) ) ;
#89800=CARTESIAN_POINT ( 'NONE',  ( 3.866910228754817158, -0.2097145705111657654, -2.106837283413672601 ) ) ;
#89802=CARTESIAN_POINT ( 'NONE',  ( 5.424307079040114665, 1.017280057988108499, 1.803113764695261523 ) ) ;
#89804=CARTESIAN_POINT ( 'NONE',  ( 0.8375780558756993344, 0.8438101838260108067, -1.913087135030653974 ) ) ;
#89805=CARTESIAN_POINT ( 'NONE',  ( 6.720655732516659597, 0.5653683226944251627, 2.225905711026022971 ) ) ;
#89806=CARTESIAN_POINT ( 'NONE',  ( 6.774438514930277933, -1.120217847261167243, 1.442041797927499980 ) ) ;
#89814=CARTESIAN_POINT ( 'NONE',  ( 6.147114339676178041, 0.1922309238813116328, 1.902605946959089689 ) ) ;
#89821=CARTESIAN_POINT ( 'NONE',  ( 6.450795914701256351, -1.844717532910484570, -0.8146137538835170888 ) ) ;
#89823=CARTESIAN_POINT ( 'NONE',  ( -0.1405533004718754753, 0.003749010675345095921, -1.720146753850452681 ) ) ;
#89826=CARTESIAN_POINT ( 'NONE',  ( 2.219528804134728528, 0.3415968887231227713, -1.939435228410562484 ) ) ;
#89827=CARTESIAN_POINT ( 'NONE',  ( 4.657827466662149973, 1.163286545301238206, 1.646828140416577657 ) ) ;
#89830=CARTESIAN_POINT ( 'NONE',  ( 4.453197812796324762, 0.4814713343750369190, -2.137748681182354726 ) ) ;
#89832=CARTESIAN_POINT ( 'NONE',  ( 3.170836325157891267, -1.779339148710285867, -0.7386555552950261339 ) ) ;
#89834=CARTESIAN_POINT ( 'NONE',  ( -0.1298852118744257267, 5.725805934370246320, -2.320586200942467148 ) ) ;
#89835=CARTESIAN_POINT ( 'NONE',  ( 0.2763675079364875664, 1.274320874971252460, 1.801605125401319007 ) ) ;
#89841=CARTESIAN_POINT ( 'NONE',  ( 5.847170753249844033, 0.5281823367668266878, -1.763884204139199330 ) ) ;
#89842=CARTESIAN_POINT ( 'NONE',  ( 3.088541981101311507, -1.197259257089001716, 1.618239360019198880 ) ) ;
#89843=CARTESIAN_POINT ( 'NONE',  ( 4.868718825205943901, -0.6189299756741394321, 2.213421903294809034 ) ) ;
#89845=CARTESIAN_POINT ( 'NONE',  ( 3.397144026274971029, -1.643366908016094641, 0.8731178804023755902 ) ) ;
#89846=CARTESIAN_POINT ( 'NONE',  ( -0.1290005225502676156, 1.324981729379502537, -2.425680704180297464 ) ) ;
#89850=CARTESIAN_POINT ( 'NONE',  ( 6.304249618663324561, 1.548718018665395713, -1.404690827926929453 ) ) ;
#89855=CARTESIAN_POINT ( 'NONE',  ( 6.234932630344998117, 0.1766075427261544484, 1.715814389380666327 ) ) ;
#89857=CARTESIAN_POINT ( 'NONE',  ( 2.215074966175926363, 1.682300057933778126, 0.4202854259360877531 ) ) ;
#89863=CARTESIAN_POINT ( 'NONE',  ( 0.4794554595633391814, -0.1051018081165492196, 2.067734805981166435 ) ) ;
#89864=CARTESIAN_POINT ( 'NONE',  ( 5.672426548614882158, -1.154804106291613675, 1.414059844683832834 ) ) ;
#89865=CARTESIAN_POINT ( 'NONE',  ( 3.854310441289869882, -1.959320932037407426, -0.1006921081871253454 ) ) ;
#89869=CARTESIAN_POINT ( 'NONE',  ( 3.299587915756982515, 1.916203934664402198, -0.9084051299479002362 ) ) ;
#89872=CARTESIAN_POINT ( 'NONE',  ( 1.850524992189076290, -2.059912964915584954, -0.2069831422613493399 ) ) ;
#89875=CARTESIAN_POINT ( 'NONE',  ( 3.967602866622577107, -1.847128000506767176, -1.233534119358855152 ) ) ;
#89876=EDGE_LOOP ( 'NONE', ( #211684, #86775, #26644, #47882 ) ) ;
#89877=CARTESIAN_POINT ( 'NONE',  ( 1.460084154473238138, -2.184713004772549372, -0.7151137612169417013 ) ) ;
#89879=CARTESIAN_POINT ( 'NONE',  ( 0.3034670832338138835, -1.512625156342655819, -1.248876549296701333 ) ) ;
#89883=CARTESIAN_POINT ( 'NONE',  ( 6.146043377905669125, 0.5841948715668408010, 1.746183665442810007 ) ) ;
#89886=CARTESIAN_POINT ( 'NONE',  ( 3.427896188528327226, -1.883279545317056547, 0.3315703044584616399 ) ) ;
#89887=CARTESIAN_POINT ( 'NONE',  ( -0.2104748580754201015, 7.629137130509078268, -2.703678718140526627 ) ) ;
#89888=CARTESIAN_POINT ( 'NONE',  ( 4.067213672036010585, 0.2104045600922407611, -1.711820660605578137 ) ) ;
#89889=CARTESIAN_POINT ( 'NONE',  ( 2.378138974734815392, -2.011451771401792321, -0.1435188914247695346 ) ) ;
#89890=CARTESIAN_POINT ( 'NONE',  ( 4.078954460043759056, -0.8795263853869551562, 2.123946672719174700 ) ) ;
#89891=CARTESIAN_POINT ( 'NONE',  ( 3.198750403210961490, -0.6533003841502099673, -2.166054703861711506 ) ) ;
#89892=CARTESIAN_POINT ( 'NONE',  ( 5.320966398826527666, 1.945490409060679049, 0.8070863781705228668 ) ) ;
#89895=CARTESIAN_POINT ( 'NONE',  ( 4.797990518455403475, -1.769373726167685623, -0.04385371103611360177 ) ) ;
#89897=CARTESIAN_POINT ( 'NONE',  ( 0.6391472400242370622, -1.963128197947199727, 1.183262795983427207 ) ) ;
#89898=CARTESIAN_POINT ( 'NONE',  ( 6.052668933152094866, -1.581501214056714177, -0.9424504099920794076 ) ) ;
#89900=CARTESIAN_POINT ( 'NONE',  ( 5.964808794498538624, 0.1646014364122504459, -2.185315939793014639 ) ) ;
#89903=CARTESIAN_POINT ( 'NONE',  ( 5.652806998763869828, -0.4994405740583847675, -2.009109930559597856 ) ) ;
#89904=CARTESIAN_POINT ( 'NONE',  ( -0.2058462039469660110, -0.8663896114125648751, -1.819200108291472606 ) ) ;
#89906=CARTESIAN_POINT ( 'NONE',  ( 4.758382555496592836, 0.7388506920381915366, 1.779377657810585767 ) ) ;
#89909=CARTESIAN_POINT ( 'NONE',  ( 1.494693441997055894, -1.183060725354843079, 1.879997432091018217 ) ) ;
#89911=ORIENTED_EDGE ( 'NONE', *, *, #110985, .F. ) ;
#89918=CARTESIAN_POINT ( 'NONE',  ( 1.205434515183744226, -1.544416933936803904, -1.209700862059132964 ) ) ;
#89922=CARTESIAN_POINT ( 'NONE',  ( 6.760214184729610665, -1.961454122871961747, 0.04698431645466792650 ) ) ;
#89925=CARTESIAN_POINT ( 'NONE',  ( 0.3743661609300020232, 1.305675439620108458, 1.847588536312362972 ) ) ;
#89929=CARTESIAN_POINT ( 'NONE',  ( 1.282252794574537447, -1.823689378192733912, -0.4153219600965887826 ) ) ;
#89930=CARTESIAN_POINT ( 'NONE',  ( 0.5978079470381278959, -0.2563149341858957930, 1.714925299717950491 ) ) ;
#89932=CARTESIAN_POINT ( 'NONE',  ( 4.001666433686186686, -2.185622478633037602, 0.1623105178310546570 ) ) ;
#89933=CARTESIAN_POINT ( 'NONE',  ( 3.997355382689435466, 1.951332032848082099, -1.231501813138028423 ) ) ;
#89934=CARTESIAN_POINT ( 'NONE',  ( 0.2509463769419334467, -1.655472276559850853, 1.227265982703225511 ) ) ;
#89935=CARTESIAN_POINT ( 'NONE',  ( 2.554547512858021729, -1.689694153139981392, -0.9569994400411386826 ) ) ;
#89938=CARTESIAN_POINT ( 'NONE',  ( 5.308877466510794285, -0.5174029350529658622, -2.056363676157816123 ) ) ;
#89941=CARTESIAN_POINT ( 'NONE',  ( 3.094375128876575065, -0.3905979561782264575, 1.978050703236901686 ) ) ;
#89946=CARTESIAN_POINT ( 'NONE',  ( 0.7678472254676466102, 0.8974085622692473674, 1.589837017038860045 ) ) ;
#89951=CARTESIAN_POINT ( 'NONE',  ( 6.051650376505027573, 0.6007964193008934473, -1.971360088487213780 ) ) ;
#89955=CARTESIAN_POINT ( 'NONE',  ( 4.459631813825579272, -1.562525726068206833, -1.279702784981617825 ) ) ;
#89956=CARTESIAN_POINT ( 'NONE',  ( 5.602238577124374785, -1.000643217919431116, 1.983199510308247815 ) ) ;
#89961=CARTESIAN_POINT ( 'NONE',  ( 4.416905344109374632, 1.883477791879540231, 0.8369615876049685266 ) ) ;
#89962=CARTESIAN_POINT ( 'NONE',  ( 4.430314669760617718, -1.560499787156752971, -1.277043788614096176 ) ) ;
#89968=CARTESIAN_POINT ( 'NONE',  ( 3.919295934624257960, 0.7230291454519314209, 1.882185965797255278 ) ) ;
#89969=CARTESIAN_POINT ( 'NONE',  ( 3.169683937527142170, -1.096016708463069422, 1.479218548343118389 ) ) ;
#89971=CARTESIAN_POINT ( 'NONE',  ( 0.8214423835279326402, 2.134246884609458661, 0.8782244701446385582 ) ) ;
#89973=CARTESIAN_POINT ( 'NONE',  ( 3.673254355229157664, 0.05708692194854488033, -2.161017345153878999 ) ) ;
#89978=CARTESIAN_POINT ( 'NONE',  ( 1.902992089709685031, 1.553661375375714471, 1.041555772207984676 ) ) ;
#89979=CARTESIAN_POINT ( 'NONE',  ( 0.5792891803052163668, 1.841034274367932877, -0.7053527730483382108 ) ) ;
#89983=CARTESIAN_POINT ( 'NONE',  ( 1.981372325807278623, -0.1102420082176903682, -2.204251428397439483 ) ) ;
#89988=CARTESIAN_POINT ( 'NONE',  ( 6.051636762666342761, 0.5725952485956290472, -1.886469267683591466 ) ) ;
#89989=CARTESIAN_POINT ( 'NONE',  ( 5.918676688095830585, 1.554283316268306292, -1.705954940095489203 ) ) ;
#89990=CARTESIAN_POINT ( 'NONE',  ( 6.637149568644561626, -0.09269223384644230401, -1.858852300295941395 ) ) ;
#89991=CARTESIAN_POINT ( 'NONE',  ( 3.590735542246026313, 2.011259174285257689, 0.4565010432640480564 ) ) ;
#89999=CARTESIAN_POINT ( 'NONE',  ( 5.477072320546296780, 2.003985016195033886, 0.8359633449262526828 ) ) ;
#90001=CARTESIAN_POINT ( 'NONE',  ( 5.144037045698616417, 0.5398437887287730330, 1.760322748975438500 ) ) ;
#90004=DIRECTION ( 'NONE',  ( -1.000000000000000000, 0.000000000000000000, 0.000000000000000000 ) ) ;
#90005=CARTESIAN_POINT ( 'NONE',  ( 6.754744673581316583, -1.754229693457433736, 1.428470910521584036 ) ) ;
#90011=CARTESIAN_POINT ( 'NONE',  ( 2.236828121427667071, -1.582394523617111970, 0.7928310554637070240 ) ) ;
#90012=CARTESIAN_POINT ( 'NONE',  ( 6.586586637485376983, -1.237022783311360730, 1.588989491490456762 ) ) ;
#90014=CARTESIAN_POINT ( 'NONE',  ( 3.497576124367638872, -1.886684243562693597, 0.3306681954469546936 ) ) ;
#90016=CARTESIAN_POINT ( 'NONE',  ( 3.859776292547572929, -0.5741801112500494186, 1.883974994742370068 ) ) ;
#90017=CARTESIAN_POINT ( 'NONE',  ( 6.363536886121980984, -1.624614756573187435, -1.199887179878684540 ) ) ;
#90019=CARTESIAN_POINT ( 'NONE',  ( 2.852262661058731386, 0.6285613048715790185, 1.762029509812724992 ) ) ;
#90020=CARTESIAN_POINT ( 'NONE',  ( 6.639270748794153576, -1.536914537172892725, 0.7831451356504478545 ) ) ;
#90022=CARTESIAN_POINT ( 'NONE',  ( 2.034064749695370100, -1.442962035976073309, -1.669870808145665020 ) ) ;
#90026=CARTESIAN_POINT ( 'NONE',  ( 6.162552467866693640, -0.7048080804108979303, -1.831077584432870609 ) ) ;
#90032=CARTESIAN_POINT ( 'NONE',  ( 2.330607996690749140, -1.275545549462468120, 1.630658604070814199 ) ) ;
#90036=CARTESIAN_POINT ( 'NONE',  ( 6.182307711929101224, 1.089732742074623006, 1.818925385317768928 ) ) ;
#90040=CARTESIAN_POINT ( 'NONE',  ( 0.07479286986305545837, 0.7422478802248284602, -1.939684878352589070 ) ) ;
#90042=CARTESIAN_POINT ( 'NONE',  ( 5.659529772124847646, -0.4871306767523299608, -1.956261131662299535 ) ) ;
#90043=CARTESIAN_POINT ( 'NONE',  ( 5.858580540861003882, -1.821332666672281553, -0.5942308157336049224 ) ) ;
#90044=CARTESIAN_POINT ( 'NONE',  ( 6.539320575229258026, 7.052651068779801413, 2.601414540040230428 ) ) ;
#90045=CARTESIAN_POINT ( 'NONE',  ( 3.579775959861815515, -1.078688530630707243, 1.907616655872627964 ) ) ;
#90047=CARTESIAN_POINT ( 'NONE',  ( 2.004032382285144021, -0.8144628449315849394, 1.730399521388835460 ) ) ;
#90052=CARTESIAN_POINT ( 'NONE',  ( 6.169547404874395014, 1.460173559465412829, 1.533355976833279621 ) ) ;
#90054=CARTESIAN_POINT ( 'NONE',  ( 6.497619750234602698, -2.191128968173004843, 0.05151875470104508997 ) ) ;
#90056=CARTESIAN_POINT ( 'NONE',  ( 3.346439682166453711, 0.4181539295537542444, 1.673179028346531538 ) ) ;
#90057=ORIENTED_EDGE ( 'NONE', *, *, #63333, .F. ) ;
#90061=CARTESIAN_POINT ( 'NONE',  ( 0.2913577194270203785, -1.795273245208812485, 0.7915465721433642132 ) ) ;
#90067=CARTESIAN_POINT ( 'NONE',  ( 2.824650661615616620, 1.310593810787925362, -1.250744805450889618 ) ) ;
#90071=CARTESIAN_POINT ( 'NONE',  ( 4.020002786455856736, -1.806352922022226304, 0.1370799816429474904 ) ) ;
#90075=CARTESIAN_POINT ( 'NONE',  ( 4.949569884170424316, 1.378596123743974555, 1.250361270004763714 ) ) ;
#90077=CARTESIAN_POINT ( 'NONE',  ( 2.126450742919711256, 0.4219061677965991741, 1.868383228629175719 ) ) ;
#90078=CARTESIAN_POINT ( 'NONE',  ( 1.377666516899571647, 1.084121917808708035, 1.468671923017292658 ) ) ;
#90088=CARTESIAN_POINT ( 'NONE',  ( 1.201248573238463235, -0.5064915201186767080, 2.028225233004859351 ) ) ;
#90089=CARTESIAN_POINT ( 'NONE',  ( 6.229514091203088633, -1.813738808949336478, 0.6494875524521417365 ) ) ;
#90091=CARTESIAN_POINT ( 'NONE',  ( 2.766400663125650361, -1.260407102598060103, 1.320874842943790872 ) ) ;
#90092=CARTESIAN_POINT ( 'NONE',  ( 3.053566222061272040, -1.804402116661915967, -1.270350324234906125 ) ) ;
#90094=CARTESIAN_POINT ( 'NONE',  ( 1.142663480069527671, 1.843847066288730074, 0.5072560978593986247 ) ) ;
#90095=CARTESIAN_POINT ( 'NONE',  ( 1.767950473188628857, -1.955055593144053194, 0.2378005183036585035 ) ) ;
#90096=CARTESIAN_POINT ( 'NONE',  ( 2.313922598539425390, 1.266723153581908567, -1.472183398282415956 ) ) ;
#90100=CARTESIAN_POINT ( 'NONE',  ( 6.420743829754993470, -1.316656903452334992, 1.315380689086578236 ) ) ;
#90105=CARTESIAN_POINT ( 'NONE',  ( 2.419692422129790632, -1.264489869534379141, -1.789777738334753732 ) ) ;
#90106=DIRECTION ( 'NONE',  ( -3.451266460341926649E-31, -5.200009205990155575E-32, 1.000000000000000000 ) ) ;
#90110=CARTESIAN_POINT ( 'NONE',  ( 4.037589748876240670, -1.260430739550026269, -1.321009972365666307 ) ) ;
#90114=CARTESIAN_POINT ( 'NONE',  ( -0.02968770228140016343, 1.391517546076680434, -2.083419219542380407 ) ) ;
#90117=CARTESIAN_POINT ( 'NONE',  ( 2.666528119303875233, -1.328299865307873695, 1.395581591625531193 ) ) ;
#90118=CARTESIAN_POINT ( 'NONE',  ( 6.983263157960366563, -0.003091553303710344557, 1.945923119799706669 ) ) ;
#90123=CARTESIAN_POINT ( 'NONE',  ( 0.3513568635829470432, 0.2028739153508585802, -2.107475566755373730 ) ) ;
#90126=CARTESIAN_POINT ( 'NONE',  ( 5.014543041041934046, 0.7873211189074662553, 1.914903133430221338 ) ) ;
#90127=CARTESIAN_POINT ( 'NONE',  ( 0.2746299231596514012, 1.718356743839201561, -0.6618312839273902126 ) ) ;
#90130=CARTESIAN_POINT ( 'NONE',  ( 5.344470762249110329, 0.4509167475243852086, -2.253899259558800772 ) ) ;
#90134=CARTESIAN_POINT ( 'NONE',  ( 0.5863596474044476814, -2.275655805637688989, -0.2749888630660061728 ) ) ;
#90137=CARTESIAN_POINT ( 'NONE',  ( 5.314377360232536596, 1.795021767651948208, 0.7414505486388212052 ) ) ;
#90141=CARTESIAN_POINT ( 'NONE',  ( 0.03540237040386850359, -0.09474447662855033092, 2.011072404829179483 ) ) ;
#90142=CARTESIAN_POINT ( 'NONE',  ( 0.2930059409478984467, 1.274291793118907723, 1.162708412170476713 ) ) ;
#90143=CARTESIAN_POINT ( 'NONE',  ( 5.507046092540283766, -0.04465857163906890998, 2.016188657829049991 ) ) ;
#90147=CARTESIAN_POINT ( 'NONE',  ( 2.519574111291386309, -1.204466598365286023, -1.708601439550963663 ) ) ;
#90148=CARTESIAN_POINT ( 'NONE',  ( 0.7074158718562081338, -1.761916611671160204, 0.1673130110368889201 ) ) ;
#90151=CARTESIAN_POINT ( 'NONE',  ( 4.242302733825270344, 0.6093012942862492398, 2.209731468575569124 ) ) ;
#90152=CARTESIAN_POINT ( 'NONE',  ( 2.730071887686904564, 0.2129287318765031578, 1.727178079207219552 ) ) ;
#90155=CARTESIAN_POINT ( 'NONE',  ( 3.234745892528373634, 1.342314639517484087, -1.641720766639111817 ) ) ;
#90157=CARTESIAN_POINT ( 'NONE',  ( 1.791952614948258304, -1.634470817638247642, 0.5789770405969245637 ) ) ;
#90159=CARTESIAN_POINT ( 'NONE',  ( 1.134942894344723507, -0.04051261866679262136, -1.860784445789311903 ) ) ;
#90160=CARTESIAN_POINT ( 'NONE',  ( 2.453800908837290518, 1.677244079947149302, 1.378686777781912065 ) ) ;
#90162=CARTESIAN_POINT ( 'NONE',  ( 3.942592416894859841, -1.490970858180175940, 1.357867534901323614 ) ) ;
#90163=CARTESIAN_POINT ( 'NONE',  ( 1.562500000000001554, -1.451031289061184282, -1.451031289061057050 ) ) ;
#90165=CARTESIAN_POINT ( 'NONE',  ( 1.395397119253296569, 1.457039974399224391, 1.260252556074402897 ) ) ;
#90167=CARTESIAN_POINT ( 'NONE',  ( 4.096076364168971473, 1.452574950358286765, 1.680725415074139306 ) ) ;
#90173=CARTESIAN_POINT ( 'NONE',  ( 5.871364357536254630, -1.904906058150414472, -1.142540087918672898 ) ) ;
#90175=CARTESIAN_POINT ( 'NONE',  ( 4.668382477721988444, -0.8370036265390871089, -1.774476930476886594 ) ) ;
#90180=CARTESIAN_POINT ( 'NONE',  ( 5.888003241735360938, -1.025016604251761221, 2.016990234832950701 ) ) ;
#90182=CARTESIAN_POINT ( 'NONE',  ( 3.455586768955606125, 1.624414792841613941, 1.271063249801159145 ) ) ;
#90186=CARTESIAN_POINT ( 'NONE',  ( 4.798043669735932326, -1.870115615568968881, -0.04763329477865811679 ) ) ;
#90187=CARTESIAN_POINT ( 'NONE',  ( 3.199597886960439119, 1.569373658825726769, 0.7380672391785416675 ) ) ;
#90188=CARTESIAN_POINT ( 'NONE',  ( 3.298151293307958642, 1.369808456162135091, -1.073517941977668588 ) ) ;
#90189=CARTESIAN_POINT ( 'NONE',  ( 0.7324523162463879578, 2.259705603777485639, 0.3848113418177290801 ) ) ;
#90190=CARTESIAN_POINT ( 'NONE',  ( 1.061882456046374434, 0.4290601450722114074, -2.164491299336705588 ) ) ;
#90191=CARTESIAN_POINT ( 'NONE',  ( 4.423432795095141756, -1.287707899167778169, -1.647015592753127589 ) ) ;
#90192=CARTESIAN_POINT ( 'NONE',  ( 5.683525053321154985, -0.8713906080477454852, 1.735537339962249792 ) ) ;
#90194=VERTEX_POINT ( 'NONE', #104741 ) ;
#90195=CARTESIAN_POINT ( 'NONE',  ( 0.6510177983308338412, 0.9963039324867200008, 1.753029211773032392 ) ) ;
#90197=CARTESIAN_POINT ( 'NONE',  ( 6.592432824109000222, -0.4393352932590722792, 1.975308225066509049 ) ) ;
#90201=CARTESIAN_POINT ( 'NONE',  ( 3.896943178251357054, 1.541351720387572843, -0.9781566455248569270 ) ) ;
#90207=CARTESIAN_POINT ( 'NONE',  ( 2.601824576204377681, 1.431331034542600245, 1.425341822903106515 ) ) ;
#90209=CARTESIAN_POINT ( 'NONE',  ( 2.694024576921652425, 0.8818583146339260548, -1.638763372900291726 ) ) ;
#90215=CARTESIAN_POINT ( 'NONE',  ( 5.549374350267230582, -1.441814640532925074, -1.119852386600270533 ) ) ;
#90219=CARTESIAN_POINT ( 'NONE',  ( 0.8074296549154248437, -1.491244094015523602, 0.8842416791710568935 ) ) ;
#90220=CARTESIAN_POINT ( 'NONE',  ( 0.05802509242504564485, -1.552030147408272054, -0.7874549631982865616 ) ) ;
#90221=CARTESIAN_POINT ( 'NONE',  ( 5.215558013723960329, -0.3431011331927047991, 2.281934296042067878 ) ) ;
#90223=CARTESIAN_POINT ( 'NONE',  ( 0.3509462063632540763, -1.656586674793923075, 1.225593781303188967 ) ) ;
#90225=CARTESIAN_POINT ( 'NONE',  ( 5.888098204360154853, -0.06530352750959941832, 2.297622472229691404 ) ) ;
#90228=CARTESIAN_POINT ( 'NONE',  ( 5.278141497218024725, -1.038406966791558528, 1.555765341417144842 ) ) ;
#90229=CARTESIAN_POINT ( 'NONE',  ( 3.111475685156277038, 1.510342251817019532, 1.173009309769344588 ) ) ;
#90231=CARTESIAN_POINT ( 'NONE',  ( 5.197975494389605267, -0.7968864405506062010, 2.058166701804148957 ) ) ;
#90232=CARTESIAN_POINT ( 'NONE',  ( 4.382099326012149909, -2.116931447088743923, -0.04843129487230694169 ) ) ;
#90234=CARTESIAN_POINT ( 'NONE',  ( 6.983263157960393208, 0.5798717822590447879, 1.998431770337566027 ) ) ;
#90237=CARTESIAN_POINT ( 'NONE',  ( 5.549516566986255839, -1.916978305411633166, 0.9067721062034905799 ) ) ;
#90238=CARTESIAN_POINT ( 'NONE',  ( 2.310004868091195540, -0.5052997711322243513, 2.251431844744283151 ) ) ;
#90239=CARTESIAN_POINT ( 'NONE',  ( 3.367582429956605061, -0.3852447139683997657, 1.923494667983568718 ) ) ;
#90240=CARTESIAN_POINT ( 'NONE',  ( 6.438341905586414171, -1.108352981827376738, 1.739313939070710857 ) ) ;
#90244=CARTESIAN_POINT ( 'NONE',  ( 5.876185452347599814, -2.007255679753978228, -0.1928398672442974138 ) ) ;
#90248=CARTESIAN_POINT ( 'NONE',  ( 2.061612764771907802, 1.803244147071264125, 1.208790786097496905 ) ) ;
#90254=CARTESIAN_POINT ( 'NONE',  ( 1.212264220565926198, -0.9239156619155285410, -1.842110158844072698 ) ) ;
#90256=CARTESIAN_POINT ( 'NONE',  ( 6.727182134110200273, 2.469373133786161745, 2.195552656936059055 ) ) ;
#90260=CARTESIAN_POINT ( 'NONE',  ( 3.422422624566554994, -0.7774026117220147469, -1.747318718686732497 ) ) ;
#90261=CARTESIAN_POINT ( 'NONE',  ( 5.348444421042818142, 0.5165251424982686412, 1.692803071163173634 ) ) ;
#90264=CARTESIAN_POINT ( 'NONE',  ( 0.1404700283944440298, 1.733558474490008772, 0.5260085833052421389 ) ) ;
#90266=CARTESIAN_POINT ( 'NONE',  ( 6.521099267210373363, -1.708630446951715731, 0.8662611975780337703 ) ) ;
#90267=CARTESIAN_POINT ( 'NONE',  ( 1.275928261265106833, -2.020323679977220621, 0.4517519998969782291 ) ) ;
#90269=CARTESIAN_POINT ( 'NONE',  ( 5.963714631206167738, 1.842656449598079060, -0.3214700631931910468 ) ) ;
#90270=CARTESIAN_POINT ( 'NONE',  ( 2.859763506297557711, 1.816872213737670938, -0.1792109616642542924 ) ) ;
#90271=CARTESIAN_POINT ( 'NONE',  ( 6.164705905600972535, -1.563586322211576674, 1.557672334054376773 ) ) ;
#90274=CARTESIAN_POINT ( 'NONE',  ( 3.209489602684848286, -1.684771875651757123, -1.189772946182314106 ) ) ;
#90279=CARTESIAN_POINT ( 'NONE',  ( 0.3335754702045168330, -1.976410766185803691, 0.8757516042032786885 ) ) ;
#90280=CARTESIAN_POINT ( 'NONE',  ( 6.566853775770633561, 1.536883091774071453, -1.387433097640700774 ) ) ;
#90282=CARTESIAN_POINT ( 'NONE',  ( 3.972077263441410100, 1.197190051160206936, 1.799587594625361220 ) ) ;
#90283=CARTESIAN_POINT ( 'NONE',  ( 4.582678730018482582, -1.317704446820912700, 1.530705718492784362 ) ) ;
#90284=CARTESIAN_POINT ( 'NONE',  ( 2.506241959165692812, 1.961374882610424919, 0.05109738790698423877 ) ) ;
#90290=CARTESIAN_POINT ( 'NONE',  ( 2.009000277268524481, 0.004839059525654776373, 2.016708403978189956 ) ) ;
#90293=CARTESIAN_POINT ( 'NONE',  ( 5.484596585704371030, -1.208295678440996390, 1.482354609825987213 ) ) ;
#90297=CARTESIAN_POINT ( 'NONE',  ( 3.181267708840180841, 1.591331833097202830, 1.238305487465785948 ) ) ;
#90300=CARTESIAN_POINT ( 'NONE',  ( 6.124008131756068174, -0.9624739961165188484, -1.431025375277717115 ) ) ;
#90305=CARTESIAN_POINT ( 'NONE',  ( 3.901501827272614964, -0.5455803081039903857, 1.789184164884791706 ) ) ;
#90307=CARTESIAN_POINT ( 'NONE',  ( 1.709917326824461181, 0.6048241955843024487, -1.979901091156407666 ) ) ;
#90318=CARTESIAN_POINT ( 'NONE',  ( 5.941025102908992217, -1.645668167864361431, -0.9802026474072849105 ) ) ;
#90319=CARTESIAN_POINT ( 'NONE',  ( 6.727182134110222478, 0.005875948494733079785, 1.810970247402940547 ) ) ;
#90321=EDGE_CURVE ( 'NONE', #205352, #165662, #130403, .T. ) ;
#90326=CARTESIAN_POINT ( 'NONE',  ( 2.764712544972968811, -1.491509591961352132, 1.564943835847030007 ) ) ;
#90329=CARTESIAN_POINT ( 'NONE',  ( 0.6156802735862786369, 1.737094954450137507, 1.216079458918501333 ) ) ;
#90330=CARTESIAN_POINT ( 'NONE',  ( 5.456004705108882469, 1.823398332572896186, -0.09148835057352226741 ) ) ;
#90332=CARTESIAN_POINT ( 'NONE',  ( 1.458210469330342374, 0.7952313087857125762, 1.804010633499957272 ) ) ;
#90333=CARTESIAN_POINT ( 'NONE',  ( 3.515784362865181478, -0.5505564139345071606, 1.831456330389509501 ) ) ;
#90336=CARTESIAN_POINT ( 'NONE',  ( 5.002387483831562953, 1.964158282178072312, 0.1467643733194800570 ) ) ;
#90337=CARTESIAN_POINT ( 'NONE',  ( 0.3220787244772654323, 1.858110058275804111, 0.5644625801373166496 ) ) ;
#90341=CARTESIAN_POINT ( 'NONE',  ( 6.533471381225442798, -0.1521382079053348602, 2.086446650026114735 ) ) ;
#90343=CARTESIAN_POINT ( 'NONE',  ( 3.527896108305649037, -1.883508717751972705, 0.3295761852530054159 ) ) ;
#90345=CARTESIAN_POINT ( 'NONE',  ( 0.7806487521475922176, -1.224371414366259625, 1.835764474286231129 ) ) ;
#90347=CARTESIAN_POINT ( 'NONE',  ( 6.270187311338969671, 2.007533000635489451, -0.1505373637035074819 ) ) ;
#90351=FACE_OUTER_BOUND ( 'NONE', #15721, .T. ) ;
#90352=CARTESIAN_POINT ( 'NONE',  ( 6.727182134110201162, 7.629137130509070275, 2.410944104600750038 ) ) ;
#90353=CARTESIAN_POINT ( 'NONE',  ( 1.996617168637443429, 2.047528291220417351, 0.3059219562495316125 ) ) ;
#90366=CARTESIAN_POINT ( 'NONE',  ( 6.825078400183516081, 0.5802287360496224400, 2.007770452540482697 ) ) ;
#90368=CARTESIAN_POINT ( 'NONE',  ( 4.939963660092479891, -1.468890173064988147, -0.9213945099728354515 ) ) ;
#90370=CARTESIAN_POINT ( 'NONE',  ( 2.957943426865859760, -0.6537446763684885420, 1.964363857337739105 ) ) ;
#90371=CARTESIAN_POINT ( 'NONE',  ( 3.111064062886280013, 0.05467929133608259024, 2.116691892344662929 ) ) ;
#90374=CARTESIAN_POINT ( 'NONE',  ( 1.375766793938013821, -1.922594530582939942, 0.4262983161763284623 ) ) ;
#90377=CARTESIAN_POINT ( 'NONE',  ( 0.2110004604562870645, 1.588762659912812403, -1.064147093309028680 ) ) ;
#90378=CARTESIAN_POINT ( 'NONE',  ( 3.556809736639905406, -2.021263576298555797, -1.081171400725000398 ) ) ;
#90379=CARTESIAN_POINT ( 'NONE',  ( 1.558932953716257730, -1.564965500463588732, -0.9399777662534372080 ) ) ;
#90383=CARTESIAN_POINT ( 'NONE',  ( 3.340093095703601023, -1.202498264213421209, -1.614455356613291093 ) ) ;
#90384=CARTESIAN_POINT ( 'NONE',  ( 2.975390029205774223, -0.1970676810524821243, 1.951864085487287959 ) ) ;
#90388=CARTESIAN_POINT ( 'NONE',  ( 6.562449924160270065, -1.910870307864566575, -0.8485530564429457634 ) ) ;
#90389=CARTESIAN_POINT ( 'NONE',  ( 4.135448415848129500, -1.220878049459400039, -1.281573189658680612 ) ) ;
#90391=CARTESIAN_POINT ( 'NONE',  ( 0.5159075615763093481, -1.175655012515547160, -1.849222068403690411 ) ) ;
#90392=CARTESIAN_POINT ( 'NONE',  ( 6.087833319296645840, -1.732659258567319505, -0.1633284621618599775 ) ) ;
#90394=CARTESIAN_POINT ( 'NONE',  ( 0.2331713839410602396, 2.030351879425442707, -2.369071045443218004 ) ) ;
#90395=CARTESIAN_POINT ( 'NONE',  ( 6.029976284357474903, -1.944044770632427976, 1.226447132130564999 ) ) ;
#90396=CARTESIAN_POINT ( 'NONE',  ( -0.1114211809780316365, -0.4883405756051837354, -2.144353428667714390 ) ) ;
#90397=CARTESIAN_POINT ( 'NONE',  ( 5.132092517088904238, 0.1681052705169924777, -1.725677682095213994 ) ) ;
#90398=CARTESIAN_POINT ( 'NONE',  ( 2.139570144280181108, -1.970530345926827742, 0.9937953903183869286 ) ) ;
#90399=CARTESIAN_POINT ( 'NONE',  ( 6.127409529368080143, 0.1660417618732710210, -2.164901972331951363 ) ) ;
#90401=CARTESIAN_POINT ( 'NONE',  ( 0.1986506717676014555, 1.455101728037408337, -1.538369530143603559 ) ) ;
#90402=CARTESIAN_POINT ( 'NONE',  ( 3.500000000000003109, -2.127848526677250785E-13, -2.052068128417947612 ) ) ;
#90404=CARTESIAN_POINT ( 'NONE',  ( 4.366181854897908998, 0.9076448143166337967, 1.699152538019559788 ) ) ;
#90406=CARTESIAN_POINT ( 'NONE',  ( 1.295894383074674749, 2.050542657126565249, -0.8545418985851579441 ) ) ;
#90411=CARTESIAN_POINT ( 'NONE',  ( 4.178555957833706813, 1.047420865545487523, 1.958865958838784005 ) ) ;
#90418=CARTESIAN_POINT ( 'NONE',  ( 2.057267738415057057, -1.238319999287675888, 1.591319116112683618 ) ) ;
#90420=CARTESIAN_POINT ( 'NONE',  ( 6.830530959611283315, -1.272493244265305634, 1.624195267664030995 ) ) ;
#90423=CARTESIAN_POINT ( 'NONE',  ( 6.532745107981281940, -1.550057735787165214, 0.7916670675358824516 ) ) ;
#90426=CARTESIAN_POINT ( 'NONE',  ( 1.879799676208588899, -0.9517657123069392933, 1.491821474084076726 ) ) ;
#90427=CARTESIAN_POINT ( 'NONE',  ( -0.1048463755018592264, -0.8645036352170620830, -1.819965476435807306 ) ) ;
#90428=CARTESIAN_POINT ( 'NONE',  ( 6.585563763084506306, -0.7354652392584435372, 1.576171286539735705 ) ) ;
#90429=CARTESIAN_POINT ( 'NONE',  ( 4.212625126225740146, 2.095743129530680537, 0.9292526312315220194 ) ) ;
#90431=CARTESIAN_POINT ( 'NONE',  ( 2.519273208346615167, -1.059988974693906183, -1.505194322970206722 ) ) ;
#90435=CARTESIAN_POINT ( 'NONE',  ( 3.276193339942961913, -1.088440757138483539, 1.465454812695582643 ) ) ;
#90436=CARTESIAN_POINT ( 'NONE',  ( 3.568982563115063567, -0.9913999084223242830, 1.755768870528086056 ) ) ;
#90438=CARTESIAN_POINT ( 'NONE',  ( 3.573342120354418672, 0.05797898436993471211, -2.261936065680466346 ) ) ;
#90440=CARTESIAN_POINT ( 'NONE',  ( 5.333084004640892495, 0.1517067650670254342, 2.100546829335631749 ) ) ;
#90442=CARTESIAN_POINT ( 'NONE',  ( 1.943885480841448965, 1.426152643941134501, 1.501071833787496645 ) ) ;
#90445=CARTESIAN_POINT ( 'NONE',  ( 6.322909428431959356, 1.571596504679906303, -1.423730336690950393 ) ) ;
#90448=CARTESIAN_POINT ( 'NONE',  ( 1.453605159173555705, 0.5596597320992221514, -1.843422129977128954 ) ) ;
#90456=CARTESIAN_POINT ( 'NONE',  ( 0.3170205077604414945, -0.7560223448306638838, -2.088923821510160650 ) ) ;
#90457=CARTESIAN_POINT ( 'NONE',  ( 2.714012760861806317, -2.083235677042583944, 0.3076118897425133003 ) ) ;
#90460=CARTESIAN_POINT ( 'NONE',  ( 6.473497990634856869, -0.2285008921534004422, 1.846817554525240990 ) ) ;
#90465=CARTESIAN_POINT ( 'NONE',  ( 0.4750491441844888474, -1.531729482103380224, 1.466773057065169361 ) ) ;
#90468=CARTESIAN_POINT ( 'NONE',  ( 2.822649888979886335, -1.354935067541668259, 1.419045635080482093 ) ) ;
#90469=CARTESIAN_POINT ( 'NONE',  ( 1.973706723050288936, 2.068691090354588091, -0.6273066937243013674 ) ) ;
#90475=CARTESIAN_POINT ( 'NONE',  ( 3.292619090915947844, 1.372597323508369715, 1.069791993016102172 ) ) ;
#90479=CARTESIAN_POINT ( 'NONE',  ( 2.020861031540205133, 2.010896488828680440, -0.1455087364366919322 ) ) ;
#90481=CARTESIAN_POINT ( 'NONE',  ( 0.09294085500742564621, -0.4768749645070144982, -2.116232079886640971 ) ) ;
#90482=CARTESIAN_POINT ( 'NONE',  ( 2.114083122616668309, -0.9278515453300213434, -1.739463596305758974 ) ) ;
#90486=VERTEX_POINT ( 'NONE', #193445 ) ;
#90488=EDGE_CURVE ( 'NONE', #150638, #11451, #28338, .T. ) ;
#90491=CARTESIAN_POINT ( 'NONE',  ( 2.209634141364385851, 1.562563088667227262, 1.279657157811086909 ) ) ;
#90493=CARTESIAN_POINT ( 'NONE',  ( 5.913149109437923379, 2.031366086520134395, 1.094794683655570644 ) ) ;
#90495=CARTESIAN_POINT ( 'NONE',  ( 2.588659458060487584, 1.901619664775334728, 0.4814403318105645591 ) ) ;
#90497=CARTESIAN_POINT ( 'NONE',  ( 0.7389079861009685279, 2.013985778099684154, -0.1017531103126300962 ) ) ;
#90499=CARTESIAN_POINT ( 'NONE',  ( 2.272804288956633112, -0.3671671630497001515, -2.085132402650377248 ) ) ;
#90501=CARTESIAN_POINT ( 'NONE',  ( 2.027068592762204080, -1.202062398780713748, -1.394650109237540070 ) ) ;
#90505=CARTESIAN_POINT ( 'NONE',  ( 3.885109016898561585, -1.979880364965879380, -0.7601140796509860964 ) ) ;
#90506=CARTESIAN_POINT ( 'NONE',  ( 0.6207436649305307919, -1.749090901066195691, 0.5750481222980761142 ) ) ;
#90510=CARTESIAN_POINT ( 'NONE',  ( 4.253237527111143557, -1.711175411557999348, -1.148025453137695662 ) ) ;
#90513=CARTESIAN_POINT ( 'NONE',  ( 1.171164436615620863, 1.096940724416964885, 1.478650282607060662 ) ) ;
#90519=CARTESIAN_POINT ( 'NONE',  ( 0.5400322017136415242, -1.563516176313231920, -1.557742479837947558 ) ) ;
#90520=CARTESIAN_POINT ( 'NONE',  ( 4.323666171361133514, -2.166671669000098444, 0.6512573085333557277 ) ) ;
#90523=CARTESIAN_POINT ( 'NONE',  ( 3.128980605277735361, 1.639808012139221116, 0.7702280095687010775 ) ) ;
#90524=CARTESIAN_POINT ( 'NONE',  ( 3.450306162294475065, -1.282734793626014280, 1.423081227541162841 ) ) ;
#90525=CARTESIAN_POINT ( 'NONE',  ( 4.018080225218490398, 2.055083638104511223, -0.2504045000601487492 ) ) ;
#90527=CARTESIAN_POINT ( 'NONE',  ( 2.817209029084859928, -0.1949976385870570150, 1.961808326198757335 ) ) ;
#90528=CARTESIAN_POINT ( 'NONE',  ( 0.8328817383555222609, 0.1387611642639074438, 1.921445197033289976 ) ) ;
#90529=CARTESIAN_POINT ( 'NONE',  ( 3.801501934187266230, -0.5436965770258190833, 1.789884385262895616 ) ) ;
#90530=CARTESIAN_POINT ( 'NONE',  ( 2.280263026629821166, 1.421315682977505546, 1.817977143087915026 ) ) ;
#90531=CARTESIAN_POINT ( 'NONE',  ( 4.193699477585779434, -1.282400645549033547, -1.348940618851623974 ) ) ;
#90536=CARTESIAN_POINT ( 'NONE',  ( 0.4343773424168140274, 1.080651816385242547, -1.807535387385241776 ) ) ;
#90540=CARTESIAN_POINT ( 'NONE',  ( 6.802040682177005415, -2.161276877365316818, 0.04550429416337595928 ) ) ;
#90541=CARTESIAN_POINT ( 'NONE',  ( 2.109781586379317897, 1.642293606977158538, 1.341614810521203349 ) ) ;
#90543=CARTESIAN_POINT ( 'NONE',  ( 0.9846354891296082990, -1.278160710921724341, 1.563951078967614094 ) ) ;
#90547=CARTESIAN_POINT ( 'NONE',  ( 1.177287030172860183, -0.05180490295666682898, -2.161124318685260004 ) ) ;
#90549=CARTESIAN_POINT ( 'NONE',  ( 6.825078400183575589, 6.038285016609903799, 2.450557349082567171 ) ) ;
#90552=CARTESIAN_POINT ( 'NONE',  ( -0.2104748580754426390, 2.865278511227669078, -2.591885361450113834 ) ) ;
#90553=CARTESIAN_POINT ( 'NONE',  ( 5.717982508692024624, 0.9896897593998502662, -1.756851901128737348 ) ) ;
#90558=CARTESIAN_POINT ( 'NONE',  ( 0.8489190418228099722, 0.6593363751366092540, 2.164330503585075505 ) ) ;
#90563=CARTESIAN_POINT ( 'NONE',  ( 0.7904806358284102163, 1.449672126929082872, -1.252262404471200075 ) ) ;
#90565=B_SPLINE_CURVE_WITH_KNOTS ( 'NONE', 3,
 ( #57180, #122272, #152540, #88626, #151489, #56115, #153617, #187166, #167725, #5189, #6266, #89701, #188230, #71264, #86476, #154682, #73413, #55047, #137378, #4126, #203394, #104876, #170919, #22515, #135250, #23592, #72337, #138443, #204461, #7336, #139516, #85404, #39870, #189307, #105979, #172002, #101657, #3058, #185020, #201263, #52903, #119037, #102731, #168787, #20392, #128667, #91839, #43090, #208740, #109203, #175216, #127607, #28947, #107052, #26799, #9491, #27875, #173078, #59304, #192491, #141672, #156827, #124401, #160012, #10543, #76618, #60367, #126530, #74500, #210877, #61440, #157897, #93971, #90766, #209805, #92903, #44143, #24659, #125462, #11613, #95031, #75563, #140604, #40946, #144870, #8414, #206616, #207684, #78747, #158949, #191424, #142731, #110264, #58244, #177333, #77687, #176273, #143808, #161081, #12671, #190359, #193572, #45215, #62502, #42021, #108130, #174156, #111330, #25729, #80894, #97166, #96101, #195715, #196772, #67794, #31094, #48415, #148033, #114527, #180521, #66727, #163221, #164275, #162156, #32143, #194635, #84081, #182639, #98223, #15865, #81950, #14803, #50521, #146984, #213001, #181572, #46277, #13743, #214043, #65669, #131817, #34261, #197826, #116644, #17991, #49458, #47350, #145928, #115576, #660, #100333, #79816, #33201, #198874, #166400, #99285, #165332, #150169, #16926, #129731, #132870, #1737, #64638, #112393, #178405, #83006, #30016, #211940, #63575, #149082, #113465, #179470, #130777, #155488, #136048, #153355, #69937, #37462, #122006, #53720, #103540, #7071, #202060, #119853, #3863, #72074, #133944, #185831, #169600, #134994, #23328, #19068, #167472, #4925, #186906, #21184, #87286, #183712, #20132, #39599, #71002, #204194, #85146, #137115, #138184, #55849, #203144, #54786, #171730, #120933, #68874, #6004, #117722, #36390, #38538, #201004, #187972, #52649, #104615, #105702, #89436, #170663, #118778, #101398, #199951, #22250, #88360, #154425, #51598, #86218, #168534, #35319, #102468, #151233, #2802, #184763, #152289, #189049, #156565, #192231, #42833, #143549, #75304, #176021, #190108, #9232, #139249, #107874, #93713, #40686, #91582, #28691, #73143, #41761, #110008, #177075, #157634, #173899, #172817, #160825, #94777, #26542, #125203, #57983, #124146, #140338, #206356, #77432, #90501, #205280, #27613, #61185, #25475, #141419, #207426, #108939, #56919, #142471, #59045, #123092, #24389, #193315, #8160, #43894, #106789, #74244, #191166, #11351, #174960, #92650, #10290, #208479, #158692, #76364, #159754, #60115, #126274, #209543, #127345, #44961, #111069, #161904, #13491, #79566, #99027, #63319, #34007, #144614, #14546, #78497, #132616, #194383, #15610, #97976, #145685, #46026, #100081, #80643, #31899, #162967, #130532, #146735, #195462, #213797, #210629, #30839, #164035, #113209, #62255, #112146, #212753, #114278, #128416, #82759, #64387, #115334, #129480, #196523, #178149, #47091, #32953, #181325, #48166, #81698, #29763, #96916, #131569, #404, #165083, #180275, #211683, #65420, #198623, #147781, #197570, #179214, #49214, #16674, #148832, #66477, #95848, #50270, #116388, #182377, #12417, #88101, #5740, #83818, #200751, #121751, #118527, #186655, #154173, #71817, #35061, #70748, #17729, #199692, #187719, #104358, #39347, #166143, #2544, #168280, #119597, #19880, #85963 ),
 .UNSPECIFIED., .F., .F.,
 ( 4, 1, 1, 1, 1, 1, 1, 1, 1, 1, 1, 1, 1, 1, 1, 1, 1, 1, 1, 1, 1, 1, 1, 1, 1, 1, 1, 1, 1, 1, 1, 1, 1, 1, 1, 1, 1, 1, 1, 1, 1, 1, 1, 1, 1, 1, 1, 1, 1, 1, 1, 1, 1, 1, 1, 1, 1, 1, 1, 1, 1, 1, 1, 1, 1, 1, 1, 1, 1, 1, 1, 1, 1, 1, 1, 1, 1, 1, 1, 1, 1, 1, 1, 1, 1, 1, 1, 1, 1, 1, 1, 1, 1, 1, 1, 1, 1, 1, 1, 1, 1, 1, 1, 1, 1, 1, 1, 1, 1, 1, 1, 1, 1, 1, 1, 1, 1, 1, 1, 1, 1, 1, 1, 1, 1, 1, 1, 1, 1, 1, 1, 1, 1, 1, 1, 1, 1, 1, 1, 1, 1, 1, 1, 1, 1, 1, 1, 1, 1, 1, 1, 1, 1, 1, 1, 1, 1, 1, 1, 1, 1, 1, 1, 1, 1, 1, 1, 1, 1, 1, 1, 1, 1, 1, 1, 1, 1, 1, 1, 1, 1, 1, 1, 1, 1, 1, 1, 1, 1, 1, 1, 1, 1, 1, 1, 1, 1, 1, 1, 1, 1, 1, 1, 1, 1, 1, 1, 1, 1, 1, 1, 1, 1, 1, 1, 1, 1, 1, 1, 1, 1, 1, 1, 1, 1, 1, 1, 1, 1, 1, 1, 1, 1, 1, 1, 1, 1, 1, 1, 1, 1, 1, 1, 1, 1, 1, 1, 1, 1, 1, 1, 1, 1, 1, 1, 1, 1, 1, 1, 1, 1, 1, 1, 1, 1, 1, 1, 1, 1, 1, 1, 1, 1, 1, 1, 1, 1, 1, 1, 1, 1, 1, 1, 1, 1, 1, 1, 1, 1, 1, 1, 1, 1, 1, 1, 1, 1, 1, 1, 1, 1, 1, 1, 1, 1, 1, 1, 1, 1, 1, 1, 1, 1, 1, 1, 1, 1, 1, 1, 1, 1, 1, 1, 1, 1, 1, 1, 1, 1, 1, 1, 1, 1, 1, 1, 1, 1, 1, 1, 1, 1, 1, 1, 1, 1, 1, 1, 1, 1, 1, 1, 1, 1, 1, 1, 1, 1, 1, 1, 1, 1, 1, 1, 1, 1, 1, 1, 1, 1, 1, 1, 1, 1, 1, 1, 1, 1, 1, 1, 1, 1, 1, 1, 1, 4 ),
 ( 0.000000000000000000, 0.002600209826155936224, 0.005208878553436857226, 0.007813350965615119270, 0.01041570154746907992, 0.01302155883015148306, 0.01562460066207539862, 0.01822947720112986364, 0.02083337797298438765, 0.02343721533725894035, 0.02604213897589890969, 0.02864525980212044229, 0.03125073504456635232, 0.03385369766904555017, 0.03645898980682723417, 0.03906240375024701977, 0.04166680464497042602, 0.04427120869897264999, 0.04687461886132015393, 0.04947991130494613921, 0.05208287402783655373, 0.05468834688957619622, 0.05729146186993632622, 0.05989639238693608009, 0.06250023923939096449, 0.06510408216679804128, 0.06770901469741306966, 0.07031212675311915294, 0.07291759917081726272, 0.07552056149378454097, 0.07812585104223603027, 0.08072926279340975064, 0.08333366149866272554, 0.08593806365491549193, 0.08854147146176674643, 0.09114676191340240208, 0.09374972248801059782, 0.09635519323906190092, 0.09895830628708340848, 0.1015632345865536273, 0.1041670796237980645, 0.1067709202568039306, 0.1093758509056654005, 0.1119789607794838548, 0.1145844312107493490, 0.1171873915655986947, 0.1197926790194954738, 0.1223960889855860712, 0.1250004854864837645, 0.1276048858798866925, 0.1302082914968497596, 0.1328135800830011481, 0.1354165386474412147, 0.1380220074263333041, 0.1406251186789811980, 0.1432300448973659046, 0.1458338882574615747, 0.1484377267335943440, 0.1510426556371624596, 0.1536457634674935069, 0.1562512320483212536, 0.1588541905735017246, 0.1614594760690261366, 0.1640628843880489185, 0.1666672788216651824, 0.1692716775892487424, 0.1718750811543677814, 0.1744803680111783883, 0.1770833247038955116, 0.1796887916465979840, 0.1822919012421508056, 0.1848968255159594287, 0.1875006673364670307, 0.1901045037933276616, 0.1927094310880738681, 0.1953125370132051675, 0.1979180038795354257, 0.2005209607134520455, 0.2031262443867272172, 0.2057296511966431873, 0.2083340436999963075, 0.2109384409787386505, 0.2135418426300015604, 0.2161471278935624962, 0.2187500828529475860, 0.2213555480953768861, 0.2239586561720615654, 0.2265635786377499516, 0.2291674190561798496, 0.2317712536313151217, 0.2343761794536610432, 0.2369792836118274071, 0.2395847488995502261, 0.2421877041805577391, 0.2447929861676560459, 0.2473963916063780244, 0.2500007823164346887, 0.2526051782432667259, 0.2552085781186103075, 0.2578138619249652486, 0.2604168152893601151, 0.2630222789673848927, 0.2656253856633817301, 0.2682303064573571261, 0.2708341456111751366, 0.2734379784420828963, 0.2760429029284052760, 0.2786460054577940548, 0.2812514693027542978, 0.2838544231691620401, 0.2864597036061101165, 0.2890631078115080133, 0.2916674968651886135, 0.2942718915769991783, 0.2968752898143142138, 0.2994805722994643427, 0.3020835242071668869, 0.3046889864566129091, 0.3072920919100609050, 0.3098970111686871198, 0.3125008491953192857, 0.3151046804194536644, 0.3177096037060897493, 0.3203127047448455222, 0.3229181672828482230, 0.3255211198729257016, 0.3281263988957095479, 0.3307298020056156362, 0.3333341895397992083, 0.3359385831734401084, 0.3385419799105768290, 0.3411472612104861635, 0.3437502117997557338, 0.3463556727564109927, 0.3489587771054129539, 0.3515636949650152721, 0.3541675320018531359, 0.3567713617566292128, 0.3593762839798815834, 0.3619793836661120978, 0.3645848450329270407, 0.3671877964849088460, 0.3697930742294792128, 0.3723964763816929868, 0.3750008625332226786, 0.3776052552255140804, 0.3802086506002868016, 0.3828139308508870520, 0.3854168802599494681, 0.3880223400595693151, 0.3906254434421968513, 0.3932303600390676390, 0.3958341962234732669, 0.3984380246462727593, 0.4010429459424146859, 0.4036460444141952153, 0.4062515047455624306, 0.4088544551976535102, 0.4114597317999305615, 0.4140631331322238151, 0.4166675180379114662, 0.4192719099256467796, 0.4218753040758395079, 0.4244805834130354061, 0.4270835317800880659, 0.4296889905584002634, 0.4322920931126992272, 0.4348970085831024290, 0.4375008440524135733, 0.4401046712805898320, 0.4427095917858701601, 0.4453126891812490551, 0.4479181486128839262, 0.4505210982032648026, 0.4531263737991432228, 0.4557297744492659897, 0.4583341582458977381, 0.4609385494658484461, 0.4635419425292200413, 0.4661472210888942258, 0.4687501685521111572, 0.4713556264448209299, 0.4739587283088163017, 0.4765636427889929916, 0.4791674776805284197, 0.4817713038514113699, 0.4843762237020596273, 0.4869793201590638665, 0.4895847788266616818, 0.4921877276934932821, 0.4947930024188478271, 0.4973964025245324327, 0.5000007853488734888, 0.5026051760377950872, 0.5052085681520839255, 0.5078138460701020485, 0.5104167927676396266, 0.5130222499104345468, 0.5156253512221359303, 0.5182302648483090302, 0.5208340992993732987, 0.5234379245502747136, 0.5260428438825063280, 0.5286459395391455152, 0.5312513975783873521, 0.5338543458598166147, 0.5364596198505067193, 0.5390630195494738874, 0.5416674015382738627, 0.5442717918329101900, 0.5468751831358398263, 0.5494804605480556603, 0.5520834066180569932, 0.5546888631466128095, 0.5572919640440190392, 0.5598968769523987588, 0.5625007111002878757, 0.5651045355685063720, 0.5677094545185276120, 0.5703125495128006373, 0.5729180070593572482, 0.5755209548935220631, 0.5781262282853970591, 0.5807296277153600750, 0.5833340090053582561, 0.5859383990424469335, 0.5885417896717308750, 0.5911470667139914204, 0.5937500122945923442, 0.5963554683445766447, 0.5989585689656815592, 0.6015634812924701702, 0.6041673152744758690, 0.6067711390973024033, 0.6093760578013157625, 0.6119791522712144660, 0.6145846094607528842, 0.6171875569857874222, 0.6197928299146914233, 0.6223962292133623508, 0.6250006099412922511, 0.6276049998575695676, 0.6302083899509167697, 0.6328136667590675835, 0.6354166119884008257, 0.6380220676954796444, 0.6406251681782773044, 0.6432300800596744139, 0.6458339140130902045, 0.6484377373278128465, 0.6510426559220214848, 0.6536457500055372627, 0.6562512069737248543, 0.6588541543277639523, 0.6614594269295416273, 0.6640628262346358612, 0.6666672065372305500, 0.6692715964694370134, 0.6718749861645568755, 0.6744802628744462902, 0.6770832078906477980, 0.6796886633904898334, 0.6822917638729786294, 0.6848966754451861760, 0.6875005095073121186, 0.6901043324512210475, 0.6927092510718347862, 0.6953123449069624762, 0.6979178017894718256, 0.7005207491106575368, 0.7031260215211581066, 0.7057294209703992571, 0.7083338009843969107, 0.7109381910692819107, 0.7135415805038890502, 0.7161468572513741693, 0.7187498021925872171, 0.7213552576208688283, 0.7239583582410578089, 0.7265632696402853918, 0.7291671039484327599, 0.7317709266588259265, 0.7343758454420658000, 0.7369789391668094547, 0.7395843960993241373, 0.7421873435258099505, 0.7447926158808931829, 0.7473960156120186271, 0.7500003954741673029, 0.7526047858484943287, 0.7552081751603144655, 0.7578134520812660480, 0.7604163970856469001, 0.7630218525780576577, 0.7656249534739711926, 0.7682298648364407345, 0.7708336995279378989, 0.7734375221421257995, 0.7760424412242287184, 0.7786455349766069345, 0.7812509920948264019, 0.7838539397647821261, 0.7864592122003229990, 0.7890626123510894319, 0.7916669921981516200, 0.7942713829987035901, 0.7968747723254782089, 0.7994800495557851105, 0.8020829947615083499, 0.8046884504537559213, 0.8072915517634385862, 0.8098964632253897733, 0.8125002984375870874, 0.8151041210928977598, 0.8177090406101226172, 0.8203121345281733090, 0.8229175919678175521, 0.8255205400194353116, 0.8281258126713292311, 0.8307292133795166622, 0.8333335933482756142, 0.8359379847118599827, 0.8385413741913512187, 0.8411466518669262760, 0.8437495974121898001, 0.8463550534400045011, 0.8489581553015269622, 0.8515630669992224622, 0.8541669028694969246, 0.8567707257032814994, 0.8593756457919137226, 0.8619787400136992295, 0.8645841979105142183, 0.8671871464820134490, 0.8697924194861808012, 0.8723958208895988831, 0.8750002011168627192, 0.8776045931803160283, 0.8802079829503125508, 0.8828132612070975771, 0.8854162072301272612, 0.8880216637292678294, 0.8906247662807315058, 0.8932296783504612980, 0.8958335150162225480, 0.8984373381658604663, 0.9010422589622166800, 0.9036453536258294283, 0.9062508121155921081, 0.9088537613452241093, 0.9114590348376164775, 0.9140624370741091687, 0.9166668176967164294, 0.9192712105969091940, 0.9218746007952320909, 0.9244798797692056480, 0.9270828264082496828, 0.9296882835145078294, 0.9322913868941045124, 0.9348962994721256026, 0.9375001370706889103, 0.9401039606740361210, 0.9427088823143441321, 0.9453119775565693717, 0.9479174367776000976, 0.9505203868030935865, 0.9531256609099927335, 0.9557290641454977420, 0.9583334452981105978, 0.9609378390199675435, 0.9635412300619400350, 0.9661465102466426647, 0.9687494557931184413, 0.9713549143510965544, 0.9739580252604012056, 0.9765629275426017664, 0.9791667581373608709, 0.9817706348486141543, 0.9843755007711335603, 0.9869785191422796311, 0.9895843624858681187, 0.9921867025132995455, 0.9947911529560371502, 0.9973998138561904758, 1.000000000000000000 ),
 .UNSPECIFIED. ) ;
#90568=CARTESIAN_POINT ( 'NONE',  ( 2.842114037233371082, 1.711851238368550909, 0.2109339381748502329 ) ) ;
#90571=CARTESIAN_POINT ( 'NONE',  ( 0.9129390864682377371, -0.2673504635808711671, 1.749312949811430373 ) ) ;
#90572=CARTESIAN_POINT ( 'NONE',  ( 1.506495127224609876, -2.003582159550582276, -0.1952931609562995052 ) ) ;
#90574=CARTESIAN_POINT ( 'NONE',  ( 4.050008041959299199, 0.7462531942188169731, -2.076888956485785975 ) ) ;
#90578=CARTESIAN_POINT ( 'NONE',  ( 4.336665864168765872, 1.303721989063952424, -1.672289659653345639 ) ) ;
#90579=CARTESIAN_POINT ( 'NONE',  ( 4.060172857048785389, -1.158672032380179573, 1.650094836768666084 ) ) ;
#90580=CARTESIAN_POINT ( 'NONE',  ( 3.726654843667742689, 1.277109331127034952, -1.285116454894990268 ) ) ;
#90584=CARTESIAN_POINT ( 'NONE',  ( 1.762360912074714125, -1.325010844092512796, 1.320751239342173200 ) ) ;
#90586=CARTESIAN_POINT ( 'NONE',  ( 6.217409598193539999, -0.2183660865492654257, 1.812524795094340835 ) ) ;
#90595=CARTESIAN_POINT ( 'NONE',  ( 3.902672080109194752, -2.098000727953463151, -0.3078000538283760523 ) ) ;
#90596=CARTESIAN_POINT ( 'NONE',  ( -0.02948999725181991258, 7.629137130509059617, -2.526318448094333480 ) ) ;
#90598=CARTESIAN_POINT ( 'NONE',  ( 3.971915101536928283, 1.092440305464415840, 1.640793377567103528 ) ) ;
#90600=CARTESIAN_POINT ( 'NONE',  ( 0.07056460990086978191, 0.7743322593966313061, 1.858523817361916963 ) ) ;
#90602=CARTESIAN_POINT ( 'NONE',  ( 0.07011551774125344971, -0.9937341303020963412, 1.869520526064169408 ) ) ;
#90604=CARTESIAN_POINT ( 'NONE',  ( 1.328672132201724532, -1.314895749051579132, 1.599177317581280455 ) ) ;
#90609=CARTESIAN_POINT ( 'NONE',  ( 3.591813267288586520, -2.088258123952376977, -0.1022297611361303732 ) ) ;
#90612=CARTESIAN_POINT ( 'NONE',  ( 2.186296784933777992, -1.789763940591000191, -0.3589617604915079085 ) ) ;
#90613=CARTESIAN_POINT ( 'NONE',  ( 1.207327558334120754, 1.371319684050668730, 1.183719584703796679 ) ) ;
#90616=CARTESIAN_POINT ( 'NONE',  ( 5.936183876523434932, 1.091049494364674466, -1.918236432931222257 ) ) ;
#90618=CARTESIAN_POINT ( 'NONE',  ( 4.243358471946375943, -1.921622210924242458, 1.084848892642875429 ) ) ;
#90621=CARTESIAN_POINT ( 'NONE',  ( 2.947808941170467545, -1.285945688040548207, -1.415481726668985196 ) ) ;
#90623=CARTESIAN_POINT ( 'NONE',  ( 4.879381568908511824, -0.1049739508458477355, 2.067839077007492143 ) ) ;
#90626=CARTESIAN_POINT ( 'NONE',  ( 5.653911837654605144, 0.8871495062587383407, 2.004161502255866090 ) ) ;
#90633=CARTESIAN_POINT ( 'NONE',  ( -0.1104750535120025967, -0.004616138082884357029, -2.103378236956429337 ) ) ;
#90636=CARTESIAN_POINT ( 'NONE',  ( 5.524307029080702591, 1.015476208609331188, 1.803995072556117574 ) ) ;
#90637=CARTESIAN_POINT ( 'NONE',  ( 4.283760221956850245, 1.259274395394771817, 1.458037640750938779 ) ) ;
#90638=CARTESIAN_POINT ( 'NONE',  ( 0.1754079408978586052, 1.496066871905444629, 1.352139405095334590 ) ) ;
#90642=CARTESIAN_POINT ( 'NONE',  ( 6.685440801012543233, -0.9854850593251741619, 2.067252628450669594 ) ) ;
#90643=CARTESIAN_POINT ( 'NONE',  ( 5.725187622324654946, -0.04035785615889506128, 1.825416780793003069 ) ) ;
#90650=CARTESIAN_POINT ( 'NONE',  ( 2.243484787601189634, 1.840893492186860492, 0.04347913094143729396 ) ) ;
#90651=CARTESIAN_POINT ( 'NONE',  ( 6.345953593097265255, -1.318148336383131669, -1.521719194605136494 ) ) ;
#90652=CARTESIAN_POINT ( 'NONE',  ( 0.8436309607196719185, -1.274966737007717343, 1.912178556870794521 ) ) ;
#90653=CARTESIAN_POINT ( 'NONE',  ( 6.578960362708798471, 1.829258725439562916, 0.7091506158454219388 ) ) ;
#90656=CARTESIAN_POINT ( 'NONE',  ( 0.4849360239999983557, 1.980737741294085419, 0.6024896509310638804 ) ) ;
#90658=CARTESIAN_POINT ( 'NONE',  ( 2.964485117831549665, -1.932750628810533389, -0.7978010075700513459 ) ) ;
#90659=CARTESIAN_POINT ( 'NONE',  ( 1.481098450213329976, 1.729700800547562478, -0.7128637423776186255 ) ) ;
#90660=CARTESIAN_POINT ( 'NONE',  ( 1.598982282203027516, 0.9961506480390787122, -1.752761228829378126 ) ) ;
#90662=ORIENTED_EDGE ( 'NONE', *, *, #30212, .T. ) ;
#90664=CARTESIAN_POINT ( 'NONE',  ( 1.645671328968565605, 0.5460171089132167532, 1.652615436037402130 ) ) ;
#90668=CARTESIAN_POINT ( 'NONE',  ( 2.894803161253765467, 1.479297447286776590, -0.8868043451095276586 ) ) ;
#90669=CARTESIAN_POINT ( 'NONE',  ( 3.140350738262797314, 0.5347024899306859202, 2.125194831261326911 ) ) ;
#90670=CARTESIAN_POINT ( 'NONE',  ( 5.408869034151480903, 1.673104959687292448, -1.439203791633147267 ) ) ;
#90673=CARTESIAN_POINT ( 'NONE',  ( 2.026474435558190734, 1.113403481674969608, 1.863675736879222278 ) ) ;
#90674=CARTESIAN_POINT ( 'NONE',  ( 1.172165686010542274, -1.159919637379997814, 1.409874495853599141 ) ) ;
#90675=SURFACE_SIDE_STYLE ('',( #139421 ) ) ;
#90676=CARTESIAN_POINT ( 'NONE',  ( 4.522735144945882801, 0.3654406173194921781, 2.085432885242066270 ) ) ;
#90680=CARTESIAN_POINT ( 'NONE',  ( 4.247812404936269992, 2.291854478692372687, -0.05604449276840757499 ) ) ;
#90684=CARTESIAN_POINT ( 'NONE',  ( 0.2762449081346768365, 2.096790360132039233, -0.3154013857558089495 ) ) ;
#90689=CARTESIAN_POINT ( 'NONE',  ( 6.825078400183556049, 7.053092130845653784, 2.453807127456457238 ) ) ;
#90691=CARTESIAN_POINT ( 'NONE',  ( 5.713517581197447015, 1.944070655204039433, 0.5350908816983344085 ) ) ;
#90693=CARTESIAN_POINT ( 'NONE',  ( 3.414939784243501641, -1.565044402038212379, 1.343584798420148774 ) ) ;
#90695=CARTESIAN_POINT ( 'NONE',  ( -0.2408018239684642792, 7.629137130509051623, -2.700476273684692785 ) ) ;
#90699=CARTESIAN_POINT ( 'NONE',  ( 6.492125937493531396, -0.5805207454109837517, -2.113085764653479082 ) ) ;
#90700=CARTESIAN_POINT ( 'NONE',  ( 3.393204081532863459, -0.8197727808607684352, -1.842447475547980495 ) ) ;
#90701=CARTESIAN_POINT ( 'NONE',  ( 3.280630368989821743, 1.663260157205956880, -0.7901080472864712156 ) ) ;
#90705=CARTESIAN_POINT ( 'NONE',  ( 6.809597967592865508, -0.3964169337347979161, 1.788522171948719874 ) ) ;
#90706=CARTESIAN_POINT ( 'NONE',  ( 0.3175262209036809891, 1.174723722100686762, -1.975753589677962552 ) ) ;
#90708=CARTESIAN_POINT ( 'NONE',  ( 6.825078400183548055, -0.008500281443135982926, 2.244262395727573356 ) ) ;
#90709=CARTESIAN_POINT ( 'NONE',  ( 2.280028682641733973, 1.296546612978483504, 1.659573824544317455 ) ) ;
#90718=CARTESIAN_POINT ( 'NONE',  ( 4.025785557498418044, -0.3775041287265075152, 2.188942893082143293 ) ) ;
#90719=CARTESIAN_POINT ( 'NONE',  ( 1.974822964535282610, -0.1094934731284517848, -2.188836591978132518 ) ) ;
#90721=CARTESIAN_POINT ( 'NONE',  ( 0.5224629442122545875, -1.184049029929446828, -1.862174541895257995 ) ) ;
#90723=CARTESIAN_POINT ( 'NONE',  ( 4.545333077707183200, 1.753367681936630840, -0.8802267832125689750 ) ) ;
#90729=CARTESIAN_POINT ( 'NONE',  ( 3.041385797112206912, 0.05609166564453024750, 2.120036961950934273 ) ) ;
#90731=CARTESIAN_POINT ( 'NONE',  ( 4.997027575558514734, 1.799266821141291661, -1.197868618907194316 ) ) ;
#90732=CARTESIAN_POINT ( 'NONE',  ( 4.177188522404684079, 1.205947341878073287, 1.391433828303423326 ) ) ;
#90735=CARTESIAN_POINT ( 'NONE',  ( 0.3975144409600079309, -0.5839149016878465437, -1.639678601710597983 ) ) ;
#90736=CARTESIAN_POINT ( 'NONE',  ( 6.727182134110231360, 6.039168392632435989, 2.405853653942995773 ) ) ;
#90739=CARTESIAN_POINT ( 'NONE',  ( 3.854492016355787420, 0.7758605394001509836, 2.017853709245204463 ) ) ;
#90742=CARTESIAN_POINT ( 'NONE',  ( 5.255232437486731634, -2.000551055875991580, -0.2495666058281582056 ) ) ;
#90745=CARTESIAN_POINT ( 'NONE',  ( 4.012696165952275962, 1.530467462299599513, -1.526897427004340280 ) ) ;
#90746=CARTESIAN_POINT ( 'NONE',  ( 4.218015588379292247, -1.010805368333337562, -1.692340417948991371 ) ) ;
#90748=CARTESIAN_POINT ( 'NONE',  ( -0.02351032182101517320, -2.127384168920816165, -0.5261613093957145937 ) ) ;
#90749=CARTESIAN_POINT ( 'NONE',  ( 0.5698726823011552867, 0.2221484770595567870, -2.296888066578778087 ) ) ;
#90750=CARTESIAN_POINT ( 'NONE',  ( 4.024726114628586870, 1.955573890245201785, 0.6501785607586229032 ) ) ;
#90751=CARTESIAN_POINT ( 'NONE',  ( 5.636261916347573120, 0.3829244189050336478, 1.903776902374450630 ) ) ;
#90757=CARTESIAN_POINT ( 'NONE',  ( 2.204404769108789797, -2.206272049354717879, 0.05393164079612459277 ) ) ;
#90760=CARTESIAN_POINT ( 'NONE',  ( 6.420756404446519738, -1.389671697431221542, 1.384925340169262054 ) ) ;
#90761=CARTESIAN_POINT ( 'NONE',  ( -0.02880301295726198432, 6.946859453142047336, -2.868871865197111681 ) ) ;
#90766=CARTESIAN_POINT ( 'NONE',  ( 5.454971364017034752, 0.3553261626877933788, -1.806350769464920569 ) ) ;
#90768=CARTESIAN_POINT ( 'NONE',  ( 2.659116476608857305, -1.792500920499852546, -1.016832356063899656 ) ) ;
#90774=CARTESIAN_POINT ( 'NONE',  ( 0.7255486961553169190, -1.957115920898297112, 0.6459669076722980297 ) ) ;
#90776=CARTESIAN_POINT ( 'NONE',  ( 4.792441439910442469, 1.527937338083688923, -1.027124420945781935 ) ) ;
#90779=CARTESIAN_POINT ( 'NONE',  ( -0.2409995289980246258, 2.020898751655671788, -2.415740196953279462 ) ) ;
#90781=CARTESIAN_POINT ( 'NONE',  ( 4.160898416275903067, -1.636102012888400292, 1.481223685352812680 ) ) ;
#90782=CARTESIAN_POINT ( 'NONE',  ( 0.4917760118960182170, 1.601382895956671826, 1.452064325093614716 ) ) ;
#90784=CARTESIAN_POINT ( 'NONE',  ( 0.6856317642073318508, 1.842354612247762091, -0.5124485439033445999 ) ) ;
#90785=CARTESIAN_POINT ( 'NONE',  ( 0.7785302072789467287, -0.4946362931835950327, -1.954778448132548752 ) ) ;
#90788=CARTESIAN_POINT ( 'NONE',  ( 6.305323439471717251, 1.661359358424657318, -0.9468341723649562613 ) ) ;
#90789=CARTESIAN_POINT ( 'NONE',  ( 0.6724591444495706671, -1.759989063064151038, -0.6342292696241008665 ) ) ;
#90790=CARTESIAN_POINT ( 'NONE',  ( 1.850796360583713884, -1.845628094615419768, -0.8128149310912060610 ) ) ;
#90794=CARTESIAN_POINT ( 'NONE',  ( 3.598352328373265685, -2.103663943315597251, -0.1031874809700270568 ) ) ;
#90799=CARTESIAN_POINT ( 'NONE',  ( 3.726823374262774990, 1.425363347867984798, -1.431309510556647346 ) ) ;
#90802=CARTESIAN_POINT ( 'NONE',  ( 4.130267194010744269, 1.160198474277823300, -1.823679694223250491 ) ) ;
#90808=CARTESIAN_POINT ( 'NONE',  ( 2.313135284333038832, -1.679484837851461965, 1.376015783590480934 ) ) ;
#90811=CARTESIAN_POINT ( 'NONE',  ( 1.223879446662301307, 1.774596971308094018, 0.4907264878865265634 ) ) ;
#90813=CARTESIAN_POINT ( 'NONE',  ( 3.280998142716429200, 1.980384277226649559, -0.9389412094223739125 ) ) ;
#90815=CARTESIAN_POINT ( 'NONE',  ( 4.153392199625399073, -1.879142691831453105, -1.259808711832038464 ) ) ;
#90817=CARTESIAN_POINT ( 'NONE',  ( 4.645720405014278853, 1.993893748393640086, -0.3006458143828410479 ) ) ;
#90822=CARTESIAN_POINT ( 'NONE',  ( 4.833122733705673468, -1.618250600028045216, 0.7167863974541763827 ) ) ;
#90824=CARTESIAN_POINT ( 'NONE',  ( 0.2882880397960294605, -0.9922573751702695732, 1.857558580286112981 ) ) ;
#90828=CARTESIAN_POINT ( 'NONE',  ( 0.7659823462377189918, -1.960405762330315049, 0.1893847968462581133 ) ) ;
#90831=CARTESIAN_POINT ( 'NONE',  ( 5.607607993782223410, 1.377354484090735243, 1.176896650239395603 ) ) ;
#90835=CARTESIAN_POINT ( 'NONE',  ( 5.172658500931742509, -1.761684834526537680, -0.6294727512598657926 ) ) ;
#90837=CARTESIAN_POINT ( 'NONE',  ( 4.012602964903419611, 0.7404812365185128309, 1.933494928807255153 ) ) ;
#90847=CARTESIAN_POINT ( 'NONE',  ( 4.422284181769401634, 0.9229163912191931107, 1.731201473044993167 ) ) ;
#90849=CARTESIAN_POINT ( 'NONE',  ( 2.161482305958133399, -0.5350050527693461788, -1.943774068525660148 ) ) ;
#90853=CARTESIAN_POINT ( 'NONE',  ( 1.651402116136031051, 0.5479989942898423338, -1.788454331708405620 ) ) ;
#90855=CARTESIAN_POINT ( 'NONE',  ( 3.797138801009732667, -0.2017130330635922841, -2.003102573442970158 ) ) ;
#90857=CARTESIAN_POINT ( 'NONE',  ( 3.445011857661818944, -1.868279436719679110, -0.9960484452814029055 ) ) ;
#90858=CARTESIAN_POINT ( 'NONE',  ( 6.825078400183544503, 3.684911640780349718, 2.658296617506946458 ) ) ;
#90859=CARTESIAN_POINT ( 'NONE',  ( 4.439934286204096914, 1.349936692791346093, 1.569845735447549906 ) ) ;
#90861=CARTESIAN_POINT ( 'NONE',  ( 0.2750908068406934803, 1.949304727321942599, -0.7563943737528535660 ) ) ;
#90863=CARTESIAN_POINT ( 'NONE',  ( 5.807590115592688562, -0.4411735188285180187, 1.771332044933016547 ) ) ;
#90872=CARTESIAN_POINT ( 'NONE',  ( 5.760397938718036848, 1.910310778393434106, 0.08934430699411573251 ) ) ;
#90881=CARTESIAN_POINT ( 'NONE',  ( 5.378529868213833609, -0.4926607797600784933, -1.955169007017331317 ) ) ;
#90885=CARTESIAN_POINT ( 'NONE',  ( -0.1399997263889611598, 6.947783040739049731, -2.595329734540325006 ) ) ;
#90888=CARTESIAN_POINT ( 'NONE',  ( 2.571101405699018017, 1.757081157110135017, 0.8898057773328130748 ) ) ;
#90889=CARTESIAN_POINT ( 'NONE',  ( 4.728138764314923748, 2.011206665557175199, 0.1455158850461671372 ) ) ;
#90891=CARTESIAN_POINT ( 'NONE',  ( 6.827182134110238110, -0.009824402486291110986, 2.288967694407703313 ) ) ;
#90892=CARTESIAN_POINT ( 'NONE',  ( 4.242245924764226572, 0.5834501570099770440, 2.112278566661344392 ) ) ;
#90893=CARTESIAN_POINT ( 'NONE',  ( 2.819263867200746176, -0.1907306445340165024, 1.916936124417574661 ) ) ;
#90902=CARTESIAN_POINT ( 'NONE',  ( 5.794452930745782382, 1.501506822132542718, -1.065412412061928160 ) ) ;
#90903=CARTESIAN_POINT ( 'NONE',  ( 3.369792252087350892, 0.4868432662692974144, -1.953231169037449533 ) ) ;
#90904=CARTESIAN_POINT ( 'NONE',  ( 5.747524558462486333, -2.240600987983232262, -0.5116226552598357458 ) ) ;
#90906=CARTESIAN_POINT ( 'NONE',  ( 2.799463494909336880, -1.375353214051901807, -1.253764128285854706 ) ) ;
#90911=CARTESIAN_POINT ( 'NONE',  ( 6.515180868147061766, -2.027822497041928518, 0.5085933055150316795 ) ) ;
#90918=CARTESIAN_POINT ( 'NONE',  ( 6.393153111415212031, 1.496800677787715639, -0.8570667202875602575 ) ) ;
#90920=CARTESIAN_POINT ( 'NONE',  ( 1.441630353877725979, -1.487241779905050576, -0.8915045353455192112 ) ) ;
#90924=CARTESIAN_POINT ( 'NONE',  ( 6.403213944470495633, -1.838587781526521248, 1.154350301468348272 ) ) ;
#90925=CARTESIAN_POINT ( 'NONE',  ( 4.617693566336190436, -1.789886777702164089, 0.3589094947460610974 ) ) ;
#90926=CARTESIAN_POINT ( 'NONE',  ( 2.518345088137901477, 0.8342845254802437882, 1.775630740545742992 ) ) ;
#90930=CARTESIAN_POINT ( 'NONE',  ( 3.229257539231108698, 1.917844101178723504, 0.9048822562475050679 ) ) ;
#90934=CARTESIAN_POINT ( 'NONE',  ( 1.481394567461959522, -0.05474761849930119550, 2.069712792878583230 ) ) ;
#90937=CARTESIAN_POINT ( 'NONE',  ( 3.651236063859903069, 0.3270389233705518484, 2.196992388787385231 ) ) ;
#90939=CARTESIAN_POINT ( 'NONE',  ( 1.741309990946012132, 2.292119649597070374, -0.1747640694012199680 ) ) ;
#90941=CARTESIAN_POINT ( 'NONE',  ( 6.315292642669888323, -1.766025379077978741, -1.065358839237473099 ) ) ;
#90948=CARTESIAN_POINT ( 'NONE',  ( -0.1104750535120268828, 2.006893987364383403, -2.517811492722863864 ) ) ;
#90949=CARTESIAN_POINT ( 'NONE',  ( 3.328823242065849008, 0.04121275867331047893, 1.724443917160731976 ) ) ;
#90950=CARTESIAN_POINT ( 'NONE',  ( 2.659388954101277847, 1.913261587491304150, -0.6371546050257800298 ) ) ;
#90951=CARTESIAN_POINT ( 'NONE',  ( 3.323114718373169740, 1.032193166631629078, -2.053959190227053533 ) ) ;
#90952=( BOUNDED_SURFACE ( )  B_SPLINE_SURFACE ( 3, 3, ( 
 ( #106772, #69916, #8143, #72055, #119833, #185812, #37444, #169580, #104597, #21163, #54766, #38519, #207410, #79551, #11335, #61169, #193299, #44944, #59029, #174944, #161888, #26526, #25458, #145669, #125187, #127330, #92634, #176004, #208463, #211666, #78481, #112129, #143531, #10272, #12400, #129462, #28675, #158675, #94762, #91565, #191148, #42817, #29747, #76348, #142455, #95831, #126256, #210613, #9215, #160809, #144598, #46008, #63302, #47075, #62240, #108922, #157618, #60098, #192215, #13475, #209527, #111052, #177058, #128399, #75286, #194366, #178132, #27596, #113193, #141401, #195446, #43878, #109992, #93695, #159737, #77416, #387, #2527, #166127, #99008, #101114, #181307, #67527, #167201, #197552, #82742, #182360, #15591, #146718, #18790, #165064, #66459, #132600, #198606, #212734, #114261, #84873, #180258, #179198, #150962, #64371, #50252, #31882, #115317, #147764, #68602, #17713, #51317, #148815, #164017, #83801, #134725, #33989, #97959, #100064, #30822, #130517, #196506, #183439, #81677, #213780, #35043, #65403, #149894, #162951, #1462, #133670, #199674, #200731, #52382, #117444, #48148, #96900, #131550, #49196, #14529, #116372, #80626, #32934, #16656, #184494, #203932, #23050, #120658, #206083, #36113, #6801, #69668, #185562, #119578, #205006, #85948, #136841, #104340, #38263, #202866, #155220, #56653, #103267, #55580, #4656, #121735, #135775, #118510, #186637, #54514, #37191, #70728, #24127, #169329, #20913, #201798, #187701, #156294, #72877, #89168, #153079, #170384, #21972, #7878, #53440, #88082, #122816, #19863, #87008, #152023, #154155, #5722, #138985, #71801, #188774, #40413, #102196, #106516, #140061, #168262, #90229, #3591, #172542, #73966, #137912, #39329, #105425, #171462, #91307, #158421, #61991, #175749, #143279, #77157, #209270, #123876, #60915, #176801, #59845, #145417, #189841, #160549, #8958, #124934, #58780, #144350, #25202, #76096, #43623, #191956, #142199, #94511, #210352, #42561, #127074, #10020, #193036, #75033, #57717, #125997, #208214, #190897, #109738, #177879, #108663, #174694, #141147, #44690, #95584, #12157, #28418, #92385, #27340, #93442, #161633, #207157, #159481, #128147, #173631, #26268, #157364, #11081, #110798, #78228, #194107, #45756, #111875, #41488, #29492, #79301, #107600, #13227, #178952, #141, #97706, #115064, #65157, #81434, #99816, #32678, #34795, #198357, #131313, #133416, #213534, #165881, #199422, #15342, #181060, #66207, #47902, #30566, #51066, #197305, #98757, #164813, #16405, #96646, #146463, #117189, #212480, #211417, #183189, #162700, #82485, #64123, #147513, #180007, #100869, #49997, #83551, #148572, #196255, #116120, #166956, #132354, #130266, #182108, #63049, #14272, #80367, #1214, #114012, #31629, #67277, #163764, #33737, #195190, #17467, #149633, #48944, #18546, #84622, #129214, #46826, #112939, #24678, #39888, #90784, #170935, #150714, #7353, #23610, #154700, #105998, #59327, #6283, #204478, #22534, #156847, #191446, #108152, #124422, #188247, #205560, #73432, #43111, #88643, #172019, #91862, #55064, #72356, #187183, #57200, #138459, #174178, #189325, #157917, #25749, #68350, #190380, #175236, #2274, #125484, #121214, #8431, #89719, #123360, #139535, #155769, #42040, #40966, #109226, #140622, #107074, #75584, #173097, #9512, #141694, #74519, #206634 ),
 ( #56131, #134483, #26820, #38810, #58265, #122290, #207707, #203411, #104896, #145947, #179491, #210897, #77708, #79839, #196792, #96121, #93992, #162176, #92924, #44164, #192512, #97187, #143828, #11635, #163240, #193591, #63596, #76639, #13762, #211958, #113484, #64657, #114549, #129751, #110284, #158970, #126551, #45235, #14822, #62524, #178426, #112414, #30035, #10564, #195736, #47371, #95052, #180540, #142753, #31113, #176293, #160033, #209825, #80914, #60387, #111350, #177355, #128686, #147004, #61461, #27897, #213022, #78767, #194655, #46299, #130798, #127627, #28969, #48433, #161103, #208762, #12691, #144890, #67814, #181591, #182659, #681, #86236, #85167, #118796, #150188, #16946, #19087, #136066, #35339, #33220, #101419, #32163, #197844, #131837, #36409, #83025, #165352, #102488, #132889, #2820, #15884, #167491, #151251, #52667, #3884, #53739, #68891, #49477, #98240, #65689, #198892, #168552, #1757, #117740, #51617, #183733, #164295, #135010, #201024, #34279, #119871, #81968, #184783, #115597, #99304, #149102, #20151, #214061, #50538, #18012, #166420, #116661, #152307, #69954, #66748, #202079, #100352, #148055, #84101, #133961, #199969, #55869, #186926, #138204, #91602, #38558, #22268, #203162, #56939, #9251, #140356, #156585, #6024, #23346, #105721, #75322, #54807, #72094, #124165, #87304, #120955, #4944, #89457, #170681, #206374, #7091, #190127, #58001, #103559, #8179, #207445, #37482, #157653, #153373, #189069, #204216, #155509, #39617, #122025, #74263, #73164, #141439, #172837, #171750, #107895, #187992, #41781, #173922, #25495, #71020, #139270, #205300, #123111, #40704, #59064, #185850, #88377, #106808, #24408, #90523, #104634, #169618, #21202, #137133, #154444, #77448, #30857, #192248, #176038, #142490, #210646, #162984, #79584, #95865, #159770, #177093, #44978, #14565, #208496, #11369, #63338, #26559, #60131, #158710, #28708, #110024, #145702, #160842, #129497, #211702, #42850, #161921, #146752, #191182, #96934, #92666, #128433, #143566, #94794, #193332, #209559, #13512, #12434, #80661, #112163, #111086, #47111, #127362, #195478, #113227, #61204, #78514, #194400, #27630, #10307, #179231, #144631, #62272, #46042, #178166, #76381, #126289, #212770, #43910, #125224, #108957, #93730, #29781, #174977, #424, #32971, #118547, #117483, #150999, #182399, #49234, #51359, #168302, #67564, #65437, #133707, #64406, #15632, #164053, #68638, #115353, #197590, #134762, #165102, #35081, #48184, #199713, #183474, #84911, #36151, #85982, #101153, #81719, #130550, #97995, #16693, #200770, #34028, #149929, #83839, #1498, #196541, #167238, #18827, #66497, #152058, #114296, #2567, #147801, #131588, #181344, #213819, #99047, #52421, #180294, #82779, #148851, #116409, #132636, #184529, #100102, #102231, #19898, #31917, #198642, #50290, #166162, #17749, #119615, #187739, #54550, #5759, #170424, #38299, #6839, #71838, #24161, #171498, #22011, #122856, #104377, #155257, #188817, #186672, #137947, #39367, #70765, #185600, #40451, #88121, #203969, #55615, #121770, #37231, #20949, #106553, #87046, #3628, #172580, #103302, #105464, #153119, #154191, #120697, #90264, #23089, #56689, #89204, #136879, #72917, #156332, #139022, #4690, #205046, #69706, #202905, #169364, #7917, #135810, #201833, #53478, #22328, #104692, #6082, #11164, #192044 ),
 ( #170743, #43707, #94592, #76179, #77241, #158506, #121017, #185904, #186983, #88442, #72153, #28501, #109825, #204275, #21259, #142286, #208296, #143358, #39679, #93525, #23405, #209354, #175836, #59928, #105788, #12235, #37540, #138262, #171814, #136124, #202138, #126083, #55931, #122086, #27427, #71078, #53797, #188048, #89518, #119929, #193128, #5005, #159567, #10106, #61001, #103619, #154504, #127157, #160634, #44777, #110883, #176889, #38615, #169672, #87365, #153434, #137196, #203219, #54864, #146552, #177963, #81518, #147596, #82572, #196340, #32768, #180090, #148659, #115150, #213615, #47984, #165966, #194196, #80454, #114099, #78309, #144433, #65241, #212570, #64209, #15429, #13311, #210435, #130350, #31715, #62076, #132446, #49031, #113026, #164898, #128233, #98847, #226, #96737, #161719, #162785, #97789, #50090, #131392, #163850, #46909, #197389, #45841, #181146, #66298, #33827, #16491, #198445, #116213, #182200, #99906, #111961, #29577, #79384, #95667, #145503, #211501, #63137, #129300, #195275, #179033, #30651, #14363, #170227, #21811, #4494, #67361, #87916, #19704, #120499, #134571, #100952, #53282, #200572, #85783, #185402, #202707, #133506, #169162, #70563, #201634, #52218, #18634, #118347, #117277, #105254, #121569, #167041, #51155, #54358, #136681, #184333, #17551, #149724, #37020, #103104, #153989, #151863, #35958, #102035, #168105, #104178, #186470, #137752, #1302, #187540, #3439, #5558, #203771, #183275, #71639, #69506, #38106, #55415, #39170, #83637, #199510, #152916, #20757, #34879, #84714, #150801, #2365, #68442, #135614, #119414, #86851, #175579, #74870, #42392, #190729, #108501, #22886, #174525, #75931, #173457, #44517, #89002, #59675, #122647, #23965, #172376, #43453, #138815, #189673, #157194, #91137, #41323, #208048, #109575, #156130, #26102, #57554, #92215, #188609, #171294, #25037, #107433, #90067, #123711, #76983, #7712, #73795, #40242, #158266, #209101, #125834, #142033, #205920, #8790, #140976, #60738, #106353, #206985, #27169, #72721, #139890, #204836, #58614, #124770, #191793, #9855, #93274, #159310, #155055, #10907, #192859, #6642, #143109, #56488, #126901, #211243, #14099, #178779, #195011, #213367, #146294, #148404, #97533, #30391, #32506, #112766, #64988, #98581, #129035, #80189, #113839, #161463, #78058, #164642, #96479, #212306, #63941, #130095, #144184, #45583, #16226, #111700, #110633, #82309, #210175, #196090, #177707, #46644, #79122, #214403, #163590, #197132, #47722, #95411, #15173, #66033, #179835, #29317, #31456, #176635, #61815, #13043, #132181, #145238, #28247, #198187, #127983, #81260, #62868, #162526, #147338, #94340, #131143, #48770, #114885, #180884, #160382, #11982, #193936, #50890, #53014, #49822, #1039, #149456, #54091, #84449, #152651, #102841, #5294, #20500, #33567, #185130, #119148, #70305, #21545, #71372, #168897, #67102, #115947, #83372, #150537, #120229, #167836, #135356, #69239, #201373, #181936, #36755, #86585, #51964, #137488, #99638, #4235, #133238, #117013, #183012, #136421, #17295, #68175, #35692, #184073, #134305, #202437, #186202, #34629, #37837, #2100, #103913, #199243, #165706, #118087, #200313, #100699, #101768, #169958, #166776, #18372, #19434, #87656, #153725, #85514, #151600, #3168, #41055, #123451, #26901, #6378, #23704, #141776, #104988, #72449 ),
 ( #125567, #159050, #156934, #207783, #91942, #93005, #108237, #158003, #171029, #204572, #174261, #175314, #59410, #25833, #22625, #189413, #191528, #56221, #73526, #43192, #109305, #190465, #38904, #10642, #205651, #9592, #106088, #75668, #42124, #89814, #203503, #121302, #8523, #74604, #76718, #57288, #155859, #172111, #139628, #55155, #187276, #88735, #154791, #138549, #7446, #122384, #188341, #39980, #107164, #173189, #24769, #90872, #140708, #206723, #58350, #124506, #80991, #162251, #127707, #192591, #193668, #29051, #78844, #32242, #47448, #210970, #27979, #146022, #212033, #147079, #46372, #97261, #30111, #213101, #179567, #63675, #112491, #15962, #44246, #144964, #178502, #142835, #208841, #129829, #62598, #128760, #79914, #77789, #60471, #194734, #96202, #126628, #196869, #113564, #177434, #14897, #110367, #163315, #64731, #161184, #11715, #12769, #13838, #114627, #195812, #31188, #111429, #130876, #176373, #48507, #180617, #98313, #164377, #94072, #160113, #143910, #209903, #61541, #45311, #95134, #52753, #53834, #20240, #118888, #197923, #67903, #3976, #149189, #166509, #86325, #152397, #68980, #131914, #70044, #84187, #184873, #198976, #165435, #117828, #50621, #150274, #35430, #36499, #49551, #19176, #135099, #51706, #116746, #83109, #182746, #181671, #169706, #185940, #17031, #115677, #201113, #200057, #168637, #33298, #34364, #102577, #37575, #85251, #136159, #101507, #66831, #99382, #132974, #100438, #18099, #103655, #202177, #1844, #764, #151338, #2908, #119965, #183819, #82045, #167577, #148139, #214141, #65767, #134047, #109051, #137232, #23442, #57035, #21296, #87401, #24511, #89553, #155603, #172934, #170776, #153467, #7188, #123202, #5040, #75419, #206470, #55967, #107987, #71116, #190217, #157749, #39714, #104728, #105822, #73260, #207539, #90621, #189163, #204310, #139365, #203253, #40801, #9347, #191275, #106909, #174014, #124258, #59159, #140458, #41876, #54897, #22365, #58097, #125317, #25585, #91696, #121050, #205396, #141531, #88477, #171848, #42942, #187017, #8271, #38650, #154537, #156678, #6117, #138294, #72186, #74354, #122119, #188084, #128525, #145792, #76473, #112253, #13604, #144727, #77542, #176132, #143664, #60224, #48273, #64498, #44001, #208591, #211797, #79678, #61299, #175069, #92758, #194494, #46137, #179331, #177188, #127460, #209658, #45075, #47210, #63433, #80754, #158803, #130640, #193432, #163081, #146843, #110120, #111185, #129585, #195572, #196632, #113324, #10400, #95961, #178266, #30952, #212862, #26656, #97026, #126383, #142584, #192343, #28803, #14662, #78606, #29877, #162015, #27731, #93826, #159867, #11470, #94888, #160940, #12533, #210739, #62362, #181432, #115441, #200852, #81810, #132725, #100188, #34117, #198730, #151089, #52501, #99140, #199803, #515, #51448, #131678, #114386, #182488, #50376, #33062, #66583, #19984, #165189, #16783, #197680, #117568, #152145, #68727, #84998, #148943, #166253, #17843, #3712, #49325, #116499, #118634, #15724, #82867, #147893, #83928, #150017, #134848, #1587, #184619, #36236, #32005, #2653, #135897, #180381, #86069, #213909, #183563, #67648, #133794, #35169, #101246, #102314, #167328, #69789, #18914, #168388, #201915, #98086, #164140, #65532, #71925, #171581, #56774, #104466, #21035, #107727, #39451, #89290, #6923, #73000, #87134 ),
 ( #106641, #140187, #23176, #38384, #40538, #157493, #122939, #54634, #188896, #53568, #4775, #153205, #57836, #172669, #120782, #24246, #119702, #70853, #136967, #123998, #88208, #156417, #90347, #9087, #8004, #37314, #74095, #206208, #189966, #25331, #75161, #41615, #202995, #185685, #186760, #154279, #173754, #155341, #139103, #205130, #91431, #103389, #141271, #169450, #55698, #170513, #22095, #5853, #138035, #204048, #121854, #187825, #105546, #11207, #193169, #127202, #77289, #29620, #79425, #192084, #78350, #93565, #144473, #10144, #207281, #61041, #143400, #208340, #159610, #113066, #59970, #43750, #76219, #210478, #30693, #161759, #178004, #27467, #44818, #110924, #96775, #142328, #209396, #145543, #108794, #126124, #26396, #176928, #109863, #13350, #28546, #211540, #63175, #125063, #95705, #14402, #58909, #179072, #174820, #62116, #94635, #160679, #12274, #128276, #129340, #194237, #162826, #45882, #112003, #195318, #46949, #80494, #191020, #42687, #92509, #158546, #175877, #114139, #203535, #135385, #185164, #102872, #168931, #180131, #81554, #71406, #147637, #146591, #55188, #31758, #36788, #213655, #82612, #115191, #121335, #202471, #21576, #53045, #131428, #136453, #38938, #212609, #3202, #16530, #65281, #98885, #187311, #197430, #49071, #163894, #20534, #105021, #103948, #120260, #181184, #201406, #69271, #171060, #15470, #32810, #87682, #48023, #164937, #97829, #119178, #148697, #169990, #86616, #153755, #5326, #64249, #186236, #22656, #130391, #196382, #152684, #4266, #70336, #54124, #37870, #137518, #191561, #124541, #126663, #75699, #8557, #10679, #90903, #43225, #76750, #107197, #206754, #91977, #139662, #56256, #142871, #74636, #190498, #42156, #108271, #122413, #23736, #208873, #89842, #88767, #60503, #188372, #174292, #155891, #24801, #57319, #192628, #141813, #175352, #58385, #73561, #207816, #44280, #158035, #7479, #9622, #154824, #40010, #106121, #93040, #123484, #109342, #59444, #110401, #125601, #72481, #26932, #159082, #176405, #6409, #138582, #204605, #172144, #205683, #189447, #41089, #173222, #25867, #156966, #140743, #113597, #94109, #179600, #147112, #30146, #115712, #160150, #130910, #193702, #95169, #29085, #114660, #209939, #46407, #13873, #162285, #112523, #64768, #180654, #12805, #31221, #128789, #97295, #45346, #196902, #143943, #161218, #213138, #214174, #32279, #48541, #61577, #79951, #164410, #78878, #178536, #98345, #146054, #28011, #63706, #195846, #47487, #127745, #177471, #15994, #145001, #11747, #148172, #111465, #129863, #211006, #96235, #62629, #82079, #81024, #65801, #212068, #194770, #14929, #131948, #163354, #197959, #49588, #77822, #133009, #66864, #185974, #1873, #70078, #20274, #137263, #152429, #165468, #102615, #184904, #202210, #153501, #203283, #86358, #199009, #33332, #796, #67933, #37607, #85286, #52785, #201147, #118924, #99414, #36528, #4008, #183850, #54930, #17064, #136192, #50654, #34395, #182777, #53864, #149221, #200086, #167609, #101540, #51735, #119997, #103688, #166542, #168670, #134078, #169737, #116780, #181702, #35462, #117858, #100467, #19207, #87433, #18130, #84219, #150307, #21326, #5071, #71146, #83143, #151372, #2941, #69013, #135130, #138324, #155633, #59190, #22400, #204340, #154571, #172964, #105853, #75448, #156712, #125345, #207569, #38681, #157779 ),
 ( #123230, #9377, #23477, #55998, #8303, #89584, #189195, #74387, #91728, #88509, #58130, #174043, #90651, #7218, #122149, #73292, #6147, #208623, #10432, #188117, #72217, #141561, #25616, #139395, #121082, #104760, #140488, #206499, #191308, #40832, #205428, #57066, #106941, #42976, #109086, #26688, #170809, #76504, #24543, #175101, #92790, #39748, #158835, #124289, #142615, #171880, #190248, #187049, #41906, #108017, #212896, #79707, #45108, #110150, #111218, #160971, #210771, #164168, #179360, #128556, #159897, #63464, #129618, #64528, #178299, #14691, #162044, #130673, #97057, #195605, #29906, #147922, #176163, #62391, #95991, #60257, #126414, #47240, #194521, #46169, #211827, #209690, #192377, #112283, #13634, #44032, #114413, #30982, #94922, #146875, #27763, #80786, #196661, #78635, #143698, #144760, #145822, #32031, #113355, #163110, #28834, #48302, #93859, #180413, #98117, #15754, #81838, #11504, #77575, #61334, #127493, #193464, #177221, #12561, #184648, #185712, #152174, #36268, #115471, #199836, #135926, #66609, #83958, #2685, #119734, #116527, #182517, #53599, #52531, #86102, #117601, #198759, #200885, #103420, #68757, #544, #134878, #213938, #165220, #99167, #3743, #34147, #102346, #118665, #169481, #168417, #197710, #20014, #69818, #201944, #37346, #21065, #87163, #16812, #65559, #33093, #100217, #131706, #183593, #85031, #18946, #151119, #49352, #181463, #82897, #1619, #148970, #132756, #50408, #166285, #17874, #150048, #67679, #133823, #51478, #35200, #101275, #167359, #189997, #25363, #138065, #24277, #39482, #90383, #170542, #153233, #6953, #23207, #154309, #105580, #58939, #5881, #204078, #22126, #156452, #191054, #107761, #124031, #187855, #205160, #73034, #42719, #88239, #171614, #91463, #54665, #71955, #186790, #56802, #55731, #173787, #188931, #157524, #9119, #70885, #41647, #174853, #4804, #125096, #120813, #8036, #89321, #122972, #139132, #155368, #75194, #40570, #108827, #140222, #106676, #141306, #172699, #207317, #26431, #74127, #206243, #57868, #136996, #203023, #38417, #104498, #121885, #45917, #112036, #126158, #27502, #14435, #93602, #92541, #212639, #192121, #128309, #159647, #28582, #78387, #12306, #176965, #129370, #179103, #77322, #178038, #193205, #29654, #109899, #158581, #160712, #94670, #11244, #44852, #64281, #143435, #209432, #175911, #95740, #130427, #46981, #63206, #127236, #144507, #210515, #196412, #61076, #110958, #30725, #208373, #62150, #43787, #194272, #161791, #113097, #13382, #96808, #162857, #10181, #195349, #114170, #76255, #48057, #60005, #79458, #145574, #211572, #80525, #146622, #180164, #142364, #69575, #18702, #166041, #168175, #33897, #134638, #19774, #50161, #149800, #34953, #52292, #15500, #83710, #31790, #67435, #199584, #51227, #65311, #181215, #85856, #32841, #97864, #151930, #131460, #133580, #98918, #182273, #298, #3505, #84785, #118421, #1374, #16563, #150873, #135686, #101024, #164971, #167115, #163925, #197461, #49104, #36026, #66369, #200643, #2437, #201711, #68511, #81587, #184407, #102104, #53353, #119487, #147672, #213689, #115225, #82646, #148730, #132517, #198515, #117351, #183349, #116282, #99976, #17625, #56566, #90141, #187612, #58691, #37098, #73878, #136752, #38178, #186549, #57629, #152992, #203845, #54430, #6716, #154066, #39240, #138894 ),
 ( #188687, #104250, #40323, #185474, #202779, #70641, #189746, #5631, #139971, #24038, #141054, #156209, #169238, #106428, #172451, #205993, #157275, #207061, #7785, #120572, #103177, #4568, #71712, #41398, #89077, #122725, #204913, #123788, #20826, #107508, #173537, #105332, #86924, #170296, #25111, #21884, #87993, #137825, #91214, #55491, #121645, #171369, #22962, #155134, #8864, #74943, #72794, #210254, #10985, #61892, #142110, #124839, #192940, #209180, #125912, #77059, #30466, #191871, #175656, #208123, #128054, #162599, #79203, #95491, #159387, #176707, #44592, #14174, #59752, #143189, #62945, #26179, #43531, #158338, #28320, #109654, #145319, #160455, #129114, #211321, #42465, #161537, #146366, #190805, #96552, #92294, #194009, #60820, #94416, #110707, #126981, #13124, #12063, #80267, #111776, #78131, #46727, #144261, #195090, #112839, #45658, #177782, #29398, #178855, #108575, #212380, #174603, #9932, #76007, #27244, #93350, #213439, #101844, #18448, #34701, #98659, #116024, #198259, #167914, #81335, #164714, #2175, #179910, #147414, #97608, #182009, #48846, #84525, #99714, #68251, #150614, #196160, #100770, #85588, #130168, #184146, #31533, #67182, #16303, #33640, #132252, #148478, #166852, #165786, #19511, #50967, #49902, #200387, #66110, #134384, #52035, #82388, #17369, #133318, #118161, #47801, #83453, #64022, #149533, #1119, #199320, #163665, #65062, #35770, #131218, #113914, #151676, #15248, #117089, #197206, #46, #32582, #114960, #183089, #180961, #5372, #4306, #171106, #89886, #38983, #86658, #105068, #3246, #168973, #102913, #188419, #120303, #138626, #88811, #73606, #6452, #201446, #22699, #154869, #204650, #155937, #69314, #72529, #20574, #135424, #152725, #103989, #172191, #55233, #56299, #122461, #40055, #53089, #106164, #23780, #71451, #119222, #36830, #7523, #70378, #186278, #54165, #185206, #37915, #136494, #202516, #170033, #21619, #87727, #153799, #137564, #203581, #121380, #187353, #214110, #196840, #50587, #66797, #197893, #149152, #102540, #49522, #33267, #65737, #67866, #83074, #100404, #116710, #132937, #85217, #18064, #20205, #183785, #182711, #118852, #198943, #151303, #184835, #731, #166472, #200020, #2873, #180588, #34329, #48480, #84152, #150239, #1808, #15933, #131885, #36465, #115644, #114597, #168603, #82016, #134013, #181639, #51672, #165402, #86292, #35393, #68943, #117793, #99351, #101470, #152363, #167541, #16998, #19140, #32211, #148107, #135065, #201078, #52719, #3940, #70008, #98285, #164344, #150040, #166275, #185706, #88232, #17866, #138059, #134872, #170535, #154301, #51469, #87156, #86092, #54659, #83949, #2678, #153227, #204072, #119727, #120807, #201937, #167351, #1611, #18938, #68750, #118657, #71949, #4797, #36261, #67670, #37340, #103414, #186784, #152168, #136990, #69812, #38410, #70877, #169474, #3737, #55724, #133814, #184642, #135918, #182509, #34139, #21059, #102339, #168411, #203017, #117593, #100208, #20008, #53593, #199828, #22120, #104492, #200879, #5875, #183584, #35192, #101267, #52524, #85023, #151112, #189990, #93595, #58932, #157517, #90377, #124024, #39475, #141300, #43778, #77315, #206235, #122965, #74120, #27495, #188924, #172693, #139126, #207309, #159639, #76248, #92535, #156446, #173781, #41641, #11236, #205153, #8030, #59998, #23200, #56796 ) ),
 .UNSPECIFIED., .T., .F., .F. ) 
 B_SPLINE_SURFACE_WITH_KNOTS ( ( 4, 3, 4 ),
 ( 4, 1, 1, 1, 1, 1, 1, 1, 1, 1, 1, 1, 1, 1, 1, 1, 1, 1, 1, 1, 1, 1, 1, 1, 1, 1, 1, 1, 1, 1, 1, 1, 1, 1, 1, 1, 1, 1, 1, 1, 1, 1, 1, 1, 1, 1, 1, 1, 1, 1, 1, 1, 1, 1, 1, 1, 1, 1, 1, 1, 1, 1, 1, 1, 1, 1, 1, 1, 1, 1, 1, 1, 1, 1, 1, 1, 1, 1, 1, 1, 1, 1, 1, 1, 1, 1, 1, 1, 1, 1, 1, 1, 1, 1, 1, 1, 1, 1, 1, 1, 1, 1, 1, 1, 1, 1, 1, 1, 1, 1, 1, 1, 1, 1, 1, 1, 1, 1, 1, 1, 1, 1, 1, 1, 1, 1, 1, 1, 1, 1, 1, 1, 1, 1, 1, 1, 1, 1, 1, 1, 1, 1, 1, 1, 1, 1, 1, 1, 1, 1, 1, 1, 1, 1, 1, 1, 1, 1, 1, 1, 1, 1, 1, 1, 1, 1, 1, 1, 1, 1, 1, 1, 1, 1, 1, 1, 1, 1, 1, 1, 1, 1, 1, 1, 1, 1, 1, 1, 1, 1, 1, 1, 1, 1, 1, 1, 1, 1, 1, 1, 1, 1, 1, 1, 1, 1, 1, 1, 1, 1, 1, 1, 1, 1, 1, 1, 1, 1, 1, 1, 1, 1, 1, 1, 1, 1, 1, 1, 1, 1, 1, 1, 1, 1, 1, 1, 1, 1, 1, 1, 1, 1, 1, 1, 1, 1, 1, 1, 1, 1, 1, 1, 1, 1, 1, 1, 1, 1, 1, 1, 1, 1, 1, 1, 1, 1, 1, 1, 1, 1, 1, 1, 1, 1, 1, 1, 1, 1, 1, 1, 1, 1, 1, 1, 1, 1, 1, 1, 1, 1, 1, 1, 1, 1, 1, 1, 1, 1, 1, 1, 1, 1, 1, 1, 1, 1, 1, 1, 1, 1, 1, 1, 1, 1, 1, 1, 1, 1, 1, 1, 1, 1, 1, 1, 1, 1, 1, 1, 1, 1, 1, 1, 1, 1, 1, 1, 1, 1, 1, 1, 1, 1, 1, 1, 1, 1, 1, 1, 1, 1, 1, 1, 1, 1, 1, 1, 1, 1, 1, 1, 1, 1, 1, 1, 1, 1, 1, 1, 1, 1, 1, 1, 1, 1, 1, 1, 1, 1, 1, 1, 1, 1, 1, 1, 4 ),
 ( 0.000000000000000000, 0.5000000000000000000, 1.000000000000000000 ),
 ( 0.000000000000000000, 0.002600137934918278840, 0.005208846947063642402, 0.007813284371963545236, 0.01041597565644012714, 0.01302123463190214131, 0.01562472912267370319, 0.01822934229245065652, 0.02083335053635077330, 0.02343730581734793095, 0.02604195799539401474, 0.02864545692284610826, 0.03125045498156164142, 0.03385385361191795006, 0.03645873261014952182, 0.03906243010681619693, 0.04166674480109257978, 0.04427107247243720900, 0.04687475664952634596, 0.04947964045798968619, 0.05208303702386667122, 0.05468803228817373241, 0.05729153353077973132, 0.05989618223844375006, 0.06250015876865079589, 0.06510412050499821135, 0.06770877833268285073, 0.07031227041168378045, 0.07291726700687002627, 0.07552066596874357218, 0.07812554330212571896, 0.08072923942118487295, 0.08333355289058355653, 0.08593787945419822938, 0.08854156225015286097, 0.09114644488045960113, 0.09374984019314609729, 0.09635483420994474246, 0.09895833431534489799, 0.1015629817166532611, 0.1041669571688737805, 0.1067709175595765864, 0.1093755742645453749, 0.1119790650618166516, 0.1145840604711090005, 0.1171874582687142119, 0.1197923343547293018, 0.1223960294069747767, 0.1250003415701952669, 0.1276046670722256471, 0.1302083485727723866, 0.1328132300777099817, 0.1354166241949035232, 0.1380216170238739992, 0.1406251160503516617, 0.1432297622036773077, 0.1458337366370238142, 0.1484376957407889386, 0.1510423513813509144, 0.1536458409560605698, 0.1562508352375901466, 0.1588542319300798034, 0.1614591068269417562, 0.1640628008713490293, 0.1666671117869774343, 0.1692714362859856492, 0.1718751165501164191, 0.1744799969878772505, 0.1770833899687347668, 0.1796883816679979429, 0.1822918796746371972, 0.1848965246383280081, 0.1875004981115827030, 0.1901044559872153150, 0.1927091106216977379, 0.1953125990329364348, 0.1979175922448092595, 0.2005209878913200294, 0.2031258616572126918, 0.2057295547527302204, 0.2083338644793258920, 0.2109381880338489224, 0.2135418671205281671, 0.2161467465492790951, 0.2187501384529311477, 0.2213551290805818306, 0.2239586261264417955, 0.2265632699588193688, 0.2291672425307399730, 0.2317711992370185270, 0.2343758529237242316, 0.2369793402305566954, 0.2395843324308542799, 0.2421877270904984059, 0.2447925997835804779, 0.2473962919891333490, 0.2500006005852301039, 0.2526049232537817546, 0.2552086012219486610, 0.2578134796998332035, 0.2604168705853860954, 0.2630218601994954719, 0.2656253563436123954, 0.2682299991029740149, 0.2708339708322964334, 0.2734379264279751531, 0.2760425792251849364, 0.2786460654866522724, 0.2812510567334335909, 0.2838544504653006673, 0.2864593221437078951, 0.2890630135181997962, 0.2916673210423081364, 0.2942716428833813125, 0.2968753197919519748, 0.2994801973770923054, 0.3020835873036303854, 0.3046885759622478540, 0.3072920712636373342, 0.3098967130082584398, 0.3125006839536987324, 0.3151046384975096371, 0.3177092904634842285, 0.3203127757386058927, 0.3229177660899096303, 0.3255211589530693228, 0.3281260296749167193, 0.3307297202772326306, 0.3333340267878420748, 0.3359383478599109463, 0.3385420237677806976, 0.3411469005182800607, 0.3437502895448679152, 0.3463552773060237788, 0.3489587718236830116, 0.3515634126118191150, 0.3541673828320756612, 0.3567713363827305639, 0.3593759875757128741, 0.3619794719234893932, 0.3645844614373360826, 0.3671878534908398217, 0.3697927233142242476, 0.3723964132032320795, 0.3750007187588132451, 0.3776050391203355505, 0.3802087140863810166, 0.3828135900603256703, 0.3854169782460106219, 0.3880219651677176973, 0.3906254589606275029, 0.3932300988505167960, 0.3958340684042725433, 0.3984380210204655492, 0.4010426714986830565, 0.4036461549780977487, 0.4062511437124918245, 0.4088545350153757196, 0.4114594039983773821, 0.4140630932329303349, 0.4166673978919369636, 0.4192717176013560643, 0.4218753916844373286, 0.4244802669398990425, 0.4270836543437129262, 0.4296886404839689866, 0.4322921336110964741, 0.4348967726609613837, 0.4375007416068860122, 0.4401046933472957945, 0.4427093431689624881, 0.4453128258389836835, 0.4479178138519160357, 0.4505212044632024293, 0.4531260726638874359, 0.4557297613028266636, 0.4583340651236982866, 0.4609383842394453867, 0.4635420574984087105, 0.4661469320934465421, 0.4687503187744080368, 0.4713553041911981989, 0.4739587967114984313, 0.4765634349795482838, 0.4791674033763006491, 0.4817713542995921694, 0.4843760035229108252, 0.4869794854424946973, 0.4895844727919445583, 0.4921878627706443576, 0.4947927302470669919, 0.4973964183492232127, 0.5000007213903868708, 0.5026050399708832384, 0.5052087124645624483, 0.5078135864572254077, 0.5104169724743423675, 0.5130219572256408123, 0.5156254491980594157, 0.5182300867424926016, 0.5208340546487225664, 0.5234380048135498509, 0.5260426534967141965, 0.5286461347248060383, 0.5312511214687432037, 0.5338545108738584899, 0.5364593776840630435, 0.5390630653082590928, 0.5416673676281316130, 0.5442716857317909662, 0.5468753575190105076, 0.5494802309673390006, 0.5520836163796108975, 0.5546886005233833128, 0.5572920920068584749, 0.5598967288858642810, 0.5625006963602153798, 0.5651046458252231286, 0.5677092940264200083, 0.5703127746219572858, 0.5729177608183441128, 0.5755211497088699169, 0.5781260159108934094, 0.5807297031159460721, 0.5833340047729366207, 0.5859383224581667937, 0.5885419935977430628, 0.5911468665597719996, 0.5937502514261915332, 0.5963552350203973340, 0.5989587260738620245, 0.6015633623456233536, 0.6041673294467342359, 0.6067712782705607655, 0.6093759260479724160, 0.6119794060698863225, 0.6145843917766802278, 0.6171877802116071399, 0.6197926458634805957, 0.6223963327082033814, 0.6250006337607152407, 0.6276049510859208480, 0.6302086216366651339, 0.6328134941704254279, 0.6354168785499811900, 0.6380218616525755726, 0.6406253523349600965, 0.6432299880576550777, 0.6458339548441623945, 0.6484379030854412473, 0.6510425504972472410, 0.6536460300044655281, 0.6562510152796211527, 0.6588544033179367654, 0.6614592684776883225, 0.6640629550208935195, 0.6666672555273263079, 0.6692715725509107427, 0.6718752425716313370, 0.6744801147351520143, 0.6770834986868305982, 0.6796884813557668714, 0.6822919717260003125, 0.6848966069578048543, 0.6875005734883452568, 0.6901045212057073108, 0.6927091683100871089, 0.6953126473615357517, 0.6979176322630067375, 0.7005210199636988655, 0.7031258846893556624, 0.7057295709898557812, 0.7083338710086078960, 0.7109381877889758838, 0.7135418573384794128, 0.7161467291897904985, 0.7187501127725786088, 0.7213550950658099703, 0.7239585851828231888, 0.7265632199819130888, 0.7291671863151253374, 0.7317711335672014705, 0.7343757804223364216, 0.7369792590769420615, 0.7395842436626837157, 0.7421876310847422831, 0.7447924954343322357, 0.7473961815509432283, 0.7500004811404139549, 0.7526047977359727748, 0.7552084668730677519, 0.7578133384702019359, 0.7604167217430886083, 0.7630217037185706985, 0.7656251936412983294, 0.7682298280658512724, 0.7708337942603785686, 0.7734377411058018792, 0.7760423877698768846, 0.7786458660865690495, 0.7812508504145402322, 0.7838542376169586046, 0.7864591016485131814, 0.7890627876400562180, 0.7916670868586475063, 0.7942714033278103214, 0.7968750721113085911, 0.7994799435123028930, 0.8020833265342820484, 0.8046883082499752815, 0.8072917980373575109, 0.8098964321455554005, 0.8125003982600473851, 0.8151043447574546352, 0.8177089912886614798, 0.8203124693263749156, 0.8229174534545398156, 0.8255208404963184643, 0.8281257042678743518, 0.8307293901931780411, 0.8333336890992975032, 0.8359380055004849153, 0.8385416739892034288, 0.8411465452521027508, 0.8437499280821748604, 0.8463549095960458679, 0.8489583993070312085, 0.8515630331570626099, 0.8541669992501779163, 0.8567709454582125295, 0.8593755919147509914, 0.8619790697324273276, 0.8645840537187589048, 0.8671874406589066275, 0.8697923042285079509, 0.8723959901464106714, 0.8750002887984731359, 0.8776046051901155165, 0.8802082734428797739, 0.8828131446257380111, 0.8854165273229123168, 0.8880215086929368340, 0.8906249983864840125, 0.8932296320365455955, 0.8958335981669537373, 0.8984375441442679078, 0.9010421905843485346, 0.9036456682409392815, 0.9062506521434200435, 0.9088540390409564074, 0.9114589024666573946, 0.9140625884360091824, 0.9166668868924389146, 0.9192712033329777377, 0.9218748714086243412, 0.9244797425695093773, 0.9270831251927963423, 0.9296881064769593195, 0.9322915962120889022, 0.9348962297203436966, 0.9375001959466012780, 0.9401041417521586174, 0.9427087882339971747, 0.9453122657876905643, 0.9479172496658602176, 0.9505206365780075606, 0.9531254999124115779, 0.9557291860198475764, 0.9583334843266348990, 0.9609378007344983041, 0.9635414689593263526, 0.9661463405142474148, 0.9687497214891268582, 0.9713547029754164841, 0.9739581985331400293, 0.9765628250748574768, 0.9791667834374845336, 0.9817707607320566021, 0.9843753697534296521, 0.9869788348889786400, 0.9895840831931937975, 0.9921867700316038263, 0.9947911815772807476, 0.9973998924267860611, 1.000000000000000000 ),
 .UNSPECIFIED. ) 
 GEOMETRIC_REPRESENTATION_ITEM ( )  RATIONAL_B_SPLINE_SURFACE ( (
 ( 1.000000000000000000, 1.000000000000000000, 1.000000000000000000, 1.000000000000000222, 0.9999999999999996669, 1.000000000000000222, 0.9999999999999997780, 1.000000000000000000, 0.9999999999999997780, 1.000000000000000444, 1.000000000000000000, 0.9999999999999997780, 1.000000000000000222, 1.000000000000000000, 0.9999999999999997780, 1.000000000000000222, 0.9999999999999996669, 1.000000000000000000, 1.000000000000000222, 1.000000000000000000, 1.000000000000000000, 1.000000000000000444, 0.9999999999999994449, 1.000000000000000444, 0.9999999999999996669, 1.000000000000000222, 1.000000000000000000, 1.000000000000000444, 1.000000000000000000, 0.9999999999999997780, 1.000000000000000000, 1.000000000000000222, 0.9999999999999997780, 0.9999999999999997780, 1.000000000000000444, 0.9999999999999997780, 1.000000000000000444, 1.000000000000000222, 0.9999999999999996669, 1.000000000000000222, 1.000000000000000000, 1.000000000000000444, 0.9999999999999997780, 1.000000000000000222, 1.000000000000000222, 1.000000000000000222, 0.9999999999999997780, 1.000000000000000000, 1.000000000000000000, 1.000000000000000000, 0.9999999999999994449, 1.000000000000000444, 0.9999999999999997780, 1.000000000000000444, 0.9999999999999997780, 1.000000000000000000, 1.000000000000000000, 0.9999999999999997780, 1.000000000000000444, 0.9999999999999996669, 1.000000000000000444, 0.9999999999999996669, 1.000000000000000222, 0.9999999999999994449, 1.000000000000000222, 1.000000000000000000, 1.000000000000000000, 1.000000000000000000, 1.000000000000000000, 1.000000000000000222, 1.000000000000000000, 1.000000000000000222, 0.9999999999999996669, 1.000000000000000222, 1.000000000000000000, 1.000000000000000444, 1.000000000000000000, 1.000000000000000000, 0.9999999999999997780, 1.000000000000000222, 0.9999999999999997780, 0.9999999999999997780, 1.000000000000000444, 1.000000000000000000, 1.000000000000000222, 0.9999999999999996669, 1.000000000000000444, 0.9999999999999997780, 1.000000000000000222, 0.9999999999999997780, 1.000000000000000222, 1.000000000000000000, 1.000000000000000000, 1.000000000000000000, 1.000000000000000000, 1.000000000000000222, 1.000000000000000222, 0.9999999999999997780, 1.000000000000000222, 1.000000000000000000, 1.000000000000000222, 0.9999999999999997780, 1.000000000000000222, 1.000000000000000000, 1.000000000000000000, 0.9999999999999997780, 1.000000000000000000, 1.000000000000000000, 0.9999999999999997780, 1.000000000000000222, 0.9999999999999997780, 1.000000000000000222, 0.9999999999999997780, 1.000000000000000444, 1.000000000000000000, 0.9999999999999996669, 1.000000000000000444, 1.000000000000000000, 0.9999999999999997780, 1.000000000000000000, 0.9999999999999996669, 1.000000000000000000, 1.000000000000000222, 0.9999999999999996669, 1.000000000000000222, 0.9999999999999997780, 1.000000000000000000, 1.000000000000000222, 0.9999999999999997780, 1.000000000000000222, 0.9999999999999997780, 1.000000000000000222, 1.000000000000000000, 1.000000000000000000, 1.000000000000000000, 0.9999999999999997780, 1.000000000000000222, 0.9999999999999997780, 1.000000000000000222, 1.000000000000000000, 1.000000000000000000, 1.000000000000000000, 1.000000000000000000, 1.000000000000000444, 0.9999999999999997780, 1.000000000000000444, 0.9999999999999997780, 1.000000000000000222, 1.000000000000000000, 1.000000000000000000, 1.000000000000000000, 1.000000000000000000, 0.9999999999999997780, 1.000000000000000000, 1.000000000000000222, 0.9999999999999997780, 1.000000000000000222, 1.000000000000000000, 1.000000000000000000, 1.000000000000000222, 0.9999999999999997780, 1.000000000000000222, 0.9999999999999996669, 1.000000000000000444, 0.9999999999999994449, 1.000000000000000444, 0.9999999999999997780, 0.9999999999999997780, 1.000000000000000000, 1.000000000000000000, 1.000000000000000222, 1.000000000000000000, 1.000000000000000000, 1.000000000000000000, 1.000000000000000000, 1.000000000000000222, 1.000000000000000444, 0.9999999999999997780, 1.000000000000000222, 1.000000000000000000, 0.9999999999999996669, 1.000000000000000222, 1.000000000000000222, 1.000000000000000222, 1.000000000000000222, 1.000000000000000000, 1.000000000000000000, 1.000000000000000222, 1.000000000000000000, 1.000000000000000222, 1.000000000000000000, 1.000000000000000000, 1.000000000000000000, 1.000000000000000222, 0.9999999999999997780, 1.000000000000000000, 1.000000000000000222, 1.000000000000000000, 1.000000000000000222, 1.000000000000000000, 0.9999999999999997780, 1.000000000000000444, 1.000000000000000000, 0.9999999999999996669, 1.000000000000000222, 0.9999999999999997780, 1.000000000000000222, 1.000000000000000000, 1.000000000000000000, 1.000000000000000444, 0.9999999999999996669, 1.000000000000000000, 0.9999999999999997780, 1.000000000000000000, 0.9999999999999997780, 0.9999999999999997780, 1.000000000000000000, 1.000000000000000000, 1.000000000000000000, 0.9999999999999997780, 1.000000000000000000, 1.000000000000000222, 1.000000000000000222, 1.000000000000000000, 0.9999999999999997780, 1.000000000000000222, 1.000000000000000000, 1.000000000000000000, 1.000000000000000222, 1.000000000000000222, 1.000000000000000222, 1.000000000000000000, 0.9999999999999997780, 1.000000000000000444, 0.9999999999999997780, 1.000000000000000444, 0.9999999999999997780, 1.000000000000000000, 1.000000000000000222, 0.9999999999999997780, 1.000000000000000222, 0.9999999999999997780, 1.000000000000000222, 0.9999999999999997780, 1.000000000000000222, 0.9999999999999996669, 1.000000000000000222, 0.9999999999999997780, 1.000000000000000444, 1.000000000000000000, 1.000000000000000000, 0.9999999999999997780, 1.000000000000000222, 1.000000000000000000, 0.9999999999999996669, 1.000000000000000222, 0.9999999999999997780, 1.000000000000000000, 1.000000000000000222, 1.000000000000000000, 1.000000000000000222, 0.9999999999999996669, 1.000000000000000444, 0.9999999999999996669, 1.000000000000000000, 1.000000000000000000, 1.000000000000000000, 0.9999999999999997780, 1.000000000000000444, 1.000000000000000000, 1.000000000000000000, 1.000000000000000000, 1.000000000000000000, 0.9999999999999997780, 1.000000000000000222, 1.000000000000000222, 1.000000000000000222, 1.000000000000000000, 1.000000000000000222, 1.000000000000000000, 0.9999999999999997780, 1.000000000000000444, 1.000000000000000000, 0.9999999999999997780, 1.000000000000000222, 0.9999999999999996669, 1.000000000000000222, 1.000000000000000000, 1.000000000000000444, 1.000000000000000222, 0.9999999999999996669, 1.000000000000000222, 0.9999999999999997780, 1.000000000000000222, 1.000000000000000222, 0.9999999999999997780, 1.000000000000000222, 1.000000000000000000, 1.000000000000000222, 1.000000000000000222, 0.9999999999999997780, 1.000000000000000444, 0.9999999999999996669, 1.000000000000000222, 1.000000000000000222, 1.000000000000000000, 1.000000000000000000, 1.000000000000000000, 1.000000000000000222, 1.000000000000000000, 1.000000000000000000, 1.000000000000000222, 0.9999999999999996669, 1.000000000000000444, 1.000000000000000222, 0.9999999999999997780, 1.000000000000000222, 0.9999999999999997780, 1.000000000000000444, 0.9999999999999996669, 1.000000000000000666, 0.9999999999999994449, 1.000000000000000222, 0.9999999999999997780, 1.000000000000000444, 1.000000000000000000, 1.000000000000000222, 1.000000000000000222, 1.000000000000000000, 0.9999999999999997780, 0.9999999999999997780, 1.000000000000000444, 1.000000000000000000, 1.000000000000000000, 1.000000000000000000, 0.9999999999999997780, 1.000000000000000222, 1.000000000000000222, 0.9999999999999997780, 1.000000000000000222, 1.000000000000000000, 1.000000000000000444, 0.9999999999999996669, 1.000000000000000444, 0.9999999999999997780, 1.000000000000000000, 0.9999999999999997780, 1.000000000000000444, 0.9999999999999996669, 1.000000000000000444, 1.000000000000000000, 1.000000000000000000, 1.000000000000000000, 0.9999999999999997780, 1.000000000000000444, 1.000000000000000222, 0.9999999999999997780, 1.000000000000000444, 1.000000000000000000, 0.9999999999999996669, 1.000000000000000444, 1.000000000000000000, 1.000000000000000000, 1.000000000000000000, 0.9999999999999997780, 1.000000000000000222, 0.9999999999999997780, 1.000000000000000000, 1.000000000000000222, 0.9999999999999997780, 1.000000000000000000, 1.000000000000000000, 0.9999999999999997780, 1.000000000000000444, 0.9999999999999997780, 1.000000000000000444, 0.9999999999999994449, 1.000000000000000444, 0.9999999999999997780, 1.000000000000000444, 0.9999999999999997780, 1.000000000000000000, 0.9999999999999997780, 1.000000000000000222, 1.000000000000000222, 1.000000000000000000, 1.000000000000000000),
 ( 0.3333333333333333703, 0.3333333333333333703, 0.3333333333333333703, 0.3333333333333335369, 0.3333333333333333148, 0.3333333333333333703, 0.3333333333333333703, 0.3333333333333333148, 0.3333333333333333148, 0.3333333333333334259, 0.3333333333333333703, 0.3333333333333333148, 0.3333333333333334259, 0.3333333333333333148, 0.3333333333333334259, 0.3333333333333333148, 0.3333333333333333703, 0.3333333333333333148, 0.3333333333333334814, 0.3333333333333333148, 0.3333333333333334814, 0.3333333333333334814, 0.3333333333333333148, 0.3333333333333334259, 0.3333333333333333148, 0.3333333333333333703, 0.3333333333333333148, 0.3333333333333334814, 0.3333333333333333703, 0.3333333333333333703, 0.3333333333333333703, 0.3333333333333334259, 0.3333333333333333148, 0.3333333333333333148, 0.3333333333333334259, 0.3333333333333333703, 0.3333333333333334259, 0.3333333333333334259, 0.3333333333333332038, 0.3333333333333334814, 0.3333333333333333703, 0.3333333333333334814, 0.3333333333333332593, 0.3333333333333334259, 0.3333333333333333703, 0.3333333333333334259, 0.3333333333333333148, 0.3333333333333333703, 0.3333333333333334259, 0.3333333333333333148, 0.3333333333333332038, 0.3333333333333335369, 0.3333333333333332593, 0.3333333333333334814, 0.3333333333333333148, 0.3333333333333333703, 0.3333333333333334259, 0.3333333333333333703, 0.3333333333333334814, 0.3333333333333333703, 0.3333333333333334259, 0.3333333333333333148, 0.3333333333333334814, 0.3333333333333332038, 0.3333333333333334259, 0.3333333333333333148, 0.3333333333333333703, 0.3333333333333333703, 0.3333333333333334259, 0.3333333333333333148, 0.3333333333333333703, 0.3333333333333334259, 0.3333333333333333148, 0.3333333333333333703, 0.3333333333333333703, 0.3333333333333335369, 0.3333333333333333148, 0.3333333333333333703, 0.3333333333333333703, 0.3333333333333333703, 0.3333333333333333148, 0.3333333333333333703, 0.3333333333333334814, 0.3333333333333333148, 0.3333333333333334814, 0.3333333333333333703, 0.3333333333333334259, 0.3333333333333333148, 0.3333333333333334259, 0.3333333333333333148, 0.3333333333333334259, 0.3333333333333333148, 0.3333333333333333703, 0.3333333333333333703, 0.3333333333333333703, 0.3333333333333334259, 0.3333333333333334259, 0.3333333333333332593, 0.3333333333333334259, 0.3333333333333333703, 0.3333333333333334259, 0.3333333333333333148, 0.3333333333333334259, 0.3333333333333333703, 0.3333333333333333703, 0.3333333333333333148, 0.3333333333333334259, 0.3333333333333333703, 0.3333333333333333148, 0.3333333333333334259, 0.3333333333333332038, 0.3333333333333334814, 0.3333333333333333148, 0.3333333333333335369, 0.3333333333333334259, 0.3333333333333332038, 0.3333333333333334814, 0.3333333333333333703, 0.3333333333333332593, 0.3333333333333333703, 0.3333333333333332593, 0.3333333333333333703, 0.3333333333333334814, 0.3333333333333333148, 0.3333333333333334814, 0.3333333333333333148, 0.3333333333333334259, 0.3333333333333334259, 0.3333333333333333148, 0.3333333333333334259, 0.3333333333333333148, 0.3333333333333334259, 0.3333333333333333703, 0.3333333333333333703, 0.3333333333333334259, 0.3333333333333332593, 0.3333333333333334814, 0.3333333333333333148, 0.3333333333333333703, 0.3333333333333333703, 0.3333333333333333703, 0.3333333333333334259, 0.3333333333333334259, 0.3333333333333334814, 0.3333333333333333703, 0.3333333333333334259, 0.3333333333333333703, 0.3333333333333333703, 0.3333333333333333148, 0.3333333333333333703, 0.3333333333333334259, 0.3333333333333333148, 0.3333333333333333148, 0.3333333333333333148, 0.3333333333333334259, 0.3333333333333333148, 0.3333333333333334814, 0.3333333333333333148, 0.3333333333333334259, 0.3333333333333334259, 0.3333333333333333148, 0.3333333333333334814, 0.3333333333333333148, 0.3333333333333334814, 0.3333333333333332593, 0.3333333333333335369, 0.3333333333333333148, 0.3333333333333333703, 0.3333333333333333703, 0.3333333333333334259, 0.3333333333333333703, 0.3333333333333333703, 0.3333333333333333148, 0.3333333333333333703, 0.3333333333333332593, 0.3333333333333335369, 0.3333333333333334259, 0.3333333333333333703, 0.3333333333333334259, 0.3333333333333334259, 0.3333333333333332038, 0.3333333333333334814, 0.3333333333333333703, 0.3333333333333334259, 0.3333333333333333703, 0.3333333333333333703, 0.3333333333333333148, 0.3333333333333334814, 0.3333333333333333148, 0.3333333333333334814, 0.3333333333333334259, 0.3333333333333333148, 0.3333333333333333703, 0.3333333333333333703, 0.3333333333333333703, 0.3333333333333333703, 0.3333333333333334259, 0.3333333333333333148, 0.3333333333333334814, 0.3333333333333333148, 0.3333333333333333703, 0.3333333333333334814, 0.3333333333333332593, 0.3333333333333333148, 0.3333333333333334259, 0.3333333333333332593, 0.3333333333333335369, 0.3333333333333333703, 0.3333333333333334259, 0.3333333333333335369, 0.3333333333333333148, 0.3333333333333333703, 0.3333333333333333148, 0.3333333333333333703, 0.3333333333333333148, 0.3333333333333333148, 0.3333333333333333703, 0.3333333333333333703, 0.3333333333333333703, 0.3333333333333333148, 0.3333333333333333703, 0.3333333333333333703, 0.3333333333333334259, 0.3333333333333333703, 0.3333333333333333148, 0.3333333333333333703, 0.3333333333333333703, 0.3333333333333333703, 0.3333333333333334259, 0.3333333333333334259, 0.3333333333333334814, 0.3333333333333332593, 0.3333333333333334259, 0.3333333333333334259, 0.3333333333333333148, 0.3333333333333334259, 0.3333333333333333703, 0.3333333333333333148, 0.3333333333333334814, 0.3333333333333333703, 0.3333333333333334259, 0.3333333333333332593, 0.3333333333333334259, 0.3333333333333332593, 0.3333333333333334814, 0.3333333333333332593, 0.3333333333333334259, 0.3333333333333333148, 0.3333333333333334259, 0.3333333333333333703, 0.3333333333333334259, 0.3333333333333333703, 0.3333333333333333703, 0.3333333333333333703, 0.3333333333333333148, 0.3333333333333334259, 0.3333333333333333703, 0.3333333333333333148, 0.3333333333333334259, 0.3333333333333333148, 0.3333333333333333703, 0.3333333333333333148, 0.3333333333333334814, 0.3333333333333332593, 0.3333333333333333703, 0.3333333333333333703, 0.3333333333333334259, 0.3333333333333332593, 0.3333333333333335369, 0.3333333333333333703, 0.3333333333333333703, 0.3333333333333333703, 0.3333333333333333148, 0.3333333333333333148, 0.3333333333333334259, 0.3333333333333334814, 0.3333333333333334259, 0.3333333333333333703, 0.3333333333333334259, 0.3333333333333334259, 0.3333333333333333703, 0.3333333333333334814, 0.3333333333333333148, 0.3333333333333333148, 0.3333333333333334259, 0.3333333333333332038, 0.3333333333333334814, 0.3333333333333333148, 0.3333333333333335369, 0.3333333333333334259, 0.3333333333333333148, 0.3333333333333334814, 0.3333333333333333703, 0.3333333333333333703, 0.3333333333333334259, 0.3333333333333333703, 0.3333333333333334259, 0.3333333333333333703, 0.3333333333333334259, 0.3333333333333333148, 0.3333333333333333703, 0.3333333333333335369, 0.3333333333333332038, 0.3333333333333334814, 0.3333333333333333703, 0.3333333333333333148, 0.3333333333333334259, 0.3333333333333333703, 0.3333333333333333148, 0.3333333333333334259, 0.3333333333333333703, 0.3333333333333334259, 0.3333333333333332593, 0.3333333333333335369, 0.3333333333333334814, 0.3333333333333333148, 0.3333333333333334259, 0.3333333333333333148, 0.3333333333333335369, 0.3333333333333332593, 0.3333333333333335924, 0.3333333333333332593, 0.3333333333333333703, 0.3333333333333333703, 0.3333333333333334814, 0.3333333333333333703, 0.3333333333333334814, 0.3333333333333333703, 0.3333333333333334259, 0.3333333333333332593, 0.3333333333333334259, 0.3333333333333335369, 0.3333333333333333148, 0.3333333333333334814, 0.3333333333333333148, 0.3333333333333333703, 0.3333333333333334259, 0.3333333333333334259, 0.3333333333333332593, 0.3333333333333334259, 0.3333333333333333148, 0.3333333333333335369, 0.3333333333333332593, 0.3333333333333335369, 0.3333333333333333148, 0.3333333333333333148, 0.3333333333333333703, 0.3333333333333334814, 0.3333333333333333148, 0.3333333333333334259, 0.3333333333333333148, 0.3333333333333334259, 0.3333333333333333703, 0.3333333333333333148, 0.3333333333333334259, 0.3333333333333334814, 0.3333333333333333148, 0.3333333333333334814, 0.3333333333333333703, 0.3333333333333332593, 0.3333333333333334259, 0.3333333333333333703, 0.3333333333333334259, 0.3333333333333333703, 0.3333333333333333148, 0.3333333333333334259, 0.3333333333333333703, 0.3333333333333333148, 0.3333333333333334259, 0.3333333333333333148, 0.3333333333333333148, 0.3333333333333333703, 0.3333333333333333703, 0.3333333333333334259, 0.3333333333333333148, 0.3333333333333334259, 0.3333333333333332593, 0.3333333333333334259, 0.3333333333333333703, 0.3333333333333334259, 0.3333333333333333703, 0.3333333333333333703, 0.3333333333333333148, 0.3333333333333334814, 0.3333333333333334259, 0.3333333333333333703, 0.3333333333333333703),
 ( 0.3333333333333333703, 0.3333333333333333703, 0.3333333333333333703, 0.3333333333333335369, 0.3333333333333333148, 0.3333333333333333703, 0.3333333333333333703, 0.3333333333333333148, 0.3333333333333333148, 0.3333333333333334259, 0.3333333333333333703, 0.3333333333333333148, 0.3333333333333334259, 0.3333333333333333148, 0.3333333333333334259, 0.3333333333333333148, 0.3333333333333333703, 0.3333333333333333148, 0.3333333333333334814, 0.3333333333333333148, 0.3333333333333334814, 0.3333333333333334814, 0.3333333333333333148, 0.3333333333333334259, 0.3333333333333333148, 0.3333333333333333703, 0.3333333333333333148, 0.3333333333333334814, 0.3333333333333333703, 0.3333333333333333703, 0.3333333333333333703, 0.3333333333333334259, 0.3333333333333333148, 0.3333333333333333148, 0.3333333333333334259, 0.3333333333333333703, 0.3333333333333334259, 0.3333333333333334259, 0.3333333333333332038, 0.3333333333333334814, 0.3333333333333333703, 0.3333333333333334814, 0.3333333333333332593, 0.3333333333333334259, 0.3333333333333333703, 0.3333333333333334259, 0.3333333333333333148, 0.3333333333333333703, 0.3333333333333334259, 0.3333333333333333148, 0.3333333333333332038, 0.3333333333333335369, 0.3333333333333332593, 0.3333333333333334814, 0.3333333333333333148, 0.3333333333333333703, 0.3333333333333334259, 0.3333333333333333703, 0.3333333333333334814, 0.3333333333333333703, 0.3333333333333334259, 0.3333333333333333148, 0.3333333333333334814, 0.3333333333333332038, 0.3333333333333334259, 0.3333333333333333148, 0.3333333333333333703, 0.3333333333333333703, 0.3333333333333334259, 0.3333333333333333148, 0.3333333333333333703, 0.3333333333333334259, 0.3333333333333333148, 0.3333333333333333703, 0.3333333333333333703, 0.3333333333333335369, 0.3333333333333333148, 0.3333333333333333703, 0.3333333333333333703, 0.3333333333333333703, 0.3333333333333333148, 0.3333333333333333703, 0.3333333333333334814, 0.3333333333333333148, 0.3333333333333334814, 0.3333333333333333703, 0.3333333333333334259, 0.3333333333333333148, 0.3333333333333334259, 0.3333333333333333148, 0.3333333333333334259, 0.3333333333333333148, 0.3333333333333333703, 0.3333333333333333703, 0.3333333333333333703, 0.3333333333333334259, 0.3333333333333334259, 0.3333333333333332593, 0.3333333333333334259, 0.3333333333333333703, 0.3333333333333334259, 0.3333333333333333148, 0.3333333333333334259, 0.3333333333333333703, 0.3333333333333333703, 0.3333333333333333148, 0.3333333333333334259, 0.3333333333333333703, 0.3333333333333333148, 0.3333333333333334259, 0.3333333333333332038, 0.3333333333333334814, 0.3333333333333333148, 0.3333333333333335369, 0.3333333333333334259, 0.3333333333333332038, 0.3333333333333334814, 0.3333333333333333703, 0.3333333333333332593, 0.3333333333333333703, 0.3333333333333332593, 0.3333333333333333703, 0.3333333333333334814, 0.3333333333333333148, 0.3333333333333334814, 0.3333333333333333148, 0.3333333333333334259, 0.3333333333333334259, 0.3333333333333333148, 0.3333333333333334259, 0.3333333333333333148, 0.3333333333333334259, 0.3333333333333333703, 0.3333333333333333703, 0.3333333333333334259, 0.3333333333333332593, 0.3333333333333334814, 0.3333333333333333148, 0.3333333333333333703, 0.3333333333333333703, 0.3333333333333333703, 0.3333333333333334259, 0.3333333333333334259, 0.3333333333333334814, 0.3333333333333333703, 0.3333333333333334259, 0.3333333333333333703, 0.3333333333333333703, 0.3333333333333333148, 0.3333333333333333703, 0.3333333333333334259, 0.3333333333333333148, 0.3333333333333333148, 0.3333333333333333148, 0.3333333333333334259, 0.3333333333333333148, 0.3333333333333334814, 0.3333333333333333148, 0.3333333333333334259, 0.3333333333333334259, 0.3333333333333333148, 0.3333333333333334814, 0.3333333333333333148, 0.3333333333333334814, 0.3333333333333332593, 0.3333333333333335369, 0.3333333333333333148, 0.3333333333333333703, 0.3333333333333333703, 0.3333333333333334259, 0.3333333333333333703, 0.3333333333333333703, 0.3333333333333333148, 0.3333333333333333703, 0.3333333333333332593, 0.3333333333333335369, 0.3333333333333334259, 0.3333333333333333703, 0.3333333333333334259, 0.3333333333333334259, 0.3333333333333332038, 0.3333333333333334814, 0.3333333333333333703, 0.3333333333333334259, 0.3333333333333333703, 0.3333333333333333703, 0.3333333333333333148, 0.3333333333333334814, 0.3333333333333333148, 0.3333333333333334814, 0.3333333333333334259, 0.3333333333333333148, 0.3333333333333333703, 0.3333333333333333703, 0.3333333333333333703, 0.3333333333333333703, 0.3333333333333334259, 0.3333333333333333148, 0.3333333333333334814, 0.3333333333333333148, 0.3333333333333333703, 0.3333333333333334814, 0.3333333333333332593, 0.3333333333333333148, 0.3333333333333334259, 0.3333333333333332593, 0.3333333333333335369, 0.3333333333333333703, 0.3333333333333334259, 0.3333333333333335369, 0.3333333333333333148, 0.3333333333333333703, 0.3333333333333333148, 0.3333333333333333703, 0.3333333333333333148, 0.3333333333333333148, 0.3333333333333333703, 0.3333333333333333703, 0.3333333333333333703, 0.3333333333333333148, 0.3333333333333333703, 0.3333333333333333703, 0.3333333333333334259, 0.3333333333333333703, 0.3333333333333333148, 0.3333333333333333703, 0.3333333333333333703, 0.3333333333333333703, 0.3333333333333334259, 0.3333333333333334259, 0.3333333333333334814, 0.3333333333333332593, 0.3333333333333334259, 0.3333333333333334259, 0.3333333333333333148, 0.3333333333333334259, 0.3333333333333333703, 0.3333333333333333148, 0.3333333333333334814, 0.3333333333333333703, 0.3333333333333334259, 0.3333333333333332593, 0.3333333333333334259, 0.3333333333333332593, 0.3333333333333334814, 0.3333333333333332593, 0.3333333333333334259, 0.3333333333333333148, 0.3333333333333334259, 0.3333333333333333703, 0.3333333333333334259, 0.3333333333333333703, 0.3333333333333333703, 0.3333333333333333703, 0.3333333333333333148, 0.3333333333333334259, 0.3333333333333333703, 0.3333333333333333148, 0.3333333333333334259, 0.3333333333333333148, 0.3333333333333333703, 0.3333333333333333148, 0.3333333333333334814, 0.3333333333333332593, 0.3333333333333333703, 0.3333333333333333703, 0.3333333333333334259, 0.3333333333333332593, 0.3333333333333335369, 0.3333333333333333703, 0.3333333333333333703, 0.3333333333333333703, 0.3333333333333333148, 0.3333333333333333148, 0.3333333333333334259, 0.3333333333333334814, 0.3333333333333334259, 0.3333333333333333703, 0.3333333333333334259, 0.3333333333333334259, 0.3333333333333333703, 0.3333333333333334814, 0.3333333333333333148, 0.3333333333333333148, 0.3333333333333334259, 0.3333333333333332038, 0.3333333333333334814, 0.3333333333333333148, 0.3333333333333335369, 0.3333333333333334259, 0.3333333333333333148, 0.3333333333333334814, 0.3333333333333333703, 0.3333333333333333703, 0.3333333333333334259, 0.3333333333333333703, 0.3333333333333334259, 0.3333333333333333703, 0.3333333333333334259, 0.3333333333333333148, 0.3333333333333333703, 0.3333333333333335369, 0.3333333333333332038, 0.3333333333333334814, 0.3333333333333333703, 0.3333333333333333148, 0.3333333333333334259, 0.3333333333333333703, 0.3333333333333333148, 0.3333333333333334259, 0.3333333333333333703, 0.3333333333333334259, 0.3333333333333332593, 0.3333333333333335369, 0.3333333333333334814, 0.3333333333333333148, 0.3333333333333334259, 0.3333333333333333148, 0.3333333333333335369, 0.3333333333333332593, 0.3333333333333335924, 0.3333333333333332593, 0.3333333333333333703, 0.3333333333333333703, 0.3333333333333334814, 0.3333333333333333703, 0.3333333333333334814, 0.3333333333333333703, 0.3333333333333334259, 0.3333333333333332593, 0.3333333333333334259, 0.3333333333333335369, 0.3333333333333333148, 0.3333333333333334814, 0.3333333333333333148, 0.3333333333333333703, 0.3333333333333334259, 0.3333333333333334259, 0.3333333333333332593, 0.3333333333333334259, 0.3333333333333333148, 0.3333333333333335369, 0.3333333333333332593, 0.3333333333333335369, 0.3333333333333333148, 0.3333333333333333148, 0.3333333333333333703, 0.3333333333333334814, 0.3333333333333333148, 0.3333333333333334259, 0.3333333333333333148, 0.3333333333333334259, 0.3333333333333333703, 0.3333333333333333148, 0.3333333333333334259, 0.3333333333333334814, 0.3333333333333333148, 0.3333333333333334814, 0.3333333333333333703, 0.3333333333333332593, 0.3333333333333334259, 0.3333333333333333703, 0.3333333333333334259, 0.3333333333333333703, 0.3333333333333333148, 0.3333333333333334259, 0.3333333333333333703, 0.3333333333333333148, 0.3333333333333334259, 0.3333333333333333148, 0.3333333333333333148, 0.3333333333333333703, 0.3333333333333333703, 0.3333333333333334259, 0.3333333333333333148, 0.3333333333333334259, 0.3333333333333332593, 0.3333333333333334259, 0.3333333333333333703, 0.3333333333333334259, 0.3333333333333333703, 0.3333333333333333703, 0.3333333333333333148, 0.3333333333333334814, 0.3333333333333334259, 0.3333333333333333703, 0.3333333333333333703),
 ( 1.000000000000000000, 1.000000000000000000, 1.000000000000000000, 1.000000000000000222, 0.9999999999999996669, 1.000000000000000222, 0.9999999999999997780, 1.000000000000000000, 0.9999999999999997780, 1.000000000000000444, 1.000000000000000000, 0.9999999999999997780, 1.000000000000000222, 1.000000000000000000, 0.9999999999999997780, 1.000000000000000222, 0.9999999999999996669, 1.000000000000000000, 1.000000000000000222, 1.000000000000000000, 1.000000000000000000, 1.000000000000000444, 0.9999999999999994449, 1.000000000000000444, 0.9999999999999996669, 1.000000000000000222, 1.000000000000000000, 1.000000000000000444, 1.000000000000000000, 0.9999999999999997780, 1.000000000000000000, 1.000000000000000222, 0.9999999999999997780, 0.9999999999999997780, 1.000000000000000444, 0.9999999999999997780, 1.000000000000000444, 1.000000000000000222, 0.9999999999999996669, 1.000000000000000222, 1.000000000000000000, 1.000000000000000444, 0.9999999999999997780, 1.000000000000000222, 1.000000000000000222, 1.000000000000000222, 0.9999999999999997780, 1.000000000000000000, 1.000000000000000000, 1.000000000000000000, 0.9999999999999994449, 1.000000000000000444, 0.9999999999999997780, 1.000000000000000444, 0.9999999999999997780, 1.000000000000000000, 1.000000000000000000, 0.9999999999999997780, 1.000000000000000444, 0.9999999999999996669, 1.000000000000000444, 0.9999999999999996669, 1.000000000000000222, 0.9999999999999994449, 1.000000000000000222, 1.000000000000000000, 1.000000000000000000, 1.000000000000000000, 1.000000000000000000, 1.000000000000000222, 1.000000000000000000, 1.000000000000000222, 0.9999999999999996669, 1.000000000000000222, 1.000000000000000000, 1.000000000000000444, 1.000000000000000000, 1.000000000000000000, 0.9999999999999997780, 1.000000000000000222, 0.9999999999999997780, 0.9999999999999997780, 1.000000000000000444, 1.000000000000000000, 1.000000000000000222, 0.9999999999999996669, 1.000000000000000444, 0.9999999999999997780, 1.000000000000000222, 0.9999999999999997780, 1.000000000000000222, 1.000000000000000000, 1.000000000000000000, 1.000000000000000000, 1.000000000000000000, 1.000000000000000222, 1.000000000000000222, 0.9999999999999997780, 1.000000000000000222, 1.000000000000000000, 1.000000000000000222, 0.9999999999999997780, 1.000000000000000222, 1.000000000000000000, 1.000000000000000000, 0.9999999999999997780, 1.000000000000000000, 1.000000000000000000, 0.9999999999999997780, 1.000000000000000222, 0.9999999999999997780, 1.000000000000000222, 0.9999999999999997780, 1.000000000000000444, 1.000000000000000000, 0.9999999999999996669, 1.000000000000000444, 1.000000000000000000, 0.9999999999999997780, 1.000000000000000000, 0.9999999999999996669, 1.000000000000000000, 1.000000000000000222, 0.9999999999999996669, 1.000000000000000222, 0.9999999999999997780, 1.000000000000000000, 1.000000000000000222, 0.9999999999999997780, 1.000000000000000222, 0.9999999999999997780, 1.000000000000000222, 1.000000000000000000, 1.000000000000000000, 1.000000000000000000, 0.9999999999999997780, 1.000000000000000222, 0.9999999999999997780, 1.000000000000000222, 1.000000000000000000, 1.000000000000000000, 1.000000000000000000, 1.000000000000000000, 1.000000000000000444, 0.9999999999999997780, 1.000000000000000444, 0.9999999999999997780, 1.000000000000000222, 1.000000000000000000, 1.000000000000000000, 1.000000000000000000, 1.000000000000000000, 0.9999999999999997780, 1.000000000000000000, 1.000000000000000222, 0.9999999999999997780, 1.000000000000000222, 1.000000000000000000, 1.000000000000000000, 1.000000000000000222, 0.9999999999999997780, 1.000000000000000222, 0.9999999999999996669, 1.000000000000000444, 0.9999999999999994449, 1.000000000000000444, 0.9999999999999997780, 0.9999999999999997780, 1.000000000000000000, 1.000000000000000000, 1.000000000000000222, 1.000000000000000000, 1.000000000000000000, 1.000000000000000000, 1.000000000000000000, 1.000000000000000222, 1.000000000000000444, 0.9999999999999997780, 1.000000000000000222, 1.000000000000000000, 0.9999999999999996669, 1.000000000000000222, 1.000000000000000222, 1.000000000000000222, 1.000000000000000222, 1.000000000000000000, 1.000000000000000000, 1.000000000000000222, 1.000000000000000000, 1.000000000000000222, 1.000000000000000000, 1.000000000000000000, 1.000000000000000000, 1.000000000000000222, 0.9999999999999997780, 1.000000000000000000, 1.000000000000000222, 1.000000000000000000, 1.000000000000000222, 1.000000000000000000, 0.9999999999999997780, 1.000000000000000444, 1.000000000000000000, 0.9999999999999996669, 1.000000000000000222, 0.9999999999999997780, 1.000000000000000222, 1.000000000000000000, 1.000000000000000000, 1.000000000000000444, 0.9999999999999996669, 1.000000000000000000, 0.9999999999999997780, 1.000000000000000000, 0.9999999999999997780, 0.9999999999999997780, 1.000000000000000000, 1.000000000000000000, 1.000000000000000000, 0.9999999999999997780, 1.000000000000000000, 1.000000000000000222, 1.000000000000000222, 1.000000000000000000, 0.9999999999999997780, 1.000000000000000222, 1.000000000000000000, 1.000000000000000000, 1.000000000000000222, 1.000000000000000222, 1.000000000000000222, 1.000000000000000000, 0.9999999999999997780, 1.000000000000000444, 0.9999999999999997780, 1.000000000000000444, 0.9999999999999997780, 1.000000000000000000, 1.000000000000000222, 0.9999999999999997780, 1.000000000000000222, 0.9999999999999997780, 1.000000000000000222, 0.9999999999999997780, 1.000000000000000222, 0.9999999999999996669, 1.000000000000000222, 0.9999999999999997780, 1.000000000000000444, 1.000000000000000000, 1.000000000000000000, 0.9999999999999997780, 1.000000000000000222, 1.000000000000000000, 0.9999999999999996669, 1.000000000000000222, 0.9999999999999997780, 1.000000000000000000, 1.000000000000000222, 1.000000000000000000, 1.000000000000000222, 0.9999999999999996669, 1.000000000000000444, 0.9999999999999996669, 1.000000000000000000, 1.000000000000000000, 1.000000000000000000, 0.9999999999999997780, 1.000000000000000444, 1.000000000000000000, 1.000000000000000000, 1.000000000000000000, 1.000000000000000000, 0.9999999999999997780, 1.000000000000000222, 1.000000000000000222, 1.000000000000000222, 1.000000000000000000, 1.000000000000000222, 1.000000000000000000, 0.9999999999999997780, 1.000000000000000444, 1.000000000000000000, 0.9999999999999997780, 1.000000000000000222, 0.9999999999999996669, 1.000000000000000222, 1.000000000000000000, 1.000000000000000444, 1.000000000000000222, 0.9999999999999996669, 1.000000000000000222, 0.9999999999999997780, 1.000000000000000222, 1.000000000000000222, 0.9999999999999997780, 1.000000000000000222, 1.000000000000000000, 1.000000000000000222, 1.000000000000000222, 0.9999999999999997780, 1.000000000000000444, 0.9999999999999996669, 1.000000000000000222, 1.000000000000000222, 1.000000000000000000, 1.000000000000000000, 1.000000000000000000, 1.000000000000000222, 1.000000000000000000, 1.000000000000000000, 1.000000000000000222, 0.9999999999999996669, 1.000000000000000444, 1.000000000000000222, 0.9999999999999997780, 1.000000000000000222, 0.9999999999999997780, 1.000000000000000444, 0.9999999999999996669, 1.000000000000000666, 0.9999999999999994449, 1.000000000000000222, 0.9999999999999997780, 1.000000000000000444, 1.000000000000000000, 1.000000000000000222, 1.000000000000000222, 1.000000000000000000, 0.9999999999999997780, 0.9999999999999997780, 1.000000000000000444, 1.000000000000000000, 1.000000000000000000, 1.000000000000000000, 0.9999999999999997780, 1.000000000000000222, 1.000000000000000222, 0.9999999999999997780, 1.000000000000000222, 1.000000000000000000, 1.000000000000000444, 0.9999999999999996669, 1.000000000000000444, 0.9999999999999997780, 1.000000000000000000, 0.9999999999999997780, 1.000000000000000444, 0.9999999999999996669, 1.000000000000000444, 1.000000000000000000, 1.000000000000000000, 1.000000000000000000, 0.9999999999999997780, 1.000000000000000444, 1.000000000000000222, 0.9999999999999997780, 1.000000000000000444, 1.000000000000000000, 0.9999999999999996669, 1.000000000000000444, 1.000000000000000000, 1.000000000000000000, 1.000000000000000000, 0.9999999999999997780, 1.000000000000000222, 0.9999999999999997780, 1.000000000000000000, 1.000000000000000222, 0.9999999999999997780, 1.000000000000000000, 1.000000000000000000, 0.9999999999999997780, 1.000000000000000444, 0.9999999999999997780, 1.000000000000000444, 0.9999999999999994449, 1.000000000000000444, 0.9999999999999997780, 1.000000000000000444, 0.9999999999999997780, 1.000000000000000000, 0.9999999999999997780, 1.000000000000000222, 1.000000000000000222, 1.000000000000000000, 1.000000000000000000),
 ( 0.3333333333333333703, 0.3333333333333333703, 0.3333333333333333703, 0.3333333333333335369, 0.3333333333333333148, 0.3333333333333333703, 0.3333333333333333703, 0.3333333333333333148, 0.3333333333333333148, 0.3333333333333334259, 0.3333333333333333703, 0.3333333333333333148, 0.3333333333333334259, 0.3333333333333333148, 0.3333333333333334259, 0.3333333333333333148, 0.3333333333333333703, 0.3333333333333333148, 0.3333333333333334814, 0.3333333333333333148, 0.3333333333333334814, 0.3333333333333334814, 0.3333333333333333148, 0.3333333333333334259, 0.3333333333333333148, 0.3333333333333333703, 0.3333333333333333148, 0.3333333333333334814, 0.3333333333333333703, 0.3333333333333333703, 0.3333333333333333703, 0.3333333333333334259, 0.3333333333333333148, 0.3333333333333333148, 0.3333333333333334259, 0.3333333333333333703, 0.3333333333333334259, 0.3333333333333334259, 0.3333333333333332038, 0.3333333333333334814, 0.3333333333333333703, 0.3333333333333334814, 0.3333333333333332593, 0.3333333333333334259, 0.3333333333333333703, 0.3333333333333334259, 0.3333333333333333148, 0.3333333333333333703, 0.3333333333333334259, 0.3333333333333333148, 0.3333333333333332038, 0.3333333333333335369, 0.3333333333333332593, 0.3333333333333334814, 0.3333333333333333148, 0.3333333333333333703, 0.3333333333333334259, 0.3333333333333333703, 0.3333333333333334814, 0.3333333333333333703, 0.3333333333333334259, 0.3333333333333333148, 0.3333333333333334814, 0.3333333333333332038, 0.3333333333333334259, 0.3333333333333333148, 0.3333333333333333703, 0.3333333333333333703, 0.3333333333333334259, 0.3333333333333333148, 0.3333333333333333703, 0.3333333333333334259, 0.3333333333333333148, 0.3333333333333333703, 0.3333333333333333703, 0.3333333333333335369, 0.3333333333333333148, 0.3333333333333333703, 0.3333333333333333703, 0.3333333333333333703, 0.3333333333333333148, 0.3333333333333333703, 0.3333333333333334814, 0.3333333333333333148, 0.3333333333333334814, 0.3333333333333333703, 0.3333333333333334259, 0.3333333333333333148, 0.3333333333333334259, 0.3333333333333333148, 0.3333333333333334259, 0.3333333333333333148, 0.3333333333333333703, 0.3333333333333333703, 0.3333333333333333703, 0.3333333333333334259, 0.3333333333333334259, 0.3333333333333332593, 0.3333333333333334259, 0.3333333333333333703, 0.3333333333333334259, 0.3333333333333333148, 0.3333333333333334259, 0.3333333333333333703, 0.3333333333333333703, 0.3333333333333333148, 0.3333333333333334259, 0.3333333333333333703, 0.3333333333333333148, 0.3333333333333334259, 0.3333333333333332038, 0.3333333333333334814, 0.3333333333333333148, 0.3333333333333335369, 0.3333333333333334259, 0.3333333333333332038, 0.3333333333333334814, 0.3333333333333333703, 0.3333333333333332593, 0.3333333333333333703, 0.3333333333333332593, 0.3333333333333333703, 0.3333333333333334814, 0.3333333333333333148, 0.3333333333333334814, 0.3333333333333333148, 0.3333333333333334259, 0.3333333333333334259, 0.3333333333333333148, 0.3333333333333334259, 0.3333333333333333148, 0.3333333333333334259, 0.3333333333333333703, 0.3333333333333333703, 0.3333333333333334259, 0.3333333333333332593, 0.3333333333333334814, 0.3333333333333333148, 0.3333333333333333703, 0.3333333333333333703, 0.3333333333333333703, 0.3333333333333334259, 0.3333333333333334259, 0.3333333333333334814, 0.3333333333333333703, 0.3333333333333334259, 0.3333333333333333703, 0.3333333333333333703, 0.3333333333333333148, 0.3333333333333333703, 0.3333333333333334259, 0.3333333333333333148, 0.3333333333333333148, 0.3333333333333333148, 0.3333333333333334259, 0.3333333333333333148, 0.3333333333333334814, 0.3333333333333333148, 0.3333333333333334259, 0.3333333333333334259, 0.3333333333333333148, 0.3333333333333334814, 0.3333333333333333148, 0.3333333333333334814, 0.3333333333333332593, 0.3333333333333335369, 0.3333333333333333148, 0.3333333333333333703, 0.3333333333333333703, 0.3333333333333334259, 0.3333333333333333703, 0.3333333333333333703, 0.3333333333333333148, 0.3333333333333333703, 0.3333333333333332593, 0.3333333333333335369, 0.3333333333333334259, 0.3333333333333333703, 0.3333333333333334259, 0.3333333333333334259, 0.3333333333333332038, 0.3333333333333334814, 0.3333333333333333703, 0.3333333333333334259, 0.3333333333333333703, 0.3333333333333333703, 0.3333333333333333148, 0.3333333333333334814, 0.3333333333333333148, 0.3333333333333334814, 0.3333333333333334259, 0.3333333333333333148, 0.3333333333333333703, 0.3333333333333333703, 0.3333333333333333703, 0.3333333333333333703, 0.3333333333333334259, 0.3333333333333333148, 0.3333333333333334814, 0.3333333333333333148, 0.3333333333333333703, 0.3333333333333334814, 0.3333333333333332593, 0.3333333333333333148, 0.3333333333333334259, 0.3333333333333332593, 0.3333333333333335369, 0.3333333333333333703, 0.3333333333333334259, 0.3333333333333335369, 0.3333333333333333148, 0.3333333333333333703, 0.3333333333333333148, 0.3333333333333333703, 0.3333333333333333148, 0.3333333333333333148, 0.3333333333333333703, 0.3333333333333333703, 0.3333333333333333703, 0.3333333333333333148, 0.3333333333333333703, 0.3333333333333333703, 0.3333333333333334259, 0.3333333333333333703, 0.3333333333333333148, 0.3333333333333333703, 0.3333333333333333703, 0.3333333333333333703, 0.3333333333333334259, 0.3333333333333334259, 0.3333333333333334814, 0.3333333333333332593, 0.3333333333333334259, 0.3333333333333334259, 0.3333333333333333148, 0.3333333333333334259, 0.3333333333333333703, 0.3333333333333333148, 0.3333333333333334814, 0.3333333333333333703, 0.3333333333333334259, 0.3333333333333332593, 0.3333333333333334259, 0.3333333333333332593, 0.3333333333333334814, 0.3333333333333332593, 0.3333333333333334259, 0.3333333333333333148, 0.3333333333333334259, 0.3333333333333333703, 0.3333333333333334259, 0.3333333333333333703, 0.3333333333333333703, 0.3333333333333333703, 0.3333333333333333148, 0.3333333333333334259, 0.3333333333333333703, 0.3333333333333333148, 0.3333333333333334259, 0.3333333333333333148, 0.3333333333333333703, 0.3333333333333333148, 0.3333333333333334814, 0.3333333333333332593, 0.3333333333333333703, 0.3333333333333333703, 0.3333333333333334259, 0.3333333333333332593, 0.3333333333333335369, 0.3333333333333333703, 0.3333333333333333703, 0.3333333333333333703, 0.3333333333333333148, 0.3333333333333333148, 0.3333333333333334259, 0.3333333333333334814, 0.3333333333333334259, 0.3333333333333333703, 0.3333333333333334259, 0.3333333333333334259, 0.3333333333333333703, 0.3333333333333334814, 0.3333333333333333148, 0.3333333333333333148, 0.3333333333333334259, 0.3333333333333332038, 0.3333333333333334814, 0.3333333333333333148, 0.3333333333333335369, 0.3333333333333334259, 0.3333333333333333148, 0.3333333333333334814, 0.3333333333333333703, 0.3333333333333333703, 0.3333333333333334259, 0.3333333333333333703, 0.3333333333333334259, 0.3333333333333333703, 0.3333333333333334259, 0.3333333333333333148, 0.3333333333333333703, 0.3333333333333335369, 0.3333333333333332038, 0.3333333333333334814, 0.3333333333333333703, 0.3333333333333333148, 0.3333333333333334259, 0.3333333333333333703, 0.3333333333333333148, 0.3333333333333334259, 0.3333333333333333703, 0.3333333333333334259, 0.3333333333333332593, 0.3333333333333335369, 0.3333333333333334814, 0.3333333333333333148, 0.3333333333333334259, 0.3333333333333333148, 0.3333333333333335369, 0.3333333333333332593, 0.3333333333333335924, 0.3333333333333332593, 0.3333333333333333703, 0.3333333333333333703, 0.3333333333333334814, 0.3333333333333333703, 0.3333333333333334814, 0.3333333333333333703, 0.3333333333333334259, 0.3333333333333332593, 0.3333333333333334259, 0.3333333333333335369, 0.3333333333333333148, 0.3333333333333334814, 0.3333333333333333148, 0.3333333333333333703, 0.3333333333333334259, 0.3333333333333334259, 0.3333333333333332593, 0.3333333333333334259, 0.3333333333333333148, 0.3333333333333335369, 0.3333333333333332593, 0.3333333333333335369, 0.3333333333333333148, 0.3333333333333333148, 0.3333333333333333703, 0.3333333333333334814, 0.3333333333333333148, 0.3333333333333334259, 0.3333333333333333148, 0.3333333333333334259, 0.3333333333333333703, 0.3333333333333333148, 0.3333333333333334259, 0.3333333333333334814, 0.3333333333333333148, 0.3333333333333334814, 0.3333333333333333703, 0.3333333333333332593, 0.3333333333333334259, 0.3333333333333333703, 0.3333333333333334259, 0.3333333333333333703, 0.3333333333333333148, 0.3333333333333334259, 0.3333333333333333703, 0.3333333333333333148, 0.3333333333333334259, 0.3333333333333333148, 0.3333333333333333148, 0.3333333333333333703, 0.3333333333333333703, 0.3333333333333334259, 0.3333333333333333148, 0.3333333333333334259, 0.3333333333333332593, 0.3333333333333334259, 0.3333333333333333703, 0.3333333333333334259, 0.3333333333333333703, 0.3333333333333333703, 0.3333333333333333148, 0.3333333333333334814, 0.3333333333333334259, 0.3333333333333333703, 0.3333333333333333703),
 ( 0.3333333333333333703, 0.3333333333333333703, 0.3333333333333333703, 0.3333333333333335369, 0.3333333333333333148, 0.3333333333333333703, 0.3333333333333333703, 0.3333333333333333148, 0.3333333333333333148, 0.3333333333333334259, 0.3333333333333333703, 0.3333333333333333148, 0.3333333333333334259, 0.3333333333333333148, 0.3333333333333334259, 0.3333333333333333148, 0.3333333333333333703, 0.3333333333333333148, 0.3333333333333334814, 0.3333333333333333148, 0.3333333333333334814, 0.3333333333333334814, 0.3333333333333333148, 0.3333333333333334259, 0.3333333333333333148, 0.3333333333333333703, 0.3333333333333333148, 0.3333333333333334814, 0.3333333333333333703, 0.3333333333333333703, 0.3333333333333333703, 0.3333333333333334259, 0.3333333333333333148, 0.3333333333333333148, 0.3333333333333334259, 0.3333333333333333703, 0.3333333333333334259, 0.3333333333333334259, 0.3333333333333332038, 0.3333333333333334814, 0.3333333333333333703, 0.3333333333333334814, 0.3333333333333332593, 0.3333333333333334259, 0.3333333333333333703, 0.3333333333333334259, 0.3333333333333333148, 0.3333333333333333703, 0.3333333333333334259, 0.3333333333333333148, 0.3333333333333332038, 0.3333333333333335369, 0.3333333333333332593, 0.3333333333333334814, 0.3333333333333333148, 0.3333333333333333703, 0.3333333333333334259, 0.3333333333333333703, 0.3333333333333334814, 0.3333333333333333703, 0.3333333333333334259, 0.3333333333333333148, 0.3333333333333334814, 0.3333333333333332038, 0.3333333333333334259, 0.3333333333333333148, 0.3333333333333333703, 0.3333333333333333703, 0.3333333333333334259, 0.3333333333333333148, 0.3333333333333333703, 0.3333333333333334259, 0.3333333333333333148, 0.3333333333333333703, 0.3333333333333333703, 0.3333333333333335369, 0.3333333333333333148, 0.3333333333333333703, 0.3333333333333333703, 0.3333333333333333703, 0.3333333333333333148, 0.3333333333333333703, 0.3333333333333334814, 0.3333333333333333148, 0.3333333333333334814, 0.3333333333333333703, 0.3333333333333334259, 0.3333333333333333148, 0.3333333333333334259, 0.3333333333333333148, 0.3333333333333334259, 0.3333333333333333148, 0.3333333333333333703, 0.3333333333333333703, 0.3333333333333333703, 0.3333333333333334259, 0.3333333333333334259, 0.3333333333333332593, 0.3333333333333334259, 0.3333333333333333703, 0.3333333333333334259, 0.3333333333333333148, 0.3333333333333334259, 0.3333333333333333703, 0.3333333333333333703, 0.3333333333333333148, 0.3333333333333334259, 0.3333333333333333703, 0.3333333333333333148, 0.3333333333333334259, 0.3333333333333332038, 0.3333333333333334814, 0.3333333333333333148, 0.3333333333333335369, 0.3333333333333334259, 0.3333333333333332038, 0.3333333333333334814, 0.3333333333333333703, 0.3333333333333332593, 0.3333333333333333703, 0.3333333333333332593, 0.3333333333333333703, 0.3333333333333334814, 0.3333333333333333148, 0.3333333333333334814, 0.3333333333333333148, 0.3333333333333334259, 0.3333333333333334259, 0.3333333333333333148, 0.3333333333333334259, 0.3333333333333333148, 0.3333333333333334259, 0.3333333333333333703, 0.3333333333333333703, 0.3333333333333334259, 0.3333333333333332593, 0.3333333333333334814, 0.3333333333333333148, 0.3333333333333333703, 0.3333333333333333703, 0.3333333333333333703, 0.3333333333333334259, 0.3333333333333334259, 0.3333333333333334814, 0.3333333333333333703, 0.3333333333333334259, 0.3333333333333333703, 0.3333333333333333703, 0.3333333333333333148, 0.3333333333333333703, 0.3333333333333334259, 0.3333333333333333148, 0.3333333333333333148, 0.3333333333333333148, 0.3333333333333334259, 0.3333333333333333148, 0.3333333333333334814, 0.3333333333333333148, 0.3333333333333334259, 0.3333333333333334259, 0.3333333333333333148, 0.3333333333333334814, 0.3333333333333333148, 0.3333333333333334814, 0.3333333333333332593, 0.3333333333333335369, 0.3333333333333333148, 0.3333333333333333703, 0.3333333333333333703, 0.3333333333333334259, 0.3333333333333333703, 0.3333333333333333703, 0.3333333333333333148, 0.3333333333333333703, 0.3333333333333332593, 0.3333333333333335369, 0.3333333333333334259, 0.3333333333333333703, 0.3333333333333334259, 0.3333333333333334259, 0.3333333333333332038, 0.3333333333333334814, 0.3333333333333333703, 0.3333333333333334259, 0.3333333333333333703, 0.3333333333333333703, 0.3333333333333333148, 0.3333333333333334814, 0.3333333333333333148, 0.3333333333333334814, 0.3333333333333334259, 0.3333333333333333148, 0.3333333333333333703, 0.3333333333333333703, 0.3333333333333333703, 0.3333333333333333703, 0.3333333333333334259, 0.3333333333333333148, 0.3333333333333334814, 0.3333333333333333148, 0.3333333333333333703, 0.3333333333333334814, 0.3333333333333332593, 0.3333333333333333148, 0.3333333333333334259, 0.3333333333333332593, 0.3333333333333335369, 0.3333333333333333703, 0.3333333333333334259, 0.3333333333333335369, 0.3333333333333333148, 0.3333333333333333703, 0.3333333333333333148, 0.3333333333333333703, 0.3333333333333333148, 0.3333333333333333148, 0.3333333333333333703, 0.3333333333333333703, 0.3333333333333333703, 0.3333333333333333148, 0.3333333333333333703, 0.3333333333333333703, 0.3333333333333334259, 0.3333333333333333703, 0.3333333333333333148, 0.3333333333333333703, 0.3333333333333333703, 0.3333333333333333703, 0.3333333333333334259, 0.3333333333333334259, 0.3333333333333334814, 0.3333333333333332593, 0.3333333333333334259, 0.3333333333333334259, 0.3333333333333333148, 0.3333333333333334259, 0.3333333333333333703, 0.3333333333333333148, 0.3333333333333334814, 0.3333333333333333703, 0.3333333333333334259, 0.3333333333333332593, 0.3333333333333334259, 0.3333333333333332593, 0.3333333333333334814, 0.3333333333333332593, 0.3333333333333334259, 0.3333333333333333148, 0.3333333333333334259, 0.3333333333333333703, 0.3333333333333334259, 0.3333333333333333703, 0.3333333333333333703, 0.3333333333333333703, 0.3333333333333333148, 0.3333333333333334259, 0.3333333333333333703, 0.3333333333333333148, 0.3333333333333334259, 0.3333333333333333148, 0.3333333333333333703, 0.3333333333333333148, 0.3333333333333334814, 0.3333333333333332593, 0.3333333333333333703, 0.3333333333333333703, 0.3333333333333334259, 0.3333333333333332593, 0.3333333333333335369, 0.3333333333333333703, 0.3333333333333333703, 0.3333333333333333703, 0.3333333333333333148, 0.3333333333333333148, 0.3333333333333334259, 0.3333333333333334814, 0.3333333333333334259, 0.3333333333333333703, 0.3333333333333334259, 0.3333333333333334259, 0.3333333333333333703, 0.3333333333333334814, 0.3333333333333333148, 0.3333333333333333148, 0.3333333333333334259, 0.3333333333333332038, 0.3333333333333334814, 0.3333333333333333148, 0.3333333333333335369, 0.3333333333333334259, 0.3333333333333333148, 0.3333333333333334814, 0.3333333333333333703, 0.3333333333333333703, 0.3333333333333334259, 0.3333333333333333703, 0.3333333333333334259, 0.3333333333333333703, 0.3333333333333334259, 0.3333333333333333148, 0.3333333333333333703, 0.3333333333333335369, 0.3333333333333332038, 0.3333333333333334814, 0.3333333333333333703, 0.3333333333333333148, 0.3333333333333334259, 0.3333333333333333703, 0.3333333333333333148, 0.3333333333333334259, 0.3333333333333333703, 0.3333333333333334259, 0.3333333333333332593, 0.3333333333333335369, 0.3333333333333334814, 0.3333333333333333148, 0.3333333333333334259, 0.3333333333333333148, 0.3333333333333335369, 0.3333333333333332593, 0.3333333333333335924, 0.3333333333333332593, 0.3333333333333333703, 0.3333333333333333703, 0.3333333333333334814, 0.3333333333333333703, 0.3333333333333334814, 0.3333333333333333703, 0.3333333333333334259, 0.3333333333333332593, 0.3333333333333334259, 0.3333333333333335369, 0.3333333333333333148, 0.3333333333333334814, 0.3333333333333333148, 0.3333333333333333703, 0.3333333333333334259, 0.3333333333333334259, 0.3333333333333332593, 0.3333333333333334259, 0.3333333333333333148, 0.3333333333333335369, 0.3333333333333332593, 0.3333333333333335369, 0.3333333333333333148, 0.3333333333333333148, 0.3333333333333333703, 0.3333333333333334814, 0.3333333333333333148, 0.3333333333333334259, 0.3333333333333333148, 0.3333333333333334259, 0.3333333333333333703, 0.3333333333333333148, 0.3333333333333334259, 0.3333333333333334814, 0.3333333333333333148, 0.3333333333333334814, 0.3333333333333333703, 0.3333333333333332593, 0.3333333333333334259, 0.3333333333333333703, 0.3333333333333334259, 0.3333333333333333703, 0.3333333333333333148, 0.3333333333333334259, 0.3333333333333333703, 0.3333333333333333148, 0.3333333333333334259, 0.3333333333333333148, 0.3333333333333333148, 0.3333333333333333703, 0.3333333333333333703, 0.3333333333333334259, 0.3333333333333333148, 0.3333333333333334259, 0.3333333333333332593, 0.3333333333333334259, 0.3333333333333333703, 0.3333333333333334259, 0.3333333333333333703, 0.3333333333333333703, 0.3333333333333333148, 0.3333333333333334814, 0.3333333333333334259, 0.3333333333333333703, 0.3333333333333333703),
 ( 1.000000000000000000, 1.000000000000000000, 1.000000000000000000, 1.000000000000000222, 0.9999999999999996669, 1.000000000000000222, 0.9999999999999997780, 1.000000000000000000, 0.9999999999999997780, 1.000000000000000444, 1.000000000000000000, 0.9999999999999997780, 1.000000000000000222, 1.000000000000000000, 0.9999999999999997780, 1.000000000000000222, 0.9999999999999996669, 1.000000000000000000, 1.000000000000000222, 1.000000000000000000, 1.000000000000000000, 1.000000000000000444, 0.9999999999999994449, 1.000000000000000444, 0.9999999999999996669, 1.000000000000000222, 1.000000000000000000, 1.000000000000000444, 1.000000000000000000, 0.9999999999999997780, 1.000000000000000000, 1.000000000000000222, 0.9999999999999997780, 0.9999999999999997780, 1.000000000000000444, 0.9999999999999997780, 1.000000000000000444, 1.000000000000000222, 0.9999999999999996669, 1.000000000000000222, 1.000000000000000000, 1.000000000000000444, 0.9999999999999997780, 1.000000000000000222, 1.000000000000000222, 1.000000000000000222, 0.9999999999999997780, 1.000000000000000000, 1.000000000000000000, 1.000000000000000000, 0.9999999999999994449, 1.000000000000000444, 0.9999999999999997780, 1.000000000000000444, 0.9999999999999997780, 1.000000000000000000, 1.000000000000000000, 0.9999999999999997780, 1.000000000000000444, 0.9999999999999996669, 1.000000000000000444, 0.9999999999999996669, 1.000000000000000222, 0.9999999999999994449, 1.000000000000000222, 1.000000000000000000, 1.000000000000000000, 1.000000000000000000, 1.000000000000000000, 1.000000000000000222, 1.000000000000000000, 1.000000000000000222, 0.9999999999999996669, 1.000000000000000222, 1.000000000000000000, 1.000000000000000444, 1.000000000000000000, 1.000000000000000000, 0.9999999999999997780, 1.000000000000000222, 0.9999999999999997780, 0.9999999999999997780, 1.000000000000000444, 1.000000000000000000, 1.000000000000000222, 0.9999999999999996669, 1.000000000000000444, 0.9999999999999997780, 1.000000000000000222, 0.9999999999999997780, 1.000000000000000222, 1.000000000000000000, 1.000000000000000000, 1.000000000000000000, 1.000000000000000000, 1.000000000000000222, 1.000000000000000222, 0.9999999999999997780, 1.000000000000000222, 1.000000000000000000, 1.000000000000000222, 0.9999999999999997780, 1.000000000000000222, 1.000000000000000000, 1.000000000000000000, 0.9999999999999997780, 1.000000000000000000, 1.000000000000000000, 0.9999999999999997780, 1.000000000000000222, 0.9999999999999997780, 1.000000000000000222, 0.9999999999999997780, 1.000000000000000444, 1.000000000000000000, 0.9999999999999996669, 1.000000000000000444, 1.000000000000000000, 0.9999999999999997780, 1.000000000000000000, 0.9999999999999996669, 1.000000000000000000, 1.000000000000000222, 0.9999999999999996669, 1.000000000000000222, 0.9999999999999997780, 1.000000000000000000, 1.000000000000000222, 0.9999999999999997780, 1.000000000000000222, 0.9999999999999997780, 1.000000000000000222, 1.000000000000000000, 1.000000000000000000, 1.000000000000000000, 0.9999999999999997780, 1.000000000000000222, 0.9999999999999997780, 1.000000000000000222, 1.000000000000000000, 1.000000000000000000, 1.000000000000000000, 1.000000000000000000, 1.000000000000000444, 0.9999999999999997780, 1.000000000000000444, 0.9999999999999997780, 1.000000000000000222, 1.000000000000000000, 1.000000000000000000, 1.000000000000000000, 1.000000000000000000, 0.9999999999999997780, 1.000000000000000000, 1.000000000000000222, 0.9999999999999997780, 1.000000000000000222, 1.000000000000000000, 1.000000000000000000, 1.000000000000000222, 0.9999999999999997780, 1.000000000000000222, 0.9999999999999996669, 1.000000000000000444, 0.9999999999999994449, 1.000000000000000444, 0.9999999999999997780, 0.9999999999999997780, 1.000000000000000000, 1.000000000000000000, 1.000000000000000222, 1.000000000000000000, 1.000000000000000000, 1.000000000000000000, 1.000000000000000000, 1.000000000000000222, 1.000000000000000444, 0.9999999999999997780, 1.000000000000000222, 1.000000000000000000, 0.9999999999999996669, 1.000000000000000222, 1.000000000000000222, 1.000000000000000222, 1.000000000000000222, 1.000000000000000000, 1.000000000000000000, 1.000000000000000222, 1.000000000000000000, 1.000000000000000222, 1.000000000000000000, 1.000000000000000000, 1.000000000000000000, 1.000000000000000222, 0.9999999999999997780, 1.000000000000000000, 1.000000000000000222, 1.000000000000000000, 1.000000000000000222, 1.000000000000000000, 0.9999999999999997780, 1.000000000000000444, 1.000000000000000000, 0.9999999999999996669, 1.000000000000000222, 0.9999999999999997780, 1.000000000000000222, 1.000000000000000000, 1.000000000000000000, 1.000000000000000444, 0.9999999999999996669, 1.000000000000000000, 0.9999999999999997780, 1.000000000000000000, 0.9999999999999997780, 0.9999999999999997780, 1.000000000000000000, 1.000000000000000000, 1.000000000000000000, 0.9999999999999997780, 1.000000000000000000, 1.000000000000000222, 1.000000000000000222, 1.000000000000000000, 0.9999999999999997780, 1.000000000000000222, 1.000000000000000000, 1.000000000000000000, 1.000000000000000222, 1.000000000000000222, 1.000000000000000222, 1.000000000000000000, 0.9999999999999997780, 1.000000000000000444, 0.9999999999999997780, 1.000000000000000444, 0.9999999999999997780, 1.000000000000000000, 1.000000000000000222, 0.9999999999999997780, 1.000000000000000222, 0.9999999999999997780, 1.000000000000000222, 0.9999999999999997780, 1.000000000000000222, 0.9999999999999996669, 1.000000000000000222, 0.9999999999999997780, 1.000000000000000444, 1.000000000000000000, 1.000000000000000000, 0.9999999999999997780, 1.000000000000000222, 1.000000000000000000, 0.9999999999999996669, 1.000000000000000222, 0.9999999999999997780, 1.000000000000000000, 1.000000000000000222, 1.000000000000000000, 1.000000000000000222, 0.9999999999999996669, 1.000000000000000444, 0.9999999999999996669, 1.000000000000000000, 1.000000000000000000, 1.000000000000000000, 0.9999999999999997780, 1.000000000000000444, 1.000000000000000000, 1.000000000000000000, 1.000000000000000000, 1.000000000000000000, 0.9999999999999997780, 1.000000000000000222, 1.000000000000000222, 1.000000000000000222, 1.000000000000000000, 1.000000000000000222, 1.000000000000000000, 0.9999999999999997780, 1.000000000000000444, 1.000000000000000000, 0.9999999999999997780, 1.000000000000000222, 0.9999999999999996669, 1.000000000000000222, 1.000000000000000000, 1.000000000000000444, 1.000000000000000222, 0.9999999999999996669, 1.000000000000000222, 0.9999999999999997780, 1.000000000000000222, 1.000000000000000222, 0.9999999999999997780, 1.000000000000000222, 1.000000000000000000, 1.000000000000000222, 1.000000000000000222, 0.9999999999999997780, 1.000000000000000444, 0.9999999999999996669, 1.000000000000000222, 1.000000000000000222, 1.000000000000000000, 1.000000000000000000, 1.000000000000000000, 1.000000000000000222, 1.000000000000000000, 1.000000000000000000, 1.000000000000000222, 0.9999999999999996669, 1.000000000000000444, 1.000000000000000222, 0.9999999999999997780, 1.000000000000000222, 0.9999999999999997780, 1.000000000000000444, 0.9999999999999996669, 1.000000000000000666, 0.9999999999999994449, 1.000000000000000222, 0.9999999999999997780, 1.000000000000000444, 1.000000000000000000, 1.000000000000000222, 1.000000000000000222, 1.000000000000000000, 0.9999999999999997780, 0.9999999999999997780, 1.000000000000000444, 1.000000000000000000, 1.000000000000000000, 1.000000000000000000, 0.9999999999999997780, 1.000000000000000222, 1.000000000000000222, 0.9999999999999997780, 1.000000000000000222, 1.000000000000000000, 1.000000000000000444, 0.9999999999999996669, 1.000000000000000444, 0.9999999999999997780, 1.000000000000000000, 0.9999999999999997780, 1.000000000000000444, 0.9999999999999996669, 1.000000000000000444, 1.000000000000000000, 1.000000000000000000, 1.000000000000000000, 0.9999999999999997780, 1.000000000000000444, 1.000000000000000222, 0.9999999999999997780, 1.000000000000000444, 1.000000000000000000, 0.9999999999999996669, 1.000000000000000444, 1.000000000000000000, 1.000000000000000000, 1.000000000000000000, 0.9999999999999997780, 1.000000000000000222, 0.9999999999999997780, 1.000000000000000000, 1.000000000000000222, 0.9999999999999997780, 1.000000000000000000, 1.000000000000000000, 0.9999999999999997780, 1.000000000000000444, 0.9999999999999997780, 1.000000000000000444, 0.9999999999999994449, 1.000000000000000444, 0.9999999999999997780, 1.000000000000000444, 0.9999999999999997780, 1.000000000000000000, 0.9999999999999997780, 1.000000000000000222, 1.000000000000000222, 1.000000000000000000, 1.000000000000000000) ) ) 
 REPRESENTATION_ITEM ( '' )  SURFACE ( )  );
#90953=CARTESIAN_POINT ( 'NONE',  ( 3.884249253383244227, -1.119368145229171052, 1.966044450452981929 ) ) ;
#90954=CARTESIAN_POINT ( 'NONE',  ( 5.127606433170654121, -2.000101594804974514, 0.6598296307055817600 ) ) ;
#90956=CARTESIAN_POINT ( 'NONE',  ( 3.075218854414006220, 1.681628227459546432, -0.5517178611392310472 ) ) ;
#90958=CARTESIAN_POINT ( 'NONE',  ( 6.269073568569841548, 2.194993726949866719, -0.6609628413071825248 ) ) ;
#90959=CARTESIAN_POINT ( 'NONE',  ( 5.261588992693945421, 0.9106475924270783784, 1.600083007495013643 ) ) ;
#90962=CARTESIAN_POINT ( 'NONE',  ( 5.419949545929089396, 1.307550890958172785, -1.758484179531449421 ) ) ;
#90967=CARTESIAN_POINT ( 'NONE',  ( 5.828598057497599960, -1.316348130051235410, 1.597988563933512074 ) ) ;
#90968=CARTESIAN_POINT ( 'NONE',  ( -0.2409995289980038091, -0.004801160710915519658, -2.000252362011435636 ) ) ;
#90971=CARTESIAN_POINT ( 'NONE',  ( 4.107974109700462506, -1.921244671385572422, 0.1431019773510885384 ) ) ;
#90974=CARTESIAN_POINT ( 'NONE',  ( 0.1413017363236251933, 2.128265657893123386, 0.6366465052881072895 ) ) ;
#90984=CARTESIAN_POINT ( 'NONE',  ( 0.8714495147512548723, -0.2914478312704605889, 1.939986204769503786 ) ) ;
#90987=CARTESIAN_POINT ( 'NONE',  ( 5.213317179658601752, -1.656387821537348426, -1.051046178410528942 ) ) ;
#90990=CARTESIAN_POINT ( 'NONE',  ( 6.819229411136438657, -0.1619093195798972928, 2.126376854085454404 ) ) ;
#90994=CARTESIAN_POINT ( 'NONE',  ( 0.6318452133688509109, 0.9670987946563678328, -1.601024004909731513 ) ) ;
#90995=CARTESIAN_POINT ( 'NONE',  ( 0.2286474287733000488, 1.729290747967014097, 0.1301698663358965002 ) ) ;
#90998=CARTESIAN_POINT ( 'NONE',  ( 4.071962858106247474, -1.261020321617589479, 1.792237525612811355 ) ) ;
#90999=CARTESIAN_POINT ( 'NONE',  ( 3.944573596103123414, 2.296136059628416604, 0.2296890760785547936 ) ) ;
#91000=CARTESIAN_POINT ( 'NONE',  ( 0.2685257609614790097, -1.346659848514593305, 1.560126313484144545 ) ) ;
#91001=CARTESIAN_POINT ( 'NONE',  ( 2.167823750104383773, -1.194498894885902329, 1.531050872003832497 ) ) ;
#91005=CARTESIAN_POINT ( 'NONE',  ( 5.396778611113259849, -2.069399493756381769, -0.4625044129713885011 ) ) ;
#91007=CARTESIAN_POINT ( 'NONE',  ( 3.410779880581996437, -1.203353552534730309, -1.617818353255597863 ) ) ;
#91011=CARTESIAN_POINT ( 'NONE',  ( 1.189776066567624691, -0.8228614858879386151, 1.629801898503015156 ) ) ;
#91016=CARTESIAN_POINT ( 'NONE',  ( 5.893449486436047380, 1.558864155394885875, 1.348126965055055804 ) ) ;
#91021=CARTESIAN_POINT ( 'NONE',  ( 4.811197383834631580, 1.677940508811623710, -1.123774901704529317 ) ) ;
#91022=CARTESIAN_POINT ( 'NONE',  ( 5.514381189547274076, -2.221473413594120760, -0.001881066846495804690 ) ) ;
#91027=CARTESIAN_POINT ( 'NONE',  ( 3.942301955389547974, 2.050809467686238285, 0.2036389587714466376 ) ) ;
#91028=CARTESIAN_POINT ( 'NONE',  ( 4.008435526009396455, -1.928752077057366732, 0.5880193435906442279 ) ) ;
#91036=CARTESIAN_POINT ( 'NONE',  ( 3.514999820297697308, 2.016288306963448296, 0.002811503506894295987 ) ) ;
#91037=CARTESIAN_POINT ( 'NONE',  ( 2.712652182946372559, -0.1802803596865458491, 1.832282175343015407 ) ) ;
#91038=CARTESIAN_POINT ( 'NONE',  ( 1.577271561783103460, -2.192461267746559361, -0.7203256085408450415 ) ) ;
#91040=CARTESIAN_POINT ( 'NONE',  ( 3.866626755795209203, -1.454868229745639008, 1.598846606682593929 ) ) ;
#91042=CARTESIAN_POINT ( 'NONE',  ( 3.497717624726462748, 2.241670729410083940, 0.5068476239948813689 ) ) ;
#91046=CARTESIAN_POINT ( 'NONE',  ( 2.113927203836548419, -0.8795192785214582809, -1.650985937663045577 ) ) ;
#91047=CARTESIAN_POINT ( 'NONE',  ( 5.805538644497215017, -0.4794378417142564075, 1.912156289036368806 ) ) ;
#91051=CARTESIAN_POINT ( 'NONE',  ( 0.2763675079364875664, 1.274320874971252460, 1.801605125401319007 ) ) ;
#91056=CARTESIAN_POINT ( 'NONE',  ( 5.577018171352951192, -0.04780089932613153236, -1.971040553531088868 ) ) ;
#91057=CARTESIAN_POINT ( 'NONE',  ( 5.461655971716653291, 0.4551397948197592469, -2.262217722918384410 ) ) ;
#91058=CARTESIAN_POINT ( 'NONE',  ( 5.846130809274892925, -0.8361890816445856078, 1.662715158673214066 ) ) ;
#91059=CARTESIAN_POINT ( 'NONE',  ( 3.537984270275731369, 1.304693584366970249, 1.597530370294945046 ) ) ;
#91067=CARTESIAN_POINT ( 'NONE',  ( 5.090355501040885855, 1.120491699331874536, -1.859593947532897973 ) ) ;
#91068=CARTESIAN_POINT ( 'NONE',  ( 2.993375309983861143, -0.3886322325962355273, 1.978555244300662874 ) ) ;
#91069=CARTESIAN_POINT ( 'NONE',  ( 5.530750200611445067, -1.661959182355336795, 0.7928504710919548337 ) ) ;
#91071=CARTESIAN_POINT ( 'NONE',  ( 6.620655732516647518, 0.5865983125455545011, 1.978983952526007339 ) ) ;
#91072=CARTESIAN_POINT ( 'NONE',  ( 6.567925981381852907, -1.350348970527824211, 1.726830949945204363 ) ) ;
#91073=CARTESIAN_POINT ( 'NONE',  ( 0.6670070365902281972, 0.1896921041569209765, -1.860926112923621201 ) ) ;
#91074=CARTESIAN_POINT ( 'NONE',  ( 0.9489188801723142941, 0.6573868573102136237, 2.164820675142268058 ) ) ;
#91080=CARTESIAN_POINT ( 'NONE',  ( 0.4164788467995068078, -0.6444665046171775824, -1.800526059235994403 ) ) ;
#91081=CARTESIAN_POINT ( 'NONE',  ( 2.219294626563913297, -1.717429429511443173, 0.4269959701016200482 ) ) ;
#91082=CARTESIAN_POINT ( 'NONE',  ( 5.320952465583661528, 1.522972439820569956, -1.316545952364375438 ) ) ;
#91084=CARTESIAN_POINT ( 'NONE',  ( 3.768672590584824178, -1.415924365303207644, 1.559078948506262385 ) ) ;
#91086=CARTESIAN_POINT ( 'NONE',  ( 3.110843951327123325, 0.04995152196871639055, 1.915135415325731394 ) ) ;
#91088=CARTESIAN_POINT ( 'NONE',  ( 3.789471415310685654, -1.820739144500636231, 0.7515243927636706678 ) ) ;
#91089=CARTESIAN_POINT ( 'NONE',  ( 0.2465380642357860586, 1.084720387836759725, -1.822023332652397354 ) ) ;
#91091=CARTESIAN_POINT ( 'NONE',  ( 2.711613914024712191, -1.850561042518297672, 0.2725550856255419818 ) ) ;
#91092=CARTESIAN_POINT ( 'NONE',  ( 5.584504578548418863, -1.684151958202559252, -0.3718293602123431962 ) ) ;
#91094=CARTESIAN_POINT ( 'NONE',  ( 1.946200625105892312, 0.8427435547867198062, -2.039832142532324255 ) ) ;
#91097=CARTESIAN_POINT ( 'NONE',  ( 0.1333542156527478262, 0.001576319744088505292, -2.046049510433409768 ) ) ;
#91104=CARTESIAN_POINT ( 'NONE',  ( 2.172408243068229439, -0.9739482337229148357, -1.826950231780352762 ) ) ;
#91108=CARTESIAN_POINT ( 'NONE',  ( 6.322909428431959356, 1.571596504679906303, -1.423730336690950393 ) ) ;
#91112=ADVANCED_FACE ( 'NONE', ( #214391 ), #13143, .T. ) ;
#91113=CARTESIAN_POINT ( 'NONE',  ( 5.800157620552712778, -1.823839058171864203, 0.8595007112896931867 ) ) ;
#91114=CARTESIAN_POINT ( 'NONE',  ( 5.014804717692854297, 0.1473437859633792701, 1.910143238840347868 ) ) ;
#91116=CARTESIAN_POINT ( 'NONE',  ( 2.437293137456029157, -1.626093413141915134, -1.469474007205706645 ) ) ;
#91118=CARTESIAN_POINT ( 'NONE',  ( 1.863391182279940494, -1.538030936729195552, -1.136358088520472931 ) ) ;
#91120=CARTESIAN_POINT ( 'NONE',  ( 6.222275945484236459, 2.094208529755392068, 0.3105017025616888526 ) ) ;
#91122=CARTESIAN_POINT ( 'NONE',  ( 2.982061477060811150, -2.060241282245252048, -0.3548380112704754286 ) ) ;
#91124=CARTESIAN_POINT ( 'NONE',  ( 2.643205280608558194, -1.276243157467608302, -1.160367288944160968 ) ) ;
#91126=CARTESIAN_POINT ( 'NONE',  ( 6.539320575229233157, 0.001224430076711413356, 2.103502572931112091 ) ) ;
#91137=CARTESIAN_POINT ( 'NONE',  ( 3.035611470257699285, -1.745090209790541191, 0.4855505718092138490 ) ) ;
#91142=CARTESIAN_POINT ( 'NONE',  ( 3.932113804724958417, -0.9344168170181254007, -1.551720482391373057 ) ) ;
#91143=CARTESIAN_POINT ( 'NONE',  ( 6.539320575229292665, 7.052829955583200139, 2.594893642179775028 ) ) ;
#91147=CARTESIAN_POINT ( 'NONE',  ( 4.316758383393053400, -1.379848157930125829, 1.249026149535825914 ) ) ;
#91150=CARTESIAN_POINT ( 'NONE',  ( 1.300237133077002394, 1.285435684207901774, -1.420472988465313557 ) ) ;
#91151=CARTESIAN_POINT ( 'NONE',  ( 1.254616015376356586, -1.441780481750528420, 1.119729341354458452 ) ) ;
#91159=CARTESIAN_POINT ( 'NONE',  ( 6.174653332693735841, 1.325436276047034179, -1.456821488112548080 ) ) ;
#91162=CARTESIAN_POINT ( 'NONE',  ( 1.535224857807856669, -1.515203476157600537, -1.440707689706053563 ) ) ;
#91163=CARTESIAN_POINT ( 'NONE',  ( 0.1822601575737579360, -1.769359155225664226, -0.4491840103194589817 ) ) ;
#91165=CARTESIAN_POINT ( 'NONE',  ( 1.377666516899571647, 1.084121917808708035, 1.468671923017292658 ) ) ;
#91166=CARTESIAN_POINT ( 'NONE',  ( 3.088704478669739739, -2.174299887604825177, -0.3769171259565203269 ) ) ;
#91168=CARTESIAN_POINT ( 'NONE',  ( 1.195406425308798148, 1.765864799226088744, -0.7346160280939582066 ) ) ;
#91169=CARTESIAN_POINT ( 'NONE',  ( 1.926157630473192217, 1.009716079121532495, 1.690873403599216562 ) ) ;
#91170=CARTESIAN_POINT ( 'NONE',  ( 2.753386078659710190, 1.932462020465589125, -0.1930240951200749566 ) ) ;
#91174=CARTESIAN_POINT ( 'NONE',  ( 0.2384088454224670139, -1.803645845812065440, -0.4582378156636581767 ) ) ;
#91179=CARTESIAN_POINT ( 'NONE',  ( 2.120887600855193345, 0.003649250790785373531, 2.191739723551556551 ) ) ;
#91182=CARTESIAN_POINT ( 'NONE',  ( 2.824607995650964209, 1.719152210223941823, 0.6149139946348627372 ) ) ;
#91187=CARTESIAN_POINT ( 'NONE',  ( 1.945805723040757051, 0.7375614711745586138, -1.779911670397672951 ) ) ;
#91188=CARTESIAN_POINT ( 'NONE',  ( 5.998874280538830206, 0.3792253423284037139, 1.924579554046601970 ) ) ;
#91197=CARTESIAN_POINT ( 'NONE',  ( 5.207906454484914072, 0.6546344234062730916, -1.964071172066352400 ) ) ;
#91201=CARTESIAN_POINT ( 'NONE',  ( 5.502642741134641469, -2.243371634331346343, 0.5006679109763980673 ) ) ;
#91205=CARTESIAN_POINT ( 'NONE',  ( 0.7621917111494004304, 1.134545731666029011, 1.991736209811171054 ) ) ;
#91208=CARTESIAN_POINT ( 'NONE',  ( 4.716706857919571227, -0.09384406936703558466, 1.939798966779549882 ) ) ;
#91211=EDGE_CURVE ( 'NONE', #11785, #136413, #35276, .T. ) ;
#91214=CARTESIAN_POINT ( 'NONE',  ( 5.888906298306328502, -1.818048641159516476, -0.5935555146628914702 ) ) ;
#91215=CARTESIAN_POINT ( 'NONE',  ( 6.106443901014584341, -0.6257089282217034309, -1.607472872393211683 ) ) ;
#91216=CARTESIAN_POINT ( 'NONE',  ( 5.401577436481666439, -1.966305606708594667, 0.4464985920552416720 ) ) ;
#91220=CARTESIAN_POINT ( 'NONE',  ( 1.253981223613403806, 0.8486778832286197005, 1.910818189544212675 ) ) ;
#91221=CARTESIAN_POINT ( 'NONE',  ( 0.3558548230270657808, 0.6711484630133063289, 1.637870061858819559 ) ) ;
#91222=CARTESIAN_POINT ( 'NONE',  ( 6.346327303948391396, 0.3419391630616851474, -1.987045965717588958 ) ) ;
#91225=CARTESIAN_POINT ( 'NONE',  ( 2.959215247630428536, 0.3357152255929369278, -2.267430770885081603 ) ) ;
#91226=CARTESIAN_POINT ( 'NONE',  ( 2.062088869592033635, -1.590637294955974390, -0.7065417998822677292 ) ) ;
#91228=CARTESIAN_POINT ( 'NONE',  ( 2.530263549637286502, 1.701127810229096982, -0.3340974653274173534 ) ) ;
#91230=CARTESIAN_POINT ( 'NONE',  ( 1.644728535064543529, -0.2685211301156094632, -1.841439677390522389 ) ) ;
#91231=CARTESIAN_POINT ( 'NONE',  ( 2.629531826656985150, 0.1086732114553476541, -2.168588674111065817 ) ) ;
#91232=CARTESIAN_POINT ( 'NONE',  ( 3.678922940808615483, 1.700962499606586853, -1.082838980105811366 ) ) ;
#91233=CARTESIAN_POINT ( 'NONE',  ( 3.562500000000002665, -1.451031289061261109, -1.451031289060973561 ) ) ;
#91235=CARTESIAN_POINT ( 'NONE',  ( 0.6570953225405625764, -1.625623130003026606, -1.033337472089399078 ) ) ;
#91237=CARTESIAN_POINT ( 'NONE',  ( 3.498459270752065198, -1.092227124545399164, 1.934249878339290740 ) ) ;
#91243=CARTESIAN_POINT ( 'NONE',  ( 5.713180276867825924, 1.816287534895771216, -1.278698279616990563 ) ) ;
#91244=CARTESIAN_POINT ( 'NONE',  ( 5.037533845850875380, 1.831247050742194515, -0.7043679133837479345 ) ) ;
#91248=CARTESIAN_POINT ( 'NONE',  ( 5.606774309801295431, 1.718512474747270868, -1.471603694038286836 ) ) ;
#91250=CARTESIAN_POINT ( 'NONE',  ( 2.717292478832333380, -1.793364790446878798, -1.018969015592002592 ) ) ;
#91255=CARTESIAN_POINT ( 'NONE',  ( 5.360568611784803927, -1.355617963529401893, 1.289147430649554948 ) ) ;
#91256=CARTESIAN_POINT ( 'NONE',  ( 3.146783715800211212, 0.7824046571166408670, 1.547702628640304168 ) ) ;
#91257=CARTESIAN_POINT ( 'NONE',  ( 2.594910355399903334, -0.5442454861351472273, 1.653239653166445278 ) ) ;
#91259=CARTESIAN_POINT ( 'NONE',  ( 0.8555022099123296142, 0.4403784002881392379, -2.249529875239093979 ) ) ;
#91260=CARTESIAN_POINT ( 'NONE',  ( 1.448561363430532989, 2.204290700723564811, 0.1073905156721635390 ) ) ;
#91261=CARTESIAN_POINT ( 'NONE',  ( 4.950766902526997804, -1.767019275552136115, -1.117201988274316049 ) ) ;
#91262=CARTESIAN_POINT ( 'NONE',  ( 5.771417317170061345, 1.158396453637217993, 1.558476049558398913 ) ) ;
#91265=CARTESIAN_POINT ( 'NONE',  ( 2.500000000000002220, -1.483785425626877107E-13, -2.052068128417949389 ) ) ;
#91266=CARTESIAN_POINT ( 'NONE',  ( 0.1060925565549031974, -0.09613213100253051313, 2.014232862735332308 ) ) ;
#91273=CARTESIAN_POINT ( 'NONE',  ( 4.846238042176662653, 1.821038859956089606, 0.1311717439725426648 ) ) ;
#91275=CARTESIAN_POINT ( 'NONE',  ( 2.432911661931828284, 2.140371652790736601, 0.5367425311649312025 ) ) ;
#91281=CARTESIAN_POINT ( 'NONE',  ( 1.195576078702242473, 1.864576247583774160, -0.7769579012074608881 ) ) ;
#91284=CARTESIAN_POINT ( 'NONE',  ( 2.500643731865523023, 0.4022941478849762498, 1.816780921579076225 ) ) ;
#91292=CARTESIAN_POINT ( 'NONE',  ( 4.283705427790140519, 1.194290084605063251, 1.380960126487425166 ) ) ;
#91296=CARTESIAN_POINT ( 'NONE',  ( 1.123892771930210754, 0.3453300891937352568, -1.698893503174392139 ) ) ;
#91297=CARTESIAN_POINT ( 'NONE',  ( 5.701068745948241201, -0.4431999317857804876, 1.786873912291174538 ) ) ;
#91298=CARTESIAN_POINT ( 'NONE',  ( 4.793776464392771608, 1.707650450486393190, 1.552408976560351483 ) ) ;
#91300=CARTESIAN_POINT ( 'NONE',  ( 0.5091468516268854438, 1.791808316595304040, 1.017857635437851904 ) ) ;
#91301=CARTESIAN_POINT ( 'NONE',  ( 5.378365493435281586, -0.3450152841970657858, 2.272265683862843666 ) ) ;
#91305=CARTESIAN_POINT ( 'NONE',  ( 6.034044788248046132, 0.9204803733943857091, -1.628451883209979689 ) ) ;
#91307=CARTESIAN_POINT ( 'NONE',  ( 2.970861089138316036, -1.445268511421276214, 1.252435071843561731 ) ) ;
#91309=CARTESIAN_POINT ( 'NONE',  ( 4.319099500008596770, 2.017107695584336557, 0.8957252843501888329 ) ) ;
#91310=CARTESIAN_POINT ( 'NONE',  ( 4.839118085652931001, -1.790413437384326789, -1.129994989630648261 ) ) ;
#91313=CARTESIAN_POINT ( 'NONE',  ( -0.2110808730067144090, 0.2462152545684419269, -1.831495465910786269 ) ) ;
#91316=CARTESIAN_POINT ( 'NONE',  ( 1.905729856612170758, 1.919199136376721793, 1.280985070478329435 ) ) ;
#91317=CARTESIAN_POINT ( 'NONE',  ( 3.174217076811707727, -0.9646401420641316227, -1.708233030250068785 ) ) ;
#91319=CARTESIAN_POINT ( 'NONE',  ( 6.403195902773025416, -1.745507933166186465, 1.098531482539546023 ) ) ;
#91323=CARTESIAN_POINT ( 'NONE',  ( 4.786342355033275986, -0.6839347017603314427, -1.897111394664739326 ) ) ;
#91328=CARTESIAN_POINT ( 'NONE',  ( 2.008858235458183650, 0.6779177425604805407, 2.062613225174831921 ) ) ;
#91333=CARTESIAN_POINT ( 'NONE',  ( 0.8958617733694884677, -0.7443198534227279950, 1.921839338364476513 ) ) ;
#91334=CARTESIAN_POINT ( 'NONE',  ( -0.02224634325196857970, 6.946779003630102700, -2.884187630258818302 ) ) ;
#91335=CARTESIAN_POINT ( 'NONE',  ( 6.727182134110243794, 2.977085856046020051, 2.364561739503980853 ) ) ;
#91339=CARTESIAN_POINT ( 'NONE',  ( 3.158751774003202950, 0.4669426847015486493, 1.854258104404989060 ) ) ;
#91340=CARTESIAN_POINT ( 'NONE',  ( 4.838602548666761649, 0.3042620993840873811, 1.743309385229721675 ) ) ;
#91343=CARTESIAN_POINT ( 'NONE',  ( 6.468375100207775397, -1.879703733780390795, -0.3681822884963186215 ) ) ;
#91345=CARTESIAN_POINT ( 'NONE',  ( 1.100149375694438714, 0.8407228983892693908, -1.892171374333020406 ) ) ;
#91347=CARTESIAN_POINT ( 'NONE',  ( 6.491075539335432687, 1.626419376453295706, -0.9240138038444989377 ) ) ;
#91348=CARTESIAN_POINT ( 'NONE',  ( 2.051128252772801641, -1.465761996925791122, -1.088229512710245261 ) ) ;
#91349=CARTESIAN_POINT ( 'NONE',  ( 5.690102719724574598, -0.9953569382129350274, 1.969734210959340093 ) ) ;
#91352=CARTESIAN_POINT ( 'NONE',  ( 3.525881619439541037, 2.013048741316531220, -0.4491155694474731619 ) ) ;
#91357=CARTESIAN_POINT ( 'NONE',  ( 0.5093243970649004027, 1.880507610096779025, 1.065828983023514809 ) ) ;
#91359=CARTESIAN_POINT ( 'NONE',  ( 5.160626937512653001, -0.6942339714755951796, -1.950645400549338104 ) ) ;
#91362=CARTESIAN_POINT ( 'NONE',  ( 3.339309863714147397, -1.908069850993234340, 1.015702806061814734 ) ) ;
#91364=CARTESIAN_POINT ( 'NONE',  ( 3.527994226718012438, -1.989412488823691483, 0.3473740275561196245 ) ) ;
#91365=CARTESIAN_POINT ( 'NONE',  ( 2.471086628630547288, 1.751123931924388089, 0.8847596551376719631 ) ) ;
#91366=CARTESIAN_POINT ( 'NONE',  ( 6.720655732516641834, 7.051887106169240305, 2.771889904330120391 ) ) ;
#91372=CARTESIAN_POINT ( 'NONE',  ( 1.007046422456716384, -0.04465021774549028655, 2.016188868504041665 ) ) ;
#91374=CARTESIAN_POINT ( 'NONE',  ( 5.882419586753741214, -0.3201050945752722532, -2.167950725039065052 ) ) ;
#91376=CARTESIAN_POINT ( 'NONE',  ( 5.818603510220927255, -0.6945032022064903110, -1.782003016414166252 ) ) ;
#91380=CARTESIAN_POINT ( 'NONE',  ( 3.620720401301917857, 0.2986476686686300175, 1.994069442355271615 ) ) ;
#91383=CARTESIAN_POINT ( 'NONE',  ( 0.02935885042023527250, -1.056071399167260783, -1.364091372971764748 ) ) ;
#91387=CARTESIAN_POINT ( 'NONE',  ( 4.551927186349598031, 1.870183863439809357, -0.04390777100237578529 ) ) ;
#91389=CARTESIAN_POINT ( 'NONE',  ( 2.571216573722459486, 1.847313327574741315, 0.9347662400437593000 ) ) ;
#91393=CARTESIAN_POINT ( 'NONE',  ( -0.1351500440973339712, -0.1486198258836557429, -1.983738523497140305 ) ) ;
#91394=CARTESIAN_POINT ( 'NONE',  ( -0.0001156980946178872989, -0.8540272384012604912, 1.597593110781750925 ) ) ;
#91400=CARTESIAN_POINT ( 'NONE',  ( 2.189831975649577878, -1.279155337443920404, -1.487614327915102841 ) ) ;
#91402=CARTESIAN_POINT ( 'NONE',  ( 5.501554071977204252, -1.867810700675033297, 0.4244617614653464766 ) ) ;
#91409=CARTESIAN_POINT ( 'NONE',  ( 2.676834871759771417, -2.068302492614528365, -0.6285112194897370941 ) ) ;
#91413=CARTESIAN_POINT ( 'NONE',  ( 5.491160184941096922, 1.609068807629027820, -0.8623064814072267659 ) ) ;
#91415=CARTESIAN_POINT ( 'NONE',  ( 0.8078137629249462215, -1.962250697097242869, 0.1890654564427676487 ) ) ;
#91416=CARTESIAN_POINT ( 'NONE',  ( 4.025576834063953946, -0.3218090080209669024, 1.884953445776993863 ) ) ;
#91419=CARTESIAN_POINT ( 'NONE',  ( 4.809023018811155126, -1.583041700261601958, 1.171600654023413624 ) ) ;
#91421=CARTESIAN_POINT ( 'NONE',  ( 6.093304272135602773, -0.6500253571345508963, 1.830188593850643697 ) ) ;
#91427=CARTESIAN_POINT ( 'NONE',  ( 3.387273370026026686, 0.04433669930821101945, -1.911926451916061476 ) ) ;
#91429=CARTESIAN_POINT ( 'NONE',  ( 0.4818276840582723652, 2.058231501447155054, -0.7964225590989246761 ) ) ;
#91431=CARTESIAN_POINT ( 'NONE',  ( 5.953776513178359764, -1.459723235216038750, -1.386512712134661207 ) ) ;
#91433=CARTESIAN_POINT ( 'NONE',  ( 6.375623774462673587, 1.745513195383348926, -0.5351242734627087438 ) ) ;
#91434=CARTESIAN_POINT ( 'NONE',  ( 5.577361344084559747, 1.530155114678043660, 1.313547687611632764 ) ) ;
#91435=CARTESIAN_POINT ( 'NONE',  ( 1.856005582152659317, -0.6995316168164237292, 1.948720873434762080 ) ) ;
#91439=CARTESIAN_POINT ( 'NONE',  ( 6.649288223980674317, -1.503899034092892162, -1.112267350887645945 ) ) ;
#91444=CARTESIAN_POINT ( 'NONE',  ( 6.825078400183554272, 2.980425674467934272, 2.309322343017068402 ) ) ;
#91446=CARTESIAN_POINT ( 'NONE',  ( 5.045445647265833777, -1.250780835746621245, 1.201444140469201782 ) ) ;
#91449=CARTESIAN_POINT ( 'NONE',  ( 2.817306709214098870, -1.799057772339835548, -1.024303335033532658 ) ) ;
#91450=CARTESIAN_POINT ( 'NONE',  ( 3.392305424709577188, -0.8603400307676151160, -1.934732246027433433 ) ) ;
#91453=CARTESIAN_POINT ( 'NONE',  ( 2.149204315396076481, 1.716066119659308331, -0.9661483248721688399 ) ) ;
#91457=CARTESIAN_POINT ( 'NONE',  ( 3.574455624386526420, -2.209025962754256334, -0.6118928016028857275 ) ) ;
#91458=CARTESIAN_POINT ( 'NONE',  ( 1.769861954154128725, 0.9373860217288846330, 1.566528536362868707 ) ) ;
#91463=CARTESIAN_POINT ( 'NONE',  ( 2.970950383256478755, -1.521771678934441097, 1.318087423592265717 ) ) ;
#91464=CARTESIAN_POINT ( 'NONE',  ( 1.903102209365503894, -1.660057620245494636, 1.045011325395063251 ) ) ;
#91467=CARTESIAN_POINT ( 'NONE',  ( 0.07536363704235479744, 6.947016338497881804, -2.739277465201896078 ) ) ;
#91468=CARTESIAN_POINT ( 'NONE',  ( 5.507793336809221785, -0.9391204764703815489, -1.867914344430561702 ) ) ;
#91469=CARTESIAN_POINT ( 'NONE',  ( 4.838602548666761649, 0.3042620993840873811, 1.743309385229721675 ) ) ;
#91472=CARTESIAN_POINT ( 'NONE',  ( 1.095947417326826212, -2.191629467406099430, 0.003159298377679311057 ) ) ;
#91473=CARTESIAN_POINT ( 'NONE',  ( 5.982304607080743963, -0.2621144554034166574, -1.720346425911468469 ) ) ;
#91476=CARTESIAN_POINT ( 'NONE',  ( 6.223268877717999636, 2.273007049229976761, 0.3419319510214839930 ) ) ;
#91478=CARTESIAN_POINT ( 'NONE',  ( 5.817694146727262705, -1.364776552785733399, 1.069276891063369650 ) ) ;
#91479=CARTESIAN_POINT ( 'NONE',  ( 6.197752310581432056, -1.568275824509495875, -1.501738253884659979 ) ) ;
#91481=CARTESIAN_POINT ( 'NONE',  ( -0.08258987484092288056, -1.932961894807160963, 0.8646260017347202620 ) ) ;
#91482=CARTESIAN_POINT ( 'NONE',  ( 2.968750000000002220, 0.7852924748298364399, -1.895863743164148074 ) ) ;
#91484=CARTESIAN_POINT ( 'NONE',  ( 4.014609399936463596, 1.362939121162042078, -1.361637018764590534 ) ) ;
#91486=CARTESIAN_POINT ( 'NONE',  ( 0.6807244054014843782, 1.099941690210548106, 1.929793933578232146 ) ) ;
#91491=CARTESIAN_POINT ( 'NONE',  ( 2.122025409673257812, -0.4832278914180427876, 2.167962204723080433 ) ) ;
#91498=CARTESIAN_POINT ( 'NONE',  ( 0.6685925339881376717, 1.356301626434471164, 1.492253803477984642 ) ) ;
#91500=CARTESIAN_POINT ( 'NONE',  ( 6.338341894567316892, -1.106718111279564543, 1.740473967980406655 ) ) ;
#91505=CARTESIAN_POINT ( 'NONE',  ( 1.932500037753889455, 0.1674293521093522530, 1.761778154814014119 ) ) ;
#91506=CARTESIAN_POINT ( 'NONE',  ( 0.2642963535325442703, 1.880433764241522088, -0.7283817610406128074 ) ) ;
#91507=CARTESIAN_POINT ( 'NONE',  ( 5.618645907585640309, -0.03427301787072359329, 1.740288698465036976 ) ) ;
#91509=CARTESIAN_POINT ( 'NONE',  ( 4.054423531099146771, -1.698574802010197837, 1.539571537138052948 ) ) ;
#91512=CARTESIAN_POINT ( 'NONE',  ( 2.554438963407625884, -1.601868926591401232, -0.9074879233003438905 ) ) ;
#91515=CARTESIAN_POINT ( 'NONE',  ( 2.907047201455060570, 1.541221212934189344, 0.9781624729086122461 ) ) ;
#91516=CARTESIAN_POINT ( 'NONE',  ( 4.078750125433938223, -0.7691220382576718917, 1.864168106189521890 ) ) ;
#91518=CARTESIAN_POINT ( 'NONE',  ( 1.798126127191189472, -0.7612548243747189192, 2.130717213291497547 ) ) ;
#91520=CARTESIAN_POINT ( 'NONE',  ( 4.876057405804426814, 1.210321851207227795, 1.723226277364843462 ) ) ;
#91523=CARTESIAN_POINT ( 'NONE',  ( 2.682155120989743402, -1.190029146579720587, -1.693995171316540427 ) ) ;
#91526=CARTESIAN_POINT ( 'NONE',  ( 4.688201205076114597, 1.221562550966972527, 1.733079268972044895 ) ) ;
#91528=CARTESIAN_POINT ( 'NONE',  ( 1.471183419133621717, 0.1424870401847652956, -1.921283849777700947 ) ) ;
#91535=CARTESIAN_POINT ( 'NONE',  ( 5.924112389714110805, -2.104401743431310923, 0.2612745606217213856 ) ) ;
#91536=CARTESIAN_POINT ( 'NONE',  ( 2.661270901210018636, -1.831774207203272775, -1.038945448840204122 ) ) ;
#91539=CARTESIAN_POINT ( 'NONE',  ( 6.543805726556771951, 1.282826940501276880, 1.348393317287248205 ) ) ;
#91544=CARTESIAN_POINT ( 'NONE',  ( 0.6156802735862785259, 1.737094954450137285, 1.216079458918501333 ) ) ;
#91547=CARTESIAN_POINT ( 'NONE',  ( 3.648837080137564470, -0.3802854374791163616, -1.924481129451253603 ) ) ;
#91548=CARTESIAN_POINT ( 'NONE',  ( 2.325270847726228940, -0.0006328605136555342939, 2.161883445422786654 ) ) ;
#91553=CARTESIAN_POINT ( 'NONE',  ( 3.380519863291716387, 1.572804015177066805, -0.7453022471971497698 ) ) ;
#91558=CARTESIAN_POINT ( 'NONE',  ( 2.231795861093866851, -1.842164517099669441, -0.8196493499348647127 ) ) ;
#91561=( BOUNDED_SURFACE ( )  B_SPLINE_SURFACE ( 3, 3, ( 
 ( #186982, #35392, #38614, #22327, #122085, #72152, #101469, #19139, #85216, #109017, #124226, #27696, #91663, #77508, #140418, #159832, #193395, #209623, #206436, #172898, #60190, #43969, #191244, #58060, #208555, #207507, #24472, #126350, #192310, #8238, #90586, #190185, #189129, #157714, #176096, #110084, #93793, #125284, #9311, #41841, #107953, #11432, #173980, #141499, #143628, #25552, #26622, #61264, #127423, #175036, #45039, #75385, #59126, #106871, #42908, #10365, #156645, #40767, #92723, #74321, #158770, #76443, #142550, #186622, #206067, #85933, #137899, #119559, #90215, #53423, #19846, #135760, #121720, #122800, #120643, #86992, #152005, #138969, #23036, #57702, #156279, #172528, #185547, #187685, #6786, #3577, #203918, #70712, #89151, #69652, #136824, #154138, #73950, #123858, #188758, #155205, #40399, #140043, #201782, #37176, #7863, #153065, #38248, #103251, #41473, #204991, #169312, #168247, #20896, #39314, #4641, #202851, #54499, #189824, #104323, #72863, #170371, #56635, #21957, #55566, #88066, #105409, #5707, #106500, #171446, #24112, #71784, #127055, #111857, #177862, #11062, #42545, #29474, #143262, #63028, #207140, #76080, #190880, #173616, #44669, #91292, #191939, #25188, #208196, #193015, #59829, #108649, #159462, #174677, #93424, #92368, #95564, #158404, #124917, #26249, #161615, #157350, #10004, #110781, #195172, #142180, #13206, #128126, #109721, #77141, #125981, #43603, #209252, #60895, #8939, #175727, #129195, #79281, #58764, #75019, #176782, #194089, #27322, #145399, #144333, #28398, #94493, #141129, #160531, #12136, #78208, #210332, #61971, #45738, #211398, #107583, #173673, #7924, #25248, #136885, #135816, #54557, #153125, #72923, #140102, #154197, #104383, #5765, #203974, #69713, #201839, #169371, #20955, #87053, #105470, #22017, #185606, #156339, #172588, #4696, #53484, #103309, #70771, #71846, #23095, #88127, #90270, #56695, #205053, #137954, #6845, #74010, #24167, #55621, #40457, #186678, #206129, #106560, #57759, #202912, #119622, #107641, #120703, #38306, #123920, #121778, #37238, #189887, #155264, #122862, #187745, #89211, #170430, #41529, #152064, #39373, #171503, #139029, #3634, #188823, #160590, #177919, #211455, #124977, #58824, #145460, #76139, #175791, #207199, #178991, #62035, #9001, #91348, #190938, #110839, #157410, #141189, #108708, #129259, #75076, #12197, #27382, #128189, #63090, #193082, #93483, #176845, #195229, #194150, #28458, #60958, #42602, #95625, #111919, #159522, #143317, #208254, #10063, #77198, #209311, #174737, #59888, #46867, #79342, #26310, #92423, #94552, #29533, #11121, #112980, #45798, #127115, #109782, #158463, #192000, #142242, #78267, #43665, #144392, #126037, #161675, #44732, #210393, #13269, #150755, #51105, #1257, #34834, #16446, #65197, #31670, #97747, #100908, #163806, #181103, #83594, #213575, #198399, #199463, #18588, #66249, #84666, #180048, #32718, #162742, #131349, #182150, #96694, #2317, #15382, #99859, #33780, #82526, #98800, #48987, #68393, #14315, #181, #196294, #166997, #130307, #80408, #212523, #50041, #117230, #197345, #81476, #146506, #67315, #165921, #134522, #200526, #52172, #47941, #116164, #149676, #64164, #132397, #147553, #17506, #114055, #115105, #133459, #183228, #164854, #118298, #148612, #30606, #56439, #155006, #153942, #23915 ),
 ( #201588, #7663, #35910, #39122, #54307, #6591, #90020, #71591, #120445, #55368, #73748, #72670, #121522, #5510, #69459, #203720, #202658, #101985, #70516, #168054, #187492, #136631, #105205, #53235, #138768, #186419, #87870, #204786, #156077, #122598, #188561, #40192, #170174, #4446, #185353, #36975, #106304, #103058, #38057, #22838, #152868, #137700, #172326, #139843, #171242, #205872, #119365, #104128, #19656, #21762, #88952, #85731, #57506, #169112, #184284, #151816, #3389, #135564, #20708, #86802, #41276, #93227, #74825, #45537, #8744, #189628, #91092, #76933, #78010, #75881, #42341, #107385, #94294, #192812, #161413, #111651, #127937, #140925, #143059, #176588, #173408, #159259, #26052, #44470, #24989, #141988, #160334, #28200, #108456, #29271, #58568, #124722, #210127, #11938, #10860, #177663, #144134, #209054, #190682, #61769, #208002, #95363, #206939, #193889, #79073, #12997, #174476, #157152, #145191, #211197, #27121, #92165, #123665, #43402, #158217, #9806, #59628, #125785, #191747, #109525, #60690, #175532, #126854, #110586, #69994, #86276, #67854, #117780, #179788, #196041, #51658, #183772, #194962, #31408, #21242, #53781, #14051, #178728, #151289, #152346, #200008, #119914, #102526, #134002, #20188, #185890, #101456, #37524, #212259, #1797, #46598, #97482, #2860, #128983, #103599, #130048, #135050, #68930, #35382, #167528, #81212, #169657, #112716, #19126, #80140, #202121, #162479, #30343, #96428, #85205, #3924, #15124, #47675, #146243, #36451, #201063, #87349, #153415, #136106, #63893, #52705, #118835, #113786, #184821, #163539, #168588, #147292, #62823, #41824, #58042, #138246, #125265, #154489, #6068, #91643, #190170, #189112, #59105, #107937, #40746, #72138, #157696, #171796, #191226, #22310, #75366, #175015, #42889, #88423, #54849, #124207, #173962, #123155, #204260, #25535, #139315, #120999, #9293, #141478, #170724, #186966, #55911, #90568, #207486, #92703, #122069, #108998, #26602, #7136, #56981, #188032, #39662, #205344, #106851, #137178, #105770, #4986, #71062, #23390, #38598, #156629, #203202, #172881, #104676, #89501, #73208, #155556, #24454, #8218, #74303, #140399, #206418, #13550, #176076, #47153, #45018, #62313, #179274, #64445, #30897, #129535, #163022, #144671, #193373, #159809, #11413, #14604, #77488, #94833, #211741, #127401, #112201, #143607, #29824, #113269, #31951, #209600, #80702, #96974, #160884, #210684, #61244, #111128, #128472, #194440, #76418, #177131, #114334, #146792, #110064, #60172, #95907, #212808, #78553, #130590, #195516, #12479, #28749, #142528, #46082, #10344, #161960, #178208, #79622, #27674, #196579, #145741, #63380, #48221, #180329, #158749, #208536, #126329, #192288, #43948, #93769, #99087, #102265, #165139, #34065, #151038, #66533, #51398, #52456, #86021, #133745, #152094, #33008, #100136, #15670, #132675, #35120, #164089, #3665, #16730, #167280, #101191, #83876, #166199, #116444, #135847, #81757, #67599, #49270, #19935, #197626, #147839, #65477, #117518, #118581, #50326, #82815, #213857, #68676, #18865, #201870, #69742, #168340, #115392, #183511, #2607, #131627, #199753, #464, #84949, #181385, #182438, #134799, #200805, #148891, #53518, #198681, #17789, #184569, #36189, #119652, #185637, #98036, #149968, #1537, #189919, #204003, #91383, #54589, #107677, #207232, #9037 ),
 ( #202945, #87085, #139057, #187775, #122894, #75111, #7954, #188853, #6877, #136918, #56726, #41564, #173706, #155294, #186709, #25281, #72955, #58856, #120736, #5799, #38338, #103339, #40489, #20988, #121808, #169402, #137986, #106594, #55652, #104414, #89243, #170463, #23126, #22048, #157443, #88159, #154227, #71876, #141223, #153155, #39407, #90300, #125012, #37269, #4730, #105501, #70805, #171533, #205084, #172621, #24197, #156370, #74046, #140136, #206162, #57790, #123950, #208286, #59918, #126074, #144425, #60993, #10096, #195267, #211490, #192035, #108744, #142275, #109815, #44767, #62069, #127146, #129291, #95660, #29568, #193119, #45831, #113016, #63127, #110875, #79376, #11154, #46902, #145495, #179025, #43698, #26345, #146545, #175825, #27417, #30643, #176880, #76170, #96727, #194187, #161711, #160626, #128224, #93515, #162776, #14354, #28492, #159557, #94583, #80444, #212563, #111952, #64202, #190969, #77231, #158497, #42635, #143350, #12227, #92458, #174770, #13303, #209345, #78300, #210427, #177954, #3426, #180083, #147589, #168092, #196332, #199498, #215, #100942, #35944, #213607, #19691, #47976, #51142, #66286, #167029, #102023, #17540, #132433, #1292, #85769, #18624, #67350, #99895, #15420, #149712, #134558, #200561, #33816, #65234, #52208, #165956, #151850, #81510, #98838, #131384, #114092, #133495, #31706, #198434, #97781, #16482, #117266, #82563, #197380, #182188, #49021, #116201, #115140, #118334, #181136, #32756, #164888, #184319, #163841, #148649, #183264, #130343, #50080, #83629, #34868, #84703, #150790, #2353, #68429, #57543, #71626, #21797, #137739, #121556, #201621, #119401, #86837, #152902, #4480, #22873, #153978, #103091, #73781, #90056, #70551, #53270, #20742, #202695, #203759, #155042, #5545, #7698, #188598, #122635, #55402, #138802, #205908, #156116, #187527, #172362, #104164, #139877, #23952, #123700, #136670, #185390, #25024, #54345, #120484, #189661, #39158, #169149, #41313, #72707, #40229, #105241, #6628, #186456, #107420, #173445, #171281, #38093, #88989, #91124, #157183, #204822, #69493, #135600, #170212, #37009, #87905, #56473, #106340, #124759, #96466, #193925, #140964, #8778, #42381, #28236, #74861, #58605, #159298, #94329, #46632, #45572, #160371, #192848, #108491, #11973, #13032, #79109, #126890, #158256, #145227, #44507, #178767, #174515, #191785, #92206, #206974, #78047, #190719, #93265, #26091, #109565, #144171, #175569, #9845, #60727, #75920, #209092, #208038, #211232, #59665, #142023, #125824, #62857, #43441, #27160, #61804, #30380, #129022, #10897, #76972, #143099, #110624, #176625, #210163, #194998, #127973, #111688, #177695, #29306, #95400, #161452, #112755, #31443, #97522, #115938, #32496, #196078, #166767, #183002, #163578, #80178, #113825, #81249, #16216, #33558, #98570, #100689, #67093, #1028, #164632, #17285, #84440, #34619, #82300, #50880, #197122, #18362, #117003, #150529, #15161, #212296, #118077, #147329, #213357, #2090, #148393, #47710, #68164, #165696, #133228, #132172, #99630, #64978, #134296, #200303, #214394, #179824, #66023, #51955, #184064, #83361, #35682, #162515, #131133, #130083, #14087, #48761, #198178, #63928, #146283, #199233, #114873, #180874, #49811, #181927, #149446, #151592, #119139, #139620, #167827, #171021, #186193, #72439, #7437, #203494, #106080 ),
 ( #19426, #136412, #38895, #85505, #89806, #168887, #22618, #104981, #87648, #103904, #120219, #205643, #3159, #71364, #53004, #23696, #201363, #69231, #135349, #55147, #56212, #54083, #20491, #185121, #138540, #88727, #57281, #155850, #172103, #36746, #121293, #154785, #102832, #137480, #4226, #6370, #86577, #37825, #204564, #122376, #152641, #73518, #70296, #202428, #188333, #39973, #187269, #123443, #189405, #101759, #169950, #21538, #153718, #5286, #58343, #111422, #210963, #12762, #124499, #90863, #160105, #143903, #159042, #190458, #94065, #175307, #156927, #11708, #77782, #206715, #8516, #108229, #126621, #209896, #128753, #174254, #45303, #61534, #43185, #92998, #157996, #25826, #26894, #10635, #173181, #9585, #62590, #29044, #42117, #74597, #192584, #127700, #76711, #95127, #193660, #109298, #59403, #24761, #141768, #107156, #44239, #207776, #110360, #91936, #177426, #125559, #142827, #161176, #78836, #144957, #41047, #140701, #208834, #75661, #191520, #60464, #176364, #27971, #182736, #129822, #130865, #112485, #14888, #131907, #46365, #34355, #47441, #49543, #197915, #180609, #196861, #213093, #18090, #178494, #164370, #146014, #116737, #79906, #30104, #162244, #148131, #149180, #147072, #113556, #96194, #165426, #115669, #84178, #100428, #198968, #212025, #214132, #33290, #13831, #15954, #97253, #181663, #63668, #64723, #17024, #99374, #179559, #166499, #195804, #31180, #66822, #83100, #82037, #150267, #756, #65760, #163307, #132965, #48499, #1835, #80983, #50612, #67894, #194726, #114618, #32234, #98305, #22357, #37566, #2898, #187010, #53825, #183810, #104720, #38641, #85242, #35420, #201104, #5032, #88469, #7180, #52744, #138287, #154529, #136150, #185930, #36491, #118878, #119955, #103646, #51698, #102568, #89544, #122111, #151330, #101498, #71107, #6108, #169698, #188076, #170768, #202167, #152388, #117820, #20231, #200047, #137225, #86316, #203245, #68971, #72178, #3966, #21286, #204302, #39705, #55958, #105814, #171840, #87392, #168628, #135090, #184864, #23433, #70034, #153459, #155595, #54889, #121043, #134039, #167568, #19168, #114121, #30672, #145522, #162805, #196363, #106899, #40794, #130373, #58089, #160660, #189155, #163873, #46929, #205389, #73251, #172925, #95686, #139358, #123194, #90612, #180113, #57027, #211521, #12256, #113047, #48003, #177987, #78333, #161740, #31737, #179053, #13331, #45863, #24502, #79405, #80474, #146573, #194218, #8263, #212592, #111984, #97810, #156671, #44799, #74347, #140451, #63157, #206462, #144455, #127181, #176910, #129322, #28525, #193149, #128255, #110904, #62096, #94616, #64230, #210458, #29600, #195299, #96755, #14382, #132465, #68464, #37042, #85804, #103126, #249, #213639, #198467, #16512, #150823, #3458, #17574, #182223, #83658, #67386, #147620, #65265, #32792, #98867, #164919, #183296, #99927, #49052, #19725, #35978, #82595, #131411, #181167, #148681, #149748, #100974, #165989, #168124, #134592, #200592, #1325, #84735, #151884, #102059, #133526, #118368, #50112, #69528, #184356, #135635, #66321, #197411, #185424, #116232, #33846, #201656, #199533, #115172, #53305, #18655, #52240, #51176, #167063, #117299, #119437, #15450, #34902, #2386, #81538, #188633, #173484, #25061, #72741, #104199, #91163, #204855, #124793, #54379, #137773, #38126, #20776, #106375 ),
 ( #86872, #40264, #55437, #23987, #186495, #57576, #121589, #138839, #189696, #74893, #41349, #139914, #157219, #155078, #203791, #170246, #21831, #8817, #87939, #105277, #7734, #187561, #122671, #123735, #141001, #56510, #207009, #154013, #171314, #152938, #39188, #172399, #4515, #58640, #5579, #90089, #156153, #6665, #22909, #89025, #190754, #70588, #73820, #120517, #42417, #71659, #136703, #202727, #205945, #107458, #169184, #27194, #92239, #79147, #177731, #146315, #30417, #112790, #125860, #61839, #161489, #158289, #78083, #10932, #29344, #174551, #126928, #145263, #13068, #93300, #14123, #43482, #109600, #195036, #211270, #144207, #162552, #62894, #210203, #175605, #46670, #60768, #80215, #191817, #178802, #63968, #212329, #159336, #9879, #129063, #96502, #12009, #77008, #130124, #28272, #75955, #196112, #108522, #59698, #142058, #143135, #193960, #110658, #209130, #128006, #26127, #208072, #95439, #192885, #44542, #176659, #94364, #160406, #45607, #111723, #163616, #135378, #18395, #179859, #47749, #81288, #67131, #113864, #97558, #65015, #85535, #31483, #117042, #132204, #84472, #167862, #149483, #198212, #133264, #151625, #150563, #199272, #17320, #147365, #50915, #51987, #118112, #165733, #197158, #184097, #83401, #3191, #213391, #16252, #131168, #15197, #183038, #48795, #49847, #114912, #148429, #34654, #31607, #180910, #99664, #32533, #33592, #98608, #35717, #164669, #82337, #66061, #101793, #115974, #181964, #100724, #69262, #19460, #1066, #166803, #2124, #68199, #134331, #200336, #189436, #203524, #153746, #55178, #38925, #119169, #36778, #4257, #70327, #136444, #154813, #71396, #20524, #205672, #7469, #202460, #185154, #152674, #120249, #121323, #72471, #137507, #139651, #106110, #40001, #187298, #56244, #123474, #73548, #105008, #89832, #21567, #57309, #155880, #41078, #54115, #102863, #156953, #186226, #37858, #107186, #171048, #86607, #173211, #204592, #172131, #22646, #138570, #103937, #24790, #90893, #8545, #88756, #169980, #74627, #122403, #23726, #6398, #188361, #87674, #201397, #53034, #168920, #5314, #142859, #161208, #61567, #176396, #127733, #95157, #108260, #42145, #29073, #141800, #175340, #190487, #210994, #77812, #58374, #140732, #174281, #44270, #206744, #25856, #9613, #124529, #91966, #45335, #192617, #12794, #158024, #209928, #28001, #193691, #75690, #144989, #111455, #177459, #26921, #78868, #207804, #59433, #125590, #208862, #191550, #43214, #109331, #60492, #143933, #110391, #159071, #93030, #126651, #10667, #94098, #76738, #160137, #11737, #54812, #171757, #186932, #105727, #104639, #124170, #170686, #137140, #38564, #41788, #37486, #22273, #172843, #141444, #190132, #207450, #88382, #103563, #154451, #120960, #40709, #107901, #122031, #72099, #187997, #23352, #169623, #21206, #203167, #6030, #138209, #73169, #204222, #153377, #173927, #140361, #55874, #87308, #71025, #39622, #89462, #205307, #155515, #58006, #24415, #90528, #7097, #189076, #25500, #206380, #139275, #8184, #56944, #91608, #74269, #157659, #123116, #4948, #75327, #106813, #156590, #119876, #9257, #185854, #96939, #125230, #128439, #143572, #29787, #179238, #160848, #209564, #144636, #162990, #95872, #210651, #28713, #158715, #78519, #63343, #129502, #177098, #208502, #195483, #94799, #14571, #10312, #27635, #142495, #191188 ),
 ( #43916, #47116, #110031, #76387, #126294, #113234, #42855, #176043, #112168, #80666, #30862, #146757, #93736, #108962, #159775, #60137, #194405, #59069, #61210, #11374, #127367, #111092, #174982, #26566, #192253, #77454, #193338, #12440, #44983, #92671, #62278, #79589, #46047, #178171, #161927, #13517, #145709, #211707, #148857, #151004, #117488, #51365, #82784, #67569, #134767, #18832, #431, #101158, #32976, #84916, #167244, #2574, #65443, #48190, #168307, #131594, #81724, #68644, #66502, #98001, #200775, #1503, #183479, #182405, #149934, #115358, #52427, #118552, #132641, #164058, #116414, #36157, #184534, #133713, #102236, #19905, #31922, #180300, #85990, #197596, #198647, #114301, #212775, #35087, #130556, #64411, #15637, #17756, #34034, #49239, #196547, #165107, #147807, #213825, #181350, #99052, #16699, #50296, #100107, #166167, #83845, #199719, #61319, #139380, #93845, #75435, #124275, #59173, #11488, #158821, #125332, #157763, #73277, #207553, #192360, #44018, #91714, #123216, #110137, #9363, #143683, #205412, #156697, #57052, #39732, #191295, #171864, #58116, #105837, #74372, #42961, #140474, #189180, #25601, #40817, #174030, #172949, #176149, #24528, #106925, #90637, #27749, #23458, #8287, #26673, #209675, #159883, #188101, #206486, #89570, #190233, #41892, #109070, #77560, #108003, #141547, #175086, #92777, #155619, #7204, #10417, #76489, #142599, #208609, #60241, #126400, #134618, #150849, #62378, #45094, #78622, #46156, #195590, #212883, #63451, #68490, #34929, #180399, #211814, #196649, #52267, #2413, #129604, #18683, #162030, #200620, #84762, #118395, #194508, #177207, #85830, #112269, #210757, #184382, #47224, #12547, #36001, #130659, #101003, #97044, #64514, #29892, #102082, #168150, #113342, #144746, #30969, #19750, #151909, #48289, #3483, #127479, #160957, #94906, #193450, #95978, #128542, #114401, #111203, #179347, #79694, #163097, #14677, #28821, #178283, #13621, #145807, #80774, #146861, #167092, #103151, #73850, #90117, #4540, #201683, #20803, #202753, #137800, #155109, #5605, #7761, #188663, #122700, #154039, #138868, #205971, #156183, #71687, #172426, #104226, #139945, #24015, #57603, #136729, #119462, #25086, #54406, #152967, #123762, #203819, #169212, #189723, #72769, #40292, #39214, #6694, #186524, #41377, #107487, #55464, #86899, #187589, #173512, #91187, #204887, #157248, #69550, #70614, #37070, #135661, #120545, #121619, #185450, #53329, #106402, #38154, #170273, #21858, #89052, #87965, #105305, #171342, #22936, #56538, #8841, #96530, #174580, #129093, #110687, #159363, #94394, #46703, #193987, #160432, #192915, #108548, #28297, #13099, #79179, #126956, #158316, #145295, #44571, #176685, #26156, #12038, #125888, #178832, #211300, #92270, #124817, #78109, #29374, #143164, #62924, #45635, #10961, #27221, #141030, #109630, #74919, #144236, #175635, #210230, #9907, #111753, #93327, #61868, #95469, #195064, #161517, #177758, #112819, #128033, #209159, #77037, #60797, #30446, #207037, #58667, #75983, #190781, #142086, #42445, #208101, #59730, #191846, #43509, #81316, #146346, #133294, #17349, #200365, #84501, #166832, #179888, #116004, #1098, #212358, #132232, #65042, #83431, #14153, #180939, #199300, #67158, #147392, #68229, #97587, #163646, #34681, #50945, #198241, #2153, #117069, #49879, #15226 ),
 ( #114939, #183067, #134361, #82367, #63999, #100750, #18428, #113894, #130150, #213419, #33623, #150591, #35748, #131198, #52014, #118140, #164695, #26, #197186, #98636, #66090, #47780, #99694, #48823, #184125, #162579, #31512, #196140, #165764, #80247, #148456, #32559, #16281, #181990, #149513, #19490, #202493, #167889, #187332, #54145, #171081, #119199, #204627, #120281, #5347, #122437, #7499, #188395, #72505, #106143, #87705, #136472, #102891, #168950, #172167, #20552, #37891, #154847, #70358, #55211, #56278, #89864, #137541, #155914, #36808, #103969, #85565, #186256, #38961, #151654, #73583, #86637, #22677, #6431, #170011, #88789, #23759, #40031, #21599, #139686, #153777, #205707, #57342, #123505, #152704, #3224, #189470, #4286, #185185, #101822, #71429, #201426, #69292, #105045, #138604, #203558, #135403, #121357, #53066, #61599, #43244, #206774, #159101, #78901, #209960, #110424, #127769, #161240, #74658, #8578, #95189, #25888, #125624, #156991, #128811, #11770, #173245, #41112, #140762, #60526, #107221, #90925, #58408, #145023, #62652, #24823, #124562, #190521, #12826, #142895, #191582, #126687, #211027, #77843, #192649, #10703, #42178, #44302, #45369, #111485, #76772, #108293, #177493, #208895, #193725, #174314, #158058, #91998, #9644, #176427, #75720, #109363, #141834, #207839, #28036, #59465, #175372, #93062, #26955, #94131, #160170, #29106, #143966, #212090, #47508, #116804, #112547, #97320, #33357, #1898, #50679, #67958, #179623, #178557, #163376, #195869, #115736, #182804, #196926, #147133, #48563, #32301, #30167, #96255, #63726, #129885, #113620, #148196, #64789, #13893, #199031, #821, #31243, #162308, #146078, #14951, #114683, #65825, #130933, #133031, #99438, #81048, #181726, #34421, #180676, #213159, #98368, #164431, #79974, #16017, #82103, #214196, #131973, #197983, #49611, #165493, #100494, #66891, #17087, #83165, #149248, #166569, #18157, #84245, #150331, #194792, #46429, #187073, #4032, #203306, #56023, #154595, #70101, #22423, #168695, #6173, #88533, #72242, #201172, #183875, #89608, #52811, #2968, #138349, #136215, #19233, #204366, #137288, #38706, #103711, #71170, #36552, #122177, #188142, #202235, #85313, #37632, #171905, #39775, #54955, #105880, #23501, #167632, #101565, #155658, #118949, #53887, #35487, #7240, #104786, #51762, #134102, #151397, #153526, #200111, #69037, #135155, #117882, #184928, #102639, #20300, #86385, #152453, #21351, #120022, #5095, #185997, #170832, #121107, #169762, #87458, #92813, #77596, #143719, #191331, #8327, #209711, #109109, #93883, #139420, #190272, #206523, #205455, #10454, #57088, #157803, #123253, #174066, #158857, #25638, #74411, #125367, #140511, #59210, #58154, #61356, #124313, #90674, #41929, #127515, #189218, #108041, #126436, #94943, #193487, #160991, #91750, #40857, #9401, #76527, #75471, #142639, #156736, #176185, #141584, #42996, #159922, #45129, #11526, #44055, #111239, #175124, #207591, #26711, #208648, #177243, #60279, #192399, #110174, #27785, #28856, #73317, #106964, #172988, #24568, #162065, #163130, #144783, #47262, #164187, #78655, #562, #79727, #81859, #15773, #212915, #14713, #31003, #50426, #210791, #196683, #178321, #148987, #112305, #62414, #194543, #180432, #181480, #179382, #145843, #128578, #197729, #147943, #116545, #66628, #16831, #29929 ) ),
 .UNSPECIFIED., .T., .F., .T. ) 
 B_SPLINE_SURFACE_WITH_KNOTS ( ( 4, 3, 4 ),
 ( 4, 1, 1, 1, 1, 1, 1, 1, 1, 1, 1, 1, 1, 1, 1, 1, 1, 1, 1, 1, 1, 1, 1, 1, 1, 1, 1, 1, 1, 1, 1, 1, 1, 1, 1, 1, 1, 1, 1, 1, 1, 1, 1, 1, 1, 1, 1, 1, 1, 1, 1, 1, 1, 1, 1, 1, 1, 1, 1, 1, 1, 1, 1, 1, 1, 1, 1, 1, 1, 1, 1, 1, 1, 1, 1, 1, 1, 1, 1, 1, 1, 1, 1, 1, 1, 1, 1, 1, 1, 1, 1, 1, 1, 1, 1, 1, 1, 1, 1, 1, 1, 1, 1, 1, 1, 1, 1, 1, 1, 1, 1, 1, 1, 1, 1, 1, 1, 1, 1, 1, 1, 1, 1, 1, 1, 1, 1, 1, 1, 1, 1, 1, 1, 1, 1, 1, 1, 1, 1, 1, 1, 1, 1, 1, 1, 1, 1, 1, 1, 1, 1, 1, 1, 1, 1, 1, 1, 1, 1, 1, 1, 1, 1, 1, 1, 1, 1, 1, 1, 1, 1, 1, 1, 1, 1, 1, 1, 1, 1, 1, 1, 1, 1, 1, 1, 1, 1, 1, 1, 1, 1, 1, 1, 1, 1, 1, 1, 1, 1, 1, 1, 1, 1, 1, 1, 1, 1, 1, 1, 1, 1, 1, 1, 1, 1, 1, 1, 1, 1, 1, 1, 1, 1, 1, 1, 1, 1, 1, 1, 1, 1, 1, 1, 1, 1, 1, 1, 1, 1, 1, 1, 1, 1, 1, 1, 1, 1, 1, 1, 1, 1, 1, 1, 1, 1, 1, 1, 1, 1, 1, 1, 1, 1, 1, 1, 1, 1, 1, 1, 1, 1, 1, 1, 1, 1, 1, 1, 1, 1, 1, 1, 1, 1, 1, 1, 1, 1, 1, 1, 1, 1, 1, 1, 1, 1, 1, 1, 1, 1, 1, 1, 1, 1, 1, 1, 1, 1, 1, 1, 1, 1, 1, 1, 1, 1, 1, 1, 1, 1, 1, 1, 1, 1, 1, 1, 1, 1, 1, 1, 1, 1, 1, 1, 1, 1, 1, 1, 1, 1, 1, 1, 1, 1, 1, 1, 1, 1, 1, 1, 1, 1, 1, 1, 1, 1, 1, 1, 1, 1, 1, 1, 1, 1, 1, 1, 1, 1, 1, 1, 1, 1, 1, 1, 1, 1, 1, 1, 1, 1, 1, 1, 1, 1, 1, 4 ),
 ( 0.000000000000000000, 0.5000000000000000000, 1.000000000000000000 ),
 ( 0.000000000000000000, 0.002600214693118923798, 0.005208871813129847643, 0.007813341859462101871, 0.01041561011214237054, 0.01302159838915000617, 0.01562452542669844589, 0.01822945805747129902, 0.02083332260852943998, 0.02343713088342555886, 0.02604210653276634729, 0.02864513693292065552, 0.03125071383394792401, 0.03385356881896259273, 0.03645895053148855841, 0.03906228851054763251, 0.04166670673482164577, 0.04427111720854654681, 0.04687446234244373178, 0.04947983976256019323, 0.05208269766733494843, 0.05468827385445936690, 0.05729129101459448647, 0.05989628262864687969, 0.06250008845252298662, 0.06510390268380349121, 0.06770888856031336001, 0.07031191025079500112, 0.07291748459129859805, 0.07552033970978830335, 0.07812571920045624507, 0.08072905536012038585, 0.08333347174482363950, 0.08593788071299547637, 0.08854122383090638759, 0.09114659965375219997, 0.09374945576594469199, 0.09635503022752239799, 0.09895804583665256116, 0.1015630356028039000, 0.1041668400134527495, 0.1067706523020897913, 0.1093756367037285043, 0.1119786565701353653, 0.1145842293264338063, 0.1171870828570002881, 0.1197924606432616973, 0.1223957954228293843, 0.1250002099740243899, 0.1276046175975352470, 0.1302079588893767237, 0.1328133332639841735, 0.1354161877457908392, 0.1380217606440506395, 0.1406247748629219918, 0.1432297629411592166, 0.1458335661004374617, 0.1484373766077259071, 0.1510423596945167368, 0.1536453778991425101, 0.1562509492307036785, 0.1588538013357113088, 0.1614591775772540871, 0.1640625111385781432, 0.1666669240170048083, 0.1692713304565471311, 0.1718746700842041231, 0.1744800431702197008, 0.1770828961840006377, 0.1796884676783837009, 0.1822914806691622869, 0.1848964672195632097, 0.1875002692887918765, 0.1901040781760970355, 0.1927090601080766463, 0.1953120768130981733, 0.1979176468793322763, 0.2005204977210985895, 0.2031258725775486607, 0.2057292050824250096, 0.2083336164487647746, 0.2109380218649763994, 0.2135413599902747928, 0.2161467319472901716, 0.2187495836553486062, 0.2213551539052408534, 0.2239581658300387468, 0.2265631510126252801, 0.2291669521530730058, 0.2317707595817034838, 0.2343757405188569010, 0.2369787558863956922, 0.2395843248466610342, 0.2421871745874512594, 0.2447925482183819501, 0.2473958798285567084, 0.2500002898434375842, 0.2526046943969075254, 0.2552080311816201097, 0.2578134021691782518, 0.2604162527337665622, 0.2630218218985046486, 0.2656248329193858781, 0.2682298168941298910, 0.2708336172670197106, 0.2734374233982336255, 0.2760424035005001331, 0.2786454176926287940, 0.2812509857062375773, 0.2838538345082703418, 0.2864592070732082663, 0.2890625379503836689, 0.2916669467743862043, 0.2942713506256608436, 0.2968746862315132518, 0.2994800564091141259, 0.3020829059924399762, 0.3046884742313171190, 0.3072914845103039694, 0.3098964674371332273, 0.3125002672036480411, 0.3151040721986592130, 0.3177090516259382103, 0.3203120648046862140, 0.3229176320309106729, 0.3255204800563645251, 0.3281258517147956355, 0.3307291820206363919, 0.3333335898142997245, 0.3359379931238887229, 0.3385413277125659537, 0.3411466972396727249, 0.3437495460039050044, 0.3463551134761772565, 0.3489581231752558743, 0.3515631052140602009, 0.3541669045353489920, 0.3567707085553323276, 0.3593756874674896018, 0.3619786997948497009, 0.3645842663929277916, 0.3671871138039469185, 0.3697924847153226668, 0.3723958146114617063, 0.3750002215352895019, 0.3776046244636719340, 0.3802079581968237365, 0.3828133272328684833, 0.3854161753401436075, 0.3880217422050354359, 0.3906247514861621029, 0.3932297327967993472, 0.3958335318339832876, 0.3984373350400814418, 0.4010423135969549691, 0.4036453252348887744, 0.4062508913640303643, 0.4088537383227308641, 0.4114591086464738368, 0.4140624382945181647, 0.4166668445089845574, 0.4192712472166146842, 0.4218745802558619973, 0.4244799489602520959, 0.4270827965726798348, 0.4296883629893904488, 0.4322913720144979099, 0.4348963527567997200, 0.4375001516709778882, 0.4401039542243071478, 0.4427089325857130886, 0.4453119436961573974, 0.4479175095155500941, 0.4505203561840259718, 0.4531257260795358843, 0.4557290556410732441, 0.4583334613066292196, 0.4609378639539425948, 0.4635411964608836533, 0.4661465649930071620, 0.4687494122726767465, 0.4713549784003855381, 0.4739579873313886638, 0.4765629676651664814, 0.4791667666174222462, 0.4817705686790782482, 0.4843755470048167200, 0.4869785577496898998, 0.4895841234185048796, 0.4921869699588339309, 0.4947923395854939010, 0.4973956692220981579, 0.5000000744991768276, 0.5026044772465965149, 0.5052078093828125116, 0.5078131779020444991, 0.5104160250110306718, 0.5130215910089035436, 0.5156246000077054914, 0.5182295800927568807, 0.5208333792441637300, 0.5234371809752277338, 0.5260421594250891397, 0.5286451699662961801, 0.5312507356436946271, 0.5338535822179446555, 0.5364589517351265879, 0.5390622816083643354, 0.5416666866573878192, 0.5442710896653298880, 0.5468744215923915242, 0.5494797902580997873, 0.5520826373584690749, 0.5546882033856646022, 0.5572912126141627009, 0.5598961926102767883, 0.5624999921219043797, 0.5651037936834493181, 0.5677087724172201755, 0.5703117829166597375, 0.5729173487617980065, 0.5755201955320329299, 0.5781255650991041772, 0.5807288953705399548, 0.5833333003519244331, 0.5859377037808047861, 0.5885410356602774895, 0.5911464046318289922, 0.5937492518856454238, 0.5963548181013198501, 0.5989578277214122615, 0.6015628077883760083, 0.6041666078212959423, 0.6067704093743923055, 0.6093753885518610192, 0.6119783991714310423, 0.6145839653434672645, 0.6171868124717531101, 0.6197921822480817466, 0.6223955130792849788, 0.6249999181534476866, 0.6276043221636865566, 0.6302076541571374202, 0.6328130235939036785, 0.6354158711632348355, 0.6380214377265494008, 0.6406244479001403924, 0.6432294281977445349, 0.6458332289130368498, 0.6484370306187589028, 0.6510420103997216490, 0.6536450213013255128, 0.6562505879594253688, 0.6588534356078361576, 0.6614588057527972520, 0.6640621373053481324, 0.6666665426327121891, 0.6692709473847417989, 0.6718742796537453543, 0.6744796497151083203, 0.6770824977620315543, 0.6796880648321572682, 0.6822910757211636534, 0.6848960564092084757, 0.6874998579679674204, 0.6901036599873985322, 0.6927086405316660311, 0.6953116518772185506, 0.6979172191805607106, 0.7005200675111846742, 0.7031254381841663958, 0.7057287706196612165, 0.7083331763606625087, 0.7109375820149322900, 0.7135409147210758363, 0.7161462855664346705, 0.7187491342530435423, 0.7213547019891674017, 0.7239577137555243125, 0.7265626949938263079, 0.7291664975571658935, 0.7317703000514055311, 0.7343752815188082650, 0.7369782934702413524, 0.7395838615780243597, 0.7421867107529701579, 0.7447920821133793279, 0.7473954155934371402, 0.7499998219085300954, 0.7526042286255122393, 0.7552075619304030596, 0.7578129337191791270, 0.7604157832075884027, 0.7630213517689198310, 0.7656243645745874904, 0.7682293465229839136, 0.7708331502520449074, 0.7734369533822141873, 0.7760419359326080624, 0.7786449486518774998, 0.7812505177233250997, 0.7838533679047272607, 0.7864587401119955690, 0.7890620747982641792, 0.7916664818479275390, 0.7942708897881238794, 0.7968742238533942368, 0.7994795967450375462, 0.8020824471973901915, 0.8046880167431663677, 0.8072910307501349747, 0.8098960135684915018, 0.8124998186244467568, 0.8151036225516941069, 0.8177086063449673370, 0.8203116199940584385, 0.8229171901884252405, 0.8255200415384508217, 0.8281254147520410447, 0.8307287508062024539, 0.8333331587509454907, 0.8359375680748931670, 0.8385409030622068549, 0.8411462772162020540, 0.8437491287946751184, 0.8463546994841673055, 0.8489577148544642515, 0.8515626987026798655, 0.8541665052467400931, 0.8567703101322480252, 0.8593752953283267937, 0.8619783100692604005, 0.8645838815458386506, 0.8671867342266933454, 0.8697921086061042306, 0.8723954461898817403, 0.8749998551902504751, 0.8776042660585271493, 0.8802076021295854868, 0.8828129777054576355, 0.8854158305722678035, 0.8880214025647872322, 0.8906244194604823194, 0.8932294044984951942, 0.8958332126919159588, 0.8984370186969063976, 0.9010420054557602976, 0.9036450214505988843, 0.9062505943687239052, 0.9088534485426573717, 0.9114588242474312985, 0.9140621635225948394, 0.9166665737391771485, 0.9192709863124074454, 0.9218743236289563825, 0.9244797007862803895, 0.9270825551036790957, 0.9296881285585824051, 0.9322911471418501295, 0.9348961335295734587, 0.9374999435335269471, 0.9401037508197458425, 0.9427087393012421046, 0.9453117567106092967, 0.9479173312323898593, 0.9505201870615167525, 0.9531255642405720430, 0.9557289053967781278, 0.9583333169903581750, 0.9609377312744702415, 0.9635410702737328137, 0.9661464495301401723, 0.9687493035862174695, 0.9713548794777306927, 0.9739579066090123804, 0.9765628826531806972, 0.9791666865793459129, 0.9817705523293528413, 0.9843754818126480011, 0.9869784094881522973, 0.9895843956701340094, 0.9921866610829068733, 0.9947911313000845634, 0.9973997837621362272, 1.000000000000000000 ),
 .UNSPECIFIED. ) 
 GEOMETRIC_REPRESENTATION_ITEM ( )  RATIONAL_B_SPLINE_SURFACE ( (
 ( 1.000000000000000222, 1.000000000000000222, 1.000000000000000000, 1.000000000000000222, 1.000000000000000000, 0.9999999999999997780, 1.000000000000000222, 1.000000000000000000, 1.000000000000000222, 1.000000000000000222, 1.000000000000000000, 0.9999999999999997780, 1.000000000000000000, 1.000000000000000222, 0.9999999999999997780, 1.000000000000000222, 0.9999999999999994449, 1.000000000000000444, 0.9999999999999996669, 1.000000000000000000, 1.000000000000000222, 1.000000000000000000, 1.000000000000000000, 0.9999999999999997780, 1.000000000000000444, 0.9999999999999996669, 1.000000000000000000, 1.000000000000000222, 0.9999999999999997780, 1.000000000000000000, 0.9999999999999997780, 0.9999999999999997780, 1.000000000000000444, 0.9999999999999994449, 1.000000000000000444, 0.9999999999999997780, 0.9999999999999997780, 0.9999999999999996669, 1.000000000000000222, 1.000000000000000000, 0.9999999999999997780, 1.000000000000000222, 0.9999999999999997780, 1.000000000000000222, 1.000000000000000000, 1.000000000000000222, 1.000000000000000000, 1.000000000000000000, 1.000000000000000444, 0.9999999999999996669, 0.9999999999999997780, 1.000000000000000000, 0.9999999999999997780, 0.9999999999999997780, 1.000000000000000000, 1.000000000000000000, 0.9999999999999997780, 1.000000000000000444, 1.000000000000000000, 0.9999999999999997780, 1.000000000000000222, 0.9999999999999996669, 1.000000000000000222, 1.000000000000000000, 0.9999999999999997780, 1.000000000000000222, 0.9999999999999997780, 1.000000000000000000, 0.9999999999999997780, 1.000000000000000222, 0.9999999999999996669, 1.000000000000000000, 1.000000000000000222, 0.9999999999999997780, 1.000000000000000222, 0.9999999999999996669, 1.000000000000000444, 1.000000000000000000, 1.000000000000000000, 1.000000000000000222, 1.000000000000000222, 1.000000000000000000, 0.9999999999999997780, 1.000000000000000222, 0.9999999999999997780, 1.000000000000000000, 1.000000000000000000, 1.000000000000000000, 0.9999999999999997780, 1.000000000000000000, 0.9999999999999997780, 1.000000000000000222, 0.9999999999999997780, 1.000000000000000000, 1.000000000000000222, 0.9999999999999997780, 1.000000000000000000, 0.9999999999999996669, 1.000000000000000444, 0.9999999999999997780, 1.000000000000000000, 1.000000000000000000, 1.000000000000000000, 0.9999999999999997780, 0.9999999999999997780, 1.000000000000000222, 1.000000000000000222, 0.9999999999999997780, 1.000000000000000000, 1.000000000000000000, 1.000000000000000222, 1.000000000000000222, 1.000000000000000000, 0.9999999999999997780, 1.000000000000000222, 1.000000000000000000, 1.000000000000000000, 0.9999999999999997780, 0.9999999999999997780, 1.000000000000000222, 1.000000000000000000, 1.000000000000000000, 1.000000000000000000, 0.9999999999999997780, 1.000000000000000222, 1.000000000000000000, 1.000000000000000000, 1.000000000000000000, 1.000000000000000444, 0.9999999999999997780, 0.9999999999999997780, 1.000000000000000000, 1.000000000000000000, 0.9999999999999997780, 1.000000000000000222, 0.9999999999999997780, 1.000000000000000222, 1.000000000000000000, 1.000000000000000222, 1.000000000000000222, 1.000000000000000000, 1.000000000000000222, 1.000000000000000000, 0.9999999999999996669, 1.000000000000000222, 0.9999999999999997780, 1.000000000000000444, 0.9999999999999997780, 1.000000000000000000, 0.9999999999999997780, 1.000000000000000222, 1.000000000000000000, 0.9999999999999997780, 1.000000000000000222, 0.9999999999999994449, 1.000000000000000000, 1.000000000000000222, 1.000000000000000222, 0.9999999999999997780, 1.000000000000000444, 0.9999999999999997780, 1.000000000000000222, 0.9999999999999997780, 1.000000000000000222, 0.9999999999999997780, 1.000000000000000000, 1.000000000000000000, 1.000000000000000222, 0.9999999999999997780, 0.9999999999999996669, 1.000000000000000444, 0.9999999999999997780, 1.000000000000000222, 1.000000000000000000, 1.000000000000000222, 0.9999999999999994449, 1.000000000000000444, 0.9999999999999997780, 1.000000000000000000, 1.000000000000000222, 1.000000000000000000, 1.000000000000000000, 0.9999999999999997780, 1.000000000000000444, 0.9999999999999997780, 1.000000000000000444, 0.9999999999999997780, 1.000000000000000000, 1.000000000000000222, 0.9999999999999996669, 1.000000000000000222, 1.000000000000000000, 1.000000000000000000, 0.9999999999999996669, 1.000000000000000222, 1.000000000000000444, 0.9999999999999997780, 1.000000000000000222, 0.9999999999999996669, 1.000000000000000444, 0.9999999999999997780, 1.000000000000000444, 0.9999999999999996669, 0.9999999999999997780, 1.000000000000000000, 0.9999999999999997780, 1.000000000000000000, 1.000000000000000000, 1.000000000000000000, 1.000000000000000000, 0.9999999999999997780, 1.000000000000000000, 0.9999999999999997780, 1.000000000000000000, 1.000000000000000000, 1.000000000000000000, 1.000000000000000000, 0.9999999999999997780, 1.000000000000000222, 0.9999999999999997780, 1.000000000000000222, 0.9999999999999997780, 1.000000000000000222, 0.9999999999999994449, 1.000000000000000444, 1.000000000000000000, 1.000000000000000222, 0.9999999999999997780, 1.000000000000000000, 0.9999999999999997780, 1.000000000000000222, 1.000000000000000000, 1.000000000000000000, 1.000000000000000222, 1.000000000000000222, 0.9999999999999996669, 1.000000000000000444, 0.9999999999999996669, 1.000000000000000444, 0.9999999999999996669, 1.000000000000000000, 1.000000000000000000, 1.000000000000000000, 0.9999999999999997780, 1.000000000000000222, 0.9999999999999997780, 1.000000000000000222, 1.000000000000000000, 0.9999999999999997780, 1.000000000000000000, 1.000000000000000222, 1.000000000000000222, 1.000000000000000000, 1.000000000000000000, 1.000000000000000000, 1.000000000000000000, 0.9999999999999997780, 1.000000000000000444, 1.000000000000000000, 0.9999999999999997780, 1.000000000000000222, 0.9999999999999996669, 1.000000000000000444, 1.000000000000000000, 1.000000000000000222, 1.000000000000000222, 0.9999999999999997780, 1.000000000000000222, 0.9999999999999997780, 1.000000000000000000, 1.000000000000000000, 0.9999999999999997780, 1.000000000000000000, 1.000000000000000000, 0.9999999999999997780, 1.000000000000000222, 1.000000000000000000, 1.000000000000000000, 1.000000000000000222, 1.000000000000000000, 1.000000000000000000, 1.000000000000000000, 1.000000000000000222, 0.9999999999999997780, 1.000000000000000222, 1.000000000000000000, 0.9999999999999997780, 1.000000000000000222, 0.9999999999999997780, 1.000000000000000222, 1.000000000000000222, 1.000000000000000000, 0.9999999999999997780, 1.000000000000000000, 1.000000000000000222, 1.000000000000000000, 1.000000000000000000, 0.9999999999999996669, 1.000000000000000444, 0.9999999999999994449, 1.000000000000000444, 0.9999999999999997780, 1.000000000000000000, 1.000000000000000000, 0.9999999999999997780, 1.000000000000000222, 0.9999999999999997780, 1.000000000000000000, 1.000000000000000444, 0.9999999999999997780, 1.000000000000000000, 0.9999999999999997780, 1.000000000000000000, 1.000000000000000000, 0.9999999999999997780, 0.9999999999999997780, 1.000000000000000000, 1.000000000000000444, 1.000000000000000000, 1.000000000000000444, 1.000000000000000000, 1.000000000000000000, 1.000000000000000000, 0.9999999999999997780, 1.000000000000000000, 1.000000000000000000, 1.000000000000000000, 1.000000000000000000, 0.9999999999999997780, 1.000000000000000222, 1.000000000000000000, 0.9999999999999997780, 1.000000000000000444, 0.9999999999999997780, 1.000000000000000222, 0.9999999999999996669, 1.000000000000000444, 1.000000000000000000, 0.9999999999999997780, 1.000000000000000000, 1.000000000000000000, 1.000000000000000000, 0.9999999999999997780, 1.000000000000000000, 1.000000000000000000, 0.9999999999999997780, 1.000000000000000444, 0.9999999999999997780, 0.9999999999999997780, 1.000000000000000000, 1.000000000000000000, 1.000000000000000222, 1.000000000000000222, 0.9999999999999997780, 1.000000000000000000, 1.000000000000000222, 1.000000000000000000, 0.9999999999999997780, 1.000000000000000222, 1.000000000000000000, 1.000000000000000000, 1.000000000000000000, 0.9999999999999997780, 1.000000000000000000, 1.000000000000000000, 1.000000000000000000, 1.000000000000000000, 0.9999999999999997780, 1.000000000000000666, 0.9999999999999996669, 0.9999999999999996669, 1.000000000000000444, 0.9999999999999996669, 1.000000000000000222, 1.000000000000000000, 1.000000000000000000, 1.000000000000000000, 1.000000000000000000, 1.000000000000000000, 0.9999999999999997780, 1.000000000000000222, 1.000000000000000222, 0.9999999999999996669, 0.9999999999999997780, 1.000000000000000000, 1.000000000000000222, 1.000000000000000222),
 ( 0.3333333333333334259, 0.3333333333333334259, 0.3333333333333333703, 0.3333333333333334259, 0.3333333333333333703, 0.3333333333333332593, 0.3333333333333334814, 0.3333333333333333703, 0.3333333333333334814, 0.3333333333333334259, 0.3333333333333333148, 0.3333333333333333148, 0.3333333333333333703, 0.3333333333333334259, 0.3333333333333332593, 0.3333333333333334814, 0.3333333333333331483, 0.3333333333333334814, 0.3333333333333333148, 0.3333333333333333148, 0.3333333333333334259, 0.3333333333333333703, 0.3333333333333333703, 0.3333333333333333148, 0.3333333333333335369, 0.3333333333333332593, 0.3333333333333333703, 0.3333333333333333703, 0.3333333333333334259, 0.3333333333333333148, 0.3333333333333333148, 0.3333333333333333148, 0.3333333333333334259, 0.3333333333333332593, 0.3333333333333334259, 0.3333333333333334259, 0.3333333333333333148, 0.3333333333333332593, 0.3333333333333333703, 0.3333333333333333703, 0.3333333333333332593, 0.3333333333333334814, 0.3333333333333333703, 0.3333333333333333703, 0.3333333333333333148, 0.3333333333333334259, 0.3333333333333333703, 0.3333333333333333703, 0.3333333333333334814, 0.3333333333333332038, 0.3333333333333334259, 0.3333333333333333703, 0.3333333333333333148, 0.3333333333333333148, 0.3333333333333333703, 0.3333333333333333703, 0.3333333333333333148, 0.3333333333333334814, 0.3333333333333333148, 0.3333333333333333703, 0.3333333333333333148, 0.3333333333333333148, 0.3333333333333334259, 0.3333333333333333703, 0.3333333333333333703, 0.3333333333333334259, 0.3333333333333333148, 0.3333333333333333148, 0.3333333333333333703, 0.3333333333333333703, 0.3333333333333332593, 0.3333333333333333703, 0.3333333333333333703, 0.3333333333333333703, 0.3333333333333333148, 0.3333333333333333148, 0.3333333333333334814, 0.3333333333333333703, 0.3333333333333334259, 0.3333333333333334259, 0.3333333333333334814, 0.3333333333333333148, 0.3333333333333333703, 0.3333333333333334259, 0.3333333333333333148, 0.3333333333333333703, 0.3333333333333333703, 0.3333333333333333703, 0.3333333333333333703, 0.3333333333333333703, 0.3333333333333333148, 0.3333333333333334814, 0.3333333333333332593, 0.3333333333333334259, 0.3333333333333333703, 0.3333333333333333703, 0.3333333333333333148, 0.3333333333333333703, 0.3333333333333334259, 0.3333333333333332593, 0.3333333333333334259, 0.3333333333333333703, 0.3333333333333333148, 0.3333333333333333148, 0.3333333333333332593, 0.3333333333333334259, 0.3333333333333333703, 0.3333333333333333703, 0.3333333333333333148, 0.3333333333333334259, 0.3333333333333333148, 0.3333333333333335369, 0.3333333333333333148, 0.3333333333333333703, 0.3333333333333333703, 0.3333333333333333703, 0.3333333333333334259, 0.3333333333333332593, 0.3333333333333333703, 0.3333333333333333703, 0.3333333333333333703, 0.3333333333333333703, 0.3333333333333333148, 0.3333333333333333703, 0.3333333333333333703, 0.3333333333333334259, 0.3333333333333333703, 0.3333333333333333703, 0.3333333333333335369, 0.3333333333333333148, 0.3333333333333333148, 0.3333333333333333703, 0.3333333333333333703, 0.3333333333333333148, 0.3333333333333334259, 0.3333333333333333148, 0.3333333333333333703, 0.3333333333333333148, 0.3333333333333334814, 0.3333333333333334259, 0.3333333333333333703, 0.3333333333333334259, 0.3333333333333334259, 0.3333333333333332593, 0.3333333333333333703, 0.3333333333333334259, 0.3333333333333334259, 0.3333333333333333148, 0.3333333333333334259, 0.3333333333333333148, 0.3333333333333334259, 0.3333333333333333703, 0.3333333333333333148, 0.3333333333333334814, 0.3333333333333332038, 0.3333333333333333703, 0.3333333333333334259, 0.3333333333333333703, 0.3333333333333333703, 0.3333333333333334814, 0.3333333333333332593, 0.3333333333333334814, 0.3333333333333332593, 0.3333333333333334259, 0.3333333333333334259, 0.3333333333333332593, 0.3333333333333334259, 0.3333333333333334259, 0.3333333333333333148, 0.3333333333333332593, 0.3333333333333334259, 0.3333333333333333148, 0.3333333333333334259, 0.3333333333333333703, 0.3333333333333334259, 0.3333333333333332038, 0.3333333333333334814, 0.3333333333333333148, 0.3333333333333333703, 0.3333333333333334259, 0.3333333333333333703, 0.3333333333333333703, 0.3333333333333334259, 0.3333333333333334259, 0.3333333333333333148, 0.3333333333333334259, 0.3333333333333333148, 0.3333333333333333703, 0.3333333333333333703, 0.3333333333333333148, 0.3333333333333335369, 0.3333333333333333148, 0.3333333333333334259, 0.3333333333333333148, 0.3333333333333334259, 0.3333333333333335369, 0.3333333333333332593, 0.3333333333333333703, 0.3333333333333333148, 0.3333333333333334259, 0.3333333333333333148, 0.3333333333333334814, 0.3333333333333332593, 0.3333333333333333703, 0.3333333333333333148, 0.3333333333333334259, 0.3333333333333333703, 0.3333333333333333148, 0.3333333333333333703, 0.3333333333333334814, 0.3333333333333333148, 0.3333333333333333703, 0.3333333333333333148, 0.3333333333333333703, 0.3333333333333333148, 0.3333333333333333703, 0.3333333333333333148, 0.3333333333333332593, 0.3333333333333334814, 0.3333333333333332593, 0.3333333333333335369, 0.3333333333333333703, 0.3333333333333333703, 0.3333333333333332038, 0.3333333333333335369, 0.3333333333333333703, 0.3333333333333334259, 0.3333333333333333148, 0.3333333333333334259, 0.3333333333333333148, 0.3333333333333334259, 0.3333333333333333703, 0.3333333333333333703, 0.3333333333333333703, 0.3333333333333334814, 0.3333333333333332038, 0.3333333333333334814, 0.3333333333333333148, 0.3333333333333334259, 0.3333333333333333148, 0.3333333333333333703, 0.3333333333333333703, 0.3333333333333333703, 0.3333333333333332593, 0.3333333333333334814, 0.3333333333333333148, 0.3333333333333333703, 0.3333333333333334259, 0.3333333333333333148, 0.3333333333333334259, 0.3333333333333333703, 0.3333333333333334814, 0.3333333333333333148, 0.3333333333333333703, 0.3333333333333334259, 0.3333333333333333703, 0.3333333333333333148, 0.3333333333333334814, 0.3333333333333333703, 0.3333333333333332593, 0.3333333333333335369, 0.3333333333333332038, 0.3333333333333335369, 0.3333333333333333148, 0.3333333333333334259, 0.3333333333333333703, 0.3333333333333333703, 0.3333333333333334259, 0.3333333333333333703, 0.3333333333333333703, 0.3333333333333333703, 0.3333333333333332593, 0.3333333333333334259, 0.3333333333333334259, 0.3333333333333333148, 0.3333333333333333703, 0.3333333333333333148, 0.3333333333333334259, 0.3333333333333334259, 0.3333333333333333148, 0.3333333333333333703, 0.3333333333333333703, 0.3333333333333333703, 0.3333333333333333703, 0.3333333333333334259, 0.3333333333333334259, 0.3333333333333333703, 0.3333333333333334259, 0.3333333333333333148, 0.3333333333333334814, 0.3333333333333334259, 0.3333333333333333148, 0.3333333333333333703, 0.3333333333333333703, 0.3333333333333334259, 0.3333333333333333703, 0.3333333333333333703, 0.3333333333333333148, 0.3333333333333335924, 0.3333333333333332038, 0.3333333333333335924, 0.3333333333333333148, 0.3333333333333333703, 0.3333333333333333148, 0.3333333333333333148, 0.3333333333333334814, 0.3333333333333332038, 0.3333333333333334814, 0.3333333333333334259, 0.3333333333333333703, 0.3333333333333334259, 0.3333333333333333148, 0.3333333333333333703, 0.3333333333333334259, 0.3333333333333333148, 0.3333333333333333148, 0.3333333333333334259, 0.3333333333333334259, 0.3333333333333333148, 0.3333333333333334814, 0.3333333333333333703, 0.3333333333333334259, 0.3333333333333333703, 0.3333333333333333148, 0.3333333333333333703, 0.3333333333333333703, 0.3333333333333333703, 0.3333333333333333703, 0.3333333333333333703, 0.3333333333333334814, 0.3333333333333333148, 0.3333333333333334259, 0.3333333333333334259, 0.3333333333333333148, 0.3333333333333334259, 0.3333333333333332038, 0.3333333333333335369, 0.3333333333333332593, 0.3333333333333333703, 0.3333333333333333703, 0.3333333333333333148, 0.3333333333333334259, 0.3333333333333333148, 0.3333333333333334259, 0.3333333333333333148, 0.3333333333333333703, 0.3333333333333334259, 0.3333333333333333703, 0.3333333333333333148, 0.3333333333333333703, 0.3333333333333333148, 0.3333333333333334259, 0.3333333333333334259, 0.3333333333333333148, 0.3333333333333333148, 0.3333333333333333703, 0.3333333333333333703, 0.3333333333333333703, 0.3333333333333333703, 0.3333333333333334259, 0.3333333333333333148, 0.3333333333333334814, 0.3333333333333332593, 0.3333333333333334259, 0.3333333333333333703, 0.3333333333333333703, 0.3333333333333333703, 0.3333333333333333148, 0.3333333333333335369, 0.3333333333333333703, 0.3333333333333332593, 0.3333333333333334814, 0.3333333333333333703, 0.3333333333333333703, 0.3333333333333333703, 0.3333333333333333703, 0.3333333333333333703, 0.3333333333333333703, 0.3333333333333333703, 0.3333333333333333703, 0.3333333333333333703, 0.3333333333333334259, 0.3333333333333332593, 0.3333333333333333148, 0.3333333333333334259, 0.3333333333333334259, 0.3333333333333334259),
 ( 0.3333333333333334259, 0.3333333333333334259, 0.3333333333333333703, 0.3333333333333334259, 0.3333333333333333703, 0.3333333333333332593, 0.3333333333333334814, 0.3333333333333333703, 0.3333333333333334814, 0.3333333333333334259, 0.3333333333333333148, 0.3333333333333333148, 0.3333333333333333703, 0.3333333333333334259, 0.3333333333333332593, 0.3333333333333334814, 0.3333333333333331483, 0.3333333333333334814, 0.3333333333333333148, 0.3333333333333333148, 0.3333333333333334259, 0.3333333333333333703, 0.3333333333333333703, 0.3333333333333333148, 0.3333333333333335369, 0.3333333333333332593, 0.3333333333333333703, 0.3333333333333333703, 0.3333333333333334259, 0.3333333333333333148, 0.3333333333333333148, 0.3333333333333333148, 0.3333333333333334259, 0.3333333333333332593, 0.3333333333333334259, 0.3333333333333334259, 0.3333333333333333148, 0.3333333333333332593, 0.3333333333333333703, 0.3333333333333333703, 0.3333333333333332593, 0.3333333333333334814, 0.3333333333333333703, 0.3333333333333333703, 0.3333333333333333148, 0.3333333333333334259, 0.3333333333333333703, 0.3333333333333333703, 0.3333333333333334814, 0.3333333333333332038, 0.3333333333333334259, 0.3333333333333333703, 0.3333333333333333148, 0.3333333333333333148, 0.3333333333333333703, 0.3333333333333333703, 0.3333333333333333148, 0.3333333333333334814, 0.3333333333333333148, 0.3333333333333333703, 0.3333333333333333148, 0.3333333333333333148, 0.3333333333333334259, 0.3333333333333333703, 0.3333333333333333703, 0.3333333333333334259, 0.3333333333333333148, 0.3333333333333333148, 0.3333333333333333703, 0.3333333333333333703, 0.3333333333333332593, 0.3333333333333333703, 0.3333333333333333703, 0.3333333333333333703, 0.3333333333333333148, 0.3333333333333333148, 0.3333333333333334814, 0.3333333333333333703, 0.3333333333333334259, 0.3333333333333334259, 0.3333333333333334814, 0.3333333333333333148, 0.3333333333333333703, 0.3333333333333334259, 0.3333333333333333148, 0.3333333333333333703, 0.3333333333333333703, 0.3333333333333333703, 0.3333333333333333703, 0.3333333333333333703, 0.3333333333333333148, 0.3333333333333334814, 0.3333333333333332593, 0.3333333333333334259, 0.3333333333333333703, 0.3333333333333333703, 0.3333333333333333148, 0.3333333333333333703, 0.3333333333333334259, 0.3333333333333332593, 0.3333333333333334259, 0.3333333333333333703, 0.3333333333333333148, 0.3333333333333333148, 0.3333333333333332593, 0.3333333333333334259, 0.3333333333333333703, 0.3333333333333333703, 0.3333333333333333148, 0.3333333333333334259, 0.3333333333333333148, 0.3333333333333335369, 0.3333333333333333148, 0.3333333333333333703, 0.3333333333333333703, 0.3333333333333333703, 0.3333333333333334259, 0.3333333333333332593, 0.3333333333333333703, 0.3333333333333333703, 0.3333333333333333703, 0.3333333333333333703, 0.3333333333333333148, 0.3333333333333333703, 0.3333333333333333703, 0.3333333333333334259, 0.3333333333333333703, 0.3333333333333333703, 0.3333333333333335369, 0.3333333333333333148, 0.3333333333333333148, 0.3333333333333333703, 0.3333333333333333703, 0.3333333333333333148, 0.3333333333333334259, 0.3333333333333333148, 0.3333333333333333703, 0.3333333333333333148, 0.3333333333333334814, 0.3333333333333334259, 0.3333333333333333703, 0.3333333333333334259, 0.3333333333333334259, 0.3333333333333332593, 0.3333333333333333703, 0.3333333333333334259, 0.3333333333333334259, 0.3333333333333333148, 0.3333333333333334259, 0.3333333333333333148, 0.3333333333333334259, 0.3333333333333333703, 0.3333333333333333148, 0.3333333333333334814, 0.3333333333333332038, 0.3333333333333333703, 0.3333333333333334259, 0.3333333333333333703, 0.3333333333333333703, 0.3333333333333334814, 0.3333333333333332593, 0.3333333333333334814, 0.3333333333333332593, 0.3333333333333334259, 0.3333333333333334259, 0.3333333333333332593, 0.3333333333333334259, 0.3333333333333334259, 0.3333333333333333148, 0.3333333333333332593, 0.3333333333333334259, 0.3333333333333333148, 0.3333333333333334259, 0.3333333333333333703, 0.3333333333333334259, 0.3333333333333332038, 0.3333333333333334814, 0.3333333333333333148, 0.3333333333333333703, 0.3333333333333334259, 0.3333333333333333703, 0.3333333333333333703, 0.3333333333333334259, 0.3333333333333334259, 0.3333333333333333148, 0.3333333333333334259, 0.3333333333333333148, 0.3333333333333333703, 0.3333333333333333703, 0.3333333333333333148, 0.3333333333333335369, 0.3333333333333333148, 0.3333333333333334259, 0.3333333333333333148, 0.3333333333333334259, 0.3333333333333335369, 0.3333333333333332593, 0.3333333333333333703, 0.3333333333333333148, 0.3333333333333334259, 0.3333333333333333148, 0.3333333333333334814, 0.3333333333333332593, 0.3333333333333333703, 0.3333333333333333148, 0.3333333333333334259, 0.3333333333333333703, 0.3333333333333333148, 0.3333333333333333703, 0.3333333333333334814, 0.3333333333333333148, 0.3333333333333333703, 0.3333333333333333148, 0.3333333333333333703, 0.3333333333333333148, 0.3333333333333333703, 0.3333333333333333148, 0.3333333333333332593, 0.3333333333333334814, 0.3333333333333332593, 0.3333333333333335369, 0.3333333333333333703, 0.3333333333333333703, 0.3333333333333332038, 0.3333333333333335369, 0.3333333333333333703, 0.3333333333333334259, 0.3333333333333333148, 0.3333333333333334259, 0.3333333333333333148, 0.3333333333333334259, 0.3333333333333333703, 0.3333333333333333703, 0.3333333333333333703, 0.3333333333333334814, 0.3333333333333332038, 0.3333333333333334814, 0.3333333333333333148, 0.3333333333333334259, 0.3333333333333333148, 0.3333333333333333703, 0.3333333333333333703, 0.3333333333333333703, 0.3333333333333332593, 0.3333333333333334814, 0.3333333333333333148, 0.3333333333333333703, 0.3333333333333334259, 0.3333333333333333148, 0.3333333333333334259, 0.3333333333333333703, 0.3333333333333334814, 0.3333333333333333148, 0.3333333333333333703, 0.3333333333333334259, 0.3333333333333333703, 0.3333333333333333148, 0.3333333333333334814, 0.3333333333333333703, 0.3333333333333332593, 0.3333333333333335369, 0.3333333333333332038, 0.3333333333333335369, 0.3333333333333333148, 0.3333333333333334259, 0.3333333333333333703, 0.3333333333333333703, 0.3333333333333334259, 0.3333333333333333703, 0.3333333333333333703, 0.3333333333333333703, 0.3333333333333332593, 0.3333333333333334259, 0.3333333333333334259, 0.3333333333333333148, 0.3333333333333333703, 0.3333333333333333148, 0.3333333333333334259, 0.3333333333333334259, 0.3333333333333333148, 0.3333333333333333703, 0.3333333333333333703, 0.3333333333333333703, 0.3333333333333333703, 0.3333333333333334259, 0.3333333333333334259, 0.3333333333333333703, 0.3333333333333334259, 0.3333333333333333148, 0.3333333333333334814, 0.3333333333333334259, 0.3333333333333333148, 0.3333333333333333703, 0.3333333333333333703, 0.3333333333333334259, 0.3333333333333333703, 0.3333333333333333703, 0.3333333333333333148, 0.3333333333333335924, 0.3333333333333332038, 0.3333333333333335924, 0.3333333333333333148, 0.3333333333333333703, 0.3333333333333333148, 0.3333333333333333148, 0.3333333333333334814, 0.3333333333333332038, 0.3333333333333334814, 0.3333333333333334259, 0.3333333333333333703, 0.3333333333333334259, 0.3333333333333333148, 0.3333333333333333703, 0.3333333333333334259, 0.3333333333333333148, 0.3333333333333333148, 0.3333333333333334259, 0.3333333333333334259, 0.3333333333333333148, 0.3333333333333334814, 0.3333333333333333703, 0.3333333333333334259, 0.3333333333333333703, 0.3333333333333333148, 0.3333333333333333703, 0.3333333333333333703, 0.3333333333333333703, 0.3333333333333333703, 0.3333333333333333703, 0.3333333333333334814, 0.3333333333333333148, 0.3333333333333334259, 0.3333333333333334259, 0.3333333333333333148, 0.3333333333333334259, 0.3333333333333332038, 0.3333333333333335369, 0.3333333333333332593, 0.3333333333333333703, 0.3333333333333333703, 0.3333333333333333148, 0.3333333333333334259, 0.3333333333333333148, 0.3333333333333334259, 0.3333333333333333148, 0.3333333333333333703, 0.3333333333333334259, 0.3333333333333333703, 0.3333333333333333148, 0.3333333333333333703, 0.3333333333333333148, 0.3333333333333334259, 0.3333333333333334259, 0.3333333333333333148, 0.3333333333333333148, 0.3333333333333333703, 0.3333333333333333703, 0.3333333333333333703, 0.3333333333333333703, 0.3333333333333334259, 0.3333333333333333148, 0.3333333333333334814, 0.3333333333333332593, 0.3333333333333334259, 0.3333333333333333703, 0.3333333333333333703, 0.3333333333333333703, 0.3333333333333333148, 0.3333333333333335369, 0.3333333333333333703, 0.3333333333333332593, 0.3333333333333334814, 0.3333333333333333703, 0.3333333333333333703, 0.3333333333333333703, 0.3333333333333333703, 0.3333333333333333703, 0.3333333333333333703, 0.3333333333333333703, 0.3333333333333333703, 0.3333333333333333703, 0.3333333333333334259, 0.3333333333333332593, 0.3333333333333333148, 0.3333333333333334259, 0.3333333333333334259, 0.3333333333333334259),
 ( 1.000000000000000222, 1.000000000000000222, 1.000000000000000000, 1.000000000000000222, 1.000000000000000000, 0.9999999999999997780, 1.000000000000000222, 1.000000000000000000, 1.000000000000000222, 1.000000000000000222, 1.000000000000000000, 0.9999999999999997780, 1.000000000000000000, 1.000000000000000222, 0.9999999999999997780, 1.000000000000000222, 0.9999999999999994449, 1.000000000000000444, 0.9999999999999996669, 1.000000000000000000, 1.000000000000000222, 1.000000000000000000, 1.000000000000000000, 0.9999999999999997780, 1.000000000000000444, 0.9999999999999996669, 1.000000000000000000, 1.000000000000000222, 0.9999999999999997780, 1.000000000000000000, 0.9999999999999997780, 0.9999999999999997780, 1.000000000000000444, 0.9999999999999994449, 1.000000000000000444, 0.9999999999999997780, 0.9999999999999997780, 0.9999999999999996669, 1.000000000000000222, 1.000000000000000000, 0.9999999999999997780, 1.000000000000000222, 0.9999999999999997780, 1.000000000000000222, 1.000000000000000000, 1.000000000000000222, 1.000000000000000000, 1.000000000000000000, 1.000000000000000444, 0.9999999999999996669, 0.9999999999999997780, 1.000000000000000000, 0.9999999999999997780, 0.9999999999999997780, 1.000000000000000000, 1.000000000000000000, 0.9999999999999997780, 1.000000000000000444, 1.000000000000000000, 0.9999999999999997780, 1.000000000000000222, 0.9999999999999996669, 1.000000000000000222, 1.000000000000000000, 0.9999999999999997780, 1.000000000000000222, 0.9999999999999997780, 1.000000000000000000, 0.9999999999999997780, 1.000000000000000222, 0.9999999999999996669, 1.000000000000000000, 1.000000000000000222, 0.9999999999999997780, 1.000000000000000222, 0.9999999999999996669, 1.000000000000000444, 1.000000000000000000, 1.000000000000000000, 1.000000000000000222, 1.000000000000000222, 1.000000000000000000, 0.9999999999999997780, 1.000000000000000222, 0.9999999999999997780, 1.000000000000000000, 1.000000000000000000, 1.000000000000000000, 0.9999999999999997780, 1.000000000000000000, 0.9999999999999997780, 1.000000000000000222, 0.9999999999999997780, 1.000000000000000000, 1.000000000000000222, 0.9999999999999997780, 1.000000000000000000, 0.9999999999999996669, 1.000000000000000444, 0.9999999999999997780, 1.000000000000000000, 1.000000000000000000, 1.000000000000000000, 0.9999999999999997780, 0.9999999999999997780, 1.000000000000000222, 1.000000000000000222, 0.9999999999999997780, 1.000000000000000000, 1.000000000000000000, 1.000000000000000222, 1.000000000000000222, 1.000000000000000000, 0.9999999999999997780, 1.000000000000000222, 1.000000000000000000, 1.000000000000000000, 0.9999999999999997780, 0.9999999999999997780, 1.000000000000000222, 1.000000000000000000, 1.000000000000000000, 1.000000000000000000, 0.9999999999999997780, 1.000000000000000222, 1.000000000000000000, 1.000000000000000000, 1.000000000000000000, 1.000000000000000444, 0.9999999999999997780, 0.9999999999999997780, 1.000000000000000000, 1.000000000000000000, 0.9999999999999997780, 1.000000000000000222, 0.9999999999999997780, 1.000000000000000222, 1.000000000000000000, 1.000000000000000222, 1.000000000000000222, 1.000000000000000000, 1.000000000000000222, 1.000000000000000000, 0.9999999999999996669, 1.000000000000000222, 0.9999999999999997780, 1.000000000000000444, 0.9999999999999997780, 1.000000000000000000, 0.9999999999999997780, 1.000000000000000222, 1.000000000000000000, 0.9999999999999997780, 1.000000000000000222, 0.9999999999999994449, 1.000000000000000000, 1.000000000000000222, 1.000000000000000222, 0.9999999999999997780, 1.000000000000000444, 0.9999999999999997780, 1.000000000000000222, 0.9999999999999997780, 1.000000000000000222, 0.9999999999999997780, 1.000000000000000000, 1.000000000000000000, 1.000000000000000222, 0.9999999999999997780, 0.9999999999999996669, 1.000000000000000444, 0.9999999999999997780, 1.000000000000000222, 1.000000000000000000, 1.000000000000000222, 0.9999999999999994449, 1.000000000000000444, 0.9999999999999997780, 1.000000000000000000, 1.000000000000000222, 1.000000000000000000, 1.000000000000000000, 0.9999999999999997780, 1.000000000000000444, 0.9999999999999997780, 1.000000000000000444, 0.9999999999999997780, 1.000000000000000000, 1.000000000000000222, 0.9999999999999996669, 1.000000000000000222, 1.000000000000000000, 1.000000000000000000, 0.9999999999999996669, 1.000000000000000222, 1.000000000000000444, 0.9999999999999997780, 1.000000000000000222, 0.9999999999999996669, 1.000000000000000444, 0.9999999999999997780, 1.000000000000000444, 0.9999999999999996669, 0.9999999999999997780, 1.000000000000000000, 0.9999999999999997780, 1.000000000000000000, 1.000000000000000000, 1.000000000000000000, 1.000000000000000000, 0.9999999999999997780, 1.000000000000000000, 0.9999999999999997780, 1.000000000000000000, 1.000000000000000000, 1.000000000000000000, 1.000000000000000000, 0.9999999999999997780, 1.000000000000000222, 0.9999999999999997780, 1.000000000000000222, 0.9999999999999997780, 1.000000000000000222, 0.9999999999999994449, 1.000000000000000444, 1.000000000000000000, 1.000000000000000222, 0.9999999999999997780, 1.000000000000000000, 0.9999999999999997780, 1.000000000000000222, 1.000000000000000000, 1.000000000000000000, 1.000000000000000222, 1.000000000000000222, 0.9999999999999996669, 1.000000000000000444, 0.9999999999999996669, 1.000000000000000444, 0.9999999999999996669, 1.000000000000000000, 1.000000000000000000, 1.000000000000000000, 0.9999999999999997780, 1.000000000000000222, 0.9999999999999997780, 1.000000000000000222, 1.000000000000000000, 0.9999999999999997780, 1.000000000000000000, 1.000000000000000222, 1.000000000000000222, 1.000000000000000000, 1.000000000000000000, 1.000000000000000000, 1.000000000000000000, 0.9999999999999997780, 1.000000000000000444, 1.000000000000000000, 0.9999999999999997780, 1.000000000000000222, 0.9999999999999996669, 1.000000000000000444, 1.000000000000000000, 1.000000000000000222, 1.000000000000000222, 0.9999999999999997780, 1.000000000000000222, 0.9999999999999997780, 1.000000000000000000, 1.000000000000000000, 0.9999999999999997780, 1.000000000000000000, 1.000000000000000000, 0.9999999999999997780, 1.000000000000000222, 1.000000000000000000, 1.000000000000000000, 1.000000000000000222, 1.000000000000000000, 1.000000000000000000, 1.000000000000000000, 1.000000000000000222, 0.9999999999999997780, 1.000000000000000222, 1.000000000000000000, 0.9999999999999997780, 1.000000000000000222, 0.9999999999999997780, 1.000000000000000222, 1.000000000000000222, 1.000000000000000000, 0.9999999999999997780, 1.000000000000000000, 1.000000000000000222, 1.000000000000000000, 1.000000000000000000, 0.9999999999999996669, 1.000000000000000444, 0.9999999999999994449, 1.000000000000000444, 0.9999999999999997780, 1.000000000000000000, 1.000000000000000000, 0.9999999999999997780, 1.000000000000000222, 0.9999999999999997780, 1.000000000000000000, 1.000000000000000444, 0.9999999999999997780, 1.000000000000000000, 0.9999999999999997780, 1.000000000000000000, 1.000000000000000000, 0.9999999999999997780, 0.9999999999999997780, 1.000000000000000000, 1.000000000000000444, 1.000000000000000000, 1.000000000000000444, 1.000000000000000000, 1.000000000000000000, 1.000000000000000000, 0.9999999999999997780, 1.000000000000000000, 1.000000000000000000, 1.000000000000000000, 1.000000000000000000, 0.9999999999999997780, 1.000000000000000222, 1.000000000000000000, 0.9999999999999997780, 1.000000000000000444, 0.9999999999999997780, 1.000000000000000222, 0.9999999999999996669, 1.000000000000000444, 1.000000000000000000, 0.9999999999999997780, 1.000000000000000000, 1.000000000000000000, 1.000000000000000000, 0.9999999999999997780, 1.000000000000000000, 1.000000000000000000, 0.9999999999999997780, 1.000000000000000444, 0.9999999999999997780, 0.9999999999999997780, 1.000000000000000000, 1.000000000000000000, 1.000000000000000222, 1.000000000000000222, 0.9999999999999997780, 1.000000000000000000, 1.000000000000000222, 1.000000000000000000, 0.9999999999999997780, 1.000000000000000222, 1.000000000000000000, 1.000000000000000000, 1.000000000000000000, 0.9999999999999997780, 1.000000000000000000, 1.000000000000000000, 1.000000000000000000, 1.000000000000000000, 0.9999999999999997780, 1.000000000000000666, 0.9999999999999996669, 0.9999999999999996669, 1.000000000000000444, 0.9999999999999996669, 1.000000000000000222, 1.000000000000000000, 1.000000000000000000, 1.000000000000000000, 1.000000000000000000, 1.000000000000000000, 0.9999999999999997780, 1.000000000000000222, 1.000000000000000222, 0.9999999999999996669, 0.9999999999999997780, 1.000000000000000000, 1.000000000000000222, 1.000000000000000222),
 ( 0.3333333333333334259, 0.3333333333333334259, 0.3333333333333333703, 0.3333333333333334259, 0.3333333333333333703, 0.3333333333333332593, 0.3333333333333334814, 0.3333333333333333703, 0.3333333333333334814, 0.3333333333333334259, 0.3333333333333333148, 0.3333333333333333148, 0.3333333333333333703, 0.3333333333333334259, 0.3333333333333332593, 0.3333333333333334814, 0.3333333333333331483, 0.3333333333333334814, 0.3333333333333333148, 0.3333333333333333148, 0.3333333333333334259, 0.3333333333333333703, 0.3333333333333333703, 0.3333333333333333148, 0.3333333333333335369, 0.3333333333333332593, 0.3333333333333333703, 0.3333333333333333703, 0.3333333333333334259, 0.3333333333333333148, 0.3333333333333333148, 0.3333333333333333148, 0.3333333333333334259, 0.3333333333333332593, 0.3333333333333334259, 0.3333333333333334259, 0.3333333333333333148, 0.3333333333333332593, 0.3333333333333333703, 0.3333333333333333703, 0.3333333333333332593, 0.3333333333333334814, 0.3333333333333333703, 0.3333333333333333703, 0.3333333333333333148, 0.3333333333333334259, 0.3333333333333333703, 0.3333333333333333703, 0.3333333333333334814, 0.3333333333333332038, 0.3333333333333334259, 0.3333333333333333703, 0.3333333333333333148, 0.3333333333333333148, 0.3333333333333333703, 0.3333333333333333703, 0.3333333333333333148, 0.3333333333333334814, 0.3333333333333333148, 0.3333333333333333703, 0.3333333333333333148, 0.3333333333333333148, 0.3333333333333334259, 0.3333333333333333703, 0.3333333333333333703, 0.3333333333333334259, 0.3333333333333333148, 0.3333333333333333148, 0.3333333333333333703, 0.3333333333333333703, 0.3333333333333332593, 0.3333333333333333703, 0.3333333333333333703, 0.3333333333333333703, 0.3333333333333333148, 0.3333333333333333148, 0.3333333333333334814, 0.3333333333333333703, 0.3333333333333334259, 0.3333333333333334259, 0.3333333333333334814, 0.3333333333333333148, 0.3333333333333333703, 0.3333333333333334259, 0.3333333333333333148, 0.3333333333333333703, 0.3333333333333333703, 0.3333333333333333703, 0.3333333333333333703, 0.3333333333333333703, 0.3333333333333333148, 0.3333333333333334814, 0.3333333333333332593, 0.3333333333333334259, 0.3333333333333333703, 0.3333333333333333703, 0.3333333333333333148, 0.3333333333333333703, 0.3333333333333334259, 0.3333333333333332593, 0.3333333333333334259, 0.3333333333333333703, 0.3333333333333333148, 0.3333333333333333148, 0.3333333333333332593, 0.3333333333333334259, 0.3333333333333333703, 0.3333333333333333703, 0.3333333333333333148, 0.3333333333333334259, 0.3333333333333333148, 0.3333333333333335369, 0.3333333333333333148, 0.3333333333333333703, 0.3333333333333333703, 0.3333333333333333703, 0.3333333333333334259, 0.3333333333333332593, 0.3333333333333333703, 0.3333333333333333703, 0.3333333333333333703, 0.3333333333333333703, 0.3333333333333333148, 0.3333333333333333703, 0.3333333333333333703, 0.3333333333333334259, 0.3333333333333333703, 0.3333333333333333703, 0.3333333333333335369, 0.3333333333333333148, 0.3333333333333333148, 0.3333333333333333703, 0.3333333333333333703, 0.3333333333333333148, 0.3333333333333334259, 0.3333333333333333148, 0.3333333333333333703, 0.3333333333333333148, 0.3333333333333334814, 0.3333333333333334259, 0.3333333333333333703, 0.3333333333333334259, 0.3333333333333334259, 0.3333333333333332593, 0.3333333333333333703, 0.3333333333333334259, 0.3333333333333334259, 0.3333333333333333148, 0.3333333333333334259, 0.3333333333333333148, 0.3333333333333334259, 0.3333333333333333703, 0.3333333333333333148, 0.3333333333333334814, 0.3333333333333332038, 0.3333333333333333703, 0.3333333333333334259, 0.3333333333333333703, 0.3333333333333333703, 0.3333333333333334814, 0.3333333333333332593, 0.3333333333333334814, 0.3333333333333332593, 0.3333333333333334259, 0.3333333333333334259, 0.3333333333333332593, 0.3333333333333334259, 0.3333333333333334259, 0.3333333333333333148, 0.3333333333333332593, 0.3333333333333334259, 0.3333333333333333148, 0.3333333333333334259, 0.3333333333333333703, 0.3333333333333334259, 0.3333333333333332038, 0.3333333333333334814, 0.3333333333333333148, 0.3333333333333333703, 0.3333333333333334259, 0.3333333333333333703, 0.3333333333333333703, 0.3333333333333334259, 0.3333333333333334259, 0.3333333333333333148, 0.3333333333333334259, 0.3333333333333333148, 0.3333333333333333703, 0.3333333333333333703, 0.3333333333333333148, 0.3333333333333335369, 0.3333333333333333148, 0.3333333333333334259, 0.3333333333333333148, 0.3333333333333334259, 0.3333333333333335369, 0.3333333333333332593, 0.3333333333333333703, 0.3333333333333333148, 0.3333333333333334259, 0.3333333333333333148, 0.3333333333333334814, 0.3333333333333332593, 0.3333333333333333703, 0.3333333333333333148, 0.3333333333333334259, 0.3333333333333333703, 0.3333333333333333148, 0.3333333333333333703, 0.3333333333333334814, 0.3333333333333333148, 0.3333333333333333703, 0.3333333333333333148, 0.3333333333333333703, 0.3333333333333333148, 0.3333333333333333703, 0.3333333333333333148, 0.3333333333333332593, 0.3333333333333334814, 0.3333333333333332593, 0.3333333333333335369, 0.3333333333333333703, 0.3333333333333333703, 0.3333333333333332038, 0.3333333333333335369, 0.3333333333333333703, 0.3333333333333334259, 0.3333333333333333148, 0.3333333333333334259, 0.3333333333333333148, 0.3333333333333334259, 0.3333333333333333703, 0.3333333333333333703, 0.3333333333333333703, 0.3333333333333334814, 0.3333333333333332038, 0.3333333333333334814, 0.3333333333333333148, 0.3333333333333334259, 0.3333333333333333148, 0.3333333333333333703, 0.3333333333333333703, 0.3333333333333333703, 0.3333333333333332593, 0.3333333333333334814, 0.3333333333333333148, 0.3333333333333333703, 0.3333333333333334259, 0.3333333333333333148, 0.3333333333333334259, 0.3333333333333333703, 0.3333333333333334814, 0.3333333333333333148, 0.3333333333333333703, 0.3333333333333334259, 0.3333333333333333703, 0.3333333333333333148, 0.3333333333333334814, 0.3333333333333333703, 0.3333333333333332593, 0.3333333333333335369, 0.3333333333333332038, 0.3333333333333335369, 0.3333333333333333148, 0.3333333333333334259, 0.3333333333333333703, 0.3333333333333333703, 0.3333333333333334259, 0.3333333333333333703, 0.3333333333333333703, 0.3333333333333333703, 0.3333333333333332593, 0.3333333333333334259, 0.3333333333333334259, 0.3333333333333333148, 0.3333333333333333703, 0.3333333333333333148, 0.3333333333333334259, 0.3333333333333334259, 0.3333333333333333148, 0.3333333333333333703, 0.3333333333333333703, 0.3333333333333333703, 0.3333333333333333703, 0.3333333333333334259, 0.3333333333333334259, 0.3333333333333333703, 0.3333333333333334259, 0.3333333333333333148, 0.3333333333333334814, 0.3333333333333334259, 0.3333333333333333148, 0.3333333333333333703, 0.3333333333333333703, 0.3333333333333334259, 0.3333333333333333703, 0.3333333333333333703, 0.3333333333333333148, 0.3333333333333335924, 0.3333333333333332038, 0.3333333333333335924, 0.3333333333333333148, 0.3333333333333333703, 0.3333333333333333148, 0.3333333333333333148, 0.3333333333333334814, 0.3333333333333332038, 0.3333333333333334814, 0.3333333333333334259, 0.3333333333333333703, 0.3333333333333334259, 0.3333333333333333148, 0.3333333333333333703, 0.3333333333333334259, 0.3333333333333333148, 0.3333333333333333148, 0.3333333333333334259, 0.3333333333333334259, 0.3333333333333333148, 0.3333333333333334814, 0.3333333333333333703, 0.3333333333333334259, 0.3333333333333333703, 0.3333333333333333148, 0.3333333333333333703, 0.3333333333333333703, 0.3333333333333333703, 0.3333333333333333703, 0.3333333333333333703, 0.3333333333333334814, 0.3333333333333333148, 0.3333333333333334259, 0.3333333333333334259, 0.3333333333333333148, 0.3333333333333334259, 0.3333333333333332038, 0.3333333333333335369, 0.3333333333333332593, 0.3333333333333333703, 0.3333333333333333703, 0.3333333333333333148, 0.3333333333333334259, 0.3333333333333333148, 0.3333333333333334259, 0.3333333333333333148, 0.3333333333333333703, 0.3333333333333334259, 0.3333333333333333703, 0.3333333333333333148, 0.3333333333333333703, 0.3333333333333333148, 0.3333333333333334259, 0.3333333333333334259, 0.3333333333333333148, 0.3333333333333333148, 0.3333333333333333703, 0.3333333333333333703, 0.3333333333333333703, 0.3333333333333333703, 0.3333333333333334259, 0.3333333333333333148, 0.3333333333333334814, 0.3333333333333332593, 0.3333333333333334259, 0.3333333333333333703, 0.3333333333333333703, 0.3333333333333333703, 0.3333333333333333148, 0.3333333333333335369, 0.3333333333333333703, 0.3333333333333332593, 0.3333333333333334814, 0.3333333333333333703, 0.3333333333333333703, 0.3333333333333333703, 0.3333333333333333703, 0.3333333333333333703, 0.3333333333333333703, 0.3333333333333333703, 0.3333333333333333703, 0.3333333333333333703, 0.3333333333333334259, 0.3333333333333332593, 0.3333333333333333148, 0.3333333333333334259, 0.3333333333333334259, 0.3333333333333334259),
 ( 0.3333333333333334259, 0.3333333333333334259, 0.3333333333333333703, 0.3333333333333334259, 0.3333333333333333703, 0.3333333333333332593, 0.3333333333333334814, 0.3333333333333333703, 0.3333333333333334814, 0.3333333333333334259, 0.3333333333333333148, 0.3333333333333333148, 0.3333333333333333703, 0.3333333333333334259, 0.3333333333333332593, 0.3333333333333334814, 0.3333333333333331483, 0.3333333333333334814, 0.3333333333333333148, 0.3333333333333333148, 0.3333333333333334259, 0.3333333333333333703, 0.3333333333333333703, 0.3333333333333333148, 0.3333333333333335369, 0.3333333333333332593, 0.3333333333333333703, 0.3333333333333333703, 0.3333333333333334259, 0.3333333333333333148, 0.3333333333333333148, 0.3333333333333333148, 0.3333333333333334259, 0.3333333333333332593, 0.3333333333333334259, 0.3333333333333334259, 0.3333333333333333148, 0.3333333333333332593, 0.3333333333333333703, 0.3333333333333333703, 0.3333333333333332593, 0.3333333333333334814, 0.3333333333333333703, 0.3333333333333333703, 0.3333333333333333148, 0.3333333333333334259, 0.3333333333333333703, 0.3333333333333333703, 0.3333333333333334814, 0.3333333333333332038, 0.3333333333333334259, 0.3333333333333333703, 0.3333333333333333148, 0.3333333333333333148, 0.3333333333333333703, 0.3333333333333333703, 0.3333333333333333148, 0.3333333333333334814, 0.3333333333333333148, 0.3333333333333333703, 0.3333333333333333148, 0.3333333333333333148, 0.3333333333333334259, 0.3333333333333333703, 0.3333333333333333703, 0.3333333333333334259, 0.3333333333333333148, 0.3333333333333333148, 0.3333333333333333703, 0.3333333333333333703, 0.3333333333333332593, 0.3333333333333333703, 0.3333333333333333703, 0.3333333333333333703, 0.3333333333333333148, 0.3333333333333333148, 0.3333333333333334814, 0.3333333333333333703, 0.3333333333333334259, 0.3333333333333334259, 0.3333333333333334814, 0.3333333333333333148, 0.3333333333333333703, 0.3333333333333334259, 0.3333333333333333148, 0.3333333333333333703, 0.3333333333333333703, 0.3333333333333333703, 0.3333333333333333703, 0.3333333333333333703, 0.3333333333333333148, 0.3333333333333334814, 0.3333333333333332593, 0.3333333333333334259, 0.3333333333333333703, 0.3333333333333333703, 0.3333333333333333148, 0.3333333333333333703, 0.3333333333333334259, 0.3333333333333332593, 0.3333333333333334259, 0.3333333333333333703, 0.3333333333333333148, 0.3333333333333333148, 0.3333333333333332593, 0.3333333333333334259, 0.3333333333333333703, 0.3333333333333333703, 0.3333333333333333148, 0.3333333333333334259, 0.3333333333333333148, 0.3333333333333335369, 0.3333333333333333148, 0.3333333333333333703, 0.3333333333333333703, 0.3333333333333333703, 0.3333333333333334259, 0.3333333333333332593, 0.3333333333333333703, 0.3333333333333333703, 0.3333333333333333703, 0.3333333333333333703, 0.3333333333333333148, 0.3333333333333333703, 0.3333333333333333703, 0.3333333333333334259, 0.3333333333333333703, 0.3333333333333333703, 0.3333333333333335369, 0.3333333333333333148, 0.3333333333333333148, 0.3333333333333333703, 0.3333333333333333703, 0.3333333333333333148, 0.3333333333333334259, 0.3333333333333333148, 0.3333333333333333703, 0.3333333333333333148, 0.3333333333333334814, 0.3333333333333334259, 0.3333333333333333703, 0.3333333333333334259, 0.3333333333333334259, 0.3333333333333332593, 0.3333333333333333703, 0.3333333333333334259, 0.3333333333333334259, 0.3333333333333333148, 0.3333333333333334259, 0.3333333333333333148, 0.3333333333333334259, 0.3333333333333333703, 0.3333333333333333148, 0.3333333333333334814, 0.3333333333333332038, 0.3333333333333333703, 0.3333333333333334259, 0.3333333333333333703, 0.3333333333333333703, 0.3333333333333334814, 0.3333333333333332593, 0.3333333333333334814, 0.3333333333333332593, 0.3333333333333334259, 0.3333333333333334259, 0.3333333333333332593, 0.3333333333333334259, 0.3333333333333334259, 0.3333333333333333148, 0.3333333333333332593, 0.3333333333333334259, 0.3333333333333333148, 0.3333333333333334259, 0.3333333333333333703, 0.3333333333333334259, 0.3333333333333332038, 0.3333333333333334814, 0.3333333333333333148, 0.3333333333333333703, 0.3333333333333334259, 0.3333333333333333703, 0.3333333333333333703, 0.3333333333333334259, 0.3333333333333334259, 0.3333333333333333148, 0.3333333333333334259, 0.3333333333333333148, 0.3333333333333333703, 0.3333333333333333703, 0.3333333333333333148, 0.3333333333333335369, 0.3333333333333333148, 0.3333333333333334259, 0.3333333333333333148, 0.3333333333333334259, 0.3333333333333335369, 0.3333333333333332593, 0.3333333333333333703, 0.3333333333333333148, 0.3333333333333334259, 0.3333333333333333148, 0.3333333333333334814, 0.3333333333333332593, 0.3333333333333333703, 0.3333333333333333148, 0.3333333333333334259, 0.3333333333333333703, 0.3333333333333333148, 0.3333333333333333703, 0.3333333333333334814, 0.3333333333333333148, 0.3333333333333333703, 0.3333333333333333148, 0.3333333333333333703, 0.3333333333333333148, 0.3333333333333333703, 0.3333333333333333148, 0.3333333333333332593, 0.3333333333333334814, 0.3333333333333332593, 0.3333333333333335369, 0.3333333333333333703, 0.3333333333333333703, 0.3333333333333332038, 0.3333333333333335369, 0.3333333333333333703, 0.3333333333333334259, 0.3333333333333333148, 0.3333333333333334259, 0.3333333333333333148, 0.3333333333333334259, 0.3333333333333333703, 0.3333333333333333703, 0.3333333333333333703, 0.3333333333333334814, 0.3333333333333332038, 0.3333333333333334814, 0.3333333333333333148, 0.3333333333333334259, 0.3333333333333333148, 0.3333333333333333703, 0.3333333333333333703, 0.3333333333333333703, 0.3333333333333332593, 0.3333333333333334814, 0.3333333333333333148, 0.3333333333333333703, 0.3333333333333334259, 0.3333333333333333148, 0.3333333333333334259, 0.3333333333333333703, 0.3333333333333334814, 0.3333333333333333148, 0.3333333333333333703, 0.3333333333333334259, 0.3333333333333333703, 0.3333333333333333148, 0.3333333333333334814, 0.3333333333333333703, 0.3333333333333332593, 0.3333333333333335369, 0.3333333333333332038, 0.3333333333333335369, 0.3333333333333333148, 0.3333333333333334259, 0.3333333333333333703, 0.3333333333333333703, 0.3333333333333334259, 0.3333333333333333703, 0.3333333333333333703, 0.3333333333333333703, 0.3333333333333332593, 0.3333333333333334259, 0.3333333333333334259, 0.3333333333333333148, 0.3333333333333333703, 0.3333333333333333148, 0.3333333333333334259, 0.3333333333333334259, 0.3333333333333333148, 0.3333333333333333703, 0.3333333333333333703, 0.3333333333333333703, 0.3333333333333333703, 0.3333333333333334259, 0.3333333333333334259, 0.3333333333333333703, 0.3333333333333334259, 0.3333333333333333148, 0.3333333333333334814, 0.3333333333333334259, 0.3333333333333333148, 0.3333333333333333703, 0.3333333333333333703, 0.3333333333333334259, 0.3333333333333333703, 0.3333333333333333703, 0.3333333333333333148, 0.3333333333333335924, 0.3333333333333332038, 0.3333333333333335924, 0.3333333333333333148, 0.3333333333333333703, 0.3333333333333333148, 0.3333333333333333148, 0.3333333333333334814, 0.3333333333333332038, 0.3333333333333334814, 0.3333333333333334259, 0.3333333333333333703, 0.3333333333333334259, 0.3333333333333333148, 0.3333333333333333703, 0.3333333333333334259, 0.3333333333333333148, 0.3333333333333333148, 0.3333333333333334259, 0.3333333333333334259, 0.3333333333333333148, 0.3333333333333334814, 0.3333333333333333703, 0.3333333333333334259, 0.3333333333333333703, 0.3333333333333333148, 0.3333333333333333703, 0.3333333333333333703, 0.3333333333333333703, 0.3333333333333333703, 0.3333333333333333703, 0.3333333333333334814, 0.3333333333333333148, 0.3333333333333334259, 0.3333333333333334259, 0.3333333333333333148, 0.3333333333333334259, 0.3333333333333332038, 0.3333333333333335369, 0.3333333333333332593, 0.3333333333333333703, 0.3333333333333333703, 0.3333333333333333148, 0.3333333333333334259, 0.3333333333333333148, 0.3333333333333334259, 0.3333333333333333148, 0.3333333333333333703, 0.3333333333333334259, 0.3333333333333333703, 0.3333333333333333148, 0.3333333333333333703, 0.3333333333333333148, 0.3333333333333334259, 0.3333333333333334259, 0.3333333333333333148, 0.3333333333333333148, 0.3333333333333333703, 0.3333333333333333703, 0.3333333333333333703, 0.3333333333333333703, 0.3333333333333334259, 0.3333333333333333148, 0.3333333333333334814, 0.3333333333333332593, 0.3333333333333334259, 0.3333333333333333703, 0.3333333333333333703, 0.3333333333333333703, 0.3333333333333333148, 0.3333333333333335369, 0.3333333333333333703, 0.3333333333333332593, 0.3333333333333334814, 0.3333333333333333703, 0.3333333333333333703, 0.3333333333333333703, 0.3333333333333333703, 0.3333333333333333703, 0.3333333333333333703, 0.3333333333333333703, 0.3333333333333333703, 0.3333333333333333703, 0.3333333333333334259, 0.3333333333333332593, 0.3333333333333333148, 0.3333333333333334259, 0.3333333333333334259, 0.3333333333333334259),
 ( 1.000000000000000222, 1.000000000000000222, 1.000000000000000000, 1.000000000000000222, 1.000000000000000000, 0.9999999999999997780, 1.000000000000000222, 1.000000000000000000, 1.000000000000000222, 1.000000000000000222, 1.000000000000000000, 0.9999999999999997780, 1.000000000000000000, 1.000000000000000222, 0.9999999999999997780, 1.000000000000000222, 0.9999999999999994449, 1.000000000000000444, 0.9999999999999996669, 1.000000000000000000, 1.000000000000000222, 1.000000000000000000, 1.000000000000000000, 0.9999999999999997780, 1.000000000000000444, 0.9999999999999996669, 1.000000000000000000, 1.000000000000000222, 0.9999999999999997780, 1.000000000000000000, 0.9999999999999997780, 0.9999999999999997780, 1.000000000000000444, 0.9999999999999994449, 1.000000000000000444, 0.9999999999999997780, 0.9999999999999997780, 0.9999999999999996669, 1.000000000000000222, 1.000000000000000000, 0.9999999999999997780, 1.000000000000000222, 0.9999999999999997780, 1.000000000000000222, 1.000000000000000000, 1.000000000000000222, 1.000000000000000000, 1.000000000000000000, 1.000000000000000444, 0.9999999999999996669, 0.9999999999999997780, 1.000000000000000000, 0.9999999999999997780, 0.9999999999999997780, 1.000000000000000000, 1.000000000000000000, 0.9999999999999997780, 1.000000000000000444, 1.000000000000000000, 0.9999999999999997780, 1.000000000000000222, 0.9999999999999996669, 1.000000000000000222, 1.000000000000000000, 0.9999999999999997780, 1.000000000000000222, 0.9999999999999997780, 1.000000000000000000, 0.9999999999999997780, 1.000000000000000222, 0.9999999999999996669, 1.000000000000000000, 1.000000000000000222, 0.9999999999999997780, 1.000000000000000222, 0.9999999999999996669, 1.000000000000000444, 1.000000000000000000, 1.000000000000000000, 1.000000000000000222, 1.000000000000000222, 1.000000000000000000, 0.9999999999999997780, 1.000000000000000222, 0.9999999999999997780, 1.000000000000000000, 1.000000000000000000, 1.000000000000000000, 0.9999999999999997780, 1.000000000000000000, 0.9999999999999997780, 1.000000000000000222, 0.9999999999999997780, 1.000000000000000000, 1.000000000000000222, 0.9999999999999997780, 1.000000000000000000, 0.9999999999999996669, 1.000000000000000444, 0.9999999999999997780, 1.000000000000000000, 1.000000000000000000, 1.000000000000000000, 0.9999999999999997780, 0.9999999999999997780, 1.000000000000000222, 1.000000000000000222, 0.9999999999999997780, 1.000000000000000000, 1.000000000000000000, 1.000000000000000222, 1.000000000000000222, 1.000000000000000000, 0.9999999999999997780, 1.000000000000000222, 1.000000000000000000, 1.000000000000000000, 0.9999999999999997780, 0.9999999999999997780, 1.000000000000000222, 1.000000000000000000, 1.000000000000000000, 1.000000000000000000, 0.9999999999999997780, 1.000000000000000222, 1.000000000000000000, 1.000000000000000000, 1.000000000000000000, 1.000000000000000444, 0.9999999999999997780, 0.9999999999999997780, 1.000000000000000000, 1.000000000000000000, 0.9999999999999997780, 1.000000000000000222, 0.9999999999999997780, 1.000000000000000222, 1.000000000000000000, 1.000000000000000222, 1.000000000000000222, 1.000000000000000000, 1.000000000000000222, 1.000000000000000000, 0.9999999999999996669, 1.000000000000000222, 0.9999999999999997780, 1.000000000000000444, 0.9999999999999997780, 1.000000000000000000, 0.9999999999999997780, 1.000000000000000222, 1.000000000000000000, 0.9999999999999997780, 1.000000000000000222, 0.9999999999999994449, 1.000000000000000000, 1.000000000000000222, 1.000000000000000222, 0.9999999999999997780, 1.000000000000000444, 0.9999999999999997780, 1.000000000000000222, 0.9999999999999997780, 1.000000000000000222, 0.9999999999999997780, 1.000000000000000000, 1.000000000000000000, 1.000000000000000222, 0.9999999999999997780, 0.9999999999999996669, 1.000000000000000444, 0.9999999999999997780, 1.000000000000000222, 1.000000000000000000, 1.000000000000000222, 0.9999999999999994449, 1.000000000000000444, 0.9999999999999997780, 1.000000000000000000, 1.000000000000000222, 1.000000000000000000, 1.000000000000000000, 0.9999999999999997780, 1.000000000000000444, 0.9999999999999997780, 1.000000000000000444, 0.9999999999999997780, 1.000000000000000000, 1.000000000000000222, 0.9999999999999996669, 1.000000000000000222, 1.000000000000000000, 1.000000000000000000, 0.9999999999999996669, 1.000000000000000222, 1.000000000000000444, 0.9999999999999997780, 1.000000000000000222, 0.9999999999999996669, 1.000000000000000444, 0.9999999999999997780, 1.000000000000000444, 0.9999999999999996669, 0.9999999999999997780, 1.000000000000000000, 0.9999999999999997780, 1.000000000000000000, 1.000000000000000000, 1.000000000000000000, 1.000000000000000000, 0.9999999999999997780, 1.000000000000000000, 0.9999999999999997780, 1.000000000000000000, 1.000000000000000000, 1.000000000000000000, 1.000000000000000000, 0.9999999999999997780, 1.000000000000000222, 0.9999999999999997780, 1.000000000000000222, 0.9999999999999997780, 1.000000000000000222, 0.9999999999999994449, 1.000000000000000444, 1.000000000000000000, 1.000000000000000222, 0.9999999999999997780, 1.000000000000000000, 0.9999999999999997780, 1.000000000000000222, 1.000000000000000000, 1.000000000000000000, 1.000000000000000222, 1.000000000000000222, 0.9999999999999996669, 1.000000000000000444, 0.9999999999999996669, 1.000000000000000444, 0.9999999999999996669, 1.000000000000000000, 1.000000000000000000, 1.000000000000000000, 0.9999999999999997780, 1.000000000000000222, 0.9999999999999997780, 1.000000000000000222, 1.000000000000000000, 0.9999999999999997780, 1.000000000000000000, 1.000000000000000222, 1.000000000000000222, 1.000000000000000000, 1.000000000000000000, 1.000000000000000000, 1.000000000000000000, 0.9999999999999997780, 1.000000000000000444, 1.000000000000000000, 0.9999999999999997780, 1.000000000000000222, 0.9999999999999996669, 1.000000000000000444, 1.000000000000000000, 1.000000000000000222, 1.000000000000000222, 0.9999999999999997780, 1.000000000000000222, 0.9999999999999997780, 1.000000000000000000, 1.000000000000000000, 0.9999999999999997780, 1.000000000000000000, 1.000000000000000000, 0.9999999999999997780, 1.000000000000000222, 1.000000000000000000, 1.000000000000000000, 1.000000000000000222, 1.000000000000000000, 1.000000000000000000, 1.000000000000000000, 1.000000000000000222, 0.9999999999999997780, 1.000000000000000222, 1.000000000000000000, 0.9999999999999997780, 1.000000000000000222, 0.9999999999999997780, 1.000000000000000222, 1.000000000000000222, 1.000000000000000000, 0.9999999999999997780, 1.000000000000000000, 1.000000000000000222, 1.000000000000000000, 1.000000000000000000, 0.9999999999999996669, 1.000000000000000444, 0.9999999999999994449, 1.000000000000000444, 0.9999999999999997780, 1.000000000000000000, 1.000000000000000000, 0.9999999999999997780, 1.000000000000000222, 0.9999999999999997780, 1.000000000000000000, 1.000000000000000444, 0.9999999999999997780, 1.000000000000000000, 0.9999999999999997780, 1.000000000000000000, 1.000000000000000000, 0.9999999999999997780, 0.9999999999999997780, 1.000000000000000000, 1.000000000000000444, 1.000000000000000000, 1.000000000000000444, 1.000000000000000000, 1.000000000000000000, 1.000000000000000000, 0.9999999999999997780, 1.000000000000000000, 1.000000000000000000, 1.000000000000000000, 1.000000000000000000, 0.9999999999999997780, 1.000000000000000222, 1.000000000000000000, 0.9999999999999997780, 1.000000000000000444, 0.9999999999999997780, 1.000000000000000222, 0.9999999999999996669, 1.000000000000000444, 1.000000000000000000, 0.9999999999999997780, 1.000000000000000000, 1.000000000000000000, 1.000000000000000000, 0.9999999999999997780, 1.000000000000000000, 1.000000000000000000, 0.9999999999999997780, 1.000000000000000444, 0.9999999999999997780, 0.9999999999999997780, 1.000000000000000000, 1.000000000000000000, 1.000000000000000222, 1.000000000000000222, 0.9999999999999997780, 1.000000000000000000, 1.000000000000000222, 1.000000000000000000, 0.9999999999999997780, 1.000000000000000222, 1.000000000000000000, 1.000000000000000000, 1.000000000000000000, 0.9999999999999997780, 1.000000000000000000, 1.000000000000000000, 1.000000000000000000, 1.000000000000000000, 0.9999999999999997780, 1.000000000000000666, 0.9999999999999996669, 0.9999999999999996669, 1.000000000000000444, 0.9999999999999996669, 1.000000000000000222, 1.000000000000000000, 1.000000000000000000, 1.000000000000000000, 1.000000000000000000, 1.000000000000000000, 0.9999999999999997780, 1.000000000000000222, 1.000000000000000222, 0.9999999999999996669, 0.9999999999999997780, 1.000000000000000000, 1.000000000000000222, 1.000000000000000222) ) ) 
 REPRESENTATION_ITEM ( '' )  SURFACE ( )  );
#91563=CARTESIAN_POINT ( 'NONE',  ( 1.955877382181537838, 1.966306777096353153, -0.1432868284926436253 ) ) ;
#91565=CARTESIAN_POINT ( 'NONE',  ( 5.871340715825057011, -1.643613990083541143, -0.9773822251149253404 ) ) ;
#91571=CARTESIAN_POINT ( 'NONE',  ( 1.963541569377712959, -1.623395098231813494, -1.201329681988633657 ) ) ;
#91573=CARTESIAN_POINT ( 'NONE',  ( 5.227664224568670193, -2.193190438267843323, 0.7177837189984050958 ) ) ;
#91575=CARTESIAN_POINT ( 'NONE',  ( 2.465611527742004760, -0.4346729355233553416, 1.912824223707191296 ) ) ;
#91577=CARTESIAN_POINT ( 'NONE',  ( 0.9850002542920628379, -2.016597020373378513, 0.002813405579435435122 ) ) ;
#91579=CARTESIAN_POINT ( 'NONE',  ( 2.817688460867060485, -1.425471633543059724, -1.565750481055405263 ) ) ;
#91582=CARTESIAN_POINT ( 'NONE',  ( 2.343484645521694887, 1.840739972059933560, 0.04548452486473342216 ) ) ;
#91586=CARTESIAN_POINT ( 'NONE',  ( 2.848016566918720294, -1.427295477286108394, -1.568503593382633454 ) ) ;
#91587=CARTESIAN_POINT ( 'NONE',  ( 6.720655732516681802, 0.002698097948229584257, 1.926293798961112858 ) ) ;
#91591=CARTESIAN_POINT ( 'NONE',  ( 4.499328421682089463, 1.652694973434418291, 1.230784805264173221 ) ) ;
#91593=CARTESIAN_POINT ( 'NONE',  ( 1.839159199666509981, 0.7036077657225293658, -1.701706503975081830 ) ) ;
#91595=CARTESIAN_POINT ( 'NONE',  ( -0.02224634325196597762, 0.2233488839939681836, -2.322587069611138144 ) ) ;
#91599=CARTESIAN_POINT ( 'NONE',  ( 1.401302286655212948, 1.802556353783949517, -1.272968949304439379 ) ) ;
#91600=CARTESIAN_POINT ( 'NONE',  ( 2.794484930487377561, -2.256151742081555334, -0.1692699688307132133 ) ) ;
#91602=CARTESIAN_POINT ( 'NONE',  ( 4.095841850722721667, 1.188128187434208893, 1.367607970084052660 ) ) ;
#91604=CARTESIAN_POINT ( 'NONE',  ( 3.133901338358492161, 1.915903397621956383, -0.005105665024216290114 ) ) ;
#91605=CARTESIAN_POINT ( 'NONE',  ( 4.246580143467587831, -2.047389768388275577, -0.3068500204662719666 ) ) ;
#91607=CARTESIAN_POINT ( 'NONE',  ( 2.342595614570395668, 0.4301288016448929774, 1.923825502367804141 ) ) ;
#91608=CARTESIAN_POINT ( 'NONE',  ( 0.6922523098862876090, -1.911435030786556855, -0.2391616053641909545 ) ) ;
#91609=CARTESIAN_POINT ( 'NONE',  ( 3.994877460428855276, 1.580554378303768992, -1.000287695324620252 ) ) ;
#91610=CARTESIAN_POINT ( 'NONE',  ( 1.840857126529979126, 2.283052885565831858, 0.3356036407394235033 ) ) ;
#91611=CARTESIAN_POINT ( 'NONE',  ( 3.930005801358939621, 1.032382326871328804, 1.548228005463901491 ) ) ;
#91617=CARTESIAN_POINT ( 'NONE',  ( 1.137491875146545039, -1.903277616399126293, 0.9019996372539202945 ) ) ;
#91621=CARTESIAN_POINT ( 'NONE',  ( 2.584367824843319283, 1.138156186954141003, 1.789115803205274080 ) ) ;
#91622=CARTESIAN_POINT ( 'NONE',  ( -0.1579319072057436268, -1.246015270063109748, -1.590120154594099278 ) ) ;
#91626=CARTESIAN_POINT ( 'NONE',  ( 1.054251131370760319, 2.159144779032458050, -0.1049546803274861440 ) ) ;
#91628=CARTESIAN_POINT ( 'NONE',  ( 6.925078400183577010, 7.053014648177382995, 2.453806744102948745 ) ) ;
#91630=CARTESIAN_POINT ( 'NONE',  ( -0.2104748580754409459, 6.947232144882289795, -2.698723162346649662 ) ) ;
#91631=CARTESIAN_POINT ( 'NONE',  ( 6.104703911763087909, 1.883310800321544409, 0.7212973825745233603 ) ) ;
#91635=CARTESIAN_POINT ( 'NONE',  ( 0.8665589547518313118, 1.117614298721156585, 1.967126077831014896 ) ) ;
#91639=CARTESIAN_POINT ( 'NONE',  ( 6.292592244351721043, 1.492246071875057423, -1.356311808412967723 ) ) ;
#91643=CARTESIAN_POINT ( 'NONE',  ( 3.334305206967770552, 1.683047542859770429, 0.3767605245002195180 ) ) ;
#91646=CARTESIAN_POINT ( 'NONE',  ( 0.7547153349467434769, -1.490676808382383145, -0.9535711479493594878 ) ) ;
#91648=CARTESIAN_POINT ( 'NONE',  ( 1.418609115998151982, -0.7265329536030593616, -1.877579518606347531 ) ) ;
#91650=CARTESIAN_POINT ( 'NONE',  ( 4.366400497975233996, 1.037236317483503312, 1.947806255051434121 ) ) ;
#91653=CARTESIAN_POINT ( 'NONE',  ( 4.635462950926918957, -0.1032030737609032217, 2.118083805499561656 ) ) ;
#91654=CARTESIAN_POINT ( 'NONE',  ( 2.917592388753763366, -1.356314522985989424, -1.492243612603139757 ) ) ;
#91655=CARTESIAN_POINT ( 'NONE',  ( 3.568453337068989928, 0.6571482028082703541, 1.688366419454911727 ) ) ;
#91660=CARTESIAN_POINT ( 'NONE',  ( 0.6373110600932235803, -1.319858442276698129, -1.325903642019378381 ) ) ;
#91663=CARTESIAN_POINT ( 'NONE',  ( 6.533835636172961259, -1.196796279342365210, -1.378804128639096849 ) ) ;
#91665=CARTESIAN_POINT ( 'NONE',  ( 2.922943415214097396, -1.687269874283424453, 0.9073053738915691779 ) ) ;
#91674=CARTESIAN_POINT ( 'NONE',  ( 3.006218798242997980, -0.8556837461295876412, 1.940463308995137526 ) ) ;
#91675=FACE_OUTER_BOUND ( 'NONE', #132441, .T. ) ;
#91677=CARTESIAN_POINT ( 'NONE',  ( 4.798096821016461178, -1.970857504970180862, -0.05141287852120436652 ) ) ;
#91679=CARTESIAN_POINT ( 'NONE',  ( 0.1232915322694717181, 1.753566389086946398, 0.9887636377800024245 ) ) ;
#91681=CARTESIAN_POINT ( 'NONE',  ( 0.3689691111537584112, -0.2640367098126532031, -2.100658933187772526 ) ) ;
#91682=CARTESIAN_POINT ( 'NONE',  ( 1.627480586986803868, 0.1543294891723171747, -2.064685722993148342 ) ) ;
#91683=CARTESIAN_POINT ( 'NONE',  ( 2.308448745193259821, 1.734665721750632938, 0.8731161087585439518 ) ) ;
#91686=CARTESIAN_POINT ( 'NONE',  ( 3.626972257435066460, -1.931581639804475614, 0.8003350836045771688 ) ) ;
#91689=CARTESIAN_POINT ( 'NONE',  ( 0.9612203838427415548, -1.427409828940959136, -1.115214234437786223 ) ) ;
#91691=CARTESIAN_POINT ( 'NONE',  ( 5.918643953348324160, 1.484978324971843566, -1.632713241052483832 ) ) ;
#91693=CARTESIAN_POINT ( 'NONE',  ( 3.891806949550260519, 1.596497936513015192, 1.523729906679156754 ) ) ;
#91696=CARTESIAN_POINT ( 'NONE',  ( 2.613799471529183460, -0.5979904443059110841, 1.816458080996792068 ) ) ;
#91698=CARTESIAN_POINT ( 'NONE',  ( 5.600075274486990828, 0.8424382930321882013, -1.891409743246947217 ) ) ;
#91701=CARTESIAN_POINT ( 'NONE',  ( 2.536181837661064087, 1.019768383293401248, -1.906060392209196763 ) ) ;
#91702=CARTESIAN_POINT ( 'NONE',  ( 5.196902890030515643, 1.791362914573800369, 1.262263373074036688 ) ) ;
#91713=CARTESIAN_POINT ( 'NONE',  ( 5.471561611210747245, -0.3092806512635417060, 2.046926588373791933 ) ) ;
#91714=CARTESIAN_POINT ( 'NONE',  ( 4.705647360784301014, -0.5120751438620478879, 1.857136557572524715 ) ) ;
#91715=CARTESIAN_POINT ( 'NONE',  ( -0.05311194370935175268, -1.802413661875476913, -0.9041393574176490588 ) ) ;
#91718=CARTESIAN_POINT ( 'NONE',  ( 5.242998352400915607, -0.2370019515391492138, -1.955029394545240162 ) ) ;
#91719=CARTESIAN_POINT ( 'NONE',  ( 0.1292129718690297469, -2.001788180159810970, 0.8922102942980969509 ) ) ;
#91720=CARTESIAN_POINT ( 'NONE',  ( 5.531824841778981927, -1.161409778037244100, -1.408645805323349487 ) ) ;
#91721=AXIS2_PLACEMENT_3D ( 'NONE', #106126, #125606, #139667 ) ;
#91727=CARTESIAN_POINT ( 'NONE',  ( 3.104851637799400876, -0.3563606998662186554, 1.806257425991746546 ) ) ;
#91728=CARTESIAN_POINT ( 'NONE',  ( 6.416276891523604142, -2.012660772237227391, 0.05378525197091872656 ) ) ;
#91729=CARTESIAN_POINT ( 'NONE',  ( 0.6151802255017734256, 0.7180209600621060284, -2.183386540618210692 ) ) ;
#91730=CARTESIAN_POINT ( 'NONE',  ( 6.280128941539553367, -1.086961472313338284, -1.632890767417946032 ) ) ;
#91734=CARTESIAN_POINT ( 'NONE',  ( 0.1861046438572169504, -1.272802160389638892, -1.633586439835111648 ) ) ;
#91736=CARTESIAN_POINT ( 'NONE',  ( 2.929326106026585830, -1.406127681732218360, -1.547418247020322601 ) ) ;
#91737=CARTESIAN_POINT ( 'NONE',  ( 0.7603692911175019553, -1.357789551990191246, 1.287012767582619510 ) ) ;
#91738=CARTESIAN_POINT ( 'NONE',  ( 2.143907462275076892, -0.09611812122205246056, -2.013924455302518624 ) ) ;
#91741=CARTESIAN_POINT ( 'NONE',  ( 2.366429680491717313, 0.08383053003592833008, -1.738530308508005273 ) ) ;
#91745=CARTESIAN_POINT ( 'NONE',  ( 2.631144668424452604, -1.609571295485120457, 0.6205441041484575093 ) ) ;
#91746=CARTESIAN_POINT ( 'NONE',  ( 3.017305944477025825, -2.111434807548946857, 0.5868732223921411251 ) ) ;
#91747=CARTESIAN_POINT ( 'NONE',  ( 5.707716145626243964, -0.5396369327701348029, 2.139774205771049154 ) ) ;
#91749=CARTESIAN_POINT ( 'NONE',  ( 2.993230899678362089, 0.2615320595270088644, 2.155169926569647565 ) ) ;
#91750=CARTESIAN_POINT ( 'NONE',  ( 1.013953575274041619, -0.8186894766500467657, -1.631917417583013341 ) ) ;
#91751=CARTESIAN_POINT ( 'NONE',  ( 3.679011075472499392, 1.786488794941149871, -1.136238802782759238 ) ) ;
#91754=CARTESIAN_POINT ( 'NONE',  ( 3.579850016053500728, -1.128938594042153021, 1.995021623459404703 ) ) ;
#91758=CARTESIAN_POINT ( 'NONE',  ( 5.531947820799793192, -2.167606221786242848, 0.4847573843902542312 ) ) ;
#91764=CARTESIAN_POINT ( 'NONE',  ( 4.043592392309851569, -1.492256208629010761, 1.356298961253152413 ) ) ;
#91766=CARTESIAN_POINT ( 'NONE',  ( 3.696185820831139779, 0.9318344738791024540, -1.840181792940546179 ) ) ;
#91770=CARTESIAN_POINT ( 'NONE',  ( 5.964808794498537736, 0.1646014364122504459, -2.185315939793014639 ) ) ;
#91771=CARTESIAN_POINT ( 'NONE',  ( 3.779922787921150995, 1.701948043757589124, -1.081065327119046016 ) ) ;
#91772=CARTESIAN_POINT ( 'NONE',  ( 3.034521004542716227, -1.622529355458858236, 0.8704296449140033198 ) ) ;
#91774=CARTESIAN_POINT ( 'NONE',  ( 6.194357462883206544, -1.817092693925310032, -0.1759843941628037589 ) ) ;
#91775=CARTESIAN_POINT ( 'NONE',  ( 0.08910568399025410591, -0.6041685166103001325, 2.217849651370594088 ) ) ;
#91777=CARTESIAN_POINT ( 'NONE',  ( 0.3161853103110903729, -2.218393710063219615, 0.4432750438988151687 ) ) ;
#91778=CARTESIAN_POINT ( 'NONE',  ( 1.928482936185798247, 1.211665229685221057, -1.722411974427066506 ) ) ;
#91789=CARTESIAN_POINT ( 'NONE',  ( 2.092179824929023102, 1.308410154019133076, 1.668721082780571408 ) ) ;
#91790=CARTESIAN_POINT ( 'NONE',  ( 4.447658085050952614, -2.030299463072975819, 0.9018405843745944672 ) ) ;
#91791=CARTESIAN_POINT ( 'NONE',  ( 0.7971425760184660536, 1.793611693402120455, 1.258865353619270433 ) ) ;
#91792=CARTESIAN_POINT ( 'NONE',  ( 0.2060869173217265982, -0.5842117877600698783, 2.128085570573131413 ) ) ;
#91794=CARTESIAN_POINT ( 'NONE',  ( 4.422284181769401634, 0.9229163912191931107, 1.731201473044993167 ) ) ;
#91799=CARTESIAN_POINT ( 'NONE',  ( 6.610000000000010090, 0.5825982378308904863, 2.053072689460200273 ) ) ;
#91802=CARTESIAN_POINT ( 'NONE',  ( 3.744478000529617656, 1.131475959888720295, -1.793321066073015224 ) ) ;
#91804=CARTESIAN_POINT ( 'NONE',  ( 5.295850518597075229, -0.7817450549502875656, 2.015575934489414411 ) ) ;
#91805=CARTESIAN_POINT ( 'NONE',  ( 4.388128076750056117, -0.4078595375654435751, -1.795341762384855544 ) ) ;
#91806=CARTESIAN_POINT ( 'NONE',  ( 5.384000029850495750, -2.016708404008683786, 0.004832792792668073358 ) ) ;
#91809=CARTESIAN_POINT ( 'NONE',  ( -0.09478571475088257148, -0.7418789811804274992, -1.573373712294885207 ) ) ;
#91810=CARTESIAN_POINT ( 'NONE',  ( 6.727182134110203826, 2.985950691969770254, 2.264927069331075238 ) ) ;
#91813=CARTESIAN_POINT ( 'NONE',  ( 3.696290335837215668, -2.159122111672501454, -0.1082323872379290647 ) ) ;
#91815=CARTESIAN_POINT ( 'NONE',  ( 5.870470189955956819, -0.4925641237488035395, 1.954873771647095415 ) ) ;
#91817=CARTESIAN_POINT ( 'NONE',  ( 3.502937704049163159, 1.705309618848281472, -1.328393843302433153 ) ) ;
#91818=CARTESIAN_POINT ( 'NONE',  ( 3.409407428336236556, -0.3879349331968630077, 1.932650128172111126 ) ) ;
#91820=CARTESIAN_POINT ( 'NONE',  ( 0.09952931447375359952, -0.5783855404800625211, 2.113812074898171023 ) ) ;
#91821=CARTESIAN_POINT ( 'NONE',  ( 0.9741375256873509025, 2.223107509294399264, -0.6184994596578182735 ) ) ;
#91822=CARTESIAN_POINT ( 'NONE',  ( 2.214203678495901606, -0.9685002052983943122, -1.818986401426671229 ) ) ;
#91823=CARTESIAN_POINT ( 'NONE',  ( 5.179219622276672652, 1.307079648806110050, 1.436513822289321674 ) ) ;
#91831=CARTESIAN_POINT ( 'NONE',  ( 2.468050989216635127, 2.164326253657654853, -0.4298898877757306725 ) ) ;
#91833=CARTESIAN_POINT ( 'NONE',  ( 6.104347744599991188, 1.959368324604572775, 0.09974838594294095639 ) ) ;
#91835=CARTESIAN_POINT ( 'NONE',  ( 6.539320575229237598, 1.252639605590206928, 2.218328189723097754 ) ) ;
#91838=CARTESIAN_POINT ( 'NONE',  ( 6.720655732516642722, 0.008434553976904573744, 1.726293928996263549 ) ) ;
#91839=CARTESIAN_POINT ( 'NONE',  ( 5.929618730664214077, 0.9035273275350870215, -1.604119651413847603 ) ) ;
#91841=CARTESIAN_POINT ( 'NONE',  ( 2.184514296101589537, -2.020881322650217360, -0.4031914428916544280 ) ) ;
#91843=UNCERTAINTY_MEASURE_WITH_UNIT (LENGTH_MEASURE( 1.000000000000000082E-05 ), #145996, 'distance_accuracy_value', 'NONE');
#91846=CARTESIAN_POINT ( 'NONE',  ( 6.345950370838200350, -1.386202306585911925, -1.604841549997563455 ) ) ;
#91849=CARTESIAN_POINT ( 'NONE',  ( 0.8661736431406670267, 1.015005012832224329, 1.793514120848164195 ) ) ;
#91851=CARTESIAN_POINT ( 'NONE',  ( 4.423293856316495187, -1.136390847421838490, -1.448631019334602144 ) ) ;
#91857=( GEOMETRIC_REPRESENTATION_CONTEXT ( 3 ) GLOBAL_UNCERTAINTY_ASSIGNED_CONTEXT ( ( #192437 ) ) GLOBAL_UNIT_ASSIGNED_CONTEXT ( ( #50885, #134301, #202433 ) ) REPRESENTATION_CONTEXT ( 'NONE', 'WORKASPACE' ) );
#91858=CARTESIAN_POINT ( 'NONE',  ( 4.231241840954825584, 0.1069408422738199749, 2.204416794138922331 ) ) ;
#91859=CARTESIAN_POINT ( 'NONE',  ( 0.4390364970160881564, 0.3691015439823107092, 2.129678967336546602 ) ) ;
#91860=CARTESIAN_POINT ( 'NONE',  ( 3.678922940808615483, 1.700962499606586853, -1.082838980105811366 ) ) ;
#91862=CARTESIAN_POINT ( 'NONE',  ( 0.3164790345465406385, -0.6463921985436006379, -1.799943259716822341 ) ) ;
#91863=CARTESIAN_POINT ( 'NONE',  ( -0.2234322562767385167, -0.4468160588090731022, -1.973564571300358228 ) ) ;
#91866=CARTESIAN_POINT ( 'NONE',  ( 5.602191078447533279, -0.8559053986842228845, 1.710104642658970775 ) ) ;
#91868=CARTESIAN_POINT ( 'NONE',  ( 0.7779422811538607707, -1.042605501850740080, 1.552959968518424771 ) ) ;
#91870=CARTESIAN_POINT ( 'NONE',  ( 2.553923023464285347, 1.082840749376843270, 1.700961377887353798 ) ) ;
#91872=CARTESIAN_POINT ( 'NONE',  ( 4.178421505988277218, -1.212938584752444093, 1.721516029631239064 ) ) ;
#91877=CARTESIAN_POINT ( 'NONE',  ( 3.586198609924298175, 1.125526462575956010, 1.676902781687271915 ) ) ;
#91881=CARTESIAN_POINT ( 'NONE',  ( 4.095124908492456584, 1.828510582809875107, -1.152538879107746439 ) ) ;
#91887=CARTESIAN_POINT ( 'NONE',  ( 2.137404458564879484, -0.1051889750803415707, -2.168730265314787076 ) ) ;
#91890=CARTESIAN_POINT ( 'NONE',  ( 0.7316835000789992938, 1.813914744281470925, 0.3150931809976220133 ) ) ;
#91892=CARTESIAN_POINT ( 'NONE',  ( 2.894263506066748093, -0.6386881658498286818, -2.096408367471907841 ) ) ;
#91894=CARTESIAN_POINT ( 'NONE',  ( 3.924925821460770514, 2.147445456087885063, 0.7125370657276063335 ) ) ;
#91900=CARTESIAN_POINT ( 'NONE',  ( 4.253014324580971284, -1.470476824294727702, -0.9843664617138027095 ) ) ;
#91902=CARTESIAN_POINT ( 'NONE',  ( 0.3058767667667975365, -0.5614299121656821656, 2.029657625958045664 ) ) ;
#91905=CARTESIAN_POINT ( 'NONE',  ( 1.469134468336911192, 1.735519167469494084, 0.9312130504785380847 ) ) ;
#91907=CARTESIAN_POINT ( 'NONE',  ( 6.521112179100128969, -1.799899466697444383, 0.9092066555835758290 ) ) ;
#91911=CARTESIAN_POINT ( 'NONE',  ( 4.293723057671197552, -0.7160966649314598476, 1.728361679364013748 ) ) ;
#91912=CARTESIAN_POINT ( 'NONE',  ( 4.311429529933403337, -1.718370896367764189, -1.154329086688666184 ) ) ;
#91922=CARTESIAN_POINT ( 'NONE',  ( 4.035565188342554954, 1.848088059160474694, -0.6588067414724924076 ) ) ;
#91923=CARTESIAN_POINT ( 'NONE',  ( 1.774767310740912984, -2.001205085354029301, 0.2439901982170673556 ) ) ;
#91926=CARTESIAN_POINT ( 'NONE',  ( 1.053721402318724021, 1.868689351376726204, -0.08586956420430363890 ) ) ;
#91928=CARTESIAN_POINT ( 'NONE',  ( 2.760023647720879492, 0.7205980239477025595, -1.880007780590841282 ) ) ;
#91930=CARTESIAN_POINT ( 'NONE',  ( 3.321969493568678988, 0.9498371968033242352, -1.892263307760349900 ) ) ;
#91932=CARTESIAN_POINT ( 'NONE',  ( 4.387213907293201487, 0.09840592021137170575, 2.068135374880715638 ) ) ;
#91934=CARTESIAN_POINT ( 'NONE',  ( 0.4332924875789189167, -1.481350984940564830, -1.475676199967065338 ) ) ;
#91936=CARTESIAN_POINT ( 'NONE',  ( 5.034128509002383289, 0.9373949799435166153, -1.566401400633938179 ) ) ;
#91942=CARTESIAN_POINT ( 'NONE',  ( 6.586579894266018975, -1.172543786506787145, 1.511232097859278367 ) ) ;
#91951=CARTESIAN_POINT ( 'NONE',  ( 5.483999976877721672, -2.016598147233912730, 0.002826481282774962345 ) ) ;
#91959=CARTESIAN_POINT ( 'NONE',  ( 2.465619613223976270, -0.4363654233677862759, 1.920310867443141278 ) ) ;
#91961=CARTESIAN_POINT ( 'NONE',  ( 3.620720401301917857, 0.2986476686686300175, 1.994069442355271615 ) ) ;
#91963=CARTESIAN_POINT ( 'NONE',  ( 6.727182134110195832, 2.427649464305783322, 2.470530574517680655 ) ) ;
#91964=CARTESIAN_POINT ( 'NONE',  ( 4.207102436150745639, -0.3756362130699179014, 2.158856393654845274 ) ) ;
#91966=CARTESIAN_POINT ( 'NONE',  ( 2.186434445367648749, -1.888794084208703206, -0.3779312967549207092 ) ) ;
#91970=CARTESIAN_POINT ( 'NONE',  ( 0.1329588055935214119, 5.724880713053031478, -2.439996743105294907 ) ) ;
#91976=CARTESIAN_POINT ( 'NONE',  ( 6.427308110136687347, -1.208249125052461181, -1.389453836245766016 ) ) ;
#91977=CARTESIAN_POINT ( 'NONE',  ( 3.281892451336921201, 1.963554472591656053, -0.4431533499722385416 ) ) ;
#91978=CARTESIAN_POINT ( 'NONE',  ( 4.622621100999918298, 0.5092349069827777353, -2.241135911243127055 ) ) ;
#91979=CARTESIAN_POINT ( 'NONE',  ( -0.02900071798684483726, 7.629137130509101361, -2.773797386654376584 ) ) ;
#91980=CARTESIAN_POINT ( 'NONE',  ( 2.676407432925419272, 1.219717815897247259, -1.405545362062944559 ) ) ;
#91983=CARTESIAN_POINT ( 'NONE',  ( 6.521744167503259249, -0.4122283346772101509, 1.874327247564554266 ) ) ;
#91986=CARTESIAN_POINT ( 'NONE',  ( 5.583562150179168349, -0.9389753047652232842, 1.868084059271076347 ) ) ;
#91991=CARTESIAN_POINT ( 'NONE',  ( 6.094358798449852621, -1.717309950877196956, -0.1615796057152525667 ) ) ;
#91993=CARTESIAN_POINT ( 'NONE',  ( 1.494300775288709415, -1.721104260995092838, 0.2117000974225565491 ) ) ;
#91997=CARTESIAN_POINT ( 'NONE',  ( 5.805598453987085072, -1.706804643700374102, -1.341652511797826186 ) ) ;
#91998=CARTESIAN_POINT ( 'NONE',  ( 4.160648861918358143, -1.351394993475165673, 1.227733137840483879 ) ) ;
#91999=CARTESIAN_POINT ( 'NONE',  ( 2.254674508890702089, -0.5182927192734412269, -1.892014123021222627 ) ) ;
#92003=CARTESIAN_POINT ( 'NONE',  ( 3.123802294713691641, -0.4116375371931815796, 2.079978743196985391 ) ) ;
#92009=CARTESIAN_POINT ( 'NONE',  ( 0.5849358142855852760, 1.980036476162419845, 0.6043757699017647811 ) ) ;
#92012=CARTESIAN_POINT ( 'NONE',  ( 3.510577332121900707, -2.218788133798971884, -0.1078075537720973032 ) ) ;
#92014=CARTESIAN_POINT ( 'NONE',  ( 1.020660257703887908, -2.075033540828072454, 0.9893533861183384515 ) ) ;
#92016=CARTESIAN_POINT ( 'NONE',  ( 6.930530977065029852, -1.274000060550171787, 1.622871787371343855 ) ) ;
#92023=CARTESIAN_POINT ( 'NONE',  ( -0.2106725631050307412, 6.947230693896488951, -2.598707507344534040 ) ) ;
#92024=CARTESIAN_POINT ( 'NONE',  ( 2.977275877015468364, 1.638319938685417476, -0.5394319952881917457 ) ) ;
#92025=CARTESIAN_POINT ( 'NONE',  ( 2.237517880698642880, 0.5331670712399002587, -1.944730990508992008 ) ) ;
#92026=CARTESIAN_POINT ( 'NONE',  ( 2.479437202158024878, -2.292751561675594907, -0.1657748548101884711 ) ) ;
#92027=CARTESIAN_POINT ( 'NONE',  ( 3.040562418613635742, 2.244949603584453612, 0.2802003048723368805 ) ) ;
#92028=CARTESIAN_POINT ( 'NONE',  ( 4.793641967770590817, 1.559994068796449529, 1.415095702743226047 ) ) ;
#92030=CARTESIAN_POINT ( 'NONE',  ( 3.708038350156193541, -0.7148330724025107052, -1.619118029916452262 ) ) ;
#92032=CARTESIAN_POINT ( 'NONE',  ( 0.05906008026819106055, -2.050595067678960604, -1.024705011274627431 ) ) ;
#92033=CARTESIAN_POINT ( 'NONE',  ( 5.788959344212086577, 1.397023377451442228, 1.199316859253784839 ) ) ;
#92038=CARTESIAN_POINT ( 'NONE',  ( 5.156268285673103691, -1.588865937562380148, 1.509524371192130676 ) ) ;
#92041=CARTESIAN_POINT ( 'NONE',  ( 5.424307079040114665, 1.017280057988108499, 1.803113764695261523 ) ) ;
#92042=CARTESIAN_POINT ( 'NONE',  ( 0.1984543448181053105, 1.387095780679182377, -1.463931301963219855 ) ) ;
#92044=CARTESIAN_POINT ( 'NONE',  ( 2.859893552614915180, 1.917175687707149967, -0.1893568897016733310 ) ) ;
#92047=CARTESIAN_POINT ( 'NONE',  ( -0.2044637419536878831, -0.1604900674421188000, -2.186121014245277383 ) ) ;
#92056=CARTESIAN_POINT ( 'NONE',  ( 0.8011316787140990714, -1.684513426579350659, 1.005393624328714264 ) ) ;
#92058=CARTESIAN_POINT ( 'NONE',  ( 5.881297811770386907, -0.04968318840743202180, 1.961410508136133712 ) ) ;
#92061=CARTESIAN_POINT ( 'NONE',  ( 6.719591497160966931, -2.098179372288328182, 0.5198544864785522579 ) ) ;
#92062=CARTESIAN_POINT ( 'NONE',  ( -0.2106725631050202496, 0.2307243749109839093, -2.036935839376171842 ) ) ;
#92065=CARTESIAN_POINT ( 'NONE',  ( 0.3154175708385241750, -1.835744252435017598, 0.3582649291258357960 ) ) ;
#92066=CARTESIAN_POINT ( 'NONE',  ( 6.714187037452940210, -1.395258515317991943, -1.029009966057025549 ) ) ;
#92068=CARTESIAN_POINT ( 'NONE',  ( 3.052458795248469414, -1.657928338269051505, 1.433322580492613296 ) ) ;
#92069=CARTESIAN_POINT ( 'NONE',  ( 4.630063564305310742, -1.415688044924306555, -1.822237510073132949 ) ) ;
#92070=CARTESIAN_POINT ( 'NONE',  ( 0.2333700457068142997, -1.884473515381725361, 0.8346939899398809759 ) ) ;
#92071=CARTESIAN_POINT ( 'NONE',  ( 1.904143259493733309, 1.439083257011425587, -1.304092337848123062 ) ) ;
#92075=CARTESIAN_POINT ( 'NONE',  ( 5.256147377898004791, 0.8573370980917979223, -1.939729252509444279 ) ) ;
#92077=CARTESIAN_POINT ( 'NONE',  ( 3.129529892704606464, 0.4926417352555876872, 1.955172657653013957 ) ) ;
#92081=CARTESIAN_POINT ( 'NONE',  ( 1.488595654847742145, -0.2661386877833261111, -1.806066791206423439 ) ) ;
#92087=CARTESIAN_POINT ( 'NONE',  ( 5.260643881022500246, -1.494227509126961451, 1.419604852646045634 ) ) ;
#92093=CARTESIAN_POINT ( 'NONE',  ( 4.512370939326771691, -2.019285345247460839, -0.04732774261236893931 ) ) ;
#92094=CARTESIAN_POINT ( 'NONE',  ( 6.147183147440572704, 0.2149688563512392736, 2.210895739474004529 ) ) ;
#92099=CARTESIAN_POINT ( 'NONE',  ( 4.311438335051980708, -0.3541389166773502573, 2.030069380940119572 ) ) ;
#92100=CARTESIAN_POINT ( 'NONE',  ( 2.356092462967720458, 0.09613450340887133572, -2.014232768679749430 ) ) ;
#92107=CARTESIAN_POINT ( 'NONE',  ( 2.583361055862750000, 1.319027862724517552, -1.524809160041600498 ) ) ;
#92108=CARTESIAN_POINT ( 'NONE',  ( 2.097363409947244683, -1.840767647902554982, 0.04455809990146220728 ) ) ;
#92109=CARTESIAN_POINT ( 'NONE',  ( 0.7335963760657808752, 0.1754145531542888048, 2.301085101356622697 ) ) ;
#92111=CARTESIAN_POINT ( 'NONE',  ( 4.007220386668823409, 1.851715269821294640, 1.114988852100415651 ) ) ;
#92115=CARTESIAN_POINT ( 'NONE',  ( 3.040662745855776006, 2.183360198754655812, -0.7182390863737651010 ) ) ;
#92119=CARTESIAN_POINT ( 'NONE',  ( 1.569004590881704075, 0.1408476687595125731, -1.865417194689425795 ) ) ;
#92120=CARTESIAN_POINT ( 'NONE',  ( 5.119980909927547508, -1.054019455064346689, -1.665871061098343819 ) ) ;
#92125=CARTESIAN_POINT ( 'NONE',  ( 0.2939702064862387276, 1.638257335637434364, 1.478849500172851217 ) ) ;
#92129=CARTESIAN_POINT ( 'NONE',  ( 4.803572714498323570, -0.5265354887679043472, 1.899778226852407936 ) ) ;
#92130=CARTESIAN_POINT ( 'NONE',  ( 5.180430901434020186, -1.285682204016626029, 1.916193241175147666 ) ) ;
#92131=CARTESIAN_POINT ( 'NONE',  ( 6.021894344906984387, 1.833355594513026876, -0.3188260975769128813 ) ) ;
#92132=CARTESIAN_POINT ( 'NONE',  ( 2.659094170149599368, 1.659314987522000795, -1.224949181800268017 ) ) ;
#92139=CARTESIAN_POINT ( 'NONE',  ( 5.354042097475935513, -0.7863316197885154013, 2.023950393233854061 ) ) ;
#92143=CARTESIAN_POINT ( 'NONE',  ( 4.194743914777058436, 1.481411246205705412, 1.093257649623424754 ) ) ;
#92145=CARTESIAN_POINT ( 'NONE',  ( 6.620655732516649294, 2.985444497229528427, 2.280274006979409407 ) ) ;
#92146=CARTESIAN_POINT ( 'NONE',  ( 6.233935805145816467, 2.167428969419796125, 0.3234103439683775894 ) ) ;
#92148=CARTESIAN_POINT ( 'NONE',  ( 0.8786447689848001508, -1.256089115395578659, 1.881495417452299312 ) ) ;
#92154=CARTESIAN_POINT ( 'NONE',  ( 0.5395309102857149819, -1.815710607404594334, 0.6001554849531522962 ) ) ;
#92155=CARTESIAN_POINT ( 'NONE',  ( 1.305125929463516909, -0.4348595813401417987, 1.715451362885108466 ) ) ;
#92156=CARTESIAN_POINT ( 'NONE',  ( 5.707686766122681554, 1.525977179164988540, 1.313104676043591601 ) ) ;
#92158=CARTESIAN_POINT ( 'NONE',  ( 4.208114709606614490, -2.100488694582537619, 0.1524824656061254391 ) ) ;
#92159=CARTESIAN_POINT ( 'NONE',  ( 2.812013442917372430, 1.061847183940438422, -1.594151112820214822 ) ) ;
#92161=CARTESIAN_POINT ( 'NONE',  ( 4.791434771068385778, -1.801603960925775016, 0.7962418042333998525 ) ) ;
#92163=CARTESIAN_POINT ( 'NONE',  ( 5.642833896779382741, 1.947644361699039983, 0.5348221497712030148 ) ) ;
#92164=CARTESIAN_POINT ( 'NONE',  ( 3.151090109352538082, -1.528452604574185525, -1.078222621661927061 ) ) ;
#92165=CARTESIAN_POINT ( 'NONE',  ( 4.793404903408416295, 1.281069664470562142, 1.155212482600373125 ) ) ;
#92166=CARTESIAN_POINT ( 'NONE',  ( 1.599720133015330337, 1.321132142916726204, 1.382909031182079307 ) ) ;
#92168=CARTESIAN_POINT ( 'NONE',  ( 2.297764732281985633, 1.706874461811638044, 1.398895601573101111 ) ) ;
#92172=CARTESIAN_POINT ( 'NONE',  ( 6.408651779211167465, 0.6141799454031526828, 1.863335524608072502 ) ) ;
#92179=CARTESIAN_POINT ( 'NONE',  ( 1.803268859043684058, -1.750145871244257467, 1.105767233283899920 ) ) ;
#92184=CARTESIAN_POINT ( 'NONE',  ( 6.639320575229281651, -0.0007625845807879281287, 2.103388539994067497 ) ) ;
#92192=CARTESIAN_POINT ( 'NONE',  ( 5.097029748277864591, 1.038832625704217527, -1.727738606215820205 ) ) ;
#92193=CARTESIAN_POINT ( 'NONE',  ( 4.926915384452605018, -1.639780065798799757, 0.9903009516807855794 ) ) ;
#92195=CARTESIAN_POINT ( 'NONE',  ( 2.191216702865448784, 1.696344223602393786, 1.387594652289561470 ) ) ;
#92198=CARTESIAN_POINT ( 'NONE',  ( 5.308844932141564499, -0.4931833774270472648, -1.951727149811402828 ) ) ;
#92199=CARTESIAN_POINT ( 'NONE',  ( 1.634869402278725348, 1.785593253932623803, 0.6852637533772618639 ) ) ;
#92202=CARTESIAN_POINT ( 'NONE',  ( 0.4390776481996219727, -1.704952938511293814, -1.076296438737800454 ) ) ;
#92204=CARTESIAN_POINT ( 'NONE',  ( 3.755486520148888729, 2.074727465276064997, -0.2578676962887976321 ) ) ;
#92206=CARTESIAN_POINT ( 'NONE',  ( 2.010387792931751516, 1.280683741330263858, -1.155484876777863379 ) ) ;
#92209=CARTESIAN_POINT ( 'NONE',  ( 0.02680830797223074380, 7.629137130509076492, -2.410890733638766825 ) ) ;
#92215=CARTESIAN_POINT ( 'NONE',  ( 2.912559398657811549, -0.5280806737378342941, -1.732764662445994919 ) ) ;
#92219=CARTESIAN_POINT ( 'NONE',  ( 3.914574264990647201, -0.5719694332564858597, -1.718857104472475861 ) ) ;
#92223=CARTESIAN_POINT ( 'NONE',  ( 3.719077791506773423, -1.640430839875358204, -0.8789487387581331745 ) ) ;
#92224=CARTESIAN_POINT ( 'NONE',  ( 1.722145930190256191, 1.895023070986867619, 0.2790570245742740041 ) ) ;
#92225=CARTESIAN_POINT ( 'NONE',  ( 0.5514207423844892375, 0.5776932562693118944, -1.731835939664846613 ) ) ;
#92233=CARTESIAN_POINT ( 'NONE',  ( 5.242998352400915607, -0.2370019515391492138, -1.955029394545240162 ) ) ;
#92237=CARTESIAN_POINT ( 'NONE',  ( 6.474583112218436298, -0.1034247314782872212, -2.189140632845664403 ) ) ;
#92239=CARTESIAN_POINT ( 'NONE',  ( 5.930678043039342207, 1.856691256794128053, 0.5132231078649931444 ) ) ;
#92242=CARTESIAN_POINT ( 'NONE',  ( 1.096400207583309028, -0.4391605778215034173, -1.771851442210800709 ) ) ;
#92243=CARTESIAN_POINT ( 'NONE',  ( 1.700138637298425737, -0.7412910010123252569, 2.078789392164873906 ) ) ;
#92245=CARTESIAN_POINT ( 'NONE',  ( 1.406358598101828283, -1.903450966454448334, -0.1843715739238485363 ) ) ;
#92247=CARTESIAN_POINT ( 'NONE',  ( 6.983263157960363010, -0.003310164959547181717, 1.953544951557646403 ) ) ;
#92248=CARTESIAN_POINT ( 'NONE',  ( 2.806119653986011819, 1.404935138194723265, -1.341025529631818980 ) ) ;
#92251=CARTESIAN_POINT ( 'NONE',  ( 0.7903884775103054983, -1.915307795730588181, 0.6297756287277083143 ) ) ;
#92253=CARTESIAN_POINT ( 'NONE',  ( 6.614093472281312280, 1.855988364702824800, -0.1360997465041282051 ) ) ;
#92259=CARTESIAN_POINT ( 'NONE',  ( 2.560326853991791829, -1.509077608345666066, 1.589458984681046516 ) ) ;
#92264=CARTESIAN_POINT ( 'NONE',  ( 2.631258204695927194, -1.703542010001803275, 0.6570300758180421807 ) ) ;
#92270=CARTESIAN_POINT ( 'NONE',  ( 1.137189532436083672, -1.741952243817600721, 0.8230948124841385161 ) ) ;
#92271=CARTESIAN_POINT ( 'NONE',  ( 5.295737746731337126, -1.384591195607473235, -1.390005841682784959 ) ) ;
#92275=CARTESIAN_POINT ( 'NONE',  ( 5.214472588068230330, 2.024700573814151028, 0.8392323156421463981 ) ) ;
#92279=CARTESIAN_POINT ( 'NONE',  ( 5.700075226665620498, 0.8442301939139056355, -1.890501578402821847 ) ) ;
#92283=CARTESIAN_POINT ( 'NONE',  ( 5.537770794106480210, -1.814135573521371780, 1.411581493584870728 ) ) ;
#92287=CARTESIAN_POINT ( 'NONE',  ( 0.6391472400242370622, -1.963128197947199727, 1.183262795983427207 ) ) ;
#92290=CARTESIAN_POINT ( 'NONE',  ( 5.208904604407663008, -0.2832176519766657630, 1.921071368630644649 ) ) ;
#92294=CARTESIAN_POINT ( 'NONE',  ( 5.062724140118719518, 0.5608846916410530348, 1.828269531156314853 ) ) ;
#92295=CARTESIAN_POINT ( 'NONE',  ( 6.422847680425099348, 1.611446996373969265, 0.6153535913232581755 ) ) ;
#92296=CARTESIAN_POINT ( 'NONE',  ( 5.366422816783521732, -1.968444216653497003, -0.4370823996120917765 ) ) ;
#92300=CARTESIAN_POINT ( 'NONE',  ( 1.974669457019386787, -0.1036536715517746843, -2.088194013563466012 ) ) ;
#92301=CARTESIAN_POINT ( 'NONE',  ( 0.2503970875498504056, -1.425519035090598852, 1.048718885610238294 ) ) ;
#92302=CARTESIAN_POINT ( 'NONE',  ( 6.276017556857773627, 1.753032240926259311, -0.9962986157117934560 ) ) ;
#92304=CARTESIAN_POINT ( 'NONE',  ( 3.082263327019618249, -2.258438545724365643, -0.3914850642001906356 ) ) ;
#92305=CARTESIAN_POINT ( 'NONE',  ( 1.780815255366276162, 1.198741944763829004, 1.261882163386177869 ) ) ;
#92306=CARTESIAN_POINT ( 'NONE',  ( 3.217144136595586179, 1.669276650691432495, -1.307696563879121365 ) ) ;
#92308=CARTESIAN_POINT ( 'NONE',  ( 1.967715241700284556, 1.438441333088829266, 0.9676545092154006378 ) ) ;
#92310=CARTESIAN_POINT ( 'NONE',  ( 6.350795928397162449, -1.845624747684541989, -0.8128223418941012968 ) ) ;
#92311=CARTESIAN_POINT ( 'NONE',  ( 1.662329954472214322, -0.6657413170317361129, -1.738099805993092106 ) ) ;
#92312=CARTESIAN_POINT ( 'NONE',  ( 2.981114689849233113, 2.043561189653697152, 0.7337040362941152916 ) ) ;
#92313=CARTESIAN_POINT ( 'NONE',  ( 3.643767777461913493, 2.000731686840724333, -0.2516315899964287617 ) ) ;
#92314=CARTESIAN_POINT ( 'NONE',  ( 5.312500000000002665, 1.451031289061327501, 1.451031289060900065 ) ) ;
#92318=CARTESIAN_POINT ( 'NONE',  ( 6.481085492957645577, -0.09751705652460275486, -1.924153034975156995 ) ) ;
#92320=CARTESIAN_POINT ( 'NONE',  ( 3.129344976949835822, 2.009775620968552445, 0.9465212012665072949 ) ) ;
#92325=CARTESIAN_POINT ( 'NONE',  ( 6.486594595706023370, -1.368296875179885852, 1.750867008312809059 ) ) ;
#92327=CARTESIAN_POINT ( 'NONE',  ( 4.809014631063706524, -1.576880339463518022, 1.167019128429528374 ) ) ;
#92331=CARTESIAN_POINT ( 'NONE',  ( 5.993528260394247020, 1.707464403934123798, 1.484360591965392828 ) ) ;
#92332=CARTESIAN_POINT ( 'NONE',  ( 2.471201797017197777, 1.841352583063287529, 0.9297268146766042296 ) ) ;
#92336=CARTESIAN_POINT ( 'NONE',  ( 4.112460492241882370, 1.324567223757302292, -1.321038939096484066 ) ) ;
#92337=CARTESIAN_POINT ( 'NONE',  ( 2.584235440824592001, -0.5423091454765850417, 1.647252552357024280 ) ) ;
#92338=CARTESIAN_POINT ( 'NONE',  ( -0.1112335732281382050, -0.5161050057324081397, -2.242239947022279356 ) ) ;
#92339=CARTESIAN_POINT ( 'NONE',  ( 0.6927435329204565395, -2.190372518412486702, -0.2681103625320201411 ) ) ;
#92340=CARTESIAN_POINT ( 'NONE',  ( 6.210880146794990786, -0.2354563166601444379, 1.927560789186753665 ) ) ;
#92344=CARTESIAN_POINT ( 'NONE',  ( 0.1236729436712938751, 0.3474707636354073537, 1.986100063511665237 ) ) ;
#92345=CARTESIAN_POINT ( 'NONE',  ( 0.1938080739139167730, 1.976361990896974508, -0.7691651810952588875 ) ) ;
#92351=CARTESIAN_POINT ( 'NONE',  ( 4.881388680972560401, 1.702354803207173584, -0.6601141376258444771 ) ) ;
#92352=CARTESIAN_POINT ( 'NONE',  ( 1.993488836774780060, 1.919990754028239488, -1.087721427556323617 ) ) ;
#92357=CARTESIAN_POINT ( 'NONE',  ( 1.002220075199202309, -0.9041908160717628817, 1.806139134770538002 ) ) ;
#92362=CARTESIAN_POINT ( 'NONE',  ( 3.010441868158566958, 0.6223964701937385602, 1.753942229013090159 ) ) ;
#92368=CARTESIAN_POINT ( 'NONE',  ( 4.107882937833263526, -1.820653182827164596, 0.1363937739093170898 ) ) ;
#92371=CARTESIAN_POINT ( 'NONE',  ( 0.9481301099739076754, 1.159027798429014045, 1.289721149823976676 ) ) ;
#92372=CARTESIAN_POINT ( 'NONE',  ( 5.525302006934727395, -1.171079710934025186, -1.420692760577553226 ) ) ;
#92373=CARTESIAN_POINT ( 'NONE',  ( 3.985262446249608903, -0.2245550567474114134, -2.296750103337093396 ) ) ;
#92375=CARTESIAN_POINT ( 'NONE',  ( 0.7728169288007546989, -1.939476032597256872, -0.6969182633713083552 ) ) ;
#92377=CARTESIAN_POINT ( 'NONE',  ( 2.507286712376335824, -1.920573583173491139, 0.2874136252781610001 ) ) ;
#92380=CARTESIAN_POINT ( 'NONE',  ( 5.448667688119189556, 1.537605954158068666, 1.708491323253034100 ) ) ;
#92383=CARTESIAN_POINT ( 'NONE',  ( 5.190257414508706368, -1.856628772771324210, -0.2281712211116558864 ) ) ;
#92385=CARTESIAN_POINT ( 'NONE',  ( 2.214975196874233720, 1.533708969217022933, -1.142120075431733994 ) ) ;
#92387=CARTESIAN_POINT ( 'NONE',  ( 3.422699507934781060, 1.400174360247144589, -1.705827624971032686 ) ) ;
#92389=CARTESIAN_POINT ( 'NONE',  ( 6.883263157960373135, 2.058310207169287143, 2.252834201749584153 ) ) ;
#92392=CARTESIAN_POINT ( 'NONE',  ( 2.204549329899041510, -2.307029201398633322, 0.05716382847485364238 ) ) ;
#92393=CARTESIAN_POINT ( 'NONE',  ( 2.611707774152134842, 0.5260268489151798121, -1.889944157703125072 ) ) ;
#92394=CARTESIAN_POINT ( 'NONE',  ( 6.174688434915334589, 1.389358497796209013, -1.524562697504736164 ) ) ;
#92396=CARTESIAN_POINT ( 'NONE',  ( 3.907435596788138010, -1.928258004016227378, 0.5899861904685861358 ) ) ;
#92399=CARTESIAN_POINT ( 'NONE',  ( 4.487517715496184501, -0.5331711073110931842, 1.944729879240604253 ) ) ;
#92403=CARTESIAN_POINT ( 'NONE',  ( 2.536178501573463695, 1.332599179293973091, 1.713937585783622541 ) ) ;
#92407=CARTESIAN_POINT ( 'NONE',  ( 2.231529376059933956, -1.218349341866202362, -1.419469154777988518 ) ) ;
#92408=CARTESIAN_POINT ( 'NONE',  ( 6.485629946217342123, 1.485420011660616657, 1.570608065930901187 ) ) ;
#92409=CARTESIAN_POINT ( 'NONE',  ( 0.07775346131144458828, -0.005211914751935413023, -2.288974916015192651 ) ) ;
#92413=CARTESIAN_POINT ( 'NONE',  ( 3.281800106729782840, 1.865104756965057620, -0.4213900744019505318 ) ) ;
#92414=CARTESIAN_POINT ( 'NONE',  ( 4.416719503454580753, 1.618597840523916753, 0.7163212975811702465 ) ) ;
#92415=CARTESIAN_POINT ( 'NONE',  ( 1.418461073652961257, -0.6892283116659430053, -1.783923526276688154 ) ) ;
#92418=CARTESIAN_POINT ( 'NONE',  ( -0.2353475280464593089, -0.1482846297235005661, -1.883952934485186415 ) ) ;
#92420=CARTESIAN_POINT ( 'NONE',  ( 1.258353326579707776, -2.070544811992577561, -0.001879966208345739808 ) ) ;
#92422=CARTESIAN_POINT ( 'NONE',  ( 6.649288223980674317, -1.503899034092892162, -1.112267350887645945 ) ) ;
#92423=CARTESIAN_POINT ( 'NONE',  ( 1.471042373949003501, 0.1361147407585860392, -1.820667060309004937 ) ) ;
#92424=CARTESIAN_POINT ( 'NONE',  ( 5.303435803989668074, 1.802500012205746183, 1.273053691228965389 ) ) ;
#92427=CARTESIAN_POINT ( 'NONE',  ( 3.508308746731583216, 2.062851380131548229, 0.002797760368935045105 ) ) ;
#92431=CARTESIAN_POINT ( 'NONE',  ( 0.7905619602705875604, -2.145198653374354336, -0.2653712149464776959 ) ) ;
#92435=CARTESIAN_POINT ( 'NONE',  ( 5.916483165358986440, 0.8355632440216669288, 1.894440869009452300 ) ) ;
#92437=CARTESIAN_POINT ( 'NONE',  ( 3.058072297120766780, 2.151488047868503894, -0.2085137855245971505 ) ) ;
#92439=CARTESIAN_POINT ( 'NONE',  ( 2.983074145627107931, -1.866958838928289399, -0.7709177042417614256 ) ) ;
#92440=CARTESIAN_POINT ( 'NONE',  ( 2.172246964874047670, -0.9220853831424129510, -1.731647142839589648 ) ) ;
#92441=CARTESIAN_POINT ( 'NONE',  ( 6.720655732516649827, 0.5759399164693942419, 2.126764875236677454 ) ) ;
#92448=CARTESIAN_POINT ( 'NONE',  ( 1.376185782568883020, -2.007256511855738612, -0.1928315418098166534 ) ) ;
#92450=CARTESIAN_POINT ( 'NONE',  ( 6.550331612656306035, -1.695486744446069727, 1.388264742925699569 ) ) ;
#92452=CARTESIAN_POINT ( 'NONE',  ( 5.396708386617175890, -1.867154475869851504, -0.4128305108781898936 ) ) ;
#92456=CARTESIAN_POINT ( 'NONE',  ( 2.970327539257538341, -1.987051465770898417, -0.3419137282784574516 ) ) ;
#92458=CARTESIAN_POINT ( 'NONE',  ( 4.840679758638335883, 0.2971110944181546976, 1.698800604571904849 ) ) ;
#92462=CARTESIAN_POINT ( 'NONE',  ( 4.411305886619627081, -0.3218996851035611506, 1.842484647571709822 ) ) ;
#92466=CARTESIAN_POINT ( 'NONE',  ( 0.7958623839904412911, -1.461433461687311253, -1.466603172318406090 ) ) ;
#92470=CARTESIAN_POINT ( 'NONE',  ( -0.01795374796791787686, -2.016030408028956167, -0.04665595434990427171 ) ) ;
#92471=CARTESIAN_POINT ( 'NONE',  ( -0.05289022600267567070, -1.656485410061825592, 0.7338673832079073422 ) ) ;
#92475=CARTESIAN_POINT ( 'NONE',  ( 0.5374593765826127800, 1.831924746014142791, -0.7026076897959919743 ) ) ;
#92477=CARTESIAN_POINT ( 'NONE',  ( 5.026915340915774522, -1.640707562863060520, 0.9885212758144015233 ) ) ;
#92485=CARTESIAN_POINT ( 'NONE',  ( 2.202237438260604030, -2.161223104231101644, 0.05255616829508147347 ) ) ;
#92490=CARTESIAN_POINT ( 'NONE',  ( 4.489149150750438189, 1.630474666268775685, -0.8212668906743822994 ) ) ;
#92492=CARTESIAN_POINT ( 'NONE',  ( 1.036326318785439016, 1.941456103877332140, 0.3412654001589945918 ) ) ;
#92495=CARTESIAN_POINT ( 'NONE',  ( 3.912524032909367566, 0.7067130192578415793, 1.838586846604377323 ) ) ;
#92497=CARTESIAN_POINT ( 'NONE',  ( 5.636261916347573120, 0.3829244189050336478, 1.903776902374450630 ) ) ;
#92501=CARTESIAN_POINT ( 'NONE',  ( 6.152600690169603759, 2.097733681304454034, 0.3095894981632040244 ) ) ;
#92503=CARTESIAN_POINT ( 'NONE',  ( 4.406835678522929456, -0.4222698756407486931, -1.864907683101609370 ) ) ;
#92509=CARTESIAN_POINT ( 'NONE',  ( 4.652993947568984545, 0.3464272572618365964, 1.982917695270119518 ) ) ;
#92511=CARTESIAN_POINT ( 'NONE',  ( 5.760330229460346452, 0.7440287100829169331, 1.667389206893993725 ) ) ;
#92512=CARTESIAN_POINT ( 'NONE',  ( 1.645070734656968625, -0.3017366986639742343, -2.048123538821472245 ) ) ;
#92525=CARTESIAN_POINT ( 'NONE',  ( 4.359819935191601381, -0.006009022472676025205, -1.734343005118470726 ) ) ;
#92527=CARTESIAN_POINT ( 'NONE',  ( 2.887621454190898884, -1.933326653459125355, 0.7409182656877840722 ) ) ;
#92528=CARTESIAN_POINT ( 'NONE',  ( 3.023186137256496764, -1.865899319694108272, 1.000581237753160879 ) ) ;
#92531=CARTESIAN_POINT ( 'NONE',  ( 1.744903480705553012, -0.2836847097360816194, -1.948756091721944861 ) ) ;
#92535=CARTESIAN_POINT ( 'NONE',  ( -0.07025823700084612988, -1.875094440630159065, 0.3749275819610526916 ) ) ;
#92536=CARTESIAN_POINT ( 'NONE',  ( 3.785359544849807190, 1.659571404495253866, 1.581462771572618609 ) ) ;
#92537=CARTESIAN_POINT ( 'NONE',  ( 0.4690313652776016418, 0.1822212253758948297, -1.816563760317004395 ) ) ;
#92541=CARTESIAN_POINT ( 'NONE',  ( 2.197523118450269486, 1.838911438263282738, -0.8198142501213819822 ) ) ;
#92542=CARTESIAN_POINT ( 'NONE',  ( 2.535929169054650156, 1.202975682259961765, 1.549578550289295586 ) ) ;
#92546=CARTESIAN_POINT ( 'NONE',  ( 0.07536363704233395300, 5.720741966631408104, -2.738263776839637398 ) ) ;
#92547=CARTESIAN_POINT ( 'NONE',  ( 5.455056007322736100, 0.4086298902603173744, -2.050129383449701415 ) ) ;
#92548=CARTESIAN_POINT ( 'NONE',  ( 3.695971326421595204, -1.767833007231565334, -0.08711813594433276409 ) ) ;
#92550=CARTESIAN_POINT ( 'NONE',  ( 6.544901331262317434, -1.836973039681317088, -1.370978055005685370 ) ) ;
#92551=CARTESIAN_POINT ( 'NONE',  ( 5.402228116617870946, 1.314032936993884793, -1.141193381800218232 ) ) ;
#92553=CARTESIAN_POINT ( 'NONE',  ( 5.766309430914762224, 2.125181855325126712, -0.8765443895848085143 ) ) ;
#92555=CARTESIAN_POINT ( 'NONE',  ( 6.116466030266402676, 0.5002120791919911769, -1.660072079997718442 ) ) ;
#92556=CARTESIAN_POINT ( 'NONE',  ( 5.846172790272405884, -0.9815748167120906809, 1.936718618010783377 ) ) ;
#92558=CARTESIAN_POINT ( 'NONE',  ( 0.5150563930837145366, 0.1624822992478615336, 2.111197286521369065 ) ) ;
#92559=CARTESIAN_POINT ( 'NONE',  ( 6.437500000220395258, 1.451031294483499545, -1.451031289061371021 ) ) ;
#92561=CARTESIAN_POINT ( 'NONE',  ( 4.489231697071988769, 1.720940496173857470, -0.8657641181536148700 ) ) ;
#92563=CARTESIAN_POINT ( 'NONE',  ( 0.1709645942036420174, 0.8561845417300646410, 2.049862257243968422 ) ) ;
#92568=CARTESIAN_POINT ( 'NONE',  ( 2.702056655550812980, 1.572631313784816687, 1.569006521454456848 ) ) ;
#92574=CARTESIAN_POINT ( 'NONE',  ( 0.2642963535325442703, 1.880433764241522088, -0.7283817610406128074 ) ) ;
#92576=CARTESIAN_POINT ( 'NONE',  ( 5.705554990011762584, -1.623920158085298437, -1.271698733341574350 ) ) ;
#92582=CARTESIAN_POINT ( 'NONE',  ( 0.6668358675281795822, 0.1816249057532189626, -1.760414781625377234 ) ) ;
#92583=CARTESIAN_POINT ( 'NONE',  ( 0.1236729436712938751, 0.3474707636354073537, 1.986100063511665237 ) ) ;
#92584=CARTESIAN_POINT ( 'NONE',  ( 6.163578228761874556, 0.9028020746227163329, 1.487850569839582970 ) ) ;
#92585=CARTESIAN_POINT ( 'NONE',  ( 3.439304851068147428, -1.736875716534720615, -1.496195766483783274 ) ) ;
#92587=CARTESIAN_POINT ( 'NONE',  ( 1.956743257466783570, 0.3155556147324266036, -1.813728304320901596 ) ) ;
#92590=CARTESIAN_POINT ( 'NONE',  ( 2.994927033977520470, 1.566606242385214731, -0.9370212210159312161 ) ) ;
#92591=CARTESIAN_POINT ( 'NONE',  ( 3.445935549842124690, -1.779626424299302956, -0.9480406757386842242 ) ) ;
#92594=CARTESIAN_POINT ( 'NONE',  ( 5.913134528375765697, 1.855721070963678443, 0.9956851948400150532 ) ) ;
#92596=CARTESIAN_POINT ( 'NONE',  ( 2.348173244826061268, -0.8873571809006628452, 1.870714752860686447 ) ) ;
#92599=CARTESIAN_POINT ( 'NONE',  ( 4.951869195850400196, -1.499954228463634243, -1.499123153458590707 ) ) ;
#92600=CARTESIAN_POINT ( 'NONE',  ( 0.4340449649811276012, 0.9916047912509761142, -1.651568591070247116 ) ) ;
#92606=CARTESIAN_POINT ( 'NONE',  ( -0.1750823283547575382, -0.9565501389544858180, -2.002587789130043205 ) ) ;
#92607=CARTESIAN_POINT ( 'NONE',  ( 2.292140615954643579, -0.9012634372634602542, 1.903512165690796065 ) ) ;
#92610=CARTESIAN_POINT ( 'NONE',  ( 6.807467476049567701, -1.494282888040651347, -1.108890849153229441 ) ) ;
#92617=CARTESIAN_POINT ( 'NONE',  ( 0.4223351350958382544, -2.109807164369668087, 0.2139620856976830743 ) ) ;
#92620=CARTESIAN_POINT ( 'NONE',  ( 3.789464544343919883, -1.813617537123424661, 0.7486148740368094856 ) ) ;
#92621=CARTESIAN_POINT ( 'NONE',  ( 1.463986924769441478, 2.129665692569195024, -0.3698555562515608020 ) ) ;
#92625=CARTESIAN_POINT ( 'NONE',  ( 2.624636096055412704, -1.623921194558699765, 0.6262662122848341451 ) ) ;
#92630=CARTESIAN_POINT ( 'NONE',  ( 2.583361055862750000, 1.319027862724517552, -1.524809160041600498 ) ) ;
#92631=CARTESIAN_POINT ( 'NONE',  ( 6.825078400183551608, 4.689370880799383912, 2.706890346843467299 ) ) ;
#92633=CARTESIAN_POINT ( 'NONE',  ( 1.850399468497238242, 0.6164509289473228959, 1.872685729773468255 ) ) ;
#92634=CARTESIAN_POINT ( 'NONE',  ( 6.099862406061942188, 1.323743610676546334, 1.380425988546908567 ) ) ;
#92639=CARTESIAN_POINT ( 'NONE',  ( 0.6276103948988649428, -0.2939658443398012744, 1.998026100167526575 ) ) ;
#92640=CARTESIAN_POINT ( 'NONE',  ( 5.965930945686983122, 2.274828880937030728, -0.3866611637039600313 ) ) ;
#92641=CARTESIAN_POINT ( 'NONE',  ( 5.617619635959271385, 0.3843197845415853853, -1.923678648292715732 ) ) ;
#92643=CARTESIAN_POINT ( 'NONE',  ( 3.291801117278610800, -1.314073873198824627, -1.456807609480186061 ) ) ;
#92645=CARTESIAN_POINT ( 'NONE',  ( 1.160779977835691312, 1.203355533934968635, 1.617816888933524710 ) ) ;
#92647=CARTESIAN_POINT ( 'NONE',  ( 0.7259617406208430657, 0.8522569803141609723, -1.938411259892757421 ) ) ;
#92650=CARTESIAN_POINT ( 'NONE',  ( 1.657894046870052485, -1.302874822933766774, 1.301145727299134025 ) ) ;
#92653=CARTESIAN_POINT ( 'NONE',  ( 3.463236921083117981, -1.731491641549892435, 1.224000437801611163 ) ) ;
#92657=CARTESIAN_POINT ( 'NONE',  ( 4.815729912100211507, -2.021797975182148654, 0.3980178507551126454 ) ) ;
#92659=CARTESIAN_POINT ( 'NONE',  ( 1.610644152589552958, -0.2245515952020246675, 1.827417025815617935 ) ) ;
#92663=CARTESIAN_POINT ( 'NONE',  ( 1.207977004800918852, -0.5332226995428279714, 2.141375170867452660 ) ) ;
#92664=CARTESIAN_POINT ( 'NONE',  ( 2.161739655719534081, 0.3883039046224411317, -2.228698702525088393 ) ) ;
#92666=CARTESIAN_POINT ( 'NONE',  ( 2.496125854487367235, -0.9279945471987390837, 1.555666070890851627 ) ) ;
#92667=CARTESIAN_POINT ( 'NONE',  ( 2.887788952342277948, -1.913322710806207194, 0.09880452340514658816 ) ) ;
#92668=CARTESIAN_POINT ( 'NONE',  ( 3.684089399883890614, -1.230936008959164996, -1.664559344884769088 ) ) ;
#92670=CARTESIAN_POINT ( 'NONE',  ( 2.834795904189919558, 0.2398841137210059038, 1.956746676604983248 ) ) ;
#92671=CARTESIAN_POINT ( 'NONE',  ( 6.234985708453399944, 0.1916802727454213762, 1.916943350541326030 ) ) ;
#92672=CARTESIAN_POINT ( 'NONE',  ( 4.170664822833985319, -1.745344833062393075, -0.6735866001992969476 ) ) ;
#92673=CARTESIAN_POINT ( 'NONE',  ( 2.086955060466778811, -2.263696646927360501, -0.4477047476570076290 ) ) ;
#92675=CARTESIAN_POINT ( 'NONE',  ( 3.349909636924102596, -0.7564274094383013347, 1.700591413421480125 ) ) ;
#92680=CARTESIAN_POINT ( 'NONE',  ( 0.5046868689226053917, -0.7117215327378585421, -1.982300686916990573 ) ) ;
#92682=CARTESIAN_POINT ( 'NONE',  ( 6.485629946217342123, 1.485420011660616879, 1.570608065930901187 ) ) ;
#92683=CARTESIAN_POINT ( 'NONE',  ( 0.1233147457768641181, 1.759488896278412540, 0.9916404401272023161 ) ) ;
#92688=CARTESIAN_POINT ( 'NONE',  ( 6.925078400183547700, 0.5992389604297322370, 1.809181922849491198 ) ) ;
#92691=CARTESIAN_POINT ( 'NONE',  ( 4.540250091716044878, 0.7762272601403925609, 1.861345588084816871 ) ) ;
#92695=CARTESIAN_POINT ( 'NONE',  ( 5.998930166150279852, 1.769978137569449883, -1.240765152474863520 ) ) ;
#92699=CARTESIAN_POINT ( 'NONE',  ( 6.204703874486805049, 1.882480396761162744, 0.7231267579426368108 ) ) ;
#92703=CARTESIAN_POINT ( 'NONE',  ( 2.806937704738516448, 1.457146550840708210, 0.9226662414157487113 ) ) ;
#92707=CARTESIAN_POINT ( 'NONE',  ( 0.8425835904034431056, -1.521979116790536768, 0.9028166612478020214 ) ) ;
#92708=CARTESIAN_POINT ( 'NONE',  ( 2.420566579892877268, -0.7724838186086988578, -1.859170112617714699 ) ) ;
#92710=CARTESIAN_POINT ( 'NONE',  ( 4.665167916288286420, -1.969490514480085164, -0.9956290437203789701 ) ) ;
#92712=CARTESIAN_POINT ( 'NONE',  ( 4.873980352634836422, -2.130485078384927178, 0.4170503277054308788 ) ) ;
#92716=CARTESIAN_POINT ( 'NONE',  ( 2.772263606761758759, 2.110060413066455975, -0.2101530891244970389 ) ) ;
#92717=CARTESIAN_POINT ( 'NONE',  ( 2.372672929649359386, -0.3474902101525711995, -1.986097784353996643 ) ) ;
#92718=CARTESIAN_POINT ( 'NONE',  ( 3.515680188161012687, -0.5209108127710823100, 1.735096886039680930 ) ) ;
#92722=CARTESIAN_POINT ( 'NONE',  ( 0.8306673739700667358, 0.1335802410974036292, 1.865940672528036304 ) ) ;
#92723=CARTESIAN_POINT ( 'NONE',  ( 5.725187622324654946, -0.04035785615889506128, 1.825416780793003069 ) ) ;
#92725=CARTESIAN_POINT ( 'NONE',  ( 1.551812156574260637, 0.9880582627100834570, 1.641127140810652252 ) ) ;
#92734=CARTESIAN_POINT ( 'NONE',  ( 3.146849984228027974, 2.069795010335002239, 0.4607391970517027979 ) ) ;
#92737=CARTESIAN_POINT ( 'NONE',  ( 4.973880039175529788, 1.132619354422999436, 1.613344424267410204 ) ) ;
#92738=CARTESIAN_POINT ( 'NONE',  ( 6.117437049485344502, 1.593764408019750389, 1.056661447057717362 ) ) ;
#92740=CARTESIAN_POINT ( 'NONE',  ( -0.0001774970986804374768, -2.075397304607224047, 0.4179963677126071753 ) ) ;
#92743=CARTESIAN_POINT ( 'NONE',  ( 2.066927875543830950, 1.535623996113824496, -1.388825173883188713 ) ) ;
#92744=CARTESIAN_POINT ( 'NONE',  ( 2.712754350931959380, -0.1900897480172674958, 1.932619341894822540 ) ) ;
#92748=CARTESIAN_POINT ( 'NONE',  ( 3.468770583794348550, 0.05092928562340763576, -2.090184462658881248 ) ) ;
#92751=CARTESIAN_POINT ( 'NONE',  ( 0.8206315121990900296, 1.372318096965993384, -1.182507040619881877 ) ) ;
#92753=CARTESIAN_POINT ( 'NONE',  ( 5.233140740401229785, 0.1595256157847015632, 2.201181388321731713 ) ) ;
#92755=CARTESIAN_POINT ( 'NONE',  ( 3.364504783244476993, 0.9904720576699842516, 1.972067388187691339 ) ) ;
#92758=CARTESIAN_POINT ( 'NONE',  ( 1.980978873585538480, -1.748965405663160944, -0.7736543689686598002 ) ) ;
#92761=CARTESIAN_POINT ( 'NONE',  ( 5.002425025097493538, 2.064580399062130311, 0.1557331365308264881 ) ) ;
#92763=CARTESIAN_POINT ( 'NONE',  ( 3.221700144506876917, -2.083771231579465866, 0.5749860669421112958 ) ) ;
#92764=CARTESIAN_POINT ( 'NONE',  ( 4.652002595327206613, 0.8389548150543740812, 2.024815518666116088 ) ) ;
#92766=CARTESIAN_POINT ( 'NONE',  ( -0.1296875068448159751, 0.001480089298542403009, -1.826395826379861864 ) ) ;
#92776=CARTESIAN_POINT ( 'NONE',  ( 5.893440691016273547, -1.874049447596724427, 0.8799615681738190975 ) ) ;
#92777=CARTESIAN_POINT ( 'NONE',  ( 3.984924265943972532, -0.1901312170250069600, -1.917098255223735004 ) ) ;
#92778=CARTESIAN_POINT ( 'NONE',  ( 0.2984541275833849094, 1.388471424577278235, -1.462460896543740674 ) ) ;
#92781=CARTESIAN_POINT ( 'NONE',  ( 5.032068834786890044, 1.130672129898707245, 1.612349476345806831 ) ) ;
#92782=CARTESIAN_POINT ( 'NONE',  ( 0.3401085955914601722, 2.185883683461706362, 0.1570275565265024931 ) ) ;
#92783=CARTESIAN_POINT ( 'NONE',  ( 5.145057536039753465, -1.563975785779356587, 0.9416349707431560523 ) ) ;
#92789=CARTESIAN_POINT ( 'NONE',  ( 2.331387312403776946, 0.8663521307504215008, -1.624669977836174839 ) ) ;
#92790=CARTESIAN_POINT ( 'NONE',  ( 5.853776559028295523, -1.461190594579380608, -1.385140169207878413 ) ) ;
#92791=CARTESIAN_POINT ( 'NONE',  ( 1.212782571277282395, -1.812964642495185963, -1.412582873482233659 ) ) ;
#92792=CARTESIAN_POINT ( 'NONE',  ( 5.102378460580520247, 1.956245014681293970, 0.1482201060269832671 ) ) ;
#92796=CARTESIAN_POINT ( 'NONE',  ( 0.8189040078958352842, -1.500748464528355974, 1.426492703164506937 ) ) ;
#92798=CARTESIAN_POINT ( 'NONE',  ( 1.839510613029649466, 0.7972044211956804682, -1.932997742640076400 ) ) ;
#92799=CARTESIAN_POINT ( 'NONE',  ( 6.614108672291515667, -0.8387186360741160085, -1.558468296174354784 ) ) ;
#92802=CARTESIAN_POINT ( 'NONE',  ( 1.733560280482333571, 1.721479560191770730, 0.2551580012965410371 ) ) ;
#92807=CARTESIAN_POINT ( 'NONE',  ( 2.349869733406087402, 1.724505987646451688, 0.04327962033413671611 ) ) ;
#92809=CARTESIAN_POINT ( 'NONE',  ( 2.525153347276567484, -2.043736813514348771, 0.7916865192442237298 ) ) ;
#92810=CARTESIAN_POINT ( 'NONE',  ( 5.074942902252104204, -2.077123540546990110, -0.7459609299403434646 ) ) ;
#92812=CARTESIAN_POINT ( 'NONE',  ( 2.184662588793543136, 1.252765144364040850, -1.772974741507940211 ) ) ;
#92813=CARTESIAN_POINT ( 'NONE',  ( 1.629252094361890890, -1.719607636260962025, 0.6136192449261099746 ) ) ;
#92814=CARTESIAN_POINT ( 'NONE',  ( 3.503210936237437068, -0.1516218309994079028, 2.111938774394610974 ) ) ;
#92817=CARTESIAN_POINT ( 'NONE',  ( 3.913864042289341150, -1.178888685321772156, -1.965896434285055117 ) ) ;
#92821=CARTESIAN_POINT ( 'NONE',  ( 6.305373609846285810, 1.934184411435871498, -1.092212275460135773 ) ) ;
#92828=CARTESIAN_POINT ( 'NONE',  ( 4.201796189063250253, 1.844709454618495670, 0.8146275914719460776 ) ) ;
#92830=CARTESIAN_POINT ( 'NONE',  ( 2.518489969072700507, 0.8780072382167501965, 1.866465334303254897 ) ) ;
#92835=CARTESIAN_POINT ( 'NONE',  ( 6.246043798300164873, 0.6838514278588082584, 2.082077653496945402 ) ) ;
#92836=CARTESIAN_POINT ( 'NONE',  ( 3.938125092175647879, -1.678004675797317713, -1.117833462672225497 ) ) ;
#92837=CARTESIAN_POINT ( 'NONE',  ( 2.348939331405873077, 0.4892633877765646400, -1.774999737812533063 ) ) ;
#92840=CARTESIAN_POINT ( 'NONE',  ( 6.387720234973090605, 1.261301916940280154, 1.320039730931761524 ) ) ;
#92841=CARTESIAN_POINT ( 'NONE',  ( -0.1335965759122420549, -0.1551069838626080166, -2.263292908747056131 ) ) ;
#92843=CARTESIAN_POINT ( 'NONE',  ( 5.823173511171203742, -0.06224829877122214916, 2.261828766561886361 ) ) ;
#92845=CARTESIAN_POINT ( 'NONE',  ( 2.192140752285096639, -0.8994906754480420652, 1.904460908831892008 ) ) ;
#92854=CARTESIAN_POINT ( 'NONE',  ( 3.076664410187186505, 1.002321471918452556, 1.982530577833590879 ) ) ;
#92855=CARTESIAN_POINT ( 'NONE',  ( 0.01274299142895937362, -0.9473294304004549193, -1.991142614049784099 ) ) ;
#92858=CARTESIAN_POINT ( 'NONE',  ( 4.017981030900905637, 1.947309607215493621, -0.2378496960543720617 ) ) ;
#92867=CARTESIAN_POINT ( 'NONE',  ( 3.937823072884456099, -2.028283017459261650, 0.6187693826033290323 ) ) ;
#92869=CARTESIAN_POINT ( 'NONE',  ( 4.241217004700631676, -1.882188537963986219, 1.063020064016991117 ) ) ;
#92870=CARTESIAN_POINT ( 'NONE',  ( 3.790429961727882713, 1.553415782126759792, -0.9881970032953185656 ) ) ;
#92873=CARTESIAN_POINT ( 'NONE',  ( 5.911982399937937949, 1.163873415549965262, -1.294066288734674997 ) ) ;
#92874=CARTESIAN_POINT ( 'NONE',  ( 6.827182134110207024, 2.985003573113382824, 2.264833014350222662 ) ) ;
#92877=EDGE_CURVE ( 'NONE', #185672, #92893, #163936, .T. ) ;
#92878=CARTESIAN_POINT ( 'NONE',  ( 2.905317003618158367, 1.825515667692039878, 1.157497049167732550 ) ) ;
#92879=CARTESIAN_POINT ( 'NONE',  ( 5.888046020683160187, -0.05228737891407529703, 2.015604419750731680 ) ) ;
#92882=CARTESIAN_POINT ( 'NONE',  ( 2.044033295145482043, 0.8276103948961744949, -1.997198329219296742 ) ) ;
#92883=CARTESIAN_POINT ( 'NONE',  ( 3.251204012874517879, -1.609649185575717123, -1.137836448096725794 ) ) ;
#92885=CARTESIAN_POINT ( 'NONE',  ( 0.9390046912478089425, 2.274041295854188238, 0.3912414073941206105 ) ) ;
#92886=CARTESIAN_POINT ( 'NONE',  ( 4.247558953154553230, 1.941557341479711152, -0.05109960196620494388 ) ) ;
#92891=CARTESIAN_POINT ( 'NONE',  ( -0.02244404828157658613, -0.004869073801674199918, -2.189079685368473527 ) ) ;
#92893=VERTEX_POINT ( 'NONE', #210703 ) ;
#92895=CARTESIAN_POINT ( 'NONE',  ( 2.397764582540245382, 1.705505620506567510, 1.400368488499253994 ) ) ;
#92897=CARTESIAN_POINT ( 'NONE',  ( 6.262552437187629550, -0.7028992384056665932, -1.831702256219314151 ) ) ;
#92901=CARTESIAN_POINT ( 'NONE',  ( 0.1749903794560749015, 6.948553613792602057, -2.550375946188668586 ) ) ;
#92903=CARTESIAN_POINT ( 'NONE',  ( 5.419803763747102821, 1.093575605593154920, -1.481025086994464113 ) ) ;
#92908=CARTESIAN_POINT ( 'NONE',  ( 6.047156637250688860, 0.2094617991648151656, 2.110256208591613003 ) ) ;
#92911=CARTESIAN_POINT ( 'NONE',  ( 0.4091470207043126917, 1.792883176943863122, 1.016159331636699470 ) ) ;
#92913=CARTESIAN_POINT ( 'NONE',  ( 1.978732740145513480, 1.735006779315110492, 0.6737207639663128633 ) ) ;
#92914=CARTESIAN_POINT ( 'NONE',  ( 5.038538826285253514, -1.576363729006284187, 0.9512496309353533075 ) ) ;
#92921=CARTESIAN_POINT ( 'NONE',  ( 4.582781371344160526, -2.140174514510746029, -0.5380331057033281850 ) ) ;
#92922=CARTESIAN_POINT ( 'NONE',  ( 6.468092748254181679, 1.154776641680499205, 1.945382213218769252 ) ) ;
#92924=CARTESIAN_POINT ( 'NONE',  ( 6.240474538790502734, 1.035194401182498281, -1.486496517754380742 ) ) ;
#92925=CARTESIAN_POINT ( 'NONE',  ( 6.157445398352582977, 1.830988975552667153, -0.5633538272611648967 ) ) ;
#92928=CARTESIAN_POINT ( 'NONE',  ( 0.07536363704233400851, 2.864322694550157422, -2.632457840217193645 ) ) ;
#92929=CARTESIAN_POINT ( 'NONE',  ( 6.147114339676178041, 0.1922309238813116050, 1.902605946959089689 ) ) ;
#92931=CARTESIAN_POINT ( 'NONE',  ( 1.270139834521961886, -1.189467451172643964, 1.443775233441677130 ) ) ;
#92932=CARTESIAN_POINT ( 'NONE',  ( 1.903530124611974017, -1.954778955200174861, 0.4946342604733033887 ) ) ;
#92934=CARTESIAN_POINT ( 'NONE',  ( 4.002637171539184635, -0.6605693356034693098, -1.999858192447926397 ) ) ;
#92939=CARTESIAN_POINT ( 'NONE',  ( 2.707290811070970804, 1.730213373471348737, -1.041854834777849126 ) ) ;
#92942=CARTESIAN_POINT ( 'NONE',  ( 3.972077263441410100, 1.197190051160206936, 1.799587594625361220 ) ) ;
#92948=CARTESIAN_POINT ( 'NONE',  ( 2.154941862968827504, -0.5775488349282401623, -2.092905974620140164 ) ) ;
#92951=CARTESIAN_POINT ( 'NONE',  ( 0.6965153189463432204, 1.505040478001760107, 1.060415605250275339 ) ) ;
#92953=CARTESIAN_POINT ( 'NONE',  ( 2.454835928891830221, -1.908367152989149718, -1.077367144120815023 ) ) ;
#92954=CARTESIAN_POINT ( 'NONE',  ( 6.983263157960386991, 6.036006179461032239, 2.548702536770989457 ) ) ;
#92955=CARTESIAN_POINT ( 'NONE',  ( 4.030342351814687696, 1.213150246598847293, -1.909612865279747052 ) ) ;
#92962=CARTESIAN_POINT ( 'NONE',  ( 4.499107683057060214, 1.420662411309661088, 1.055048638519467286 ) ) ;
#92964=CARTESIAN_POINT ( 'NONE',  ( 0.7277292075377658209, -1.999665741513008799, 0.6608504825312794262 ) ) ;
#92969=CARTESIAN_POINT ( 'NONE',  ( 6.275017575846199236, 1.753023089329442064, -0.9963169848806670004 ) ) ;
#92973=CARTESIAN_POINT ( 'NONE',  ( 3.309304339999539657, -0.3661640501408692794, 1.834289908569000538 ) ) ;
#92974=CARTESIAN_POINT ( 'NONE',  ( 4.680570891794395116, 1.277791010243028991, -1.628752506732597638 ) ) ;
#92983=CARTESIAN_POINT ( 'NONE',  ( 3.789464544343919883, -1.813617537123424661, 0.7486148740368094856 ) ) ;
#92984=CARTESIAN_POINT ( 'NONE',  ( 0.7376574009502724349, -1.897405874265755354, -0.6818954202830116440 ) ) ;
#92987=CARTESIAN_POINT ( 'NONE',  ( 0.4560483712790652233, 0.7097975879313439540, 1.730851494400275747 ) ) ;
#92989=CARTESIAN_POINT ( 'NONE',  ( 3.006110871101048687, -0.8120814715368419590, 1.842311383860009588 ) ) ;
#92991=CARTESIAN_POINT ( 'NONE',  ( 3.040728130433269616, -1.601530262690466389, 1.384902248896832333 ) ) ;
#92994=CARTESIAN_POINT ( 'NONE',  ( 5.090316257491098284, 1.067296284200716983, -1.773933887923849984 ) ) ;
#92996=CARTESIAN_POINT ( 'NONE',  ( 0.2047783418026409563, 1.821168281471240435, 1.026754182986739927 ) ) ;
#92998=CARTESIAN_POINT ( 'NONE',  ( 5.456004705108882469, 1.823398332572896186, -0.09148835057352226741 ) ) ;
#93005=CARTESIAN_POINT ( 'NONE',  ( 6.569012486276131213, -1.474873517498687558, 1.216900358440069052 ) ) ;
#93015=CARTESIAN_POINT ( 'NONE',  ( -0.02299388927990211537, 2.886218872804919400, -2.399728103386359557 ) ) ;
#93024=CARTESIAN_POINT ( 'NONE',  ( 2.008593398387849671, 0.6130636034600014383, 1.871695086544410636 ) ) ;
#93025=CARTESIAN_POINT ( 'NONE',  ( 3.321888824615967906, 0.9040932542298124597, -1.802426844439278142 ) ) ;
#93027=CARTESIAN_POINT ( 'NONE',  ( 6.827182134110223011, 1.235230467647760788, 2.302354205009625954 ) ) ;
#93028=CARTESIAN_POINT ( 'NONE',  ( 3.468858241077877214, 0.05382521638562161315, -2.190950023606648145 ) ) ;
#93030=CARTESIAN_POINT ( 'NONE',  ( 1.746969779936607292, -1.628684531152933657, 1.028491977540356705 ) ) ;
#93033=CARTESIAN_POINT ( 'NONE',  ( 0.2329586101569528500, 5.725166970077667727, -2.439795138137319963 ) ) ;
#93039=CARTESIAN_POINT ( 'NONE',  ( 6.585540641348407220, -0.7802508550805786758, 1.666130356082275998 ) ) ;
#93040=CARTESIAN_POINT ( 'NONE',  ( 2.719391910328097683, 1.701792079550172421, 1.075097526896612088 ) ) ;
#93041=CARTESIAN_POINT ( 'NONE',  ( 4.200743080572525656, -1.581147070632774598, -1.668312408496865684 ) ) ;
#93042=CARTESIAN_POINT ( 'NONE',  ( -0.1288028175206907822, 6.946859453142047336, -2.869069570226709498 ) ) ;
#93043=CARTESIAN_POINT ( 'NONE',  ( 1.920531177235841103, -1.320465346956477992, 1.311572250416197960 ) ) ;
#93046=CARTESIAN_POINT ( 'NONE',  ( 6.275647926998929371, 0.3200337115364471074, -1.885262484646982095 ) ) ;
#93049=CARTESIAN_POINT ( 'NONE',  ( 4.915614241032515430, -1.119620181645267776, -1.765504464341709934 ) ) ;
#93050=CARTESIAN_POINT ( 'NONE',  ( 4.082764389539480732, -0.1829629792115642917, -1.861669828791753467 ) ) ;
#93056=CARTESIAN_POINT ( 'NONE',  ( 5.637229722410256549, -1.556708995667484441, 0.7431856355405024317 ) ) ;
#93058=CARTESIAN_POINT ( 'NONE',  ( 1.968989728591052479, -1.700769290752032870, -0.3374826141460812168 ) ) ;
#93061=CARTESIAN_POINT ( 'NONE',  ( 6.420782495146515778, -1.541274310347956922, 1.529322475779694601 ) ) ;
#93062=CARTESIAN_POINT ( 'NONE',  ( 3.984828715814022981, -0.1808549858164226476, -1.816707794649790708 ) ) ;
#93063=CARTESIAN_POINT ( 'NONE',  ( 2.588659458060487584, 1.901619664775334728, 0.4814403318105645591 ) ) ;
#93066=CARTESIAN_POINT ( 'NONE',  ( 2.385534290476189145, 0.1013982516714604792, -2.118174289320504666 ) ) ;
#93071=CARTESIAN_POINT ( 'NONE',  ( 0.6903901511902330590, 1.067356595782501749, -1.773781848916009096 ) ) ;
#93074=CARTESIAN_POINT ( 'NONE',  ( 3.440272213978716742, -1.324219266349660806, -1.783276862766651760 ) ) ;
#93076=CARTESIAN_POINT ( 'NONE',  ( 0.7745980011552360267, 2.023606461939434720, -1.090472508649400263 ) ) ;
#93078=CARTESIAN_POINT ( 'NONE',  ( 6.807491137956053429, -1.653082740107037152, -1.233284719700310506 ) ) ;
#93081=CARTESIAN_POINT ( 'NONE',  ( 0.1331565106231329398, 0.7299000548664087429, -2.029785554894456556 ) ) ;
#93082=CARTESIAN_POINT ( 'NONE',  ( 5.636236351835953506, 0.3653394402399374741, 1.804471444190151930 ) ) ;
#93084=CARTESIAN_POINT ( 'NONE',  ( -0.1104750535120234134, 0.7027814200676918421, -2.185477693842474256 ) ) ;
#93085=CARTESIAN_POINT ( 'NONE',  ( 2.467434050970338077, 1.692020480068063826, -0.3335236308374764369 ) ) ;
#93086=CARTESIAN_POINT ( 'NONE',  ( 1.182827746461931229, 1.645757370610765102, -1.164989914844760444 ) ) ;
#93088=CARTESIAN_POINT ( 'NONE',  ( 2.760663040853128525, 2.181856774409622890, -0.7236605881647265592 ) ) ;
#93089=CARTESIAN_POINT ( 'NONE',  ( 1.827766392559232012, -2.130618655838847353, 0.7612957800654009954 ) ) ;
#93090=CARTESIAN_POINT ( 'NONE',  ( 4.863951442137788739, 2.083289488599335826, -0.3080729427491457062 ) ) ;
#93092=CARTESIAN_POINT ( 'NONE',  ( 3.479546766767865673, 1.120508650343427171, 1.369845563140754230 ) ) ;
#93094=CARTESIAN_POINT ( 'NONE',  ( 6.462434034201492317, -2.093801447487374734, -0.9336288876484639676 ) ) ;
#93095=CARTESIAN_POINT ( 'NONE',  ( 4.452959842461719830, 0.4008590389125502029, -1.796806262838637647 ) ) ;
#93099=CARTESIAN_POINT ( 'NONE',  ( 4.418054252288761141, 1.349281245414082342, -1.726737887558588591 ) ) ;
#93102=CARTESIAN_POINT ( 'NONE',  ( 4.598136200040512378, 0.8882050449813773119, -1.870312673664726644 ) ) ;
#93103=CARTESIAN_POINT ( 'NONE',  ( 0.4797043241997685503, -0.7212876333932433104, 1.883314553594167107 ) ) ;
#93105=CARTESIAN_POINT ( 'NONE',  ( 3.686086919817387564, -0.9488725894866935073, 1.676545010912360745 ) ) ;
#93108=CARTESIAN_POINT ( 'NONE',  ( 6.345950370838200350, -1.386202306585911925, -1.604841549997563455 ) ) ;
#93111=DIRECTION ( 'NONE',  ( 1.039099362110107450E-15, 1.000000000000000000, -4.583713267641621330E-32 ) ) ;
#93118=CARTESIAN_POINT ( 'NONE',  ( 1.609737659951641309, 0.5726723138891122167, -1.876404140693301636 ) ) ;
#93120=( GEOMETRIC_REPRESENTATION_CONTEXT ( 3 ) GLOBAL_UNCERTAINTY_ASSIGNED_CONTEXT ( ( #180772 ) ) GLOBAL_UNIT_ASSIGNED_CONTEXT ( ( #67595, #68671, #37264 ) ) REPRESENTATION_CONTEXT ( 'NONE', 'WORKASPACE' ) );
#93123=CARTESIAN_POINT ( 'NONE',  ( 5.072687121480487171, 1.354251660176824856, -1.419695456575476689 ) ) ;
#93126=CARTESIAN_POINT ( 'NONE',  ( 0.1458946441583548470, -1.751458424797154523, -1.431810583859528974 ) ) ;
#93130=CARTESIAN_POINT ( 'NONE',  ( 0.4033012769992084245, -0.5052730135347226481, 1.800932346938296069 ) ) ;
#93131=CARTESIAN_POINT ( 'NONE',  ( 6.749374558768074017, -1.701276501228730309, -0.3333242692393871831 ) ) ;
#93133=CARTESIAN_POINT ( 'NONE',  ( 2.613028500285840661, -0.2118117899099076218, 2.181281865515646068 ) ) ;
#93134=CARTESIAN_POINT ( 'NONE',  ( 4.805897800482852311, -0.6205396350037055697, 2.222522205952178975 ) ) ;
#93135=CARTESIAN_POINT ( 'NONE',  ( 5.694623797941932963, -0.4965738858758206309, -1.999944147208564171 ) ) ;
#93136=CARTESIAN_POINT ( 'NONE',  ( 1.763517528630250686, 0.9983118466501934574, 1.665567687315899992 ) ) ;
#93140=CARTESIAN_POINT ( 'NONE',  ( 4.939744792934912532, -2.012803497507458683, 0.6676120485993168874 ) ) ;
#93141=CARTESIAN_POINT ( 'NONE',  ( 2.250625165576759290, 1.976955744075848065, -0.3961026872240576702 ) ) ;
#93143=CARTESIAN_POINT ( 'NONE',  ( 5.350674426004140116, 0.6359874849255696683, 2.113150234885258438 ) ) ;
#93146=CARTESIAN_POINT ( 'NONE',  ( 0.2756506080626683342, 1.048234779247591453, 1.494575289200591239 ) ) ;
#93152=CARTESIAN_POINT ( 'NONE',  ( 5.366112562010656895, 1.013659120426290361, 1.794278544449072088 ) ) ;
#93157=CARTESIAN_POINT ( 'NONE',  ( 4.477216424163804831, -1.805109318760585779, -0.9060198856494814379 ) ) ;
#93163=CARTESIAN_POINT ( 'NONE',  ( 4.118082307656718122, -1.057753326809774963, -1.768578378466668877 ) ) ;
#93164=CARTESIAN_POINT ( 'NONE',  ( 2.320935597664942396, 0.9480396085976349196, -1.779626998253575509 ) ) ;
#93172=CARTESIAN_POINT ( 'NONE',  ( 3.093124880496417983, 1.122326866504215426, -1.674630914042275709 ) ) ;
#93173=CARTESIAN_POINT ( 'NONE',  ( 2.519273208346615167, -1.059988974693906183, -1.505194322970206722 ) ) ;
#93175=CARTESIAN_POINT ( 'NONE',  ( 0.5226545517994193313, -1.239659060731788998, -1.946298918093934960 ) ) ;
#93177=CARTESIAN_POINT ( 'NONE',  ( 2.776834730583700228, -2.067601613962879448, -0.6303956341740593050 ) ) ;
#93180=CARTESIAN_POINT ( 'NONE',  ( 2.741952636841408442, -2.198962954702073702, -0.6686182857488265352 ) ) ;
#93183=CARTESIAN_POINT ( 'NONE',  ( 1.410794581852807150, 1.648159533202856686, 0.8848386531258023435 ) ) ;
#93185=CARTESIAN_POINT ( 'NONE',  ( 5.981319044003478247, 1.821754654810204599, -0.7540403668018207384 ) ) ;
#93190=CARTESIAN_POINT ( 'NONE',  ( 1.032169062358662348, -1.402649970393770484, -1.703791656331831605 ) ) ;
#93195=CARTESIAN_POINT ( 'NONE',  ( 5.506699291815658093, 1.493407355681115378, -1.287129089984188290 ) ) ;
#93196=CARTESIAN_POINT ( 'NONE',  ( -0.1929003719821283658, -0.4722129235960635940, -2.074948700427194481 ) ) ;
#93197=CARTESIAN_POINT ( 'NONE',  ( 4.020403473283917783, -1.184823721361260018, -1.980193191683382148 ) ) ;
#93198=CARTESIAN_POINT ( 'NONE',  ( 3.045816552677531597, 1.455321998776702319, 1.461834479831431555 ) ) ;
#93205=CARTESIAN_POINT ( 'NONE',  ( 5.670445308384678640, -0.9712495897680500923, -1.941886722523916253 ) ) ;
#93208=CARTESIAN_POINT ( 'NONE',  ( 3.808014051635350672, 1.299385917162833692, -1.304790556973287163 ) ) ;
#93209=CARTESIAN_POINT ( 'NONE',  ( 6.620655732516647518, 0.007553340620044743381, 1.826407896915738238 ) ) ;
#93210=CARTESIAN_POINT ( 'NONE',  ( 5.161759341795384870, 1.079763445194487970, 1.907048802792680631 ) ) ;
#93212=CARTESIAN_POINT ( 'NONE',  ( 0.7028506612886147309, -0.7633063118723592000, -2.129901512202157399 ) ) ;
#93219=CARTESIAN_POINT ( 'NONE',  ( 0.3207183204587023551, -0.09351970983179427876, 1.767511165302604326 ) ) ;
#93220=CARTESIAN_POINT ( 'NONE',  ( 5.531894615797754433, -1.963542475010676469, 0.4432068886008522779 ) ) ;
#93221=CARTESIAN_POINT ( 'NONE',  ( 4.014754730066903754, 1.490810813664491974, -1.487730979428596223 ) ) ;
#93222=CARTESIAN_POINT ( 'NONE',  ( 3.761272268043499345, 1.802513535502557218, -0.6487917036162252904 ) ) ;
#93224=CARTESIAN_POINT ( 'NONE',  ( 4.844182406995376944, -0.9301426015250592316, 1.736093160643120914 ) ) ;
#93225=CARTESIAN_POINT ( 'NONE',  ( 5.502215278945715937, -0.9042992897083046433, 1.806084391566422198 ) ) ;
#93226=CARTESIAN_POINT ( 'NONE',  ( 2.236979667955760309, -1.672073921526989748, 0.8388852543278202401 ) ) ;
#93227=CARTESIAN_POINT ( 'NONE',  ( 5.672382752830540831, -1.089361703149527072, 1.337344134918318606 ) ) ;
#93228=CARTESIAN_POINT ( 'NONE',  ( 1.740342883905017013, 1.098329146349947827, -1.565357986077076990 ) ) ;
#93230=CARTESIAN_POINT ( 'NONE',  ( 2.438337523484556790, 1.039148161723329578, -1.946916322307743474 ) ) ;
#93233=CARTESIAN_POINT ( 'NONE',  ( 6.391066755906244623, 0.1909826923555627554, 1.952524381009380861 ) ) ;
#93240=CARTESIAN_POINT ( 'NONE',  ( 2.523957353938070192, 2.030885678308389952, -0.4015143504868187718 ) ) ;
#93245=CARTESIAN_POINT ( 'NONE',  ( -0.1106727585415967219, -0.002281114264979232885, -2.003378291782103471 ) ) ;
#93250=CARTESIAN_POINT ( 'NONE',  ( 5.272814466252145671, -2.006652483137221665, 0.1948127969565379425 ) ) ;
#93251=CARTESIAN_POINT ( 'NONE',  ( 4.311684426593565433, -1.183387839401760511, -1.506387502079686191 ) ) ;
#93253=CARTESIAN_POINT ( 'NONE',  ( 2.947022816757137065, -1.793111998972513277, -1.259777465452505796 ) ) ;
#93254=CARTESIAN_POINT ( 'NONE',  ( 0.1333692844072559280, 0.001398348041498076455, -2.053671342968105051 ) ) ;
#93256=CARTESIAN_POINT ( 'NONE',  ( 5.502202757749218520, -0.9014697883563610459, 1.800137906301606305 ) ) ;
#93257=CARTESIAN_POINT ( 'NONE',  ( 1.775505761281343631, 0.3235837346332003372, -1.884644527778083001 ) ) ;
#93260=CARTESIAN_POINT ( 'NONE',  ( 6.556269899348222907, -1.302956475595556496, 1.669668561148303976 ) ) ;
#93263=CARTESIAN_POINT ( 'NONE',  ( 3.351197789220595080, 0.5058271172731694243, -2.028516034726547623 ) ) ;
#93265=CARTESIAN_POINT ( 'NONE',  ( 1.940065037515970037, 1.705369652917272383, 0.2570983470618106170 ) ) ;
#93267=CARTESIAN_POINT ( 'NONE',  ( 6.469000917296717112, -1.638331675554663747, 1.346054232038436105 ) ) ;
#93274=CARTESIAN_POINT ( 'NONE',  ( 2.402729293200474459, -0.3110027565414590356, -1.784399550462684392 ) ) ;
#93278=CARTESIAN_POINT ( 'NONE',  ( 3.246531836744088295, 1.767876921188500150, 0.3942315000180166562 ) ) ;
#93279=CARTESIAN_POINT ( 'NONE',  ( 6.639320575229248789, 2.444019389566108647, 2.379739370560208567 ) ) ;
#93283=AXIS2_PLACEMENT_3D ( 'NONE', #95938, #80733, #62345 ) ;
#93284=CARTESIAN_POINT ( 'NONE',  ( 3.912436197073854593, 0.6682525715841195479, 1.737132965711101873 ) ) ;
#93286=CARTESIAN_POINT ( 'NONE',  ( 1.616650230726389248, 0.1894562617417178962, 1.906227014244334717 ) ) ;
#93287=CARTESIAN_POINT ( 'NONE',  ( 0.3932109892899987580, 1.349039491128176449, 1.230163767592551638 ) ) ;
#93295=CARTESIAN_POINT ( 'NONE',  ( 6.297704708030454235, -1.423956832742166112, -1.360762174370538258 ) ) ;
#93298=CARTESIAN_POINT ( 'NONE',  ( 0.5508686287750690358, -1.767239575335936230, -1.116659500934626514 ) ) ;
#93300=CARTESIAN_POINT ( 'NONE',  ( 5.631840744973369617, -1.222119163988559354, -1.489112003571291476 ) ) ;
#93302=CARTESIAN_POINT ( 'NONE',  ( 1.571042225754931465, 0.1381101175703668971, -1.820421783975199048 ) ) ;
#93303=CARTESIAN_POINT ( 'NONE',  ( 2.526237079854487089, -1.271617311931704686, -1.803507373242494438 ) ) ;
#93305=CARTESIAN_POINT ( 'NONE',  ( 0.4570967503451648373, -1.639016809899789040, 0.9851245988263114262 ) ) ;
#93307=CARTESIAN_POINT ( 'NONE',  ( 0.7132589462262963753, -1.661971685727476000, -1.056574055910926013 ) ) ;
#93308=CARTESIAN_POINT ( 'NONE',  ( 2.085399755688497336, -0.8285669363069894100, 1.756555673176816157 ) ) ;
#93310=CARTESIAN_POINT ( 'NONE',  ( 0.4388270972612972609, 1.158508728638860230, 1.649830871073371119 ) ) ;
#93312=CARTESIAN_POINT ( 'NONE',  ( 6.051566885458855793, 1.408179756913958913, 1.216655509429155124 ) ) ;
#93317=CARTESIAN_POINT ( 'NONE',  ( 2.296645709751913955, 1.758124065145909798, -1.308193547052277861 ) ) ;
#93321=CARTESIAN_POINT ( 'NONE',  ( 2.349991895876184511, 1.825291697999480434, 0.04531359951509549705 ) ) ;
#93327=CARTESIAN_POINT ( 'NONE',  ( 0.8383531591091289981, 1.897801360490163569, 0.3304300003270659314 ) ) ;
#93328=CARTESIAN_POINT ( 'NONE',  ( 5.313317156408340125, -1.655227327604656740, -1.052681782574490743 ) ) ;
#93333=CARTESIAN_POINT ( 'NONE',  ( 5.548420995840112724, -1.728225626343689925, 1.347513067664840358 ) ) ;
#93336=CARTESIAN_POINT ( 'NONE',  ( 4.205968427668831389, 0.7022645179026367757, -1.947615878368731623 ) ) ;
#93340=CARTESIAN_POINT ( 'NONE',  ( 4.588719013068318198, -0.6136123943910645195, 2.215248572529082693 ) ) ;
#93344=CARTESIAN_POINT ( 'NONE',  ( 6.620655732516643965, 2.083750514537034970, 2.135603474206409835 ) ) ;
#93346=CARTESIAN_POINT ( 'NONE',  ( 4.681548850490841573, -0.9142078566968904196, 1.713296222823880166 ) ) ;
#93350=CARTESIAN_POINT ( 'NONE',  ( 4.623256175466385010, 1.666654777633369555, 0.9376445158523971646 ) ) ;
#93351=CARTESIAN_POINT ( 'NONE',  ( 6.317413179709785886, -0.2053877530918957195, 1.712446389806308256 ) ) ;
#93352=CARTESIAN_POINT ( 'NONE',  ( 4.944546133779973651, -1.457238331152037825, 1.394083050251286870 ) ) ;
#93356=CARTESIAN_POINT ( 'NONE',  ( 1.289138792185164251, 1.584031432202914313, 1.364508995882382170 ) ) ;
#93357=CARTESIAN_POINT ( 'NONE',  ( 0.4086181399716379281, 1.536643064871806574, 0.8779792868154213670 ) ) ;
#93358=CARTESIAN_POINT ( 'NONE',  ( 6.293592298849589817, 1.492257802130890765, -1.356297202127904944 ) ) ;
#93361=CARTESIAN_POINT ( 'NONE',  ( 3.433774379101984575, 1.031038968642459475, -2.047360584804863493 ) ) ;
#93362=CARTESIAN_POINT ( 'NONE',  ( 2.554330413957212276, -1.514043700042773111, -0.8579764065595529843 ) ) ;
#93365=CARTESIAN_POINT ( 'NONE',  ( 0.5613444508567478897, 1.446164810419462432, -0.9560955100236142590 ) ) ;
#93367=CARTESIAN_POINT ( 'NONE',  ( 1.328301213181204421, -1.184495032981685014, 1.435421900094263403 ) ) ;
#93368=CARTESIAN_POINT ( 'NONE',  ( 2.401036581340802556, 0.4739146800750834165, 2.118683212603386767 ) ) ;
#93369=CARTESIAN_POINT ( 'NONE',  ( 3.995327539805045181, -0.3399590882401174463, 1.987497567597557468 ) ) ;
#93370=CARTESIAN_POINT ( 'NONE',  ( 4.281250000000002665, 0.7852924748302082536, 1.895863743163987980 ) ) ;
#93372=CARTESIAN_POINT ( 'NONE',  ( 0.4285742275551830960, 1.842496385298073580, 0.5622912056609475906 ) ) ;
#93374=CARTESIAN_POINT ( 'NONE',  ( 3.270003694065525046, 0.5362613544047705183, -2.155619276402853224 ) ) ;
#93380=CARTESIAN_POINT ( 'NONE',  ( -0.09271296656673803926, -0.4979868145295326953, -2.173146351408902888 ) ) ;
#93381=CARTESIAN_POINT ( 'NONE',  ( 4.281663391851794565, -1.878042059144067633, 0.5673916069991249422 ) ) ;
#93386=CARTESIAN_POINT ( 'NONE',  ( 5.958357971250668683, 0.9089415708923481718, 2.071969630155451547 ) ) ;
#93387=CARTESIAN_POINT ( 'NONE',  ( 2.541531169099729759, 1.886825176844410645, -0.8337591773379445792 ) ) ;
#93391=CARTESIAN_POINT ( 'NONE',  ( 3.409304255485625657, -0.3681080166235695117, 1.833790788056933962 ) ) ;
#93392=CARTESIAN_POINT ( 'NONE',  ( 2.601899516932767220, -0.1674142849007881351, 1.726012112926772701 ) ) ;
#93393=CARTESIAN_POINT ( 'NONE',  ( 6.444889499930222421, -1.758869480593090673, -1.307235502039267860 ) ) ;
#93394=CARTESIAN_POINT ( 'NONE',  ( 1.466163881440044836, 2.173982691173735216, -0.3780781022180225159 ) ) ;
#93396=CARTESIAN_POINT ( 'NONE',  ( 3.538091169922503276, 0.9737216987566952309, -1.930062384640649054 ) ) ;
#93397=CARTESIAN_POINT ( 'NONE',  ( 5.595633723370948331, -1.942124712531563491, 0.002075263307293323100 ) ) ;
#93401=CARTESIAN_POINT ( 'NONE',  ( 0.07077104593807002908, 0.8175350930016941353, 1.956879683024402183 ) ) ;
#93407=CARTESIAN_POINT ( 'NONE',  ( 3.668406916800326822, -1.225078373119499187, 1.353803248016255178 ) ) ;
#93408=CARTESIAN_POINT ( 'NONE',  ( 1.764966765715753949, -1.560254191817540992, 1.560848541443552895 ) ) ;
#93413=CARTESIAN_POINT ( 'NONE',  ( 0.8088602503539430444, -0.4949860548154049189, -1.958043583812353550 ) ) ;
#93414=CARTESIAN_POINT ( 'NONE',  ( 0.7508259783030580836, 2.089789393294994468, 0.3585813216958123606 ) ) ;
#93418=CARTESIAN_POINT ( 'NONE',  ( 2.746734941909965588, -0.3128536233567563163, -1.834277165529672793 ) ) ;
#93420=CARTESIAN_POINT ( 'NONE',  ( 0.3917762336288696523, 1.602822130585265015, 1.450656209987542855 ) ) ;
#93421=CARTESIAN_POINT ( 'NONE',  ( 5.748672702226536479, 1.986101125435947301, -0.3474646712962395911 ) ) ;
#93424=CARTESIAN_POINT ( 'NONE',  ( 4.125493313500066428, -1.746467973620144942, 0.5319596651164605339 ) ) ;
#93428=CARTESIAN_POINT ( 'NONE',  ( 6.151720201709268920, -0.2930281871833945173, -1.994563951915592881 ) ) ;
#93429=CARTESIAN_POINT ( 'NONE',  ( 5.841722611436679813, 1.839261846420519930, 0.08593139445873398952 ) ) ;
#93431=CARTESIAN_POINT ( 'NONE',  ( 4.090657727307928759, -2.282307194306469444, -0.3406017358680757390 ) ) ;
#93433=CARTESIAN_POINT ( 'NONE',  ( 6.696550776676711614, -0.5693818166121329405, -2.085215994158528208 ) ) ;
#93435=CARTESIAN_POINT ( 'NONE',  ( 2.261185778363482779, 1.904153404235246594, -0.3810316102009890238 ) ) ;
#93437=CARTESIAN_POINT ( 'NONE',  ( 5.483857608503296177, 2.120574376644312586, 0.8868611222285858187 ) ) ;
#93440=CARTESIAN_POINT ( 'NONE',  ( 4.416781281874038179, 1.710313510141375115, 0.7581657270378170388 ) ) ;
#93442=CARTESIAN_POINT ( 'NONE',  ( 2.179812656587180264, 1.874749209517186710, -0.3766967574026017229 ) ) ;
#93446=CARTESIAN_POINT ( 'NONE',  ( 3.633602750639616019, -2.039237483250630589, 0.8441791899983088765 ) ) ;
#93448=CARTESIAN_POINT ( 'NONE',  ( 6.983263157960335477, 6.035714437257905018, 2.641087593604172667 ) ) ;
#93451=CARTESIAN_POINT ( 'NONE',  ( 1.739464312186237871, -1.425129977898047740, -1.362296117697106013 ) ) ;
#93453=CARTESIAN_POINT ( 'NONE',  ( 2.046342449252246620, 0.8823731130137985046, -2.132409122670553270 ) ) ;
#93454=CARTESIAN_POINT ( 'NONE',  ( 2.840232074097197579, -1.010955899468408248, 1.681206195012739046 ) ) ;
#93456=CARTESIAN_POINT ( 'NONE',  ( 6.702015009205530838, 0.7948373677021604022, -1.903462506645931640 ) ) ;
#93458=CARTESIAN_POINT ( 'NONE',  ( 3.801970467005914678, -1.040791964576088358, -1.727064642965264740 ) ) ;
#93463=CARTESIAN_POINT ( 'NONE',  ( 1.920994505713587541, -1.537477318048833475, 1.533119463567463203 ) ) ;
#93467=CARTESIAN_POINT ( 'NONE',  ( 1.985418980784030119, 1.286400883397397221, 1.358229366437320618 ) ) ;
#93468=CARTESIAN_POINT ( 'NONE',  ( 6.098930168602409552, 1.771044849343451633, -1.239067683784184970 ) ) ;
#93469=CARTESIAN_POINT ( 'NONE',  ( 0.07775346131144719730, 4.079442786094135798, -2.843586357576178614 ) ) ;
#93470=CARTESIAN_POINT ( 'NONE',  ( 6.727182134110170075, 7.629137130509032971, 2.310944104600751281 ) ) ;
#93472=DIRECTION ( 'NONE',  ( 1.214306433183764966E-17, 1.000000000000000000, 5.200010849845536803E-32 ) ) ;
#93473=CARTESIAN_POINT ( 'NONE',  ( 2.701700744156261713, 1.353761940859641966, 1.350867010771430898 ) ) ;
#93475=CARTESIAN_POINT ( 'NONE',  ( 4.047515533282939337, 0.5961193180711570339, -1.666553171763493602 ) ) ;
#93476=CARTESIAN_POINT ( 'NONE',  ( 1.629408300089076889, -0.2329066467734330903, 1.897959532673603844 ) ) ;
#93478=CARTESIAN_POINT ( 'NONE',  ( 0.1103573706816539240, 1.834011727325855379, 0.5536052920952787559 ) ) ;
#93480=CARTESIAN_POINT ( 'NONE',  ( 1.135311898753359472, -0.04898221611688948623, -2.069941200615910581 ) ) ;
#93482=CARTESIAN_POINT ( 'NONE',  ( 5.330866702616011921, 0.1386157390740362649, 1.865562100978317206 ) ) ;
#93483=CARTESIAN_POINT ( 'NONE',  ( 1.822601884235462766, 1.703052241681313861, 0.6583118566880485911 ) ) ;
#93484=CARTESIAN_POINT ( 'NONE',  ( 6.024089167411393220, -1.222679950896175205, -1.837027303407394507 ) ) ;
#93487=CARTESIAN_POINT ( 'NONE',  ( 3.402832357982612077, 0.4983898525147857361, 2.001458950477213339 ) ) ;
#93495=CARTESIAN_POINT ( 'NONE',  ( 5.600075274486990828, 0.8424382930321882013, -1.891409743246947217 ) ) ;
#93497=CARTESIAN_POINT ( 'NONE',  ( 2.811983876933336735, -2.138515761559431461, 0.3140893029918228052 ) ) ;
#93499=CARTESIAN_POINT ( 'NONE',  ( 3.686198542540094714, 1.123799323442754572, 1.677924191584168501 ) ) ;
#93500=CARTESIAN_POINT ( 'NONE',  ( 6.720655732516665815, 3.683894443391816154, 2.687682123607849416 ) ) ;
#93505=CARTESIAN_POINT ( 'NONE',  ( 1.885954221117658092, -2.015980662343511032, 0.05432778586660082232 ) ) ;
#93507=CARTESIAN_POINT ( 'NONE',  ( 6.304242050522723240, 1.625252681175231029, -1.470355468214133321 ) ) ;
#93509=CARTESIAN_POINT ( 'NONE',  ( 4.306835718904429733, -0.4242474483713705169, -1.864571660543254739 ) ) ;
#93513=CARTESIAN_POINT ( 'NONE',  ( 3.814077502958601595, 1.076299547611740293, -1.704950967544152984 ) ) ;
#93515=CARTESIAN_POINT ( 'NONE',  ( 5.121954690102882957, -0.9251313946504275965, -1.455449238992040373 ) ) ;
#93519=CARTESIAN_POINT ( 'NONE',  ( 4.534354090784907143, 1.834037221929617711, 0.3668691113338993226 ) ) ;
#93522=CARTESIAN_POINT ( 'NONE',  ( 0.8661811918178536907, -2.060611401584189650, 0.1992402130865863485 ) ) ;
#93525=CARTESIAN_POINT ( 'NONE',  ( 6.322923312362423331, 1.337123347216003788, -1.222299563558794766 ) ) ;
#93528=CARTESIAN_POINT ( 'NONE',  ( 0.6503002719215627003, 1.784868618687754926, 0.3088405841149675091 ) ) ;
#93532=CARTESIAN_POINT ( 'NONE',  ( 1.099968687278202406, 0.7983322178258808188, -1.792280776234013828 ) ) ;
#93534=CARTESIAN_POINT ( 'NONE',  ( 4.763251566037994600, 1.785832754541897049, -0.6935334960865118248 ) ) ;
#93541=CARTESIAN_POINT ( 'NONE',  ( 2.237400686453533183, -1.931180590798301955, 0.9714560045831142077 ) ) ;
#93544=CARTESIAN_POINT ( 'NONE',  ( -0.1753031400193918454, -0.9122597987226389593, -1.912455998546586544 ) ) ;
#93545=CARTESIAN_POINT ( 'NONE',  ( 4.735264887803245060, -1.668767028523497675, 0.7406363711058363553 ) ) ;
#93547=CARTESIAN_POINT ( 'NONE',  ( 1.071480742727632940, 1.901078573484305201, -0.5215319001752088957 ) ) ;
#93548=CARTESIAN_POINT ( 'NONE',  ( 4.043146078444789460, 0.09904687726844901841, 1.909973672635330910 ) ) ;
#93551=CARTESIAN_POINT ( 'NONE',  ( 4.351979406267578732, -0.7558620137302939357, 1.818942442720396624 ) ) ;
#93553=CARTESIAN_POINT ( 'NONE',  ( 6.022988683830415191, -1.827201308531730017, 0.6583088893449047241 ) ) ;
#93557=CARTESIAN_POINT ( 'NONE',  ( 5.994406619193555663, -1.133004004027007294, 1.792352430775605798 ) ) ;
#93559=CARTESIAN_POINT ( 'NONE',  ( 4.494721087910216184, -1.855708629272670773, -0.4612273479895279138 ) ) ;
#93561=CARTESIAN_POINT ( 'NONE',  ( 6.983263157960366563, 2.056882910316945701, 2.252511522010155698 ) ) ;
#93565=CARTESIAN_POINT ( 'NONE',  ( 5.584640334855505373, -1.275214923639787834, 1.557698558565046243 ) ) ;
#93567=CARTESIAN_POINT ( 'NONE',  ( 6.568987803155795113, -1.671525225137669102, -0.7347104647430282576 ) ) ;
#93568=CARTESIAN_POINT ( 'NONE',  ( 1.715371797147913435, -1.774658612622433296, -1.066089629202723765 ) ) ;
#93585=CARTESIAN_POINT ( 'NONE',  ( 3.586273015720359503, -0.4996269028240771237, 1.660617844614233674 ) ) ;
#93587=CARTESIAN_POINT ( 'NONE',  ( 1.762639944428091576, -0.7413553172891698129, -1.933158369416078770 ) ) ;
#93588=CARTESIAN_POINT ( 'NONE',  ( 3.286815299386883549, 1.667571603535710434, -1.304429798788673267 ) ) ;
#93591=CARTESIAN_POINT ( 'NONE',  ( 1.129674139269299049, 1.899472608897791348, -0.5201393403096374879 ) ) ;
#93595=CARTESIAN_POINT ( 'NONE',  ( 0.2637284958507991606, 0.5978344860198721022, -1.816641584731902626 ) ) ;
#93596=CARTESIAN_POINT ( 'NONE',  ( 4.259948577007838466, 1.078808246893525391, 2.022540810160260882 ) ) ;
#93597=CARTESIAN_POINT ( 'NONE',  ( 0.2053145577999641314, -0.4904175937916722128, 1.758528939493007259 ) ) ;
#93598=CARTESIAN_POINT ( 'NONE',  ( 3.340010735810138520, -1.142844047782382466, -1.533173144288489276 ) ) ;
#93602=CARTESIAN_POINT ( 'NONE',  ( 2.215092046557234795, 1.614471179978003823, -1.202476892717120105 ) ) ;
#93603=CARTESIAN_POINT ( 'NONE',  ( 2.448037131198562921, -0.8433605282326918084, 1.771390271482737200 ) ) ;
#93607=CARTESIAN_POINT ( 'NONE',  ( 5.402318495819277366, 1.583515501651384438, -1.365094957383119700 ) ) ;
#93608=CARTESIAN_POINT ( 'NONE',  ( 2.975218959772182536, 1.681091501613757533, -0.5536541633112538330 ) ) ;
#93610=CARTESIAN_POINT ( 'NONE',  ( 6.421853422025334268, 1.325270252340422061, -1.870170258788282247 ) ) ;
#93611=CARTESIAN_POINT ( 'NONE',  ( 5.648340061037051107, -1.368025295233719074, 1.075653158840290891 ) ) ;
#93614=CARTESIAN_POINT ( 'NONE',  ( 5.870364492519208888, -0.4185229733149243292, 1.682389803524992011 ) ) ;
#93616=CARTESIAN_POINT ( 'NONE',  ( 5.811019572999191141, -1.715256576162796032, 1.331060940585542030 ) ) ;
#93618=CARTESIAN_POINT ( 'NONE',  ( -0.02988430322643093051, -0.9920087411236072628, 1.870552836459241419 ) ) ;
#93619=CARTESIAN_POINT ( 'NONE',  ( 4.531250000000003553, -0.7852924748302230196, -1.895863743163982429 ) ) ;
#93621=CARTESIAN_POINT ( 'NONE',  ( 3.786086853528514151, -0.9505683805260138897, 1.675471031514904396 ) ) ;
#93623=CARTESIAN_POINT ( 'NONE',  ( 6.381102873985867063, -2.030373413249999093, -0.9015990085984818547 ) ) ;
#93627=CARTESIAN_POINT ( 'NONE',  ( 2.842673000788879634, 1.232056068812878991, -1.848115600964394867 ) ) ;
#93632=CARTESIAN_POINT ( 'NONE',  ( 0.4928148368598186946, -2.006445878461552645, 0.2004378712678403507 ) ) ;
#93634=CARTESIAN_POINT ( 'NONE',  ( 5.336407798562197158, -1.148744492729685707, 1.713005319730724008 ) ) ;
#93639=CARTESIAN_POINT ( 'NONE',  ( 0.7547153349467434769, -1.490676808382383145, -0.9535711479493594878 ) ) ;
#93640=CARTESIAN_POINT ( 'NONE',  ( 5.783786074351109363, 1.412321387942861328, -1.005976269456631211 ) ) ;
#93641=CARTESIAN_POINT ( 'NONE',  ( 5.390116981161272136, -0.4305884537129686662, -1.686203596905116342 ) ) ;
#93642=CARTESIAN_POINT ( 'NONE',  ( 2.753816761298252036, 2.281055701876167685, -0.2276813034018300430 ) ) ;
#93644=CARTESIAN_POINT ( 'NONE',  ( 2.818100271072516261, 1.733748696238574416, 0.6199764264002775027 ) ) ;
#93648=CARTESIAN_POINT ( 'NONE',  ( 2.485134345765506847, 1.670108983700506977, -0.7376146046164517855 ) ) ;
#93649=CARTESIAN_POINT ( 'NONE',  ( 3.358046224211252095, 0.04667712216412447934, -2.016033814150198999 ) ) ;
#93652=CARTESIAN_POINT ( 'NONE',  ( 3.979594558520031189, 1.983667836772174509, -0.7075980189445835178 ) ) ;
#93655=CARTESIAN_POINT ( 'NONE',  ( 2.084514231050747401, 1.193861083872927109, -1.691280048542340708 ) ) ;
#93658=CARTESIAN_POINT ( 'NONE',  ( 4.635462950926918957, -0.1032030737609032217, 2.118083805499561656 ) ) ;
#93661=CARTESIAN_POINT ( 'NONE',  ( 1.383290355582541542, 1.780271273866357529, -0.7366933121468289825 ) ) ;
#93668=CARTESIAN_POINT ( 'NONE',  ( 6.011998765391792787, -0.7129019540204998284, 1.997330473063135381 ) ) ;
#93669=CARTESIAN_POINT ( 'NONE',  ( 1.219907122830860446, -2.054670964268051847, 0.4612076382107341277 ) ) ;
#93672=CARTESIAN_POINT ( 'NONE',  ( 6.297681919442434939, -1.347125180836796998, -1.284110876681610725 ) ) ;
#93678=CARTESIAN_POINT ( 'NONE',  ( 0.5277791401020451856, -0.3051165123582540994, 2.098401203810342786 ) ) ;
#93681=CARTESIAN_POINT ( 'NONE',  ( 2.611707774152134842, 0.5260268489151798121, -1.889944157703125072 ) ) ;
#93682=CARTESIAN_POINT ( 'NONE',  ( 1.165152350680317195, -1.954565670758709128, -0.9236901323337529668 ) ) ;
#93686=CARTESIAN_POINT ( 'NONE',  ( 2.600625072996507470, 0.8205526226049694172, -1.527383475524378031 ) ) ;
#93687=CARTESIAN_POINT ( 'NONE',  ( 2.923474784230184920, 0.9664119506291848349, -1.447106689822146963 ) ) ;
#93690=CARTESIAN_POINT ( 'NONE',  ( 2.126327167286511166, 0.3474154575464418748, -1.985796285822030161 ) ) ;
#93691=CARTESIAN_POINT ( 'NONE',  ( 6.825078400183572036, 7.629137130509069387, 2.744348168701661095 ) ) ;
#93694=CARTESIAN_POINT ( 'NONE',  ( 1.410939872204178602, 1.737622768476089430, 0.9313336078424112596 ) ) ;
#93695=CARTESIAN_POINT ( 'NONE',  ( 5.273660385517703553, 0.3669835118517566497, -1.876681294024808988 ) ) ;
#93701=CARTESIAN_POINT ( 'NONE',  ( 1.049479869930733944, -1.824965358647975489, 0.8655331567536515003 ) ) ;
#93704=CARTESIAN_POINT ( 'NONE',  ( 5.719831105939597649, -2.253009325453013023, 0.4983019283236743702 ) ) ;
#93705=CARTESIAN_POINT ( 'NONE',  ( 6.127397123722368555, 0.1457569626216181913, -1.956525209266091192 ) ) ;
#93706=CARTESIAN_POINT ( 'NONE',  ( 3.274216958324972726, -0.9628348462043828659, -1.709115330885315087 ) ) ;
#93708=CARTESIAN_POINT ( 'NONE',  ( 0.3170300144729014669, 1.034162889623980286, -1.730867746391979933 ) ) ;
#93710=CARTESIAN_POINT ( 'NONE',  ( 1.481820193039787403, -0.7077492718140475647, 1.995708955693164199 ) ) ;
#93713=CARTESIAN_POINT ( 'NONE',  ( 2.378628397106247849, 1.683441843134887428, -0.7459445200509451368 ) ) ;
#93716=CARTESIAN_POINT ( 'NONE',  ( 2.812858766682566181, -0.6196351552101020399, -2.028021595557969015 ) ) ;
#93721=CARTESIAN_POINT ( 'NONE',  ( 2.759116376063870391, -1.791426917979478395, -1.018529149919424892 ) ) ;
#93723=CARTESIAN_POINT ( 'NONE',  ( 0.08126746489400815676, -0.8690269180096841239, 1.623235155968821841 ) ) ;
#93725=FACE_OUTER_BOUND ( 'NONE', #86124, .T. ) ;
#93727=CARTESIAN_POINT ( 'NONE',  ( 0.4345545588612038657, 1.130843733186673639, -1.894998796914903139 ) ) ;
#93728=CARTESIAN_POINT ( 'NONE',  ( 2.829655204463392693, -2.111994357890615071, 0.8116228763568857918 ) ) ;
#93730=CARTESIAN_POINT ( 'NONE',  ( 1.951130291612662715, -1.617002164660426677, 0.8169817665307582688 ) ) ;
#93731=CARTESIAN_POINT ( 'NONE',  ( 3.538217205509861962, 0.6946294275822698649, 1.785521036047182486 ) ) ;
#93732=CARTESIAN_POINT ( 'NONE',  ( 4.633297751427938316, 0.003287558298453730800, -2.070544812459538253 ) ) ;
#93735=CARTESIAN_POINT ( 'NONE',  ( 3.203940287746226634, -1.969268756981055635, 0.09538867180547243307 ) ) ;
#93736=CARTESIAN_POINT ( 'NONE',  ( 6.533821582689818719, -1.260454884444404122, -1.457021811732343686 ) ) ;
#93737=CARTESIAN_POINT ( 'NONE',  ( 2.447944060942487621, 1.870205405844455049, 0.04815357881200743595 ) ) ;
#93738=CARTESIAN_POINT ( 'NONE',  ( 2.825201024400230132, 2.173230126089547909, 0.7765846127750095640 ) ) ;
#93740=CARTESIAN_POINT ( 'NONE',  ( 2.787383077106736273, -1.737616373609903286, 0.6669969758191662823 ) ) ;
#93742=CARTESIAN_POINT ( 'NONE',  ( 6.672339319202143848, -0.9689918024566068766, -1.820889590527257740 ) ) ;
#93746=CARTESIAN_POINT ( 'NONE',  ( 0.1707221987203759173, -1.373943582462642921, 1.596272430080846405 ) ) ;
#93748=CARTESIAN_POINT ( 'NONE',  ( 5.958325562381369345, 0.8699925256120243366, 1.978967057501494820 ) ) ;
#93749=CARTESIAN_POINT ( 'NONE',  ( 6.445964431295706731, -1.320945465521980555, -1.527872228271543342 ) ) ;
#93753=CARTESIAN_POINT ( 'NONE',  ( 6.825078400183581806, 2.095667212029386661, 2.065897939415714646 ) ) ;
#93755=CARTESIAN_POINT ( 'NONE',  ( 4.944546133779973651, -1.457238331152037825, 1.394083050251286870 ) ) ;
#93760=CARTESIAN_POINT ( 'NONE',  ( 6.561405286136595905, 0.3748316153167965403, -2.128808860954830795 ) ) ;
#93765=CARTESIAN_POINT ( 'NONE',  ( -0.03574161356561295771, -1.858227405880557015, -0.4649775414454700995 ) ) ;
#93768=FACE_OUTER_BOUND ( 'NONE', #188488, .T. ) ;
#93769=CARTESIAN_POINT ( 'NONE',  ( 1.207153632009206223, -0.4226329412084055548, 1.672169654609439116 ) ) ;
#93773=CARTESIAN_POINT ( 'NONE',  ( 1.211743588231738888, -0.7890745783359112142, -1.584151303567796543 ) ) ;
#93775=CARTESIAN_POINT ( 'NONE',  ( 1.981109662258444537, -1.841391200710382980, -0.8139001868950055396 ) ) ;
#93778=CARTESIAN_POINT ( 'NONE',  ( 4.542132036680512464, 0.9468659437555368985, -1.993456357439137960 ) ) ;
#93780=CARTESIAN_POINT ( 'NONE',  ( 5.190355475387732120, 1.122157983508360157, -1.858477351540340328 ) ) ;
#93785=CARTESIAN_POINT ( 'NONE',  ( 3.176547234745368264, 0.9552152173708803318, 1.893241096743401464 ) ) ;
#93786=CARTESIAN_POINT ( 'NONE',  ( 2.442982655898734645, -1.755780842375562312, -0.9913809985205720432 ) ) ;
#93787=CARTESIAN_POINT ( 'NONE',  ( 3.445387325821075652, -1.671857736322950094, 0.6981543005735133534 ) ) ;
#93791=CARTESIAN_POINT ( 'NONE',  ( 0.7076149179639171782, -1.862046558926268913, 0.1791945732521060819 ) ) ;
#93793=CARTESIAN_POINT ( 'NONE',  ( 6.111906964637446649, -1.811269838261083232, 0.2284818145076653595 ) ) ;
#93795=CARTESIAN_POINT ( 'NONE',  ( 1.182675045768744271, 1.564012596108365072, -1.105954659444969401 ) ) ;
#93800=CARTESIAN_POINT ( 'NONE',  ( 5.207972885698374022, -2.151664816535401314, 0.2080130470862306957 ) ) ;
#93803=CARTESIAN_POINT ( 'NONE',  ( 2.812858766682566181, -0.6196351552101020399, -2.028021595557969015 ) ) ;
#93804=PLANE ( 'NONE',  #93283 ) ;
#93806=CARTESIAN_POINT ( 'NONE',  ( 4.112542095708375811, 1.396345452295008727, -1.391819494878621111 ) ) ;
#93807=CARTESIAN_POINT ( 'NONE',  ( 6.469012471580376733, -1.473683540339595810, 1.218514635347216046 ) ) ;
#93808=CARTESIAN_POINT ( 'NONE',  ( 5.190659055775300956, 1.601436234092843414, -1.385157061098884146 ) ) ;
#93810=CARTESIAN_POINT ( 'NONE',  ( 0.4673438449808891004, 1.800595422158430825, 1.021790579661909781 ) ) ;
#93811=CARTESIAN_POINT ( 'NONE',  ( 3.222533412629301708, 0.04844597582449915174, 1.941506634493498362 ) ) ;
#93815=CARTESIAN_POINT ( 'NONE',  ( 3.398458197991469643, 1.647775209707361466, -1.286576258924768235 ) ) ;
#93818=CARTESIAN_POINT ( 'NONE',  ( 0.6272531361488179469, -0.2670696439982013781, 1.791522762418327419 ) ) ;
#93820=CARTESIAN_POINT ( 'NONE',  ( 5.215527394842717435, -0.3265260713646127022, 2.182469266582609091 ) ) ;
#93823=CARTESIAN_POINT ( 'NONE',  ( 3.153566124713353513, -1.803153744294363703, -1.271922660818012973 ) ) ;
#93826=CARTESIAN_POINT ( 'NONE',  ( 1.312987857083922627, 1.562780923097413677, -1.101767902142808175 ) ) ;
#93828=CARTESIAN_POINT ( 'NONE',  ( 5.705552448923417508, -1.629793913574303588, -1.276656259598766940 ) ) ;
#93830=CARTESIAN_POINT ( 'NONE',  ( 2.835029207381420502, 0.2633842809251253358, 2.145520918749081574 ) ) ;
#93831=CARTESIAN_POINT ( 'NONE',  ( 4.511385190476093321, -2.149204750630455241, 0.4279282578087198474 ) ) ;
#93833=DIRECTION ( 'NONE',  ( -0.9999980456341537316, 0.000000000000000000, -0.001977050295958610645 ) ) ;
#93840=CARTESIAN_POINT ( 'NONE',  ( 0.08851783505585240908, -0.5350849913869708541, 1.944072358963434555 ) ) ;
#93844=CARTESIAN_POINT ( 'NONE',  ( 5.541872263726007830, 1.386227983376321582, 1.537841262885197846 ) ) ;
#93845=CARTESIAN_POINT ( 'NONE',  ( 4.916589582839517192, 1.327171671461774061, -1.396654247447129960 ) ) ;
#93846=CARTESIAN_POINT ( 'NONE',  ( 6.292584676692968948, 1.568786179414104032, -1.421969346915842092 ) ) ;
#93849=CARTESIAN_POINT ( 'NONE',  ( 5.119951519371389814, 1.948576354197928628, -0.2848888285253112218 ) ) ;
#93850=CARTESIAN_POINT ( 'NONE',  ( 0.3928598746986839974, 1.819701785225702473, -1.220828600141062203 ) ) ;
#93851=CARTESIAN_POINT ( 'NONE',  ( 3.791466046568803705, 1.323482414808102137, 1.257835202898072380 ) ) ;
#93858=CARTESIAN_POINT ( 'NONE',  ( 1.329379181053941483, 0.9071106928158387817, -1.602193565413398968 ) ) ;
#93859=CARTESIAN_POINT ( 'NONE',  ( 4.763936024516410406, 0.6273381447981136727, -1.913061789696899995 ) ) ;
#93860=CARTESIAN_POINT ( 'NONE',  ( 1.370962024642598864, -0.5571102548348834116, 2.229726662508556778 ) ) ;
#93861=CARTESIAN_POINT ( 'NONE',  ( 5.524254240939322713, 0.9636562883742012531, 1.708648623189083393 ) ) ;
#93863=CARTESIAN_POINT ( 'NONE',  ( 0.2333690889706926119, 0.7157316027301027228, -2.136973218959358434 ) ) ;
#93865=CARTESIAN_POINT ( 'NONE',  ( 0.6431357727456864515, -0.2518013131528433757, -2.054909676291870380 ) ) ;
#93867=CARTESIAN_POINT ( 'NONE',  ( 1.997712292880989837, -2.090220067774691159, 0.05436529341687650757 ) ) ;
#93868=CARTESIAN_POINT ( 'NONE',  ( 0.07479286986305370977, 0.004866263145587856019, -1.855573292446038414 ) ) ;
#93871=CARTESIAN_POINT ( 'NONE',  ( -0.2104748580754183807, 4.084054299358617079, -2.658391380015924010 ) ) ;
#93872=CARTESIAN_POINT ( 'NONE',  ( 1.698380523978352485, 1.446983168995601199, 0.9667953101664509274 ) ) ;
#93877=CARTESIAN_POINT ( 'NONE',  ( 3.105755298912396878, -1.722902020775359144, 0.08520973767557615819 ) ) ;
#93878=CARTESIAN_POINT ( 'NONE',  ( 1.154151856878969928, 0.8927059368322427524, 2.001694687108931170 ) ) ;
#93879=CARTESIAN_POINT ( 'NONE',  ( 0.07043219980315276740, -0.8200377064033654850, 1.527959277978730768 ) ) ;
#93880=CARTESIAN_POINT ( 'NONE',  ( 4.512475528931441104, -0.9420208833846724916, -1.995868093903986118 ) ) ;
#93882=CARTESIAN_POINT ( 'NONE',  ( 2.360437767749205218, -2.170642449777848260, 0.04973808404824981572 ) ) ;
#93883=CARTESIAN_POINT ( 'NONE',  ( 1.506192966688112422, -0.6554880476431452774, -1.704135612709246184 ) ) ;
#93884=CARTESIAN_POINT ( 'NONE',  ( 3.028621024253768113, 0.5188578782318100657, 2.052648472271414448 ) ) ;
#93885=CARTESIAN_POINT ( 'NONE',  ( 6.639320575229251453, 0.008029245381881154262, 1.796863947021019481 ) ) ;
#93887=CARTESIAN_POINT ( 'NONE',  ( 3.193229341380324549, 1.808410471145019960, 1.408695239656273301 ) ) ;
#93892=CARTESIAN_POINT ( 'NONE',  ( 6.076846083367460238, -1.572777764080468321, 1.568860064416939037 ) ) ;
#93898=CARTESIAN_POINT ( 'NONE',  ( 3.867814693791224112, -0.2004342644464084944, -2.006446243107910199 ) ) ;
#93900=CARTESIAN_POINT ( 'NONE',  ( 2.360284975695529752, -2.062195451902974597, 0.04632573159841534699 ) ) ;
#93905=CARTESIAN_POINT ( 'NONE',  ( 5.121103774788174690, -2.081602751171758747, 0.6852947426586111224 ) ) ;
#93906=CARTESIAN_POINT ( 'NONE',  ( 2.619767714365705658, 0.2496074646863334634, 2.000857082853441327 ) ) ;
#93907=CARTESIAN_POINT ( 'NONE',  ( 2.630204301513817455, 0.2276190002089127917, 1.827071974840013269 ) ) ;
#93910=CARTESIAN_POINT ( 'NONE',  ( 0.07661050522433668353, 0.008287133257128471639, -1.710863442170395432 ) ) ;
#93912=CARTESIAN_POINT ( 'NONE',  ( 5.577129106639307388, -0.04938619725537891220, -2.262140991306497373 ) ) ;
#93914=CARTESIAN_POINT ( 'NONE',  ( 2.051528240825768012, -1.692106715078506296, -1.253703384363166196 ) ) ;
#93924=CARTESIAN_POINT ( 'NONE',  ( 3.006315081767933606, -0.8967225907310495403, 2.032537921011686954 ) ) ;
#93925=CARTESIAN_POINT ( 'NONE',  ( 6.883263157960374912, 7.629137130509066722, 2.546189081643289942 ) ) ;
#93928=CARTESIAN_POINT ( 'NONE',  ( 4.879329150013382410, -0.09822140645733207220, 1.959542894978071992 ) ) ;
#93937=CARTESIAN_POINT ( 'NONE',  ( 3.410498715577559015, -2.118327196165440185, -0.1003008382433126094 ) ) ;
#93939=CARTESIAN_POINT ( 'NONE',  ( 3.924826023212550030, 2.051882857192890430, 0.6804245187241527715 ) ) ;
#93940=CARTESIAN_POINT ( 'NONE',  ( 3.491602800004707241, -1.839307750763185645, -0.08696504193297231733 ) ) ;
#93944=CARTESIAN_POINT ( 'NONE',  ( 5.402228116617870946, 1.314032936993884793, -1.141193381800218232 ) ) ;
#93948=CARTESIAN_POINT ( 'NONE',  ( 3.362350911093567873, 0.9703303321016673033, 1.931748911306984784 ) ) ;
#93949=CARTESIAN_POINT ( 'NONE',  ( 5.431017465639029318, 0.9912489969874547224, 1.755499476546865445 ) ) ;
#93951=CARTESIAN_POINT ( 'NONE',  ( 2.237400686453533183, -1.931180590798301955, 0.9714560045831142077 ) ) ;
#93952=CARTESIAN_POINT ( 'NONE',  ( 3.602765292730988556, 1.556248219076960870, -1.210034843411099681 ) ) ;
#93954=CARTESIAN_POINT ( 'NONE',  ( 4.493657767381210810, -1.941711754461509232, -0.04422589797668275563 ) ) ;
#93963=CARTESIAN_POINT ( 'NONE',  ( 1.764966765715753949, -1.560254191817540992, 1.560848541443552895 ) ) ;
#93965=CARTESIAN_POINT ( 'NONE',  ( 6.860214158839045950, -1.961385418603446062, 0.04497666117601883257 ) ) ;
#93971=CARTESIAN_POINT ( 'NONE',  ( 5.472543265827003012, -0.04911201564661467345, -1.840652735559132669 ) ) ;
#93977=CARTESIAN_POINT ( 'NONE',  ( 5.871359616481898414, -1.819694913365289768, -1.088597390283413402 ) ) ;
#93980=CARTESIAN_POINT ( 'NONE',  ( 0.08096513915848214948, -0.1534363407719694927, -2.027498111301667905 ) ) ;
#93982=CARTESIAN_POINT ( 'NONE',  ( 2.136937089482681795, -0.08731620468203694918, -1.859122327218107218 ) ) ;
#93983=CARTESIAN_POINT ( 'NONE',  ( 3.913478945735289205, -0.9499487412085620974, -1.577145280185827447 ) ) ;
#93989=CARTESIAN_POINT ( 'NONE',  ( 4.705825944637973990, -0.5905853116198942487, 2.126329296355852883 ) ) ;
#93990=CARTESIAN_POINT ( 'NONE',  ( 6.011039796215681186, 1.991063742206979459, 1.074381780396720165 ) ) ;
#93992=CARTESIAN_POINT ( 'NONE',  ( 6.275650443109183740, 0.3000964294621047967, -1.786390703358155196 ) ) ;
#93993=CARTESIAN_POINT ( 'NONE',  ( 0.1457207355009884908, 1.993892511249679034, -0.3006540981884687214 ) ) ;
#93995=CARTESIAN_POINT ( 'NONE',  ( 5.928550619183988957, 1.803260976426118489, 0.4972845834502263584 ) ) ;
#93996=CARTESIAN_POINT ( 'NONE',  ( 5.145129553670328981, 0.1446803459003667969, 1.906877450533930096 ) ) ;
#94000=CARTESIAN_POINT ( 'NONE',  ( 0.9537216069140028729, 1.868711056098860235, -0.08788249432020722729 ) ) ;
#94001=CARTESIAN_POINT ( 'NONE',  ( 0.7609543035823238544, -0.05432987398422234326, -2.015980609757315190 ) ) ;
#94003=CARTESIAN_POINT ( 'NONE',  ( 3.862027066150780730, 2.090197335813360979, -0.2575193119012611498 ) ) ;
#94008=CARTESIAN_POINT ( 'NONE',  ( 3.304948908139183406, -0.3981353638667082806, -1.979975013379015936 ) ) ;
#94011=CARTESIAN_POINT ( 'NONE',  ( 3.884175197147401892, -1.069116497136082700, 1.878640351225938421 ) ) ;
#94017=CARTESIAN_POINT ( 'NONE',  ( 0.4675213905811578807, 1.889292113317426969, 1.069767032291484288 ) ) ;
#94021=CARTESIAN_POINT ( 'NONE',  ( 1.699035084177059174, 1.824418957995146195, 1.213967346723361596 ) ) ;
#94023=CARTESIAN_POINT ( 'NONE',  ( 2.641812911801244113, -1.676132216910112493, -1.519885475924544593 ) ) ;
#94030=CARTESIAN_POINT ( 'NONE',  ( 3.971743243459349149, 0.9813984145389564873, 1.472460009610305320 ) ) ;
#94033=CARTESIAN_POINT ( 'NONE',  ( 1.026558790958994383, 1.254618057004111886, -1.691278660206218420 ) ) ;
#94037=CARTESIAN_POINT ( 'NONE',  ( 6.556263154800560322, -1.238474754573844816, 1.591913907798309769 ) ) ;
#94041=CARTESIAN_POINT ( 'NONE',  ( 4.065207594588423845, 0.2294239933214488880, -1.856472568989680161 ) ) ;
#94042=CARTESIAN_POINT ( 'NONE',  ( 4.733297664174529906, 0.005294743050891088411, -2.070434559870132585 ) ) ;
#94049=CARTESIAN_POINT ( 'NONE',  ( 3.578520225191741844, 1.246510459297203610, -1.514941731618473009 ) ) ;
#94050=CARTESIAN_POINT ( 'NONE',  ( 0.9310172746952742884, 0.9912447863934905623, 1.755501862388042067 ) ) ;
#94054=CARTESIAN_POINT ( 'NONE',  ( 1.458040028222376439, 0.7530789129696242590, 1.712431740859089668 ) ) ;
#94056=CARTESIAN_POINT ( 'NONE',  ( 2.918229521859570408, -2.010703624536396728, 0.1031290223681199103 ) ) ;
#94058=CARTESIAN_POINT ( 'NONE',  ( 2.197004041102487371, 1.892657838527435299, 0.9490559450526787622 ) ) ;
#94059=MANIFOLD_SOLID_BREP ( 'Sweep1[5]', #184790 ) ;
#94061=CARTESIAN_POINT ( 'NONE',  ( 3.842288295254093100, -1.023014542950370975, 1.799900136785845817 ) ) ;
#94063=CARTESIAN_POINT ( 'NONE',  ( 6.492138175525482779, -0.5563555211482211771, -2.015168333173870785 ) ) ;
#94065=CARTESIAN_POINT ( 'NONE',  ( 5.719710266082651096, -1.780569991979109590, 0.4021758204828808081 ) ) ;
#94070=CARTESIAN_POINT ( 'NONE',  ( 6.247136877606230598, -1.867572634706683443, 1.175315980461520304 ) ) ;
#94072=CARTESIAN_POINT ( 'NONE',  ( 4.670513044250029999, 0.7352163052343118066, 1.765496816765201427 ) ) ;
#94084=CARTESIAN_POINT ( 'NONE',  ( 0.07700591528352926374, 4.093948292925152721, -2.465843965391618209 ) ) ;
#94088=( BOUNDED_SURFACE ( )  B_SPLINE_SURFACE ( 3, 3, ( 
 ( #153237, #4808, #66613, #182521, #67683, #185717, #137000, #151124, #85035, #100221 ),
 ( #132760, #38422, #104502, #203028, #54669, #133828, #52535, #168422, #21069, #186794 ),
 ( #2689, #120817, #116532, #200889, #86106, #548, #35204, #167363, #68762, #166289 ),
 ( #170546, #134882, #18951, #22130, #119738, #36273, #83963, #184652, #102350, #150052 ),
 ( #20018, #199840, #51482, #152178, #3747, #135930, #69822, #125100, #192126, #106680 ),
 ( #141310, #57873, #191058, #204082, #88243, #40574, #126162, #207322, #58943, #172703 ),
 ( #10185, #108831, #24281, #42723, #122976, #174857, #26435, #92546, #91467, #55735 ) ),
 .UNSPECIFIED., .T., .F., .T. ) 
 B_SPLINE_SURFACE_WITH_KNOTS ( ( 4, 3, 4 ),
 ( 4, 1, 1, 1, 1, 1, 1, 4 ),
 ( 0.000000000000000000, 0.5000000000000000000, 1.000000000000000000 ),
 ( 0.000000000000000000, 0.09183773654504942541, 0.1838067853904964410, 0.2558923657893393822, 0.3606054339151033017, 0.5206678126786191685, 0.7335446035554463728, 1.000000000000000000 ),
 .UNSPECIFIED. ) 
 GEOMETRIC_REPRESENTATION_ITEM ( )  RATIONAL_B_SPLINE_SURFACE ( (
 ( 1.000000000000000222, 1.000000000000000222, 0.9999999999999997780, 1.000000000000000000, 1.000000000000000222, 0.9999999999999996669, 1.000000000000000222, 1.000000000000000444, 1.000000000000000000, 1.000000000000000000),
 ( 0.3333333333333334259, 0.3333333333333334814, 0.3333333333333333703, 0.3333333333333333703, 0.3333333333333333703, 0.3333333333333332593, 0.3333333333333334814, 0.3333333333333334814, 0.3333333333333333703, 0.3333333333333333703),
 ( 0.3333333333333334259, 0.3333333333333334814, 0.3333333333333333703, 0.3333333333333333703, 0.3333333333333333703, 0.3333333333333332593, 0.3333333333333334814, 0.3333333333333334814, 0.3333333333333333703, 0.3333333333333333703),
 ( 1.000000000000000222, 1.000000000000000222, 0.9999999999999997780, 1.000000000000000000, 1.000000000000000222, 0.9999999999999996669, 1.000000000000000222, 1.000000000000000444, 1.000000000000000000, 1.000000000000000000),
 ( 0.3333333333333334259, 0.3333333333333334814, 0.3333333333333333703, 0.3333333333333333703, 0.3333333333333333703, 0.3333333333333332593, 0.3333333333333334814, 0.3333333333333334814, 0.3333333333333333703, 0.3333333333333333703),
 ( 0.3333333333333334259, 0.3333333333333334814, 0.3333333333333333703, 0.3333333333333333703, 0.3333333333333333703, 0.3333333333333332593, 0.3333333333333334814, 0.3333333333333334814, 0.3333333333333333703, 0.3333333333333333703),
 ( 1.000000000000000222, 1.000000000000000222, 0.9999999999999997780, 1.000000000000000000, 1.000000000000000222, 0.9999999999999996669, 1.000000000000000222, 1.000000000000000444, 1.000000000000000000, 1.000000000000000000) ) ) 
 REPRESENTATION_ITEM ( '' )  SURFACE ( )  );
#94091=CARTESIAN_POINT ( 'NONE',  ( 2.905082208348725548, -1.640047651136176565, 1.090064613274278837 ) ) ;
#94092=CARTESIAN_POINT ( 'NONE',  ( 3.603138812553498216, -0.1455146663824242736, 2.011206757212272933 ) ) ;
#94095=CARTESIAN_POINT ( 'NONE',  ( 6.827182134110200806, 4.685259207053684705, 2.851548537572299313 ) ) ;
#94096=CARTESIAN_POINT ( 'NONE',  ( 3.099763004921416876, -2.188912590334081809, 0.1079765428157742069 ) ) ;
#94098=CARTESIAN_POINT ( 'NONE',  ( 1.694233118518298165, -1.916858602850049609, -0.1915058630488040703 ) ) ;
#94100=CARTESIAN_POINT ( 'NONE',  ( -0.1296875068448159474, 0.7431874094961619104, -1.910093690679348200 ) ) ;
#94101=CARTESIAN_POINT ( 'NONE',  ( 0.2333540202161792088, 6.948072531064760859, -2.640811564931430766 ) ) ;
#94108=CARTESIAN_POINT ( 'NONE',  ( 6.181194517112824194, 1.274813594131599226, 1.328792456347933637 ) ) ;
#94109=CARTESIAN_POINT ( 'NONE',  ( 2.332683495817444719, 1.313167467523576715, -1.525923137932885476 ) ) ;
#94110=CARTESIAN_POINT ( 'NONE',  ( 4.341395233127314235, -1.327617041990782010, 1.876015773706960932 ) ) ;
#94111=CARTESIAN_POINT ( 'NONE',  ( -0.02880301295725678015, 0.2243704974793322426, -2.307247863525173859 ) ) ;
#94112=CARTESIAN_POINT ( 'NONE',  ( 2.359995855038379720, -1.860683555027684788, 0.03984664071272727565 ) ) ;
#94114=CARTESIAN_POINT ( 'NONE',  ( -0.1290005225502675879, -0.006633637972621592160, -2.173875058097324064 ) ) ;
#94115=CARTESIAN_POINT ( 'NONE',  ( 5.730699431777452446, 1.279516236652695316, -1.421498520143074540 ) ) ;
#94118=CARTESIAN_POINT ( 'NONE',  ( 5.126549769544753055, 0.1549841644245806838, 2.085076985156742779 ) ) ;
#94119=CARTESIAN_POINT ( 'NONE',  ( 3.555401268124198655, 0.4554524271490404952, -1.814226883376020671 ) ) ;
#94125=CARTESIAN_POINT ( 'NONE',  ( 6.551377187490000864, -1.390289022577213984, -1.020726160236499203 ) ) ;
#94127=CARTESIAN_POINT ( 'NONE',  ( 1.652526702274889514, 0.8913305402388423948, 1.487382274443969754 ) ) ;
#94130=CARTESIAN_POINT ( 'NONE',  ( 6.297752264732417338, -1.566808387090750765, -1.503110733841714675 ) ) ;
#94131=CARTESIAN_POINT ( 'NONE',  ( 3.949673224339702138, 0.6133576713117370183, -1.719707012317383432 ) ) ;
#94132=CARTESIAN_POINT ( 'NONE',  ( 2.448037131198562921, -0.8433605282326918084, 1.771390271482737200 ) ) ;
#94133=CARTESIAN_POINT ( 'NONE',  ( 0.3865160979802947927, -0.7177084582802439883, -1.991989965223327275 ) ) ;
#94137=CARTESIAN_POINT ( 'NONE',  ( 2.895306150831237879, -0.1582170333116576511, -2.114654843180157950 ) ) ;
#94142=CARTESIAN_POINT ( 'NONE',  ( 0.8134373588399683719, -1.746984811521329339, -1.110588058507409936 ) ) ;
#94144=CARTESIAN_POINT ( 'NONE',  ( 3.000855645084123946, -2.188801376007823762, -0.3777086580352209122 ) ) ;
#94146=CARTESIAN_POINT ( 'NONE',  ( 0.8624555810839064085, -0.06381188527813246025, -2.297968782114163222 ) ) ;
#94148=CARTESIAN_POINT ( 'NONE',  ( 5.471554536677815328, -0.3081364425130261320, 2.039334399838355960 ) ) ;
#94151=CARTESIAN_POINT ( 'NONE',  ( 0.2331563151865694850, 5.724144821786467219, -2.539778028485844441 ) ) ;
#94152=CARTESIAN_POINT ( 'NONE',  ( 5.671403949121008203, 1.101820082107987098, 1.475039313902235305 ) ) ;
#94155=CARTESIAN_POINT ( 'NONE',  ( 3.276077977556953513, -1.028358954114884094, 1.384488693430762085 ) ) ;
#94156=CARTESIAN_POINT ( 'NONE',  ( 1.112517963266421939, 1.944731545904467396, 0.5331650539944567946 ) ) ;
#94157=CARTESIAN_POINT ( 'NONE',  ( 2.883697495508124042, -0.6696099726914479522, -2.198986239785024388 ) ) ;
#94158=CARTESIAN_POINT ( 'NONE',  ( 2.829655204463392693, -2.111994357890615071, 0.8116228763568857918 ) ) ;
#94159=CARTESIAN_POINT ( 'NONE',  ( 5.338542076627605937, 2.074711179890481816, 0.3611063368853023592 ) ) ;
#94161=CARTESIAN_POINT ( 'NONE',  ( 3.180641231044952555, -0.1265111898236283006, -1.765250312072360162 ) ) ;
#94164=CARTESIAN_POINT ( 'NONE',  ( 6.567932727852480390, -1.414834124515697011, 1.804577934655810401 ) ) ;
#94165=CARTESIAN_POINT ( 'NONE',  ( 4.101369424419714527, -1.836060619117799497, 0.1375280490283348478 ) ) ;
#94170=CARTESIAN_POINT ( 'NONE',  ( 4.699289266375740404, -0.5861454505808120219, 2.111544493182772708 ) ) ;
#94176=CARTESIAN_POINT ( 'NONE',  ( 3.404829243095872648, 1.518349439661485389, -1.185654278882039669 ) ) ;
#94179=CARTESIAN_POINT ( 'NONE',  ( -0.03451705771533463557, -1.778989527951052141, 1.330178892887582398 ) ) ;
#94188=CARTESIAN_POINT ( 'NONE',  ( 0.1858947801188018389, -1.204007190563995078, -1.549573762531175625 ) ) ;
#94190=CARTESIAN_POINT ( 'NONE',  ( 6.614160618316515361, -1.014195557614630205, -1.909021090911746654 ) ) ;
#94191=CARTESIAN_POINT ( 'NONE',  ( 5.336364984333265227, -1.091323163865608459, 1.630109012322231266 ) ) ;
#94194=CARTESIAN_POINT ( 'NONE',  ( 5.682550338946039226, -2.108058120380253087, -0.4779004524640489970 ) ) ;
#94195=CARTESIAN_POINT ( 'NONE',  ( -0.2106725631050176684, -0.004273297132624876912, -2.003483006309703995 ) ) ;
#94198=CARTESIAN_POINT ( 'NONE',  ( 0.7724589312842686795, -1.759198622581410021, -0.6360808729843556719 ) ) ;
#94199=CARTESIAN_POINT ( 'NONE',  ( 6.028594920762765597, 1.707543762964639722, -0.2996114793598329551 ) ) ;
#94201=CARTESIAN_POINT ( 'NONE',  ( 3.509492838045696672, -2.158849082856160173, 0.3763758916049686487 ) ) ;
#94202=CARTESIAN_POINT ( 'NONE',  ( 3.311855287401725523, -0.4521268412439309325, 2.262704599374213643 ) ) ;
#94203=CARTESIAN_POINT ( 'NONE',  ( 6.362583954249420692, -1.460576210990358614, 1.454072064785590479 ) ) ;
#94204=CARTESIAN_POINT ( 'NONE',  ( 1.587728922880219384, -1.932555244376774617, -0.1907308274580049312 ) ) ;
#94207=CARTESIAN_POINT ( 'NONE',  ( 5.080389167821143026, 1.047295930500062866, 1.843893106414703054 ) ) ;
#94209=CARTESIAN_POINT ( 'NONE',  ( 2.197888892816081796, 1.802417619043535701, 0.9041091288993635677 ) ) ;
#94211=CARTESIAN_POINT ( 'NONE',  ( 5.913141818906856528, 1.943543578741913969, 1.045239939247793792 ) ) ;
#94214=CARTESIAN_POINT ( 'NONE',  ( 6.825078400183572924, 7.629137130509068498, 2.744348168701661095 ) ) ;
#94220=CARTESIAN_POINT ( 'NONE',  ( 4.223548136977580469, -1.972658117897459151, 0.5965803236557595257 ) ) ;
#94227=CARTESIAN_POINT ( 'NONE',  ( 4.652993067401423488, 0.3473450764862345830, 1.989417523455960568 ) ) ;
#94232=CARTESIAN_POINT ( 'NONE',  ( 3.151298293300933029, -1.683901109147158737, -1.187873040408020886 ) ) ;
#94233=CARTESIAN_POINT ( 'NONE',  ( 3.375625116643202972, -0.3961014713874110305, -1.976955985980306307 ) ) ;
#94239=CARTESIAN_POINT ( 'NONE',  ( 2.776720060080526853, -1.994564479802892087, 0.2930246351905210211 ) ) ;
#94240=CARTESIAN_POINT ( 'NONE',  ( 2.448939195788137013, 0.4911642875529352303, -1.774347143093172097 ) ) ;
#94241=CARTESIAN_POINT ( 'NONE',  ( 1.120229914364691659, -2.250463172007353130, 0.5101417434775123994 ) ) ;
#94243=CARTESIAN_POINT ( 'NONE',  ( 2.495597164219889308, 1.669172397749154380, 1.373402732410613725 ) ) ;
#94247=CARTESIAN_POINT ( 'NONE',  ( 1.111929834214450796, -0.8377583890188080584, -1.672643128629976772 ) ) ;
#94249=EDGE_CURVE ( 'NONE', #100328, #53173, #179273, .T. ) ;
#94250=CARTESIAN_POINT ( 'NONE',  ( 6.034049845351773023, 0.9722699467793812778, -1.714982496439126924 ) ) ;
#94254=CARTESIAN_POINT ( 'NONE',  ( 0.6103625832605160673, -2.195865045534075133, 0.2202409711149767024 ) ) ;
#94255=CARTESIAN_POINT ( 'NONE',  ( 6.461392557816405535, 1.719054114842766268, 1.153505076091146053 ) ) ;
#94258=CARTESIAN_POINT ( 'NONE',  ( 6.639320575229294086, 2.948176855103799454, 2.655556053213734558 ) ) ;
#94259=CARTESIAN_POINT ( 'NONE',  ( 5.401234739183408351, 1.611344100708357097, 1.135629011227519358 ) ) ;
#94260=CARTESIAN_POINT ( 'NONE',  ( 6.240491321897984278, 1.159586379754873331, -1.653562141909877603 ) ) ;
#94262=CARTESIAN_POINT ( 'NONE',  ( 5.022255751415273473, -1.231121986244879452, -1.951710362602774307 ) ) ;
#94263=CARTESIAN_POINT ( 'NONE',  ( 1.991156689281988745, 0.1981002678682428353, 2.053003549438499054 ) ) ;
#94270=CARTESIAN_POINT ( 'NONE',  ( 4.773980394326226673, -2.130202496963151670, 0.4190362392007019876 ) ) ;
#94272=CARTESIAN_POINT ( 'NONE',  ( 4.616662711240536510, -0.08544939198026380023, 1.839383977539174264 ) ) ;
#94273=DIRECTION ( 'NONE',  ( -0.9999980456341537316, 0.000000000000000000, -0.001977050295949902767 ) ) ;
#94274=CARTESIAN_POINT ( 'NONE',  ( 6.720655732516650716, 1.268691918110446570, 2.040305333170799429 ) ) ;
#94275=CARTESIAN_POINT ( 'NONE',  ( 6.023007056224171762, -2.064090639567913499, 0.7368321019862942300 ) ) ;
#94277=CARTESIAN_POINT ( 'NONE',  ( 6.069232182892009497, 0.1736634173518056545, -2.255917496054614446 ) ) ;
#94285=CARTESIAN_POINT ( 'NONE',  ( 1.094210320218844679, -0.4249228298987791086, -1.717946482988210510 ) ) ;
#94286=CARTESIAN_POINT ( 'NONE',  ( 4.951819039462027838, -1.425199631963388391, -1.421988410718623586 ) ) ;
#94288=CARTESIAN_POINT ( 'NONE',  ( 4.331157237497373025, 0.1008371559532254685, 2.103664472247131378 ) ) ;
#94289=CARTESIAN_POINT ( 'NONE',  ( 1.774859612008858667, 1.665787454739732221, -0.9457685036825744795 ) ) ;
#94291=CARTESIAN_POINT ( 'NONE',  ( 2.980859429886784984, 1.853565342000351501, 0.6662430357459552255 ) ) ;
#94292=CARTESIAN_POINT ( 'NONE',  ( 6.047130097259819870, 0.2019483658235003143, 2.009690058136243351 ) ) ;
#94293=CARTESIAN_POINT ( 'NONE',  ( 1.885419139999934934, 1.287927767047767125, 1.356919574424742203 ) ) ;
#94294=CARTESIAN_POINT ( 'NONE',  ( 5.479022876622000382, -0.04827441000932602283, -1.724383337574379116 ) ) ;
#94295=CARTESIAN_POINT ( 'NONE',  ( 1.617294888471169312, 1.591762500684265946, 1.059657513450793953 ) ) ;
#94297=CARTESIAN_POINT ( 'NONE',  ( 1.366164030173490973, 2.173753390890633685, -0.3800739277931909355 ) ) ;
#94301=CARTESIAN_POINT ( 'NONE',  ( 6.508674657442179878, 1.384610780642284711, -1.258058027910214927 ) ) ;
#94306=CARTESIAN_POINT ( 'NONE',  ( 2.471216696211364638, 1.848302923701108158, 0.9330170062570308787 ) ) ;
#94311=CARTESIAN_POINT ( 'NONE',  ( 6.586587867412674768, -1.305319418013479948, 1.671791285998667442 ) ) ;
#94316=CARTESIAN_POINT ( 'NONE',  ( 3.936874915731437774, 1.117662071392529377, 1.677747830363854664 ) ) ;
#94317=CARTESIAN_POINT ( 'NONE',  ( 4.628101268237789334, 1.911029739866540345, 0.1345505791198585988 ) ) ;
#94319=CARTESIAN_POINT ( 'NONE',  ( 3.140350738262797314, 0.5347024899306859202, 2.125194831261326911 ) ) ;
#94320=CARTESIAN_POINT ( 'NONE',  ( 0.1335669894368343991, 0.2365985627143319114, -2.188050374159770772 ) ) ;
#94322=CARTESIAN_POINT ( 'NONE',  ( 5.168231636832498310, 2.010700947019973039, -0.1031825239030410013 ) ) ;
#94325=CARTESIAN_POINT ( 'NONE',  ( 6.327753876788817955, 0.8101538176374730726, -1.956283944203747849 ) ) ;
#94327=CARTESIAN_POINT ( 'NONE',  ( 3.122686798916929352, 0.05371976762510695391, 2.090236283336026180 ) ) ;
#94329=CARTESIAN_POINT ( 'NONE',  ( 2.291662735322400835, -0.7404417586454847822, 1.557896076775511451 ) ) ;
#94331=CARTESIAN_POINT ( 'NONE',  ( 5.414351406770180120, -2.120778210838507150, 0.002142078463891750485 ) ) ;
#94340=CARTESIAN_POINT ( 'NONE',  ( 1.260107830910334181, 1.809384220011617028, 0.08917393313457448734 ) ) ;
#94346=CARTESIAN_POINT ( 'NONE',  ( 2.683996807801437789, 0.9705641499191748345, 1.529316921005590357 ) ) ;
#94350=CARTESIAN_POINT ( 'NONE',  ( 3.543253484755361615, 1.683469864222198797, -0.7936445362404942472 ) ) ;
#94351=CARTESIAN_POINT ( 'NONE',  ( 1.124461781556247431, 0.3751114458506888405, 1.878329865892948813 ) ) ;
#94352=CARTESIAN_POINT ( 'NONE',  ( 1.096400207583309028, -0.4391605778215034173, -1.771851442210800709 ) ) ;
#94359=CARTESIAN_POINT ( 'NONE',  ( 5.348484190341658007, -1.954120660473107396, -0.2448405522006945334 ) ) ;
#94362=CARTESIAN_POINT ( 'NONE',  ( 0.6739141125756157313, -1.159797070128726793, 1.739218980263528946 ) ) ;
#94364=CARTESIAN_POINT ( 'NONE',  ( 4.893539313097565291, 1.427316681580325763, 1.293898783310668987 ) ) ;
#94366=CARTESIAN_POINT ( 'NONE',  ( 0.8326870614539466642, 0.1294382003846420159, 1.821050407652326619 ) ) ;
#94367=CARTESIAN_POINT ( 'NONE',  ( 1.875870136999336246, 2.111227540014638304, -0.6426800678154331870 ) ) ;
#94369=CARTESIAN_POINT ( 'NONE',  ( -0.1581436608063293003, -1.178060542814472367, -1.506996232563104776 ) ) ;
#94371=CARTESIAN_POINT ( 'NONE',  ( 0.4671662993806492414, 1.711898730999446228, 0.9738141270322558940 ) ) ;
#94372=CARTESIAN_POINT ( 'NONE',  ( 3.017060306806388148, -1.870969668351904147, 0.5203628790987256947 ) ) ;
#94373=CARTESIAN_POINT ( 'NONE',  ( 0.6673420201736457447, -0.6766069248959759586, -1.899328980164962877 ) ) ;
#94375=CARTESIAN_POINT ( 'NONE',  ( 5.172628746253565168, 1.285086882066178937, -1.346197146212588347 ) ) ;
#94382=CARTESIAN_POINT ( 'NONE',  ( 1.101424459656743071, -0.5276332240332289869, 2.126988402630063835 ) ) ;
#94386=CARTESIAN_POINT ( 'NONE',  ( 2.332394550857110893, 1.770734860448031300, 0.4440693575865002907 ) ) ;
#94394=CARTESIAN_POINT ( 'NONE',  ( 1.471183419133621717, 0.1424870401847652956, -1.921283849777700947 ) ) ;
#94395=CARTESIAN_POINT ( 'NONE',  ( 5.067221110791254368, 1.704927679941736329, 0.9703409489375603991 ) ) ;
#94398=CARTESIAN_POINT ( 'NONE',  ( 5.003566749295822014, -2.181051155298455058, 0.2145382695054529609 ) ) ;
#94401=CARTESIAN_POINT ( 'NONE',  ( 4.539934223682924319, 1.348354173984022575, 1.571082123823979826 ) ) ;
#94405=CARTESIAN_POINT ( 'NONE',  ( 3.621995078338976715, 0.3387333280310041994, 2.273515639168000035 ) ) ;
#94412=CARTESIAN_POINT ( 'NONE',  ( 3.925673184153520179, 1.037972095618071133, -1.641099617876127015 ) ) ;
#94416=CARTESIAN_POINT ( 'NONE',  ( 5.009976098083095408, -0.6827417919906975108, 1.786564173047608062 ) ) ;
#94417=CARTESIAN_POINT ( 'NONE',  ( 5.877914075457827181, 1.031193140389017548, 1.382412309478407542 ) ) ;
#94418=CARTESIAN_POINT ( 'NONE',  ( 4.575407832915947104, 1.497500392235490807, 1.350737390116145242 ) ) ;
#94420=CARTESIAN_POINT ( 'NONE',  ( 2.034064749695370100, -1.442962035976073309, -1.669870808145665020 ) ) ;
#94423=CARTESIAN_POINT ( 'NONE',  ( 2.150438955405692631, -1.615297803084648098, 1.327229747913031055 ) ) ;
#94424=CARTESIAN_POINT ( 'NONE',  ( 0.6547154952327862709, -1.491839214215221698, -0.9519326369243490404 ) ) ;
#94425=CARTESIAN_POINT ( 'NONE',  ( 5.485000066852382616, -2.016597020608828839, 0.002808655738886777897 ) ) ;
#94427=CARTESIAN_POINT ( 'NONE',  ( 2.941680396524527286, 0.8243158943622121981, -2.139088555740241038 ) ) ;
#94428=CARTESIAN_POINT ( 'NONE',  ( 1.077605773158099023, -1.697095445269660496, -0.3847248992609655915 ) ) ;
#94430=CARTESIAN_POINT ( 'NONE',  ( 3.076547362214879566, 0.9570632234598417387, 1.892448740577145738 ) ) ;
#94432=CARTESIAN_POINT ( 'NONE',  ( 1.106332979110283610, 0.7092076354480534306, -1.582373438193741322 ) ) ;
#94435=CARTESIAN_POINT ( 'NONE',  ( 0.7663804396884700276, -2.160669279729439562, 0.2131170157090022665 ) ) ;
#94436=CARTESIAN_POINT ( 'NONE',  ( 3.292204118033771110, -0.8216723425069611952, -1.841733987974409237 ) ) ;
#94437=CARTESIAN_POINT ( 'NONE',  ( 3.531250000000002220, -0.7852924748301699509, -1.895863743164005744 ) ) ;
#94439=CARTESIAN_POINT ( 'NONE',  ( 6.164670984062957437, -1.360496472042394656, 1.364235590486153837 ) ) ;
#94441=CARTESIAN_POINT ( 'NONE',  ( 3.234858691920166951, 1.406421598713000432, -1.719528915531160385 ) ) ;
#94447=CARTESIAN_POINT ( 'NONE',  ( 5.741712943377584644, 1.738890731700697412, 0.07666446624409603561 ) ) ;
#94448=CARTESIAN_POINT ( 'NONE',  ( 4.826587731031282580, -1.282962940432516907, 1.484285152025546672 ) ) ;
#94452=CARTESIAN_POINT ( 'NONE',  ( 4.394006599171666139, -0.8711832027283890056, 2.088141772348524050 ) ) ;
#94454=CARTESIAN_POINT ( 'NONE',  ( 2.436046450607622926, 1.266989887546982052, 1.627633791282004250 ) ) ;
#94458=CARTESIAN_POINT ( 'NONE',  ( 4.200366636497298245, -0.5845007089231197828, -1.776970133648393624 ) ) ;
#94459=CARTESIAN_POINT ( 'NONE',  ( 2.742450610247765486, 1.725592070310760118, -0.1720703960508932762 ) ) ;
#94460=CARTESIAN_POINT ( 'NONE',  ( 5.899973326018037589, -0.7874313895239596350, -2.045375389432432467 ) ) ;
#94461=CARTESIAN_POINT ( 'NONE',  ( 1.431021430919703574, 2.126993092707793132, 0.5877070120439558121 ) ) ;
#94462=CARTESIAN_POINT ( 'NONE',  ( 3.731458613173586514, -1.998165266068991253, 0.8252760040215676440 ) ) ;
#94463=CARTESIAN_POINT ( 'NONE',  ( 4.857337426984369877, 1.920559571908975194, -0.2866867867914507650 ) ) ;
#94469=CARTESIAN_POINT ( 'NONE',  ( 5.467422714486909641, -1.967887220244109558, -0.4390321945699494632 ) ) ;
#94473=CARTESIAN_POINT ( 'NONE',  ( 2.930095790256614485, 1.013914413367119627, -1.518051517300327502 ) ) ;
#94474=CARTESIAN_POINT ( 'NONE',  ( 2.204404769108789797, -2.206272049354717879, 0.05393164079612459277 ) ) ;
#94480=CARTESIAN_POINT ( 'NONE',  ( 0.6506561817731060238, 1.990614601344290691, 0.3409984238087642727 ) ) ;
#94481=CARTESIAN_POINT ( 'NONE',  ( 0.7684181764250408442, 2.117871390293009526, -0.1079879263860619443 ) ) ;
#94486=CARTESIAN_POINT ( 'NONE',  ( 1.762329786688419109, -0.6638292341827031207, -1.738725725234435693 ) ) ;
#94488=CARTESIAN_POINT ( 'NONE',  ( 0.2862814217290919894, -1.017545141758866789, 1.907252267444502269 ) ) ;
#94489=CARTESIAN_POINT ( 'NONE',  ( 5.871720251644387822, -0.2986239867289949834, -1.994071864161291119 ) ) ;
#94493=CARTESIAN_POINT ( 'NONE',  ( 3.562960707638890501, -1.610701098693729350, -0.8595150645765645692 ) ) ;
#94497=CARTESIAN_POINT ( 'NONE',  ( 6.309922681198771421, -1.704675833164914778, 1.076154833852351000 ) ) ;
#94498=CARTESIAN_POINT ( 'NONE',  ( 5.947170714876299336, 0.5300644225827764178, -1.763184533696081857 ) ) ;
#94499=CARTESIAN_POINT ( 'NONE',  ( -0.02299388927990211537, 2.886218872804919400, -2.399728103386359557 ) ) ;
#94500=CARTESIAN_POINT ( 'NONE',  ( 4.231326342634161186, 0.1110341807785204943, 2.305146914567071548 ) ) ;
#94502=CARTESIAN_POINT ( 'NONE',  ( 6.397764797294555272, -0.7349420381566433846, 2.032942830986879557 ) ) ;
#94504=CARTESIAN_POINT ( 'NONE',  ( 1.751409898207861415, 1.936723520591139058, -0.1449614948935191994 ) ) ;
#94506=CARTESIAN_POINT ( 'NONE',  ( 4.499567255430725332, 2.252980053716880704, 0.4539551632626090405 ) ) ;
#94509=CARTESIAN_POINT ( 'NONE',  ( 4.522238337509359773, 1.150754656758418593, -1.474723989322044959 ) ) ;
#94511=CARTESIAN_POINT ( 'NONE',  ( 2.566550162062298579, 0.6480892470011965223, 1.799338185917313870 ) ) ;
#94514=CARTESIAN_POINT ( 'NONE',  ( 3.545738602337618506, -1.670889076328873069, -1.441789439710974063 ) ) ;
#94519=CARTESIAN_POINT ( 'NONE',  ( 2.196496099369545263, -0.5219070890916230887, -1.900975273168264534 ) ) ;
#94520=CARTESIAN_POINT ( 'NONE',  ( 1.571738265064129836, 0.1679657064320304316, -2.301541284809864862 ) ) ;
#94521=CARTESIAN_POINT ( 'NONE',  ( 2.664445928352857429, -0.7481792696971515388, -1.813797970468238985 ) ) ;
#94523=CARTESIAN_POINT ( 'NONE',  ( 5.594603800059450904, 2.031116569408123240, 0.3580809986778245024 ) ) ;
#94530=CARTESIAN_POINT ( 'NONE',  ( 2.149520630032801805, 1.890536112741852959, -1.067247343769129442 ) ) ;
#94533=CARTESIAN_POINT ( 'NONE',  ( 2.424885678431305092, -0.004389691185376768875, 1.870726058193001196 ) ) ;
#94534=CARTESIAN_POINT ( 'NONE',  ( 6.626263010475290649, 1.250585457657760635, -1.762915812992614129 ) ) ;
#94535=CARTESIAN_POINT ( 'NONE',  ( -0.02224634325196857623, 5.718740092702407907, -2.883150554214870098 ) ) ;
#94538=CARTESIAN_POINT ( 'NONE',  ( 2.244649938279310142, 1.855272219182309668, 0.4629769397326845004 ) ) ;
#94541=CARTESIAN_POINT ( 'NONE',  ( 4.363939919551316216, 0.8349522575829392279, 1.560488599360178474 ) ) ;
#94542=CARTESIAN_POINT ( 'NONE',  ( 1.822773347178743286, 1.416086463930026573, -1.285276961632122683 ) ) ;
#94546=CARTESIAN_POINT ( 'NONE',  ( -0.1532965272393977951, -1.712378426511364404, -0.8589627718659180733 ) ) ;
#94548=CARTESIAN_POINT ( 'NONE',  ( 1.029834584532058672, 1.995790600324919506, -0.5504719462680053299 ) ) ;
#94551=CARTESIAN_POINT ( 'NONE',  ( 5.049604242677837362, 0.5861553263475408615, -1.776501995420045832 ) ) ;
#94552=CARTESIAN_POINT ( 'NONE',  ( 1.453431991042982041, 0.5316948868413253759, -1.746555546766684675 ) ) ;
#94553=CARTESIAN_POINT ( 'NONE',  ( 4.248781725523794073, 0.5872999373685274804, 2.127227798101683387 ) ) ;
#94556=CARTESIAN_POINT ( 'NONE',  ( 2.910651161647914265, 0.6924047515337331538, 1.943132885215630878 ) ) ;
#94562=CARTESIAN_POINT ( 'NONE',  ( 5.248515149483167441, -2.054309126314420642, -0.2569322651706855143 ) ) ;
#94564=CARTESIAN_POINT ( 'NONE',  ( 2.917419293707240069, -0.2150262876145451196, 2.150894318904146729 ) ) ;
#94566=CARTESIAN_POINT ( 'NONE',  ( 2.684245096118286877, 1.082265567382127758, 1.705031398228576078 ) ) ;
#94572=CARTESIAN_POINT ( 'NONE',  ( 1.200408080392855181, 1.350732740426639822, -1.497504596960941958 ) ) ;
#94574=CARTESIAN_POINT ( 'NONE',  ( 5.847271748948593029, 0.6375361197438635941, -2.096799129279611762 ) ) ;
#94576=CARTESIAN_POINT ( 'NONE',  ( 4.640819915729988310, 1.831716588661407963, 0.5496940206762626069 ) ) ;
#94580=CARTESIAN_POINT ( 'NONE',  ( 3.040638836679772528, -1.525031945187466098, 1.319243992433154267 ) ) ;
#94583=CARTESIAN_POINT ( 'NONE',  ( 5.034089265250761613, 0.8841871275974706457, -1.480748092288231454 ) ) ;
#94589=CARTESIAN_POINT ( 'NONE',  ( 1.340777958403309267, -2.018934908790828597, -0.4573474576154838989 ) ) ;
#94590=CARTESIAN_POINT ( 'NONE',  ( 6.877413708759195998, -0.1538780216673047430, 2.036608477593480959 ) ) ;
#94592=CARTESIAN_POINT ( 'NONE',  ( 6.621734039712152686, -0.3858887922842542673, 1.776151629007856281 ) ) ;
#94594=CARTESIAN_POINT ( 'NONE',  ( -0.1759689521645991239, -0.7750936178016191169, -1.636263868569738600 ) ) ;
#94598=CARTESIAN_POINT ( 'NONE',  ( 2.713028398602938651, -0.2137989841624072795, 2.180988865010752509 ) ) ;
#94601=CARTESIAN_POINT ( 'NONE',  ( 0.8714495147512549833, -0.2914478312704605889, 1.939986204769503786 ) ) ;
#94603=CARTESIAN_POINT ( 'NONE',  ( 5.202711523826980766, 1.771732004023411911, 0.7288693050919017313 ) ) ;
#94612=CARTESIAN_POINT ( 'NONE',  ( 2.079201547314021070, -0.1057080177612122057, -2.159229931372666389 ) ) ;
#94616=CARTESIAN_POINT ( 'NONE',  ( 1.518276268637512194, 1.228937244518006011, -1.350148523839814096 ) ) ;
#94618=CARTESIAN_POINT ( 'NONE',  ( 4.172732250082421324, -1.703408510751417193, -0.6570589383413025786 ) ) ;
#94621=CARTESIAN_POINT ( 'NONE',  ( 3.234525475359388391, 1.209690070866603406, -1.481213593849866950 ) ) ;
#94623=CARTESIAN_POINT ( 'NONE',  ( 3.982825254072485777, 1.869399454171687180, 0.6202158817144760583 ) ) ;
#94624=ORIENTED_EDGE ( 'NONE', *, *, #102016, .F. ) ;
#94625=CARTESIAN_POINT ( 'NONE',  ( 6.286669113786358842, 1.687405947569386999, -0.9612952809280647104 ) ) ;
#94629=CARTESIAN_POINT ( 'NONE',  ( 6.258074605086497932, 0.8102346573028992305, -1.959903593942226685 ) ) ;
#94631=CARTESIAN_POINT ( 'NONE',  ( 3.598220562318912741, -0.9401235635465958751, 1.665135908046413871 ) ) ;
#94635=CARTESIAN_POINT ( 'NONE',  ( 4.899092244908956673, -0.2488113327579875855, -1.997608342807774218 ) ) ;
#94637=CARTESIAN_POINT ( 'NONE',  ( 5.777927443424748510, 1.091106472389313131, 1.463626628978510702 ) ) ;
#94638=CARTESIAN_POINT ( 'NONE',  ( 0.5728211633247158874, 1.428863753495920763, -1.498466819491943047 ) ) ;
#94642=CARTESIAN_POINT ( 'NONE',  ( 6.614126560844452385, -0.8839695271746010885, -1.648598838400926692 ) ) ;
#94650=CARTESIAN_POINT ( 'NONE',  ( 4.025767975679870325, -1.506360102045413596, 0.8590090823815172971 ) ) ;
#94652=CARTESIAN_POINT ( 'NONE',  ( 1.006788857090525013, 0.5974033793386055446, 1.982218910981221827 ) ) ;
#94653=CARTESIAN_POINT ( 'NONE',  ( 3.427469813117941744, -1.604901852541072760, -1.381049200617268102 ) ) ;
#94658=CARTESIAN_POINT ( 'NONE',  ( 0.9890311015656474414, 0.1392606914251882932, 1.964554613873798594 ) ) ;
#94663=CARTESIAN_POINT ( 'NONE',  ( 3.961076342171603315, 0.2821129637899103537, -2.274769079453589526 ) ) ;
#94664=CARTESIAN_POINT ( 'NONE',  ( 0.9612317138737861422, 0.3586375672061762887, -1.789940867121169843 ) ) ;
#94665=CARTESIAN_POINT ( 'NONE',  ( 3.216961742616857745, 1.504763323797538410, -1.180078671740567131 ) ) ;
#94670=CARTESIAN_POINT ( 'NONE',  ( 1.881109812905419343, -1.842300511448742739, -0.8121059663154740482 ) ) ;
#94671=CARTESIAN_POINT ( 'NONE',  ( 1.744895479173363517, -0.2825750800353257208, -1.941159045430330465 ) ) ;
#94675=CARTESIAN_POINT ( 'NONE',  ( 5.015614203636001633, -1.117866415629315435, -1.766478577331761723 ) ) ;
#94676=CARTESIAN_POINT ( 'NONE',  ( 3.133429157788733654, -1.187652617478820227, -1.312364946228376628 ) ) ;
#94678=FILL_AREA_STYLE ('',( #7241 ) ) ;
#94679=CARTESIAN_POINT ( 'NONE',  ( 5.894527261468666346, 1.877221869688485700, -1.315242172555250555 ) ) ;
#94680=CARTESIAN_POINT ( 'NONE',  ( 4.716618446111438878, -0.08105245650613655817, 1.738572149171065062 ) ) ;
#94683=CARTESIAN_POINT ( 'NONE',  ( 4.657415279524609986, -0.3804069660688877974, -1.691394979786196684 ) ) ;
#94685=CARTESIAN_POINT ( 'NONE',  ( 4.246645257758387970, -2.146983142244869747, -0.3225670219409969008 ) ) ;
#94687=CARTESIAN_POINT ( 'NONE',  ( -0.1880716927101276914, -1.308626981353334662, -1.665352682907685233 ) ) ;
#94688=CARTESIAN_POINT ( 'NONE',  ( 6.000000000000004441, -3.414667428843525066E-13, -2.052068128417939619 ) ) ;
#94691=CARTESIAN_POINT ( 'NONE',  ( 2.872000511136533873, 1.029149822700244465, 1.628267440728261573 ) ) ;
#94693=CARTESIAN_POINT ( 'NONE',  ( 0.5049021242206577220, -2.205252279087748235, -0.2660074523756980058 ) ) ;
#94695=CARTESIAN_POINT ( 'NONE',  ( -0.2411972340275969906, 1.382285239182699854, -2.157708601731861187 ) ) ;
#94698=CARTESIAN_POINT ( 'NONE',  ( 2.280208067491045654, 2.177836876428246971, -0.4364916025852043635 ) ) ;
#94703=CARTESIAN_POINT ( 'NONE',  ( 0.4225002777262388265, -1.427939226333583500, -1.423959630194884696 ) ) ;
#94705=CARTESIAN_POINT ( 'NONE',  ( 5.160619382589332282, -0.6916465251813638249, -1.943403241031741002 ) ) ;
#94709=CARTESIAN_POINT ( 'NONE',  ( 0.6140562859980386312, 1.226574898224697119, -1.275979240986246710 ) ) ;
#94710=CARTESIAN_POINT ( 'NONE',  ( 5.449791032962750137, -1.571470184986222263, -0.7336466892688772168 ) ) ;
#94711=CARTESIAN_POINT ( 'NONE',  ( 6.005355179794888976, -1.726165566969834586, 0.2220549178573327509 ) ) ;
#94712=CARTESIAN_POINT ( 'NONE',  ( 3.368946006165595364, 0.05471657373835739357, -2.291868861755571363 ) ) ;
#94714=CARTESIAN_POINT ( 'NONE',  ( 2.378628397106247849, 1.683441843134887428, -0.7459445200509451368 ) ) ;
#94717=CARTESIAN_POINT ( 'NONE',  ( 2.080808903162992607, -0.08653491207171599975, -1.823647505904809174 ) ) ;
#94718=CARTESIAN_POINT ( 'NONE',  ( 2.707657903872981553, 1.899618770239443366, 0.6767133375917554483 ) ) ;
#94721=CARTESIAN_POINT ( 'NONE',  ( 4.419037640130375699, 1.924477966361681780, 0.8556825127635151462 ) ) ;
#94724=CARTESIAN_POINT ( 'NONE',  ( 2.365759603224312446, -0.4558734232973959966, 2.019384234097781228 ) ) ;
#94727=CARTESIAN_POINT ( 'NONE',  ( 4.846395287928321416, 1.089488137594313510, -1.819044145143506208 ) ) ;
#94728=CARTESIAN_POINT ( 'NONE',  ( 0.3285744372712772199, 1.843197283691574873, 0.5604049541020996728 ) ) ;
#94735=CARTESIAN_POINT ( 'NONE',  ( 6.240501835383900797, 1.219778281852833546, -1.734492557903525523 ) ) ;
#94736=CARTESIAN_POINT ( 'NONE',  ( 1.536301591958776802, 1.038269187514633485, -1.832158284056581543 ) ) ;
#94739=CARTESIAN_POINT ( 'NONE',  ( 5.348444835920818541, -1.846650980718677726, -0.2298375257220597323 ) ) ;
#94747=CARTESIAN_POINT ( 'NONE',  ( 2.277722772326017608, -1.903703133612335119, 0.4737097981617058862 ) ) ;
#94748=CARTESIAN_POINT ( 'NONE',  ( 1.077287230265553397, -0.05381693868444264311, -2.161191418701657430 ) ) ;
#94752=CARTESIAN_POINT ( 'NONE',  ( 3.303724397909554078, -1.530444925530007216, 0.8147494179842218465 ) ) ;
#94753=CARTESIAN_POINT ( 'NONE',  ( 1.886251080576596406, 1.515106702303461894, -0.8561229301769134326 ) ) ;
#94756=CARTESIAN_POINT ( 'NONE',  ( 0.9485920322965735174, 1.351945250224910744, 1.495824703658617416 ) ) ;
#94757=CARTESIAN_POINT ( 'NONE',  ( 6.925078400183531713, 7.629137130509035636, 2.844348168701658075 ) ) ;
#94760=CARTESIAN_POINT ( 'NONE',  ( 0.8835904138565253696, 1.322268204680861814, 1.462458760404183433 ) ) ;
#94762=CARTESIAN_POINT ( 'NONE',  ( 5.888906298306328502, -1.818048641159516476, -0.5935555146628914702 ) ) ;
#94767=CARTESIAN_POINT ( 'NONE',  ( 0.9615888033541221125, -1.593469042607889463, -1.240847856016368489 ) ) ;
#94768=CARTESIAN_POINT ( 'NONE',  ( 4.050101169753547836, 0.7808133845815302676, -2.171591319759837546 ) ) ;
#94769=CARTESIAN_POINT ( 'NONE',  ( 6.197705743426439540, -1.420020466879829302, -1.353909852041992767 ) ) ;
#94770=CARTESIAN_POINT ( 'NONE',  ( 2.746866186719683967, -0.3305370478365337039, -1.933541032166598672 ) ) ;
#94774=CARTESIAN_POINT ( 'NONE',  ( 0.8665975061730617490, -2.067159395656243515, -0.4576585243742418152 ) ) ;
#94777=CARTESIAN_POINT ( 'NONE',  ( 2.167674216824653222, -1.133089441918342599, 1.451089449600144521 ) ) ;
#94780=CARTESIAN_POINT ( 'NONE',  ( 2.426173717206762781, -2.096881089210366422, 0.3156149858808757203 ) ) ;
#94784=CARTESIAN_POINT ( 'NONE',  ( 3.690745141589413691, -0.3983964448436724259, -2.021722667813256269 ) ) ;
#94786=CARTESIAN_POINT ( 'NONE',  ( 0.3625324912872701089, 0.1813134127766780901, -1.832273687604975665 ) ) ;
#94788=CARTESIAN_POINT ( 'NONE',  ( 0.07775346131142638062, 0.2253410668615995205, -2.322482355083537175 ) ) ;
#94791=CARTESIAN_POINT ( 'NONE',  ( 0.3466626200071438180, 2.201290530325435757, 0.1579762268871589825 ) ) ;
#94792=CARTESIAN_POINT ( 'NONE',  ( 3.040562418613635742, 2.244949603584453612, 0.2802003048723368805 ) ) ;
#94794=CARTESIAN_POINT ( 'NONE',  ( 2.443383269832733795, -1.689004019812107460, 0.6554920229192174874 ) ) ;
#94795=CARTESIAN_POINT ( 'NONE',  ( 3.555789339581526320, 1.068723753765013162, 1.589688962476828005 ) ) ;
#94796=CARTESIAN_POINT ( 'NONE',  ( 4.053231837324381637, 1.750648263899981849, -1.104974720517466480 ) ) ;
#94798=CARTESIAN_POINT ( 'NONE',  ( 1.850399468497238242, 0.6164509289473228959, 1.872685729773468255 ) ) ;
#94799=CARTESIAN_POINT ( 'NONE',  ( 0.1473221176215748218, -1.486828977120215001, -1.224531343831699592 ) ) ;
#94800=CARTESIAN_POINT ( 'NONE',  ( 2.764352523130030548, -1.291370965961564421, 1.353630663414123969 ) ) ;
#94801=ADVANCED_FACE ( 'NONE', ( #130344 ), #113172, .F. ) ;
#94802=CARTESIAN_POINT ( 'NONE',  ( 2.368180137760375281, 2.262835426277497675, -0.4520343961368147312 ) ) ;
#94804=CARTESIAN_POINT ( 'NONE',  ( 2.804952713220637328, -1.548975583508698683, 1.031263495014663523 ) ) ;
#94806=CARTESIAN_POINT ( 'NONE',  ( 0.2333540202161610289, 0.003568502611739353923, -2.045944795905803471 ) ) ;
#94810=CARTESIAN_POINT ( 'NONE',  ( 6.001026715709635972, 1.723673884808615497, -1.209685691799726737 ) ) ;
#94812=CARTESIAN_POINT ( 'NONE',  ( 5.923154835166895893, -0.05960684409221649049, 2.160954015416292506 ) ) ;
#94813=CARTESIAN_POINT ( 'NONE',  ( -0.08762443420157886576, -2.019435065594810119, -0.04520711721162430641 ) ) ;
#94817=CARTESIAN_POINT ( 'NONE',  ( 6.925078400183545035, 3.707308446744279617, 2.270182774727365516 ) ) ;
#94820=CARTESIAN_POINT ( 'NONE',  ( 4.962125165302472496, -1.116212726388360998, 1.679221540125563905 ) ) ;
#94825=CARTESIAN_POINT ( 'NONE',  ( 6.034075718726629844, 1.069613854859407631, -1.878468107683453514 ) ) ;
#94829=CARTESIAN_POINT ( 'NONE',  ( 6.603150281434943203, -0.1430492952050037847, 1.984088717376513822 ) ) ;
#94833=CARTESIAN_POINT ( 'NONE',  ( 2.033451192367647042, -1.125475165956592694, -1.307177254964901003 ) ) ;
#94837=CARTESIAN_POINT ( 'NONE',  ( 1.194210174654856127, -0.4229520329555501723, -1.718335688698314101 ) ) ;
#94838=CARTESIAN_POINT ( 'NONE',  ( 0.8561085696928095734, 0.8139254773164643630, -1.841379974997810143 ) ) ;
#94840=CARTESIAN_POINT ( 'NONE',  ( 3.557846488308267663, 0.5383450771202847873, -2.139971664446515653 ) ) ;
#94841=CARTESIAN_POINT ( 'NONE',  ( 5.717690620771469945, 0.4309847871033903877, -2.127713340945025511 ) ) ;
#94845=CARTESIAN_POINT ( 'NONE',  ( 2.807414684038778141, 1.817529592918063708, -1.092056846721880969 ) ) ;
#94846=CARTESIAN_POINT ( 'NONE',  ( 3.374625213368151133, -0.3961236654455925765, -1.976952669325626299 ) ) ;
#94847=CARTESIAN_POINT ( 'NONE',  ( 3.392628153686805259, -1.747241832701627473, -0.4783254123041839057 ) ) ;
#94851=CARTESIAN_POINT ( 'NONE',  ( 0.4966798268824790252, 1.557709316500059726, -1.035497600327957235 ) ) ;
#94854=CARTESIAN_POINT ( 'NONE',  ( 1.428765994036251818, -1.616370030362016985, 1.027966131488191381 ) ) ;
#94855=CARTESIAN_POINT ( 'NONE',  ( 0.07459516483346910476, 0.007201286963446154772, -1.755573347271716544 ) ) ;
#94860=CARTESIAN_POINT ( 'NONE',  ( 5.260679775997886054, -1.568431141927080219, 1.487858469166832398 ) ) ;
#94864=CARTESIAN_POINT ( 'NONE',  ( 3.603867943843573673, 1.538443694073919898, 1.459757404076333698 ) ) ;
#94865=CARTESIAN_POINT ( 'NONE',  ( -0.02988540731103071432, 7.629137130509069387, -2.326318838967501357 ) ) ;
#94867=CARTESIAN_POINT ( 'NONE',  ( 4.516842978191152547, 1.801120551983675266, 0.8018027747202867150 ) ) ;
#94868=CARTESIAN_POINT ( 'NONE',  ( 0.2463402104127752068, 1.031448792800106595, -1.728751203700854111 ) ) ;
#94870=CARTESIAN_POINT ( 'NONE',  ( 5.348860635491798909, -1.915306066586830669, -0.9028416433708542632 ) ) ;
#94872=CARTESIAN_POINT ( 'NONE',  ( 0.6255436495894195481, 0.2045281481408110225, -2.060252820462626477 ) ) ;
#94873=CARTESIAN_POINT ( 'NONE',  ( 2.870961461768199108, 1.843879596475753502, -0.6095136124301904212 ) ) ;
#94878=CARTESIAN_POINT ( 'NONE',  ( 2.027394857466585432, -1.366561296588153063, -1.582253647643002914 ) ) ;
#94881=CARTESIAN_POINT ( 'NONE',  ( -0.04078422793344065045, -1.398654746659812043, -1.150989216800960335 ) ) ;
#94882=ORIENTED_EDGE ( 'NONE', *, *, #80635, .T. ) ;
#94883=CARTESIAN_POINT ( 'NONE',  ( 4.336686996305870068, 2.164023489887345164, 0.4319772483800735086 ) ) ;
#94885=CARTESIAN_POINT ( 'NONE',  ( 3.557846488308267663, 0.5383450771202848983, -2.139971664446515653 ) ) ;
#94888=CARTESIAN_POINT ( 'NONE',  ( 1.260255548581414642, 1.910129771108992625, 0.09294656408432439010 ) ) ;
#94890=CARTESIAN_POINT ( 'NONE',  ( 5.828598057497599960, -1.316348130051235410, 1.597988563933512074 ) ) ;
#94892=CARTESIAN_POINT ( 'NONE',  ( 3.010779355932476253, 1.566693023359872372, -1.489686202715050145 ) ) ;
#94893=CARTESIAN_POINT ( 'NONE',  ( 4.423480980095358284, -1.348712413769267426, -1.727291790683552541 ) ) ;
#94902=CARTESIAN_POINT ( 'NONE',  ( 0.5279704824466545654, -1.728000714500482982, 1.038995864524896673 ) ) ;
#94905=CARTESIAN_POINT ( 'NONE',  ( 5.084861876562203342, 1.979495018489594305, 0.6061691862097525751 ) ) ;
#94906=CARTESIAN_POINT ( 'NONE',  ( 3.000521647167487593, -0.5595019940488660248, -1.843462078654713343 ) ) ;
#94907=CARTESIAN_POINT ( 'NONE',  ( 6.503513627744350600, -2.053693679520858684, 0.5143327402655095693 ) ) ;
#94912=CARTESIAN_POINT ( 'NONE',  ( 3.555474331475856786, 1.549626312082365898, 1.215309171139463684 ) ) ;
#94913=CARTESIAN_POINT ( 'NONE',  ( 0.2522424171345696298, 0.8426718423822797677, 2.023156535103701970 ) ) ;
#94914=CARTESIAN_POINT ( 'NONE',  ( 4.494645072041675071, -0.4025399330690944133, -1.780595394402582077 ) ) ;
#94921=CARTESIAN_POINT ( 'NONE',  ( 1.206327419354651820, 1.623952629372883427, 0.8676893986077349741 ) ) ;
#94922=CARTESIAN_POINT ( 'NONE',  ( 5.010025764882303001, -0.7205479882510434919, 1.880027049715059073 ) ) ;
#94923=CARTESIAN_POINT ( 'NONE',  ( 0.7382080005397623212, -2.165046367600947708, -0.7717227881791683952 ) ) ;
#94924=CARTESIAN_POINT ( 'NONE',  ( 5.295737746731337126, -1.384591195607473235, -1.390005841682784959 ) ) ;
#94926=CARTESIAN_POINT ( 'NONE',  ( 0.2333690889706682703, 0.003390530909083006028, -2.053566628440507635 ) ) ;
#94930=CARTESIAN_POINT ( 'NONE',  ( 1.769195444908505888, 1.999712852614519143, -0.6101556835421716452 ) ) ;
#94931=CARTESIAN_POINT ( 'NONE',  ( 6.631742710195931423, -1.160100399838214891, -1.336722620761298330 ) ) ;
#94933=CARTESIAN_POINT ( 'NONE',  ( -0.1104750535120268828, 2.006893987364383403, -2.517811492722863864 ) ) ;
#94934=CARTESIAN_POINT ( 'NONE',  ( 1.399541807966601104, -0.6259456572170263300, -1.624154832779246993 ) ) ;
#94938=CARTESIAN_POINT ( 'NONE',  ( 1.629113003107704793, -1.625012167801738183, 0.5787621435916143753 ) ) ;
#94939=CARTESIAN_POINT ( 'NONE',  ( 1.593588134247824639, -0.7342643958434189599, 2.065040727587868830 ) ) ;
#94940=CARTESIAN_POINT ( 'NONE',  ( 3.879664727460280904, 2.078262106501146622, -0.7427522710690689367 ) ) ;
#94942=CARTESIAN_POINT ( 'NONE',  ( 1.376089442288459752, -2.118726187661602367, 0.4732455120740781673 ) ) ;
#94943=CARTESIAN_POINT ( 'NONE',  ( 1.066719475142905216, -1.649486405746130258, -0.7827983987617056494 ) ) ;
#94944=CARTESIAN_POINT ( 'NONE',  ( 3.011064194431464003, 0.05668958241028876355, 2.116758953476727267 ) ) ;
#94945=CARTESIAN_POINT ( 'NONE',  ( 6.539320575229249144, 0.007148032025052972194, 1.896977914940492393 ) ) ;
#94947=CARTESIAN_POINT ( 'NONE',  ( 3.544716187562162446, -1.873399702441876480, 1.320855843532109608 ) ) ;
#94949=CARTESIAN_POINT ( 'NONE',  ( 0.07755575628184004089, 7.629137130509076492, -2.788902932953695846 ) ) ;
#94951=CARTESIAN_POINT ( 'NONE',  ( 6.217462558288930019, 1.845152235743243052, 1.236491063047394201 ) ) ;
#94957=CARTESIAN_POINT ( 'NONE',  ( 3.692029868468839737, 1.730865839653324079, 1.034166058993556181 ) ) ;
#94959=CARTESIAN_POINT ( 'NONE',  ( 2.008709601793839283, 0.6428708581102732245, 1.959923294053036669 ) ) ;
#94964=CARTESIAN_POINT ( 'NONE',  ( 5.402338782601354694, 1.661146971675907302, -1.429436781345946317 ) ) ;
#94965=CARTESIAN_POINT ( 'NONE',  ( 1.899064777474347654, -0.9530127170578571727, -1.777010740487514173 ) ) ;
#94966=CARTESIAN_POINT ( 'NONE',  ( 2.542321706073047416, -1.529623444112483632, 1.024600984555257277 ) ) ;
#94969=CARTESIAN_POINT ( 'NONE',  ( 2.281250000000002220, 0.7852924748301068902, 1.895863743164037718 ) ) ;
#94970=CARTESIAN_POINT ( 'NONE',  ( 5.350558509363329662, 0.5315954154057299652, 1.746479326997903092 ) ) ;
#94972=CARTESIAN_POINT ( 'NONE',  ( 6.170546107226446253, 1.392543322632183722, 1.458558933167881211 ) ) ;
#94974=CARTESIAN_POINT ( 'NONE',  ( 5.998944898715565799, 1.853732409352136568, -1.296943227565182877 ) ) ;
#94976=CARTESIAN_POINT ( 'NONE',  ( 0.2410290108679030985, 0.3623031737408002884, 2.074505700167991407 ) ) ;
#94987=CARTESIAN_POINT ( 'NONE',  ( 1.389100911873580646, -2.015333191458138273, -0.6601287711371638389 ) ) ;
#94988=CARTESIAN_POINT ( 'NONE',  ( 2.408681662258719047, -2.215777464676274011, -0.1586666079704464882 ) ) ;
#94992=CARTESIAN_POINT ( 'NONE',  ( 3.859774877264535053, -0.5717695562157121270, 1.876676618968641019 ) ) ;
#94999=CARTESIAN_POINT ( 'NONE',  ( 2.549219474610735947, 0.2639673528169217964, 2.104066465523121376 ) ) ;
#95001=CARTESIAN_POINT ( 'NONE',  ( 4.065412822539622439, 0.2671453805177248508, -2.145074402785766665 ) ) ;
#95002=CARTESIAN_POINT ( 'NONE',  ( 3.755264181858388284, 1.826884192416846853, -0.2291247506851084581 ) ) ;
#95005=CARTESIAN_POINT ( 'NONE',  ( 5.824081541776103599, 1.678935111502709354, 0.4578980800337121848 ) ) ;
#95009=CARTESIAN_POINT ( 'NONE',  ( 3.485389320157119997, 1.955090977548096687, -0.9225387301767663528 ) ) ;
#95010=CARTESIAN_POINT ( 'NONE',  ( 5.764999918528635803, -2.016288307888712161, -0.002809016773450134351 ) ) ;
#95012=CARTESIAN_POINT ( 'NONE',  ( 2.202237438260604030, -2.161223104231101644, 0.05255616829508147347 ) ) ;
#95013=CARTESIAN_POINT ( 'NONE',  ( 3.620352162249322880, 1.253078330817010588, -1.521826374184510389 ) ) ;
#95014=CARTESIAN_POINT ( 'NONE',  ( -0.09381621004311831158, -0.9424329983100244723, -1.976553698157037076 ) ) ;
#95015=CARTESIAN_POINT ( 'NONE',  ( 4.581548892214976298, -0.9124856661332171326, 1.714327114426909882 ) ) ;
#95024=CARTESIAN_POINT ( 'NONE',  ( 0.8157880970438775581, -0.3219574891645953785, 2.183050487710703536 ) ) ;
#95026=CARTESIAN_POINT ( 'NONE',  ( 6.368018226480639754, -1.947316962026977682, 0.2367824842242904348 ) ) ;
#95030=CARTESIAN_POINT ( 'NONE',  ( 0.07479286986303290696, 5.725009232006174287, -2.449550298930736059 ) ) ;
#95031=CARTESIAN_POINT ( 'NONE',  ( 5.331922971087851515, 1.814509544241477146, 0.3110680438872318043 ) ) ;
#95036=CARTESIAN_POINT ( 'NONE',  ( 6.486587849989844834, -1.303813291173651301, 1.673118453357678392 ) ) ;
#95040=CARTESIAN_POINT ( 'NONE',  ( 6.362583954249420692, -1.460576210990358614, 1.454072064785590479 ) ) ;
#95042=CARTESIAN_POINT ( 'NONE',  ( 1.697469458906812667, -1.344883679737416404, -1.286638954052413908 ) ) ;
#95043=CARTESIAN_POINT ( 'NONE',  ( 3.597050949361340511, -0.5310884314010614338, 1.763007376093472800 ) ) ;
#95049=CARTESIAN_POINT ( 'NONE',  ( 3.387540773601561916, 1.995160029947869340, -0.9435142334218297178 ) ) ;
#95050=CARTESIAN_POINT ( 'NONE',  ( 5.624405936800197736, 1.354097840178031475, -1.812292894430814094 ) ) ;
#95052=CARTESIAN_POINT ( 'NONE',  ( 5.748286673958676651, 0.8850744635948673000, -1.580567631948928797 ) ) ;
#95053=CARTESIAN_POINT ( 'NONE',  ( 6.104688764726555306, 1.790162971792093272, 0.6826718079199489697 ) ) ;
#95054=EDGE_CURVE ( 'NONE', #119587, #150638, #34621, .T. ) ;
#95056=CARTESIAN_POINT ( 'NONE',  ( 6.543822781336226413, 0.7137633992815132222, -1.729328153040734506 ) ) ;
#95058=CARTESIAN_POINT ( 'NONE',  ( 5.531871257421491883, -1.864710570029969317, 0.4231498525801706823 ) ) ;
#95061=CARTESIAN_POINT ( 'NONE',  ( 1.147088892781012781, -1.472398045354219365, -1.153743250124287689 ) ) ;
#95062=CARTESIAN_POINT ( 'NONE',  ( 1.762908039156896978, -0.1037823317905466058, -2.014007988105172231 ) ) ;
#95064=CARTESIAN_POINT ( 'NONE',  ( 3.071027892464781583, -1.946086441943569723, -0.8056474276203289264 ) ) ;
#95070=CARTESIAN_POINT ( 'NONE',  ( 2.672133692126318127, 2.009681031688851593, -0.2020390005853574256 ) ) ;
#95073=CARTESIAN_POINT ( 'NONE',  ( 3.251412196806032995, -1.765091617811213931, -1.247493029685270649 ) ) ;
#95079=CARTESIAN_POINT ( 'NONE',  ( 0.3621003815536598669, -0.5783089063249653439, 2.092656953901766315 ) ) ;
#95084=CARTESIAN_POINT ( 'NONE',  ( 2.366952063387484095, 0.1042156695447923470, -2.189191704635709890 ) ) ;
#95085=CARTESIAN_POINT ( 'NONE',  ( 6.983263157960366563, 3.694515354052980260, 2.467960814016751936 ) ) ;
#95086=CARTESIAN_POINT ( 'NONE',  ( 2.290224401178039049, -0.9674489778378884131, 2.045383877150886320 ) ) ;
#95093=CARTESIAN_POINT ( 'NONE',  ( 4.042088942692352305, 1.761052656288846663, 0.1752445044498444349 ) ) ;
#95095=CARTESIAN_POINT ( 'NONE',  ( 0.3586045525620683017, 0.8063113102214304329, 1.945692106844071789 ) ) ;
#95099=CARTESIAN_POINT ( 'NONE',  ( 6.485953897545715385, -2.015913262743720402, 0.05231248585663844652 ) ) ;
#95102=CARTESIAN_POINT ( 'NONE',  ( 3.133525119713890472, -1.255248497922526463, -1.387151338369890574 ) ) ;
#95103=CARTESIAN_POINT ( 'NONE',  ( 3.291909242638372923, -1.386922682245657734, -1.537212927083357217 ) ) ;
#95108=CARTESIAN_POINT ( 'NONE',  ( 6.614160618316515361, -1.014195557614630427, -1.909021090911746876 ) ) ;
#95111=CARTESIAN_POINT ( 'NONE',  ( 2.892962425504439050, 0.2373818416543191367, 1.947367909387688112 ) ) ;
#95112=CARTESIAN_POINT ( 'NONE',  ( 1.018907413236518789, 2.013924516646655949, -0.09611688112247382398 ) ) ;
#95117=CARTESIAN_POINT ( 'NONE',  ( 1.071320448993583918, 1.804315561281001123, -0.4931735697189034151 ) ) ;
#95119=CARTESIAN_POINT ( 'NONE',  ( 3.410405542056849981, -2.011076457950426555, -0.09466423678533388009 ) ) ;
#95121=CARTESIAN_POINT ( 'NONE',  ( 1.810321443220731075, 1.215999664948445913, -1.733040945678490319 ) ) ;
#95123=CARTESIAN_POINT ( 'NONE',  ( 4.053231837324381637, 1.750648263899981849, -1.104974720517466480 ) ) ;
#95125=CARTESIAN_POINT ( 'NONE',  ( 0.02900754732045561154, -1.909850462538491778, 0.8511534736125156986 ) ) ;
#95127=CARTESIAN_POINT ( 'NONE',  ( 5.209893869493905427, -1.816617279468687229, 0.1804919988709560719 ) ) ;
#95132=CARTESIAN_POINT ( 'NONE',  ( 6.528370574810466564, 1.275976099532463603, -1.800301716031265764 ) ) ;
#95134=CARTESIAN_POINT ( 'NONE',  ( 4.565046243057500952, -1.533749416048999947, 1.141898535029245432 ) ) ;
#95142=CARTESIAN_POINT ( 'NONE',  ( 4.938664768831324992, 0.3182328507864222722, 1.843102042236575366 ) ) ;
#95143=CARTESIAN_POINT ( 'NONE',  ( -0.02319159430949797526, 7.629137130509074716, -2.410989586153565067 ) ) ;
#95149=CARTESIAN_POINT ( 'NONE',  ( 0.9890311015656474414, 0.1392606914251882932, 1.964554613873798594 ) ) ;
#95150=CARTESIAN_POINT ( 'NONE',  ( 3.040638836679772528, -1.525031945187466098, 1.319243992433154267 ) ) ;
#95153=CARTESIAN_POINT ( 'NONE',  ( 6.727182134110167411, 4.685720203848058318, 2.851561905840187983 ) ) ;
#95155=CARTESIAN_POINT ( 'NONE',  ( 3.310656966840678894, 1.981231107410564851, 0.9368519390955745152 ) ) ;
#95157=CARTESIAN_POINT ( 'NONE',  ( 2.485270279442112429, 1.762041721199611333, -0.7789696210150058864 ) ) ;
#95159=CARTESIAN_POINT ( 'NONE',  ( -0.1296875068448125057, 0.2507808023153486054, -1.861542470327881560 ) ) ;
#95160=CARTESIAN_POINT ( 'NONE',  ( 0.1331565106231606399, 5.723858289613107608, -2.539976893513963052 ) ) ;
#95168=CARTESIAN_POINT ( 'NONE',  ( 4.563899478665734755, -1.199029595066217313, 1.397436126395680267 ) ) ;
#95169=CARTESIAN_POINT ( 'NONE',  ( 2.192043262494451916, 1.240095455230303401, 1.585687145212981042 ) ) ;
#95170=CARTESIAN_POINT ( 'NONE',  ( 4.323764262282871584, -1.706850429308865547, 1.539420282360188574 ) ) ;
#95171=CARTESIAN_POINT ( 'NONE',  ( -0.02880301295726198432, 2.855735178999906587, -2.761736421759506399 ) ) ;
#95172=CARTESIAN_POINT ( 'NONE',  ( 2.008444763995967275, 0.5780311502073384178, 1.769000597778628947 ) ) ;
#95175=CARTESIAN_POINT ( 'NONE',  ( 5.590081826628392925, 1.144292256163012667, 1.532101299821154949 ) ) ;
#95178=CARTESIAN_POINT ( 'NONE',  ( 4.423432795095141756, -1.287707899167778169, -1.647015592753127589 ) ) ;
#95179=CARTESIAN_POINT ( 'NONE',  ( 3.010468980803046257, 1.356049738124785353, -1.288842618233053683 ) ) ;
#95183=CARTESIAN_POINT ( 'NONE',  ( 4.898908426394765314, 1.431408964483871227, -0.9620984105884394788 ) ) ;
#95185=CARTESIAN_POINT ( 'NONE',  ( 0.7735316488602840268, 1.530413877909537979, -0.8155550471512038602 ) ) ;
#95187=SURFACE_STYLE_FILL_AREA ( #128809 ) ;
#95188=CARTESIAN_POINT ( 'NONE',  ( 5.594640809421455252, 2.137687854117083841, 0.3785394800270032167 ) ) ;
#95189=CARTESIAN_POINT ( 'NONE',  ( 4.811078068098579408, 1.589968679568127596, 0.8971634079883783475 ) ) ;
#95190=CARTESIAN_POINT ( 'NONE',  ( 2.430452978529148655, -1.210835280720125917, 1.543375930141199115 ) ) ;
#95191=CARTESIAN_POINT ( 'NONE',  ( -0.01776408051935850912, -2.116861762172245420, -0.04693027993646693707 ) ) ;
#95195=CARTESIAN_POINT ( 'NONE',  ( 2.262495435604610527, 2.120074037919957632, 0.04929290001921824566 ) ) ;
#95201=CARTESIAN_POINT ( 'NONE',  ( 1.094682738308445202, 2.038987083759949304, 0.3576228084290478115 ) ) ;
#95205=CARTESIAN_POINT ( 'NONE',  ( 2.403257875557132994, -0.3827610287685556112, -2.187935401104672994 ) ) ;
#95207=CARTESIAN_POINT ( 'NONE',  ( 0.2648075084464130979, 2.141788565065712913, -0.8351287359565621182 ) ) ;
#95209=CARTESIAN_POINT ( 'NONE',  ( 5.366109125895877519, -2.053123361074739250, 0.1969011160823062045 ) ) ;
#95213=CARTESIAN_POINT ( 'NONE',  ( 0.1331565106231571705, 6.948071080078889850, -2.540993614958915181 ) ) ;
#95214=CARTESIAN_POINT ( 'NONE',  ( 5.020983453748395497, -1.746657797055195305, 0.5827527221545365510 ) ) ;
#95216=CARTESIAN_POINT ( 'NONE',  ( 0.000000000000000000, 0.000000000000000000, 0.000000000000000000 ) ) ;
#95217=CARTESIAN_POINT ( 'NONE',  ( 3.416762500535154068, 1.558979225792535006, 0.7381585831351898941 ) ) ;
#95218=CARTESIAN_POINT ( 'NONE',  ( 1.428923106112218067, -1.700960256238340573, 1.082842518468102089 ) ) ;
#95219=CARTESIAN_POINT ( 'NONE',  ( 3.217717873326145117, 2.243214920517083044, 0.5014430322199947554 ) ) ;
#95221=CARTESIAN_POINT ( 'NONE',  ( 2.548426268707996822, 2.261836392764454473, 0.05785012348054861114 ) ) ;
#95222=CARTESIAN_POINT ( 'NONE',  ( 3.668672709498523865, -1.414518211590541252, 1.560516469030509334 ) ) ;
#95224=CARTESIAN_POINT ( 'NONE',  ( 3.690472162876729190, -0.3426837954879756731, -1.736044821310823938 ) ) ;
#95227=CARTESIAN_POINT ( 'NONE',  ( 6.058190142838977721, -1.623990863767441617, 1.618158029567408729 ) ) ;
#95228=CARTESIAN_POINT ( 'NONE',  ( 5.015489797737916255, -0.9877249803392706973, -1.553577481828890106 ) ) ;
#95234=CARTESIAN_POINT ( 'NONE',  ( 4.154361996720875361, -1.624486827992781990, 1.471056368041193441 ) ) ;
#95239=CARTESIAN_POINT ( 'NONE',  ( 2.965364049027201965, 0.2823637808789316028, -1.905579842893694975 ) ) ;
#95243=CARTESIAN_POINT ( 'NONE',  ( 0.1061415085658158342, 1.651838695520141398, 1.485519503937395402 ) ) ;
#95252=CARTESIAN_POINT ( 'NONE',  ( 2.050002923743666550, -1.344770872215072632, 1.104816081682137963 ) ) ;
#95254=CARTESIAN_POINT ( 'NONE',  ( 0.4144086874100678664, 0.7473079093508437909, 1.814158889769983185 ) ) ;
#95257=CARTESIAN_POINT ( 'NONE',  ( 6.772347375734490527, -1.334533509509854943, 1.701269717329929820 ) ) ;
#95261=CARTESIAN_POINT ( 'NONE',  ( 5.207972885698374022, -2.151664816535401314, 0.2080130470862306957 ) ) ;
#95265=CARTESIAN_POINT ( 'NONE',  ( 6.889933812677610625, -0.8438472966565238043, 1.779621742589713618 ) ) ;
#95266=CARTESIAN_POINT ( 'NONE',  ( 6.696678128945787734, -1.136521523357211017, -1.309519827187540564 ) ) ;
#95268=CARTESIAN_POINT ( 'NONE',  ( 3.491892070630482348, -2.189115664112693871, -0.1057334378413293807 ) ) ;
#95269=CARTESIAN_POINT ( 'NONE',  ( 2.819673282491507393, -0.2271757706859862669, 2.296386706371948527 ) ) ;
#95270=CARTESIAN_POINT ( 'NONE',  ( 5.729779026133646092, -1.304086877343976880, -1.595700086769378023 ) ) ;
#95271=CARTESIAN_POINT ( 'NONE',  ( 0.6912261618599843116, -0.6995774015170745930, 1.811736774657431548 ) ) ;
#95276=CARTESIAN_POINT ( 'NONE',  ( 3.691739789689612472, 1.995538565534977549, -0.7177698711837015022 ) ) ;
#95278=CARTESIAN_POINT ( 'NONE',  ( 2.830704105008190030, 0.7231396562890278767, -1.882474209725725434 ) ) ;
#95280=CARTESIAN_POINT ( 'NONE',  ( 5.333140672905051893, 0.1575165696711364749, 2.201206011701982934 ) ) ;
#95286=CARTESIAN_POINT ( 'NONE',  ( 6.825078400183554272, 2.951006455646578264, 2.596623860847916188 ) ) ;
#95289=CARTESIAN_POINT ( 'NONE',  ( 4.856353099686935515, 0.7867916563346208925, 1.904994776275979129 ) ) ;
#95295=CARTESIAN_POINT ( 'NONE',  ( 3.756514258062096712, 2.010158954970509892, 0.1956256540626959695 ) ) ;
#95300=CARTESIAN_POINT ( 'NONE',  ( 2.694271958740936945, -2.055289539400024790, -0.1528356987768857700 ) ) ;
#95301=CARTESIAN_POINT ( 'NONE',  ( 2.637342451166882373, 0.6819965276749391236, 1.897697610567940174 ) ) ;
#95307=CARTESIAN_POINT ( 'NONE',  ( 2.917342117414220670, 0.6766092434087739305, 1.899328150365031664 ) ) ;
#95308=CARTESIAN_POINT ( 'NONE',  ( 2.466542765887615563, 0.09048117372523720170, -1.839033023284454060 ) ) ;
#95309=CARTESIAN_POINT ( 'NONE',  ( 0.2589922964784003301, 0.8893095213439340396, 2.129655304206728328 ) ) ;
#95311=CARTESIAN_POINT ( 'NONE',  ( 2.583474834239877449, 1.977432880963815309, -0.8734481387390122809 ) ) ;
#95313=CARTESIAN_POINT ( 'NONE',  ( 4.540305813605725938, 0.8135460886731570307, 1.954998174167394520 ) ) ;
#95315=CARTESIAN_POINT ( 'NONE',  ( 2.689158180196444814, -1.321807234245642615, -1.880123443969876629 ) ) ;
#95319=CARTESIAN_POINT ( 'NONE',  ( 1.762360912074714125, -1.325010844092512796, 1.320751239342173200 ) ) ;
#95320=CARTESIAN_POINT ( 'NONE',  ( 6.086792475191005636, -0.2889037430471863566, -1.950060635722290936 ) ) ;
#95324=CARTESIAN_POINT ( 'NONE',  ( 1.120068590173186163, -2.152398693614396397, 0.4866647226241942459 ) ) ;
#95325=CARTESIAN_POINT ( 'NONE',  ( 6.760220206081136496, -2.069995208266177666, 0.04663682477341199450 ) ) ;
#95328=CARTESIAN_POINT ( 'NONE',  ( 6.539320575229294441, 2.949125184229839380, 2.655650464557571144 ) ) ;
#95329=CARTESIAN_POINT ( 'NONE',  ( 5.489129097700779170, 1.738912991666073715, -0.9288780838571459864 ) ) ;
#95330=CARTESIAN_POINT ( 'NONE',  ( -0.1225938595818750754, -1.897163925677572305, -0.9476133185889324961 ) ) ;
#95332=CARTESIAN_POINT ( 'NONE',  ( 4.283989073270632275, 1.505461842163426933, 1.749087475023381133 ) ) ;
#95333=CARTESIAN_POINT ( 'NONE',  ( 2.061455334089828284, 1.712470851095546642, 1.149345886162132402 ) ) ;
#95341=CARTESIAN_POINT ( 'NONE',  ( 4.457605324860562490, 1.741341149747036576, 1.296620029562136400 ) ) ;
#95343=CARTESIAN_POINT ( 'NONE',  ( 3.702549152423353807, 1.581054339307564449, 0.9433870219286569769 ) ) ;
#95345=CARTESIAN_POINT ( 'NONE',  ( 6.720655732516645386, 3.710664525043025019, 2.240930934554703491 ) ) ;
#95346=CARTESIAN_POINT ( 'NONE',  ( 4.968408144156593487, -2.063508908063705238, -0.7385586828293493333 ) ) ;
#95348=CARTESIAN_POINT ( 'NONE',  ( 6.368092757517858082, 1.156555634672886246, 1.944455297613384204 ) ) ;
#95354=CARTESIAN_POINT ( 'NONE',  ( 0.7250502862299773588, -1.682426168213309703, 0.5495948440489316633 ) ) ;
#95355=CARTESIAN_POINT ( 'NONE',  ( 5.461592787958983841, -1.588467041389821421, -1.236575366846304647 ) ) ;
#95357=CARTESIAN_POINT ( 'NONE',  ( 3.874133602078254413, 1.168181435743149921, 1.752046721337781054 ) ) ;
#95358=CARTESIAN_POINT ( 'NONE',  ( 2.038566206862189478, -1.479296367703235360, 1.217016582141629666 ) ) ;
#95360=CARTESIAN_POINT ( 'NONE',  ( 2.734760313433327372, -1.883857982319175450, -0.5745676990022812181 ) ) ;
#95361=CARTESIAN_POINT ( 'NONE',  ( 5.010023637874760460, -0.7231455074051349463, 1.886094130455595375 ) ) ;
#95362=CARTESIAN_POINT ( 'NONE',  ( 1.199835987674138460, -1.870836310881810682, -0.003643258294119822160 ) ) ;
#95363=CARTESIAN_POINT ( 'NONE',  ( 4.969259055160575755, 0.1640942704066571667, -1.717058449848630985 ) ) ;
#95364=CARTESIAN_POINT ( 'NONE',  ( 0.9844543725016400293, -1.211084316286781037, 1.480072698922259455 ) ) ;
#95366=CARTESIAN_POINT ( 'NONE',  ( 0.9794701899953797142, -0.05759512415488829418, -2.206297691287119722 ) ) ;
#95373=CARTESIAN_POINT ( 'NONE',  ( 6.631696427350994405, 1.982895789845315671, -0.5951614246157420629 ) ) ;
#95375=CARTESIAN_POINT ( 'NONE',  ( 1.047426762419433777, 1.826728496382063582, -0.9743617655595809834 ) ) ;
#95381=CARTESIAN_POINT ( 'NONE',  ( 5.408877457991549953, -0.5154355754800542533, -2.056752310636373426 ) ) ;
#95384=CARTESIAN_POINT ( 'NONE',  ( 6.795372052238223048, -1.752927774724974297, 0.8811163259476795240 ) ) ;
#95386=CARTESIAN_POINT ( 'NONE',  ( 3.901720107437017582, 0.2930258228103881368, 1.994564303527603499 ) ) ;
#95388=CARTESIAN_POINT ( 'NONE',  ( 4.610495038435900916, 1.835019742331613690, 0.5502660077172877306 ) ) ;
#95390=CARTESIAN_POINT ( 'NONE',  ( 2.718528139169604341, 2.064530135181973591, 0.7356957861901700646 ) ) ;
#95393=CARTESIAN_POINT ( 'NONE',  ( 4.869394097828703138, -1.702981969582622046, -1.073415598185305964 ) ) ;
#95396=CARTESIAN_POINT ( 'NONE',  ( 5.624650681053017465, 0.4137061758265787592, 2.076257688556768066 ) ) ;
#95398=CARTESIAN_POINT ( 'NONE',  ( 3.087527064991796077, -0.8449906179068911172, 1.912563079267016297 ) ) ;
#95400=CARTESIAN_POINT ( 'NONE',  ( 1.395042272690392604, 1.302445673786157831, 1.130794771346554928 ) ) ;
#95402=CARTESIAN_POINT ( 'NONE',  ( 4.746395313581045272, 1.087821826000659131, -1.820160695957805608 ) ) ;
#95411=CARTESIAN_POINT ( 'NONE',  ( 1.576514528963068429, -1.280961997807128938, 1.281107859597712118 ) ) ;
#95417=CARTESIAN_POINT ( 'NONE',  ( 2.490610001455384470, -1.733883600701890737, -0.5244944224890700779 ) ) ;
#95418=CARTESIAN_POINT ( 'NONE',  ( 6.639320575229259447, 2.969246179279591225, 2.450030562065998119 ) ) ;
#95422=CARTESIAN_POINT ( 'NONE',  ( 4.105780043149899861, 0.6285678624660723246, -1.751810336424673542 ) ) ;
#95423=CARTESIAN_POINT ( 'NONE',  ( 1.089294787249419194, -0.4641297292061612456, 1.858405954227143386 ) ) ;
#95424=CARTESIAN_POINT ( 'NONE',  ( 6.124042008734975617, -1.070608276503826950, -1.601302156493543905 ) ) ;
#95432=CARTESIAN_POINT ( 'NONE',  ( 5.928554213991230171, -1.252361881311152558, 1.519918492727867054 ) ) ;
#95437=CARTESIAN_POINT ( 'NONE',  ( 0.4629771330677232011, 0.2027323353172970355, -2.080777175944429125 ) ) ;
#95439=CARTESIAN_POINT ( 'NONE',  ( 4.963854806921006002, 1.905440169433350484, -0.2825122895667788181 ) ) ;
#95441=CARTESIAN_POINT ( 'NONE',  ( 1.237009950130557590, -1.652246606862219025, 0.7767072072360350354 ) ) ;
#95442=CARTESIAN_POINT ( 'NONE',  ( 1.805583701156989518, 1.836052299496168771, 1.224139149458243425 ) ) ;
#95444=CARTESIAN_POINT ( 'NONE',  ( 0.2110004604562870645, 1.588762659912812403, -1.064147093309028680 ) ) ;
#95447=CARTESIAN_POINT ( 'NONE',  ( 0.8011416495431540330, -1.691081937322042483, 1.009368880822520298 ) ) ;
#95448=CARTESIAN_POINT ( 'NONE',  ( 1.224054851709508451, 1.872146073007043610, 0.5162294149947727062 ) ) ;
#95449=CARTESIAN_POINT ( 'NONE',  ( 0.3509351863830567075, -0.9528684895154272416, 1.776737725368633614 ) ) ;
#95451=CARTESIAN_POINT ( 'NONE',  ( 5.770303593930925956, -0.8350939829899912681, -1.663081984830430793 ) ) ;
#95455=CARTESIAN_POINT ( 'NONE',  ( 6.509000000000010111, 6.037005099786168394, 2.594901386363585694 ) ) ;
#95458=CARTESIAN_POINT ( 'NONE',  ( 1.751786407749492014, 2.185395279939935431, -0.1653414253460702699 ) ) ;
#95462=CARTESIAN_POINT ( 'NONE',  ( 2.648829494986388422, -1.517897411861212076, 1.014145048410304284 ) ) ;
#95467=CARTESIAN_POINT ( 'NONE',  ( 6.509000000000039421, 4.695815278351551214, 2.562658139094181386 ) ) ;
#95469=CARTESIAN_POINT ( 'NONE',  ( 0.8031968939124977114, 1.574386321349549700, 1.110025428916910917 ) ) ;
#95470=CARTESIAN_POINT ( 'NONE',  ( 5.629730433169950921, 1.891637868780412068, -0.5196590155819302836 ) ) ;
#95473=CARTESIAN_POINT ( 'NONE',  ( 5.073855206572205567, -1.217758175834412260, 1.821886007100224969 ) ) ;
#95476=CARTESIAN_POINT ( 'NONE',  ( 3.907136544319700810, -1.695332804699274387, 1.187946514627869821 ) ) ;
#95480=CARTESIAN_POINT ( 'NONE',  ( 3.569189921330259807, -1.132127473341357771, 2.000487910885457854 ) ) ;
#95487=CARTESIAN_POINT ( 'NONE',  ( 3.556523421261322149, -1.712991659986836002, -0.9147756334835445147 ) ) ;
#95491=CARTESIAN_POINT ( 'NONE',  ( 5.449440537890920311, -1.726199344983204265, 0.8234401749890255529 ) ) ;
#95492=CARTESIAN_POINT ( 'NONE',  ( 6.721745554788610022, -1.671375598274482677, 0.4255071719459716517 ) ) ;
#95493=CARTESIAN_POINT ( 'NONE',  ( 4.223842396274177347, 0.8578445224393380641, -1.825075645057252727 ) ) ;
#95495=CARTESIAN_POINT ( 'NONE',  ( 1.348561525465460820, 2.204488851003219896, 0.1053889787279923829 ) ) ;
#95498=CARTESIAN_POINT ( 'NONE',  ( 1.517645033149318978, -1.162591604200275963, -1.737351732476496657 ) ) ;
#95499=CARTESIAN_POINT ( 'NONE',  ( 6.784453145350711090, -1.736176628054094007, -0.3419908188336401311 ) ) ;
#95500=CARTESIAN_POINT ( 'NONE',  ( 5.572888750952301073, -0.9041123360693378297, 1.802415994888312722 ) ) ;
#95502=CARTESIAN_POINT ( 'NONE',  ( 2.590095216689162427, -2.286210222917249180, -0.1672752534159216153 ) ) ;
#95503=CARTESIAN_POINT ( 'NONE',  ( 0.9369944060461411484, 0.7087284392868421490, -1.589666227069729265 ) ) ;
#95505=CARTESIAN_POINT ( 'NONE',  ( 1.422726403049366706, 0.6964842469411072212, 1.588000322196560399 ) ) ;
#95508=CARTESIAN_POINT ( 'NONE',  ( 1.645237833728605548, -0.3177867502775574837, -2.147667186158049191 ) ) ;
#95509=CARTESIAN_POINT ( 'NONE',  ( 2.887907956677421506, -2.014008092954455265, 0.1037802451031161477 ) ) ;
#95510=CARTESIAN_POINT ( 'NONE',  ( 4.781250000000003553, 0.7852924748302358982, 1.895863743163977100 ) ) ;
#95512=CARTESIAN_POINT ( 'NONE',  ( 6.199827818874126706, -0.6464308959919072839, 1.814938386029739892 ) ) ;
#95514=CARTESIAN_POINT ( 'NONE',  ( 3.059039825962418746, 0.5433887813283566626, 2.153793114424791710 ) ) ;
#95520=CARTESIAN_POINT ( 'NONE',  ( 5.864775363713938816, 0.1190308195875185160, -1.736441914165016476 ) ) ;
#95521=CARTESIAN_POINT ( 'NONE',  ( 4.035565188342554954, 1.848088059160474694, -0.6588067414724924076 ) ) ;
#95525=CARTESIAN_POINT ( 'NONE',  ( 4.218261219551087571, -1.158436920226207034, -1.943184041606202950 ) ) ;
#95526=CARTESIAN_POINT ( 'NONE',  ( 1.768110600389400933, -2.047337470793224146, 0.2504565381693297788 ) ) ;
#95529=CARTESIAN_POINT ( 'NONE',  ( 2.202381998968961696, -2.261980054776930427, 0.05578962468580014183 ) ) ;
#95532=CARTESIAN_POINT ( 'NONE',  ( 3.286256049847174676, -1.842268013383094427, -0.3231441395407097517 ) ) ;
#95533=CARTESIAN_POINT ( 'NONE',  ( 2.549097654585132045, -1.194521797001405927, 1.257391726941985421 ) ) ;
#95534=CARTESIAN_POINT ( 'NONE',  ( -0.05846771364293941453, -1.777572824190313261, -1.447063799157372044 ) ) ;
#95535=CARTESIAN_POINT ( 'NONE',  ( 6.493248230727125758, 2.012220109224418518, -1.129477038640940734 ) ) ;
#95536=CARTESIAN_POINT ( 'NONE',  ( 4.170900312159072421, -2.016029151617684256, -0.7805680927704603533 ) ) ;
#95537=CARTESIAN_POINT ( 'NONE',  ( 4.769442245286214188, 1.119358777157190010, 1.586704836592154333 ) ) ;
#95539=CARTESIAN_POINT ( 'NONE',  ( 6.380143124955812262, -1.000617425381218561, 1.580232162242324545 ) ) ;
#95543=CARTESIAN_POINT ( 'NONE',  ( 5.256482491209823138, 1.942542154241846397, -0.5404887192124520068 ) ) ;
#95546=CARTESIAN_POINT ( 'NONE',  ( 2.719161800852238464, -0.1789327596440904167, 1.816892639718168390 ) ) ;
#95547=CARTESIAN_POINT ( 'NONE',  ( 1.940722911589174204, 2.182806717142399489, 0.3235914145361811767 ) ) ;
#95553=CARTESIAN_POINT ( 'NONE',  ( 1.547134890100225535, 0.2020692043026971751, 2.009678023649637879 ) ) ;
#95554=CARTESIAN_POINT ( 'NONE',  ( 1.278162280329109279, 2.088516533416693743, -0.3659721813360562459 ) ) ;
#95557=CARTESIAN_POINT ( 'NONE',  ( 1.639267886685547460, 1.721996695667164845, -0.7061035538288776836 ) ) ;
#95559=CARTESIAN_POINT ( 'NONE',  ( 6.819229409281153842, -0.1590044787766713985, 2.026160355490718601 ) ) ;
#95560=CARTESIAN_POINT ( 'NONE',  ( 6.399064592084179992, -0.9530083391863402031, -1.777013033299412292 ) ) ;
#95562=ORIENTED_EDGE ( 'NONE', *, *, #4605, .T. ) ;
#95564=CARTESIAN_POINT ( 'NONE',  ( 4.090329635444483358, -1.806102819543849769, -0.2658631594732660530 ) ) ;
#95569=CARTESIAN_POINT ( 'NONE',  ( 6.503279807981923177, 1.993766592317405051, 0.2985777636397292101 ) ) ;
#95570=CARTESIAN_POINT ( 'NONE',  ( 5.859284738525260217, 1.813109059707292747, -0.3191327317438249489 ) ) ;
#95571=CARTESIAN_POINT ( 'NONE',  ( 0.07680821025396293578, 0.7488618828427398011, -1.895266105024134839 ) ) ;
#95572=CARTESIAN_POINT ( 'NONE',  ( 3.950101280099535650, 0.7789643570827823327, -2.172381230931414109 ) ) ;
#95574=CARTESIAN_POINT ( 'NONE',  ( 5.940740243836844847, 0.4152237956781511530, 2.121177236311201586 ) ) ;
#95576=CARTESIAN_POINT ( 'NONE',  ( 1.224054851709508451, 1.872146073007043610, 0.5162294149947727062 ) ) ;
#95579=CARTESIAN_POINT ( 'NONE',  ( 4.200743080572525656, -1.581147070632774598, -1.668312408496865684 ) ) ;
#95582=CARTESIAN_POINT ( 'NONE',  ( 5.014452206985246185, 1.289541220462528504, -1.355370375751355105 ) ) ;
#95583=VERTEX_POINT ( 'NONE', #125489 ) ;
#95584=CARTESIAN_POINT ( 'NONE',  ( 2.267699027020404490, 0.5063876334258295975, -1.844086191983687062 ) ) ;
#95587=CARTESIAN_POINT ( 'NONE',  ( 3.580891165198408110, -2.126768340858419926, -0.5889919780145411732 ) ) ;
#95588=CARTESIAN_POINT ( 'NONE',  ( 6.883263157960401557, 2.461427291499204362, 2.229941283862615808 ) ) ;
#95594=CARTESIAN_POINT ( 'NONE',  ( 2.020718154849282744, 1.838011538856450855, 0.7131330410372925810 ) ) ;
#95595=CARTESIAN_POINT ( 'NONE',  ( 0.9214421848816763960, 2.133375822355741303, 0.8800392910873405805 ) ) ;
#95596=CARTESIAN_POINT ( 'NONE',  ( 2.189831975649577878, -1.279155337443920404, -1.487614327915102841 ) ) ;
#95598=CARTESIAN_POINT ( 'NONE',  ( 4.768458259026512103, -0.8772815012083650110, -1.866809563962401164 ) ) ;
#95605=CARTESIAN_POINT ( 'NONE',  ( 0.5323791783840629011, 1.248846938226945369, 1.775765033185220387 ) ) ;
#95609=CARTESIAN_POINT ( 'NONE',  ( 2.249088872875557144, -1.499603784168266563, -1.117866018216478574 ) ) ;
#95610=CARTESIAN_POINT ( 'NONE',  ( 6.919229410208834530, -0.1638780278429008419, 2.126154539342207883 ) ) ;
#95611=CARTESIAN_POINT ( 'NONE',  ( 0.07775346131141076811, 6.946779003630084048, -2.883989925229225815 ) ) ;
#95612=CARTESIAN_POINT ( 'NONE',  ( 6.827182134110227452, 2.468179810210658687, 2.195371296381436022 ) ) ;
#95614=CARTESIAN_POINT ( 'NONE',  ( 2.385291144485178982, 0.09204604084523881902, -1.910175020619097275 ) ) ;
#95615=CARTESIAN_POINT ( 'NONE',  ( 3.924454612484959082, 1.680539001619888229, 0.5552615287828834845 ) ) ;
#95616=CARTESIAN_POINT ( 'NONE',  ( 1.893074787327468700, -0.09523556418119562272, -1.910042277862213034 ) ) ;
#95619=CARTESIAN_POINT ( 'NONE',  ( 5.976186790766067958, -1.906884764771042517, -0.1824196792480689000 ) ) ;
#95620=CARTESIAN_POINT ( 'NONE',  ( 6.320757381585181633, -1.393903556229304730, 1.391728847557841542 ) ) ;
#95622=CARTESIAN_POINT ( 'NONE',  ( 2.566775492539817627, 0.7186216927172992541, 1.995234744298620910 ) ) ;
#95624=CARTESIAN_POINT ( 'NONE',  ( 5.242975984329111050, -1.603930480038592510, 0.9624218375651683033 ) ) ;
#95625=CARTESIAN_POINT ( 'NONE',  ( 1.699542765152612711, -0.6164703606487754728, 1.718597393154073671 ) ) ;
#95627=CARTESIAN_POINT ( 'NONE',  ( 5.110101661328442901, -2.196521081226535443, 0.2136625748923453583 ) ) ;
#95630=CARTESIAN_POINT ( 'NONE',  ( 2.330602656244503468, -1.270745551583628785, 1.624662076113972065 ) ) ;
#95638=CARTESIAN_POINT ( 'NONE',  ( 5.863751307568212390, -0.5067217619753560109, 2.007263066363853987 ) ) ;
#95640=CARTESIAN_POINT ( 'NONE',  ( 2.249508738127777630, -1.734628566516350556, -1.289557925820798090 ) ) ;
#95642=CARTESIAN_POINT ( 'NONE',  ( 3.651039828637154372, 0.2984016815541118417, 1.997388552288078545 ) ) ;
#95643=CARTESIAN_POINT ( 'NONE',  ( 6.720655732516665815, 7.629137130509056064, 2.773739711112707340 ) ) ;
#95649=CARTESIAN_POINT ( 'NONE',  ( 1.903530124611974017, -1.954778955200174861, 0.4946342604733033887 ) ) ;
#95650=CARTESIAN_POINT ( 'NONE',  ( 5.776942576169182608, 2.025397260235710206, -0.8375503648087383457 ) ) ;
#95653=CARTESIAN_POINT ( 'NONE',  ( 4.412309042748480792, -1.912102599942141268, -0.04143165621695726192 ) ) ;
#95657=CARTESIAN_POINT ( 'NONE',  ( 2.232046197884657968, 2.016035414700023676, 0.04665772616015140262 ) ) ;
#95660=CARTESIAN_POINT ( 'NONE',  ( 5.561458258421018819, 0.3325557151471290052, -1.692213012293216190 ) ) ;
#95665=CARTESIAN_POINT ( 'NONE',  ( 1.252880909328603964, -0.4992908342843912495, -2.009044966204868388 ) ) ;
#95667=CARTESIAN_POINT ( 'NONE',  ( 4.652869415276386533, 0.3145016728411016982, 1.783790502623605834 ) ) ;
#95669=CARTESIAN_POINT ( 'NONE',  ( 6.410821795378537580, -0.4906875946298261959, -1.743675775721682752 ) ) ;
#95672=CARTESIAN_POINT ( 'NONE',  ( 3.363397379774799134, 2.138023915923603635, -0.4802275100637617977 ) ) ;
#95674=CARTESIAN_POINT ( 'NONE',  ( 0.3440982351944205653, -0.9282241650855774795, 1.728402704573737125 ) ) ;
#95676=CARTESIAN_POINT ( 'NONE',  ( 5.079654255714375566, -0.6853159911496645718, 1.789018848640187231 ) ) ;
#95683=CARTESIAN_POINT ( 'NONE',  ( 2.167066695894452888, -1.976221826324360720, -0.8764929760368762590 ) ) ;
#95686=CARTESIAN_POINT ( 'NONE',  ( 2.239018641000252607, -1.631965468365924377, 0.8183158014263000046 ) ) ;
#95688=CARTESIAN_POINT ( 'NONE',  ( 4.243042751400435186, -1.588269943899191183, 0.8999137264355041577 ) ) ;
#95690=ORIENTED_EDGE ( 'NONE', *, *, #60102, .T. ) ;
#95691=CARTESIAN_POINT ( 'NONE',  ( 4.228926779721821738, -1.836881627057206590, -0.7110872907168819257 ) ) ;
#95693=CARTESIAN_POINT ( 'NONE',  ( 5.565949569975685129, -1.228723311412585950, 1.503964349303931192 ) ) ;
#95697=CARTESIAN_POINT ( 'NONE',  ( 5.484674493353773883, -1.343714522216314489, 1.640574901390474460 ) ) ;
#95700=CARTESIAN_POINT ( 'NONE',  ( 3.229067839489424330, 1.729836904712976686, 0.8154208365811002057 ) ) ;
#95702=CARTESIAN_POINT ( 'NONE',  ( 6.983263157960370116, 6.036630394911544073, 2.541087343977180613 ) ) ;
#95705=CARTESIAN_POINT ( 'NONE',  ( 5.004545975878083475, -1.998138528169653316, -0.2443019910301855169 ) ) ;
#95707=CARTESIAN_POINT ( 'NONE',  ( 5.918537399722813674, 1.222626809077583587, -1.356019982345892050 ) ) ;
#95708=CARTESIAN_POINT ( 'NONE',  ( 0.9946828900261883710, 2.039433816042154124, 0.3556643922909968891 ) ) ;
#95721=CARTESIAN_POINT ( 'NONE',  ( 3.656634503061773067, 0.9670403524725273980, 1.439223064172075350 ) ) ;
#95723=CARTESIAN_POINT ( 'NONE',  ( 1.164989683304976875, 1.570165760251106990, -1.349419213858449318 ) ) ;
#95725=CARTESIAN_POINT ( 'NONE',  ( 1.915762678288157383, -1.385565726045881130, -1.600959455242874974 ) ) ;
#95729=CARTESIAN_POINT ( 'NONE',  ( 1.164831386079593134, 1.494809975433964100, -1.282432929305108438 ) ) ;
#95734=CARTESIAN_POINT ( 'NONE',  ( 2.906493132324819761, 1.659771084382713369, -1.581246672503307638 ) ) ;
#95735=CARTESIAN_POINT ( 'NONE',  ( 0.4514209555319322331, 0.5758240286459561652, -1.732582669633643047 ) ) ;
#95736=CARTESIAN_POINT ( 'NONE',  ( 3.129067941553372645, 1.730785544086024696, 0.8136490247460312908 ) ) ;
#95740=CARTESIAN_POINT ( 'NONE',  ( 1.758066197707741640, 0.7666020408202559588, -1.861725765494412599 ) ) ;
#95741=CARTESIAN_POINT ( 'NONE',  ( 1.604273143990111672, 1.959273547513197711, 0.1016356785708133759 ) ) ;
#95745=CARTESIAN_POINT ( 'NONE',  ( 5.033190428309433528, -1.478027449723118725, -1.478843810762977995 ) ) ;
#95746=CARTESIAN_POINT ( 'NONE',  ( 3.836565602288672938, 0.2594712388852594143, 1.750573784680304890 ) ) ;
#95748=CARTESIAN_POINT ( 'NONE',  ( 0.1292129718690297469, -2.001788180159810970, 0.8922102942980969509 ) ) ;
#95749=CARTESIAN_POINT ( 'NONE',  ( 4.980260712887213614, -0.2176769249225460612, -1.726585916463187376 ) ) ;
#95752=CARTESIAN_POINT ( 'NONE',  ( 4.885968428070557756, -0.08385511083567295798, 1.731956597358391470 ) ) ;
#95753=CARTESIAN_POINT ( 'NONE',  ( 4.949771893170417769, 1.605651206033286815, 1.461634471724428064 ) ) ;
#95755=CARTESIAN_POINT ( 'NONE',  ( 6.034388706570055660, 0.6371486477873434806, 1.913263546360920220 ) ) ;
#95756=CARTESIAN_POINT ( 'NONE',  ( 5.562500000000004441, -1.451031289061337937, -1.451031289060889851 ) ) ;
#95758=CARTESIAN_POINT ( 'NONE',  ( 3.487250860276095210, 1.742034520097140771, -0.8226350277544016709 ) ) ;
#95760=CARTESIAN_POINT ( 'NONE',  ( 0.4873737393681918384, -2.093643541511390538, -0.7425801828774351021 ) ) ;
#95761=EDGE_LOOP ( 'NONE', ( #26386, #163150, #31522, #153611 ) ) ;
#95762=CARTESIAN_POINT ( 'NONE',  ( 6.983263157960401202, 2.460233018525457727, 2.229759568558951965 ) ) ;
#95765=CARTESIAN_POINT ( 'NONE',  ( 2.754761814426693434, 2.204812966250285999, 0.2695357242936818332 ) ) ;
#95766=CARTESIAN_POINT ( 'NONE',  ( 6.478960399985357554, 1.830089090633261417, 0.7073212282268787066 ) ) ;
#95772=CARTESIAN_POINT ( 'NONE',  ( 5.723111435942265679, -1.863175293877845418, -0.8853075346121098699 ) ) ;
#95776=CARTESIAN_POINT ( 'NONE',  ( 6.696569769017397533, -0.4992639023812006638, -1.802638941973549569 ) ) ;
#95777=B_SPLINE_CURVE_WITH_KNOTS ( 'NONE', 3,
 ( #13936, #80019, #146122, #63771, #130980, #129930, #214242, #195918, #47555, #179670, #31290, #97365, #163423, #14999, #196971, #48608, #180723, #156513, #37405, #90445, #56863, #187913, #103479, #7015, #88304, #123037, #24337, #39543, #181772, #87227, #188988, #875, #120875, #99484, #40632, #4867, #55790, #155429, #105644, #169541, #21121, #38481, #73090, #153291, #119791, #66940, #89380, #17135, #165542, #115783, #172762, #171671, #186849, #140284, #70945, #185772, #137056, #203081, #54726, #33405, #104558, #8102, #83211, #74192, #22189, #53659, #139191, #49660, #170602, #135986, #202000, #154366, #106735, #5944, #72015, #138128, #149294, #23268, #204137, #121947, #205221, #193263, #28640, #13440, #26489, #141365, #45974, #175968, #44910, #111018, #174911, #57928, #191113, #192180, #173843, #25420, #43841, #92599, #27562, #161852, #124093, #160772, #208429, #94727, #76313, #112095, #177023, #190056, #79517, #42780, #158641, #109957, #91526, #10238, #126219, #93658, #78444, #207378, #142420, #143495, #12365, #77379, #209491, #41708, #206304, #60063, #61132, #107818, #157584, #9177, #125154, #178097, #144564, #159701, #210574, #11300, #29714, #62208, #75252, #58998, #108888, #127292, #128365, #194332, #95795, #147728, #167170, #162913, #145635, #49162, #100032, #149861, #98975, #115279, #211631, #213745, #15556, #146683, #80585, #182327, #47041, #212699, #32897, #96865, #179162, #17682, #50218, #30786, #33956, #101081, #197518, #199639, #196472, #166094, #133638, #165027, #18757, #16621, #81643, #65368, #117410, #183406, #66425, #63266, #180224, #1429, #14495, #131515, #195412, #51285, #97923, #148782, #83768, #132568, #48114, #114226, #64340, #31846, #129428, #130482, #163981, #67493, #113157, #181271, #82703, #35010, #198569, #352, #116337, #69634, #168231, #151987, #135742, #3561, #2492, #201764, #118477, #136807, #105390, #169293, #84842, #137882, #171429, #53405, #184462, #102163, #119543, #55548, #202833, #86977, #103233, #68567, #104304, #36080, #38230, #19828, #154119, #121702, #85913, #185528, #37154, #39296, #4622, #170353, #21938, #20878, #150931, #153047, #70694, #134694, #54482, #89134, #120627, #203902, #23017, #88048, #200698, #5689, #186603, #71766, #52350, #187666, #155188, #196107, #98602, #68193, #15191, #132199, #113859, #51981, #16245, #67125, #166795, #50909, #114906, #180903, #81282, #32527, #47743, #131161, #197152, #100718, #31477, #179854, #130117, #184091, #199265, #198206, #151619, #164663, #48789, #82331, #148423, #73002, #97552, #66055, #147358, #17315, #35710, #49841, #63962, #150558, #101787, #115969, #213385, #65009, #181957, #134325, #165727, #33586, #99658, #163610, #117037, #83393, #133258, #149477, #18389, #200331, #1060, #183032, #34648, #84466, #2118, #118106, #167856, #19453, #85529, #3178, #54101, #184084, #202445, #35702, #185138, #171037, #67117, #167846, #34641, #133250, #55167, #21554, #4243, #199256, #22634, #51974, #19446, #119155, #183025, #85523, #135366, #102851, #38913, #18381, #1052, #36765, #169968, #5302, #168906, #20510, #50902, #69249, #151609, #86595, #100712, #166787, #121312, #2111, #152661, #84459, #150549, #87664, #120237, #68185, #103924, #101778, #104997, #117028, #187286, #70314, #134316, #153734, #88744, #136430, #186213, #201382, #37845, #200324, #53022 ),
 .UNSPECIFIED., .F., .F.,
 ( 4, 1, 1, 1, 1, 1, 1, 1, 1, 1, 1, 1, 1, 1, 1, 1, 1, 1, 1, 1, 1, 1, 1, 1, 1, 1, 1, 1, 1, 1, 1, 1, 1, 1, 1, 1, 1, 1, 1, 1, 1, 1, 1, 1, 1, 1, 1, 1, 1, 1, 1, 1, 1, 1, 1, 1, 1, 1, 1, 1, 1, 1, 1, 1, 1, 1, 1, 1, 1, 1, 1, 1, 1, 1, 1, 1, 1, 1, 1, 1, 1, 1, 1, 1, 1, 1, 1, 1, 1, 1, 1, 1, 1, 1, 1, 1, 1, 1, 1, 1, 1, 1, 1, 1, 1, 1, 1, 1, 1, 1, 1, 1, 1, 1, 1, 1, 1, 1, 1, 1, 1, 1, 1, 1, 1, 1, 1, 1, 1, 1, 1, 1, 1, 1, 1, 1, 1, 1, 1, 1, 1, 1, 1, 1, 1, 1, 1, 1, 1, 1, 1, 1, 1, 1, 1, 1, 1, 1, 1, 1, 1, 1, 1, 1, 1, 1, 1, 1, 1, 1, 1, 1, 1, 1, 1, 1, 1, 1, 1, 1, 1, 1, 1, 1, 1, 1, 1, 1, 1, 1, 1, 1, 1, 1, 1, 1, 1, 1, 1, 1, 1, 1, 1, 1, 1, 1, 1, 1, 1, 1, 1, 1, 1, 1, 1, 1, 1, 1, 1, 1, 1, 1, 1, 1, 1, 1, 1, 1, 1, 1, 1, 1, 1, 1, 1, 1, 1, 1, 1, 1, 1, 1, 1, 1, 1, 1, 1, 1, 1, 1, 1, 1, 1, 1, 1, 1, 1, 1, 1, 1, 1, 1, 1, 1, 1, 1, 1, 1, 1, 1, 1, 1, 1, 1, 1, 1, 1, 1, 1, 1, 1, 1, 1, 1, 1, 1, 1, 1, 1, 1, 1, 1, 1, 1, 1, 1, 1, 1, 1, 1, 1, 1, 1, 1, 1, 1, 1, 1, 1, 1, 1, 1, 1, 1, 1, 1, 1, 1, 1, 1, 1, 1, 1, 1, 1, 1, 1, 1, 1, 1, 1, 1, 1, 1, 1, 1, 1, 1, 1, 1, 1, 1, 1, 1, 1, 1, 1, 1, 1, 1, 1, 1, 1, 1, 1, 1, 1, 1, 1, 1, 1, 1, 1, 1, 1, 1, 1, 1, 1, 1, 1, 1, 1, 1, 1, 1, 1, 1, 1, 1, 1, 1, 1, 1, 4 ),
 ( 0.000000000000000000, 0.002599942752653872004, 0.005208763852970823248, 0.007813103504395044890, 0.01041666580238601383, 0.01302040446826325734, 0.01562503794709516405, 0.01822898659850798186, 0.02083325479626091381, 0.02343751936515397344, 0.02604147156932860516, 0.02864593660736421826, 0.03124971754428982826, 0.03385421962853985695, 0.03645805019290717514, 0.03906245553539786086, 0.04166655880408994678, 0.04427067902208449424, 0.04687506736766395427, 0.04947890482860387018, 0.05208340383233839299, 0.05468718329397467132, 0.05729165635893663372, 0.05989559287350183087, 0.06249988401580178210, 0.06510415622071820396, 0.06770810475871495704, 0.07031256650665723695, 0.07291634835701975292, 0.07552085129243907291, 0.07812468146351797538, 0.08072908640827750060, 0.08333318980393969455, 0.08593730989448074287, 0.08854169822802662737, 0.09114553558425014801, 0.09375003453682481669, 0.09635381396055957282, 0.09895828689139142542, 0.1015622234206122604, 0.1041665143989399522, 0.1067707866525781646, 0.1093747350801187734, 0.1119791968332524285, 0.1145829786367304204, 0.1171874814968899975, 0.1197913116783300008, 0.1223957164865987768, 0.1249998199429257079, 0.1276039399106482508, 0.1302083283009266290, 0.1328121656006459317, 0.1354166645410730119, 0.1380204439687620910, 0.1406249168095159707, 0.1432288533966223909, 0.1458331442541831724, 0.1484374165996726891, 0.1510413649597071029, 0.1536458267615184170, 0.1562496085608837959, 0.1588541113892728840, 0.1614579416238982879, 0.1640623463390579739, 0.1666664498991252963, 0.1692705697871219883, 0.1718749582774928841, 0.1744787955635339893, 0.1770832945353020271, 0.1796870740097127606, 0.1822915468038420750, 0.1848954834917516388, 0.1874997742717963711, 0.1901040467523684718, 0.1927079950878241021, 0.1953124569817516476, 0.1979162388197689970, 0.2005207416598733527, 0.2031245719904950509, 0.2057289766559125821, 0.2083330803627857220, 0.2109372002141371993, 0.2135415888479497148, 0.2161454261631269858, 0.2187499252097131475, 0.2213537047736018060, 0.2239581775645482220, 0.2265621143961681627, 0.2291664051419355919, 0.2317706778008114532, 0.2343746261546043874, 0.2369790881840763974, 0.2395828701034999064, 0.2421873729987945312, 0.2447912034682135918, 0.2473956081272447038, 0.2499997120239797754, 0.2526038318817556694, 0.2552082207023498306, 0.2578120580894675551, 0.2604165572543392093, 0.2630203369504529598, 0.2656248097816475973, 0.2682287467998764607, 0.2708330375545950908, 0.2734373104349877015, 0.2760412588500244513, 0.2786457210584605826, 0.2812495031020356140, 0.2838540060959860445, 0.2864578367469951536, 0.2890622414429859233, 0.2916663455726313803, 0.2942704654798921071, 0.2968748545306000852, 0.2994786920324540302, 0.3020831913590704687, 0.3046869712301484290, 0.3072914441450140810, 0.3098953813927431966, 0.3124996721996327054, 0.3151039453447485039, 0.3177078938639273376, 0.3203123562947402525, 0.3229161385052047861, 0.3255206416412691484, 0.3281244725166545528, 0.3307288772929431464, 0.3333329816985414751, 0.3359371016983396796, 0.3385414910224879836, 0.3411453286818670882, 0.3437498282136811634, 0.3463536083024566503, 0.3489580813444087548, 0.3515620188645239841, 0.3541663097667969717, 0.3567705832198370119, 0.3593745318860498972, 0.3619789945826469846, 0.3645827770027332826, 0.3671872803243637073, 0.3697911114669067967, 0.3723955163668249413, 0.3749996210914142147, 0.3776037412267966853, 0.3802081308677072724, 0.3828119687273952576, 0.3854164685078552144, 0.3880202488570567709, 0.3906247220695055478, 0.3932286599048890885, 0.3958329509457525486, 0.3984372247499146091, 0.4010411736060487398, 0.4036456366118335581, 0.4062494192842699414, 0.4088539228349143406, 0.4114577542873927851, 0.4140621593542673784, 0.4166662644408827831, 0.4192703847548917562, 0.4218747747558840855, 0.4244786128586610641, 0.4270831129312115948, 0.4296868935835649328, 0.4322913670099168826, 0.4348953052034483235, 0.4374995964261053638, 0.4401038706245853915, 0.4427078197135246862, 0.4453122830718987402, 0.4479160660394111426, 0.4505205698625146526, 0.4531244016677045128, 0.4557288069448597878, 0.4583329124365353446, 0.4609370329722101700, 0.4635414233766025904, 0.4661452617652466213, 0.4687497621733308639, 0.4713535431715604185, 0.4739580168552197104, 0.4765619554497781962, 0.4791662468974299260, 0.4817705215334236457, 0.4843744708980504132, 0.4869789346524148743, 0.4895827179577280641, 0.4921872220967347111, 0.4947910542974118808, 0.4973954598281701278, 0.4999995657679404681, 0.5026036865683194410, 0.5052080774194306345, 0.5078119161367193879, 0.5104164169237808135, 0.5130201983106112973, 0.5156246722949818784, 0.5182286113334474420, 0.5208329030492938605, 0.5234371781659985512, 0.5260411278491948783, 0.5286455920429519173, 0.5312493757287917173, 0.5338538802271461936, 0.5364577128660878991, 0.5390621186937718523, 0.5416662251246735504, 0.5442703462327953545, 0.5468747375739465566, 0.5494785766626585355, 0.5520830778721422805, 0.5546868596903002935, 0.5572913340187868325, 0.5598952735440421158, 0.5624995655712847764, 0.5651038412119004928, 0.5677077912565504647, 0.5703122559331050834, 0.5729160400421993149, 0.5755205449433484777, 0.5781243780633351648, 0.5807287842312690573, 0.5833328911963423513, 0.5859370126552478908, 0.5885414045297637786, 0.5911452440326808722, 0.5937497457080352925, 0.5963535280002507655, 0.5989580027162609843, 0.6015619427711926814, 0.6041662351530351360, 0.6067705113607667622, 0.6093744618097575172, 0.6119789270125192138, 0.6145827115875999169, 0.6171872169349945647, 0.6197910505788110092, 0.6223954571303226269, 0.6249995646726131948, 0.6276036865253464825, 0.6302080789765573954, 0.6328119189364656005, 0.6354164211211439373, 0.6380202039301521300, 0.6406246790770983024, 0.6432286197045988807, 0.6458329124842493441, 0.6484371893023079814, 0.6510411401985315427, 0.6536456059709156996, 0.6562493910547204656, 0.6588538968918166150, 0.6614577311022542538, 0.6640621380806766005, 0.6666662462432366709, 0.6692703685328477148, 0.6718747616040910975, 0.6744786020637821844, 0.6770831048012443398, 0.6796868881697873954, 0.6822913637910873463, 0.6848953050340567117, 0.6874995982547292828, 0.6901038757263339152, 0.6927078271126885234, 0.6953122934981186276, 0.6979160791333920422, 0.7005205855036529261, 0.7031244203235108570, 0.7057288277721832648, 0.7083329365980738368, 0.7109370593676189731, 0.7135414531022405971, 0.7161452941045143294, 0.7187497974382286436, 0.7213535814090563658, 0.7239580575481356917, 0.7265619994494829648, 0.7291662931543987369, 0.7317705713227778963, 0.7343745232421703406, 0.7369789902840787610, 0.7395827765135741805, 0.7421872834604720248, 0.7447911189325585601, 0.7473955268948287989, 0.7499996364271210858, 0.7526037597196653106, 0.7552081541610216053, 0.7578119957486867397, 0.7604164997221309896, 0.7630202843380037292, 0.7656247610382975743, 0.7682287036409420899, 0.7708329978733315935, 0.7734372767817252470, 0.7760412292770711984, 0.7786456970189011839, 0.7812494838853828449, 0.7838539914523996455, 0.7864578276195345330, 0.7890622361387605865, 0.7916663464205372369, 0.7942704702791556493, 0.7968748654706151457, 0.7994787076864910969, 0.8020832123431549388, 0.8046869976468442598, 0.8072914749517984268, 0.8098954182986718431, 0.8124997131017763774, 0.8151039927934364826, 0.8177079459076636025, 0.8203124143928716139, 0.8229162019391148553, 0.8255207101697450423, 0.8281245470747605752, 0.8307289561943111966, 0.8333330672686687368, 0.8359371917364484261, 0.8385415877213925340, 0.8411454306083117061, 0.8437499359916976749, 0.8463537220259882421, 0.8489581999790609679, 0.8515621441131088210, 0.8541664395301816759, 0.8567707200483754004, 0.8593746738244238959, 0.8619791430964799384, 0.8645829313652741988, 0.8671874403030259693, 0.8697912779887684298, 0.8723956877520262498, 0.8749997996620757501, 0.8776039247821166844, 0.8802083216039426894, 0.8828121652047509205, 0.8854166713583762061, 0.8880204581660676721, 0.8906249368107317377, 0.8932288817749149956, 0.8958331778492237829, 0.8984374592372342816, 0.9010414137180589034, 0.9036458838204490807, 0.9062496728545991198, 0.9088541825429954368, 0.9114580210523274273, 0.9140624315026897317, 0.9166665442915585826, 0.9192706701069754960, 0.9218750678090992245, 0.9244789121666602272, 0.9270834191340497910, 0.9296872067579531329, 0.9322916861377325004, 0.9348956319750387767, 0.9374999287497546296, 0.9401042110508202043, 0.9427081662796877870, 0.9453126372565492375, 0.9479164270979697493, 0.9505209375757615042, 0.9531247769568838013, 0.9557291881641908349, 0.9583333018366511080, 0.9609374282806871781, 0.9635418271385329803, 0.9661456726567504427, 0.9687501794391485399, 0.9713539669241311181, 0.9739584505366999378, 0.9765624007674321705, 0.9791666904763859369, 0.9817709514985233366, 0.9843749191276834898, 0.9869795472165283634, 0.9895832986789295793, 0.9921868791097946394, 0.9947912178632822844, 0.9974000636350187632, 1.000000000000000000 ),
 .UNSPECIFIED. ) ;
#95778=CARTESIAN_POINT ( 'NONE',  ( 6.399014502872731214, -0.8263350558326795214, -1.524632933908439902 ) ) ;
#95779=CARTESIAN_POINT ( 'NONE',  ( 5.460439331044164568, -1.576930981450849867, -0.7368137880037448628 ) ) ;
#95780=CARTESIAN_POINT ( 'NONE',  ( 3.263489799031735750, 2.236134436263835568, -0.5039766086074470852 ) ) ;
#95782=CARTESIAN_POINT ( 'NONE',  ( 0.7789528443887736575, 1.234723402293058214, 1.365900241759879119 ) ) ;
#95785=CARTESIAN_POINT ( 'NONE',  ( 2.414841169274529520, 1.629557050654990791, 0.8231356554938076275 ) ) ;
#95786=CARTESIAN_POINT ( 'NONE',  ( 2.654922836763852878, 1.081066371885472277, 1.701947380796410059 ) ) ;
#95787=CARTESIAN_POINT ( 'NONE',  ( 0.6916816545035618935, -0.7852976098030055585, 2.046091368998310678 ) ) ;
#95789=CARTESIAN_POINT ( 'NONE',  ( 4.665121749186112332, -1.880042215448823661, -0.9491155671061396459 ) ) ;
#95792=CARTESIAN_POINT ( 'NONE',  ( 1.522023487246677798, 2.040062638832959241, -0.3519594530456415793 ) ) ;
#95795=CARTESIAN_POINT ( 'NONE',  ( 4.125719030757846184, -0.3612518283466863434, 2.089324717668067599 ) ) ;
#95797=CARTESIAN_POINT ( 'NONE',  ( 6.182242880246401562, -0.9723386526096773341, 1.545037271442825100 ) ) ;
#95804=CARTESIAN_POINT ( 'NONE',  ( 6.328397690248316110, -1.000878058022572903, -1.869571840794107986 ) ) ;
#95805=CARTESIAN_POINT ( 'NONE',  ( 0.8507726699197988296, 0.6114878368043925594, 2.015236747771311343 ) ) ;
#95808=CARTESIAN_POINT ( 'NONE',  ( 4.908966729185230804, -1.496192014157717631, 1.106395937811145203 ) ) ;
#95814=CARTESIAN_POINT ( 'NONE',  ( 2.312880826517309085, -1.518475810973318074, 1.242258525517292433 ) ) ;
#95815=CARTESIAN_POINT ( 'NONE',  ( 0.9542513359644848592, 2.159166806557303531, -0.1069676271590186134 ) ) ;
#95819=CARTESIAN_POINT ( 'NONE',  ( 3.338897068646465627, -1.034916488738941709, 1.390885369450091336 ) ) ;
#95820=CARTESIAN_POINT ( 'NONE',  ( 2.554330413957212276, -1.514043700042773111, -0.8579764065595529843 ) ) ;
#95823=CARTESIAN_POINT ( 'NONE',  ( 2.829428133295128323, -1.924058217741884125, 0.7386292696346643538 ) ) ;
#95826=CARTESIAN_POINT ( 'NONE',  ( 1.475935241056694602, 1.776738309990203213, 0.9528675108748105860 ) ) ;
#95827=CARTESIAN_POINT ( 'NONE',  ( 6.825078400183548055, -0.008500281443135982926, 2.244262395727573356 ) ) ;
#95829=CARTESIAN_POINT ( 'NONE',  ( 1.586731204520151151, -0.2873679327500404668, -1.950290023627434755 ) ) ;
#95831=CARTESIAN_POINT ( 'NONE',  ( 5.765855477156511810, 0.5488314196105298359, -1.831976909803390896 ) ) ;
#95837=CARTESIAN_POINT ( 'NONE',  ( 0.8209702097039422997, 1.527776094787479444, -1.321057435245088341 ) ) ;
#95839=CARTESIAN_POINT ( 'NONE',  ( 4.770747201329826659, -1.511217855519477293, 1.743977600800976857 ) ) ;
#95840=CARTESIAN_POINT ( 'NONE',  ( 6.320756440275016708, -1.388331291134708767, 1.386421665916007795 ) ) ;
#95841=CARTESIAN_POINT ( 'NONE',  ( 1.990992145637654698, 0.1870960246039363450, 1.952785824368876710 ) ) ;
#95845=CARTESIAN_POINT ( 'NONE',  ( 1.376322447316252306, -2.107681897322019271, -0.2017570171880012919 ) ) ;
#95848=CARTESIAN_POINT ( 'NONE',  ( 0.4097734724025984820, 1.271762808003698009, -1.331557029818277060 ) ) ;
#95850=CARTESIAN_POINT ( 'NONE',  ( 4.715793416201278454, 0.4818634375548909166, -2.116767182733831021 ) ) ;
#95852=CARTESIAN_POINT ( 'NONE',  ( 3.480829117359967917, -1.421471314662653196, 1.573842340227212366 ) ) ;
#95856=CARTESIAN_POINT ( 'NONE',  ( 3.374343653733542059, -1.230474546199412877, 1.652924668896506688 ) ) ;
#95858=CARTESIAN_POINT ( 'NONE',  ( 0.3800845246329161431, -0.2246070939678334044, -1.827447590993152682 ) ) ;
#95863=CARTESIAN_POINT ( 'NONE',  ( 3.005426500355699915, 1.909594650917462388, 1.212984053805040041 ) ) ;
#95865=CARTESIAN_POINT ( 'NONE',  ( 2.882852291059742278, -1.675512013591500482, -0.6893320933419128105 ) ) ;
#95867=CARTESIAN_POINT ( 'NONE',  ( 2.044013137410850778, 0.8228895493161382246, 1.730149048491230301 ) ) ;
#95868=CARTESIAN_POINT ( 'NONE',  ( 2.664580169416390643, -0.7900844611210651180, -1.913877855911281234 ) ) ;
#95871=CARTESIAN_POINT ( 'NONE',  ( 1.762511527598693784, -1.395553132451602174, 1.392767733363926119 ) ) ;
#95872=CARTESIAN_POINT ( 'NONE',  ( 0.3231025844343059505, -0.09812569541690382979, 1.924018777033975836 ) ) ;
#95873=CARTESIAN_POINT ( 'NONE',  ( 3.326877442632663939, 0.04465521416292458912, 1.870282673472216439 ) ) ;
#95874=CARTESIAN_POINT ( 'NONE',  ( 1.594773108836315956, -2.296930430523877575, -0.2226743027769726713 ) ) ;
#95876=CARTESIAN_POINT ( 'NONE',  ( 2.383057912469242812, -0.003606268183664260163, 1.861241884763777499 ) ) ;
#95878=CARTESIAN_POINT ( 'NONE',  ( 5.828601243409065269, -1.311231720126609490, 1.592247268936395121 ) ) ;
#95882=CARTESIAN_POINT ( 'NONE',  ( 5.895568648972373538, 1.592330039046478740, 1.378332891347531231 ) ) ;
#95885=CARTESIAN_POINT ( 'NONE',  ( 5.940740243836844847, 0.4152237956781511530, 2.121177236311201586 ) ) ;
#95886=CARTESIAN_POINT ( 'NONE',  ( 6.463536886191197262, -1.623326069159360063, -1.201424211086026261 ) ) ;
#95895=CARTESIAN_POINT ( 'NONE',  ( 5.173064673083394460, 1.776168143800487043, -0.9548534231369476544 ) ) ;
#95900=CARTESIAN_POINT ( 'NONE',  ( 6.051685545382852638, 0.6321331830463626789, -2.067208725892249799 ) ) ;
#95905=CARTESIAN_POINT ( 'NONE',  ( -0.1236200418614826352, -0.4170706148690634385, -1.876090511053402965 ) ) ;
#95907=CARTESIAN_POINT ( 'NONE',  ( 1.629113003107704793, -1.625012167801738183, 0.5787621435916143753 ) ) ;
#95912=CARTESIAN_POINT ( 'NONE',  ( 6.134044790494318278, 0.9221746925026914621, -1.627378824227587062 ) ) ;
#95913=CARTESIAN_POINT ( 'NONE',  ( 1.225244855396601551, 1.776329837998322780, 0.9471711224926461226 ) ) ;
#95915=CARTESIAN_POINT ( 'NONE',  ( 3.241465689944766915, -1.947025830926933043, 1.038692105600529159 ) ) ;
#95916=CARTESIAN_POINT ( 'NONE',  ( 5.893482054836863604, -1.966010524246808666, 0.9213097603111667366 ) ) ;
#95920=CARTESIAN_POINT ( 'NONE',  ( 3.352298257493666167, 0.9517314053594098100, -1.894962337767625904 ) ) ;
#95921=CARTESIAN_POINT ( 'NONE',  ( 2.812125237574264247, 1.117814398428567557, -1.678018709429726307 ) ) ;
#95922=CARTESIAN_POINT ( 'NONE',  ( 1.810541516808946039, -0.4857983738905074511, -1.745121406981971157 ) ) ;
#95927=CARTESIAN_POINT ( 'NONE',  ( 1.868237732200584977, -1.879526469796377164, -0.3696609625283857614 ) ) ;
#95934=CARTESIAN_POINT ( 'NONE',  ( 4.838837662799537753, 0.3661284547709364734, 2.130314178654398205 ) ) ;
#95937=CARTESIAN_POINT ( 'NONE',  ( 2.549219474610735947, 0.2639673528169218519, 2.104066465523121376 ) ) ;
#95938=CARTESIAN_POINT ( 'NONE',  ( 0.1753634416057497925, 7.629137130509101361, -2.744001747789548418 ) ) ;
#95940=CARTESIAN_POINT ( 'NONE',  ( 3.778557292509187260, -1.899022758751211182, -0.5288098451153611101 ) ) ;
#95941=CARTESIAN_POINT ( 'NONE',  ( 5.273660385517703553, 0.3669835118517566497, -1.876681294024808988 ) ) ;
#95945=CARTESIAN_POINT ( 'NONE',  ( 0.4497787391488928810, 1.533077660697563793, 1.391591089521776681 ) ) ;
#95946=CARTESIAN_POINT ( 'NONE',  ( 2.730336461235380430, 0.2382978201147344655, 1.927214864610910183 ) ) ;
#95947=ORIENTED_EDGE ( 'NONE', *, *, #103038, .T. ) ;
#95951=CARTESIAN_POINT ( 'NONE',  ( 2.818400364232038768, 1.968743758771305918, 0.7038092692753412649 ) ) ;
#95955=CARTESIAN_POINT ( 'NONE',  ( 0.6799528615496954753, 0.8915946574989388473, 1.576789060086491778 ) ) ;
#95957=CARTESIAN_POINT ( 'NONE',  ( 3.950008152305323428, 0.7444041667201055645, -2.077678867657362538 ) ) ;
#95958=CARTESIAN_POINT ( 'NONE',  ( 3.188704395469597497, -2.173853526369253331, -0.3788738375181537332 ) ) ;
#95961=CARTESIAN_POINT ( 'NONE',  ( 1.576665144504853400, -1.351504567317940664, 1.353124384123285617 ) ) ;
#95963=CARTESIAN_POINT ( 'NONE',  ( 4.668459276380106715, -0.8822503692092443783, -1.873099891353036561 ) ) ;
#95965=CARTESIAN_POINT ( 'NONE',  ( 2.553791647773369089, 0.5774160426356907960, -2.083079400968433248 ) ) ;
#95966=CARTESIAN_POINT ( 'NONE',  ( 4.669572502782517454, 1.262004115398765780, 1.791526714441132873 ) ) ;
#95974=CARTESIAN_POINT ( 'NONE',  ( 0.01820432788856435335, -1.842448466851685840, 0.8197770699841927522 ) ) ;
#95977=CARTESIAN_POINT ( 'NONE',  ( 4.698136132249701724, 0.8899761679339033282, -1.869364561350304488 ) ) ;
#95978=CARTESIAN_POINT ( 'NONE',  ( 2.965364049027201965, 0.2823637808789316028, -1.905579842893694975 ) ) ;
#95979=CARTESIAN_POINT ( 'NONE',  ( 5.571900387404195243, -0.9513999510230609635, 1.891474119154999745 ) ) ;
#95982=CARTESIAN_POINT ( 'NONE',  ( 4.012523933672189180, 0.7048025691861439235, 1.839212210364450151 ) ) ;
#95983=CARTESIAN_POINT ( 'NONE',  ( 6.263675073536269622, 1.173004239817846850, 1.969288764181243989 ) ) ;
#95984=CARTESIAN_POINT ( 'NONE',  ( 3.984828715814022981, -0.1808549858164226476, -1.816707794649790708 ) ) ;
#95990=CARTESIAN_POINT ( 'NONE',  ( 1.804012939494209267, 1.363607186100148638, -1.237405090928713092 ) ) ;
#95991=CARTESIAN_POINT ( 'NONE',  ( 5.256112987848621465, 0.8120324739511315393, -1.842333132669704554 ) ) ;
#95992=CARTESIAN_POINT ( 'NONE',  ( 5.889324137892314681, -0.8237033142024595689, -2.146187584169775953 ) ) ;
#95993=CARTESIAN_POINT ( 'NONE',  ( 6.051606296966551390, 1.483190043545830505, 1.284043323103729595 ) ) ;
#95997=CARTESIAN_POINT ( 'NONE',  ( 1.224293845215556953, 2.015865829440838031, 0.5543246906533367824 ) ) ;
#95998=CARTESIAN_POINT ( 'NONE',  ( 6.332837517263664395, 0.1779433324526000226, 1.760853854254845530 ) ) ;
#96000=CARTESIAN_POINT ( 'NONE',  ( -0.1106727585415940990, -0.002281114264979232885, -2.003378291782103027 ) ) ;
#96002=CARTESIAN_POINT ( 'NONE',  ( 1.030331162470259354, -1.574104619921200765, 0.7428470239391560259 ) ) ;
#96006=CARTESIAN_POINT ( 'NONE',  ( 1.717014342725260656, -0.2134408525867482198, 1.711538560699257916 ) ) ;
#96007=CARTESIAN_POINT ( 'NONE',  ( 2.050558489324630251, -1.691691439650149897, 1.393213601605561180 ) ) ;
#96008=CARTESIAN_POINT ( 'NONE',  ( -0.1054646484276201696, -0.7404878594409001202, -1.567598555697255369 ) ) ;
#96009=CARTESIAN_POINT ( 'NONE',  ( 3.897267319706390065, 1.864829029706360330, -1.179861312946443697 ) ) ;
#96012=CARTESIAN_POINT ( 'NONE',  ( 1.762787986429158016, -0.7786651900678620564, -2.026813006651595028 ) ) ;
#96014=CARTESIAN_POINT ( 'NONE',  ( 3.274719840360585721, -0.4174103159439371824, -2.075633323822536180 ) ) ;
#96015=CARTESIAN_POINT ( 'NONE',  ( 6.539320575229256249, 4.699150603835311912, 2.459441311396874941 ) ) ;
#96017=CARTESIAN_POINT ( 'NONE',  ( 3.281108521976669135, 2.071599159226782838, -0.9818635949487266590 ) ) ;
#96021=CARTESIAN_POINT ( 'NONE',  ( 5.619863295618399590, -0.5416267994347803150, 2.154155341088887177 ) ) ;
#96029=CARTESIAN_POINT ( 'NONE',  ( 3.586564705785996843, -0.5826563296015655480, 1.930417576838711957 ) ) ;
#96031=CARTESIAN_POINT ( 'NONE',  ( 2.325117943063298664, -1.883989625962046555, -0.8399396378151212650 ) ) ;
#96036=CARTESIAN_POINT ( 'NONE',  ( 5.138714532536901913, -1.880766731008373993, 1.124575086929799239 ) ) ;
#96037=CARTESIAN_POINT ( 'NONE',  ( 2.848279904836711118, 0.2930702634792031747, -1.994869876753922799 ) ) ;
#96038=CARTESIAN_POINT ( 'NONE',  ( 1.680954830071922812, 1.270413995023990106, 1.332975479855981416 ) ) ;
#96041=CARTESIAN_POINT ( 'NONE',  ( 4.963791182761823961, 1.805510465697376610, -0.2690417022049585438 ) ) ;
#96042=CARTESIAN_POINT ( 'NONE',  ( 5.731092321990707283, 2.014232586630093191, 0.09613807139101374077 ) ) ;
#96044=CARTESIAN_POINT ( 'NONE',  ( 5.348581951612152885, 0.6511601234850499242, 2.166799557567296919 ) ) ;
#96046=CARTESIAN_POINT ( 'NONE',  ( 1.119907265981748168, -2.054334215221398807, 0.4631877017708794231 ) ) ;
#96056=CARTESIAN_POINT ( 'NONE',  ( 2.549351761953377427, 0.2766319664159795355, 2.204086880180194274 ) ) ;
#96060=CARTESIAN_POINT ( 'NONE',  ( 3.174217076811707727, -0.9646401420641316227, -1.708233030250068785 ) ) ;
#96067=CARTESIAN_POINT ( 'NONE',  ( 2.127334043950947606, 1.896359100603739911, 0.9491756072362851349 ) ) ;
#96069=CARTESIAN_POINT ( 'NONE',  ( 4.680646922328831394, -2.095996545452833981, -0.5284188670612932626 ) ) ;
#96070=CARTESIAN_POINT ( 'NONE',  ( 2.331387312403776946, 0.8663521307504215008, -1.624669977836174839 ) ) ;
#96074=CARTESIAN_POINT ( 'NONE',  ( 5.841712918432809154, 1.738692355929325029, 0.07866246996769517275 ) ) ;
#96078=CARTESIAN_POINT ( 'NONE',  ( 2.799875798528407511, -0.6792266858460673795, 2.052276964324008635 ) ) ;
#96079=CARTESIAN_POINT ( 'NONE',  ( 5.009138659175729202, 2.010518709310470609, 0.1511151588593287465 ) ) ;
#96081=CARTESIAN_POINT ( 'NONE',  ( 2.079201547314021070, -0.1057080177612122196, -2.159229931372666389 ) ) ;
#96082=CARTESIAN_POINT ( 'NONE',  ( 2.969950176076568749, 1.051608646734447650, 1.667261953242512140 ) ) ;
#96083=CARTESIAN_POINT ( 'NONE',  ( 2.905482715143858030, -1.942096844255640109, 0.5424705965835219246 ) ) ;
#96084=CARTESIAN_POINT ( 'NONE',  ( 6.509000000000035868, 7.629137130509092479, 2.600000000000000977 ) ) ;
#96085=CARTESIAN_POINT ( 'NONE',  ( 5.021012369077997306, -1.842940949158570207, 0.6126725321249880674 ) ) ;
#96094=CARTESIAN_POINT ( 'NONE',  ( 1.677102584378454608, -2.095606157416990190, -0.6917391671936305997 ) ) ;
#96096=CARTESIAN_POINT ( 'NONE',  ( 5.506681978947471912, 0.5658967987182733639, 1.878394690154854496 ) ) ;
#96101=CARTESIAN_POINT ( 'NONE',  ( 4.786955173189685553, 1.366302399619228725, 1.234289508136581670 ) ) ;
#96106=CARTESIAN_POINT ( 'NONE',  ( 6.205353461901607304, 1.844339991697005798, -1.046509186232460697 ) ) ;
#96109=CARTESIAN_POINT ( 'NONE',  ( 6.749297902460969389, -1.652236475679531580, -1.231405567270830170 ) ) ;
#96111=CARTESIAN_POINT ( 'NONE',  ( 1.468971578825052804, 1.639158939101122758, 0.8813203298513817563 ) ) ;
#96112=CARTESIAN_POINT ( 'NONE',  ( 3.421284184235491743, -1.099380227797893905, -1.476844927387373163 ) ) ;
#96116=CARTESIAN_POINT ( 'NONE',  ( 6.610000000000009202, 6.036727194997777879, 2.594899704271665275 ) ) ;
#96118=CARTESIAN_POINT ( 'NONE',  ( 2.877765823869771644, 2.095344539500657799, -0.6929138170133213315 ) ) ;
#96119=CARTESIAN_POINT ( 'NONE',  ( 5.993528260394247020, 1.707464403934123798, 1.484360591965392828 ) ) ;
#96121=CARTESIAN_POINT ( 'NONE',  ( 6.293201719952925544, -0.09848415459409513850, -1.809066888985458199 ) ) ;
#96122=CARTESIAN_POINT ( 'NONE',  ( 0.1984543448181053105, 1.387095780679182377, -1.463931301963219855 ) ) ;
#96124=CARTESIAN_POINT ( 'NONE',  ( 6.244977087980838171, -1.579202250953464670, 1.002420361074819688 ) ) ;
#96125=CARTESIAN_POINT ( 'NONE',  ( 6.267989458847986306, -1.846849288558198188, 0.2287129521939580412 ) ) ;
#96128=CARTESIAN_POINT ( 'NONE',  ( 6.262547730648324595, -1.248425448203832611, 1.254777848270997254 ) ) ;
#96131=CARTESIAN_POINT ( 'NONE',  ( 0.9367328597341374463, -1.586666764284098807, 1.244388658875786424 ) ) ;
#96133=CARTESIAN_POINT ( 'NONE',  ( 3.281953686177707219, 1.336396692706752765, 1.627740544975244008 ) ) ;
#96139=CARTESIAN_POINT ( 'NONE',  ( 3.234633093136650928, 1.278207680322031026, -1.563912617747134970 ) ) ;
#96143=CARTESIAN_POINT ( 'NONE',  ( 3.761131992884462871, -1.904433681825665969, -1.022602951024270679 ) ) ;
#96148=CARTESIAN_POINT ( 'NONE',  ( 0.8894206616707257540, 0.1598827910747530057, 2.165323314709698632 ) ) ;
#96152=CARTESIAN_POINT ( 'NONE',  ( 2.173600921376659834, 1.351110561487681716, 1.725424542402646422 ) ) ;
#96154=CARTESIAN_POINT ( 'NONE',  ( 2.553932558351139193, 0.6037834209405189556, -2.180390065951258283 ) ) ;
#96156=CARTESIAN_POINT ( 'NONE',  ( 4.399625206644591557, -1.976670321813909892, 0.3981083777728141038 ) ) ;
#96163=CARTESIAN_POINT ( 'NONE',  ( 3.461912321176093599, 0.7928900474763724837, 1.582224000876080172 ) ) ;
#96166=CARTESIAN_POINT ( 'NONE',  ( 6.001041448284401447, 1.807427358944500684, -1.265864663738118345 ) ) ;
#96169=CARTESIAN_POINT ( 'NONE',  ( 5.817982510940042040, 0.9913841921252890543, -1.755779027446252138 ) ) ;
#96172=CARTESIAN_POINT ( 'NONE',  ( 3.485083742438867205, 1.691615344724434200, -0.7988839237506043522 ) ) ;
#96173=CARTESIAN_POINT ( 'NONE',  ( 3.344645782512998267, -2.038826501179476391, -0.3585456059004287765 ) ) ;
#96179=CARTESIAN_POINT ( 'NONE',  ( 2.611707774152134842, 0.5260268489151798121, -1.889944157703125072 ) ) ;
#96180=CARTESIAN_POINT ( 'NONE',  ( 0.3860920070548681804, -0.1017387759476989784, 2.013677428805898728 ) ) ;
#96184=CARTESIAN_POINT ( 'NONE',  ( 0.8252170375972631700, -1.778153878779257901, 0.5809004490327505099 ) ) ;
#96186=CARTESIAN_POINT ( 'NONE',  ( 2.601816991827472947, 1.426658649466717943, 1.420685320369071025 ) ) ;
#96188=CARTESIAN_POINT ( 'NONE',  ( 2.601287765717251510, -0.2046159961377100600, 2.107301599238825318 ) ) ;
#96190=CARTESIAN_POINT ( 'NONE',  ( 3.736834853878097107, -1.994506513866915576, -0.5549897870569252545 ) ) ;
#96192=CARTESIAN_POINT ( 'NONE',  ( 6.316366637557600860, 1.950215401406007354, 0.7537550503652605816 ) ) ;
#96194=CARTESIAN_POINT ( 'NONE',  ( 4.313378725478684395, -0.3118687524542098632, 1.798583714455632476 ) ) ;
#96200=CARTESIAN_POINT ( 'NONE',  ( 6.405322867445039314, 1.831175526881479776, 1.231239259074583092 ) ) ;
#96202=CARTESIAN_POINT ( 'NONE',  ( 5.074826771331380826, -1.382354945563003312, 1.321565576914075502 ) ) ;
#96207=CARTESIAN_POINT ( 'NONE',  ( 0.9250624443557056154, -1.167992581197497604, -1.423340509374780405 ) ) ;
#96211=CARTESIAN_POINT ( 'NONE',  ( 4.305816765424046011, -1.865681898550693107, 0.1353468896250972775 ) ) ;
#96212=CARTESIAN_POINT ( 'NONE',  ( -0.02319159430947542386, 1.394398620246390275, -2.068318759734718792 ) ) ;
#96218=CARTESIAN_POINT ( 'NONE',  ( 0.9714669389824581724, -0.2943045352901324518, 1.947222615934702139 ) ) ;
#96219=CARTESIAN_POINT ( 'NONE',  ( 2.355092412869797869, 0.09611577090188136441, -2.014234804981252847 ) ) ;
#96222=CARTESIAN_POINT ( 'NONE',  ( 6.727182134110200273, -0.004969159814478123736, 2.189081792362323586 ) ) ;
#96223=CARTESIAN_POINT ( 'NONE',  ( 2.994263412949605296, -0.6367403190770392074, -2.096898073876966251 ) ) ;
#96234=CARTESIAN_POINT ( 'NONE',  ( 5.020983453748395497, -1.746657797055195305, 0.5827527221545365510 ) ) ;
#96235=CARTESIAN_POINT ( 'NONE',  ( 1.453772141523026251, -1.459646937795316068, -1.386592938616920678 ) ) ;
#96236=CARTESIAN_POINT ( 'NONE',  ( 3.937115517079175842, 1.273119805769900026, 1.913412639830965434 ) ) ;
#96237=CARTESIAN_POINT ( 'NONE',  ( -0.02900071798685523866, 4.082342745036794618, -2.728474045032194262 ) ) ;
#96238=CARTESIAN_POINT ( 'NONE',  ( 2.570971337753673147, 1.659905555536644872, 0.8415416509589612737 ) ) ;
#96240=CARTESIAN_POINT ( 'NONE',  ( 6.047114369478562956, 0.1942372860762129894, 1.902532258075719351 ) ) ;
#96243=CARTESIAN_POINT ( 'NONE',  ( 5.249593148720715696, 2.088313038247250120, -0.1037309089504182269 ) ) ;
#96244=CARTESIAN_POINT ( 'NONE',  ( 3.256579335763456040, -1.417408692332474462, 1.220890361658559575 ) ) ;
#96246=CARTESIAN_POINT ( 'NONE',  ( 6.110883706712432861, -0.2185277653131960651, 1.828168259763853776 ) ) ;
#96249=CARTESIAN_POINT ( 'NONE',  ( 5.391107817497476695, 1.518517088589757424, -0.8181074574388611520 ) ) ;
#96251=CARTESIAN_POINT ( 'NONE',  ( 0.7911957196942709380, 1.314039333434241508, -1.131676627359794240 ) ) ;
#96254=CARTESIAN_POINT ( 'NONE',  ( 4.750930541093643100, -0.4693155065514472701, -2.119606683777853995 ) ) ;
#96255=CARTESIAN_POINT ( 'NONE',  ( 3.527797039230845311, -1.088449851438414218, -1.465592618984489670 ) ) ;
#96256=CARTESIAN_POINT ( 'NONE',  ( 1.059338230090471011, 1.600537254139059673, 1.134074526779847769 ) ) ;
#96257=CARTESIAN_POINT ( 'NONE',  ( 0.3689691111537584112, -0.2640367098126532031, -2.100658933187772526 ) ) ;
#96259=CARTESIAN_POINT ( 'NONE',  ( 0.1469514510107531868, -1.837142584329341410, 1.370738489780512825 ) ) ;
#96263=CARTESIAN_POINT ( 'NONE',  ( 3.018346832952636394, -2.117961878424143407, 0.1061830045200745365 ) ) ;
#96270=CARTESIAN_POINT ( 'NONE',  ( 0.7079804021624566124, 0.6528548590773940452, -1.964656565413371414 ) ) ;
#96271=CARTESIAN_POINT ( 'NONE',  ( 6.983263157960363898, 2.958708369276577432, 2.506372104999963657 ) ) ;
#96273=CARTESIAN_POINT ( 'NONE',  ( 2.508681548337174494, -2.215532678404589007, -0.1606611847707327678 ) ) ;
#96275=CARTESIAN_POINT ( 'NONE',  ( 0.9679111143040418641, -2.244285626452859450, -0.4966636800145701747 ) ) ;
#96277=CARTESIAN_POINT ( 'NONE',  ( 5.137578304370245874, 1.926469575665398448, -0.7373178810637993630 ) ) ;
#96281=CARTESIAN_POINT ( 'NONE',  ( 0.1333542156527113831, 2.876250315000815405, -2.534448870308704915 ) ) ;
#96282=CARTESIAN_POINT ( 'NONE',  ( 5.354971380013192395, 0.3533838956982695567, -1.806849549699687696 ) ) ;
#96285=CARTESIAN_POINT ( 'NONE',  ( 1.992754126006650806, 1.502677205460640764, -0.8464738358340985203 ) ) ;
#96286=CARTESIAN_POINT ( 'NONE',  ( 0.9894706735516716201, -0.4852629857438545691, 1.957171443305204761 ) ) ;
#96287=CARTESIAN_POINT ( 'NONE',  ( 1.793957786719975633, 1.699999873817940044, -1.547402956443538313 ) ) ;
#96289=CARTESIAN_POINT ( 'NONE',  ( 2.038691496156146865, 2.237626877524625524, 0.3332970034419027727 ) ) ;
#96290=CARTESIAN_POINT ( 'NONE',  ( 4.547555978022395529, -1.627529793438415417, -1.336665591334128100 ) ) ;
#96292=CARTESIAN_POINT ( 'NONE',  ( 2.178617772012156006, -0.08127397458944020381, -1.767985329221566815 ) ) ;
#96295=CARTESIAN_POINT ( 'NONE',  ( 5.337530604160453329, 0.9314408107504292822, -2.094771667654048208 ) ) ;
#96298=CARTESIAN_POINT ( 'NONE',  ( 4.066501749483540706, -2.044453849244652233, -0.7895499924894524568 ) ) ;
#96303=CARTESIAN_POINT ( 'NONE',  ( 3.756402471274498112, 0.6942424141608801724, 1.797233106274237713 ) ) ;
#96306=CARTESIAN_POINT ( 'NONE',  ( 6.099870585610251084, 1.463495690422533579, 1.534846084132005961 ) ) ;
#96312=CARTESIAN_POINT ( 'NONE',  ( 6.216338285296751032, 1.720575329815833721, 0.6561210673821930017 ) ) ;
#96316=CARTESIAN_POINT ( 'NONE',  ( 1.803882474592255258, 1.289405681850508190, -1.169162514946599174 ) ) ;
#96319=CARTESIAN_POINT ( 'NONE',  ( 0.1331565106231328843, 0.003911343561965873426, -1.946049565259087455 ) ) ;
#96322=CARTESIAN_POINT ( 'NONE',  ( 6.543834100630380846, 0.8322713294773576020, -1.995267709627518427 ) ) ;
#96325=CARTESIAN_POINT ( 'NONE',  ( 5.594645800149128156, -0.5210773734287167391, -2.097845705497362712 ) ) ;
#96329=CARTESIAN_POINT ( 'NONE',  ( 6.520779640719153392, 1.838571040693348646, 0.7116797190419403840 ) ) ;
#96330=CARTESIAN_POINT ( 'NONE',  ( 5.870364492519208888, -0.4185229733149243292, 1.682389803524992011 ) ) ;
#96332=CARTESIAN_POINT ( 'NONE',  ( 2.489988787850425656, -2.185901284972164405, -0.1580625509675498419 ) ) ;
#96333=CARTESIAN_POINT ( 'NONE',  ( 3.241587113499379669, -2.035928198617407592, 1.086232460313860892 ) ) ;
#96334=CARTESIAN_POINT ( 'NONE',  ( 5.887979924156289790, -0.9304241717780140641, 1.838884224927712419 ) ) ;
#96335=CARTESIAN_POINT ( 'NONE',  ( 1.394366005188719893, 1.587816662021741543, -1.117778254020968420 ) ) ;
#96340=CARTESIAN_POINT ( 'NONE',  ( 4.482752736079084421, -1.382999391253452615, 1.607682512923855445 ) ) ;
#96342=CARTESIAN_POINT ( 'NONE',  ( 2.461564753630896440, -1.930417925741171103, -0.5826551686555282439 ) ) ;
#96344=CARTESIAN_POINT ( 'NONE',  ( 4.050008041959299199, 0.7462531942188169731, -2.076888956485785975 ) ) ;
#96345=FACE_OUTER_BOUND ( 'NONE', #125951, .T. ) ;
#96350=CARTESIAN_POINT ( 'NONE',  ( 6.825078400183548055, -0.008500281443135982926, 2.244262395727573356 ) ) ;
#96353=CARTESIAN_POINT ( 'NONE',  ( 4.082927109850850833, -0.2000173336921743650, -2.051146848037002979 ) ) ;
#96358=CARTESIAN_POINT ( 'NONE',  ( 3.475264548829166689, -1.782285498782819610, -0.9499825727283210952 ) ) ;
#96364=CARTESIAN_POINT ( 'NONE',  ( 3.186453599190769648, -2.030135695866011503, -0.3537577654625714274 ) ) ;
#96365=CARTESIAN_POINT ( 'NONE',  ( 3.217422812353257555, 1.967887761762876941, 0.4390297752325384995 ) ) ;
#96371=CARTESIAN_POINT ( 'NONE',  ( 1.693040327840355408, -0.6214066371539993527, 1.733238834403828754 ) ) ;
#96372=CARTESIAN_POINT ( 'NONE',  ( 6.463508838306311510, 0.3818026259072569983, -2.173449913608487716 ) ) ;
#96374=CARTESIAN_POINT ( 'NONE',  ( 3.093221446634909721, 1.855696356685032633, -1.108285163885482039 ) ) ;
#96377=CARTESIAN_POINT ( 'NONE',  ( 4.153586450535729391, 2.052860580235102095, -0.5180077198428371110 ) ) ;
#96379=CARTESIAN_POINT ( 'NONE',  ( 1.709613803025863188, -1.856884215550944850, 0.2259493607114013147 ) ) ;
#96380=CARTESIAN_POINT ( 'NONE',  ( 4.821144081919094049, -0.09777198692111942202, 1.969167557456591666 ) ) ;
#96381=CARTESIAN_POINT ( 'NONE',  ( 4.575407832915947104, 1.497500392235491029, 1.350737390116145242 ) ) ;
#96385=CARTESIAN_POINT ( 'NONE',  ( 6.111965604441711442, -2.090389680133018846, 0.2559737671669787273 ) ) ;
#96390=CARTESIAN_POINT ( 'NONE',  ( 6.639320575229223031, 6.036153810275548537, 2.598155902862766542 ) ) ;
#96391=CARTESIAN_POINT ( 'NONE',  ( 4.838727080925394830, 0.3361901323847040213, 1.942436603694275510 ) ) ;
#96392=CARTESIAN_POINT ( 'NONE',  ( 6.064714679231743233, 0.6376439298158544933, 1.916535431269225098 ) ) ;
#96394=CARTESIAN_POINT ( 'NONE',  ( 4.758593218111947465, 0.8799714688421821362, 2.133523255312119726 ) ) ;
#96396=CARTESIAN_POINT ( 'NONE',  ( 2.166912933460037660, 1.531321095959611966, -1.381971985785889423 ) ) ;
#96403=CARTESIAN_POINT ( 'NONE',  ( 4.088457082891777894, 1.164728776245987918, -1.832164736925721682 ) ) ;
#96406=CARTESIAN_POINT ( 'NONE',  ( 3.192734241421916419, 1.453351889590439816, 1.130385295574042104 ) ) ;
#96408=CARTESIAN_POINT ( 'NONE',  ( 6.620655732516642189, 0.6076529131340856482, 1.780684370158796881 ) ) ;
#96409=CARTESIAN_POINT ( 'NONE',  ( 5.671465802443460547, 1.304529079428708549, 1.760837017921567771 ) ) ;
#96411=CARTESIAN_POINT ( 'NONE',  ( 6.420815857685610695, 2.108269355124866351, 0.8215519888849237562 ) ) ;
#96417=CARTESIAN_POINT ( 'NONE',  ( 0.9359865740741512008, 1.742660192269055663, 0.3080425777817352162 ) ) ;
#96419=CARTESIAN_POINT ( 'NONE',  ( 4.705731023397805579, 1.493295645070455535, 1.350234862845017592 ) ) ;
#96421=CARTESIAN_POINT ( 'NONE',  ( 2.924945619078959336, 1.982447918529605557, 0.7109604360746536456 ) ) ;
#96422=CARTESIAN_POINT ( 'NONE',  ( 1.563933522115690922, -1.023182376180698849, 1.619245466209729756 ) ) ;
#96424=CARTESIAN_POINT ( 'NONE',  ( 3.086336304319175383, 1.096367280595906601, -1.635968976963786847 ) ) ;
#96425=CARTESIAN_POINT ( 'NONE',  ( 5.361584196017279424, -1.594725845915157647, -1.239436484511841519 ) ) ;
#96426=CARTESIAN_POINT ( 'NONE',  ( 1.445950363956361340, 1.868363765441739099, 0.09516058986362013750 ) ) ;
#96427=CARTESIAN_POINT ( 'NONE',  ( 1.715213470010600538, -1.680963409367957295, -1.011360081469035999 ) ) ;
#96428=CARTESIAN_POINT ( 'NONE',  ( 3.791373243616827704, 1.250846937323921715, 1.187934608979845708 ) ) ;
#96429=CARTESIAN_POINT ( 'NONE',  ( 1.371198541116287917, -1.641758494746584418, -0.9804709962101465504 ) ) ;
#96431=CARTESIAN_POINT ( 'NONE',  ( 1.067327838873022516, -1.996528553209110379, -0.9406146916221403975 ) ) ;
#96435=CARTESIAN_POINT ( 'NONE',  ( 6.807498166657679484, -0.4075194142965677391, 1.832415718333743282 ) ) ;
#96439=CARTESIAN_POINT ( 'NONE',  ( 6.578973861349465935, 1.929489650308688464, 0.7507879531711419974 ) ) ;
#96441=CARTESIAN_POINT ( 'NONE',  ( 0.5728211633247158874, 1.428863753495920763, -1.498466819491943269 ) ) ;
#96446=CARTESIAN_POINT ( 'NONE',  ( 5.690118541956746157, 1.263103799472656164, 1.703077153987264669 ) ) ;
#96451=CARTESIAN_POINT ( 'NONE',  ( 6.584431417889404337, 1.130572321132311098, -1.603143135845342515 ) ) ;
#96453=CARTESIAN_POINT ( 'NONE',  ( 4.429064430395744267, 0.9478954142983322395, 1.779353956671766657 ) ) ;
#96454=CARTESIAN_POINT ( 'NONE',  ( 4.012823373000539817, 0.09967532595039167720, 1.913279002700827514 ) ) ;
#96456=CARTESIAN_POINT ( 'NONE',  ( 1.136565065649897344, 0.4323997850379874830, 2.148315308122191514 ) ) ;
#96457=CARTESIAN_POINT ( 'NONE',  ( 0.1333692844072559003, 2.872395615372814515, -2.542035612928101873 ) ) ;
#96459=CARTESIAN_POINT ( 'NONE',  ( 5.256112987848621465, 0.8120324739511315393, -1.842333132669704554 ) ) ;
#96462=CARTESIAN_POINT ( 'NONE',  ( 5.589508065689547500, -0.5136281568550029597, 2.053882654316901313 ) ) ;
#96464=CARTESIAN_POINT ( 'NONE',  ( 2.788710525494293879, 1.791885054564039903, -1.076980376859866029 ) ) ;
#96466=CARTESIAN_POINT ( 'NONE',  ( 2.449869591326372387, 1.724352457016034457, 0.04528501180301596624 ) ) ;
#96479=CARTESIAN_POINT ( 'NONE',  ( 1.910541399130718743, -0.4838386274770510864, -1.745561575705076862 ) ) ;
#96484=CARTESIAN_POINT ( 'NONE',  ( 2.455456329753392897, -1.343237331403211776, -1.215579648594692808 ) ) ;
#96485=CARTESIAN_POINT ( 'NONE',  ( 6.639320575229256782, 2.986994467643698137, 2.250762793112503157 ) ) ;
#96488=CARTESIAN_POINT ( 'NONE',  ( 2.927998328727512867, 0.9930260268339460294, 1.573771836281928627 ) ) ;
#96490=CARTESIAN_POINT ( 'NONE',  ( 0.1400564425528905699, 0.7337865575636399740, 1.769695213874568962 ) ) ;
#96491=CARTESIAN_POINT ( 'NONE',  ( 0.1822601575737579360, -1.769359155225664226, -0.4491840103194589817 ) ) ;
#96497=CARTESIAN_POINT ( 'NONE',  ( 4.750814831274846384, -0.4274863908861815665, -1.922328355476431216 ) ) ;
#96500=CARTESIAN_POINT ( 'NONE',  ( 0.1993191639408486426, -0.5556045495253292277, 2.015383906575985318 ) ) ;
#96502=CARTESIAN_POINT ( 'NONE',  ( 5.262690832784179484, -1.395389315813623909, 1.328347855495640273 ) ) ;
#96505=CARTESIAN_POINT ( 'NONE',  ( 1.963769682107346037, 0.3752889857368996163, -2.174583152744386627 ) ) ;
#96507=CARTESIAN_POINT ( 'NONE',  ( -0.2049973002360427898, -0.1418364932926942379, -1.881151990943498387 ) ) ;
#96510=CARTESIAN_POINT ( 'NONE',  ( 0.4495734683114894215, 1.456899865409568617, 1.325532655419828787 ) ) ;
#96511=CARTESIAN_POINT ( 'NONE',  ( 1.856878829904203165, 0.3300924852138227283, -1.913646475244117795 ) ) ;
#96513=CARTESIAN_POINT ( 'NONE',  ( 0.8607036144342284922, -0.7282710370301350711, 1.880145570116364073 ) ) ;
#96515=CARTESIAN_POINT ( 'NONE',  ( 4.961672996587167539, -0.4989766864872626217, 1.792691909438326681 ) ) ;
#96521=CARTESIAN_POINT ( 'NONE',  ( 1.593588134247824639, -0.7342643958434189599, 2.065040727587868830 ) ) ;
#96525=CARTESIAN_POINT ( 'NONE',  ( 1.418276456094772708, 1.227529518603141190, -1.351586893430449576 ) ) ;
#96530=CARTESIAN_POINT ( 'NONE',  ( 1.559075672363739118, -1.651969382833524902, -0.9909376787137593734 ) ) ;
#96531=CARTESIAN_POINT ( 'NONE',  ( 4.469553177461598636, -0.3394721387663233170, 1.932013773527321066 ) ) ;
#96536=CARTESIAN_POINT ( 'NONE',  ( 4.564136437409766600, -1.431273618155091576, 1.659743667367798103 ) ) ;
#96538=CARTESIAN_POINT ( 'NONE',  ( 4.381733404717279790, -1.982624999272282862, 0.5960583376443123749 ) ) ;
#96542=CARTESIAN_POINT ( 'NONE',  ( 4.078954460043759056, -0.8795263853869551562, 2.123946672719174700 ) ) ;
#96548=CARTESIAN_POINT ( 'NONE',  ( 4.066302494797935374, -1.812431348068560988, -0.6977731361806001065 ) ) ;
#96552=CARTESIAN_POINT ( 'NONE',  ( 5.080287894202283105, 0.9478536798121822704, 1.660923459347658282 ) ) ;
#96553=CARTESIAN_POINT ( 'NONE',  ( 5.192313411850084215, -1.712133481052197093, -0.2078965086465163203 ) ) ;
#96554=CARTESIAN_POINT ( 'NONE',  ( 4.329314735043091389, -1.561880650076686861, -1.275557594027726394 ) ) ;
#96555=CARTESIAN_POINT ( 'NONE',  ( 5.028124288008245735, -1.972403190421234687, 1.180361310613570414 ) ) ;
#96557=CARTESIAN_POINT ( 'NONE',  ( 0.6806489137391663613, -1.222764829241920648, 1.836970590647703627 ) ) ;
#96560=CARTESIAN_POINT ( 'NONE',  ( 6.081276588353502710, 1.634447734625959825, -0.6791225938206167934 ) ) ;
#96561=CARTESIAN_POINT ( 'NONE',  ( 5.045546153961558922, -1.458558117013383892, 1.392544180963309230 ) ) ;
#96563=CARTESIAN_POINT ( 'NONE',  ( 2.344040366607359704, 2.291775683190785173, 0.05432913299479279201 ) ) ;
#96564=CARTESIAN_POINT ( 'NONE',  ( 1.323703871734905890, 1.676395044522845712, 0.4671252976603932350 ) ) ;
#96566=CARTESIAN_POINT ( 'NONE',  ( 1.159081676615776990, -0.4145447896758222561, -1.683414020171439818 ) ) ;
#96569=CARTESIAN_POINT ( 'NONE',  ( 1.223348113247175961, -1.962646724111057672, -0.9287667758015824004 ) ) ;
#96570=CARTESIAN_POINT ( 'NONE',  ( 2.290250256651988892, -0.7762311197250795214, -1.861343989391924358 ) ) ;
#96573=CARTESIAN_POINT ( 'NONE',  ( 6.059198490463121090, -1.653572398999035853, -0.9882694798356050914 ) ) ;
#96575=CARTESIAN_POINT ( 'NONE',  ( 2.338390812749164827, -1.283062462031187456, -1.813217020134863411 ) ) ;
#96581=CARTESIAN_POINT ( 'NONE',  ( 5.179165720741062628, 1.174484231026547976, 1.284593650646998375 ) ) ;
#96582=CARTESIAN_POINT ( 'NONE',  ( 4.070719198475009293, 1.388998261151509039, -1.385754695631277844 ) ) ;
#96586=CARTESIAN_POINT ( 'NONE',  ( 4.429186382639688446, 0.1052742795825665628, 2.260063922926962121 ) ) ;
#96587=CARTESIAN_POINT ( 'NONE',  ( 1.574752048370867907, 1.386759265612296455, -1.527078818449955966 ) ) ;
#96589=CARTESIAN_POINT ( 'NONE',  ( 2.290224401178039049, -0.9674489778378884131, 2.045383877150886320 ) ) ;
#96592=CARTESIAN_POINT ( 'NONE',  ( 3.989402248074361612, 1.353031944225962624, 1.291829963354161892 ) ) ;
#96593=CARTESIAN_POINT ( 'NONE',  ( 3.041388834704723099, -1.310848641452688979, 1.135385315042459542 ) ) ;
#96594=CARTESIAN_POINT ( 'NONE',  ( 6.427279137517246888, -1.429865906218323435, -1.660902671979214595 ) ) ;
#96595=CARTESIAN_POINT ( 'NONE',  ( 0.4115098346569624477, 1.921242953230850148, 1.085561749797583797 ) ) ;
#96596=CARTESIAN_POINT ( 'NONE',  ( 3.713887418366210280, -2.130098009959373151, 0.3673708613747132534 ) ) ;
#96597=CARTESIAN_POINT ( 'NONE',  ( 5.033120997586177481, -1.374529083251808892, -1.372050024763036280 ) ) ;
#96599=CARTESIAN_POINT ( 'NONE',  ( 6.292256349370360269, -1.861554482619768525, -0.1834065582871149958 ) ) ;
#96604=CARTESIAN_POINT ( 'NONE',  ( 5.660779783930850684, 1.203351582566011047, 1.617819807990819481 ) ) ;
#96608=CARTESIAN_POINT ( 'NONE',  ( 3.228933428962964758, 0.04559371896543929631, 1.825288036790246204 ) ) ;
#96615=CARTESIAN_POINT ( 'NONE',  ( 6.287761640583830136, 1.932026593981367002, -0.5884565063561957299 ) ) ;
#96616=CARTESIAN_POINT ( 'NONE',  ( 0.6805317496583452863, 1.048634805427307359, 1.842989218901350812 ) ) ;
#96619=CARTESIAN_POINT ( 'NONE',  ( 1.920531177235841103, -1.320465346956477992, 1.311572250416197960 ) ) ;
#96621=CARTESIAN_POINT ( 'NONE',  ( 6.772340629568521564, -1.270048932776141726, 1.623522132280514896 ) ) ;
#96622=CARTESIAN_POINT ( 'NONE',  ( 6.311172677262812059, 1.158691452862798954, -1.650079838712660063 ) ) ;
#96627=CARTESIAN_POINT ( 'NONE',  ( 0.07680821025391955381, 1.395885924038504644, -2.068540888291516833 ) ) ;
#96630=CARTESIAN_POINT ( 'NONE',  ( 6.766953912288387940, -2.015720078709513086, 0.04667315333419658208 ) ) ;
#96631=CARTESIAN_POINT ( 'NONE',  ( 4.189278935350455590, -0.7026162016144417155, 1.701997885059022497 ) ) ;
#96633=CARTESIAN_POINT ( 'NONE',  ( 3.739178398684524396, 0.3374720328367666888, 2.282779155512550062 ) ) ;
#96635=CARTESIAN_POINT ( 'NONE',  ( 5.448557382023540896, 0.6217387762853660016, 2.070273951448368788 ) ) ;
#96637=CARTESIAN_POINT ( 'NONE',  ( 0.7142757748631656245, 1.794906310038762109, 0.7420174003010558961 ) ) ;
#96641=CARTESIAN_POINT ( 'NONE',  ( 5.149944687579217195, -0.2746161857135383522, -2.281865060072391760 ) ) ;
#96644=CARTESIAN_POINT ( 'NONE',  ( 4.698043743269282757, -1.870269067358639958, -0.04562963166049315705 ) ) ;
#96646=CARTESIAN_POINT ( 'NONE',  ( 1.406358598101828283, -1.903450966454448334, -0.1843715739238485363 ) ) ;
#96649=CARTESIAN_POINT ( 'NONE',  ( 3.299657469156279888, 1.739734091921738557, 1.357710657151039779 ) ) ;
#96656=CARTESIAN_POINT ( 'NONE',  ( 1.352734582195244561, -1.556726207391207817, 1.209420702486432297 ) ) ;
#96657=CARTESIAN_POINT ( 'NONE',  ( 0.7632353006940760798, -1.668858575275869116, 1.593938313602519363 ) ) ;
#96658=CARTESIAN_POINT ( 'NONE',  ( 2.541395235131336694, 1.794889867694851260, -0.7924082849640816661 ) ) ;
#96659=CARTESIAN_POINT ( 'NONE',  ( 5.489153638472886954, 0.1464082308396240373, 2.057405090433866324 ) ) ;
#96667=CARTESIAN_POINT ( 'NONE',  ( 1.217902493145516463, 0.4257177869225349243, -2.128761017034991543 ) ) ;
#96674=CARTESIAN_POINT ( 'NONE',  ( 2.864352374448192240, -1.292745417840787781, 1.352161534859085412 ) ) ;
#96676=CARTESIAN_POINT ( 'NONE',  ( 6.345025448074324892, -1.829860219143174982, 1.150409744987097804 ) ) ;
#96679=CARTESIAN_POINT ( 'NONE',  ( 6.727182134110201162, 0.6069527724139511804, 1.765151538780465712 ) ) ;
#96682=CARTESIAN_POINT ( 'NONE',  ( 2.314975094136799694, 1.534822137071165438, -1.140449143091977646 ) ) ;
#96683=CARTESIAN_POINT ( 'NONE',  ( 3.643183530381717716, -1.339777920602200467, -1.156514101391445948 ) ) ;
#96684=CARTESIAN_POINT ( 'NONE',  ( 2.244649938279310142, 1.855272219182309668, 0.4629769397326845004 ) ) ;
#96687=CARTESIAN_POINT ( 'NONE',  ( 5.026915340915774522, -1.640707562863060520, 0.9885212758144015233 ) ) ;
#96690=CARTESIAN_POINT ( 'NONE',  ( 6.549268392505379843, 1.714383406945050980, -0.9693629108104614422 ) ) ;
#96692=CARTESIAN_POINT ( 'NONE',  ( 1.828540510153942922, -1.004066958311781832, -1.867862179375394005 ) ) ;
#96693=CARTESIAN_POINT ( 'NONE',  ( 4.926551758443064699, 1.790249073151507497, 0.5424879929923772659 ) ) ;
#96694=CARTESIAN_POINT ( 'NONE',  ( 0.7326872660318053398, 0.1314506862302306234, 1.821024990000128518 ) ) ;
#96696=CARTESIAN_POINT ( 'NONE',  ( 4.424592250794217030, 1.359014646446855767, -1.738718759629574118 ) ) ;
#96700=CARTESIAN_POINT ( 'NONE',  ( 2.365751517750969146, -0.4541778970535991777, 2.011898661289913903 ) ) ;
#96708=CARTESIAN_POINT ( 'NONE',  ( 3.789561645344252661, -1.914057400617325433, 0.7896510022299551013 ) ) ;
#96710=CARTESIAN_POINT ( 'NONE',  ( 2.724079341238437646, -1.242159841233332562, -1.768869243570107885 ) ) ;
#96712=CARTESIAN_POINT ( 'NONE',  ( 2.121745675717867652, -0.4403476065239861903, 1.970919799026500607 ) ) ;
#96717=CARTESIAN_POINT ( 'NONE',  ( -0.1179535434602772825, -2.016182236903838465, -0.04464881524945257807 ) ) ;
#96718=CARTESIAN_POINT ( 'NONE',  ( 4.493798347139664529, -2.191065130646638437, -0.05333993539427539510 ) ) ;
#96720=CARTESIAN_POINT ( 'NONE',  ( 4.166199421025417848, 1.911861072351704882, -0.05224187775455800542 ) ) ;
#96724=CARTESIAN_POINT ( 'NONE',  ( 2.355092412869797869, 0.09611577090188136441, -2.014234804981252847 ) ) ;
#96727=CARTESIAN_POINT ( 'NONE',  ( 5.209832820053398983, -1.716139821054706749, 0.1720855783484842860 ) ) ;
#96728=CARTESIAN_POINT ( 'NONE',  ( 0.1405533004714800693, 1.287645162063441928, -2.525240623925705474 ) ) ;
#96733=CARTESIAN_POINT ( 'NONE',  ( 0.7079804021624566124, 0.6528548590773939342, -1.964656565413371414 ) ) ;
#96737=CARTESIAN_POINT ( 'NONE',  ( 5.022017691244989201, -1.802217576119311770, 0.1829344734397136685 ) ) ;
#96740=CARTESIAN_POINT ( 'NONE',  ( 6.428355384240774129, -0.8606449381524762243, -1.593976378398887173 ) ) ;
#96743=CARTESIAN_POINT ( 'NONE',  ( 3.574349206294104242, -2.111947977397998777, -0.5846811180381800144 ) ) ;
#96744=CARTESIAN_POINT ( 'NONE',  ( 0.5023040531197673353, 1.956348610274569744, 0.1481081594910879096 ) ) ;
#96746=CARTESIAN_POINT ( 'NONE',  ( 5.466386403393696192, -1.869944189333021090, -0.4150143681153609654 ) ) ;
#96752=CARTESIAN_POINT ( 'NONE',  ( 1.885829143180400624, 1.490600019384461294, 1.565824011241300440 ) ) ;
#96755=CARTESIAN_POINT ( 'NONE',  ( 1.430379662499326354, 1.758314708518812663, 0.4907259477668829972 ) ) ;
#96757=CARTESIAN_POINT ( 'NONE',  ( 4.612205747861584548, -0.7811881352849485705, -1.650120847746315622 ) ) ;
#96759=CARTESIAN_POINT ( 'NONE',  ( 2.619282413590624525, 1.617716081779559278, 1.019604094833974628 ) ) ;
#96761=CARTESIAN_POINT ( 'NONE',  ( 3.701571259021796845, -1.489687541828330852, -1.288469680017936048 ) ) ;
#96763=CARTESIAN_POINT ( 'NONE',  ( 5.425317942119275649, -1.235012148030777412, -1.498765763798795891 ) ) ;
#96767=CARTESIAN_POINT ( 'NONE',  ( 5.590118541908202232, 1.264772504208915072, 1.701965355810124203 ) ) ;
#96769=CARTESIAN_POINT ( 'NONE',  ( 2.648957786072099641, 0.2360777847093403214, 1.897596177352772306 ) ) ;
#96775=CARTESIAN_POINT ( 'NONE',  ( 5.250644345176154637, 1.983683461502975254, 0.3419521592970317103 ) ) ;
#96777=CARTESIAN_POINT ( 'NONE',  ( 4.740742070742828496, 0.3150700179065483719, 1.798135100120237251 ) ) ;
#96778=CARTESIAN_POINT ( 'NONE',  ( 0.7837444799244470683, -1.966470238067185905, 0.6478734989143406509 ) ) ;
#96782=CARTESIAN_POINT ( 'NONE',  ( 5.629731426258720361, -1.187751674602673058, -1.445209747047627946 ) ) ;
#96793=CARTESIAN_POINT ( 'NONE',  ( 1.059532578591013463, 1.690300726139557952, 1.195051122980017144 ) ) ;
#96794=CARTESIAN_POINT ( 'NONE',  ( 2.179462045401040715, 1.638881033884627803, 1.340452329455198210 ) ) ;
#96797=CARTESIAN_POINT ( 'NONE',  ( 0.2331713839410576583, 0.005725554726919174046, -1.953566683266183102 ) ) ;
#96802=CARTESIAN_POINT ( 'NONE',  ( 2.765910322896072859, 1.227222833649963540, 1.935908780871216761 ) ) ;
#96803=CARTESIAN_POINT ( 'NONE',  ( 0.7678472254676466102, 0.8974085622692473674, 1.589837017038860045 ) ) ;
#96804=CARTESIAN_POINT ( 'NONE',  ( 1.986440140746603911, -1.173720106059353396, 1.509789020923378189 ) ) ;
#96808=CARTESIAN_POINT ( 'NONE',  ( 1.441653692521651653, -1.894234556111865420, 0.6821031695033189513 ) ) ;
#96809=CARTESIAN_POINT ( 'NONE',  ( 0.5319879461419263489, 1.124744735265088780, 1.607134405190835391 ) ) ;
#96813=CARTESIAN_POINT ( 'NONE',  ( 3.503930302474305591, -0.8474990640115993568, -1.911341529346534118 ) ) ;
#96814=CARTESIAN_POINT ( 'NONE',  ( 3.238855601640895809, -1.561498447111120402, 0.8330696194922878606 ) ) ;
#96816=CARTESIAN_POINT ( 'NONE',  ( 0.1643758432304382178, -1.428106194732338352, 1.662303017507735792 ) ) ;
#96817=CARTESIAN_POINT ( 'NONE',  ( 5.015436155323918399, -0.9350583589616268121, -1.467585299639478702 ) ) ;
#96820=CARTESIAN_POINT ( 'NONE',  ( 4.833154173618329885, -1.132187431169606739, 1.313192701189482614 ) ) ;
#96821=CARTESIAN_POINT ( 'NONE',  ( 4.334556721604589491, -1.253389318223859350, 1.772677672673736771 ) ) ;
#96823=CARTESIAN_POINT ( 'NONE',  ( 5.700407750362016301, 1.350738941191354625, -1.497498989668680114 ) ) ;
#96824=CARTESIAN_POINT ( 'NONE',  ( 6.406249999940950346, 1.895863741710943406, -0.7852924748303196090 ) ) ;
#96826=CARTESIAN_POINT ( 'NONE',  ( 3.205993170255555302, -1.924248618553949353, 0.09317337220685062427 ) ) ;
#96828=CARTESIAN_POINT ( 'NONE',  ( 6.328415579541645464, -1.046111920768664660, -1.959710881125435789 ) ) ;
#96830=CARTESIAN_POINT ( 'NONE',  ( 6.983263157960393208, 0.5798717822590447879, 1.998431770337566027 ) ) ;
#96833=CARTESIAN_POINT ( 'NONE',  ( 1.366231352279376310, 0.6402347118669349246, -2.127050378772620487 ) ) ;
#96838=B_SPLINE_CURVE_WITH_KNOTS ( 'NONE', 3,
 ( #52452, #50322, #3661, #169397, #70800, #104409, #170458, #36185, #182434, #69738, #100132 ),
 .UNSPECIFIED., .F., .F.,
 ( 4, 1, 1, 1, 1, 1, 1, 1, 4 ),
 ( 0.000000000000000000, 0.2257091236145174484, 0.3979912149639216468, 0.5260416812932605657, 0.6190739408849097458, 0.6862087210430605211, 0.7361363507675404705, 0.7768852254246026989, 0.9999999999999998890 ),
 .UNSPECIFIED. ) ;
#96839=CARTESIAN_POINT ( 'NONE',  ( 0.08851783505585240908, -0.5350849913869708541, 1.944072358963434555 ) ) ;
#96841=CARTESIAN_POINT ( 'NONE',  ( 6.004357462130720080, 2.060136995665005522, 0.1050117271170700056 ) ) ;
#96846=CARTESIAN_POINT ( 'NONE',  ( 6.591075523649926993, 1.627300515804396941, -0.9222108319836411772 ) ) ;
#96847=CARTESIAN_POINT ( 'NONE',  ( 5.695915039874445362, 1.533740007788013449, 0.8092579662780824412 ) ) ;
#96848=CARTESIAN_POINT ( 'NONE',  ( 4.370479661831958573, -0.005723030808118654937, -1.740626722379432501 ) ) ;
#96850=CARTESIAN_POINT ( 'NONE',  ( 2.859215333236740264, 0.3337469566037793989, -2.267824818490314254 ) ) ;
#96852=CARTESIAN_POINT ( 'NONE',  ( 1.675478281319711549, -0.9859397310463119402, 1.554705294492392254 ) ) ;
#96855=CARTESIAN_POINT ( 'NONE',  ( 1.869861807837460921, 0.9356042063937075604, 1.567457579366556386 ) ) ;
#96856=CARTESIAN_POINT ( 'NONE',  ( 2.320935597664942396, 0.9480396085976348086, -1.779626998253575509 ) ) ;
#96857=CARTESIAN_POINT ( 'NONE',  ( 1.324469081069843623, 2.112754910877081560, 0.5817525768514880680 ) ) ;
#96859=CARTESIAN_POINT ( 'NONE',  ( 3.962026973360888604, 2.090321222856437178, -0.2555144258320155015 ) ) ;
#96862=CARTESIAN_POINT ( 'NONE',  ( 1.539598694730393680, 1.913698299121506352, -0.7905179490511196061 ) ) ;
#96865=CARTESIAN_POINT ( 'NONE',  ( 3.791739704763209318, 1.996120715041304061, -0.7158466834289514136 ) ) ;
#96866=CARTESIAN_POINT ( 'NONE',  ( 6.111906964637446649, -1.811269838261083232, 0.2284818145076653595 ) ) ;
#96873=CARTESIAN_POINT ( 'NONE',  ( 3.427994306938833002, -1.989183439576122758, 0.3493681432537446563 ) ) ;
#96874=CARTESIAN_POINT ( 'NONE',  ( 0.9914056592630847708, 1.857388527897243291, -0.9925227068504693939 ) ) ;
#96877=CARTESIAN_POINT ( 'NONE',  ( 5.172628746253565168, 1.285086882066178937, -1.346197146212588347 ) ) ;
#96884=CARTESIAN_POINT ( 'NONE',  ( 1.873419974815058842, -0.2433403713097622156, 1.946663811685337420 ) ) ;
#96885=CARTESIAN_POINT ( 'NONE',  ( 0.6378455412261313517, -1.529572671500577297, -1.527792216034072670 ) ) ;
#96889=CARTESIAN_POINT ( 'NONE',  ( 2.635775109972549490, 0.08874582706053059378, -1.731711113058966633 ) ) ;
#96890=CARTESIAN_POINT ( 'NONE',  ( 2.853125853291237579, 1.731928873650347311, -0.1707260732264591074 ) ) ;
#96891=CARTESIAN_POINT ( 'NONE',  ( 6.305331169356420240, 1.914788864002760160, 1.287784001537124468 ) ) ;
#96894=CARTESIAN_POINT ( 'NONE',  ( 2.636070936407476584, 0.9742463255392861399, -1.815968889038493073 ) ) ;
#96896=CARTESIAN_POINT ( 'NONE',  ( 1.300157425512000087, -1.823841169980220167, 0.8594962466553013325 ) ) ;
#96897=CARTESIAN_POINT ( 'NONE',  ( 6.925078400183569904, 6.033938712579569597, 2.739235483740619426 ) ) ;
#96899=CARTESIAN_POINT ( 'NONE',  ( 0.8308620510419548744, 0.1428995296039961560, 1.966335887032538032 ) ) ;
#96900=CARTESIAN_POINT ( 'NONE',  ( 4.236511230858605259, 1.172298487584079396, -1.510895503047122945 ) ) ;
#96905=CARTESIAN_POINT ( 'NONE',  ( 1.682291859507994092, 1.040098842697153136, 1.731126528333865933 ) ) ;
#96906=CARTESIAN_POINT ( 'NONE',  ( 4.964078638949532163, 2.283327717301757431, -0.3329734184051634238 ) ) ;
#96907=CARTESIAN_POINT ( 'NONE',  ( 6.461383593301071926, 1.630371061775518271, 1.090930979547571456 ) ) ;
#96908=CARTESIAN_POINT ( 'NONE',  ( 2.289831844592318255, -1.277571413231039399, -1.488851726829776068 ) ) ;
#96912=CARTESIAN_POINT ( 'NONE',  ( 1.341172884435502866, -1.819006327537198153, -1.083427034744638862 ) ) ;
#96916=CARTESIAN_POINT ( 'NONE',  ( 0.6734667703603390843, -1.024904740748554532, 1.529287851792550335 ) ) ;
#96918=CARTESIAN_POINT ( 'NONE',  ( 3.959984535978885667, -0.6353779353734061441, 2.075986281735443750 ) ) ;
#96920=CARTESIAN_POINT ( 'NONE',  ( 1.600013431492643745, 1.466117565985028515, 1.532352819790145482 ) ) ;
#96925=CARTESIAN_POINT ( 'NONE',  ( 2.934896792925650644, 0.2487164785463981398, 2.045624280402899231 ) ) ;
#96927=CARTESIAN_POINT ( 'NONE',  ( 0.5031362391596030381, -1.832460416942282011, 0.1798594046882526221 ) ) ;
#96929=CARTESIAN_POINT ( 'NONE',  ( -0.02244404828160087226, 6.946777552644228138, -2.784171975256703124 ) ) ;
#96932=CARTESIAN_POINT ( 'NONE',  ( 1.265308524177723326, -2.045349560253268084, -0.9672931750909097293 ) ) ;
#96934=CARTESIAN_POINT ( 'NONE',  ( 2.513665319321151337, -0.5648568745635518251, 1.721363734954905356 ) ) ;
#96935=CARTESIAN_POINT ( 'NONE',  ( 1.780357001937494799, -0.5149467098792412934, -1.845104466984174962 ) ) ;
#96936=CARTESIAN_POINT ( 'NONE',  ( 3.191909353267761151, -1.388477207968623839, -1.535938721777901472 ) ) ;
#96938=CARTESIAN_POINT ( 'NONE',  ( 1.287891803077842345, -0.8884654817012342942, 1.759997859036799284 ) ) ;
#96939=CARTESIAN_POINT ( 'NONE',  ( 0.4988883441144418840, 1.603466095971857852, -1.067369714357151222 ) ) ;
#96940=CARTESIAN_POINT ( 'NONE',  ( 3.151090109352538082, -1.528452604574185525, -1.078222621661927061 ) ) ;
#96942=CARTESIAN_POINT ( 'NONE',  ( 0.8214423835279326402, 2.134246884609458661, 0.8782244701446385582 ) ) ;
#96944=CARTESIAN_POINT ( 'NONE',  ( 2.242426168690789368, -1.824373289281261634, -0.3667376154973446267 ) ) ;
#96946=CARTESIAN_POINT ( 'NONE',  ( 5.424308963177657539, 1.013736099364664911, 1.796294033555500658 ) ) ;
#96951=CARTESIAN_POINT ( 'NONE',  ( 6.317421145955757211, -0.2613792861649695265, 2.089613723330654427 ) ) ;
#96953=CARTESIAN_POINT ( 'NONE',  ( 5.729794944320468097, -1.366427417996706417, -1.674954217032841974 ) ) ;
#96954=CARTESIAN_POINT ( 'NONE',  ( 1.188719773494644860, 1.394467456127197025, 1.202481090285527632 ) ) ;
#96955=CARTESIAN_POINT ( 'NONE',  ( 5.215492487644303843, 1.652332223238074604, 1.161132580238199541 ) ) ;
#96959=CARTESIAN_POINT ( 'NONE',  ( 6.925078400183553029, 7.053346220238264408, 2.353806654540433030 ) ) ;
#96962=CARTESIAN_POINT ( 'NONE',  ( 4.874232570624013050, -2.001857581374043349, -0.2420344392276354561 ) ) ;
#96967=CARTESIAN_POINT ( 'NONE',  ( 6.174726448494309849, -2.051094451480539149, -0.6828207641706719455 ) ) ;
#96972=CARTESIAN_POINT ( 'NONE',  ( 5.220327442464319567, 1.987051044970666647, 0.3419161450798278157 ) ) ;
#96974=CARTESIAN_POINT ( 'NONE',  ( 1.857592325351750118, 1.720440678145126467, -0.1246472719800949674 ) ) ;
#96979=CARTESIAN_POINT ( 'NONE',  ( 6.802024559211160337, -1.870114703409443857, 0.04643648283486622591 ) ) ;
#96980=CARTESIAN_POINT ( 'NONE',  ( 0.8209481077818219230, 1.523044454047136176, -1.316462280350006342 ) ) ;
#96982=CARTESIAN_POINT ( 'NONE',  ( 3.382038520680182181, 1.398480293485371284, 1.707083182650385389 ) ) ;
#96983=CARTESIAN_POINT ( 'NONE',  ( 5.559503684912662003, 1.770657277210012204, 1.256059096652543783 ) ) ;
#96987=CARTESIAN_POINT ( 'NONE',  ( 2.666775373343560407, 0.7166976873529752323, 1.995817185486338019 ) ) ;
#96988=CARTESIAN_POINT ( 'NONE',  ( 1.933220473845993492, -1.621196910160098925, -1.198842755339262212 ) ) ;
#96989=CARTESIAN_POINT ( 'NONE',  ( 2.162115752888054576, 1.811270999727595976, 0.04120172278379052866 ) ) ;
#96995=CARTESIAN_POINT ( 'NONE',  ( 0.8486862992652006721, -1.733348825135153648, -0.8160025691017428473 ) ) ;
#97002=CARTESIAN_POINT ( 'NONE',  ( 5.489210439962995736, 1.908424935776025455, -1.015307555102950010 ) ) ;
#97005=CARTESIAN_POINT ( 'NONE',  ( 2.092179824929023102, 1.308410154019133076, 1.668721082780571408 ) ) ;
#97008=CARTESIAN_POINT ( 'NONE',  ( 3.479716606839049930, 1.247861786229450543, 1.526166498753677825 ) ) ;
#97009=CARTESIAN_POINT ( 'NONE',  ( 5.203337695038355193, 1.683698669361912259, -0.9069238330124268499 ) ) ;
#97012=CARTESIAN_POINT ( 'NONE',  ( 0.6431357727456864515, -0.2518013131528433757, -2.054909676291870380 ) ) ;
#97013=CARTESIAN_POINT ( 'NONE',  ( 1.904143259493733309, 1.439083257011425587, -1.304092337848123062 ) ) ;
#97017=CARTESIAN_POINT ( 'NONE',  ( 2.414113337891873101, 1.364997783657854846, -1.583610807417460631 ) ) ;
#97020=CARTESIAN_POINT ( 'NONE',  ( 6.481121912432155519, -1.750430003815309998, -0.7703581994758443852 ) ) ;
#97022=CARTESIAN_POINT ( 'NONE',  ( 4.477303810882872881, 0.001702072213635372200, -2.207063162522747479 ) ) ;
#97023=CARTESIAN_POINT ( 'NONE',  ( 3.206306947805489305, -2.204311952916749640, 0.1065802224688369715 ) ) ;
#97026=CARTESIAN_POINT ( 'NONE',  ( 1.488763880571321030, -1.816176428755595706, -0.5988469716494760897 ) ) ;
#97030=CARTESIAN_POINT ( 'NONE',  ( 4.352052382902608763, -0.7952921280917917279, 1.911720769834826195 ) ) ;
#97032=CARTESIAN_POINT ( 'NONE',  ( 2.272554088390315030, -1.330374092946192688, 1.703740541667747133 ) ) ;
#97033=CARTESIAN_POINT ( 'NONE',  ( 4.142245973918059043, 0.5854081421233224836, 2.111838497463234710 ) ) ;
#97041=CARTESIAN_POINT ( 'NONE',  ( -0.08726289061519039436, -1.242903867559573161, -1.588418431006669351 ) ) ;
#97043=CARTESIAN_POINT ( 'NONE',  ( 4.575093719746353038, 1.890691655113156289, 0.8438020912069632562 ) ) ;
#97044=CARTESIAN_POINT ( 'NONE',  ( 3.246621724073412096, 0.4685524532376301177, 1.868535087029847386 ) ) ;
#97045=CARTESIAN_POINT ( 'NONE',  ( 6.081681791882147969, -0.7128978460711818954, 1.993742607474026984 ) ) ;
#97048=CARTESIAN_POINT ( 'NONE',  ( 3.994935505748583360, 0.2844874371618256736, 1.948636269439333546 ) ) ;
#97049=CARTESIAN_POINT ( 'NONE',  ( 5.525394443818422374, -1.450416979558573072, -1.775029086184358507 ) ) ;
#97050=CARTESIAN_POINT ( 'NONE',  ( 4.213378774425760476, -0.3099129147984269195, 1.799030153321119263 ) ) ;
#97056=CARTESIAN_POINT ( 'NONE',  ( 1.751249726499287673, 1.836263021919124050, -0.1365115386888632321 ) ) ;
#97057=CARTESIAN_POINT ( 'NONE',  ( 5.361592829351686795, -1.589796019859390563, -1.235070861824426824 ) ) ;
#97058=CARTESIAN_POINT ( 'NONE',  ( 5.818996626390088522, 1.136386364665368687, -1.998068361519554248 ) ) ;
#97059=CARTESIAN_POINT ( 'NONE',  ( 5.541838416980684023, 1.314774629379747539, 1.456173869884537675 ) ) ;
#97064=CARTESIAN_POINT ( 'NONE',  ( 1.944979630195432074, -1.681012947115037015, -1.242954243213564292 ) ) ;
#97065=CARTESIAN_POINT ( 'NONE',  ( 0.2681426532152464959, -1.225442487749365483, 1.413462724991432218 ) ) ;
#97067=CARTESIAN_POINT ( 'NONE',  ( 5.525317926099265087, -1.233401178653690033, -1.499961942869533438 ) ) ;
#97069=CARTESIAN_POINT ( 'NONE',  ( 1.241335265265028687, 1.738410175110545852, 0.08621907427421551806 ) ) ;
#97072=CARTESIAN_POINT ( 'NONE',  ( 1.330204427372463138, 1.661418051098985327, 0.4633224975721556005 ) ) ;
#97073=CARTESIAN_POINT ( 'NONE',  ( 1.611130907606239004, -0.2639259086049255965, 2.175532687872412829 ) ) ;
#97074=CARTESIAN_POINT ( 'NONE',  ( 4.108205984530819421, -2.201057848371779535, 0.1611738814469021175 ) ) ;
#97076=CARTESIAN_POINT ( 'NONE',  ( 1.745237678848761576, -0.3157848129633227807, -2.147843386395100751 ) ) ;
#97078=CARTESIAN_POINT ( 'NONE',  ( 2.448581487809509571, -1.456371601587917120, 1.537162028231451538 ) ) ;
#97079=CARTESIAN_POINT ( 'NONE',  ( 6.639320575229252341, 0.005161017367553630275, 1.896863882003448021 ) ) ;
#97082=CARTESIAN_POINT ( 'NONE',  ( 2.964700083287651999, -2.118976988643240578, -0.8750470330559836363 ) ) ;
#97086=CARTESIAN_POINT ( 'NONE',  ( 5.356174596383207032, 0.9017655805138939940, -2.030186355573161627 ) ) ;
#97092=CARTESIAN_POINT ( 'NONE',  ( 2.988907892087853568, -2.013985899409028946, 0.1017507309580278629 ) ) ;
#97094=CARTESIAN_POINT ( 'NONE',  ( 1.920832408274443903, -1.461550516301242775, 1.455605961035913776 ) ) ;
#97101=CARTESIAN_POINT ( 'NONE',  ( 4.980524279605372584, -0.2661484459187679064, -2.175167798947100994 ) ) ;
#97102=CARTESIAN_POINT ( 'NONE',  ( 2.285779929129946098, 1.617817622347239803, -1.203354541732377658 ) ) ;
#97103=CARTESIAN_POINT ( 'NONE',  ( 2.735704033801298785, 1.827604811068459956, 0.2230458208379028362 ) ) ;
#97105=CARTESIAN_POINT ( 'NONE',  ( 4.928627555176230857, 1.747287423663802075, 0.5288322122747670662 ) ) ;
#97106=CARTESIAN_POINT ( 'NONE',  ( 5.977185442992979603, -2.006959616289708315, -0.1948445219252663840 ) ) ;
#97108=CARTESIAN_POINT ( 'NONE',  ( 5.700151306344448443, -2.262689076517818254, -0.006432940626173094985 ) ) ;
#97110=CARTESIAN_POINT ( 'NONE',  ( 1.032015147355441309, -1.337601665653989302, -1.626754097558680057 ) ) ;
#97112=CARTESIAN_POINT ( 'NONE',  ( 4.264170421968140445, -2.065031762457261610, 0.1491743435546449281 ) ) ;
#97122=CARTESIAN_POINT ( 'NONE',  ( 2.689914112924804090, 2.107969469017998421, -0.7009301692152307695 ) ) ;
#97127=CARTESIAN_POINT ( 'NONE',  ( 3.297265573180406584, -1.731424309613574852, 0.9225008839797432802 ) ) ;
#97133=CARTESIAN_POINT ( 'NONE',  ( 2.514065211524143084, -0.6609878990531635745, 2.015050547854141172 ) ) ;
#97135=CARTESIAN_POINT ( 'NONE',  ( 3.854492016355787420, 0.7758605394001509836, 2.017853709245204463 ) ) ;
#97136=CARTESIAN_POINT ( 'NONE',  ( 3.122423488780329048, 0.04808623196613135559, 1.840796284283818363 ) ) ;
#97139=CARTESIAN_POINT ( 'NONE',  ( 5.894438200647534210, 1.418812651433436933, -1.007543873543685020 ) ) ;
#97140=CARTESIAN_POINT ( 'NONE',  ( 6.727182134110231360, 2.105158487175392334, 2.022197281440795358 ) ) ;
#97144=CARTESIAN_POINT ( 'NONE',  ( 2.571340117545738657, 0.1069729528509130723, -2.159185227005658181 ) ) ;
#97145=CARTESIAN_POINT ( 'NONE',  ( 4.059922587279920947, 1.704677108394496043, -1.076152822228809480 ) ) ;
#97147=CARTESIAN_POINT ( 'NONE',  ( 2.571340117545738657, 0.1069729528509130723, -2.159185227005658181 ) ) ;
#97148=CARTESIAN_POINT ( 'NONE',  ( 2.811746400649973499, -1.950408978035414354, 0.2857507918755904930 ) ) ;
#97149=CARTESIAN_POINT ( 'NONE',  ( 6.509000000000015440, 0.001920477310516938412, 2.100274754360692331 ) ) ;
#97150=CARTESIAN_POINT ( 'NONE',  ( 4.405766152992893758, -0.8336290453338083273, -1.754189941349618920 ) ) ;
#97159=CARTESIAN_POINT ( 'NONE',  ( 1.624349867039249329, -1.226448341774049267, -1.834376716147153363 ) ) ;
#97161=CARTESIAN_POINT ( 'NONE',  ( 5.453941704850034711, -0.7095916301838971485, 1.829088932523432964 ) ) ;
#97165=CARTESIAN_POINT ( 'NONE',  ( 0.07499057489260964326, 4.092262291754148684, -2.510514182268712702 ) ) ;
#97166=CARTESIAN_POINT ( 'NONE',  ( 4.804558796598876746, 1.603369264058150279, 0.9048477820690554729 ) ) ;
#97171=CARTESIAN_POINT ( 'NONE',  ( 5.572555445586866441, 0.8612648569810870125, 1.938019255899057658 ) ) ;
#97175=CARTESIAN_POINT ( 'NONE',  ( 6.309851081105539272, -2.045767358615140807, 0.2475669877257078710 ) ) ;
#97177=CARTESIAN_POINT ( 'NONE',  ( 1.873285555135986824, -0.2318667498520594894, 1.846494694648516788 ) ) ;
#97178=CARTESIAN_POINT ( 'NONE',  ( 3.175182228840720988, 1.170341537027960843, 1.421418621496411516 ) ) ;
#97183=CARTESIAN_POINT ( 'NONE',  ( 3.774219598512587037, 1.225428716765289749, 1.835190637982798023 ) ) ;
#97184=CARTESIAN_POINT ( 'NONE',  ( 5.466221857368295467, 1.108383815247836690, 1.972225493889906867 ) ) ;
#97187=CARTESIAN_POINT ( 'NONE',  ( 6.187769672300552415, 1.730736780639136496, -0.5351268960485565662 ) ) ;
#97188=CARTESIAN_POINT ( 'NONE',  ( 5.630082600720735186, 1.913861949906026538, 0.08686293782892740012 ) ) ;
#97190=CARTESIAN_POINT ( 'NONE',  ( 6.719622092096638966, -1.813896567892055112, 0.4569536213836836169 ) ) ;
#97192=CARTESIAN_POINT ( 'NONE',  ( 5.670303652858919463, -0.8369403475225531963, -1.662290214344812833 ) ) ;
#97194=CARTESIAN_POINT ( 'NONE',  ( 6.508682224664005922, 1.308065493886721775, -1.192407281889706905 ) ) ;
#97195=CARTESIAN_POINT ( 'NONE',  ( 1.464077725791514517, -1.074659653367866952, 1.706114136832518779 ) ) ;
#97197=CARTESIAN_POINT ( 'NONE',  ( 2.508543264270487683, -0.8067718606631252287, -1.945620686511064790 ) ) ;
#97202=CARTESIAN_POINT ( 'NONE',  ( 2.777608160125254688, 0.2920557517631214295, -1.998411540393054020 ) ) ;
#97206=CARTESIAN_POINT ( 'NONE',  ( 2.987745815084281276, 1.526290923294726820, 1.530918043534036599 ) ) ;
#97207=CARTESIAN_POINT ( 'NONE',  ( 6.610000000000026077, 2.442988107647511509, 2.382821027452782570 ) ) ;
#97214=CARTESIAN_POINT ( 'NONE',  ( 2.208753784402537335, 1.959192758111829136, 0.9821998110004714899 ) ) ;
#97216=CARTESIAN_POINT ( 'NONE',  ( 2.255063695347800934, -1.748954272965432155, 1.435335380440343256 ) ) ;
#97223=CARTESIAN_POINT ( 'NONE',  ( 3.303702144000867591, -1.767878013958000150, 0.08340844992380143375 ) ) ;
#97224=CARTESIAN_POINT ( 'NONE',  ( 6.440462174652990868, 2.181831651002089423, 0.3301269925025315799 ) ) ;
#97227=CARTESIAN_POINT ( 'NONE',  ( 4.675407748274028386, 1.496063595514389721, 1.352143027241403450 ) ) ;
#97229=CARTESIAN_POINT ( 'NONE',  ( 3.397188523315307407, 1.473948685399184111, 1.151750840393983344 ) ) ;
#97230=CARTESIAN_POINT ( 'NONE',  ( 3.204029340230400091, 0.7494766052340908757, -1.929994576353490032 ) ) ;
#97235=( NAMED_UNIT ( * ) SI_UNIT ( $, .STERADIAN. ) SOLID_ANGLE_UNIT ( ) );
#97237=CARTESIAN_POINT ( 'NONE',  ( 1.318461241437279607, -0.6911404020932455650, -1.783297644634279200 ) ) ;
#97238=CARTESIAN_POINT ( 'NONE',  ( 3.086327779807009009, 1.092107249913790712, -1.629585102321646328 ) ) ;
#97239=CARTESIAN_POINT ( 'NONE',  ( 1.194685229111978497, -1.276845315561925931, -1.560263297373874813 ) ) ;
#97243=CARTESIAN_POINT ( 'NONE',  ( 6.503199639966785739, 1.637674054957323433, 1.097108698291071827 ) ) ;
#97245=CARTESIAN_POINT ( 'NONE',  ( 2.408449855729302591, -2.008082631278225616, -0.1440398445633188362 ) ) ;
#97247=CARTESIAN_POINT ( 'NONE',  ( 2.021262997689095897, -1.889599275135231071, 0.9552078933684378104 ) ) ;
#97249=CARTESIAN_POINT ( 'NONE',  ( 3.297389726143421740, -1.827171938055579536, 0.9735347560282039403 ) ) ;
#97251=CARTESIAN_POINT ( 'NONE',  ( 5.806606243248950250, 1.843357943042901459, 0.9862787698241348711 ) ) ;
#97253=CARTESIAN_POINT ( 'NONE',  ( 4.119992258926360229, -0.9384382104282267267, -1.565754920925747973 ) ) ;
#97258=CARTESIAN_POINT ( 'NONE',  ( 6.124089168553260798, -1.220954261165616783, -1.838047742986161026 ) ) ;
#97261=CARTESIAN_POINT ( 'NONE',  ( 5.408822929737922003, -0.4686924282312036061, -1.853821656156897646 ) ) ;
#97269=CARTESIAN_POINT ( 'NONE',  ( 0.6261898170028465938, 0.1349980957352381883, 1.836376839866371569 ) ) ;
#97273=CARTESIAN_POINT ( 'NONE',  ( 4.692568346783878575, -0.4079999995015987091, -1.825350503840660110 ) ) ;
#97280=CARTESIAN_POINT ( 'NONE',  ( 1.797640638355556320, -1.422838571669628127, -1.361938172677351400 ) ) ;
#97281=CARTESIAN_POINT ( 'NONE',  ( 2.126577575561945821, 0.4445254776237593242, 1.966640697269490312 ) ) ;
#97285=CARTESIAN_POINT ( 'NONE',  ( 3.029421956395737858, -1.472182739719897215, -1.623467934892895759 ) ) ;
#97294=CARTESIAN_POINT ( 'NONE',  ( 4.827609030688454261, 0.9420861819694618111, -1.581835861328761528 ) ) ;
#97295=CARTESIAN_POINT ( 'NONE',  ( 1.963540897105001459, -1.618223010570983611, -1.197281337589267247 ) ) ;
#97296=CARTESIAN_POINT ( 'NONE',  ( 2.812212034788389214, -1.912053501320301718, 1.275153900055803646 ) ) ;
#97298=CARTESIAN_POINT ( 'NONE',  ( 1.656853885927531689, 1.525116498273047405, -1.066097284832379755 ) ) ;
#97301=CARTESIAN_POINT ( 'NONE',  ( 5.607647405131535479, 1.452367144367059826, 1.244281684088064166 ) ) ;
#97304=CARTESIAN_POINT ( 'NONE',  ( 5.355056023315875713, 0.4066876561409601964, -2.050628154503638889 ) ) ;
#97305=CARTESIAN_POINT ( 'NONE',  ( 3.977312496258199825, 1.761605600429091201, -0.6297503393934977822 ) ) ;
#97307=CARTESIAN_POINT ( 'NONE',  ( 5.899929530298204661, -0.6689130865737795695, -1.715630562827724637 ) ) ;
#97311=CARTESIAN_POINT ( 'NONE',  ( 4.916472993244619616, 1.186103633638861288, -1.252587755385982771 ) ) ;
#97313=( BOUNDED_SURFACE ( )  B_SPLINE_SURFACE ( 3, 3, ( 
 ( #138412, #174129, #90736, #139487, #38766, #91810, #158920, #60339, #142702, #208711, #105946 ),
 ( #74468, #9461, #171970, #206586, #23561, #22485, #89669, #6235, #40916, #109173, #154653 ),
 ( #187137, #76591, #104847, #72307, #10516, #190331, #41992, #204433, #58215, #108100, #56086 ),
 ( #122244, #189277, #8386, #188202, #39839, #92874, #155720, #7305, #205515, #25702, #75533 ),
 ( #57147, #141644, #170893, #24629, #123313, #107022, #207653, #173046, #59274, #156799, #140573 ),
 ( #125430, #191395, #43060, #175186, #194606, #98200, #63549, #97140, #12648, #159985, #13716 ),
 ( #15836, #193547, #129705, #31065, #161052, #11587, #64614, #163194, #48388, #176245, #112368 ) ),
 .UNSPECIFIED., .T., .F., .T. ) 
 B_SPLINE_SURFACE_WITH_KNOTS ( ( 4, 3, 4 ),
 ( 4, 1, 1, 1, 1, 1, 1, 1, 4 ),
 ( 0.000000000000000000, 0.5000000000000000000, 1.000000000000000000 ),
 ( 0.000000000000000000, 0.2254101072112788262, 0.3970395454107691902, 0.5239558410346354389, 0.6152342776129972046, 0.6800502191696807808, 0.7279184599320936977, 0.7685697607527866015, 1.000000000000000000 ),
 .UNSPECIFIED. ) 
 GEOMETRIC_REPRESENTATION_ITEM ( )  RATIONAL_B_SPLINE_SURFACE ( (
 ( 1.000000000000000000, 1.000000000000000000, 1.000000000000000222, 1.000000000000000222, 0.9999999999999996669, 1.000000000000000222, 0.9999999999999994449, 1.000000000000000222, 0.9999999999999992228, 1.000000000000000000, 1.000000000000000000),
 ( 0.3333333333333333703, 0.3333333333333333703, 0.3333333333333334259, 0.3333333333333333703, 0.3333333333333333148, 0.3333333333333334814, 0.3333333333333332593, 0.3333333333333334259, 0.3333333333333330928, 0.3333333333333333703, 0.3333333333333333703),
 ( 0.3333333333333333703, 0.3333333333333333703, 0.3333333333333334259, 0.3333333333333333703, 0.3333333333333333148, 0.3333333333333334814, 0.3333333333333332593, 0.3333333333333334259, 0.3333333333333330928, 0.3333333333333333703, 0.3333333333333333703),
 ( 1.000000000000000000, 1.000000000000000000, 1.000000000000000222, 1.000000000000000222, 0.9999999999999996669, 1.000000000000000222, 0.9999999999999994449, 1.000000000000000222, 0.9999999999999992228, 1.000000000000000000, 1.000000000000000000),
 ( 0.3333333333333333703, 0.3333333333333333703, 0.3333333333333334259, 0.3333333333333333703, 0.3333333333333333148, 0.3333333333333334814, 0.3333333333333332593, 0.3333333333333334259, 0.3333333333333330928, 0.3333333333333333703, 0.3333333333333333703),
 ( 0.3333333333333333703, 0.3333333333333333703, 0.3333333333333334259, 0.3333333333333333703, 0.3333333333333333148, 0.3333333333333334814, 0.3333333333333332593, 0.3333333333333334259, 0.3333333333333330928, 0.3333333333333333703, 0.3333333333333333703),
 ( 1.000000000000000000, 1.000000000000000000, 1.000000000000000222, 1.000000000000000222, 0.9999999999999996669, 1.000000000000000222, 0.9999999999999994449, 1.000000000000000222, 0.9999999999999992228, 1.000000000000000000, 1.000000000000000000) ) ) 
 REPRESENTATION_ITEM ( '' )  SURFACE ( )  );
#97319=CARTESIAN_POINT ( 'NONE',  ( 4.223599041728074432, 0.2716450895321539383, -2.153977947863388476 ) ) ;
#97320=CARTESIAN_POINT ( 'NONE',  ( 3.809063337113669068, 1.566667275063510445, 0.9371452329686791316 ) ) ;
#97321=CARTESIAN_POINT ( 'NONE',  ( 0.9011314981347726683, -1.685442764318560771, 1.003610994683441948 ) ) ;
#97322=CARTESIAN_POINT ( 'NONE',  ( 5.471900407082693540, -0.9496530807377671080, 1.892462605218522720 ) ) ;
#97324=CARTESIAN_POINT ( 'NONE',  ( 6.409759596795807646, -1.076414324555999391, -2.023967322820482639 ) ) ;
#97328=CARTESIAN_POINT ( 'NONE',  ( 2.104293207771616991, -0.9040658786637757460, 1.918231223523607865 ) ) ;
#97331=CARTESIAN_POINT ( 'NONE',  ( 6.034065736706932803, 1.286768452391522377, 1.748546487445822750 ) ) ;
#97332=CARTESIAN_POINT ( 'NONE',  ( 6.883263157960364254, 2.038911835798001171, 2.358809022084580764 ) ) ;
#97334=CARTESIAN_POINT ( 'NONE',  ( 2.877807283724475251, 0.3237236903097116536, -2.197462771414046223 ) ) ;
#97336=CARTESIAN_POINT ( 'NONE',  ( -0.1394461523061351904, -0.009327122704730000241, -2.280146446826665230 ) ) ;
#97338=CARTESIAN_POINT ( 'NONE',  ( 5.594603800059450904, 2.031116569408123240, 0.3580809986778245024 ) ) ;
#97344=CARTESIAN_POINT ( 'NONE',  ( 0.2333540202161792088, 2.022347194651296753, -2.461825824937914575 ) ) ;
#97345=CARTESIAN_POINT ( 'NONE',  ( 5.548353751603532835, -1.447698842669535413, 1.137588655622793876 ) ) ;
#97348=CARTESIAN_POINT ( 'NONE',  ( 1.500562974171329333, 1.412943827846969702, -0.9888553570028703055 ) ) ;
#97349=CARTESIAN_POINT ( 'NONE',  ( 0.1105650446291406575, 1.931126588553159884, 0.5807481968119407867 ) ) ;
#97350=CARTESIAN_POINT ( 'NONE',  ( 1.495234749544295250, -2.280609600776092094, 0.2875172478875551163 ) ) ;
#97352=CARTESIAN_POINT ( 'NONE',  ( 1.915646641569005659, -0.2780824042511415017, 2.245213254143724413 ) ) ;
#97353=CARTESIAN_POINT ( 'NONE',  ( 4.143269384990833970, -1.832638288540566318, 1.037631460274644812 ) ) ;
#97355=CARTESIAN_POINT ( 'NONE',  ( 2.969704930451398717, 0.9433242808821461489, 1.497149023046380423 ) ) ;
#97361=CARTESIAN_POINT ( 'NONE',  ( 5.853820293109783357, -1.608621682386938589, -1.532244055152881312 ) ) ;
#97362=CARTESIAN_POINT ( 'NONE',  ( 3.134921595499224445, -1.932508288125428741, 1.033376004005027715 ) ) ;
#97365=CARTESIAN_POINT ( 'NONE',  ( 6.463548717370299457, -1.702720583769131490, -1.263627255760652046 ) ) ;
#97369=CARTESIAN_POINT ( 'NONE',  ( 6.170199167347634628, 2.114832956739281400, -0.1575216572810705096 ) ) ;
#97371=VERTEX_POINT ( 'NONE', #193122 ) ;
#97375=CARTESIAN_POINT ( 'NONE',  ( 5.899929530298204661, -0.6689130865737795695, -1.715630562827724637 ) ) ;
#97379=CARTESIAN_POINT ( 'NONE',  ( 2.225747907193951214, 1.688420964825324555, 0.4218146122960535482 ) ) ;
#97381=CARTESIAN_POINT ( 'NONE',  ( 0.6605093422152423788, -0.6574743052488278838, -1.848563176889833626 ) ) ;
#97384=CARTESIAN_POINT ( 'NONE',  ( 6.350466702034289312, 0.6732396885240909956, 2.054270918568662729 ) ) ;
#97388=CARTESIAN_POINT ( 'NONE',  ( 6.315313271410192719, -0.2696487299426887363, 2.144762774094311375 ) ) ;
#97392=CARTESIAN_POINT ( 'NONE',  ( 5.923112194766430250, -0.05102361969991364710, 1.970867320657720301 ) ) ;
#97393=CARTESIAN_POINT ( 'NONE',  ( 5.149590220011600827, -0.2133714078210862675, -1.720544222028724146 ) ) ;
#97395=CARTESIAN_POINT ( 'NONE',  ( 2.437293137456029157, -1.626093413141915134, -1.469474007205706645 ) ) ;
#97396=CARTESIAN_POINT ( 'NONE',  ( 3.065757340968386035, 0.3400709678853690021, -2.282286004074239649 ) ) ;
#97397=CARTESIAN_POINT ( 'NONE',  ( 6.415316853601439995, -0.2566941480561866773, 2.044681889290477894 ) ) ;
#97398=CARTESIAN_POINT ( 'NONE',  ( 1.411946100005515126, 1.304364503314077162, -1.438846909250802053 ) ) ;
#97403=CARTESIAN_POINT ( 'NONE',  ( 4.096021571020786567, 1.387573888390711385, 1.603661410755026440 ) ) ;
#97405=CARTESIAN_POINT ( 'NONE',  ( 1.828750219146151323, 0.7691198443132395424, -1.864169014999479623 ) ) ;
#97407=CARTESIAN_POINT ( 'NONE',  ( 4.577303723630254062, 0.003709267837189236805, -2.206952907291927168 ) ) ;
#97416=CARTESIAN_POINT ( 'NONE',  ( 4.838775396685393915, 0.3501730741383273782, 2.030750449888196751 ) ) ;
#97418=FACE_OUTER_BOUND ( 'NONE', #45062, .T. ) ;
#97420=CARTESIAN_POINT ( 'NONE',  ( 3.229170203573806130, 1.826861024573895653, 0.8614713780644381869 ) ) ;
#97425=CARTESIAN_POINT ( 'NONE',  ( 3.397389285588784169, 1.623555618760182062, 1.269252347208242870 ) ) ;
#97428=CARTESIAN_POINT ( 'NONE',  ( -0.2408018239684330541, 4.084923768815020395, -2.655285172934387372 ) ) ;
#97429=CARTESIAN_POINT ( 'NONE',  ( 1.095364067855080448, -1.841320589428995236, -0.001981933617903330457 ) ) ;
#97430=CARTESIAN_POINT ( 'NONE',  ( -0.01646294620048001714, -0.1635519927996042511, -2.271437254364586877 ) ) ;
#97432=CARTESIAN_POINT ( 'NONE',  ( 2.724079341238437646, -1.242159841233332562, -1.768869243570107885 ) ) ;
#97434=CARTESIAN_POINT ( 'NONE',  ( 1.411342602523330214, -1.897109289313268166, 0.6839406069230756779 ) ) ;
#97436=CARTESIAN_POINT ( 'NONE',  ( 2.777091360721035240, -2.273647235919952880, 0.3355521655935486125 ) ) ;
#97439=CARTESIAN_POINT ( 'NONE',  ( 4.311372413323046437, -0.3381597629931332172, 1.942102657548309796 ) ) ;
#97440=CARTESIAN_POINT ( 'NONE',  ( 4.997279897388729353, -0.2910847460899004258, 1.995267753224789997 ) ) ;
#97444=CARTESIAN_POINT ( 'NONE',  ( 6.129533150132032482, -1.983608965904083421, 0.7080540597134558078 ) ) ;
#97445=CARTESIAN_POINT ( 'NONE',  ( 6.877413708759195998, -0.1538780216673047430, 2.036608477593480959 ) ) ;
#97449=CARTESIAN_POINT ( 'NONE',  ( 4.399269495383588691, 1.582840427583383613, 1.175083439883710890 ) ) ;
#97450=CARTESIAN_POINT ( 'NONE',  ( 5.888927314555610693, -1.919185580196127283, -0.6297945592430991280 ) ) ;
#97452=CARTESIAN_POINT ( 'NONE',  ( 4.371882800840491967, 2.239072524489620353, -0.5581132647194796403 ) ) ;
#97453=CARTESIAN_POINT ( 'NONE',  ( 1.815356060102671698, -1.766853000457936806, -1.063981086615989113 ) ) ;
#97460=CARTESIAN_POINT ( 'NONE',  ( 4.334556721604589491, -1.253389318223859350, 1.772677672673736771 ) ) ;
#97462=CARTESIAN_POINT ( 'NONE',  ( 3.104851637799400876, -0.3563606998662186554, 1.806257425991746546 ) ) ;
#97464=CARTESIAN_POINT ( 'NONE',  ( 5.583573808894983337, -0.9862700065477579825, 1.957137920222583372 ) ) ;
#97466=CARTESIAN_POINT ( 'NONE',  ( 6.491137613139088991, 1.972399245366265985, -1.108330356262598126 ) ) ;
#97471=CARTESIAN_POINT ( 'NONE',  ( 6.819637456808122167, -1.715783256332433115, 0.4333192982870024967 ) ) ;
#97474=CARTESIAN_POINT ( 'NONE',  ( 3.967443207080887380, -1.674941000623398457, -1.116458483097344301 ) ) ;
#97476=CARTESIAN_POINT ( 'NONE',  ( 2.485502531088045419, 1.925919180164997746, -0.8524081271456557252 ) ) ;
#97477=CARTESIAN_POINT ( 'NONE',  ( 2.284663151613754550, 1.537047112958013440, -1.143011353438025957 ) ) ;
#97479=CARTESIAN_POINT ( 'NONE',  ( 3.068762047175084717, 1.428394590129605346, -1.356294421569247177 ) ) ;
#97480=CARTESIAN_POINT ( 'NONE',  ( 1.815107966846595255, -0.2319292346777863389, 1.856160199827073587 ) ) ;
#97481=CARTESIAN_POINT ( 'NONE',  ( 1.064813361795993618, 1.487921858168140377, -1.278797858372302088 ) ) ;
#97482=CARTESIAN_POINT ( 'NONE',  ( 4.090264520950432470, -1.706510830129988499, -0.2501320830878352997 ) ) ;
#97483=CARTESIAN_POINT ( 'NONE',  ( 0.5449873876890098945, 0.1430962203496731200, 1.907122450762772647 ) ) ;
#97485=CARTESIAN_POINT ( 'NONE',  ( 1.295869073816724226, 1.673045085319382119, 1.439284050222865652 ) ) ;
#97489=CARTESIAN_POINT ( 'NONE',  ( 6.561405567229332547, 0.3174558530528899247, -1.843364171016811603 ) ) ;
#97493=CARTESIAN_POINT ( 'NONE',  ( 6.385608392048681026, -1.951384585020640383, 0.6918703269920487564 ) ) ;
#97494=CARTESIAN_POINT ( 'NONE',  ( 1.223191768902037957, -1.870915810643185795, -0.8869332102946840823 ) ) ;
#97499=CARTESIAN_POINT ( 'NONE',  ( 5.865915527372128402, 0.6157079936559420874, -2.029145397309819021 ) ) ;
#97505=CARTESIAN_POINT ( 'NONE',  ( 6.496542546517183325, 1.940334402339534581, 0.2891159199209930031 ) ) ;
#97507=CARTESIAN_POINT ( 'NONE',  ( 4.112657547701242144, 0.6818919214185631406, -1.897407125352356339 ) ) ;
#97508=CARTESIAN_POINT ( 'NONE',  ( 3.714002460163209562, 1.020071527678518164, -1.621341143276352703 ) ) ;
#97510=CARTESIAN_POINT ( 'NONE',  ( 1.365048776756357940, 0.1565470504056795942, -2.186014887712848243 ) ) ;
#97512=CARTESIAN_POINT ( 'NONE',  ( 0.1333692844072802142, 2.017199222642913625, -2.468757726274827036 ) ) ;
#97513=CARTESIAN_POINT ( 'NONE',  ( 3.215925951850879816, -0.9189154559356220719, -1.629173103855706906 ) ) ;
#97518=CARTESIAN_POINT ( 'NONE',  ( 5.202788454032899246, 1.956619031766251737, 0.8093448757829673212 ) ) ;
#97520=CARTESIAN_POINT ( 'NONE',  ( 2.489882245090881963, -2.085347646507927699, -0.1508444384941027561 ) ) ;
#97522=CARTESIAN_POINT ( 'NONE',  ( 1.324769809204975557, -0.04781147349866912699, 1.724288685672677568 ) ) ;
#97533=CARTESIAN_POINT ( 'NONE',  ( 2.121461778293322276, -0.3959642608444019496, 1.767488790605805438 ) ) ;
#97537=CARTESIAN_POINT ( 'NONE',  ( 6.639320575229278099, 1.279659970127836388, 2.012538313910294807 ) ) ;
#97541=CARTESIAN_POINT ( 'NONE',  ( 3.174093412877276865, -0.9148440431442562693, -1.620569831483926082 ) ) ;
#97542=CARTESIAN_POINT ( 'NONE',  ( 0.6849900193761117029, 1.566649212177973149, 1.102054418794357948 ) ) ;
#97543=CARTESIAN_POINT ( 'NONE',  ( 6.528350403681292491, 1.108413491673976736, -1.575378176345716419 ) ) ;
#97551=CARTESIAN_POINT ( 'NONE',  ( 5.084792200464717915, 1.883391756629303471, 0.5756752826196751549 ) ) ;
#97552=CARTESIAN_POINT ( 'NONE',  ( 1.489100733002651333, -2.014586327357254181, -0.6619970261998938676 ) ) ;
#97556=CARTESIAN_POINT ( 'NONE',  ( 6.210891007176935652, -0.2719346519345893776, 2.174439262769362280 ) ) ;
#97558=CARTESIAN_POINT ( 'NONE',  ( 4.682597122082689189, -1.868462817326870473, -0.4683620393717678465 ) ) ;
#97561=CARTESIAN_POINT ( 'NONE',  ( 0.6630615684519860498, -1.595754342771567025, 1.524677653706180802 ) ) ;
#97564=CARTESIAN_POINT ( 'NONE',  ( 0.2461629937395051204, 0.9812432698282257393, -1.641294572782559413 ) ) ;
#97568=CARTESIAN_POINT ( 'NONE',  ( 6.350452388456855779, -1.959648489363738699, -0.1964464578135850514 ) ) ;
#97569=CARTESIAN_POINT ( 'NONE',  ( 1.364679817366498904, 0.1413127912619481230, -1.936958241114185020 ) ) ;
#97570=CARTESIAN_POINT ( 'NONE',  ( 6.573571087534610058, 1.710132712828818402, -1.535791079811721360 ) ) ;
#97572=CARTESIAN_POINT ( 'NONE',  ( 5.295690652966449363, -1.314428334581790203, -1.317609258728233756 ) ) ;
#97577=CARTESIAN_POINT ( 'NONE',  ( 1.118978350340808614, -0.04878210919301298465, 2.191179638975069732 ) ) ;
#97581=CARTESIAN_POINT ( 'NONE',  ( 1.646812808029130215, -1.543121136568927243, 0.9753659028155501343 ) ) ;
#97587=CARTESIAN_POINT ( 'NONE',  ( 0.1000542341482368452, -1.926035175483146400, -0.04890095678477742597 ) ) ;
#97588=CARTESIAN_POINT ( 'NONE',  ( 4.241029431094700541, -0.1880360549168894613, -1.952691919460777026 ) ) ;
#97591=CARTESIAN_POINT ( 'NONE',  ( 3.843468145482428877, 0.7371271433744167600, -2.064019554291535830 ) ) ;
#97593=CARTESIAN_POINT ( 'NONE',  ( 3.643477671580112709, 1.873648065284461817, -0.8808079623299628347 ) ) ;
#97597=CARTESIAN_POINT ( 'NONE',  ( 4.184446765594143081, 1.846410498051667348, 1.369081834291352218 ) ) ;
#97604=CARTESIAN_POINT ( 'NONE',  ( 3.468632250064273670, 0.04687378517908299957, -1.941542025766171298 ) ) ;
#97608=CARTESIAN_POINT ( 'NONE',  ( 4.377155534175989793, -1.710687068321177007, -0.8549628122409487219 ) ) ;
#97610=CARTESIAN_POINT ( 'NONE',  ( 5.086778385480665854, -0.2138867007538784171, -1.711364050844576434 ) ) ;
#97611=CARTESIAN_POINT ( 'NONE',  ( 4.909388789075159742, -1.913262893431907141, 0.6371506334161003426 ) ) ;
#97612=CARTESIAN_POINT ( 'NONE',  ( 4.957821946367388932, -2.163970343481158132, -0.7757635736431248707 ) ) ;
#97614=CARTESIAN_POINT ( 'NONE',  ( 1.014635385311330795, -0.9952708415592588231, -1.969785480804244315 ) ) ;
#97617=CARTESIAN_POINT ( 'NONE',  ( 6.063686852112752490, 1.743171776219472280, -0.3043750889455443254 ) ) ;
#97619=CARTESIAN_POINT ( 'NONE',  ( 1.816774867096879964, 2.139948438195220071, 0.8220829075690959664 ) ) ;
#97620=CARTESIAN_POINT ( 'NONE',  ( 0.9018503542332901857, 1.320273433284512521, -1.133937880871397796 ) ) ;
#97622=CARTESIAN_POINT ( 'NONE',  ( 1.229404279783296694, -1.564619330878062931, -0.7474530596254543857 ) ) ;
#97625=CARTESIAN_POINT ( 'NONE',  ( 0.9069515603133030401, 0.6301693757862131262, 2.077734764916533639 ) ) ;
#97626=CARTESIAN_POINT ( 'NONE',  ( 2.132046339962359038, 2.016188815772378629, 0.04465230659478347519 ) ) ;
#97627=AXIS2_PLACEMENT_3D ( 'NONE', #54194, #87758, #199351 ) ;
#97629=CARTESIAN_POINT ( 'NONE',  ( 5.566998737003931552, -1.742544991934717125, -0.8218319283359241112 ) ) ;
#97631=CARTESIAN_POINT ( 'NONE',  ( 2.760263405638745393, 0.7954514732361592788, -2.074294698012415505 ) ) ;
#97632=VERTEX_POINT ( 'NONE', #47979 ) ;
#97638=CARTESIAN_POINT ( 'NONE',  ( 5.794438198198100132, 1.417746085458403638, -1.009241466377588603 ) ) ;
#97639=CARTESIAN_POINT ( 'NONE',  ( 3.051168888765115828, 1.684027830550902882, -1.006202029777767848 ) ) ;
#97643=CARTESIAN_POINT ( 'NONE',  ( 4.815850035042070765, -2.220064692501269477, 0.4349022163744782343 ) ) ;
#97644=CARTESIAN_POINT ( 'NONE',  ( 1.311062339077714078, -1.627386490012251663, 1.267307609633941956 ) ) ;
#97646=CARTESIAN_POINT ( 'NONE',  ( 1.956323303678444425, 2.256377666735286169, -0.1672192238599319314 ) ) ;
#97649=CARTESIAN_POINT ( 'NONE',  ( 2.002991962376502233, 1.552455721610061179, 1.043161660468715279 ) ) ;
#97650=CARTESIAN_POINT ( 'NONE',  ( 1.476802972400652170, -1.725769044224190196, -0.1698483453264828802 ) ) ;
#97651=CARTESIAN_POINT ( 'NONE',  ( 5.864808805604324604, 0.1626094438406736342, -2.185560445749204828 ) ) ;
#97652=CARTESIAN_POINT ( 'NONE',  ( 6.756845507909216231, -1.789895876690169585, 1.456048205946461005 ) ) ;
#97653=CARTESIAN_POINT ( 'NONE',  ( 4.153314892778156242, -1.795761387672462961, -1.203114871582221079 ) ) ;
#97654=CARTESIAN_POINT ( 'NONE',  ( 4.663973314478016441, -1.267186161278991419, 1.471619509450792229 ) ) ;
#97656=CARTESIAN_POINT ( 'NONE',  ( 6.661405586796749212, 0.3194099797865917467, -1.842918054787326065 ) ) ;
#97657=ORIENTED_EDGE ( 'NONE', *, *, #198303, .T. ) ;
#97658=CARTESIAN_POINT ( 'NONE',  ( 2.093750000000001332, -1.895863743164132531, -0.7852924748298759638 ) ) ;
#97663=CARTESIAN_POINT ( 'NONE',  ( 6.188124994278807023, 1.678003296889327034, 1.117835524071027598 ) ) ;
#97667=CARTESIAN_POINT ( 'NONE',  ( 3.334410585898534674, 1.781380905032422746, 0.3990451814587444024 ) ) ;
#97674=CARTESIAN_POINT ( 'NONE',  ( 0.2463608477257169804, 1.034524919618844407, -1.734561685378380957 ) ) ;
#97675=CARTESIAN_POINT ( 'NONE',  ( 1.137531110418067204, -0.04838959064331486287, 2.120096749846810624 ) ) ;
#97679=CARTESIAN_POINT ( 'NONE',  ( 6.368051766976638994, 1.057089778920755840, 1.768976859881221442 ) ) ;
#97680=CARTESIAN_POINT ( 'NONE',  ( 6.416638760586134360, -1.319225726833603840, -1.525046029381103452 ) ) ;
#97690=CARTESIAN_POINT ( 'NONE',  ( 5.694685421800770087, -1.276849089899323886, -1.560260200769040706 ) ) ;
#97691=CARTESIAN_POINT ( 'NONE',  ( 5.138538782746885580, -1.577291412575715812, 0.9494700402261007088 ) ) ;
#97693=CARTESIAN_POINT ( 'NONE',  ( 2.895503172138352177, 1.978892393434032559, -1.186989842046539234 ) ) ;
#97695=CARTESIAN_POINT ( 'NONE',  ( 6.046190728430958394, 2.158797838069245412, 0.1127497994189360364 ) ) ;
#97697=CARTESIAN_POINT ( 'NONE',  ( 1.065847985493496797, -1.230715344637549391, 1.502334450403658206 ) ) ;
#97700=CARTESIAN_POINT ( 'NONE',  ( 4.411641467711771014, 0.6073606466481770161, 2.216650271500276492 ) ) ;
#97704=CARTESIAN_POINT ( 'NONE',  ( 4.891396039733495016, 1.386484060982313249, 1.255958711209571810 ) ) ;
#97706=CARTESIAN_POINT ( 'NONE',  ( 1.810667312839256304, -0.5133170510521027907, -1.842115474350584980 ) ) ;
#97709=CARTESIAN_POINT ( 'NONE',  ( 2.983271218942393332, -0.1628219013674602478, -2.200934326520533446 ) ) ;
#97715=CARTESIAN_POINT ( 'NONE',  ( 1.967984887604894206, 1.010138386605848426, 1.692741100060575210 ) ) ;
#97716=CARTESIAN_POINT ( 'NONE',  ( 0.6754003219355340093, -2.174137316696134636, -0.7736760779102586083 ) ) ;
#97717=CARTESIAN_POINT ( 'NONE',  ( 1.680054527999317759, -1.087118939145682583, -1.632918184844594611 ) ) ;
#97718=CARTESIAN_POINT ( 'NONE',  ( 5.014538805069497229, 0.7844730879308317029, 1.907755517398136647 ) ) ;
#97725=CARTESIAN_POINT ( 'NONE',  ( 0.5675212215028536678, 1.888217155380923939, 1.071465276393630539 ) ) ;
#97727=CARTESIAN_POINT ( 'NONE',  ( 5.776868925826902590, 1.698781319366513998, -0.7106697882480541573 ) ) ;
#97730=CARTESIAN_POINT ( 'NONE',  ( 1.387741975113141013, -0.8460221195879283895, 1.668388151239764028 ) ) ;
#97731=CARTESIAN_POINT ( 'NONE',  ( 5.360679719606757487, -1.569739296358707570, 1.486333574453831297 ) ) ;
#97735=CARTESIAN_POINT ( 'NONE',  ( 0.07735805125222076917, 2.865712030211249761, -2.577262785371988496 ) ) ;
#97737=CARTESIAN_POINT ( 'NONE',  ( 1.875505643822904300, 0.3255412885708880433, -1.884197853084010443 ) ) ;
#97738=CARTESIAN_POINT ( 'NONE',  ( 2.834531330521594228, 0.2145198750864007742, 1.756709382032408451 ) ) ;
#97739=CARTESIAN_POINT ( 'NONE',  ( 0.7504700684401002242, 1.884043224930329385, 0.3264296256808990049 ) ) ;
#97741=CARTESIAN_POINT ( 'NONE',  ( 5.694928174475800908, 1.691819642972839599, 0.8984594094828317612 ) ) ;
#97742=CARTESIAN_POINT ( 'NONE',  ( 6.478958751509338754, 1.837172605331442332, 0.7103315708588151534 ) ) ;
#97744=CARTESIAN_POINT ( 'NONE',  ( 0.4926326669930108371, -1.172979896111199904, 1.766458537607276114 ) ) ;
#97746=CARTESIAN_POINT ( 'NONE',  ( 4.504681594071535677, 1.446009304718363087, -1.186774495104812699 ) ) ;
#97747=CARTESIAN_POINT ( 'NONE',  ( 1.013953575274041619, -0.8186894766500467657, -1.631917417583013341 ) ) ;
#97749=CARTESIAN_POINT ( 'NONE',  ( 4.196070124731249074, -0.8457972711899945928, 2.038567251995755836 ) ) ;
#97752=CARTESIAN_POINT ( 'NONE',  ( 2.400897505987206415, 0.4495084874868838232, 2.012960725780033489 ) ) ;
#97760=CARTESIAN_POINT ( 'NONE',  ( 3.719242722441223226, -1.824546119899137731, -0.9785211796824041519 ) ) ;
#97762=CARTESIAN_POINT ( 'NONE',  ( 1.282749207608822495, -2.108609127331688260, -0.4749100009155197699 ) ) ;
#97764=CARTESIAN_POINT ( 'NONE',  ( 1.840495965525708932, 1.161060486998789942, -1.652382956570614736 ) ) ;
#97770=CARTESIAN_POINT ( 'NONE',  ( 0.5500180045474002410, 0.9981291480291035745, 1.752136972055001518 ) ) ;
#97771=CARTESIAN_POINT ( 'NONE',  ( 4.546525781634036534, -1.759932548463913671, 1.305750774140898685 ) ) ;
#97773=CARTESIAN_POINT ( 'NONE',  ( 3.779479514802902340, 0.2291398179169491789, -1.898525689255560422 ) ) ;
#97777=CARTESIAN_POINT ( 'NONE',  ( 2.109000121467627498, 0.002830143620808495131, 2.016598147190066914 ) ) ;
#97779=CARTESIAN_POINT ( 'NONE',  ( 0.5215107003284430442, -2.174349661526672417, 0.7262685697029276355 ) ) ;
#97781=CARTESIAN_POINT ( 'NONE',  ( 4.032037319687285404, 0.9221689259152658913, -1.457338292308225869 ) ) ;
#97782=CARTESIAN_POINT ( 'NONE',  ( -0.1399997263889663501, 0.2375346743129815030, -2.034463206964792548 ) ) ;
#97785=CARTESIAN_POINT ( 'NONE',  ( 0.07536363704235825300, -0.001874865094115065866, -2.144269471569634433 ) ) ;
#97786=CARTESIAN_POINT ( 'NONE',  ( 0.4618902312403839194, -0.5555351291045197426, 1.994226918997483500 ) ) ;
#97789=CARTESIAN_POINT ( 'NONE',  ( 4.969312858920484466, -1.533218896822113653, -0.9643851972171797460 ) ) ;
#97794=CARTESIAN_POINT ( 'NONE',  ( 6.129554203544218538, -0.2143803907406968412, 1.798669436738309368 ) ) ;
#97797=CARTESIAN_POINT ( 'NONE',  ( 2.660326705311684581, -1.510451929809487170, 1.587989696798755013 ) ) ;
#97799=CARTESIAN_POINT ( 'NONE',  ( 5.986726177563552298, 1.793701560725208699, 0.4957798874403050449 ) ) ;
#97801=CARTESIAN_POINT ( 'NONE',  ( 3.515159831171112970, -1.768693170575957874, 0.7362056930131228860 ) ) ;
#97803=DIRECTION ( 'NONE',  ( 1.039099362110107450E-15, 1.000000000000000000, -4.583713267641621330E-32 ) ) ;
#97807=CARTESIAN_POINT ( 'NONE',  ( 0.5851287433712646369, -0.2658872486876809327, -2.145209338178376335 ) ) ;
#97810=CARTESIAN_POINT ( 'NONE',  ( 1.799542586263824795, -0.6183211656001773582, 1.717807299235304619 ) ) ;
#97812=CARTESIAN_POINT ( 'NONE',  ( 3.364083894888194592, 0.8197913233371354469, 1.631220078658943695 ) ) ;
#97813=EDGE_CURVE ( 'NONE', #53173, #76973, #53614, .T. ) ;
#97815=CARTESIAN_POINT ( 'NONE',  ( 2.548957913124219044, 0.2380835140640499836, 1.897471792728817386 ) ) ;
#97817=CARTESIAN_POINT ( 'NONE',  ( 2.752355523121536862, -1.964097686037095336, -0.1475717908260633926 ) ) ;
#97819=CARTESIAN_POINT ( 'NONE',  ( 4.476081132534933893, -1.884639481945263872, -0.4683437986269470277 ) ) ;
#97822=CARTESIAN_POINT ( 'NONE',  ( 5.607717026683647354, 1.607092460389969446, 1.383685132418293495 ) ) ;
#97824=CARTESIAN_POINT ( 'NONE',  ( 2.473184984502617478, -1.664690511387197702, -0.9409074295685518896 ) ) ;
#97826=CARTESIAN_POINT ( 'NONE',  ( 6.983263157960370116, 7.052597238847845063, 2.544342084569085838 ) ) ;
#97829=CARTESIAN_POINT ( 'NONE',  ( 3.791655721365494891, 1.894798488814054327, -0.6802303536831488806 ) ) ;
#97831=CARTESIAN_POINT ( 'NONE',  ( 5.408770660633122063, 1.379882519126625295, -1.195542987486551301 ) ) ;
#97832=CARTESIAN_POINT ( 'NONE',  ( 0.2739938332866619364, -2.030697503880642518, 0.4024348779970430834 ) ) ;
#97836=CARTESIAN_POINT ( 'NONE',  ( 5.278141497218024725, -1.038406966791558528, 1.555765341417144842 ) ) ;
#97847=CARTESIAN_POINT ( 'NONE',  ( 0.8134373588399683719, -1.746984811521329339, -1.110588058507409936 ) ) ;
#97848=CARTESIAN_POINT ( 'NONE',  ( 1.827892122045454260, 0.8069190765337170834, -1.957623834376254646 ) ) ;
#97851=CARTESIAN_POINT ( 'NONE',  ( 0.8484201349984072937, -1.953920032193863232, -0.2464512992164570593 ) ) ;
#97856=CARTESIAN_POINT ( 'NONE',  ( 2.203457528917366570, -0.4999491416500188579, 2.236933425931705521 ) ) ;
#97859=CARTESIAN_POINT ( 'NONE',  ( 2.302860652515530848, -0.3306829512400177862, -1.883434002855538081 ) ) ;
#97864=CARTESIAN_POINT ( 'NONE',  ( 0.8088407350804104334, -0.4930801656862683346, -1.951752914270672212 ) ) ;
#97865=CARTESIAN_POINT ( 'NONE',  ( 1.340592890135338555, -1.912720961655197893, -0.4351338972534216087 ) ) ;
#97870=CARTESIAN_POINT ( 'NONE',  ( 3.960945476642624641, 0.2557261242597759776, -2.074860007841982767 ) ) ;
#97871=CARTESIAN_POINT ( 'NONE',  ( 2.518099203671141595, 1.158133694123581359, -1.338384833553945663 ) ) ;
#97874=CARTESIAN_POINT ( 'NONE',  ( 5.472717818731657857, -0.05164252020756903566, -2.291847404020570966 ) ) ;
#97875=CARTESIAN_POINT ( 'NONE',  ( 4.575936575705426890, -1.688975870839603655, -0.4190883748532001629 ) ) ;
#97876=AXIS2_PLACEMENT_3D ( 'NONE', #40282, #42434, #90106 ) ;
#97879=CARTESIAN_POINT ( 'NONE',  ( 3.936634314383654853, 0.9622043370151998065, 1.442083020896669954 ) ) ;
#97880=CARTESIAN_POINT ( 'NONE',  ( 4.686072593652621521, -1.332121122860012052, -1.714431229949509250 ) ) ;
#97882=CARTESIAN_POINT ( 'NONE',  ( 5.735564631760892595, 0.5807582108038509272, -1.931123567068816493 ) ) ;
#97883=CARTESIAN_POINT ( 'NONE',  ( 0.5624999999999944489, -1.451031289061000207, -1.451031289061098795 ) ) ;
#97885=CARTESIAN_POINT ( 'NONE',  ( 3.082943253306829057, -0.1403151614269258773, -1.921328324580730440 ) ) ;
#97887=CARTESIAN_POINT ( 'NONE',  ( 5.713180276867825924, 1.816287534895771216, -1.278698279616990563 ) ) ;
#97888=EDGE_LOOP ( 'NONE', ( #125324, #181026, #75928, #203661 ) ) ;
#97889=CARTESIAN_POINT ( 'NONE',  ( 6.883263157960373135, 0.5713788194823016253, 2.097868537683903245 ) ) ;
#97892=CARTESIAN_POINT ( 'NONE',  ( 1.243189324034719823, 2.142110494306264101, 0.5876511989056328877 ) ) ;
#97898=CARTESIAN_POINT ( 'NONE',  ( 0.1060925565549031974, -0.09613213100253051313, 2.014232862735332308 ) ) ;
#97900=CARTESIAN_POINT ( 'NONE',  ( 4.844214494511547286, -0.9753611933653669741, 1.817521503207474076 ) ) ;
#97903=CARTESIAN_POINT ( 'NONE',  ( 5.606678975738343951, 1.416997745663551633, -1.221222563005261774 ) ) ;
#97904=CARTESIAN_POINT ( 'NONE',  ( 4.957493672250036454, -1.635265592371325960, -0.5776676170772595542 ) ) ;
#97905=CARTESIAN_POINT ( 'NONE',  ( 4.933026880143430049, -1.235701381803285148, -1.225916536586797667 ) ) ;
#97908=CARTESIAN_POINT ( 'NONE',  ( 2.121020962670455923, 0.004254578539099414594, 2.292545472008022056 ) ) ;
#97910=CARTESIAN_POINT ( 'NONE',  ( 0.9020086522944226193, 1.395640307904035593, -1.200911154268270664 ) ) ;
#97913=CARTESIAN_POINT ( 'NONE',  ( 2.133574855335911291, -1.190200692204022470, -1.384352166806518625 ) ) ;
#97914=CARTESIAN_POINT ( 'NONE',  ( 2.496720397819631732, -1.994071314890283553, 0.2986276487200872354 ) ) ;
#97915=CARTESIAN_POINT ( 'NONE',  ( 1.306853331985533107, 1.934050699793531836, 1.030479497498619557 ) ) ;
#97917=CARTESIAN_POINT ( 'NONE',  ( 4.014754730066903754, 1.490810813664491974, -1.487730979428596223 ) ) ;
#97920=CARTESIAN_POINT ( 'NONE',  ( 1.715371797147913435, -1.774658612622433296, -1.066089629202723765 ) ) ;
#97923=CARTESIAN_POINT ( 'NONE',  ( 3.317144061745095129, 1.670432841370917298, -1.306055464808851818 ) ) ;
#97925=CARTESIAN_POINT ( 'NONE',  ( 6.234959169399230561, 0.1841439077357870380, 1.816378869960999509 ) ) ;
#97932=CARTESIAN_POINT ( 'NONE',  ( 3.498311158119755682, -0.9917195014866404534, 1.759444004082431068 ) ) ;
#97933=CARTESIAN_POINT ( 'NONE',  ( 0.6574224672675427206, -1.779203033188281990, -1.126420244723020270 ) ) ;
#97936=CARTESIAN_POINT ( 'NONE',  ( 4.996841193152741667, 0.3155067605547862142, 1.833815385591957448 ) ) ;
#97943=CARTESIAN_POINT ( 'NONE',  ( 0.1808504484964272296, -2.097240537080494516, -0.5235256853268267507 ) ) ;
#97944=CARTESIAN_POINT ( 'NONE',  ( 3.274625289317079524, -0.3981104328964027994, -1.976669913042613747 ) ) ;
#97949=CARTESIAN_POINT ( 'NONE',  ( 2.354500945691032410, -0.7452406562851380256, 1.565668601905329638 ) ) ;
#97950=CARTESIAN_POINT ( 'NONE',  ( 1.147962396684144792, -1.373903031218721926, 1.068100470705938276 ) ) ;
#97951=CARTESIAN_POINT ( 'NONE',  ( 6.129535273836777876, -2.175136813519952916, 0.7712226964542520102 ) ) ;
#97954=CARTESIAN_POINT ( 'NONE',  ( 2.653650601580277879, 0.5529494111683015412, -1.985115717065755847 ) ) ;
#97955=CARTESIAN_POINT ( 'NONE',  ( 1.598982282203027516, 0.9961506480390787122, -1.752761228829378126 ) ) ;
#97956=CARTESIAN_POINT ( 'NONE',  ( 6.825078400183550720, 4.691998341648846882, 2.606919129228836507 ) ) ;
#97958=CARTESIAN_POINT ( 'NONE',  ( 0.6550726410136185063, -1.664185259661060234, -1.056694852926373773 ) ) ;
#97959=CARTESIAN_POINT ( 'NONE',  ( 4.570513122935188299, 0.7371126809179430195, 1.764830652192488580 ) ) ;
#97961=CARTESIAN_POINT ( 'NONE',  ( 5.901041445831936016, 1.806360628843254768, -1.267562117129708232 ) ) ;
#97965=CARTESIAN_POINT ( 'NONE',  ( 6.305353446217972113, 1.845220813986702124, -1.044706065825385943 ) ) ;
#97967=CARTESIAN_POINT ( 'NONE',  ( 4.999205796216253717, 1.921780780153565793, -1.277121366954391934 ) ) ;
#97968=CARTESIAN_POINT ( 'NONE',  ( 5.002378505967388200, 1.956489882415031190, 0.1462272935644214900 ) ) ;
#97969=CARTESIAN_POINT ( 'NONE',  ( 1.428482823135175606, -1.248714028858177283, 1.512975372890807524 ) ) ;
#97971=CARTESIAN_POINT ( 'NONE',  ( 0.01820432788856435335, -1.842448466851685840, 0.8197770699841927522 ) ) ;
#97973=CARTESIAN_POINT ( 'NONE',  ( -0.2232446489705899595, -0.4745787333681207865, -2.071451665377940010 ) ) ;
#97976=CARTESIAN_POINT ( 'NONE',  ( 1.235996726672627943, 0.3573974351761283752, 1.805938768738392319 ) ) ;
#97978=CARTESIAN_POINT ( 'NONE',  ( 4.047858276791187038, 1.568658707867241819, 1.501164901757213288 ) ) ;
#97980=CARTESIAN_POINT ( 'NONE',  ( 1.389100911873580646, -2.015333191458138273, -0.6601287711371638389 ) ) ;
#97985=CARTESIAN_POINT ( 'NONE',  ( 1.950533276942335137, 0.6436621796281314367, 1.957774297735858759 ) ) ;
#97987=CARTESIAN_POINT ( 'NONE',  ( -0.1237769027084348328, -0.1346504581853508187, -1.811164470923332104 ) ) ;
#97991=( BOUNDED_SURFACE ( )  B_SPLINE_SURFACE ( 3, 3, ( 
 ( #97785, #163846, #76175, #15425, #133502, #115145, #51149, #33822, #34875, #199506 ),
 ( #148655, #37016, #84710, #100949, #182195, #99902, #16488, #3435, #69502, #102031 ),
 ( #167036, #103099, #18631, #1298, #53278, #131389, #201630, #65238, #197385, #66294 ),
 ( #149719, #81515, #2361, #132440, #150797, #183271, #83635, #181142, #198441, #165963 ),
 ( #185399, #82568, #168101, #68437, #117273, #49027, #222, #50086, #134566, #151859 ),
 ( #164894, #147593, #116209, #98844, #200568, #32764, #17548, #119410, #213611, #52214 ),
 ( #118344, #67357, #184328, #135610, #35953, #19700, #85778, #86846, #55411, #152912 ) ),
 .UNSPECIFIED., .T., .F., .T. ) 
 B_SPLINE_SURFACE_WITH_KNOTS ( ( 4, 3, 4 ),
 ( 4, 1, 1, 1, 1, 1, 1, 4 ),
 ( 0.000000000000000000, 0.5000000000000000000, 1.000000000000000000 ),
 ( 0.000000000000000000, 0.09183773654504942541, 0.1838067853904964410, 0.2558923657893393822, 0.3606054339151033017, 0.5206678126786191685, 0.7335446035554463728, 1.000000000000000000 ),
 .UNSPECIFIED. ) 
 GEOMETRIC_REPRESENTATION_ITEM ( )  RATIONAL_B_SPLINE_SURFACE ( (
 ( 1.000000000000000222, 1.000000000000000222, 0.9999999999999997780, 1.000000000000000000, 1.000000000000000222, 0.9999999999999996669, 1.000000000000000222, 1.000000000000000444, 1.000000000000000000, 1.000000000000000000),
 ( 0.3333333333333334259, 0.3333333333333334814, 0.3333333333333333703, 0.3333333333333333703, 0.3333333333333333703, 0.3333333333333332593, 0.3333333333333334814, 0.3333333333333334814, 0.3333333333333333703, 0.3333333333333333703),
 ( 0.3333333333333334259, 0.3333333333333334814, 0.3333333333333333703, 0.3333333333333333703, 0.3333333333333333703, 0.3333333333333332593, 0.3333333333333334814, 0.3333333333333334814, 0.3333333333333333703, 0.3333333333333333703),
 ( 1.000000000000000222, 1.000000000000000222, 0.9999999999999997780, 1.000000000000000000, 1.000000000000000222, 0.9999999999999996669, 1.000000000000000222, 1.000000000000000444, 1.000000000000000000, 1.000000000000000000),
 ( 0.3333333333333334259, 0.3333333333333334814, 0.3333333333333333703, 0.3333333333333333703, 0.3333333333333333703, 0.3333333333333332593, 0.3333333333333334814, 0.3333333333333334814, 0.3333333333333333703, 0.3333333333333333703),
 ( 0.3333333333333334259, 0.3333333333333334814, 0.3333333333333333703, 0.3333333333333333703, 0.3333333333333333703, 0.3333333333333332593, 0.3333333333333334814, 0.3333333333333334814, 0.3333333333333333703, 0.3333333333333333703),
 ( 1.000000000000000222, 1.000000000000000222, 0.9999999999999997780, 1.000000000000000000, 1.000000000000000222, 0.9999999999999996669, 1.000000000000000222, 1.000000000000000444, 1.000000000000000000, 1.000000000000000000) ) ) 
 REPRESENTATION_ITEM ( '' )  SURFACE ( )  );
#97993=CARTESIAN_POINT ( 'NONE',  ( 1.880510708721146118, -1.211181421480477693, 1.910737325309288304 ) ) ;
#97995=CARTESIAN_POINT ( 'NONE',  ( 1.371055822538247870, -1.554752094505476467, -0.9295159999406394924 ) ) ;
#97996=CARTESIAN_POINT ( 'NONE',  ( 2.079167605185348044, 1.483516914179264790, 1.212129443301296128 ) ) ;
#97997=CARTESIAN_POINT ( 'NONE',  ( 2.787621587699981696, -1.932700977737045633, 0.7428295258242522126 ) ) ;
#98000=CARTESIAN_POINT ( 'NONE',  ( 1.674623549722221716, -1.871433754200592992, -0.6201854899473575600 ) ) ;
#98001=CARTESIAN_POINT ( 'NONE',  ( 5.707627890916790570, -0.4656921374228146226, 1.869253615786143685 ) ) ;
#98002=CARTESIAN_POINT ( 'NONE',  ( 0.9620547613307988133, 0.4452262838200848893, -2.264189643979396482 ) ) ;
#98005=CARTESIAN_POINT ( 'NONE',  ( 5.353991443295786468, -0.7455691153513328562, 1.923382134945450295 ) ) ;
#98011=CARTESIAN_POINT ( 'NONE',  ( 0.03009625396771432870, -1.297761387203050232, -1.659265549802463546 ) ) ;
#98013=CARTESIAN_POINT ( 'NONE',  ( 4.675171183009182663, 0.005162144975975196948, -2.161773191939574179 ) ) ;
#98014=CARTESIAN_POINT ( 'NONE',  ( 4.846356044401274765, 1.036295046036241674, -1.733382803446526621 ) ) ;
#98023=CARTESIAN_POINT ( 'NONE',  ( 4.153529959351897283, 1.954779968807466295, -0.4946301968136583849 ) ) ;
#98028=CARTESIAN_POINT ( 'NONE',  ( 4.926735330553584369, 2.067573386176469796, 0.6309256262674377558 ) ) ;
#98030=SURFACE_STYLE_FILL_AREA ( #180324 ) ;
#98033=CARTESIAN_POINT ( 'NONE',  ( 5.026970340808907700, -1.727993218758390404, 1.039010492973009514 ) ) ;
#98036=CARTESIAN_POINT ( 'NONE',  ( 0.1172359533097135365, -1.692718506494130359, 0.3305547394890032686 ) ) ;
#98041=CARTESIAN_POINT ( 'NONE',  ( 6.415307259278708152, -0.2288938695442776505, 1.856442058181500654 ) ) ;
#98042=CARTESIAN_POINT ( 'NONE',  ( 1.084635982312625924, -1.275300252541565538, 1.557628696486039077 ) ) ;
#98043=CARTESIAN_POINT ( 'NONE',  ( 3.083271082906696048, -0.1608111237268796401, -2.200959079826501075 ) ) ;
#98047=CARTESIAN_POINT ( 'NONE',  ( 1.805496089173063812, 1.843435535509674317, -1.047849062051921853 ) ) ;
#98048=CARTESIAN_POINT ( 'NONE',  ( 1.898064762488653079, -0.9530305783747442527, -1.777002450075705120 ) ) ;
#98049=CARTESIAN_POINT ( 'NONE',  ( 2.144508837627901343, 1.757922920557394519, 0.4371675498636724000 ) ) ;
#98054=CARTESIAN_POINT ( 'NONE',  ( -0.1708952380198276444, -1.482394133889615828, -1.213259445456981167 ) ) ;
#98061=CARTESIAN_POINT ( 'NONE',  ( 5.577088068215094729, -0.04877400797019536272, -2.161318155665878038 ) ) ;
#98064=CARTESIAN_POINT ( 'NONE',  ( 2.250376613284802207, 0.9954810856505690309, -1.872389709364124188 ) ) ;
#98065=CARTESIAN_POINT ( 'NONE',  ( 6.616225513087798049, -0.8637638766970030524, -1.608286988965562214 ) ) ;
#98067=CARTESIAN_POINT ( 'NONE',  ( 3.093000238167437743, 1.692540756771460764, -1.010471881233595104 ) ) ;
#98068=CARTESIAN_POINT ( 'NONE',  ( 5.994389040191065554, -1.017321598621454548, 1.619163160827830517 ) ) ;
#98071=CARTESIAN_POINT ( 'NONE',  ( 0.2212536527127808295, -1.848710500310095872, -0.9322282823912150240 ) ) ;
#98072=CARTESIAN_POINT ( 'NONE',  ( 1.956878712445113244, 0.3320500349934927820, -1.913199751371328361 ) ) ;
#98077=CARTESIAN_POINT ( 'NONE',  ( 2.185595087713845697, -0.8928614526015861141, 1.890522631819052002 ) ) ;
#98081=CARTESIAN_POINT ( 'NONE',  ( 5.725241913846256914, 1.688569718951500986, 0.8975008795490189151 ) ) ;
#98083=CARTESIAN_POINT ( 'NONE',  ( 4.073040751519330094, -2.058760688187323495, -0.7953439701907026871 ) ) ;
#98084=CARTESIAN_POINT ( 'NONE',  ( 1.887996149947854807, 1.521953097117642706, 1.598203399828190152 ) ) ;
#98086=CARTESIAN_POINT ( 'NONE',  ( 0.1000639402851908749, -0.9014739813196898099, 1.686438745833309438 ) ) ;
#98090=CARTESIAN_POINT ( 'NONE',  ( 3.859880467719906783, -0.6038372105774907350, 1.980330894321411295 ) ) ;
#98093=CARTESIAN_POINT ( 'NONE',  ( 1.217891636700708435, -2.108894920778502602, 0.4742063263511315796 ) ) ;
#98094=CARTESIAN_POINT ( 'NONE',  ( 4.001666433686186686, -2.185622478633037602, 0.1623105178310546570 ) ) ;
#98101=CARTESIAN_POINT ( 'NONE',  ( 0.3697678102792775756, -0.2496098759999023087, -2.000856779379902139 ) ) ;
#98104=CARTESIAN_POINT ( 'NONE',  ( 4.311429529933403337, -1.718370896367764411, -1.154329086688666184 ) ) ;
#98105=CARTESIAN_POINT ( 'NONE',  ( 6.011343318556897408, -1.993460012771612222, 0.7135861072808927785 ) ) ;
#98108=CARTESIAN_POINT ( 'NONE',  ( 3.871889627987592064, -1.941038753702705177, 0.3322218420921344562 ) ) ;
#98109=CARTESIAN_POINT ( 'NONE',  ( 5.824266732648851530, 2.207754452112113075, 0.6165074292824882507 ) ) ;
#98110=CARTESIAN_POINT ( 'NONE',  ( 3.826616632296374831, 1.734130841282412128, 0.5711148077138239465 ) ) ;
#98117=CARTESIAN_POINT ( 'NONE',  ( 4.728775500204083215, 1.385159600073909258, -1.461172115097974622 ) ) ;
#98118=CARTESIAN_POINT ( 'NONE',  ( 6.469376040731918742, -2.253416215261240918, -0.4533134382209720314 ) ) ;
#98119=CARTESIAN_POINT ( 'NONE',  ( 4.328923052438288899, -1.828919189252835142, -0.7100325158947774495 ) ) ;
#98125=CARTESIAN_POINT ( 'NONE',  ( 0.7848512634026264534, 1.842159585024247148, -0.9888006619010838438 ) ) ;
#98126=CARTESIAN_POINT ( 'NONE',  ( 5.735142062806906083, -1.598577407953686746, 0.7598067823499834450 ) ) ;
#98128=CARTESIAN_POINT ( 'NONE',  ( 6.527294062531273866, -1.270327234845580078, -1.468905576289506909 ) ) ;
#98129=CARTESIAN_POINT ( 'NONE',  ( 2.150558370509841666, -1.692889690492072718, 1.391600924549152296 ) ) ;
#98130=CARTESIAN_POINT ( 'NONE',  ( 1.276469996339978819, 1.608456030955440541, -0.6653204537699786147 ) ) ;
#98132=CARTESIAN_POINT ( 'NONE',  ( 0.1333692844072559003, 5.722267537706915874, -2.647605121726896105 ) ) ;
#98133=CARTESIAN_POINT ( 'NONE',  ( 1.259898821826772819, 0.6958341084943464594, 1.578493908868659146 ) ) ;
#98134=CARTESIAN_POINT ( 'NONE',  ( 1.312353134292881141, 1.468346937154514364, -1.627112938194043235 ) ) ;
#98135=CARTESIAN_POINT ( 'NONE',  ( 3.703933201646680828, -0.6411959742554216302, 2.111683309420588905 ) ) ;
#98136=CARTESIAN_POINT ( 'NONE',  ( 1.094852686531849084, 2.138608527004157711, 0.3732488551555103173 ) ) ;
#98139=CARTESIAN_POINT ( 'NONE',  ( 2.378245518041781636, -2.112004366230528785, -0.1507482023494610135 ) ) ;
#98140=CARTESIAN_POINT ( 'NONE',  ( 6.639320575229255006, 1.299223727596211519, 1.914393416674460946 ) ) ;
#98142=CARTESIAN_POINT ( 'NONE',  ( 2.630776572171345418, 0.2838290345775448809, 2.274689434353324824 ) ) ;
#98145=CARTESIAN_POINT ( 'NONE',  ( 5.110122900737038343, -0.8006010496643833907, 2.072185752117897461 ) ) ;
#98155=CARTESIAN_POINT ( 'NONE',  ( 3.147111449167848019, 0.9091449406319618287, 1.799922684605055556 ) ) ;
#98157=CARTESIAN_POINT ( 'NONE',  ( 1.235300832636996970, -0.04672723545543105983, -2.062185333280424526 ) ) ;
#98162=CARTESIAN_POINT ( 'NONE',  ( 4.048915112334880106, -1.821525731582713359, -1.218098874207810933 ) ) ;
#98163=CARTESIAN_POINT ( 'NONE',  ( 2.707657903872981553, 1.899618770239443366, 0.6767133375917554483 ) ) ;
#98164=CARTESIAN_POINT ( 'NONE',  ( 1.575478407343299692, -0.9843019613302635973, 1.555867251595323353 ) ) ;
#98166=CARTESIAN_POINT ( 'NONE',  ( 4.858326754937916547, 0.6996357133068830114, 1.686392194618462570 ) ) ;
#98167=CARTESIAN_POINT ( 'NONE',  ( 6.469375277500488686, -1.978045142091336306, -0.3906011616893814709 ) ) ;
#98169=CARTESIAN_POINT ( 'NONE',  ( 4.838899928913665605, 0.3820838354035635542, 2.229877907420589001 ) ) ;
#98171=CARTESIAN_POINT ( 'NONE',  ( 0.7683615598204245334, 1.039662503867449184, 1.831484773650635223 ) ) ;
#98173=CARTESIAN_POINT ( 'NONE',  ( 4.721179655770254335, -1.847879960204744432, -0.9338546512941485744 ) ) ;
#98181=CARTESIAN_POINT ( 'NONE',  ( 1.476976393720278002, -1.495863523836362896, 1.503369785937097136 ) ) ;
#98182=CARTESIAN_POINT ( 'NONE',  ( 1.248599636731639428, 1.089134306475655789, -1.936006665247846481 ) ) ;
#98186=CARTESIAN_POINT ( 'NONE',  ( 3.086327779807009009, 1.092107249913790712, -1.629585102321646328 ) ) ;
#98192=CARTESIAN_POINT ( 'NONE',  ( 2.144932638433934002, 2.058100890041581810, 0.5106320605416380110 ) ) ;
#98194=CARTESIAN_POINT ( 'NONE',  ( 5.898874287966751950, 0.3812104124719677412, 1.924297140916144233 ) ) ;
#98195=CARTESIAN_POINT ( 'NONE',  ( 3.608425205800522839, -0.8741791752944136906, -1.977237025433141504 ) ) ;
#98196=CARTESIAN_POINT ( 'NONE',  ( 3.104851637799400876, -0.3563606998662186554, 1.806257425991746546 ) ) ;
#98199=CARTESIAN_POINT ( 'NONE',  ( 4.927569761290923722, 0.8905454123377859466, -1.495065219958094938 ) ) ;
#98200=CARTESIAN_POINT ( 'NONE',  ( 6.727182134110241130, 2.994815527893503138, 2.165292399158074588 ) ) ;
#98202=CARTESIAN_POINT ( 'NONE',  ( 1.797963993548271411, -0.7283430984801853025, 2.035426966748521860 ) ) ;
#98203=CARTESIAN_POINT ( 'NONE',  ( 4.991564454312596766, 1.928456700051227379, 0.5879293935868237231 ) ) ;
#98205=CARTESIAN_POINT ( 'NONE',  ( 0.7081719773709761467, -2.151164098719647200, 0.2130325561137471624 ) ) ;
#98206=CARTESIAN_POINT ( 'NONE',  ( 3.145733524295030836, 0.7127697582950813793, -1.838151395584181058 ) ) ;
#98208=CARTESIAN_POINT ( 'NONE',  ( 3.667467498987980967, 1.081383794499408468, 1.612947176984424802 ) ) ;
#98213=CARTESIAN_POINT ( 'NONE',  ( 0.07755575628183573877, -0.002876890934064984216, -2.188974970840869005 ) ) ;
#98217=CARTESIAN_POINT ( 'NONE',  ( 0.7103623821160671703, -2.195938746145317477, 0.2182302698266261887 ) ) ;
#98219=CARTESIAN_POINT ( 'NONE',  ( 5.524254240939322713, 0.9636562883742012531, 1.708648623189083393 ) ) ;
#98220=CARTESIAN_POINT ( 'NONE',  ( 4.012992375354424546, 0.1078809898697324771, 2.114737393012538824 ) ) ;
#98223=CARTESIAN_POINT ( 'NONE',  ( 4.488128036367874607, -0.4058819498431766037, -1.795677737744493019 ) ) ;
#98227=CARTESIAN_POINT ( 'NONE',  ( 4.658503719480325600, 2.115088938745744329, 0.1532479335744421078 ) ) ;
#98229=CARTESIAN_POINT ( 'NONE',  ( 6.239539339872155033, -1.489444859125512277, -1.424447411405028507 ) ) ;
#98231=CARTESIAN_POINT ( 'NONE',  ( 0.7657746542184565852, -1.852627923093919771, 0.1767624929009704582 ) ) ;
#98232=CARTESIAN_POINT ( 'NONE',  ( 3.931074656914943954, -1.272613488525012659, -1.330884258478791438 ) ) ;
#98237=CARTESIAN_POINT ( 'NONE',  ( 3.756632125300945368, 0.7937082651479386852, 2.059386989456575279 ) ) ;
#98238=CARTESIAN_POINT ( 'NONE',  ( 4.657670937300908420, 0.5017462980881717272, -2.205921056424357651 ) ) ;
#98240=CARTESIAN_POINT ( 'NONE',  ( 4.728658910183288988, 1.244086218232887120, -1.317109676944823393 ) ) ;
#98241=CARTESIAN_POINT ( 'NONE',  ( 5.682812683241409424, 1.562005318756795713, -1.108807820749290851 ) ) ;
#98244=CARTESIAN_POINT ( 'NONE',  ( 6.280143113937574739, -0.9989825818290422044, 1.581392243879369053 ) ) ;
#98245=CARTESIAN_POINT ( 'NONE',  ( 5.424199618621329044, 0.9171840495176122321, 1.619240327305818683 ) ) ;
#98246=CARTESIAN_POINT ( 'NONE',  ( 6.631742710195931423, -1.160100399838214891, -1.336722620761298330 ) ) ;
#98247=CARTESIAN_POINT ( 'NONE',  ( 1.024625454658374624, 0.3981145430279106057, 1.976669095394629982 ) ) ;
#98249=CARTESIAN_POINT ( 'NONE',  ( 3.194068465612946994, -0.8531780664592978347, 1.925702383005133855 ) ) ;
#98253=CARTESIAN_POINT ( 'NONE',  ( 2.074478865019005802, 0.8673736069498124701, 1.824228476594942583 ) ) ;
#98256=CARTESIAN_POINT ( 'NONE',  ( 3.725982817344280829, -1.284327275973631277, -1.738548686538298416 ) ) ;
#98257=CARTESIAN_POINT ( 'NONE',  ( 6.620655732516644854, 4.701125524277991907, 2.388986273831222640 ) ) ;
#98265=CARTESIAN_POINT ( 'NONE',  ( 0.8201894534925309177, 1.301127354658284663, -1.763390660798454634 ) ) ;
#98267=CARTESIAN_POINT ( 'NONE',  ( 0.9895999521203084903, 1.994116446801162290, -1.068836969126084835 ) ) ;
#98274=CARTESIAN_POINT ( 'NONE',  ( 2.969704930451398717, 0.9433242808821461489, 1.497149023046380423 ) ) ;
#98276=CARTESIAN_POINT ( 'NONE',  ( 0.1828346100962909559, -2.042824957133956953, -0.5113311198858895290 ) ) ;
#98280=CARTESIAN_POINT ( 'NONE',  ( 5.062125140741547291, -1.117816439015427044, 1.678017345901124058 ) ) ;
#98282=CARTESIAN_POINT ( 'NONE',  ( 2.043623373375623942, 0.7184291972081280342, -1.727395513401897453 ) ) ;
#98283=CARTESIAN_POINT ( 'NONE',  ( 3.221598570378156001, 0.3083542414583049784, -2.047064864394084971 ) ) ;
#98285=CARTESIAN_POINT ( 'NONE',  ( 1.441514601552947417, -1.799640695080907182, 0.6472408003148700795 ) ) ;
#98288=( NAMED_UNIT ( * ) PLANE_ANGLE_UNIT ( ) SI_UNIT ( $, .RADIAN. ) );
#98291=CARTESIAN_POINT ( 'NONE',  ( 0.9668906521006037647, -1.505869814250645478, 1.178657042999963878 ) ) ;
#98292=CARTESIAN_POINT ( 'NONE',  ( 3.385159196556942085, 0.04556868695702701727, 1.961494628812537444 ) ) ;
#98293=CARTESIAN_POINT ( 'NONE',  ( 0.2103132415818432799, -1.556605082263945228, -1.280954711483893727 ) ) ;
#98296=CARTESIAN_POINT ( 'NONE',  ( 6.919227946136824237, -0.1375138451006757134, 1.940497564164916922 ) ) ;
#98298=CARTESIAN_POINT ( 'NONE',  ( 1.951433385020440836, -1.796364150513751312, 0.9090842167202308755 ) ) ;
#98300=CARTESIAN_POINT ( 'NONE',  ( 1.863061375884986104, -0.1076188601273372486, -2.114627633294167364 ) ) ;
#98301=CARTESIAN_POINT ( 'NONE',  ( 3.279797552538410876, -1.996039814156633785, 0.5495672325947635883 ) ) ;
#98303=CARTESIAN_POINT ( 'NONE',  ( 5.912080347638632993, 1.404955882617323848, -1.548356120136730851 ) ) ;
#98305=CARTESIAN_POINT ( 'NONE',  ( 3.662960631648714216, -1.609669772967847079, -0.8612380056681954166 ) ) ;
#98308=CARTESIAN_POINT ( 'NONE',  ( 6.890000000000008562, 4.693995042360769254, 2.562605081426702736 ) ) ;
#98310=CARTESIAN_POINT ( 'NONE',  ( 5.913141818906855640, 1.943543578741913969, 1.045239939247793792 ) ) ;
#98313=CARTESIAN_POINT ( 'NONE',  ( 4.705663775918221603, 1.419457463540532816, 1.281590252682027087 ) ) ;
#98320=CARTESIAN_POINT ( 'NONE',  ( 0.2394788589213901198, 1.836227513651207177, 0.1364553164684492448 ) ) ;
#98323=CARTESIAN_POINT ( 'NONE',  ( 4.921099816907485547, -0.09337705715995942013, 1.868355541605345671 ) ) ;
#98329=CARTESIAN_POINT ( 'NONE',  ( 0.7605272443651526215, -0.6583816729706105653, -1.856300379560266833 ) ) ;
#98330=CARTESIAN_POINT ( 'NONE',  ( 2.073842424929934314, -0.8596134062341630466, 1.824128527830502833 ) ) ;
#98334=CARTESIAN_POINT ( 'NONE',  ( 2.572451567087580493, -2.097416440861415321, -0.6350555677336399141 ) ) ;
#98343=ORIENTED_EDGE ( 'NONE', *, *, #141101, .F. ) ;
#98344=CARTESIAN_POINT ( 'NONE',  ( 5.354971380013192395, 0.3533838956982695567, -1.806849549699687696 ) ) ;
#98345=CARTESIAN_POINT ( 'NONE',  ( 1.717441043944417878, 1.674910534618522906, 1.116504076032026616 ) ) ;
#98346=CARTESIAN_POINT ( 'NONE',  ( 3.567963868821962592, 1.814363981409074844, -1.410851157308941506 ) ) ;
#98347=CARTESIAN_POINT ( 'NONE',  ( 1.023987020198445341, 0.9106972337104453086, 1.622782493823480943 ) ) ;
#98350=CARTESIAN_POINT ( 'NONE',  ( 5.361546783204238942, -1.511448857895525855, -1.171587532507123441 ) ) ;
#98354=CARTESIAN_POINT ( 'NONE',  ( 3.210569733434172512, 1.891194753341999935, 0.8916721373675460249 ) ) ;
#98355=CARTESIAN_POINT ( 'NONE',  ( 3.238977024203249400, -1.650389259550872456, 0.8806316622528218563 ) ) ;
#98357=CARTESIAN_POINT ( 'NONE',  ( 6.374545129912787544, -0.09763137639631430664, -1.838803627010993313 ) ) ;
#98361=CARTESIAN_POINT ( 'NONE',  ( 4.582452686631489414, -1.674003568303910949, -0.4152789331205719026 ) ) ;
#98367=CARTESIAN_POINT ( 'NONE',  ( 4.786072553063510426, -1.330480670633835683, -1.715586834332043953 ) ) ;
#98368=CARTESIAN_POINT ( 'NONE',  ( 3.123480263227970344, -1.759325740769552393, 0.4874977319994436287 ) ) ;
#98369=CARTESIAN_POINT ( 'NONE',  ( 0.6550357524967264089, 1.634203043994170157, -1.084997510809107446 ) ) ;
#98370=CARTESIAN_POINT ( 'NONE',  ( 5.331313699870084299, -1.671001674814942994, -1.300292098898154780 ) ) ;
#98371=CARTESIAN_POINT ( 'NONE',  ( 5.636350782834250062, 0.4440221345313396517, 2.248805093627189500 ) ) ;
#98375=CARTESIAN_POINT ( 'NONE',  ( 1.260569961473339440, 2.118219532560499996, 0.1004958096475216667 ) ) ;
#98380=CARTESIAN_POINT ( 'NONE',  ( 6.789883322502159757, -1.411316560962400768, -1.649898940422918514 ) ) ;
#98381=CARTESIAN_POINT ( 'NONE',  ( 6.983263157960404754, 0.5601148359399975574, 2.204851038219941106 ) ) ;
#98383=CARTESIAN_POINT ( 'NONE',  ( 1.928696271399105600, -1.050554081124959183, -1.957186058178138399 ) ) ;
#98385=CARTESIAN_POINT ( 'NONE',  ( 6.346327303948391396, 0.3419391630616851474, -1.987045965717588958 ) ) ;
#98387=CARTESIAN_POINT ( 'NONE',  ( 5.770399673640999261, -0.9225087518928692942, -1.844811731271531086 ) ) ;
#98393=CARTESIAN_POINT ( 'NONE',  ( 4.880324068823122197, -0.2306306682541107433, -1.826696389425507938 ) ) ;
#98397=CARTESIAN_POINT ( 'NONE',  ( 2.186159124499872597, -1.690733796973374004, -0.3399922242280882245 ) ) ;
#98400=CARTESIAN_POINT ( 'NONE',  ( 1.212636322461498217, -1.017548795778918214, -2.020700439389290892 ) ) ;
#98401=CARTESIAN_POINT ( 'NONE',  ( 3.879594643445562152, 1.983085605235184845, -0.7095211871808704274 ) ) ;
#98403=CARTESIAN_POINT ( 'NONE',  ( 2.442341840454059554, 0.3829199517304190947, 1.727643488062768240 ) ) ;
#98409=CARTESIAN_POINT ( 'NONE',  ( 5.238630872344578471, 1.322862460432130849, -1.784462157271723859 ) ) ;
#98410=CARTESIAN_POINT ( 'NONE',  ( 3.978626637211603700, -0.2140425413966473567, -2.180973779111646138 ) ) ;
#98415=CARTESIAN_POINT ( 'NONE',  ( 6.610000000000006537, 7.629137130509094256, 2.600000000000001421 ) ) ;
#98417=CARTESIAN_POINT ( 'NONE',  ( 6.222909436229170588, 1.570324008046734221, -1.425282903188800798 ) ) ;
#98423=CARTESIAN_POINT ( 'NONE',  ( 6.585540641348407220, -0.7802508550805787868, 1.666130356082276220 ) ) ;
#98427=CARTESIAN_POINT ( 'NONE',  ( 1.839017211142121244, 0.6657927772366920571, -1.608260388387482420 ) ) ;
#98432=CARTESIAN_POINT ( 'NONE',  ( 6.016527291255574283, 1.455332790597754000, -1.598591904487467463 ) ) ;
#98433=EDGE_CURVE ( 'NONE', #160735, #88459, #154440, .T. ) ;
#98437=CARTESIAN_POINT ( 'NONE',  ( 5.612251347527116963, -0.9680786960581324596, -1.932885698521320528 ) ) ;
#98441=CARTESIAN_POINT ( 'NONE',  ( 5.958271952116948711, 0.7966545185628256531, 1.803378638538119860 ) ) ;
#98442=CARTESIAN_POINT ( 'NONE',  ( 5.536419981033642301, 1.670246277208887742, -0.4650152690930853816 ) ) ;
#98445=CARTESIAN_POINT ( 'NONE',  ( 2.384552795368581890, -0.3778730364575392797, -2.158588602542845347 ) ) ;
#98446=CARTESIAN_POINT ( 'NONE',  ( 3.399772400530599370, 1.817812331725022101, 1.421335012277170629 ) ) ;
#98447=CARTESIAN_POINT ( 'NONE',  ( 4.429017379523855880, 0.09708327650245980600, 2.058604088861961667 ) ) ;
#98448=CARTESIAN_POINT ( 'NONE',  ( 0.6560686395847237229, -1.407132438187887136, 1.338565165000434876 ) ) ;
#98452=CARTESIAN_POINT ( 'NONE',  ( 3.849942018323779358, -1.464806807754112539, -1.533599281611098597 ) ) ;
#98453=CARTESIAN_POINT ( 'NONE',  ( 1.740861508391436274, 2.010826320759526720, -0.1511413081683593562 ) ) ;
#98455=CARTESIAN_POINT ( 'NONE',  ( 4.085166796624926100, -0.2132991444873769959, -2.196430506890618695 ) ) ;
#98461=CARTESIAN_POINT ( 'NONE',  ( 6.825078400183544503, 3.684911640780349718, 2.658296617506946458 ) ) ;
#98463=EDGE_LOOP ( 'NONE', ( #53247, #135894, #130382, #5595 ) ) ;
#98464=CARTESIAN_POINT ( 'NONE',  ( 4.030192151223922714, 1.103973922444676070, -1.740068238149700353 ) ) ;
#98467=CARTESIAN_POINT ( 'NONE',  ( 3.967448252881644155, -1.680364903119958120, -1.120146540189705497 ) ) ;
#98471=CARTESIAN_POINT ( 'NONE',  ( 3.362233863015654300, 0.9250742651227459312, 1.841665905919416035 ) ) ;
#98475=CARTESIAN_POINT ( 'NONE',  ( 0.7789528443887736575, 1.234723402293058214, 1.365900241759879119 ) ) ;
#98476=CARTESIAN_POINT ( 'NONE',  ( 6.533804136697315634, -1.437950210024591780, -1.674183229976949905 ) ) ;
#98478=CARTESIAN_POINT ( 'NONE',  ( 1.563986776035675819, 2.129895014553784272, -0.3678597298803277793 ) ) ;
#98480=CARTESIAN_POINT ( 'NONE',  ( 1.499232818411553536, -0.2420282084563407654, 2.001858358113464575 ) ) ;
#98481=CARTESIAN_POINT ( 'NONE',  ( 1.792731522490832230, -2.164186313916468762, 0.7742391241713635353 ) ) ;
#98484=CARTESIAN_POINT ( 'NONE',  ( 0.6021629784135495989, -0.6261829430146518272, -1.762877433595814614 ) ) ;
#98485=( BOUNDED_SURFACE ( )  B_SPLINE_SURFACE ( 3, 3, ( 
 ( #117612, #86115, #36280, #102357, #197723, #1631, #101288, #98132, #83970, #165231 ),
 ( #15768, #66620, #85042, #167370, #181475, #168429, #33105, #99179, #134889, #18958 ),
 ( #20025, #151130, #150059, #16824, #200896, #556, #51490, #148981, #152185, #183604 ),
 ( #132767, #2697, #69829, #147935, #198770, #135937, #48316, #182529, #81853, #213951 ),
 ( #116539, #67690, #35213, #74140, #90394, #78132, #120825, #206255, #8050, #204089 ),
 ( #104510, #138076, #105591, #87177, #139144, #170554, #157536, #190009, #153243, #103432 ),
 ( #140233, #121898, #41659, #24288, #55742, #5894, #119745, #88250, #53612, #73045 ) ),
 .UNSPECIFIED., .T., .F., .T. ) 
 B_SPLINE_SURFACE_WITH_KNOTS ( ( 4, 3, 4 ),
 ( 4, 1, 1, 1, 1, 1, 1, 4 ),
 ( 0.000000000000000000, 0.5000000000000000000, 1.000000000000000000 ),
 ( 0.000000000000000000, 0.09373397616858752945, 0.1863105892815605236, 0.2574079725677296260, 0.3612190813870841954, 0.5208938042821120717, 0.7336009914826546741, 1.000000000000000000 ),
 .UNSPECIFIED. ) 
 GEOMETRIC_REPRESENTATION_ITEM ( )  RATIONAL_B_SPLINE_SURFACE ( (
 ( 1.000000000000000000, 1.000000000000000000, 0.9999999999999997780, 1.000000000000000000, 1.000000000000000000, 1.000000000000000222, 1.000000000000000444, 1.000000000000000222, 1.000000000000000000, 1.000000000000000000),
 ( 0.3333333333333333703, 0.3333333333333333703, 0.3333333333333332593, 0.3333333333333333703, 0.3333333333333333703, 0.3333333333333334259, 0.3333333333333334814, 0.3333333333333334259, 0.3333333333333333703, 0.3333333333333333703),
 ( 0.3333333333333333703, 0.3333333333333333703, 0.3333333333333332593, 0.3333333333333333703, 0.3333333333333333703, 0.3333333333333334259, 0.3333333333333334814, 0.3333333333333334259, 0.3333333333333333703, 0.3333333333333333703),
 ( 1.000000000000000000, 1.000000000000000000, 0.9999999999999997780, 1.000000000000000000, 1.000000000000000000, 1.000000000000000222, 1.000000000000000444, 1.000000000000000222, 1.000000000000000000, 1.000000000000000000),
 ( 0.3333333333333333703, 0.3333333333333333703, 0.3333333333333332593, 0.3333333333333333703, 0.3333333333333333703, 0.3333333333333334259, 0.3333333333333334814, 0.3333333333333334259, 0.3333333333333333703, 0.3333333333333333703),
 ( 0.3333333333333333703, 0.3333333333333333703, 0.3333333333333332593, 0.3333333333333333703, 0.3333333333333333703, 0.3333333333333334259, 0.3333333333333334814, 0.3333333333333334259, 0.3333333333333333703, 0.3333333333333333703),
 ( 1.000000000000000000, 1.000000000000000000, 0.9999999999999997780, 1.000000000000000000, 1.000000000000000000, 1.000000000000000222, 1.000000000000000444, 1.000000000000000222, 1.000000000000000000, 1.000000000000000000) ) ) 
 REPRESENTATION_ITEM ( '' )  SURFACE ( )  );
#98486=CARTESIAN_POINT ( 'NONE',  ( 4.504732016840462983, 1.524723275766314279, -1.249774587014943483 ) ) ;
#98488=CARTESIAN_POINT ( 'NONE',  ( 4.241422899474024177, 0.4370803545316758743, -1.968444674787086512 ) ) ;
#98492=CARTESIAN_POINT ( 'NONE',  ( 6.481095854277318935, -0.1012916397761880333, -2.103764601514758414 ) ) ;
#98493=CARTESIAN_POINT ( 'NONE',  ( 4.896967953096117654, 0.3505727482827174502, 2.040303948762006492 ) ) ;
#98496=CARTESIAN_POINT ( 'NONE',  ( 6.539320575229260690, 0.5855366995804256458, 2.057005297509428399 ) ) ;
#98497=CARTESIAN_POINT ( 'NONE',  ( 4.746356070053968423, 1.034628734442550879, -1.734499354260822468 ) ) ;
#98499=CARTESIAN_POINT ( 'NONE',  ( 2.877863741784414842, 2.191074257732894548, -0.7245186886237849899 ) ) ;
#98502=CARTESIAN_POINT ( 'NONE',  ( 1.534110023759263308, 1.225272132802219360, 1.659075958507538973 ) ) ;
#98509=CARTESIAN_POINT ( 'NONE',  ( 3.701788104937975721, -1.641978770885927252, -1.420606208986204155 ) ) ;
#98513=CARTESIAN_POINT ( 'NONE',  ( 2.893917256732419396, -0.5369380550670297403, -1.761199466696103499 ) ) ;
#98515=CARTESIAN_POINT ( 'NONE',  ( 4.528971853086540378, -2.003544689622422936, 0.8885388601788182239 ) ) ;
#98517=CARTESIAN_POINT ( 'NONE',  ( 5.928679764299940480, 2.178688510132809064, 0.6099592146414765104 ) ) ;
#98522=CARTESIAN_POINT ( 'NONE',  ( 6.432837487460982828, 0.1759369732093341021, 1.760927613267867953 ) ) ;
#98523=CARTESIAN_POINT ( 'NONE',  ( 3.651042523073198431, 0.2976914719170896118, 1.990856138409332843 ) ) ;
#98526=CARTESIAN_POINT ( 'NONE',  ( 3.153452123856602896, -1.720715631468725526, -1.213874241417127298 ) ) ;
#98527=CARTESIAN_POINT ( 'NONE',  ( 1.827608144986846206, 0.7312883373844185630, -1.770730004348388453 ) ) ;
#98530=CARTESIAN_POINT ( 'NONE',  ( 3.420317264040674932, 0.8831254867164675115, 1.760515127234823840 ) ) ;
#98531=CARTESIAN_POINT ( 'NONE',  ( 0.5318453760667535279, 0.9654296485097979552, -1.602142582367314549 ) ) ;
#98532=CARTESIAN_POINT ( 'NONE',  ( 1.240593047436115759, -1.913272810121857237, -0.4332019784048374289 ) ) ;
#98533=CARTESIAN_POINT ( 'NONE',  ( 0.6856317642073318508, 1.842354612247762091, -0.5124485439033445999 ) ) ;
#98537=CARTESIAN_POINT ( 'NONE',  ( 5.910993886665249164, 1.650546521282238110, 0.8803886038859505270 ) ) ;
#98542=CARTESIAN_POINT ( 'NONE',  ( 1.240778115703184303, -2.019486815914430355, -0.4554155650244652853 ) ) ;
#98547=CARTESIAN_POINT ( 'NONE',  ( 5.936213163351176547, -1.177816969253571155, -1.763093882214488817 ) ) ;
#98554=CARTESIAN_POINT ( 'NONE',  ( 6.021922112293466967, 1.933069186966931863, -0.3339256516061983038 ) ) ;
#98556=CARTESIAN_POINT ( 'NONE',  ( 4.323592178502837058, -1.495822217463145476, 1.351947993609707632 ) ) ;
#98557=CARTESIAN_POINT ( 'NONE',  ( 3.221808243886138179, 0.8566008913209141040, -1.713579649959365403 ) ) ;
#98559=CARTESIAN_POINT ( 'NONE',  ( 1.242012060539962492, 2.189267750446591609, 0.1026977899005257211 ) ) ;
#98561=CARTESIAN_POINT ( 'NONE',  ( 3.286256049847174676, -1.842268013383094427, -0.3231441395407097517 ) ) ;
#98565=CARTESIAN_POINT ( 'NONE',  ( 5.114917985578482096, 0.1569784262732084601, 2.111484538518786813 ) ) ;
#98567=CARTESIAN_POINT ( 'NONE',  ( 6.742638474511262636, -2.029596885996234334, -0.4079607620106340260 ) ) ;
#98568=CARTESIAN_POINT ( 'NONE',  ( 1.786781105396139102, 1.817558579408204089, -1.033184933219722934 ) ) ;
#98570=CARTESIAN_POINT ( 'NONE',  ( 1.113767329461469835, -0.7700024601069790364, -1.543427451845545084 ) ) ;
#98581=CARTESIAN_POINT ( 'NONE',  ( 2.033590728242135715, -1.756817081591253604, 0.4409998202260062006 ) ) ;
#98590=CARTESIAN_POINT ( 'NONE',  ( 3.261990205869094162, -1.859054838292145240, 0.08865997893938745711 ) ) ;
#98591=CARTESIAN_POINT ( 'NONE',  ( 0.05214973123207015254, -1.250902960675448483, 1.450897702916327248 ) ) ;
#98592=CARTESIAN_POINT ( 'NONE',  ( 0.08272424614634911466, -0.1293432359340887239, -1.795996506534849324 ) ) ;
#98601=CARTESIAN_POINT ( 'NONE',  ( 4.381674357853755808, -1.885861198437089437, 0.5677522405800348171 ) ) ;
#98602=CARTESIAN_POINT ( 'NONE',  ( 2.016421337698256711, -2.119947128278206971, 0.05498460973795551987 ) ) ;
#98604=DIRECTION ( 'NONE',  ( 1.039099362110107450E-15, 1.000000000000000000, -4.583713267641621330E-32 ) ) ;
#98606=CARTESIAN_POINT ( 'NONE',  ( 6.369083545433415594, 2.098215621258665564, -0.6323776016037768732 ) ) ;
#98608=CARTESIAN_POINT ( 'NONE',  ( 3.997031241255116552, 1.627850364849007248, -1.029807644849835890 ) ) ;
#98610=CARTESIAN_POINT ( 'NONE',  ( 0.4986989427119004059, 1.520756344202650601, -1.009667857431728599 ) ) ;
#98611=CARTESIAN_POINT ( 'NONE',  ( 0.5576012004645107822, -1.866542136390366036, -1.177153700605698461 ) ) ;
#98613=ORIENTED_EDGE ( 'NONE', *, *, #72903, .T. ) ;
#98615=CARTESIAN_POINT ( 'NONE',  ( 6.368014371105396698, -1.954979222910321557, 0.2374047605521299453 ) ) ;
#98616=CARTESIAN_POINT ( 'NONE',  ( 2.015084816950295732, -1.883260942463622856, 0.4737542896416384597 ) ) ;
#98617=CARTESIAN_POINT ( 'NONE',  ( 6.450549897212096262, 1.577601184540510681, 1.671684124095852653 ) ) ;
#98619=CARTESIAN_POINT ( 'NONE',  ( 5.858217239054963166, -1.861131630269092341, -0.001575894832107904492 ) ) ;
#98626=CARTESIAN_POINT ( 'NONE',  ( 1.242012060539962492, 2.189267750446591609, 0.1026977899005257211 ) ) ;
#98630=CARTESIAN_POINT ( 'NONE',  ( 1.928079105319381314, 1.052063804484974385, -1.491885150056403431 ) ) ;
#98633=CARTESIAN_POINT ( 'NONE',  ( 6.509000000000035868, 7.629137130509092479, 2.600000000000000977 ) ) ;
#98636=CARTESIAN_POINT ( 'NONE',  ( 6.410779360540267646, 1.349177972556347971, -1.230185023894624141 ) ) ;
#98637=CARTESIAN_POINT ( 'NONE',  ( 4.733228419949464971, 0.004064956161661801778, -1.961936380062332397 ) ) ;
#98640=CARTESIAN_POINT ( 'NONE',  ( 4.653055333535057514, 0.3633016933833124185, 2.088981207656291250 ) ) ;
#98641=CARTESIAN_POINT ( 'NONE',  ( 4.054362073078698891, -1.623213109359676443, 1.472610181411204922 ) ) ;
#98645=CARTESIAN_POINT ( 'NONE',  ( 2.413015750098276513, -1.603085927076562500, 1.310038033242977518 ) ) ;
#98649=CARTESIAN_POINT ( 'NONE',  ( 3.041888879667261403, -1.739239095176773775, 1.503071639953108773 ) ) ;
#98653=CARTESIAN_POINT ( 'NONE',  ( 6.720655732516647163, 3.705577233864749687, 2.340827588962008488 ) ) ;
#98659=CARTESIAN_POINT ( 'NONE',  ( 4.535362393419643645, -0.08824616237496611670, 1.910463848342447202 ) ) ;
#98661=CARTESIAN_POINT ( 'NONE',  ( 4.981344092214620822, 1.608381032133517019, -0.6233497484429885160 ) ) ;
#98662=CARTESIAN_POINT ( 'NONE',  ( 3.098842478760281516, 1.825076540557273974, 0.8578426345753201732 ) ) ;
#98663=CARTESIAN_POINT ( 'NONE',  ( 5.467524615204178318, -2.242144116172717361, -0.5062228086629757540 ) ) ;
#98665=CARTESIAN_POINT ( 'NONE',  ( 1.137671262558290763, -1.993743905544292927, 0.9465009238469668240 ) ) ;
#98667=CARTESIAN_POINT ( 'NONE',  ( 6.151566388294868126, 0.5118450565497618676, -1.694058711534670358 ) ) ;
#98669=CARTESIAN_POINT ( 'NONE',  ( 2.098001248608129199, -2.291667096838309270, 0.05881920129262825647 ) ) ;
#98670=CARTESIAN_POINT ( 'NONE',  ( 6.421814705521882161, 1.055779539018763646, -1.508159643570324393 ) ) ;
#98675=CARTESIAN_POINT ( 'NONE',  ( 6.654741963219192868, -0.5482099483974657295, -1.996413779700876301 ) ) ;
#98676=CARTESIAN_POINT ( 'NONE',  ( 2.466030083290056130, -1.032479112849067793, 1.731996155473938259 ) ) ;
#98678=CARTESIAN_POINT ( 'NONE',  ( 5.865835041973252117, 1.897565194821029033, -0.3318024074076031948 ) ) ;
#98680=CARTESIAN_POINT ( 'NONE',  ( 2.162617739553638785, 2.221014589654236371, 0.04931172913892957477 ) ) ;
#98687=CARTESIAN_POINT ( 'NONE',  ( 5.038483826543846078, -1.489082695810162837, 0.9007512145987550678 ) ) ;
#98688=CARTESIAN_POINT ( 'NONE',  ( 3.683996026499200660, -1.166640140252427793, -1.577160851978461009 ) ) ;
#98693=CARTESIAN_POINT ( 'NONE',  ( 4.552213317786341307, 2.262020173471789963, -0.04951151886351152359 ) ) ;
#98694=CARTESIAN_POINT ( 'NONE',  ( 1.416547059616825699, 0.8341270235591256021, 1.886661834507087798 ) ) ;
#98697=CARTESIAN_POINT ( 'NONE',  ( 1.885968558009487595, 1.560753693757486849, 1.638220756346415508 ) ) ;
#98700=CARTESIAN_POINT ( 'NONE',  ( 2.213927045526514537, -0.8776910013945339317, -1.651823421649289081 ) ) ;
#98701=CARTESIAN_POINT ( 'NONE',  ( 1.582203977811939000, -0.5845794355729941882, 1.632800797419992955 ) ) ;
#98702=CARTESIAN_POINT ( 'NONE',  ( 5.302338810847701644, 1.659911028786088538, -1.431018553749352051 ) ) ;
#98703=CARTESIAN_POINT ( 'NONE',  ( 6.633790087849154027, -1.500048720590658302, -1.753619728580549708 ) ) ;
#98704=CARTESIAN_POINT ( 'NONE',  ( 0.9716393833266089297, 1.986344416073432484, -0.5490401152750885583 ) ) ;
#98705=CARTESIAN_POINT ( 'NONE',  ( 4.171774378167571129, -1.117019396711134371, 1.588354668226848565 ) ) ;
#98708=CARTESIAN_POINT ( 'NONE',  ( 6.257094453949625823, -1.604276942902042480, -0.9616840659161308702 ) ) ;
#98709=CARTESIAN_POINT ( 'NONE',  ( 0.7187500000000003331, -0.7852924748299483504, 1.895863743164105220 ) ) ;
#98711=CARTESIAN_POINT ( 'NONE',  ( 6.837263156049210089, -1.242709075549037312, 1.588189626643407681 ) ) ;
#98714=CARTESIAN_POINT ( 'NONE',  ( 5.994767569012836361, -2.000857541758268354, 0.2496038112331094849 ) ) ;
#98718=CARTESIAN_POINT ( 'NONE',  ( 2.578497204056416692, -1.747032809129964503, -0.5301130021647950663 ) ) ;
#98725=CARTESIAN_POINT ( 'NONE',  ( 0.2639333133152200750, 0.6296502125625064172, -1.919233096100453118 ) ) ;
#98726=CARTESIAN_POINT ( 'NONE',  ( 0.4520119014386895229, -1.502510013782244025, -1.496567369470555020 ) ) ;
#98731=CARTESIAN_POINT ( 'NONE',  ( 0.1280963075596490419, -1.331634228802502928, -1.703589906866372017 ) ) ;
#98732=CARTESIAN_POINT ( 'NONE',  ( 4.799454022740247794, 1.388487131293577592, -1.462444391756134943 ) ) ;
#98734=ORIENTED_EDGE ( 'NONE', *, *, #32479, .T. ) ;
#98741=CARTESIAN_POINT ( 'NONE',  ( 5.202499893966790800, -1.423744420606623429, -1.427717849564233532 ) ) ;
#98742=CARTESIAN_POINT ( 'NONE',  ( 4.681507052731401330, -0.8653998779965512700, 1.625073734443114759 ) ) ;
#98744=CARTESIAN_POINT ( 'NONE',  ( 3.123938245303990335, -2.224009237659807958, 0.6155878327348850432 ) ) ;
#98747=CARTESIAN_POINT ( 'NONE',  ( 6.204392391313840349, -0.7715976231806520591, -2.019385000091134419 ) ) ;
#98749=CARTESIAN_POINT ( 'NONE',  ( 1.558044835347382362, -1.372074245553561722, 1.374660786877460072 ) ) ;
#98752=CARTESIAN_POINT ( 'NONE',  ( 4.886215977948979550, -0.1196125283245419307, 2.295398719017431866 ) ) ;
#98755=CARTESIAN_POINT ( 'NONE',  ( 2.992876365407059147, 1.605230647100181596, -0.9602576221170722182 ) ) ;
#98757=CARTESIAN_POINT ( 'NONE',  ( 1.459083999156213451, -1.613880964290700160, 1.025699646091532857 ) ) ;
#98760=CARTESIAN_POINT ( 'NONE',  ( 2.508667999599442755, -0.8457060194008919618, -2.038605049697986615 ) ) ;
#98762=CARTESIAN_POINT ( 'NONE',  ( -0.1394461523061352182, -0.009327122704730076569, -2.280146446826668782 ) ) ;
#98767=CARTESIAN_POINT ( 'NONE',  ( 0.7550724807275938089, -1.663022853828221681, -1.058333363951379003 ) ) ;
#98768=CARTESIAN_POINT ( 'NONE',  ( 0.2183775786483640735, -2.262126603235939282, 0.4550015798871313577 ) ) ;
#98769=CARTESIAN_POINT ( 'NONE',  ( 1.644895634054041933, -0.2845770130874228365, -1.940982728367894206 ) ) ;
#98771=CARTESIAN_POINT ( 'NONE',  ( 4.926661567281545473, -1.351126562560464484, 1.558462338037209349 ) ) ;
#98779=CARTESIAN_POINT ( 'NONE',  ( 0.6905673677243575614, 1.117554423744430592, -1.861242299804190869 ) ) ;
#98781=CARTESIAN_POINT ( 'NONE',  ( 5.829618728418341611, 0.9018330327132916269, -1.605192750430362025 ) ) ;
#98784=CARTESIAN_POINT ( 'NONE',  ( 1.317418832401914930, -1.826178791559311509, 0.4043020138455517554 ) ) ;
#98785=CARTESIAN_POINT ( 'NONE',  ( 5.800121417639972243, -2.161773191644947634, -0.006422599366645573467 ) ) ;
#98789=CARTESIAN_POINT ( 'NONE',  ( 1.189939518123926510, 1.139724415472416652, 1.535358521287055300 ) ) ;
#98790=CARTESIAN_POINT ( 'NONE',  ( 3.221328931188462086, -1.705978018192667811, 0.4708956190180821344 ) ) ;
#98792=CARTESIAN_POINT ( 'NONE',  ( 0.6801455168885979230, 0.9429141125626202546, 1.663586755705208420 ) ) ;
#98794=CARTESIAN_POINT ( 'NONE',  ( 5.993738795899758998, -1.900512161056673088, 0.2395553810000446704 ) ) ;
#98795=CARTESIAN_POINT ( 'NONE',  ( 6.092246201825009422, 0.9720536035879873138, -1.712898845271645820 ) ) ;
#98797=CARTESIAN_POINT ( 'NONE',  ( 0.8969213510382867405, -2.070190491330957006, -0.4589741369691033857 ) ) ;
#98799=CARTESIAN_POINT ( 'NONE',  ( 3.819104250046548632, -0.1383300533824398659, 1.865606469731183825 ) ) ;
#98800=CARTESIAN_POINT ( 'NONE',  ( 0.6272434487209905818, -1.734552980249819631, 0.5698080454362154379 ) ) ;
#98802=CARTESIAN_POINT ( 'NONE',  ( 4.178501018151202118, -1.271701901513167421, 1.803451139310302986 ) ) ;
#98805=CARTESIAN_POINT ( 'NONE',  ( 2.207554788950978786, -1.655329399669298818, -1.230451883716067174 ) ) ;
#98811=CARTESIAN_POINT ( 'NONE',  ( 0.1753634416057732182, 7.629137130509072051, -2.744001747789548418 ) ) ;
#98813=CARTESIAN_POINT ( 'NONE',  ( 4.633297751427938316, 0.003287558298453730800, -2.070544812459538253 ) ) ;
#98815=CARTESIAN_POINT ( 'NONE',  ( 0.9839146201040609441, 1.450980403326153301, 1.602422216231303320 ) ) ;
#98817=CARTESIAN_POINT ( 'NONE',  ( 1.893228994919902153, -0.1012422250811425839, -2.017274448259358977 ) ) ;
#98826=CARTESIAN_POINT ( 'NONE',  ( -0.06521966986864842497, -1.616690375843790051, 1.205047459138554045 ) ) ;
#98827=CARTESIAN_POINT ( 'NONE',  ( 6.639320575229257670, 2.427506520031021520, 2.484945200759064665 ) ) ;
#98828=CARTESIAN_POINT ( 'NONE',  ( 4.581673536070863584, -1.032772929490553215, 1.932928240684625099 ) ) ;
#98830=CARTESIAN_POINT ( 'NONE',  ( 3.533378866418676711, -0.1359047358975660202, 1.907598245988059826 ) ) ;
#98834=CARTESIAN_POINT ( 'NONE',  ( 1.792592436991577109, 1.492242793082170449, -1.356315429364700176 ) ) ;
#98836=CARTESIAN_POINT ( 'NONE',  ( 0.2754559168597633390, 2.135984121793169432, -0.8326521888945382921 ) ) ;
#98838=CARTESIAN_POINT ( 'NONE',  ( 4.137519252912919221, -1.190027120290118257, -1.248710780074323567 ) ) ;
#98842=CARTESIAN_POINT ( 'NONE',  ( 0.07479286986305370977, 0.004866263145587856019, -1.855573292446038414 ) ) ;
#98844=CARTESIAN_POINT ( 'NONE',  ( 0.07516593201273635838, 1.359561921253334749, -2.300590921312398951 ) ) ;
#98847=CARTESIAN_POINT ( 'NONE',  ( 5.057183878474817540, -1.550805960166462105, 0.9359391756664036111 ) ) ;
#98851=CARTESIAN_POINT ( 'NONE',  ( 5.672461423068217989, 0.7400952288921599509, 1.653588109013460095 ) ) ;
#98854=CARTESIAN_POINT ( 'NONE',  ( 2.466951935624495551, 0.1062163371072753354, -2.188993582743845590 ) ) ;
#98855=CARTESIAN_POINT ( 'NONE',  ( 6.267989458847986306, -1.846849288558198188, 0.2287129521939580412 ) ) ;
#98857=CARTESIAN_POINT ( 'NONE',  ( 3.761272268043499345, 1.802513535502557218, -0.6487917036162252904 ) ) ;
#98863=CARTESIAN_POINT ( 'NONE',  ( 5.313701412219064224, -1.345319185855331279, -1.634962184252206630 ) ) ;
#98864=CARTESIAN_POINT ( 'NONE',  ( 0.7608789386071808103, -1.564954856162886765, 1.491513986042219297 ) ) ;
#98867=CARTESIAN_POINT ( 'NONE',  ( 1.078802750678783395, -0.04027803099338270881, -1.825304540826321542 ) ) ;
#98869=CARTESIAN_POINT ( 'NONE',  ( 4.102439050647597618, -0.5725816820084869141, -1.733541218493547476 ) ) ;
#98872=CARTESIAN_POINT ( 'NONE',  ( 2.558991062574625275, 1.583523548174452733, -1.170949712736363502 ) ) ;
#98874=CARTESIAN_POINT ( 'NONE',  ( 4.651864714057460048, 0.7465859729765094155, 1.793013943324140769 ) ) ;
#98877=CARTESIAN_POINT ( 'NONE',  ( 5.133110336712339183, 1.960249873928998410, 0.8093987030339530042 ) ) ;
#98880=CARTESIAN_POINT ( 'NONE',  ( 2.982959643696237784, -1.767753630637520779, -0.7297678730374329570 ) ) ;
#98885=CARTESIAN_POINT ( 'NONE',  ( 4.108068219531130438, -0.7683648849950328596, 1.860876229713221086 ) ) ;
#98887=CARTESIAN_POINT ( 'NONE',  ( 5.303274670167754223, 1.494737065598227943, 1.048009559513597866 ) ) ;
#98888=CARTESIAN_POINT ( 'NONE',  ( 0.7661813929631040576, -2.060537521029872643, 0.2012509062776293156 ) ) ;
#98892=CARTESIAN_POINT ( 'NONE',  ( 5.717618200960680852, -1.824738551054584379, 0.4112096411929695439 ) ) ;
#98902=CARTESIAN_POINT ( 'NONE',  ( 6.631686460494314872, 2.080164978358085559, -0.6217935382996344629 ) ) ;
#98903=CARTESIAN_POINT ( 'NONE',  ( 1.863061375884986104, -0.1076188601273372486, -2.114627633294167364 ) ) ;
#98907=CARTESIAN_POINT ( 'NONE',  ( 6.508651864089095795, 0.6437109847576475419, 1.967739590238902991 ) ) ;
#98912=CARTESIAN_POINT ( 'NONE',  ( 2.818655624875044285, 2.158736131429010996, 0.7712820022114060814 ) ) ;
#98915=CARTESIAN_POINT ( 'NONE',  ( 2.777492966359981441, 0.2764497561681695803, -1.892163382976944419 ) ) ;
#98918=CARTESIAN_POINT ( 'NONE',  ( 0.7385399849154888896, 1.195762776690506790, -1.619497776973168213 ) ) ;
#98919=CARTESIAN_POINT ( 'NONE',  ( 1.006607400890747295, 0.5640878064397096825, 1.878940696355746454 ) ) ;
#98923=CARTESIAN_POINT ( 'NONE',  ( 3.644548676374514518, -1.708972400646594503, 1.203939368798632836 ) ) ;
#98924=CARTESIAN_POINT ( 'NONE',  ( 2.184116879877880724, -1.735013770989551896, -0.3484325113714877298 ) ) ;
#98926=CARTESIAN_POINT ( 'NONE',  ( 5.806620824396801162, 2.019002025885249463, 1.085389930784508961 ) ) ;
#98927=CARTESIAN_POINT ( 'NONE',  ( 4.874825007975835511, 1.622202256106145102, -0.6307315249329782381 ) ) ;
#98931=CARTESIAN_POINT ( 'NONE',  ( 3.110371403566422277, 0.6269696901312575843, -1.616694140604297614 ) ) ;
#98932=CARTESIAN_POINT ( 'NONE',  ( 4.316952289276101418, -1.611618797226920252, 1.455085969030824211 ) ) ;
#98934=CARTESIAN_POINT ( 'NONE',  ( 5.419157771004846857, -1.820987890746316173, 0.8666037247077316152 ) ) ;
#98935=CARTESIAN_POINT ( 'NONE',  ( 0.09375222243388467436, -1.895918425137008034, -0.7852924748299833224 ) ) ;
#98938=CARTESIAN_POINT ( 'NONE',  ( 1.887598533328225692, 1.326653652590740418, 1.397000115363009609 ) ) ;
#98940=CARTESIAN_POINT ( 'NONE',  ( 5.748318879583719010, 1.095320496750437966, -1.932492775422405717 ) ) ;
#98942=CARTESIAN_POINT ( 'NONE',  ( 6.983263157960366563, 2.432509251381759441, 2.428019605373044509 ) ) ;
#98946=CARTESIAN_POINT ( 'NONE',  ( 6.496542546517183325, 1.940334402339534581, 0.2891159199209930031 ) ) ;
#98954=CARTESIAN_POINT ( 'NONE',  ( 4.387212324874685265, 0.09821595252585722802, 2.060445151624993976 ) ) ;
#98958=CARTESIAN_POINT ( 'NONE',  ( 5.694569522353672753, -0.4537686991618712362, -1.814561337198366875 ) ) ;
#98959=CARTESIAN_POINT ( 'NONE',  ( 4.869590383887318019, -0.2189826452120811340, -1.720196969245034513 ) ) ;
#98960=CARTESIAN_POINT ( 'NONE',  ( 4.440767568709752311, -1.349020001278607550, -1.099687749275481741 ) ) ;
#98962=CARTESIAN_POINT ( 'NONE',  ( 1.787097420474514031, 1.992035690054320574, -1.134270899834391999 ) ) ;
#98964=CARTESIAN_POINT ( 'NONE',  ( 5.812080397998875547, 1.403551008015807788, -1.549792465900756477 ) ) ;
#98965=CARTESIAN_POINT ( 'NONE',  ( 0.6734667703603390843, -1.024904740748554532, 1.529287851792550335 ) ) ;
#98968=CARTESIAN_POINT ( 'NONE',  ( 2.830704105008190030, 0.7231396562890278767, -1.882474209725725434 ) ) ;
#98969=CARTESIAN_POINT ( 'NONE',  ( 0.7619990552875830492, 1.083242598816274382, 1.904929396514772444 ) ) ;
#98972=CARTESIAN_POINT ( 'NONE',  ( 1.363825363374836286, -0.5049007678423790280, 2.007717453658082629 ) ) ;
#98975=CARTESIAN_POINT ( 'NONE',  ( 3.985108911058360182, -1.979049277059058864, -0.7619450576143712572 ) ) ;
#98977=CARTESIAN_POINT ( 'NONE',  ( 5.479063914364931343, -0.04889757770590653918, -1.825204647902956889 ) ) ;
#98984=CARTESIAN_POINT ( 'NONE',  ( 3.726823374262774990, 1.425363347867984798, -1.431309510556647346 ) ) ;
#98985=CARTESIAN_POINT ( 'NONE',  ( 6.510767885691055135, 1.639592601025055885, -1.477219212978691409 ) ) ;
#98988=CARTESIAN_POINT ( 'NONE',  ( 4.785918264633797214, -1.142728415277466159, -1.468712688171626812 ) ) ;
#98993=CARTESIAN_POINT ( 'NONE',  ( 0.3390366800232989530, 0.3710982241871863541, 2.129449491308422537 ) ) ;
#98997=CARTESIAN_POINT ( 'NONE',  ( 2.108352191060134828, 0.6683163022180199642, -1.600079515618204606 ) ) ;
#98998=CARTESIAN_POINT ( 'NONE',  ( 0.8490573499697011695, 1.738566659290440963, -0.08130723561216267326 ) ) ;
#98999=CARTESIAN_POINT ( 'NONE',  ( 0.2886476729930695373, -1.083662648423104891, 2.037333779670726930 ) ) ;
#99002=CARTESIAN_POINT ( 'NONE',  ( 2.389980588989379040, -0.8839831138988951675, 1.861718010716238547 ) ) ;
#99004=CARTESIAN_POINT ( 'NONE',  ( 0.9310172746952742884, 0.9912447863934905623, 1.755501862388042067 ) ) ;
#99007=CARTESIAN_POINT ( 'NONE',  ( 6.789956943122251509, -0.7972922127613899512, 1.690610701080223821 ) ) ;
#99008=CARTESIAN_POINT ( 'NONE',  ( 5.168181644781757456, 1.909928461159452251, -0.09994665148223277895 ) ) ;
#99010=CARTESIAN_POINT ( 'NONE',  ( 6.481111342790009999, -0.1036386110354891726, -2.204582208980155222 ) ) ;
#99014=CARTESIAN_POINT ( 'NONE',  ( 0.4869804533438352734, -1.902474711392083684, -0.6784070981462678729 ) ) ;
#99017=CARTESIAN_POINT ( 'NONE',  ( 4.225798673374229431, -2.209433879803673673, 0.6658836873896284425 ) ) ;
#99018=CARTESIAN_POINT ( 'NONE',  ( 4.457442142980160504, 1.574409630067734156, 1.170308293268598421 ) ) ;
#99020=CARTESIAN_POINT ( 'NONE',  ( 1.727322521004183598, 0.1496332796787832875, -1.956138870750294023 ) ) ;
#99024=CARTESIAN_POINT ( 'NONE',  ( 6.473846665049121540, -0.8576149079453172508, 1.823233050095712349 ) ) ;
#99027=CARTESIAN_POINT ( 'NONE',  ( 1.394213304513430174, 1.506067903837378097, -1.058747118707924262 ) ) ;
#99029=CARTESIAN_POINT ( 'NONE',  ( 4.557605255626766549, 1.740051450181074877, 1.298158460866901454 ) ) ;
#99032=CARTESIAN_POINT ( 'NONE',  ( 2.092179824929023102, 1.308410154019133076, 1.668721082780571408 ) ) ;
#99036=CARTESIAN_POINT ( 'NONE',  ( 2.548181945144313953, 2.060261615984103400, 0.05380422017278729124 ) ) ;
#99040=CARTESIAN_POINT ( 'NONE',  ( 0.07735805125222078305, -0.0005418671161615954465, -2.088975025666544472 ) ) ;
#99041=EDGE_CURVE ( 'NONE', #15524, #36822, #114429, .T. ) ;
#99043=CARTESIAN_POINT ( 'NONE',  ( 5.443983014310386892, -1.216401775450553169, -1.475513148251464068 ) ) ;
#99045=CARTESIAN_POINT ( 'NONE',  ( 1.845381457188604690, -1.911753278855784943, 1.209540087214598270 ) ) ;
#99047=CARTESIAN_POINT ( 'NONE',  ( 1.054613590283080660, 0.3547985653672180439, 1.776302104178028252 ) ) ;
#99048=CARTESIAN_POINT ( 'NONE',  ( 1.762754532109143124, -0.09793373165993285445, -1.913366418544469205 ) ) ;
#99049=CARTESIAN_POINT ( 'NONE',  ( 3.473154722801426786, 1.870513717286937494, 0.8877811045280564750 ) ) ;
#99051=CARTESIAN_POINT ( 'NONE',  ( 1.446098081747126951, 1.969109070040415910, 0.09893570862591105630 ) ) ;
#99052=CARTESIAN_POINT ( 'NONE',  ( 5.074797080785846681, -1.814676937445957039, -0.6471642872378483569 ) ) ;
#99053=CARTESIAN_POINT ( 'NONE',  ( 1.454236823263599376, 0.6660240913333862478, -2.209497540817098038 ) ) ;
#99056=CARTESIAN_POINT ( 'NONE',  ( 5.494603814743470593, 2.031562770168824361, 0.3561260095714424700 ) ) ;
#99060=CARTESIAN_POINT ( 'NONE',  ( 6.651405291617982662, -1.688965747674558759, -1.257743519153362355 ) ) ;
#99064=CARTESIAN_POINT ( 'NONE',  ( 5.255217470067075070, -1.823004960263453489, -1.161262906855420329 ) ) ;
#99065=CARTESIAN_POINT ( 'NONE',  ( 5.145178147197468022, 0.1505999202349363186, 2.014131245181075336 ) ) ;
#99067=PLANE ( 'NONE',  #18269 ) ;
#99074=CARTESIAN_POINT ( 'NONE',  ( 3.450407915430803385, -1.350735839785843773, 1.497501794165828626 ) ) ;
#99080=CARTESIAN_POINT ( 'NONE',  ( 5.120075222393803749, -1.153228217640640985, -1.828211184805514922 ) ) ;
#99085=CARTESIAN_POINT ( 'NONE',  ( 5.378529868213833609, -0.4926607797600784933, -1.955169007017331317 ) ) ;
#99087=CARTESIAN_POINT ( 'NONE',  ( 1.189626395179286478, -0.7786649258869399182, 1.539184141221685787 ) ) ;
#99092=CARTESIAN_POINT ( 'NONE',  ( 0.2800358821246723418, -1.714356997462190835, -0.4388462949536375279 ) ) ;
#99093=CARTESIAN_POINT ( 'NONE',  ( 0.3639315877056762405, 0.6293089562653730873, -1.912281478549708202 ) ) ;
#99094=CARTESIAN_POINT ( 'NONE',  ( 6.539320575229250920, 3.702490941164796379, 2.411252750440337156 ) ) ;
#99098=CARTESIAN_POINT ( 'NONE',  ( 2.121885542695590487, -0.4617877489709980576, 2.069441001874790409 ) ) ;
#99099=CARTESIAN_POINT ( 'NONE',  ( 1.599232692168949699, -0.2440074622011619843, 2.001515180871694888 ) ) ;
#99100=CARTESIAN_POINT ( 'NONE',  ( 2.250024469429566132, 0.8508988043372580634, -1.599271047475413932 ) ) ;
#99102=CARTESIAN_POINT ( 'NONE',  ( 6.403215362905616992, 1.794359850238020693, 1.205212418099836480 ) ) ;
#99107=CARTESIAN_POINT ( 'NONE',  ( 0.6377201071205064187, 1.913410132493647442, -0.09706281964840141052 ) ) ;
#99115=CARTESIAN_POINT ( 'NONE',  ( 4.030267251519312310, 1.158562084521784108, -1.824840551714689507 ) ) ;
#99118=CARTESIAN_POINT ( 'NONE',  ( 2.408575119285644384, -2.115224228095522907, -0.1514441693673748146 ) ) ;
#99119=CARTESIAN_POINT ( 'NONE',  ( 6.458013382736495167, 1.820430347099718293, -0.1376817787434730933 ) ) ;
#99120=CARTESIAN_POINT ( 'NONE',  ( 2.882053135459626159, -1.016639628983921684, 1.688880165396142718 ) ) ;
#99121=CARTESIAN_POINT ( 'NONE',  ( 5.765855477156511810, 0.5488314196105298359, -1.831976909803390896 ) ) ;
#99124=CARTESIAN_POINT ( 'NONE',  ( 6.514111218838506190, 1.964378047669375293, -0.1432920118879192073 ) ) ;
#99126=CARTESIAN_POINT ( 'NONE',  ( 1.763517528630250686, 0.9983118466501934574, 1.665567687315899992 ) ) ;
#99131=CARTESIAN_POINT ( 'NONE',  ( 2.308638494240814687, 1.867967618895223447, 0.9389952993345984655 ) ) ;
#99135=CARTESIAN_POINT ( 'NONE',  ( 6.041656841763191288, -1.799011877964010520, 0.6487133288125003228 ) ) ;
#99137=CARTESIAN_POINT ( 'NONE',  ( 4.108205984530819421, -2.201057848371779535, 0.1611738814469021175 ) ) ;
#99138=CARTESIAN_POINT ( 'NONE',  ( 2.028631293930313717, 1.270571802522667992, -1.804104215285810886 ) ) ;
#99140=CARTESIAN_POINT ( 'NONE',  ( 0.9965660710522583621, -1.865815080690262917, -0.4182784585613218420 ) ) ;
#99143=CARTESIAN_POINT ( 'NONE',  ( 4.686024408448190570, -1.271122505372159761, -1.634150330299996012 ) ) ;
#99146=CARTESIAN_POINT ( 'NONE',  ( 2.167066695894452888, -1.976221826324360498, -0.8764929760368763700 ) ) ;
#99147=CARTESIAN_POINT ( 'NONE',  ( 3.140350738262797314, 0.5347024899306859202, 2.125194831261326911 ) ) ;
#99153=CARTESIAN_POINT ( 'NONE',  ( 6.065060216814489813, -0.9193275656586662459, 1.470200510888696632 ) ) ;
#99155=CARTESIAN_POINT ( 'NONE',  ( 4.662978783614929235, 1.603679166536524869, -1.309313232293010776 ) ) ;
#99156=CARTESIAN_POINT ( 'NONE',  ( 5.237957716521472129, 2.114759263080950635, -0.1049963987776857816 ) ) ;
#99159=CARTESIAN_POINT ( 'NONE',  ( 3.379706166375577414, -1.899257087701329949, 0.5209217831910922802 ) ) ;
#99160=CARTESIAN_POINT ( 'NONE',  ( 5.929661055573363981, 1.134796830042347660, -1.991584109881129327 ) ) ;
#99161=CARTESIAN_POINT ( 'NONE',  ( 3.053144290054691901, -1.492835736363472110, -1.050712463094093385 ) ) ;
#99167=CARTESIAN_POINT ( 'NONE',  ( 4.113543134289789016, 1.619545278408863975, 1.195698625712667384 ) ) ;
#99168=CARTESIAN_POINT ( 'NONE',  ( 4.346505277090593644, -1.939800950321630690, -0.2920161945778113055 ) ) ;
#99173=CARTESIAN_POINT ( 'NONE',  ( 0.4860219701983969909, -2.075441973172939214, -0.2518264690121001514 ) ) ;
#99174=CARTESIAN_POINT ( 'NONE',  ( 6.121911923048983795, -0.9866791243483238327, -1.469064191006617337 ) ) ;
#99176=CARTESIAN_POINT ( 'NONE',  ( 1.412352946837617473, 1.469754387505791460, -1.625674263109680329 ) ) ;
#99177=CARTESIAN_POINT ( 'NONE',  ( 0.8897394992621279197, -0.4213058873485018840, -1.688518545418623340 ) ) ;
#99179=CARTESIAN_POINT ( 'NONE',  ( 0.1335669894368864408, 5.721243636067999461, -2.747585559332069494 ) ) ;
#99180=CARTESIAN_POINT ( 'NONE',  ( 2.033451192367647042, -1.125475165956592694, -1.307177254964901003 ) ) ;
#99181=CARTESIAN_POINT ( 'NONE',  ( 1.089736160853293168, 1.367490553916232754, -1.847165887925501515 ) ) ;
#99183=CARTESIAN_POINT ( 'NONE',  ( 0.02921319935947005314, -2.001080581411585513, 0.8940957790435491992 ) ) ;
#99184=CARTESIAN_POINT ( 'NONE',  ( -0.03512515232485542011, -1.681152455970882809, -0.4250410675877940303 ) ) ;
#99185=CARTESIAN_POINT ( 'NONE',  ( 3.405080638938757343, 1.739790774466195789, -1.357627211771177178 ) ) ;
#99186=CARTESIAN_POINT ( 'NONE',  ( 1.006951398661716901, 0.6282198290366995952, 2.078224816918782025 ) ) ;
#99188=CARTESIAN_POINT ( 'NONE',  ( 1.921263159425983913, -1.888806403119867916, 0.9570566162820994816 ) ) ;
#99189=CARTESIAN_POINT ( 'NONE',  ( 6.727182134110222478, 7.629137130509071163, 2.789055895399249252 ) ) ;
#99190=CARTESIAN_POINT ( 'NONE',  ( 5.825206220505295462, -0.04701585971965925592, 1.925982856303788182 ) ) ;
#99192=CARTESIAN_POINT ( 'NONE',  ( 2.191363998320290385, 1.774703082125920428, 1.451028844865470901 ) ) ;
#99197=CARTESIAN_POINT ( 'NONE',  ( 5.215582523826345351, 1.815199501411597582, 1.280085896050622507 ) ) ;
#99206=CARTESIAN_POINT ( 'NONE',  ( 2.795546247670523954, 1.458556481301529706, -1.392545902517070111 ) ) ;
#99208=CARTESIAN_POINT ( 'NONE',  ( 1.428664617098963863, -1.311459235982143534, 1.591897985181329966 ) ) ;
#99213=CARTESIAN_POINT ( 'NONE',  ( 3.714928722721734911, -0.1615716889580356697, 2.185543052782303874 ) ) ;
#99214=CARTESIAN_POINT ( 'NONE',  ( 1.125625214514534900, 0.3961039030971893471, 1.976955501819408711 ) ) ;
#99215=CARTESIAN_POINT ( 'NONE',  ( 1.364538772237647413, 0.1349417713633893900, -1.836341338755695940 ) ) ;
#99216=CARTESIAN_POINT ( 'NONE',  ( 4.470543924053159479, -0.002573283451708791025, -1.841320590191763973 ) ) ;
#99219=CARTESIAN_POINT ( 'NONE',  ( 4.735264887803245060, -1.668767028523497675, 0.7406363711058363553 ) ) ;
#99220=CARTESIAN_POINT ( 'NONE',  ( 5.871720251644387822, -0.2986239867289949834, -1.994071864161291119 ) ) ;
#99222=CARTESIAN_POINT ( 'NONE',  ( 4.276442053719103242, -1.305714526237568229, 1.847550228136185302 ) ) ;
#99224=CARTESIAN_POINT ( 'NONE',  ( 0.5046868689226053917, -0.7117215327378585421, -1.982300686916990573 ) ) ;
#99226=CARTESIAN_POINT ( 'NONE',  ( 4.299325596424930396, -1.802881993240162961, 1.017688063649782482 ) ) ;
#99236=CARTESIAN_POINT ( 'NONE',  ( 0.9320672075895162223, -2.067649466203642206, 0.4702014512557165515 ) ) ;
#99237=CARTESIAN_POINT ( 'NONE',  ( 1.740793075861684303, 1.274151022659695709, -1.819517169034337467 ) ) ;
#99241=CARTESIAN_POINT ( 'NONE',  ( 2.875390130891414042, -0.1950805366632331617, 1.952157403750237163 ) ) ;
#99248=CARTESIAN_POINT ( 'NONE',  ( 2.232824136269210502, 1.381628265877183903, -1.608862310199298928 ) ) ;
#99250=CARTESIAN_POINT ( 'NONE',  ( 4.756279191188107269, -1.961398630904508833, -0.05015466537350299348 ) ) ;
#99251=CARTESIAN_POINT ( 'NONE',  ( 2.782270202741622178, -1.112240752214749273, 1.853481441253836071 ) ) ;
#99252=CARTESIAN_POINT ( 'NONE',  ( 2.718100415690410721, 1.734538518968967935, 0.6181264464550640936 ) ) ;
#99255=CARTESIAN_POINT ( 'NONE',  ( 4.646296158022299672, -1.395249218123927104, 1.039982334504330197 ) ) ;
#99260=CARTESIAN_POINT ( 'NONE',  ( 1.340939272977889951, 0.4221563536682856332, 2.119910705745978508 ) ) ;
#99261=CARTESIAN_POINT ( 'NONE',  ( 4.165388622617651748, -0.6297791189726584804, -1.915306643112117291 ) ) ;
#99263=CARTESIAN_POINT ( 'NONE',  ( 1.551884642779034262, 0.6273040060550126862, -2.068667048528524344 ) ) ;
#99264=CARTESIAN_POINT ( 'NONE',  ( 3.326987498081665162, 0.04702425985559504501, 1.971060134238045602 ) ) ;
#99265=CARTESIAN_POINT ( 'NONE',  ( 2.671113287583181339, 0.1005484070672260644, -1.968930098583418387 ) ) ;
#99266=CARTESIAN_POINT ( 'NONE',  ( 6.509000000000021657, 1.267728212239338959, 2.115804336118334295 ) ) ;
#99267=CARTESIAN_POINT ( 'NONE',  ( 3.368632357871951033, 0.04486925901568206143, -1.941695523777670740 ) ) ;
#99276=CARTESIAN_POINT ( 'NONE',  ( 1.132168909276673796, -1.401036632855560349, -1.704990472574128502 ) ) ;
#99279=CARTESIAN_POINT ( 'NONE',  ( 5.647302737930705696, 1.731814717071546772, -0.9215059220915235993 ) ) ;
#99281=CARTESIAN_POINT ( 'NONE',  ( 3.327469932021313692, -1.606305723110455608, -1.379610029357878798 ) ) ;
#99283=CARTESIAN_POINT ( 'NONE',  ( 0.07479286986305369589, 0.2526433113205875935, -1.890777245541554574 ) ) ;
#99285=CARTESIAN_POINT ( 'NONE',  ( 4.013478867934616723, -0.9481684062532383939, -1.578073411074693899 ) ) ;
#99289=CARTESIAN_POINT ( 'NONE',  ( 5.062787373817618786, 0.6179034821891697948, 2.028544477791139222 ) ) ;
#99292=CARTESIAN_POINT ( 'NONE',  ( 5.712203248095857333, -0.9225367590200548307, -1.842806303608224949 ) ) ;
#99294=CARTESIAN_POINT ( 'NONE',  ( 0.6251817401201573698, 0.1879592460329523318, -1.851551742960926727 ) ) ;
#99295=CARTESIAN_POINT ( 'NONE',  ( 1.979791773625012352, -1.805961398883266344, -0.3578489297004632808 ) ) ;
#99301=CARTESIAN_POINT ( 'NONE',  ( 3.106307083854151774, -2.204334110825040494, 0.1085914373066959593 ) ) ;
#99302=CARTESIAN_POINT ( 'NONE',  ( 4.604895111943496211, 1.752856212930454127, -1.430419756957083566 ) ) ;
#99304=CARTESIAN_POINT ( 'NONE',  ( 4.447391390197759975, -1.653601938829275975, 0.7403539279892316083 ) ) ;
#99305=CARTESIAN_POINT ( 'NONE',  ( 5.559766488213514712, 1.146785110015311915, 1.534377285673252267 ) ) ;
#99307=CARTESIAN_POINT ( 'NONE',  ( 5.067206508511894469, 0.1826785619755930679, -1.861722072867748823 ) ) ;
#99308=CARTESIAN_POINT ( 'NONE',  ( 4.932013296703669170, 1.071099452130529039, 1.521725064211083112 ) ) ;
#99310=CARTESIAN_POINT ( 'NONE',  ( 6.139478286200317214, -1.284810642169451622, -1.217457132491184035 ) ) ;
#99311=CARTESIAN_POINT ( 'NONE',  ( -0.06521966986864842497, -1.616690375843790051, 1.205047459138554045 ) ) ;
#99313=CARTESIAN_POINT ( 'NONE',  ( 2.719469050394443421, -0.2056238487441063856, 2.096000168696035448 ) ) ;
#99317=CARTESIAN_POINT ( 'NONE',  ( 1.459246395511590189, -1.704040126542965661, 1.084046338683493982 ) ) ;
#99322=CARTESIAN_POINT ( 'NONE',  ( 2.776834730583700228, -2.067601613962879448, -0.6303956341740593050 ) ) ;
#99323=CARTESIAN_POINT ( 'NONE',  ( 6.610000000000030518, 1.266345627986571021, 2.115470293623383569 ) ) ;
#99330=B_SPLINE_CURVE_WITH_KNOTS ( 'NONE', 3,
 ( #38151, #167089, #104223, #170270, #18680, #107485, #8839, #58665, #12035, #27219, #190779 ),
 .UNSPECIFIED., .F., .F.,
 ( 4, 1, 1, 1, 1, 1, 1, 1, 4 ),
 ( 0.000000000000000000, 0.2254179815473072723, 0.3971144120416517653, 0.5241699701252212629, 0.6156743509408303394, 0.6807935377546089351, 0.7289379548928518471, 0.7696256121123346006, 1.000000000000000000 ),
 .UNSPECIFIED. ) ;
#99331=CARTESIAN_POINT ( 'NONE',  ( 0.8025787753177977546, 1.655945718051672566, -1.435626523826734280 ) ) ;
#99333=CARTESIAN_POINT ( 'NONE',  ( 1.059873865361460332, 0.4390357074517194369, -2.219354932451859330 ) ) ;
#99340=CARTESIAN_POINT ( 'NONE',  ( 3.655294433216628391, 0.4326292253380575881, -1.715882644387234590 ) ) ;
#99341=CARTESIAN_POINT ( 'NONE',  ( 6.563508857876433567, 0.3837567690821128696, -2.173003994120882076 ) ) ;
#99343=EDGE_LOOP ( 'NONE', ( #170738, #105357, #167042, #193101 ) ) ;
#99345=CARTESIAN_POINT ( 'NONE',  ( 5.325796065338770369, 0.8146125389149364571, -1.844717355016491478 ) ) ;
#99347=CARTESIAN_POINT ( 'NONE',  ( 2.940157781200231746, 1.856316385841882965, 0.2306766016651334850 ) ) ;
#99348=CARTESIAN_POINT ( 'NONE',  ( 3.327070777303439364, -1.911029926764183040, -0.7966718667702379353 ) ) ;
#99351=CARTESIAN_POINT ( 'NONE',  ( 1.670022949053862948, 1.907054940702714863, -0.1439945843566131367 ) ) ;
#99355=CARTESIAN_POINT ( 'NONE',  ( 0.2333690889706717397, 7.629137130509078268, -2.653349640194931247 ) ) ;
#99357=CARTESIAN_POINT ( 'NONE',  ( 0.9844543725016400293, -1.211084316286781037, 1.480072698922259677 ) ) ;
#99359=CARTESIAN_POINT ( 'NONE',  ( 3.297265573180406584, -1.731424309613574852, 0.9225008839797432802 ) ) ;
#99362=CARTESIAN_POINT ( 'NONE',  ( 5.765915565743810589, 0.6138260544302426291, -2.029845472315944921 ) ) ;
#99364=CARTESIAN_POINT ( 'NONE',  ( 6.872342997630815020, -1.214913955043941174, 1.553259342649115249 ) ) ;
#99366=CARTESIAN_POINT ( 'NONE',  ( 2.021741635325131625, -0.4369018484469379682, 1.965087169840364245 ) ) ;
#99368=CARTESIAN_POINT ( 'NONE',  ( 0.7556430218940900501, 2.039295976802601995, -0.5688827987148316057 ) ) ;
#99370=CARTESIAN_POINT ( 'NONE',  ( 2.840353284027045344, -1.066491845456703835, 1.774417039089710935 ) ) ;
#99372=CARTESIAN_POINT ( 'NONE',  ( 6.281206920390010495, 1.440802673026912117, 1.515107276980606654 ) ) ;
#99374=CARTESIAN_POINT ( 'NONE',  ( 4.032112419961201510, 0.9767663869549062516, -1.542106374223570775 ) ) ;
#99377=CARTESIAN_POINT ( 'NONE',  ( 6.890000000000007674, 6.036127733823692054, 2.594896729422516923 ) ) ;
#99379=CARTESIAN_POINT ( 'NONE',  ( 5.860442804830619856, 0.8892231252738895808, 2.019869304780027353 ) ) ;
#99382=CARTESIAN_POINT ( 'NONE',  ( 3.738835060935014276, 1.816739721148411757, 0.5971339541979635568 ) ) ;
#99388=CARTESIAN_POINT ( 'NONE',  ( 6.532779862045914321, -1.958661757936002612, 0.9833580883553474372 ) ) ;
#99390=CARTESIAN_POINT ( 'NONE',  ( 0.3800845246329161431, -0.2246070939678334044, -1.827447590993152682 ) ) ;
#99393=CARTESIAN_POINT ( 'NONE',  ( 4.850782132498069998, -1.503350029756752804, 1.112868480285071460 ) ) ;
#99398=CARTESIAN_POINT ( 'NONE',  ( 1.164831386079593134, 1.494809975433964100, -1.282432929305108438 ) ) ;
#99399=CARTESIAN_POINT ( 'NONE',  ( 2.232046197884657968, 2.016035414700023676, 0.04665772616015140262 ) ) ;
#99403=CARTESIAN_POINT ( 'NONE',  ( 3.047022719409075986, -1.791863632763015968, -1.261349808265788797 ) ) ;
#99406=CARTESIAN_POINT ( 'NONE',  ( 6.825078400183554272, 2.980425674467934272, 2.309322343017068402 ) ) ;
#99413=CARTESIAN_POINT ( 'NONE',  ( 4.792441439910442469, 1.527937338083688923, -1.027124420945781935 ) ) ;
#99414=CARTESIAN_POINT ( 'NONE',  ( 0.8033857101962671443, 1.774305754185826034, -0.9510189173033887222 ) ) ;
#99415=CARTESIAN_POINT ( 'NONE',  ( 2.935265884076414977, 1.227738246725296634, 1.942841054583419602 ) ) ;
#99417=CARTESIAN_POINT ( 'NONE',  ( 1.147037741594110427, 1.644639672688326559, -0.8707446802224245719 ) ) ;
#99420=CARTESIAN_POINT ( 'NONE',  ( -0.02319159430949970652, 0.003959926571647092407, -1.810968101872318714 ) ) ;
#99421=CARTESIAN_POINT ( 'NONE',  ( 4.535362393419643645, -0.08824616237496611670, 1.910463848342447202 ) ) ;
#99424=CARTESIAN_POINT ( 'NONE',  ( 3.192999258835881093, 1.649592175042478015, 1.284459162532962440 ) ) ;
#99425=CARTESIAN_POINT ( 'NONE',  ( 2.746779440450992649, -1.556306552617524597, 1.037596984913228937 ) ) ;
#99428=CARTESIAN_POINT ( 'NONE',  ( 6.040549724581927293, -1.551790349881351450, 0.9907606852931831742 ) ) ;
#99432=CARTESIAN_POINT ( 'NONE',  ( 5.074679841287068172, -1.625846828454122983, -0.5764380256386961721 ) ) ;
#99434=CARTESIAN_POINT ( 'NONE',  ( 0.3517064098005295292, 0.1722828621854489983, -1.725525930370126249 ) ) ;
#99437=CARTESIAN_POINT ( 'NONE',  ( 4.522458045437067753, 1.018072405813482018, 1.917541202323807203 ) ) ;
#99438=CARTESIAN_POINT ( 'NONE',  ( 3.228933428962964758, 0.04559371896543929631, 1.825288036790246204 ) ) ;
#99439=CARTESIAN_POINT ( 'NONE',  ( 0.5847188370675902025, 1.875566754216885013, 0.5750099747552291918 ) ) ;
#99440=CARTESIAN_POINT ( 'NONE',  ( 5.507064729579815854, -0.04930729212004316547, 2.116909390494752685 ) ) ;
#99442=CARTESIAN_POINT ( 'NONE',  ( 6.444901331192640193, -1.838261776244881185, -1.369441068571846554 ) ) ;
#99446=CARTESIAN_POINT ( 'NONE',  ( 1.506653248757179320, -2.110590818861147078, -0.2044851626497797559 ) ) ;
#99449=CARTESIAN_POINT ( 'NONE',  ( 6.807499178464245126, -1.738453852359397978, -1.300317965242798968 ) ) ;
#99450=CARTESIAN_POINT ( 'NONE',  ( 6.883263157960369583, 7.629137130509070275, 2.653810918356712900 ) ) ;
#99452=CARTESIAN_POINT ( 'NONE',  ( 1.823182589357236205, 1.643363032943769397, -1.494666050352111863 ) ) ;
#99454=CARTESIAN_POINT ( 'NONE',  ( 6.311172677262812059, 1.158691452862798954, -1.650079838712660063 ) ) ;
#99456=CARTESIAN_POINT ( 'NONE',  ( 4.065324354713106381, 1.766439233411433163, 1.064669890786486661 ) ) ;
#99458=CARTESIAN_POINT ( 'NONE',  ( -0.2408018239683913930, 0.6935112996086059134, -2.180753846165773169 ) ) ;
#99462=CARTESIAN_POINT ( 'NONE',  ( 0.9024203131168639924, 1.581833000263275224, -1.367050110207337799 ) ) ;
#99463=CARTESIAN_POINT ( 'NONE',  ( 4.177188522404684079, 1.205947341878073287, 1.391433828303423326 ) ) ;
#99465=CARTESIAN_POINT ( 'NONE',  ( 1.781837903662389477, -0.9264376740152606704, 1.454631767934653208 ) ) ;
#99466=CARTESIAN_POINT ( 'NONE',  ( 0.6027503803631119039, 1.865048444749048517, 0.7672877736318933772 ) ) ;
#99467=CARTESIAN_POINT ( 'NONE',  ( 1.583111924021431305, -0.7688449931826674133, 2.166437542035759556 ) ) ;
#99469=CARTESIAN_POINT ( 'NONE',  ( 1.265308524177723326, -2.045349560253268084, -0.9672931750909097293 ) ) ;
#99470=CARTESIAN_POINT ( 'NONE',  ( 4.494815117402239935, -0.4609086856197233684, -2.054844913126519401 ) ) ;
#99472=CARTESIAN_POINT ( 'NONE',  ( 2.811481186154769496, -1.751065702721636308, 0.2553572387639922447 ) ) ;
#99475=CARTESIAN_POINT ( 'NONE',  ( 5.968750000000003553, 0.7852924748296689073, -1.895863743164208026 ) ) ;
#99477=UNCERTAINTY_MEASURE_WITH_UNIT (LENGTH_MEASURE( 1.000000000000000082E-05 ), #108248, 'distance_accuracy_value', 'NONE');
#99480=CARTESIAN_POINT ( 'NONE',  ( 5.080443840416010381, 1.095562506470529884, 1.932424796230156616 ) ) ;
#99481=CARTESIAN_POINT ( 'NONE',  ( 3.627062487484993714, -2.024900418628313936, 0.8384617360315260726 ) ) ;
#99484=CARTESIAN_POINT ( 'NONE',  ( 6.076833508651091620, -1.499762292660647311, 1.499315088411487640 ) ) ;
#99486=CARTESIAN_POINT ( 'NONE',  ( 6.890000000000050306, -0.002781820520068867264, 1.999840353888074240 ) ) ;
#99489=CARTESIAN_POINT ( 'NONE',  ( 5.783468009189684622, 0.1541500780414573890, -2.115021274163720211 ) ) ;
#99493=CARTESIAN_POINT ( 'NONE',  ( 6.819229411136438657, -0.1619093195798972928, 2.126376854085454404 ) ) ;
#99495=CARTESIAN_POINT ( 'NONE',  ( 5.776868925826902590, 1.698781319366513998, -0.7106697882480541573 ) ) ;
#99498=CARTESIAN_POINT ( 'NONE',  ( 1.100653536641453156, -0.4241352534964801801, 1.687842229193817989 ) ) ;
#99503=CARTESIAN_POINT ( 'NONE',  ( 5.120075222393803749, -1.153228217640640985, -1.828211184805514922 ) ) ;
#99506=CARTESIAN_POINT ( 'NONE',  ( 5.067319851952804655, 0.2155487944876262052, -2.150937003660175595 ) ) ;
#99510=CARTESIAN_POINT ( 'NONE',  ( 6.204366038997092936, -0.7071694579776456324, -1.840334891991159738 ) ) ;
#99511=CARTESIAN_POINT ( 'NONE',  ( 5.255145817263100483, -1.720984288211702795, -0.2101651147246290929 ) ) ;
#99513=CARTESIAN_POINT ( 'NONE',  ( 1.997856853652695497, -2.190977152517746163, 0.05759783203293508680 ) ) ;
#99514=CARTESIAN_POINT ( 'NONE',  ( 1.694772972888843210, -2.296637362782745218, -0.2246623637925919403 ) ) ;
#99515=CARTESIAN_POINT ( 'NONE',  ( 4.376282966308748357, -1.189761084491423926, 1.682430632154131578 ) ) ;
#99516=CARTESIAN_POINT ( 'NONE',  ( 6.585517519612275272, -0.8250364709028266130, 1.756089425624817180 ) ) ;
#99519=CARTESIAN_POINT ( 'NONE',  ( 3.972980863544761654, -1.569110274459505350, 1.426624754300914510 ) ) ;
#99521=CARTESIAN_POINT ( 'NONE',  ( 1.072888940501380839, -0.9041080511620370741, 1.802418165037560138 ) ) ;
#99523=CARTESIAN_POINT ( 'NONE',  ( 4.700333112842928429, -2.206180118464650786, -0.05804534286662357823 ) ) ;
#99529=CARTESIAN_POINT ( 'NONE',  ( -0.1291982275798781721, -0.004298614154785804914, -2.073875112923000863 ) ) ;
#99532=CARTESIAN_POINT ( 'NONE',  ( 3.379809591947144032, 1.306296513425331263, 1.594013207155994261 ) ) ;
#99535=CARTESIAN_POINT ( 'NONE',  ( 3.615882686718306260, -0.5843173316345972035, 1.933312988646131103 ) ) ;
#99538=CARTESIAN_POINT ( 'NONE',  ( 2.254824865002862389, -1.593768082018555354, 1.306595953347834849 ) ) ;
#99541=CARTESIAN_POINT ( 'NONE',  ( -0.2411972340276230808, 0.2378665717568603510, -1.934216014300967235 ) ) ;
#99542=CARTESIAN_POINT ( 'NONE',  ( 1.464538624043790316, 0.1369371521719800755, -1.836096087760468398 ) ) ;
#99543=CARTESIAN_POINT ( 'NONE',  ( 6.199877634063251541, -0.7475181258948644381, 2.076568058718592624 ) ) ;
#99545=CARTESIAN_POINT ( 'NONE',  ( 1.880366631079612549, -1.158069840294423392, 1.825029014904603342 ) ) ;
#99547=CARTESIAN_POINT ( 'NONE',  ( 1.921111612355221654, -1.799121770747251547, 0.9110121207814986244 ) ) ;
#99550=CARTESIAN_POINT ( 'NONE',  ( 0.2329894512427649333, -1.712236961970284632, 0.7538099095961707796 ) ) ;
#99552=CARTESIAN_POINT ( 'NONE',  ( 4.610209453490740295, -0.8421727957172200352, -1.782655373600953386 ) ) ;
#99553=CARTESIAN_POINT ( 'NONE',  ( 3.942592416894859841, -1.490970858180175940, 1.357867534901323614 ) ) ;
#99557=CARTESIAN_POINT ( 'NONE',  ( 6.199853529602823876, -0.7113111419616345854, 1.982453129600779462 ) ) ;
#99558=CARTESIAN_POINT ( 'NONE',  ( 4.984861949208964305, 1.980195279717174905, 0.6042863919064264122 ) ) ;
#99562=CARTESIAN_POINT ( 'NONE',  ( 5.256120111591911837, 0.8147005317804748570, -1.848364005614275163 ) ) ;
#99565=CARTESIAN_POINT ( 'NONE',  ( 3.493080449939501619, -0.4495562565045966852, -2.263328358674908003 ) ) ;
#99566=CARTESIAN_POINT ( 'NONE',  ( 0.9540547974491294658, -0.7459001080754708024, 1.923128640884926410 ) ) ;
#99573=CARTESIAN_POINT ( 'NONE',  ( 3.543588177981399134, 1.964110833604881812, -0.9256020844959752525 ) ) ;
#99576=CARTESIAN_POINT ( 'NONE',  ( 2.630204301513817455, 0.2276190002089127917, 1.827071974840013269 ) ) ;
#99579=CARTESIAN_POINT ( 'NONE',  ( 4.458633810090739225, -1.957822973221786444, -0.9849130632908836835 ) ) ;
#99581=CARTESIAN_POINT ( 'NONE',  ( 4.540055829149266309, 0.9713072833863345412, -2.043554373614121289 ) ) ;
#99586=CARTESIAN_POINT ( 'NONE',  ( 6.046140008783082109, 1.767849252625730783, 0.08484812824352709615 ) ) ;
#99587=CARTESIAN_POINT ( 'NONE',  ( 4.565094110769337910, -1.615551665759178412, 1.200850101804177283 ) ) ;
#99589=CARTESIAN_POINT ( 'NONE',  ( 2.977667800601135895, 2.000151994021987623, -0.6593727523046940542 ) ) ;
#99590=CARTESIAN_POINT ( 'NONE',  ( 0.5092220205753159590, -1.818610674291549323, 0.6019667691262234888 ) ) ;
#99592=CARTESIAN_POINT ( 'NONE',  ( 2.506254056688070886, 1.969067392671639771, 0.05118484259234063610 ) ) ;
#99593=CARTESIAN_POINT ( 'NONE',  ( 0.3560485870845608858, 0.7116971694140910021, 1.730184004908103867 ) ) ;
#99594=CARTESIAN_POINT ( 'NONE',  ( 1.504273306027693602, 1.959471947749168663, 0.09963418240711149898 ) ) ;
#99595=CARTESIAN_POINT ( 'NONE',  ( 0.03522015555855115276, -0.09184495783944729430, 1.910282976853895587 ) ) ;
#99596=ORIENTED_EDGE ( 'NONE', *, *, #136321, .T. ) ;
#99599=CARTESIAN_POINT ( 'NONE',  ( 5.963714631206167738, 1.842656449598079060, -0.3214700631931910468 ) ) ;
#99601=CARTESIAN_POINT ( 'NONE',  ( 6.297728486381423352, -1.495382609916453998, -1.431936454106122358 ) ) ;
#99604=CARTESIAN_POINT ( 'NONE',  ( 1.275928261265106833, -2.020323679977220621, 0.4517519998969782291 ) ) ;
#99609=CARTESIAN_POINT ( 'NONE',  ( 5.654972079148370412, 0.4136758123431219514, 2.079573305287989449 ) ) ;
#99614=CARTESIAN_POINT ( 'NONE',  ( 6.057081135787192316, 1.604708697955498087, -1.128374156723031430 ) ) ;
#99616=CARTESIAN_POINT ( 'NONE',  ( 3.374374892241317703, -0.3960410224921434019, 1.976653181598592601 ) ) ;
#99617=CARTESIAN_POINT ( 'NONE',  ( 4.083139574666094340, 1.542046283821847830, 1.136513224425585555 ) ) ;
#99619=CARTESIAN_POINT ( 'NONE',  ( 1.101424459656743071, -0.5276332240332289869, 2.126988402630064279 ) ) ;
#99620=CARTESIAN_POINT ( 'NONE',  ( 0.1331715793776652446, 7.629137130509056952, -2.553547540661147419 ) ) ;
#99621=CARTESIAN_POINT ( 'NONE',  ( 3.532352470753961082, 1.824241569866682289, 0.4128566369710484629 ) ) ;
#99625=CARTESIAN_POINT ( 'NONE',  ( 5.044581972647897317, -1.532752649812264778, 1.460808053437604226 ) ) ;
#99628=CARTESIAN_POINT ( 'NONE',  ( 1.980132433977495499, -2.051005990652774447, -0.4047881525126810209 ) ) ;
#99630=CARTESIAN_POINT ( 'NONE',  ( 0.6567381767516925484, -1.453278249834984326, -0.9285724537800400524 ) ) ;
#99638=CARTESIAN_POINT ( 'NONE',  ( 0.5569035977302905227, -1.554463864252687122, 0.9298500530290281230 ) ) ;
#99644=CARTESIAN_POINT ( 'NONE',  ( 6.539320575229251808, 0.01001626003939220556, 1.796977979958065852 ) ) ;
#99649=CARTESIAN_POINT ( 'NONE',  ( 2.717075380476912994, -1.617705633067820559, -0.9199624106535415624 ) ) ;
#99650=CARTESIAN_POINT ( 'NONE',  ( 0.5092220205753159590, -1.818610674291549323, 0.6019667691262234888 ) ) ;
#99651=CARTESIAN_POINT ( 'NONE',  ( 0.1295496576057716120, -1.118478952742516519, -1.443350188048427851 ) ) ;
#99657=CARTESIAN_POINT ( 'NONE',  ( 4.926587155384105188, -1.289601243782242834, 1.488548236191704177 ) ) ;
#99658=CARTESIAN_POINT ( 'NONE',  ( 1.207859650372544280, 1.608047128250057689, 1.382383069919224106 ) ) ;
#99662=CARTESIAN_POINT ( 'NONE',  ( 6.140607899229072686, -1.853288307406484758, 1.169240172944140621 ) ) ;
#99664=CARTESIAN_POINT ( 'NONE',  ( 4.049766240643924320, 0.6497466500948418933, -1.813626049157530229 ) ) ;
#99666=CARTESIAN_POINT ( 'NONE',  ( 0.3756504392133250825, 1.046533627790873000, 1.495644344755317823 ) ) ;
#99667=CARTESIAN_POINT ( 'NONE',  ( 1.032169062358662348, -1.402649970393770484, -1.703791656331831605 ) ) ;
#99672=CARTESIAN_POINT ( 'NONE',  ( 6.789911431267126041, -1.283970416288570116, -1.493486111907322389 ) ) ;
#99673=CARTESIAN_POINT ( 'NONE',  ( 1.716251783418326848, 1.812799857666002934, 0.6971432602522424915 ) ) ;
#99674=CARTESIAN_POINT ( 'NONE',  ( 6.169324051992485458, -0.8183585724929974825, -2.147936757437307165 ) ) ;
#99676=CARTESIAN_POINT ( 'NONE',  ( 4.627703445648046809, 1.805782058207167529, -0.4492820238155226797 ) ) ;
#99683=CARTESIAN_POINT ( 'NONE',  ( -0.04112450405316381286, -1.960553898366865555, -0.9795403211517728082 ) ) ;
#99687=CARTESIAN_POINT ( 'NONE',  ( 1.119449510670032177, -1.781678707675336870, 0.3977030049751931196 ) ) ;
#99690=CARTESIAN_POINT ( 'NONE',  ( 3.428057853464313798, -1.315526611184931527, -1.130013928329278494 ) ) ;
#99692=CARTESIAN_POINT ( 'NONE',  ( 6.609000000000047947, 7.053019707385148607, 2.498153760597703332 ) ) ;
#99693=CARTESIAN_POINT ( 'NONE',  ( 0.1331565106231328843, 0.003911343561965873426, -1.946049565259087455 ) ) ;
#99694=CARTESIAN_POINT ( 'NONE',  ( 6.358013415952256331, 1.820405254634300363, -0.1396899356524081148 ) ) ;
#99695=CARTESIAN_POINT ( 'NONE',  ( 4.276187414114787089, -1.004825795036960567, -1.684713053385626269 ) ) ;
#99700=CARTESIAN_POINT ( 'NONE',  ( 4.582752651445391123, -1.384437811569695587, 1.606279107262520434 ) ) ;
#99703=CARTESIAN_POINT ( 'NONE',  ( 3.450112209602332669, -0.8433740631265237431, 1.890881698631073249 ) ) ;
#99706=CARTESIAN_POINT ( 'NONE',  ( 3.411010488035473909, -1.370397956465055245, -1.845398096504316410 ) ) ;
#99713=EDGE_CURVE ( 'NONE', #190223, #119587, #127103, .T. ) ;
#99714=CARTESIAN_POINT ( 'NONE',  ( 4.306835718904429733, -0.4242474483713705169, -1.864571660543254961 ) ) ;
#99716=CARTESIAN_POINT ( 'NONE',  ( 5.473588350598873831, 1.661195908839340873, -0.4637430927098630806 ) ) ;
#99717=CARTESIAN_POINT ( 'NONE',  ( 3.520720487665735643, 0.3006478860226591276, 1.993893439002386581 ) ) ;
#99718=CARTESIAN_POINT ( 'NONE',  ( 4.940191063930403637, -1.940984743010031544, -1.231243198015237628 ) ) ;
#99720=CARTESIAN_POINT ( 'NONE',  ( 0.5400322017136415242, -1.563516176313231920, -1.557742479837947558 ) ) ;
#99722=CARTESIAN_POINT ( 'NONE',  ( 5.342920941031360726, -1.517576202870707380, 0.9101455627106845858 ) ) ;
#99724=CARTESIAN_POINT ( 'NONE',  ( 1.974976472051133136, -0.1153332747052069479, -2.289479170392795915 ) ) ;
#99725=CARTESIAN_POINT ( 'NONE',  ( 0.09317796543232242934, -1.739829294281483474, -0.04824335600969902743 ) ) ;
#99731=CARTESIAN_POINT ( 'NONE',  ( 0.5730174903513629570, 1.496870926018354364, -1.572904236412080436 ) ) ;
#99732=CARTESIAN_POINT ( 'NONE',  ( 2.553923023464285347, 1.082840749376843270, 1.700961377887353798 ) ) ;
#99734=CARTESIAN_POINT ( 'NONE',  ( 5.988885569479125870, -0.2852814255829403955, -1.905149068243816579 ) ) ;
#99736=CARTESIAN_POINT ( 'NONE',  ( 2.672393786618231015, 2.210292516208379521, -0.2222851140616446397 ) ) ;
#99745=CARTESIAN_POINT ( 'NONE',  ( 4.528681460942417303, -1.588859801488880175, 0.7108448094420779517 ) ) ;
#99746=CARTESIAN_POINT ( 'NONE',  ( 3.877359892829432386, -0.1466975079335990917, 1.956454564409334296 ) ) ;
#99751=CARTESIAN_POINT ( 'NONE',  ( 0.6431264911748921786, -0.2508561283167276557, -2.047287668789533832 ) ) ;
#99755=CARTESIAN_POINT ( 'NONE',  ( 0.6555950923613624859, -1.913042455388717311, -1.207739878423098823 ) ) ;
#99759=CARTESIAN_POINT ( 'NONE',  ( 2.372138566722302500, -1.154253592077842727, 1.471842878544210809 ) ) ;
#99760=CARTESIAN_POINT ( 'NONE',  ( 1.248208839261849112, 1.708581046602712039, -0.2955488178391346143 ) ) ;
#99762=CARTESIAN_POINT ( 'NONE',  ( 5.319949580897746166, 1.306013235697962571, -1.759773446019400778 ) ) ;
#99763=CARTESIAN_POINT ( 'NONE',  ( 6.194374175331438082, -2.295634644278636394, -0.2347168956345067892 ) ) ;
#99764=CARTESIAN_POINT ( 'NONE',  ( 1.059529560858112340, 0.4028119719261863962, -2.020956803572224736 ) ) ;
#99765=CARTESIAN_POINT ( 'NONE',  ( 3.837779778221518168, 1.932683437559437500, 0.1894486881511766863 ) ) ;
#99768=CARTESIAN_POINT ( 'NONE',  ( 5.307814152003552444, -1.861618091082300808, 0.1822119596564600597 ) ) ;
#99769=CARTESIAN_POINT ( 'NONE',  ( 1.812500000000001554, 1.451031289061194052, 1.451031289061046170 ) ) ;
#99771=CARTESIAN_POINT ( 'NONE',  ( 0.2448742905335095366, -1.679455039217644829, -0.4304099419733271592 ) ) ;
#99774=CARTESIAN_POINT ( 'NONE',  ( 4.307267641921147749, 1.238321930042911578, -1.591317616567271775 ) ) ;
#99778=CARTESIAN_POINT ( 'NONE',  ( 2.455445036260803349, 0.4872311372507812655, -1.759406031448563557 ) ) ;
#99786=CARTESIAN_POINT ( 'NONE',  ( 6.639320575229294086, 0.002105643433562148347, 2.003388605011639179 ) ) ;
#99787=CARTESIAN_POINT ( 'NONE',  ( -0.004992717928550480244, -2.057963470346049650, -0.5107951590591561786 ) ) ;
#99791=CARTESIAN_POINT ( 'NONE',  ( 6.719606831986117967, -1.999679869198322413, 0.4981698227890380970 ) ) ;
#99792=CARTESIAN_POINT ( 'NONE',  ( 5.274064633610318076, 1.777012466945230962, -0.9530095070046653571 ) ) ;
#99802=CARTESIAN_POINT ( 'NONE',  ( 5.237657596305253627, -1.897407540178517316, -0.6818907625677357309 ) ) ;
#99803=CARTESIAN_POINT ( 'NONE',  ( 4.206863059814883066, -0.3125640686512491384, 1.814249101404527220 ) ) ;
#99804=CARTESIAN_POINT ( 'NONE',  ( 0.07661050522430808141, 2.897279719329011627, -2.199986835335824953 ) ) ;
#99805=CARTESIAN_POINT ( 'NONE',  ( 3.721538942197761379, -0.1710094959430948913, 2.301408321908961607 ) ) ;
#99807=CARTESIAN_POINT ( 'NONE',  ( 4.306063477043454490, -2.156128079323017754, 0.1542669963271598166 ) ) ;
#99809=CARTESIAN_POINT ( 'NONE',  ( 0.6263844939735198070, 0.1443197301355322315, 1.936771776935701794 ) ) ;
#99811=VERTEX_POINT ( 'NONE', #212028 ) ;
#99814=CARTESIAN_POINT ( 'NONE',  ( 3.625732356982212412, -1.113523340526129335, -1.502988901547596567 ) ) ;
#99816=CARTESIAN_POINT ( 'NONE',  ( 1.740342883905017013, 1.098329146349947827, -1.565357986077076990 ) ) ;
#99819=CARTESIAN_POINT ( 'NONE',  ( 2.649284799151204073, -1.834272514977531632, 1.226802785254533568 ) ) ;
#99825=CARTESIAN_POINT ( 'NONE',  ( 0.5441301207207068780, 1.965759916638841309, 0.1495998195316684265 ) ) ;
#99826=CARTESIAN_POINT ( 'NONE',  ( 6.656845493208900955, -1.788705722188275837, 1.457663220358196732 ) ) ;
#99827=CARTESIAN_POINT ( 'NONE',  ( 1.486689167417578394, 1.889818972856545987, 0.5264814339432166701 ) ) ;
#99828=CARTESIAN_POINT ( 'NONE',  ( 4.258677893805890236, -0.6421077783588696741, -1.960174235369451123 ) ) ;
#99836=CARTESIAN_POINT ( 'NONE',  ( 0.4621001773846104554, -0.5802113591629636247, 2.092003544004197302 ) ) ;
#99838=CARTESIAN_POINT ( 'NONE',  ( 5.917501325027624048, -1.028386522942719816, -1.527094029191010893 ) ) ;
#99842=CARTESIAN_POINT ( 'NONE',  ( 1.194370141144196706, -0.4488658031855938813, -1.815784161679114606 ) ) ;
#99843=CARTESIAN_POINT ( 'NONE',  ( 5.237646302014136168, -1.524508687941978469, -1.532700278705993790 ) ) ;
#99849=CARTESIAN_POINT ( 'NONE',  ( 0.9262460828363195953, -0.8603794558708978135, -1.707882697979688391 ) ) ;
#99851=CARTESIAN_POINT ( 'NONE',  ( 3.098275772329066591, -0.5124342443764763333, -1.694037474313156988 ) ) ;
#99852=CARTESIAN_POINT ( 'NONE',  ( 0.6098336241119780565, -0.6879379538977903330, 1.784437680087819666 ) ) ;
#99854=CARTESIAN_POINT ( 'NONE',  ( 5.747645016999404888, 1.886384853835708642, -0.3323884645628824019 ) ) ;
#99855=CARTESIAN_POINT ( 'NONE',  ( 0.1861046438572169504, -1.272802160389638892, -1.633586439835111648 ) ) ;
#99856=CARTESIAN_POINT ( 'NONE',  ( 0.6508261300204335464, 2.090236094481153550, 0.3566229023672163878 ) ) ;
#99858=CARTESIAN_POINT ( 'NONE',  ( 3.801501934187266230, -0.5436965770258190833, 1.789884385262895616 ) ) ;
#99859=CARTESIAN_POINT ( 'NONE',  ( 0.6799654140086827114, -1.016662149479659494, 1.516215539243186639 ) ) ;
#99861=CARTESIAN_POINT ( 'NONE',  ( 2.983271218942393332, -0.1628219013674602478, -2.200934326520533446 ) ) ;
#99864=CARTESIAN_POINT ( 'NONE',  ( 1.451709319293143396, 1.560653109857246701, 1.348772525646862341 ) ) ;
#99871=CARTESIAN_POINT ( 'NONE',  ( 4.809070886388271404, -1.664838503569150419, 1.230558894880565246 ) ) ;
#99873=CARTESIAN_POINT ( 'NONE',  ( 1.265152180075890254, -1.953616520262021039, -0.9254636565915741464 ) ) ;
#99875=CARTESIAN_POINT ( 'NONE',  ( 1.981123565540498177, -1.847491841353067210, -0.8164113852280636685 ) ) ;
#99882=CARTESIAN_POINT ( 'NONE',  ( 6.491422787562372676, -0.4091076066058823013, 1.878265147811091662 ) ) ;
#99883=CARTESIAN_POINT ( 'NONE',  ( 6.539320575229255361, 7.051987793746187450, 2.801414728815339039 ) ) ;
#99884=CARTESIAN_POINT ( 'NONE',  ( 4.739868811304373430, 2.185674081084403753, 0.1610935195608814985 ) ) ;
#99886=CARTESIAN_POINT ( 'NONE',  ( 4.095896644567202038, 1.253117935160457552, 1.444681106026260320 ) ) ;
#99890=CARTESIAN_POINT ( 'NONE',  ( 2.706657832681820697, 1.899625987897411772, 0.6766965020792228280 ) ) ;
#99893=CARTESIAN_POINT ( 'NONE',  ( 0.4512259348973605699, -1.940755322566484642, -1.219765617878470376 ) ) ;
#99895=CARTESIAN_POINT ( 'NONE',  ( 4.330854930063167352, 0.08572247821646634958, 1.722753318990229099 ) ) ;
#99899=CARTESIAN_POINT ( 'NONE',  ( 0.6956633456795427994, -1.384754418207832405, -1.389998539416361423 ) ) ;
#99902=CARTESIAN_POINT ( 'NONE',  ( 0.07556134207194721564, 2.859159929750184848, -2.732257853551669946 ) ) ;
#99904=CARTESIAN_POINT ( 'NONE',  ( 0.2333690889706682703, 0.003390530909083006028, -2.053566628440507635 ) ) ;
#99906=CARTESIAN_POINT ( 'NONE',  ( 4.723216582411014386, 1.578617123877921857, 0.8883131493910937371 ) ) ;
#99909=CARTESIAN_POINT ( 'NONE',  ( 5.373626179778474565, 0.3473841915581803996, -1.777664473148509838 ) ) ;
#99915=CARTESIAN_POINT ( 'NONE',  ( 6.391040216397121831, 0.1834577666269270046, 1.851959058998996710 ) ) ;
#99917=CARTESIAN_POINT ( 'NONE',  ( 3.374530662324583652, -0.3768237823980990497, -1.877989258545700535 ) ) ;
#99919=DIRECTION ( 'NONE',  ( -0.9999980456341537316, 0.000000000000000000, -0.001977050295958610645 ) ) ;
#99923=CARTESIAN_POINT ( 'NONE',  ( 5.577400755804389654, 1.605162776699980753, 1.380938528300587276 ) ) ;
#99924=CARTESIAN_POINT ( 'NONE',  ( 1.235488887756378551, -1.954010380348418119, 0.9248176494114216384 ) ) ;
#99927=CARTESIAN_POINT ( 'NONE',  ( 1.026062881544724137, 1.091098483296793820, -1.463488004260153907 ) ) ;
#99929=CARTESIAN_POINT ( 'NONE',  ( 3.399243825379614226, 1.438455020490635450, 1.123966471122700650 ) ) ;
#99931=CARTESIAN_POINT ( 'NONE',  ( 2.654443970922310214, 1.898414275235399407, 0.2300336082040748686 ) ) ;
#99933=CARTESIAN_POINT ( 'NONE',  ( 2.980859429886784984, 1.853565342000351501, 0.6662430357459552255 ) ) ;
#99934=CARTESIAN_POINT ( 'NONE',  ( 4.353030786369998850, 0.4220677823760305980, -1.895499586301018224 ) ) ;
#99937=CARTESIAN_POINT ( 'NONE',  ( 5.045234882716379765, 0.1584239314957915090, 2.114765283346302205 ) ) ;
#99940=CARTESIAN_POINT ( 'NONE',  ( 0.2331563151865729544, 6.948071805571808035, -2.540803835148666145 ) ) ;
#99944=CARTESIAN_POINT ( 'NONE',  ( 4.547361323050268744, -1.413013347330991598, -1.156083184146582177 ) ) ;
#99950=CARTESIAN_POINT ( 'NONE',  ( 6.157094445334826638, -1.605393284960114242, -0.9600186418455139981 ) ) ;
#99960=CARTESIAN_POINT ( 'NONE',  ( 6.754729744842355110, -0.5704115468931982846, -2.094772688322795506 ) ) ;
#99961=CARTESIAN_POINT ( 'NONE',  ( 1.282980312568120951, 1.728570797422763095, -1.222324810828350428 ) ) ;
#99964=CARTESIAN_POINT ( 'NONE',  ( 5.787960296632533641, -1.308950758395693414, -1.603975846202657429 ) ) ;
#99969=CARTESIAN_POINT ( 'NONE',  ( 1.904612379804408118, 1.696638126304336858, -1.541566781129146912 ) ) ;
#99972=CARTESIAN_POINT ( 'NONE',  ( 2.039183100597967258, 0.003605121848727563250, 1.912571728241836633 ) ) ;
#99976=CARTESIAN_POINT ( 'NONE',  ( 0.08813964471556486047, 1.162479488604960753, 1.643474645366525877 ) ) ;
#99977=CARTESIAN_POINT ( 'NONE',  ( 1.041763817972749750, 1.313373124611896703, 1.457441342770829262 ) ) ;
#99980=CARTESIAN_POINT ( 'NONE',  ( 3.591813267288586520, -2.088258123952376977, -0.1022297611361303732 ) ) ;
#99981=CARTESIAN_POINT ( 'NONE',  ( 2.834531330521594228, 0.2145198750864007742, 1.756709382032408451 ) ) ;
#99983=CARTESIAN_POINT ( 'NONE',  ( 5.349693066923443041, 2.289838395228523282, -0.1081633463214677210 ) ) ;
#99984=CARTESIAN_POINT ( 'NONE',  ( 3.134399458026761121, -1.534476879465409782, 0.8210378458504956622 ) ) ;
#99988=CARTESIAN_POINT ( 'NONE',  ( 3.532318661231689916, 1.691930322982236667, -0.3780173437282279281 ) ) ;
#99989=CARTESIAN_POINT ( 'NONE',  ( 3.262351433937484835, -2.168797558456833308, 0.1038475075719157148 ) ) ;
#99991=CARTESIAN_POINT ( 'NONE',  ( 5.717982508692024624, 0.9896897593998502662, -1.756851901128737348 ) ) ;
#99992=CARTESIAN_POINT ( 'NONE',  ( 0.3437500000590538174, 1.895863741711102612, 0.7852924748299703328 ) ) ;
#99994=CARTESIAN_POINT ( 'NONE',  ( 2.344641424807081709, 0.4199494819796690814, 1.879913682802894614 ) ) ;
#99996=CARTESIAN_POINT ( 'NONE',  ( 5.590131909697702461, 1.323030080273413844, 1.784280720909060758 ) ) ;
#100003=CARTESIAN_POINT ( 'NONE',  ( 1.893536009595264469, -0.1129285828431712546, -2.218558826778730619 ) ) ;
#100004=CARTESIAN_POINT ( 'NONE',  ( 6.584431417889404337, 1.130572321132311098, -1.603143135845342515 ) ) ;
#100010=CARTESIAN_POINT ( 'NONE',  ( 4.422371107804410784, 0.9697015505613596487, 1.820508916172391300 ) ) ;
#100013=EDGE_CURVE ( 'NONE', #43199, #78277, #137428, .T. ) ;
#100015=CARTESIAN_POINT ( 'NONE',  ( 5.553920895479774522, 1.868435625992425742, -0.09091641586010666687 ) ) ;
#100016=CARTESIAN_POINT ( 'NONE',  ( 5.221237796217499394, 1.709784868986977902, 0.2885349091684140665 ) ) ;
#100017=CARTESIAN_POINT ( 'NONE',  ( 4.475936636375839051, -1.689578365139619009, -0.4171736215478424881 ) ) ;
#100019=CARTESIAN_POINT ( 'NONE',  ( 1.558568218312964326, -1.617219677351620089, 1.624929221499067600 ) ) ;
#100021=CARTESIAN_POINT ( 'NONE',  ( 5.390208805286830440, -0.5092157624977285968, -2.027641083400610000 ) ) ;
#100022=CARTESIAN_POINT ( 'NONE',  ( 1.552429278155377679, -1.578373273985161473, -0.9476568548090894550 ) ) ;
#100025=CARTESIAN_POINT ( 'NONE',  ( 1.828750219146151323, 0.7691198443132395424, -1.864169014999479623 ) ) ;
#100032=CARTESIAN_POINT ( 'NONE',  ( 4.020270485675044192, -2.114722421624544157, 0.1573160286183969692 ) ) ;
#100034=CARTESIAN_POINT ( 'NONE',  ( 5.232948167349782409, 0.1380416123818763163, 1.820529236867339584 ) ) ;
#100041=CARTESIAN_POINT ( 'NONE',  ( 2.953383392634020943, -1.779389778202213446, 0.9557246442400985087 ) ) ;
#100042=CARTESIAN_POINT ( 'NONE',  ( 0.4113322892924773377, 1.832542443981843405, 1.037592781499405259 ) ) ;
#100044=CARTESIAN_POINT ( 'NONE',  ( 3.696024482597393135, 0.8403398683093143973, -1.660512506883378370 ) ) ;
#100049=CARTESIAN_POINT ( 'NONE',  ( 6.754767742037871336, -1.594745458351163103, 1.305156173170081813 ) ) ;
#100053=CARTESIAN_POINT ( 'NONE',  ( 2.213800448916534158, -1.389428533404401422, -1.036884654713841725 ) ) ;
#100054=CARTESIAN_POINT ( 'NONE',  ( 1.235833198037468827, 0.3363826672934740469, 1.707315539672292104 ) ) ;
#100055=CARTESIAN_POINT ( 'NONE',  ( 6.721333375000203780, -0.1674226297891309168, 2.271100132491596479 ) ) ;
#100058=CARTESIAN_POINT ( 'NONE',  ( 1.335309304440901235, -1.864295028495915441, 0.8784465167368092908 ) ) ;
#100060=CARTESIAN_POINT ( 'NONE',  ( 0.5091384654962345380, 2.010518347751136137, 0.1511200514899835312 ) ) ;
#100063=CARTESIAN_POINT ( 'NONE',  ( 6.526239545637954720, 1.075124705556152138, -1.530631868311462362 ) ) ;
#100064=CARTESIAN_POINT ( 'NONE',  ( 4.552931727387078631, 0.3324577288378940954, 1.883125075537089854 ) ) ;
#100066=CARTESIAN_POINT ( 'NONE',  ( 6.516270054225981490, -1.036149114087565382, -1.948532232987249424 ) ) ;
#100070=CARTESIAN_POINT ( 'NONE',  ( 0.1178396879437521028, -0.5365784638422869124, 1.947031292057841645 ) ) ;
#100072=CARTESIAN_POINT ( 'NONE',  ( 3.382123439733915493, 1.462175888237092547, 1.785228103979496384 ) ) ;
#100073=CARTESIAN_POINT ( 'NONE',  ( 4.826587731031282580, -1.282962940432516907, 1.484285152025546672 ) ) ;
#100074=CARTESIAN_POINT ( 'NONE',  ( 1.323018481131872370, -1.771187822987334570, -0.8437873667686208723 ) ) ;
#100078=CARTESIAN_POINT ( 'NONE',  ( -0.08258987484092288056, -1.932961894807160963, 0.8646260017347202620 ) ) ;
#100081=CARTESIAN_POINT ( 'NONE',  ( 1.183273638618479673, -0.8294958387620559037, 1.643756842616146630 ) ) ;
#100083=CARTESIAN_POINT ( 'NONE',  ( 4.188457025382522403, 1.166365143183651920, -1.831003835250759604 ) ) ;
#100085=CARTESIAN_POINT ( 'NONE',  ( 1.810938747355747447, -0.5704394276861005642, -2.042344090522000055 ) ) ;
#100090=CARTESIAN_POINT ( 'NONE',  ( 2.653650601580277879, 0.5529494111683015412, -1.985115717065755847 ) ) ;
#100094=CARTESIAN_POINT ( 'NONE',  ( 0.07775346131141076811, 6.946779003630084048, -2.883989925229225815 ) ) ;
#100097=CARTESIAN_POINT ( 'NONE',  ( 4.301352856729808494, 1.706663192164651122, -0.8627939227693476321 ) ) ;
#100100=CARTESIAN_POINT ( 'NONE',  ( 1.177466099744011174, -0.05591215127281846942, -2.261859306125458158 ) ) ;
#100102=CARTESIAN_POINT ( 'NONE',  ( 0.9139796618767962455, -1.811767225755844146, 0.001225010880583424656 ) ) ;
#100103=CARTESIAN_POINT ( 'NONE',  ( 1.411203511878999173, -1.802517209299081102, 0.6490724346438890846 ) ) ;
#100104=CARTESIAN_POINT ( 'NONE',  ( 2.840353284027045344, -1.066491845456703835, 1.774417039089710935 ) ) ;
#100106=CARTESIAN_POINT ( 'NONE',  ( 0.6199196518563926395, -1.052708125740812628, -1.666702442819472774 ) ) ;
#100107=CARTESIAN_POINT ( 'NONE',  ( 5.022062012317437762, -1.032219231902216761, -1.626458924502146797 ) ) ;
#100108=CARTESIAN_POINT ( 'NONE',  ( 1.243279834139981999, 0.4545127484847265031, 2.262342451343732463 ) ) ;
#100111=CARTESIAN_POINT ( 'NONE',  ( 4.932111759923301975, 1.184877397895794493, 1.688235060362786255 ) ) ;
#100115=CARTESIAN_POINT ( 'NONE',  ( 4.840906100885360885, 0.3572417793257404717, 2.075268335340733739 ) ) ;
#100117=CARTESIAN_POINT ( 'NONE',  ( 1.399139394074319753, 0.4229888639164773867, 2.129416274499373429 ) ) ;
#100119=CARTESIAN_POINT ( 'NONE',  ( 5.097027542433036018, 1.800287743887505121, -1.196142203056582920 ) ) ;
#100120=CARTESIAN_POINT ( 'NONE',  ( 5.426427855750480589, -0.9099042507111715361, -1.803185865349592021 ) ) ;
#100126=CARTESIAN_POINT ( 'NONE',  ( 3.098842478760281516, 1.825076540557273974, 0.8578426345753201732 ) ) ;
#100131=CARTESIAN_POINT ( 'NONE',  ( 5.067319851952804655, 0.2155487944876262052, -2.150937003660175595 ) ) ;
#100132=CARTESIAN_POINT ( 'NONE',  ( 6.720655732516647163, -0.004400176169771369272, 2.173773060281408931 ) ) ;
#100134=CARTESIAN_POINT ( 'NONE',  ( 6.081657687927014777, -0.6766999560612970699, 1.899624756701682626 ) ) ;
#100136=CARTESIAN_POINT ( 'NONE',  ( 0.9786238818701101794, -0.03817194980801525556, -1.724638339026884903 ) ) ;
#100141=CARTESIAN_POINT ( 'NONE',  ( 6.591075523649926993, 1.627300515804396941, -0.9222108319836411772 ) ) ;
#100142=CARTESIAN_POINT ( 'NONE',  ( -0.04036574886347610303, -1.557478217179044888, -1.275100411523772737 ) ) ;
#100147=CARTESIAN_POINT ( 'NONE',  ( 2.209781436637091367, 1.640924847721588975, 1.343087772177023131 ) ) ;
#100148=CARTESIAN_POINT ( 'NONE',  ( 1.511342449054883019, -1.897691915346022107, 0.6820157586827846341 ) ) ;
#100149=CARTESIAN_POINT ( 'NONE',  ( 1.915983733309385872, -1.811150802387480274, 0.04719988836864030118 ) ) ;
#100152=CARTESIAN_POINT ( 'NONE',  ( 6.245025451202089073, -1.828886558906620774, 1.152162773130911644 ) ) ;
#100158=CARTESIAN_POINT ( 'NONE',  ( 0.1455191377820958532, 1.894478286654190269, -0.2837363430458189062 ) ) ;
#100165=CARTESIAN_POINT ( 'NONE',  ( 4.557600102482579629, 0.4766696971462945909, -2.108333899287537339 ) ) ;
#100168=CARTESIAN_POINT ( 'NONE',  ( 2.267978396857213585, 0.5610993688725562922, -2.044979925899123252 ) ) ;
#100169=CARTESIAN_POINT ( 'NONE',  ( 6.756878055424797580, -1.408711550780303412, 1.160885376127060553 ) ) ;
#100170=CARTESIAN_POINT ( 'NONE',  ( 3.233620971007169942, -1.321289716990686980, -1.463211747571713461 ) ) ;
#100171=CARTESIAN_POINT ( 'NONE',  ( 5.801015586618943232, -0.2871438832755985326, -1.890612906794430614 ) ) ;
#100174=CARTESIAN_POINT ( 'NONE',  ( 6.461384246211865801, 1.636644077835234246, 1.095356925007910265 ) ) ;
#100175=CARTESIAN_POINT ( 'NONE',  ( 1.587728922880219384, -1.932555244376774617, -0.1907308274580049312 ) ) ;
#100176=ORIENTED_EDGE ( 'NONE', *, *, #193642, .F. ) ;
#100183=CARTESIAN_POINT ( 'NONE',  ( 6.024064539286675846, -1.897261554996135802, 0.2387622092476364699 ) ) ;
#100185=CARTESIAN_POINT ( 'NONE',  ( 2.807470779205251343, 1.864772411128329477, 1.179945617918669143 ) ) ;
#100186=CARTESIAN_POINT ( 'NONE',  ( 2.309865001130634976, -0.4838574416936823885, 2.152911442350906146 ) ) ;
#100188=CARTESIAN_POINT ( 'NONE',  ( 1.084454188491505988, -1.212558158303609135, 1.478703618145213783 ) ) ;
#100191=CARTESIAN_POINT ( 'NONE',  ( 4.457524453155742528, 1.660904245173303373, 1.235824716467534667 ) ) ;
#100194=CARTESIAN_POINT ( 'NONE',  ( 1.797963993548271411, -0.7283430984801853025, 2.035426966748521860 ) ) ;
#100195=CARTESIAN_POINT ( 'NONE',  ( 3.773127072069931032, 2.063069237518061705, -0.7396954945804237180 ) ) ;
#100201=CARTESIAN_POINT ( 'NONE',  ( 6.047464834240314779, -1.219521636822028077, 1.233209766127696616 ) ) ;
#100203=CARTESIAN_POINT ( 'NONE',  ( 3.028250241984064228, 1.103615759228196325, 1.751372171329562688 ) ) ;
#100204=CARTESIAN_POINT ( 'NONE',  ( 6.134383104757832328, 0.6643169034818379171, 2.010352329694592655 ) ) ;
#100207=CARTESIAN_POINT ( 'NONE',  ( 3.414863416077691838, -1.494280747806640885, 1.283048038104795507 ) ) ;
#100208=CARTESIAN_POINT ( 'NONE',  ( 0.5274218815167727170, -0.2782315536139517431, 1.891897276498944347 ) ) ;
#100209=CARTESIAN_POINT ( 'NONE',  ( 5.578174268327147800, -2.235363620237617255, -0.5069547310770585735 ) ) ;
#100210=CARTESIAN_POINT ( 'NONE',  ( 2.385134503015675200, 1.669401249834654211, -0.7394980648879891927 ) ) ;
#100216=ORIENTED_EDGE ( 'NONE', *, *, #194375, .T. ) ;
#100217=CARTESIAN_POINT ( 'NONE',  ( 3.814701174604028466, -0.6354162253871125099, -1.910337659313849024 ) ) ;
#100218=CARTESIAN_POINT ( 'NONE',  ( 4.416819765676714304, -1.456490764316048292, 1.314424223973277961 ) ) ;
#100221=CARTESIAN_POINT ( 'NONE',  ( 0.07536363704233051131, 7.629137130509080045, -2.744199452819145790 ) ) ;
#100222=CARTESIAN_POINT ( 'NONE',  ( -0.1116087887279961222, -0.4605761454780517572, -2.046466910313152532 ) ) ;
#100223=CARTESIAN_POINT ( 'NONE',  ( 5.295665003108637414, -0.6346038033320391403, 1.652335088206556613 ) ) ;
#100225=CARTESIAN_POINT ( 'NONE',  ( 2.009981539508858273, -1.034714594384738229, -1.931790675223004738 ) ) ;
#100226=CARTESIAN_POINT ( 'NONE',  ( 6.580030513128129144, -1.708294420148011472, -0.3314369902002142765 ) ) ;
#100228=CARTESIAN_POINT ( 'NONE',  ( 0.9786238818701101794, -0.03817194980801525556, -1.724638339026884903 ) ) ;
#100229=CARTESIAN_POINT ( 'NONE',  ( 1.107258645251009144, 0.9300933289658299685, -2.101954592823534362 ) ) ;
#100230=CARTESIAN_POINT ( 'NONE',  ( 0.8729168595149154886, -0.05911722906676297740, -2.190938979806676734 ) ) ;
#100232=CARTESIAN_POINT ( 'NONE',  ( 6.169268014014505752, -0.6277043665407368023, -1.616433383845305105 ) ) ;
#100233=CARTESIAN_POINT ( 'NONE',  ( 2.860232119962682784, 2.196193069775736362, -0.2169517147150926140 ) ) ;
#100234=CARTESIAN_POINT ( 'NONE',  ( 6.742638747055813120, -2.127943412135436585, -0.4303581323979056017 ) ) ;
#100236=CARTESIAN_POINT ( 'NONE',  ( 2.079462195143897851, 1.640249684897076898, 1.338979269010678985 ) ) ;
#100237=CARTESIAN_POINT ( 'NONE',  ( 6.827182134110198142, 3.677047352536796154, 2.802821765677898203 ) ) ;
#100238=CARTESIAN_POINT ( 'NONE',  ( 5.473632971755619359, 1.856580101505003411, -0.5137103415125721106 ) ) ;
#100240=CARTESIAN_POINT ( 'NONE',  ( 2.560454162224240271, -1.578354536769586591, 1.662689614829175211 ) ) ;
#100244=CARTESIAN_POINT ( 'NONE',  ( 5.092532722643547061, -1.235012376581679172, 1.846140261684477091 ) ) ;
#100251=CARTESIAN_POINT ( 'NONE',  ( 2.549454116737331244, -1.388485404012842261, 1.462446031800922253 ) ) ;
#100253=CARTESIAN_POINT ( 'NONE',  ( 0.8661725458788569476, -2.052963606700756394, 0.1985000389403013821 ) ) ;
#100259=CARTESIAN_POINT ( 'NONE',  ( 3.627062487484993714, -2.024900418628313936, 0.8384617360315260726 ) ) ;
#100260=CARTESIAN_POINT ( 'NONE',  ( 1.600232647554021392, -0.2440283035436350279, 2.001511509883910911 ) ) ;
#100261=CARTESIAN_POINT ( 'NONE',  ( 0.9074547957551477584, -0.8278116715597811925, -1.644758345054016191 ) ) ;
#100262=CARTESIAN_POINT ( 'NONE',  ( 5.214511053166543064, 2.117144789807279270, 0.8794703464902029477 ) ) ;
#100263=CARTESIAN_POINT ( 'NONE',  ( 4.013478867934616723, -0.9481684062532383939, -1.578073411074693899 ) ) ;
#100267=CARTESIAN_POINT ( 'NONE',  ( 3.979382468966369935, 1.719079831940514502, -0.6148086763930470378 ) ) ;
#100268=CARTESIAN_POINT ( 'NONE',  ( 4.447888798048591497, -1.802416534049579910, -0.9041112711936499791 ) ) ;
#100270=CARTESIAN_POINT ( 'NONE',  ( 4.698257824713211406, -2.261882422057570619, -0.06011341499151043322 ) ) ;
#100272=CARTESIAN_POINT ( 'NONE',  ( 0.08283480907551789285, -2.043431366640800384, -0.5094137356045270737 ) ) ;
#100273=CARTESIAN_POINT ( 'NONE',  ( 5.195788487752976081, -1.461605715988937515, -1.466586839339318882 ) ) ;
#100278=CARTESIAN_POINT ( 'NONE',  ( 2.490742943097464135, -0.3295026218355610603, -1.897965567226393979 ) ) ;
#100280=CARTESIAN_POINT ( 'NONE',  ( 0.3968417698968416674, 0.3330189415953662690, 1.941018003364772593 ) ) ;
#100284=CARTESIAN_POINT ( 'NONE',  ( 0.8793290508635929204, -1.919567575575848339, -0.9014759086384205311 ) ) ;
#100285=CARTESIAN_POINT ( 'NONE',  ( 1.881385292706035051, -2.033259550720186049, -0.8950972351880029931 ) ) ;
#100286=CARTESIAN_POINT ( 'NONE',  ( 3.364387735031381332, 0.9452183826245286191, 1.881983119561444040 ) ) ;
#100289=CARTESIAN_POINT ( 'NONE',  ( 3.385159196556942085, 0.04556868695702701727, 1.961494628812537444 ) ) ;
#100295=CARTESIAN_POINT ( 'NONE',  ( 1.617596980227502756, 1.765956010477184535, 1.173731981927571555 ) ) ;
#100298=CARTESIAN_POINT ( 'NONE',  ( 4.896903505236655185, 0.3334610245491422265, 1.933150054703360432 ) ) ;
#100300=CARTESIAN_POINT ( 'NONE',  ( 3.749029689823797806, -1.768526636652943296, 1.242828150824742961 ) ) ;
#100301=CARTESIAN_POINT ( 'NONE',  ( 2.366542893654680402, 0.08848056876738576160, -1.839231530397527736 ) ) ;
#100304=CARTESIAN_POINT ( 'NONE',  ( 4.312277775531628166, 1.592579213294993634, 0.7021690120074929320 ) ) ;
#100308=CARTESIAN_POINT ( 'NONE',  ( 1.920999885407469243, 2.016935458891587096, 0.7782144962657986387 ) ) ;
#100310=CARTESIAN_POINT ( 'NONE',  ( 4.850935385407137979, -0.9528642855485233154, 1.776740034556321568 ) ) ;
#100311=CARTESIAN_POINT ( 'NONE',  ( 1.639762333045853726, -1.565812861550972324, -1.490595759849028035 ) ) ;
#100312=CARTESIAN_POINT ( 'NONE',  ( 3.555508008102294060, 0.4801912113073670829, -1.911968381370426684 ) ) ;
#100314=B_SPLINE_CURVE_WITH_KNOTS ( 'NONE', 3,
 ( #33233, #199983, #117755, #151263, #184796, #36424, #16959, #102500, #168564, #20163 ),
 .UNSPECIFIED., .F., .F.,
 ( 4, 1, 1, 1, 1, 1, 1, 4 ),
 ( 0.000000000000000000, 0.09790276019723312406, 0.1918320694002237370, 0.2608036337010187777, 0.3626611837559554630, 0.5214803378330250538, 0.7337833476510040587, 1.000000000000000000 ),
 .UNSPECIFIED. ) ;
#100315=CARTESIAN_POINT ( 'NONE',  ( 3.544416897000971289, -1.586007893901800969, 1.120530928797113246 ) ) ;
#100324=CARTESIAN_POINT ( 'NONE',  ( 0.2709337360254741034, -1.439471777561899035, 1.672717458380864608 ) ) ;
#100326=CARTESIAN_POINT ( 'NONE',  ( 5.225427317040848507, 0.1961275920050585819, -1.951957996302315257 ) ) ;
#100327=CARTESIAN_POINT ( 'NONE',  ( 1.688125190044654556, 1.678006053171029688, 1.117831401076685660 ) ) ;
#100328=VERTEX_POINT ( 'NONE', #5036 ) ;
#100329=CARTESIAN_POINT ( 'NONE',  ( 3.749298086285374865, 0.2552367968642406115, -2.101811201404654827 ) ) ;
#100333=CARTESIAN_POINT ( 'NONE',  ( 4.101369424419714527, -1.836060619117799497, 0.1375280490283348478 ) ) ;
#100338=CARTESIAN_POINT ( 'NONE',  ( 5.730757696090861941, 1.422813033107739988, -1.572628729999878905 ) ) ;
#100341=CARTESIAN_POINT ( 'NONE',  ( 5.800091581907264704, -2.060967560761736372, -0.004405934171711199318 ) ) ;
#100343=CARTESIAN_POINT ( 'NONE',  ( 1.134942894344723507, -0.04051261866679262136, -1.860784445789311903 ) ) ;
#100344=CARTESIAN_POINT ( 'NONE',  ( 2.471991059931688106, -1.762569054296094340, -0.5325411743367302053 ) ) ;
#100349=CARTESIAN_POINT ( 'NONE',  ( 1.682535984017709874, -1.178549783888741320, 1.865657194899547733 ) ) ;
#100350=CARTESIAN_POINT ( 'NONE',  ( 5.079486683540675784, 2.113528219476542347, -0.8076395688127128158 ) ) ;
#100352=CARTESIAN_POINT ( 'NONE',  ( 4.236430684147264536, 1.109505083903281619, -1.432011362939947574 ) ) ;
#100353=CARTESIAN_POINT ( 'NONE',  ( 5.735529463276822781, 0.5494309942872098729, -1.835271804430014919 ) ) ;
#100356=CARTESIAN_POINT ( 'NONE',  ( 5.049604242677837362, 0.5861553263475408615, -1.776501995420045832 ) ) ;
#100357=CARTESIAN_POINT ( 'NONE',  ( 4.474962758555542486, 1.701137449889396747, 0.7551977096921670407 ) ) ;
#100359=CARTESIAN_POINT ( 'NONE',  ( 5.401144703012512593, 1.448466425555764658, 1.016686210146000358 ) ) ;
#100360=CARTESIAN_POINT ( 'NONE',  ( 0.07540816263147330500, 1.497505997221737273, 1.350731191893522976 ) ) ;
#100362=CARTESIAN_POINT ( 'NONE',  ( 1.471456325463766479, 0.1532790705911575568, -2.100547924479207129 ) ) ;
#100366=CARTESIAN_POINT ( 'NONE',  ( 3.533539421053989660, -0.1523460092780377639, 2.115156586662121363 ) ) ;
#100368=CARTESIAN_POINT ( 'NONE',  ( 2.109634291106620818, 1.563931847922779728, 1.278184196155268904 ) ) ;
#100373=CARTESIAN_POINT ( 'NONE',  ( 1.968271169257681752, 1.109365460190291586, 1.855047589327807778 ) ) ;
#100374=CARTESIAN_POINT ( 'NONE',  ( 6.889999999999970370, 3.679256271150095792, 2.793895465809397294 ) ) ;
#100381=CARTESIAN_POINT ( 'NONE',  ( 0.4861908890553789941, -2.175720422541329580, -0.2624175912114696252 ) ) ;
#100383=CARTESIAN_POINT ( 'NONE',  ( 1.411376899827078368, 1.996129479730743617, 1.065132602888875457 ) ) ;
#100385=CARTESIAN_POINT ( 'NONE',  ( 4.452361426671761713, -1.313546101436880109, 1.530156479064001207 ) ) ;
#100392=CARTESIAN_POINT ( 'NONE',  ( 3.690472162876729190, -0.3426837954879756731, -1.736044821310823938 ) ) ;
#100393=CARTESIAN_POINT ( 'NONE',  ( 6.247136877606230598, -1.867572634706683443, 1.175315980461520304 ) ) ;
#100397=CARTESIAN_POINT ( 'NONE',  ( 5.308220328704632784, 1.198845711980157214, -1.621194722098241003 ) ) ;
#100400=CARTESIAN_POINT ( 'NONE',  ( 2.149089010626914931, -1.500894351328721621, -1.116326037436713881 ) ) ;
#100402=CARTESIAN_POINT ( 'NONE',  ( 2.465759480183654428, -0.4578044685884518072, 2.018832516862689275 ) ) ;
#100404=CARTESIAN_POINT ( 'NONE',  ( 2.320441991784210067, -0.7354482596747033973, -1.765520077574176394 ) ) ;
#100409=CARTESIAN_POINT ( 'NONE',  ( 0.5449873876890097835, 0.1430962203496731200, 1.907122450762772425 ) ) ;
#100411=CARTESIAN_POINT ( 'NONE',  ( 2.031626174157370457, 1.878314540015123102, -0.5664888411779643862 ) ) ;
#100414=CARTESIAN_POINT ( 'NONE',  ( 5.326475955075804514, -0.9554483686352827077, -1.893264085526874974 ) ) ;
#100416=CARTESIAN_POINT ( 'NONE',  ( 6.837195077073701555, -1.761838062178729070, 0.8845485525767071699 ) ) ;
#100418=CARTESIAN_POINT ( 'NONE',  ( 1.670183121039736207, 2.007516039388768991, -0.1524388337148015193 ) ) ;
#100420=CARTESIAN_POINT ( 'NONE',  ( 0.7029266809492543677, 1.957958796488759035, 0.8061104088524527755 ) ) ;
#100422=CARTESIAN_POINT ( 'NONE',  ( 2.172408243068229439, -0.9739482337229148357, -1.826950231780352762 ) ) ;
#100426=CARTESIAN_POINT ( 'NONE',  ( 5.472635741755179417, -0.05041999219103148605, -2.090201512065153366 ) ) ;
#100428=CARTESIAN_POINT ( 'NONE',  ( 4.243042751400435186, -1.588269943899191183, 0.8999137264355041577 ) ) ;
#100429=CARTESIAN_POINT ( 'NONE',  ( 2.771877521378500742, 1.802570752484193184, -0.1794005705246705940 ) ) ;
#100434=CARTESIAN_POINT ( 'NONE',  ( 5.561621765989873900, 0.4355406452380207738, -2.163202247768724718 ) ) ;
#100438=CARTESIAN_POINT ( 'NONE',  ( 3.703681524037071071, 1.387051605615218008, 1.316649548728260344 ) ) ;
#100443=DIRECTION ( 'NONE',  ( -1.000000000000000000, 0.000000000000000000, 0.000000000000000000 ) ) ;
#100445=CARTESIAN_POINT ( 'NONE',  ( -0.09456490281532430042, -0.7861721075429689565, -1.663503389917226460 ) ) ;
#100447=CARTESIAN_POINT ( 'NONE',  ( 3.708139779478221598, -0.7553879706188313392, -1.711406342686023541 ) ) ;
#100452=CARTESIAN_POINT ( 'NONE',  ( 6.403194803628889709, -1.752124481401344358, 1.102429006916323395 ) ) ;
#100453=CARTESIAN_POINT ( 'NONE',  ( 1.775017769237042353, 1.753020666602569166, -0.9963212463810557917 ) ) ;
#100456=CARTESIAN_POINT ( 'NONE',  ( 2.941561714372803227, 0.7881326131919093037, -2.044999658057600644 ) ) ;
#100457=CARTESIAN_POINT ( 'NONE',  ( 6.393173274427864428, 1.585754722747900969, -0.9045919592586546543 ) ) ;
#100466=CARTESIAN_POINT ( 'NONE',  ( 3.825598141381767903, 0.9817388958630569595, -1.557492293685861284 ) ) ;
#100467=CARTESIAN_POINT ( 'NONE',  ( 0.3463400477153228407, 1.033117966650568986, -1.727632672016335080 ) ) ;
#100468=CARTESIAN_POINT ( 'NONE',  ( 3.497717624726462748, 2.241670729410083940, 0.5068476239948813689 ) ) ;
#100470=CARTESIAN_POINT ( 'NONE',  ( 0.6548463511123479019, 1.551493821935068906, -1.027296181188163571 ) ) ;
#100474=CARTESIAN_POINT ( 'NONE',  ( 4.904515063324526025, -1.898637117948184017, -0.2282459111111398431 ) ) ;
#100478=CARTESIAN_POINT ( 'NONE',  ( 3.632441420962172263, 0.3087965321501208726, 2.067699918487746036 ) ) ;
#100479=CARTESIAN_POINT ( 'NONE',  ( 2.852262661058731386, 0.6285613048715790185, 1.762029509812724992 ) ) ;
#100482=CARTESIAN_POINT ( 'NONE',  ( 5.478019777291557979, -1.797689181224306321, -0.3974485807837144224 ) ) ;
#100487=CARTESIAN_POINT ( 'NONE',  ( 3.668305164303451882, -1.157086425697685828, 1.279375231203205621 ) ) ;
#100493=CARTESIAN_POINT ( 'NONE',  ( 5.032167298026094748, 1.244454833084396306, 1.778855100471810280 ) ) ;
#100494=CARTESIAN_POINT ( 'NONE',  ( 2.947667120405720986, 0.6567698719579934119, -1.703645827024417914 ) ) ;
#100495=CARTESIAN_POINT ( 'NONE',  ( 0.2858946156298440844, -1.202361161835348025, -1.550730028719159215 ) ) ;
#100496=CARTESIAN_POINT ( 'NONE',  ( 5.946512563314596100, -1.495626773323457170, 1.498989405617740189 ) ) ;
#100498=CARTESIAN_POINT ( 'NONE',  ( 5.794527259016318155, 1.876155144389481721, -1.316939630280162365 ) ) ;
#100502=CARTESIAN_POINT ( 'NONE',  ( 1.190261156817543631, 1.266008754425467897, 1.700926646755014593 ) ) ;
#100506=CARTESIAN_POINT ( 'NONE',  ( 6.543812728621629660, 1.490886027097729105, 1.578480410219210928 ) ) ;
#100509=CARTESIAN_POINT ( 'NONE',  ( 0.8212868038825784645, 1.678483586613238154, -1.455034836404971665 ) ) ;
#100511=CARTESIAN_POINT ( 'NONE',  ( 6.434220164165640021, -1.621181005584397372, -1.198863592720422977 ) ) ;
#100513=CARTESIAN_POINT ( 'NONE',  ( 4.135635188098309101, 1.943850041002512352, -0.6901024340064102480 ) ) ;
#100520=CARTESIAN_POINT ( 'NONE',  ( 1.060620546929908148, -1.890798925694850974, -0.8922787324358200101 ) ) ;
#100521=CARTESIAN_POINT ( 'NONE',  ( 4.975232503164924935, -2.001511053420693020, -0.2440319332882301961 ) ) ;
#100522=CARTESIAN_POINT ( 'NONE',  ( 4.968220237687512864, -1.735557695065930606, -0.6152675618510683453 ) ) ;
#100524=CARTESIAN_POINT ( 'NONE',  ( 2.168594647197068070, -1.575507694510763335, -0.7022964154167319339 ) ) ;
#100525=CARTESIAN_POINT ( 'NONE',  ( -0.1882626618336727398, -1.244567986390752390, -1.587255334073833790 ) ) ;
#100526=CARTESIAN_POINT ( 'NONE',  ( 2.215865853697509102, 2.230823145726851475, 0.5541181435367804609 ) ) ;
#100528=CARTESIAN_POINT ( 'NONE',  ( 1.739923964384773258, -1.638176463808267647, -1.560613564838263523 ) ) ;
#100529=CARTESIAN_POINT ( 'NONE',  ( 3.035867697866540205, -1.414839191968674470, -1.560218430392734446 ) ) ;
#100534=CARTESIAN_POINT ( 'NONE',  ( 5.593750000000004441, -1.895863743164200921, -0.7852924748296893354 ) ) ;
#100538=CARTESIAN_POINT ( 'NONE',  ( 4.851916359752673991, -1.571614379473328160, -1.570179378767898370 ) ) ;
#100539=CARTESIAN_POINT ( 'NONE',  ( 3.521585679250069045, -1.305302140894725627, -1.760141160621036649 ) ) ;
#100544=CARTESIAN_POINT ( 'NONE',  ( 6.890000000000047642, 2.940278081043229186, 2.731889818495436995 ) ) ;
#100546=CARTESIAN_POINT ( 'NONE',  ( 5.168275554957600271, 2.118074532352266282, -0.1063875075708180934 ) ) ;
#100550=CARTESIAN_POINT ( 'NONE',  ( 6.807524309086420367, -0.4794501827766698421, 2.115671360755105646 ) ) ;
#100556=CARTESIAN_POINT ( 'NONE',  ( 1.610509732637079638, -0.2130687159686726062, 1.727248725346673952 ) ) ;
#100561=CARTESIAN_POINT ( 'NONE',  ( 5.735289742212391850, -1.956171686333206816, 0.9202595734885756773 ) ) ;
#100565=CARTESIAN_POINT ( 'NONE',  ( 5.102478102407745908, -0.7247817745383768884, -2.036717088958202471 ) ) ;
#100567=CARTESIAN_POINT ( 'NONE',  ( 5.887953105907347329, -0.8888255776743571035, 1.759709591642463433 ) ) ;
#100568=CARTESIAN_POINT ( 'NONE',  ( 4.674945122873967129, -0.7415060156777570910, -1.567401138452922060 ) ) ;
#100570=CARTESIAN_POINT ( 'NONE',  ( 2.015410700679621137, -2.124826835150806392, 0.5361769018528695918 ) ) ;
#100571=CARTESIAN_POINT ( 'NONE',  ( 2.520946605012349018, 1.507388781920895759, -1.747272692061818011 ) ) ;
#100572=CARTESIAN_POINT ( 'NONE',  ( 5.220021542613917376, -1.098816822949649774, -1.743189258048108314 ) ) ;
#100573=CARTESIAN_POINT ( 'NONE',  ( 0.1287130127310652239, -1.775900012335431155, 0.7861216482863192523 ) ) ;
#100577=CARTESIAN_POINT ( 'NONE',  ( 3.357788437482766675, -1.608272433257527556, -1.382313803475518244 ) ) ;
#100579=CARTESIAN_POINT ( 'NONE',  ( 1.354138928560550292, 0.1455316553338575902, -2.011204400906742240 ) ) ;
#100581=CARTESIAN_POINT ( 'NONE',  ( 4.243358471946375943, -1.921622210924242458, 1.084848892642875429 ) ) ;
#100583=CARTESIAN_POINT ( 'NONE',  ( 2.096333906143353243, 1.839810448830980105, 0.2789567515945317600 ) ) ;
#100584=CARTESIAN_POINT ( 'NONE',  ( -0.1290005225502675879, -0.006633637972621592160, -2.173875058097324064 ) ) ;
#100588=CARTESIAN_POINT ( 'NONE',  ( 6.925078400183553029, 0.5745968962584145912, 2.096956839219825230 ) ) ;
#100590=CARTESIAN_POINT ( 'NONE',  ( 3.063408159219972227, 0.3037436250956357386, -2.038260327603860222 ) ) ;
#100593=CARTESIAN_POINT ( 'NONE',  ( 2.174478703267632707, 0.8655064541149575241, 1.824978016274068082 ) ) ;
#100596=CARTESIAN_POINT ( 'NONE',  ( 2.342715047087840397, 0.4503528687099351280, 2.010914609654746332 ) ) ;
#100597=CARTESIAN_POINT ( 'NONE',  ( 6.883263157960364254, -0.001323150302089577462, 1.953658984494696549 ) ) ;
#100600=CARTESIAN_POINT ( 'NONE',  ( -0.1411974294641837879, -0.0004739540254219963859, -1.900147702309516795 ) ) ;
#100601=CARTESIAN_POINT ( 'NONE',  ( 1.341482821134845738, 1.838956754096718882, 0.09199767257135617327 ) ) ;
#100602=CARTESIAN_POINT ( 'NONE',  ( 5.549527019956425278, -1.737703232767298545, -1.360318885177333570 ) ) ;
#100604=CARTESIAN_POINT ( 'NONE',  ( 1.810078809455554438, -2.145489296895970011, 0.2626290421628638128 ) ) ;
#100606=CARTESIAN_POINT ( 'NONE',  ( 2.079314900164643820, 1.561883299538204151, 1.275554356156020308 ) ) ;
#100610=CARTESIAN_POINT ( 'NONE',  ( 4.258636414635104117, -1.461677231104720143, 1.323132448414195528 ) ) ;
#100611=CARTESIAN_POINT ( 'NONE',  ( 3.397672961473942266, -1.985868886743065609, 0.3494831190506141883 ) ) ;
#100615=CARTESIAN_POINT ( 'NONE',  ( 6.621705515693503408, -2.043321748007483674, 0.5098342655636013410 ) ) ;
#100617=CARTESIAN_POINT ( 'NONE',  ( 5.916483165358986440, 0.8355632440216669288, 1.894440869009452300 ) ) ;
#100621=CARTESIAN_POINT ( 'NONE',  ( 4.711197416960428264, 1.676919581237258372, -1.125501318796730876 ) ) ;
#100623=CARTESIAN_POINT ( 'NONE',  ( 0.4970291366834606039, 0.3490122959711927098, 2.032667101136710563 ) ) ;
#100630=CARTESIAN_POINT ( 'NONE',  ( 2.787735123443566110, -2.026669663610313865, 0.7793237752812106622 ) ) ;
#100632=CARTESIAN_POINT ( 'NONE',  ( 6.626263010475290649, 1.250585457657760635, -1.762915812992614129 ) ) ;
#100634=CARTESIAN_POINT ( 'NONE',  ( 3.263068207883256466, 1.795673413606920565, -0.4063787724192802209 ) ) ;
#100636=CARTESIAN_POINT ( 'NONE',  ( 4.634432875810733599, 0.3748786239917039631, 2.159109584303263940 ) ) ;
#100638=CARTESIAN_POINT ( 'NONE',  ( 5.084992976345711568, -0.2718087151927280343, -2.246069130642995404 ) ) ;
#100642=( GEOMETRIC_REPRESENTATION_CONTEXT ( 3 ) GLOBAL_UNCERTAINTY_ASSIGNED_CONTEXT ( ( #91843 ) ) GLOBAL_UNIT_ASSIGNED_CONTEXT ( ( #145996, #98288, #97235 ) ) REPRESENTATION_CONTEXT ( 'NONE', 'WORKASPACE' ) );
#100645=CARTESIAN_POINT ( 'NONE',  ( 6.925078400183545035, 0.003529629153843985134, 1.755452343125718073 ) ) ;
#100646=CARTESIAN_POINT ( 'NONE',  ( 4.108068219531130438, -0.7683648849950328596, 1.860876229713221086 ) ) ;
#100648=CARTESIAN_POINT ( 'NONE',  ( 3.540152450731326450, 0.9484212380423739930, -1.880392733946538719 ) ) ;
#100649=CARTESIAN_POINT ( 'NONE',  ( 1.476048981871850518, -1.906537803873010084, -0.1858940877890648546 ) ) ;
#100652=CARTESIAN_POINT ( 'NONE',  ( 1.539439451811152493, 1.821048954109681706, -0.7507764504887379786 ) ) ;
#100653=CARTESIAN_POINT ( 'NONE',  ( 0.1978467685152424937, -1.870139902624564865, -0.05068021481659244765 ) ) ;
#100654=CARTESIAN_POINT ( 'NONE',  ( 0.8890225878602634468, 0.1407106197201784259, 1.956863499422318631 ) ) ;
#100655=CARTESIAN_POINT ( 'NONE',  ( 6.469024005207689498, -1.393930998056407189, 1.156871781951673395 ) ) ;
#100661=CARTESIAN_POINT ( 'NONE',  ( 5.700035372616791385, -1.870836310086241294, 0.001406584917262864625 ) ) ;
#100662=CARTESIAN_POINT ( 'NONE',  ( 5.577033793921920335, 1.910671465402475677, 0.7975372692515870776 ) ) ;
#100671=CARTESIAN_POINT ( 'NONE',  ( 6.162552467866693640, -0.7048080804108979303, -1.831077584432870609 ) ) ;
#100673=CARTESIAN_POINT ( 'NONE',  ( 2.811874868751465417, -1.677748492350576770, 1.117661080827489606 ) ) ;
#100674=CARTESIAN_POINT ( 'NONE',  ( 3.538217205509861962, 0.6946294275822698649, 1.785521036047182486 ) ) ;
#100677=CARTESIAN_POINT ( 'NONE',  ( 1.523247060345904291, -2.062048068855956373, 0.7425582295156887280 ) ) ;
#100678=CARTESIAN_POINT ( 'NONE',  ( 0.2333690889706682703, 0.003390530909083006028, -2.053566628440507635 ) ) ;
#100679=CARTESIAN_POINT ( 'NONE',  ( 2.811613793402362393, -1.850737340378521223, 0.2705540153197931730 ) ) ;
#100681=CARTESIAN_POINT ( 'NONE',  ( 4.640889591357927557, 1.927823495868080439, 0.5801764560204000221 ) ) ;
#100684=CARTESIAN_POINT ( 'NONE',  ( 4.060252369235962888, -1.217431538915053180, 1.732033588162092297 ) ) ;
#100686=CARTESIAN_POINT ( 'NONE',  ( 5.986797818411375260, 1.994257276370488219, 0.5558945855626205024 ) ) ;
#100687=CARTESIAN_POINT ( 'NONE',  ( 2.314113491060950434, 1.363558105167931966, -1.585015408884550503 ) ) ;
#100689=CARTESIAN_POINT ( 'NONE',  ( 1.096240241049123210, -0.4132495022837120446, -1.674402075930980338 ) ) ;
#100693=CARTESIAN_POINT ( 'NONE',  ( 0.1333692844072559280, 0.001398348041498076455, -2.053671342968105051 ) ) ;
#100694=PRESENTATION_STYLE_ASSIGNMENT (( #85510 ) ) ;
#100699=CARTESIAN_POINT ( 'NONE',  ( 0.1877650794145177826, 1.041282258498995361, 1.482055844031314518 ) ) ;
#100710=CARTESIAN_POINT ( 'NONE',  ( 2.541259301162884121, 1.702954558545258346, -0.7510573925902948034 ) ) ;
#100711=CARTESIAN_POINT ( 'NONE',  ( 0.3861688966736884776, -0.6463253627202453222, -1.803393044390422029 ) ) ;
#100712=CARTESIAN_POINT ( 'NONE',  ( 0.2938078718510480081, 1.976988316466289142, -0.7672523047414223640 ) ) ;
#100717=CARTESIAN_POINT ( 'NONE',  ( 4.803538196489102852, -1.519661447750167982, -1.252675939642827529 ) ) ;
#100718=CARTESIAN_POINT ( 'NONE',  ( 1.717596852896427606, 1.764750374324057347, 1.175337852406685535 ) ) ;
#100722=CARTESIAN_POINT ( 'NONE',  ( 6.070311387754347088, -2.079788119406985825, -0.6908379657195938828 ) ) ;
#100724=CARTESIAN_POINT ( 'NONE',  ( 3.856402372034730686, 0.6923319331257683507, 1.797858303039111982 ) ) ;
#100726=CARTESIAN_POINT ( 'NONE',  ( 0.6217474354073999621, -0.9722136304874777757, -1.544982199245432897 ) ) ;
#100727=CARTESIAN_POINT ( 'NONE',  ( 0.4873205249028254027, -0.2742316277877173691, -2.189713876267186166 ) ) ;
#100731=CARTESIAN_POINT ( 'NONE',  ( 6.684429667774410611, 1.136775344189003611, -1.608021923639752604 ) ) ;
#100732=CARTESIAN_POINT ( 'NONE',  ( 0.6615421549095920062, 0.9584981283930308349, 1.688995467024148045 ) ) ;
#100733=CARTESIAN_POINT ( 'NONE',  ( 6.679114621301890153, -1.074570768553984479, -2.031732957927368410 ) ) ;
#100735=CARTESIAN_POINT ( 'NONE',  ( 4.592532296707762640, 1.824399381888962779, 0.3660411688805977337 ) ) ;
#100740=CARTESIAN_POINT ( 'NONE',  ( 0.01162390915069450026, -2.148011843722149372, 0.4338911918742721641 ) ) ;
#100744=CARTESIAN_POINT ( 'NONE',  ( 1.049113529465800054, -1.437755431736492673, -1.125068434497819680 ) ) ;
#100746=CARTESIAN_POINT ( 'NONE',  ( 3.287501071874948000, 1.364548152031169082, -1.070007228145404943 ) ) ;
#100750=CARTESIAN_POINT ( 'NONE',  ( 6.656878040733529289, -1.407521694628325770, 1.162499734694094844 ) ) ;
#100751=CARTESIAN_POINT ( 'NONE',  ( 4.592600981049492326, 1.923087700504518605, 0.3867253955378775476 ) ) ;
#100754=CARTESIAN_POINT ( 'NONE',  ( 5.233110275169113201, 1.959380141031796585, 0.8112103084707968925 ) ) ;
#100759=CARTESIAN_POINT ( 'NONE',  ( 3.063400401570901543, 1.746483293306470674, 1.111379191485066364 ) ) ;
#100762=CARTESIAN_POINT ( 'NONE',  ( 3.287964078406432566, 1.811126957681759908, -1.415446460160358688 ) ) ;
#100770=CARTESIAN_POINT ( 'NONE',  ( 4.236511230858605259, 1.172298487584079396, -1.510895503047122945 ) ) ;
#100772=CARTESIAN_POINT ( 'NONE',  ( 5.508750344372229435, 1.303470515519134842, -1.129639352617429537 ) ) ;
#100773=CARTESIAN_POINT ( 'NONE',  ( 3.169157936054858293, 1.820986098869777470, -0.8666075021629695563 ) ) ;
#100774=CARTESIAN_POINT ( 'NONE',  ( 4.658965222740456547, 1.322560505849355694, 1.879950767321969529 ) ) ;
#100776=CARTESIAN_POINT ( 'NONE',  ( 1.067327838873022516, -1.996528553209110379, -0.9406146916221403975 ) ) ;
#100778=CARTESIAN_POINT ( 'NONE',  ( 5.378098658424382172, -0.9825891054615911724, 1.471664417823245197 ) ) ;
#100781=CARTESIAN_POINT ( 'NONE',  ( 1.482826411003408840, -0.3401602582979300626, -2.266773921731002339 ) ) ;
#100782=CARTESIAN_POINT ( 'NONE',  ( 6.650350966976619205, -1.419654684173769166, 1.172063944840713523 ) ) ;
#100788=CARTESIAN_POINT ( 'NONE',  ( 0.4851436980863755299, 2.077851564382672933, 0.6296362999115376891 ) ) ;
#100789=CARTESIAN_POINT ( 'NONE',  ( 1.253139057289072822, 0.1435168058863903473, -2.011451928166609893 ) ) ;
#100791=CARTESIAN_POINT ( 'NONE',  ( 5.074797080785846681, -1.814676937445957039, -0.6471642872378483569 ) ) ;
#100793=CARTESIAN_POINT ( 'NONE',  ( 2.320824347369263574, -0.8547976213506520704, -2.050556073580122707 ) ) ;
#100800=CARTESIAN_POINT ( 'NONE',  ( 4.739680933654325301, 1.736262504677583474, 0.1214163294094624396 ) ) ;
#100802=CARTESIAN_POINT ( 'NONE',  ( 2.892962425504439050, 0.2373818416543191645, 1.947367909387688112 ) ) ;
#100807=CARTESIAN_POINT ( 'NONE',  ( 0.5024796060203519099, 2.057031790779086045, 0.1535979213492833784 ) ) ;
#100811=CARTESIAN_POINT ( 'NONE',  ( 1.411376899827078368, 1.996129479730743617, 1.065132602888875457 ) ) ;
#100814=CARTESIAN_POINT ( 'NONE',  ( 2.565516880305099612, 1.835255434019352094, -0.3607447438512822457 ) ) ;
#100815=CARTESIAN_POINT ( 'NONE',  ( 1.230678901735713593, 1.732143722507371475, 0.08558704247295551015 ) ) ;
#100816=CARTESIAN_POINT ( 'NONE',  ( 5.425378541715013547, -1.389685604419872655, -1.694579525865948844 ) ) ;
#100817=CARTESIAN_POINT ( 'NONE',  ( 5.702268328713489431, -2.307758713666784534, -0.007378162171353326235 ) ) ;
#100818=CARTESIAN_POINT ( 'NONE',  ( 0.9540633210794751129, 2.058568143186993105, -0.1002533246910724124 ) ) ;
#100819=CARTESIAN_POINT ( 'NONE',  ( 3.187375889530741802, -0.7864489302777454283, 1.775747734548535961 ) ) ;
#100821=CARTESIAN_POINT ( 'NONE',  ( 5.993391575003323091, 1.416176893967495687, 1.222094818194748189 ) ) ;
#100822=CARTESIAN_POINT ( 'NONE',  ( 0.8750000000000005551, 2.052068128417951609, -5.168192407616667353E-14 ) ) ;
#100824=CARTESIAN_POINT ( 'NONE',  ( 0.4558326304775248139, 1.278721518017480685, 1.171137906463788347 ) ) ;
#100827=CARTESIAN_POINT ( 'NONE',  ( 4.834611377684539413, 0.6298767044488963185, -1.915599524792414465 ) ) ;
#100831=CARTESIAN_POINT ( 'NONE',  ( 2.174178736149934732, -1.123764393468742684, 1.438770255985911684 ) ) ;
#100836=ORIENTED_EDGE ( 'NONE', *, *, #203422, .F. ) ;
#100840=CARTESIAN_POINT ( 'NONE',  ( 6.569012466128139494, -1.559778377529440929, 1.282785893457456750 ) ) ;
#100841=CARTESIAN_POINT ( 'NONE',  ( 0.5926325054007793858, -1.174586488569592690, 1.765252418913294319 ) ) ;
#100845=CARTESIAN_POINT ( 'NONE',  ( 5.014554672588167783, 1.422794387333496946, -1.491179163509145811 ) ) ;
#100846=CARTESIAN_POINT ( 'NONE',  ( 5.432267593368638181, -1.591316862017605471, -1.238322901282742805 ) ) ;
#100855=CARTESIAN_POINT ( 'NONE',  ( 4.903672622533055581, 0.3418847601762939337, 1.986741992616162245 ) ) ;
#100856=CARTESIAN_POINT ( 'NONE',  ( 5.191278274421009975, -0.6593680717656666967, 1.719199333795925710 ) ) ;
#100858=CARTESIAN_POINT ( 'NONE',  ( -0.02338929933905046013, 4.099262448077650944, -2.266018688142543258 ) ) ;
#100859=CARTESIAN_POINT ( 'NONE',  ( 2.666999619196269045, -1.590435880060107499, 1.672335932400937253 ) ) ;
#100861=CARTESIAN_POINT ( 'NONE',  ( 5.220075184997099882, -1.151474455836385857, -1.829185309946822713 ) ) ;
#100863=CARTESIAN_POINT ( 'NONE',  ( 6.462460624273299814, -1.686435539877573220, -0.7394478613861471539 ) ) ;
#100865=CARTESIAN_POINT ( 'NONE',  ( 4.130415602100383943, 0.2865403768554532493, -2.280420282979139124 ) ) ;
#100868=CARTESIAN_POINT ( 'NONE',  ( 3.238977024203249400, -1.650389259550872456, 0.8806316622528218563 ) ) ;
#100869=CARTESIAN_POINT ( 'NONE',  ( 1.212987991671743204, 1.561712320281399835, -1.103468303573502673 ) ) ;
#100872=CARTESIAN_POINT ( 'NONE',  ( 3.352369063006555905, 2.207063162671081713, 4.936380160885933677E-05 ) ) ;
#100873=CARTESIAN_POINT ( 'NONE',  ( 6.620655732516614655, 0.0004550665019913459623, 2.073887158236030093 ) ) ;
#100878=CARTESIAN_POINT ( 'NONE',  ( 0.7199194774221047144, -1.050951492028269874, -1.667678589039832904 ) ) ;
#100879=CARTESIAN_POINT ( 'NONE',  ( 6.445943507803128192, 0.8898977879068777908, -2.129411633396756098 ) ) ;
#100880=CARTESIAN_POINT ( 'NONE',  ( 1.170277241841523264, -0.8789641444944886750, -1.754005360843587047 ) ) ;
#100881=CARTESIAN_POINT ( 'NONE',  ( 4.118078732422246979, 2.047561256575948452, -0.2476526470514497091 ) ) ;
#100884=EDGE_LOOP ( 'NONE', ( #68128, #48416, #89355, #31084 ) ) ;
#100889=CARTESIAN_POINT ( 'NONE',  ( 6.162576015390932582, -0.7755629475397389783, -2.028117739495437277 ) ) ;
#100891=CARTESIAN_POINT ( 'NONE',  ( 6.392148736875968851, -0.4980823202534767624, -1.772533436741857260 ) ) ;
#100894=CARTESIAN_POINT ( 'NONE',  ( 1.088877184111051832, 1.652420591378001014, -0.8765777015899288704 ) ) ;
#100898=CARTESIAN_POINT ( 'NONE',  ( 1.014147342612067737, -1.912461472154961317, 0.0006945104691555297090 ) ) ;
#100899=CARTESIAN_POINT ( 'NONE',  ( 3.150976108479891735, -1.446007784402236318, -1.020181273144848744 ) ) ;
#100900=CARTESIAN_POINT ( 'NONE',  ( 0.4164788467995067522, -0.6444665046171775824, -1.800526059235994403 ) ) ;
#100902=CARTESIAN_POINT ( 'NONE',  ( 4.833546035289306708, 0.5969252065377036454, -1.820314225251006945 ) ) ;
#100904=CARTESIAN_POINT ( 'NONE',  ( 5.934039001034627780, 1.171926208273272207, 1.582800714458313385 ) ) ;
#100905=CARTESIAN_POINT ( 'NONE',  ( 0.7562902151678205787, 0.8540304730459827853, -1.941197329821432227 ) ) ;
#100907=CARTESIAN_POINT ( 'NONE',  ( 3.977312496258199825, 1.761605600429091201, -0.6297503393934977822 ) ) ;
#100908=CARTESIAN_POINT ( 'NONE',  ( 0.9964003531478006215, -0.4411313887022934033, -1.771462291394958255 ) ) ;
#100910=CARTESIAN_POINT ( 'NONE',  ( 3.914836437932368796, 1.561248537261412883, -1.560010120355350471 ) ) ;
#100914=CARTESIAN_POINT ( 'NONE',  ( 0.6958484739430546018, -1.457389369856504358, -1.459923026165359516 ) ) ;
#100919=CARTESIAN_POINT ( 'NONE',  ( 0.1753634416057497647, 2.004068818557998011, -2.558292918872175914 ) ) ;
#100921=CARTESIAN_POINT ( 'NONE',  ( 3.191909353267761151, -1.388477207968623839, -1.535938721777901472 ) ) ;
#100923=CARTESIAN_POINT ( 'NONE',  ( 1.071799524545346216, 2.083542002058445863, -0.5754571431841256635 ) ) ;
#100925=CARTESIAN_POINT ( 'NONE',  ( 1.998700280430569576, -1.981126291604264233, -0.3917822458236255301 ) ) ;
#100929=CARTESIAN_POINT ( 'NONE',  ( 6.573592277014387975, 1.495820547097841846, -1.351949839681468868 ) ) ;
#100930=CARTESIAN_POINT ( 'NONE',  ( 0.7433754753295095385, 0.3886281223182270761, -1.978556061772406505 ) ) ;
#100932=CARTESIAN_POINT ( 'NONE',  ( 5.337503337980974649, 0.8888059580158399475, -2.003405333693850654 ) ) ;
#100934=CARTESIAN_POINT ( 'NONE',  ( 3.304848191199673213, -0.3775801424153284458, -1.874573493127674961 ) ) ;
#100938=CARTESIAN_POINT ( 'NONE',  ( 0.5797041155359906606, -0.7231210598357665775, 1.882482590253447663 ) ) ;
#100940=CARTESIAN_POINT ( 'NONE',  ( 0.8203738007961014489, 1.359819376615223785, -1.845384199244608947 ) ) ;
#100942=CARTESIAN_POINT ( 'NONE',  ( 4.594587176762323644, -0.3796550294026636574, -1.682289508650273602 ) ) ;
#100943=CARTESIAN_POINT ( 'NONE',  ( -0.1399997263889820043, 5.722209607272843002, -2.594334538518060729 ) ) ;
#100945=CARTESIAN_POINT ( 'NONE',  ( -0.02264175331115856823, -0.002534049983801976106, -2.089079740194143220 ) ) ;
#100946=CARTESIAN_POINT ( 'NONE',  ( 1.486689167417578394, 1.889818972856545987, 0.5264814339432166701 ) ) ;
#100949=CARTESIAN_POINT ( 'NONE',  ( 0.07556134207192634344, 1.307170157424314638, -2.493659143521540500 ) ) ;
#100952=CARTESIAN_POINT ( 'NONE',  ( 4.354050602105923318, 0.7703955181818689102, -1.639620356061684436 ) ) ;
#100956=CARTESIAN_POINT ( 'NONE',  ( 5.285751626526108637, 1.744147384919532140, -0.4889748023358466145 ) ) ;
#100960=COLOUR_RGB ( '', 0.40784314, 0.44705882, 0.49803922) ;
#100961=CARTESIAN_POINT ( 'NONE',  ( 5.916418678859147740, 0.7547467877644217227, 1.701316312257817875 ) ) ;
#100963=CARTESIAN_POINT ( 'NONE',  ( 3.866719127221716512, -0.1911932653220274059, -1.906053554140298756 ) ) ;
#100971=CARTESIAN_POINT ( 'NONE',  ( 1.024558638192473170, 1.287004556549703693, -1.736669753874709343 ) ) ;
#100974=CARTESIAN_POINT ( 'NONE',  ( 0.8678470384533981674, 0.8956018474440343713, 1.590720368640268001 ) ) ;
#100976=CARTESIAN_POINT ( 'NONE',  ( 3.311362000969253039, -0.3573404788377898544, 1.790086433339547201 ) ) ;
#100978=CARTESIAN_POINT ( 'NONE',  ( 1.599720133015330337, 1.321132142916726204, 1.382909031182079307 ) ) ;
#100980=CARTESIAN_POINT ( 'NONE',  ( 2.805082309988204514, -1.639025760435019130, 1.091792480472515647 ) ) ;
#100981=CARTESIAN_POINT ( 'NONE',  ( 5.284693219347969873, 1.710810618512406789, -0.9191280305995457311 ) ) ;
#100984=CARTESIAN_POINT ( 'NONE',  ( 4.658503719480325600, 2.115088938745744329, 0.1532479335744421078 ) ) ;
#100995=CARTESIAN_POINT ( 'NONE',  ( 5.320859459983126705, 1.688362619374352613, 0.6951667914897319278 ) ) ;
#101001=CARTESIAN_POINT ( 'NONE',  ( 5.963714631206167738, 1.842656449598079060, -0.3214700631931910468 ) ) ;
#101003=CARTESIAN_POINT ( 'NONE',  ( 3.264201069286599477, 0.8669165009558920110, 1.720499056138290683 ) ) ;
#101011=CARTESIAN_POINT ( 'NONE',  ( 1.564221677423253798, -1.129412574612179920, 1.790659096458546706 ) ) ;
#101014=CARTESIAN_POINT ( 'NONE',  ( 6.719590346122157776, 0.3599300073104904074, -2.038585587018165945 ) ) ;
#101015=CARTESIAN_POINT ( 'NONE',  ( 1.821575194732877545, 1.059174331173462935, -1.505913648122420900 ) ) ;
#101019=CARTESIAN_POINT ( 'NONE',  ( 1.834309667284042433, 2.267783887084608097, 0.3333485250246841503 ) ) ;
#101020=CARTESIAN_POINT ( 'NONE',  ( 0.1174333910212103232, -1.791171220025630895, 0.3524246893974944395 ) ) ;
#101024=CARTESIAN_POINT ( 'NONE',  ( 0.5627444733627232631, 0.5882401669465211480, 1.925320163072720359 ) ) ;
#101025=CARTESIAN_POINT ( 'NONE',  ( 0.5847188370675902025, 1.875566754216885013, 0.5750099747552291918 ) ) ;
#101030=CARTESIAN_POINT ( 'NONE',  ( 3.802746959959231177, 1.793210335683467216, 1.074525653306056316 ) ) ;
#101031=CARTESIAN_POINT ( 'NONE',  ( 2.658786778619155022, -1.538754371767250495, -0.8742638447295988380 ) ) ;
#101035=CARTESIAN_POINT ( 'NONE',  ( 5.015721488424509822, -1.223180480392561886, -1.938471153541870384 ) ) ;
#101036=CARTESIAN_POINT ( 'NONE',  ( 2.993823619545363801, -0.5058645990140339110, -1.665172204756032448 ) ) ;
#101040=CARTESIAN_POINT ( 'NONE',  ( 2.758840240711700531, -1.728971274941538017, -0.1308756186972348801 ) ) ;
#101041=CARTESIAN_POINT ( 'NONE',  ( 3.315042099977282497, -1.646035655820307309, 1.415953490726479469 ) ) ;
#101043=CARTESIAN_POINT ( 'NONE',  ( 4.751185534883737738, 0.1928377863454934504, -2.007255887737584121 ) ) ;
#101044=CARTESIAN_POINT ( 'NONE',  ( 1.187500000000001110, -1.451031289061072815, 1.451031289061169183 ) ) ;
#101046=CARTESIAN_POINT ( 'NONE',  ( 1.852440960305309137, 0.6018503411110776025, 1.830038407220703656 ) ) ;
#101048=CARTESIAN_POINT ( 'NONE',  ( 5.115582552657226501, 1.816446842268246931, 1.278514946224351689 ) ) ;
#101050=CARTESIAN_POINT ( 'NONE',  ( -0.1108833634136975610, 0.7331455517814323697, -1.980187714524218823 ) ) ;
#101056=CARTESIAN_POINT ( 'NONE',  ( 6.057081135787192316, 1.604708697955498087, -1.128374156723031430 ) ) ;
#101059=CARTESIAN_POINT ( 'NONE',  ( 6.573497657123517079, 2.167905964706399846, -0.6471699410235329797 ) ) ;
#101064=CARTESIAN_POINT ( 'NONE',  ( 3.947761307511790552, 1.492003129663575622, 1.424497906600069363 ) ) ;
#101068=CARTESIAN_POINT ( 'NONE',  ( 6.327412175546781370, -1.761338861328298089, 0.6302073946208713862 ) ) ;
#101069=CARTESIAN_POINT ( 'NONE',  ( 4.658689525625823613, 1.003974855541647004, 1.413729434382102079 ) ) ;
#101070=CARTESIAN_POINT ( 'NONE',  ( 4.809955069398625938, 1.195453170786121788, -1.265177307932338513 ) ) ;
#101072=CARTESIAN_POINT ( 'NONE',  ( 2.226505721922732661, 2.224568380592424344, 0.5530147644091478742 ) ) ;
#101074=CARTESIAN_POINT ( 'NONE',  ( 5.724191925653110857, 2.015179739716387974, 0.5568145835738461669 ) ) ;
#101075=CARTESIAN_POINT ( 'NONE',  ( 0.02305342982030639601, -1.130023889514218505, -1.454075609423427728 ) ) ;
#101077=CARTESIAN_POINT ( 'NONE',  ( 1.072888940501380839, -0.9041080511620370741, 1.802418165037560138 ) ) ;
#101081=CARTESIAN_POINT ( 'NONE',  ( 3.686284471605893120, 1.179319764668992576, 1.762089746328721507 ) ) ;
#101083=CARTESIAN_POINT ( 'NONE',  ( 5.162654993523497993, -1.319871331358621669, 1.261628347558927166 ) ) ;
#101090=CARTESIAN_POINT ( 'NONE',  ( 2.918227964375613048, -2.017298000423489501, 0.1032239234411459483 ) ) ;
#101091=CARTESIAN_POINT ( 'NONE',  ( 6.704147062870869256, -2.206433763861126884, 0.04732420095975712476 ) ) ;
#101094=CARTESIAN_POINT ( 'NONE',  ( 3.590524784426767813, 1.814595775041549564, 0.4119230038364861679 ) ) ;
#101104=CARTESIAN_POINT ( 'NONE',  ( 1.915017753259074862, 0.5389909111754992432, 1.648018863455216643 ) ) ;
#101105=CARTESIAN_POINT ( 'NONE',  ( 0.9018503542332901857, 1.320273433284512521, -1.133937880871397796 ) ) ;
#101106=CARTESIAN_POINT ( 'NONE',  ( 0.1656154469977044186, -2.063490973871735967, -1.033197247175041467 ) ) ;
#101109=CARTESIAN_POINT ( 'NONE',  ( 1.880222553438152033, -1.104958259108330898, 1.739320704499922154 ) ) ;
#101110=CARTESIAN_POINT ( 'NONE',  ( 0.1927366488196740335, -1.238295061544148812, -1.591656064170659191 ) ) ;
#101113=CARTESIAN_POINT ( 'NONE',  ( 0.4089732319989903275, 1.714023354001862787, 0.9739579164984181192 ) ) ;
#101114=CARTESIAN_POINT ( 'NONE',  ( 5.150612376422202487, 1.885107930906554152, 0.3209214958604587054 ) ) ;
#101116=CARTESIAN_POINT ( 'NONE',  ( 5.953802724510455668, 0.6443607167232848765, -2.110727517106169682 ) ) ;
#101121=CARTESIAN_POINT ( 'NONE',  ( -0.1048592448738161903, -0.1538584160990438265, -1.986454975908092058 ) ) ;
#101123=CARTESIAN_POINT ( 'NONE',  ( 3.680997481958053541, -2.223193225534472628, -0.6181044232122161475 ) ) ;
#101124=CARTESIAN_POINT ( 'NONE',  ( 4.422284181769401634, 0.9229163912191931107, 1.731201473044993167 ) ) ;
#101125=CARTESIAN_POINT ( 'NONE',  ( 1.112071775475082402, 1.959765382314464732, -0.09068415226199526280 ) ) ;
#101129=CARTESIAN_POINT ( 'NONE',  ( -0.1704767588886099972, -1.641208087572191276, -1.337381612054800772 ) ) ;
#101133=CARTESIAN_POINT ( 'NONE',  ( 3.186559800492471783, 1.209906992153013894, -1.802498320862821579 ) ) ;
#101135=CARTESIAN_POINT ( 'NONE',  ( 1.301209403646291118, -0.3165094942152619772, -2.096747597609450953 ) ) ;
#101140=CARTESIAN_POINT ( 'NONE',  ( 1.845067233098520942, -1.742569257963645146, 1.099794920586109725 ) ) ;
#101144=CARTESIAN_POINT ( 'NONE',  ( 0.07755575628181145265, 6.946778278137147211, -2.783982195446454533 ) ) ;
#101147=CARTESIAN_POINT ( 'NONE',  ( 4.881465217424630687, 0.1836680969147832243, -1.903426456924644183 ) ) ;
#101150=CARTESIAN_POINT ( 'NONE',  ( 1.353188757747030957, -1.783583821274600911, 1.391813662893444548 ) ) ;
#101153=CARTESIAN_POINT ( 'NONE',  ( 1.423755586445039745, -1.797672382977614669, 0.2236433623570739382 ) ) ;
#101154=CARTESIAN_POINT ( 'NONE',  ( 1.147507391605587568, 1.886754179610318438, -0.3309440326291489542 ) ) ;
#101155=CARTESIAN_POINT ( 'NONE',  ( 2.066927875543830950, 1.535623996113824496, -1.388825173883188713 ) ) ;
#101157=CARTESIAN_POINT ( 'NONE',  ( 0.2859245228041712439, -0.9316758688886862538, 1.737439158343912382 ) ) ;
#101158=CARTESIAN_POINT ( 'NONE',  ( 5.918570133321236604, 1.291915522740747502, -1.429275465086258246 ) ) ;
#101159=CARTESIAN_POINT ( 'NONE',  ( 6.533804136697315634, -1.437950210024591780, -1.674183229976949905 ) ) ;
#101163=CARTESIAN_POINT ( 'NONE',  ( 4.527816470857299436, 2.001556401900002058, -0.4979991880497411372 ) ) ;
#101168=CARTESIAN_POINT ( 'NONE',  ( 5.174884205284945082, -1.981925234046210571, -0.7124256662833851061 ) ) ;
#101170=CARTESIAN_POINT ( 'NONE',  ( 0.5378411956755309031, 2.025704276806821191, -0.7818309977141599809 ) ) ;
#101172=CARTESIAN_POINT ( 'NONE',  ( 4.921240491056324551, -0.1114908479964340365, 2.158860929761210912 ) ) ;
#101173=CARTESIAN_POINT ( 'NONE',  ( 5.848308768596990781, 0.9934667122631580805, -1.758341319078795761 ) ) ;
#101180=CARTESIAN_POINT ( 'NONE',  ( 3.221888912838869690, 0.9023448338944944913, -1.803416113280359445 ) ) ;
#101184=CARTESIAN_POINT ( 'NONE',  ( 5.278265135069068137, -1.204163492603943064, 1.795060720813673738 ) ) ;
#101189=CARTESIAN_POINT ( 'NONE',  ( 5.817982510940042040, 0.9913841921252890543, -1.755779027446252138 ) ) ;
#101191=CARTESIAN_POINT ( 'NONE',  ( 0.8380132626705768528, 1.698558605200460869, 0.2991625477344951323 ) ) ;
#101197=CARTESIAN_POINT ( 'NONE',  ( 5.307814152003552444, -1.861618091082300808, 0.1822119596564600597 ) ) ;
#101198=CARTESIAN_POINT ( 'NONE',  ( -0.05795285570054254515, -1.240470478354677164, -1.586248892985191006 ) ) ;
#101204=CARTESIAN_POINT ( 'NONE',  ( 2.139458383197485603, 0.002846582261652879763, 2.120667954922689002 ) ) ;
#101205=CARTESIAN_POINT ( 'NONE',  ( 0.8961114988408731552, -0.9091644883451601711, -1.799914091915676639 ) ) ;
#101208=CARTESIAN_POINT ( 'NONE',  ( 6.280167721515548251, -1.160692707240444710, 1.823489969145650313 ) ) ;
#101212=CARTESIAN_POINT ( 'NONE',  ( 0.5498253489954890716, 0.9468162992772524156, 1.665335589065963129 ) ) ;
#101221=CARTESIAN_POINT ( 'NONE',  ( 4.012696165952275962, 1.530467462299599735, -1.526897427004340280 ) ) ;
#101225=CARTESIAN_POINT ( 'NONE',  ( 1.459403507577087700, -1.788631592985808538, 1.138920039206146928 ) ) ;
#101228=CARTESIAN_POINT ( 'NONE',  ( 2.723849342626927239, -1.131982996307562273, -1.613792087129195085 ) ) ;
#101229=CARTESIAN_POINT ( 'NONE',  ( 4.640819915729988310, 1.831716588661407963, 0.5496940206762624959 ) ) ;
#101232=CARTESIAN_POINT ( 'NONE',  ( 6.355907380368630122, -0.6650989860433678125, 1.853973344504164622 ) ) ;
#101233=CARTESIAN_POINT ( 'NONE',  ( 0.9900592867461569524, -0.4711592545371501295, -1.883805795384153381 ) ) ;
#101240=CARTESIAN_POINT ( 'NONE',  ( 6.322915745023367506, 1.413667134151237459, -1.287952294376143447 ) ) ;
#101242=CARTESIAN_POINT ( 'NONE',  ( 3.405080638938757343, 1.739790774466195789, -1.357627211771177178 ) ) ;
#101244=CARTESIAN_POINT ( 'NONE',  ( 2.468050989216635127, 2.164326253657654853, -0.4298898877757306725 ) ) ;
#101246=CARTESIAN_POINT ( 'NONE',  ( 0.2231138172586397683, 1.663799575440491285, 0.9424754157791456199 ) ) ;
#101249=CARTESIAN_POINT ( 'NONE',  ( 3.086448098943677998, 1.152334561581969785, -1.719836228861029603 ) ) ;
#101253=CARTESIAN_POINT ( 'NONE',  ( 1.376082401959723089, 1.288024388040419632, 1.735935173841046675 ) ) ;
#101254=CARTESIAN_POINT ( 'NONE',  ( 3.579775959861815515, -1.078688530630707243, 1.907616655872627964 ) ) ;
#101260=CARTESIAN_POINT ( 'NONE',  ( 6.469374514269041754, -1.702674068921444572, -0.3278888851577909658 ) ) ;
#101262=CARTESIAN_POINT ( 'NONE',  ( 4.118080132427735407, 2.055207691244304691, -0.2483996215696740451 ) ) ;
#101263=CARTESIAN_POINT ( 'NONE',  ( 5.044581972647897317, -1.532752649812264778, 1.460808053437604226 ) ) ;
#101266=CARTESIAN_POINT ( 'NONE',  ( 2.571101405699018017, 1.757081157110135017, 0.8898057773328130748 ) ) ;
#101267=CARTESIAN_POINT ( 'NONE',  ( 0.3516297456669579269, -1.353986107606550471, -1.350798769753497552 ) ) ;
#101268=CARTESIAN_POINT ( 'NONE',  ( 5.367208288505312730, 2.210367218987763671, -0.6069939957479841830 ) ) ;
#101269=CARTESIAN_POINT ( 'NONE',  ( 2.683998146737070378, -0.9385614705539682134, 1.565816405032012470 ) ) ;
#101275=CARTESIAN_POINT ( 'NONE',  ( 3.463142787923169763, -1.643428793820296718, 1.162544664348450496 ) ) ;
#101276=CARTESIAN_POINT ( 'NONE',  ( 3.994932754639446859, 0.2835094185691371393, 1.941019531709553103 ) ) ;
#101281=CARTESIAN_POINT ( 'NONE',  ( 0.3454080995960371325, 0.6521308015206389586, -1.986527616087286452 ) ) ;
#101282=CARTESIAN_POINT ( 'NONE',  ( 5.787929806067755756, -0.7924508370336593721, 1.582612139130882278 ) ) ;
#101285=CARTESIAN_POINT ( 'NONE',  ( 1.675987266036529366, -1.170314894790158933, 1.852603040092117848 ) ) ;
#101286=CARTESIAN_POINT ( 'NONE',  ( 6.632745071352946553, -1.550850273991890127, 0.7898216520882040959 ) ) ;
#101288=CARTESIAN_POINT ( 'NONE',  ( 0.1333692844072801587, 4.087911462428309051, -2.608372271572469092 ) ) ;
#101289=CARTESIAN_POINT ( 'NONE',  ( 1.031410063161166013, -1.091267733730487466, -1.335775140220570201 ) ) ;
#101290=CARTESIAN_POINT ( 'NONE',  ( 0.7382080005397623212, -2.165046367600947708, -0.7717227881791683952 ) ) ;
#101291=CARTESIAN_POINT ( 'NONE',  ( 0.3631484714031462668, 0.2087870660046411420, -2.181583536649676525 ) ) ;
#101292=CARTESIAN_POINT ( 'NONE',  ( 6.362590153729421161, -0.5805357501837383749, 1.633877867761362124 ) ) ;
#101293=CARTESIAN_POINT ( 'NONE',  ( 2.526237079854487089, -1.271617311931704686, -1.803507373242494438 ) ) ;
#101295=CARTESIAN_POINT ( 'NONE',  ( 6.602019255160630706, 0.8372048429528687885, -2.003470777635954381 ) ) ;
#101297=CARTESIAN_POINT ( 'NONE',  ( 2.202504513770195516, 1.378945901905674232, -1.606877091071600816 ) ) ;
#101298=CARTESIAN_POINT ( 'NONE',  ( 6.727182134110168299, 1.217656702865956397, 2.400974650093392171 ) ) ;
#101299=CARTESIAN_POINT ( 'NONE',  ( 5.069325366411169931, 0.1891801624123757852, -1.917091172425288370 ) ) ;
#101301=CARTESIAN_POINT ( 'NONE',  ( 2.050677904428706455, -1.769283327057631805, 1.457584778241685974 ) ) ;
#101305=CARTESIAN_POINT ( 'NONE',  ( 4.530067796519579026, -2.178530490643998174, 0.4330045798939685109 ) ) ;
#101312=CARTESIAN_POINT ( 'NONE',  ( 3.393204081532863459, -0.8197727808607684352, -1.842447475547980495 ) ) ;
#101314=CARTESIAN_POINT ( 'NONE',  ( 0.8310137546357538874, -1.940837517380919808, -0.6983779148895614686 ) ) ;
#101319=CARTESIAN_POINT ( 'NONE',  ( 4.453197812796324762, 0.4814713343750369190, -2.137748681182354726 ) ) ;
#101320=CARTESIAN_POINT ( 'NONE',  ( 0.8267963299631932994, 0.8146243292815741333, -1.844710905833810255 ) ) ;
#101321=CARTESIAN_POINT ( 'NONE',  ( 1.540310226958538475, -1.555040833713853710, 0.9856339240054690087 ) ) ;
#101322=CARTESIAN_POINT ( 'NONE',  ( 4.722401423535961484, 2.193339426362813871, 0.6665824366990577010 ) ) ;
#101323=CARTESIAN_POINT ( 'NONE',  ( 3.855264089065893351, 1.827008581971893530, -0.2271198879545410221 ) ) ;
#101326=CARTESIAN_POINT ( 'NONE',  ( 4.489149150750438189, 1.630474666268775685, -0.8212668906743822994 ) ) ;
#101327=CARTESIAN_POINT ( 'NONE',  ( 5.010388774477189777, -1.913804350592800629, 0.6351971752796632398 ) ) ;
#101329=CARTESIAN_POINT ( 'NONE',  ( 4.979486748501788185, 2.112903116282875082, -0.8095491994110515233 ) ) ;
#101331=CARTESIAN_POINT ( 'NONE',  ( 0.1355649208573142805, -1.924581242375450030, 0.8557158107796616342 ) ) ;
#101333=CARTESIAN_POINT ( 'NONE',  ( 3.367693471486675083, -0.4065805204805824635, 2.029877954327436118 ) ) ;
#101338=CARTESIAN_POINT ( 'NONE',  ( 1.787598692544673851, 1.328180555690385845, 1.395690353023341101 ) ) ;
#101341=CARTESIAN_POINT ( 'NONE',  ( 6.977413706903823787, -0.1529601955215283693, 1.936277946061695898 ) ) ;
#101345=CARTESIAN_POINT ( 'NONE',  ( 0.5277791401020451856, -0.3051165123582540994, 2.098401203810342786 ) ) ;
#101346=CARTESIAN_POINT ( 'NONE',  ( 1.512303732575480675, -0.7424040314494853021, 2.093836701676012879 ) ) ;
#101348=CARTESIAN_POINT ( 'NONE',  ( 2.837057662192625340, 0.2562861413469962879, 2.090225181913709207 ) ) ;
#101351=CARTESIAN_POINT ( 'NONE',  ( 0.3087543870234563115, -1.498283157731963966, 1.103738804280843366 ) ) ;
#101357=CARTESIAN_POINT ( 'NONE',  ( 1.318772358905948794, -0.7683209907942339933, -1.976687055281033611 ) ) ;
#101360=CARTESIAN_POINT ( 'NONE',  ( 4.562918044398325712, 1.517878595006398212, -1.242988302126393441 ) ) ;
#101361=CARTESIAN_POINT ( 'NONE',  ( 2.958072429731006370, 2.151414462573512765, -0.2105227563667099733 ) ) ;
#101362=CARTESIAN_POINT ( 'NONE',  ( 1.241482983173985533, 1.839155304979672501, 0.08999620058360720265 ) ) ;
#101365=CARTESIAN_POINT ( 'NONE',  ( 4.839680888265717407, 1.736017449284636527, 0.1234091131117609486 ) ) ;
#101369=CARTESIAN_POINT ( 'NONE',  ( 1.639762333045853726, -1.565812861550972324, -1.490595759849028035 ) ) ;
#101372=CARTESIAN_POINT ( 'NONE',  ( 3.339220083777879378, -1.203169880011810022, 1.617570133648409847 ) ) ;
#101374=CARTESIAN_POINT ( 'NONE',  ( 0.9894095316701527754, 1.906041449620498929, -1.019753361306941386 ) ) ;
#101376=CARTESIAN_POINT ( 'NONE',  ( 3.203940287746226634, -1.969268756981055635, 0.09538867180547243307 ) ) ;
#101377=CARTESIAN_POINT ( 'NONE',  ( 6.609000000000047059, 2.429201845222619394, 2.481963755843877628 ) ) ;
#101378=CARTESIAN_POINT ( 'NONE',  ( 3.614730616327064716, -0.1400294986239834782, 1.937054734790619293 ) ) ;
#101383=CARTESIAN_POINT ( 'NONE',  ( -0.2106854629475062024, 1.349218558350977260, -2.248994321313985800 ) ) ;
#101388=CARTESIAN_POINT ( 'NONE',  ( 0.09513611692719620150, -0.4880922032983874281, -2.160105283315365998 ) ) ;
#101391=CARTESIAN_POINT ( 'NONE',  ( 4.592600981049492326, 1.923087700504518605, 0.3867253955378775476 ) ) ;
#101392=CARTESIAN_POINT ( 'NONE',  ( 1.969375177810539945, -1.978050944945686673, -0.3905967402937361443 ) ) ;
#101394=CARTESIAN_POINT ( 'NONE',  ( 3.555961197718297218, 1.179765190368966321, 1.758020836099948747 ) ) ;
#101396=CARTESIAN_POINT ( 'NONE',  ( 0.1745949693968693039, 7.629137130509094256, -2.355306170041113756 ) ) ;
#101398=CARTESIAN_POINT ( 'NONE',  ( 2.818100271072515817, 1.733748696238574416, 0.6199764264002775027 ) ) ;
#101402=CARTESIAN_POINT ( 'NONE',  ( 5.115537534566190203, 1.735013203181461350, 1.219038288318145646 ) ) ;
#101407=CARTESIAN_POINT ( 'NONE',  ( 4.921196286130338216, -0.1051130969715245306, 2.058245376175421804 ) ) ;
#101409=CARTESIAN_POINT ( 'NONE',  ( 0.4493573998385214652, 1.374985906440568506, 1.254353302672887693 ) ) ;
#101410=CARTESIAN_POINT ( 'NONE',  ( 2.507154105146496725, -1.820902139252629448, 0.2722148935128121394 ) ) ;
#101415=CARTESIAN_POINT ( 'NONE',  ( 2.016531038934398445, -1.041976349804032420, -1.945408382319254503 ) ) ;
#101416=CARTESIAN_POINT ( 'NONE',  ( 5.290393965937395748, -2.244422280358076005, -0.2844362755431028567 ) ) ;
#101417=CARTESIAN_POINT ( 'NONE',  ( 3.538296236868877731, 0.7303062672313584969, 1.879804216660937666 ) ) ;
#101419=CARTESIAN_POINT ( 'NONE',  ( 5.045072953846708508, 0.1408599011454790551, 1.806194821104394777 ) ) ;
#101420=CARTESIAN_POINT ( 'NONE',  ( 4.399565145148922163, -1.877536364458038065, 0.3796658851462595408 ) ) ;
#101422=CARTESIAN_POINT ( 'NONE',  ( 3.485194120740982449, 1.782821823783652837, -0.8418218905394663221 ) ) ;
#101423=CARTESIAN_POINT ( 'NONE',  ( 4.715616592392388284, -1.834479983729628616, 0.3652084810651031743 ) ) ;
#101424=CARTESIAN_POINT ( 'NONE',  ( 5.230833165924736683, -1.752262279689630553, -0.6273003976000991466 ) ) ;
#101426=CARTESIAN_POINT ( 'NONE',  ( 0.1105650446291406575, 1.931126588553159884, 0.5807481968119408977 ) ) ;
#101428=CARTESIAN_POINT ( 'NONE',  ( 2.192140752285096639, -0.8994906754480420652, 1.904460908831892008 ) ) ;
#101433=CARTESIAN_POINT ( 'NONE',  ( 1.969016121511291795, -1.558499072447929956, 1.284715733913702085 ) ) ;
#101438=CARTESIAN_POINT ( 'NONE',  ( 2.425270691926324051, -0.002641788883844811090, 2.161773191836775521 ) ) ;
#101439=CARTESIAN_POINT ( 'NONE',  ( 6.889999999999997016, 3.693514451062899884, 2.514185260296258217 ) ) ;
#101444=CARTESIAN_POINT ( 'NONE',  ( 6.438686429976131720, -1.555646628146038157, 1.282773817382940384 ) ) ;
#101446=CARTESIAN_POINT ( 'NONE',  ( 1.031118135130421498, -1.979082047791239418, 0.9416876394413642437 ) ) ;
#101448=CARTESIAN_POINT ( 'NONE',  ( 1.481717434351536244, 2.089849803356018221, -0.8673477522002839279 ) ) ;
#101451=CARTESIAN_POINT ( 'NONE',  ( 4.276577519141481432, -0.4465006364167342645, -1.966305148836451577 ) ) ;
#101456=CARTESIAN_POINT ( 'NONE',  ( 4.178129962880992920, -0.9906059873891288614, 1.411843326160647782 ) ) ;
#101459=CARTESIAN_POINT ( 'NONE',  ( 1.633702333402654361, 0.8778187100713531477, -1.536624053347920071 ) ) ;
#101461=CARTESIAN_POINT ( 'NONE',  ( 5.227635310461984375, -2.096914331502324647, 0.6878394029543041244 ) ) ;
#101465=CARTESIAN_POINT ( 'NONE',  ( 4.745720352911135365, 1.994069623535676961, -0.2986464557954356946 ) ) ;
#101466=CARTESIAN_POINT ( 'NONE',  ( 4.728658910183288988, 1.244086218232887120, -1.317109676944823393 ) ) ;
#101468=CARTESIAN_POINT ( 'NONE',  ( 3.028041890241763401, 1.040506211802554981, -1.554362669439563360 ) ) ;
#101469=CARTESIAN_POINT ( 'NONE',  ( 6.639283661800273961, -1.628176093627232479, 0.8261057939347238310 ) ) ;
#101470=CARTESIAN_POINT ( 'NONE',  ( 1.652457426684301955, 1.892030339952909035, 0.2773405859870237133 ) ) ;
#101476=CARTESIAN_POINT ( 'NONE',  ( 0.5098338327763075606, -0.6861045072398126443, 1.785269576063217345 ) ) ;
#101478=CARTESIAN_POINT ( 'NONE',  ( 1.346068015636435522, -0.8851805579040676886, 1.750911360861057142 ) ) ;
#101479=ADVANCED_FACE ( 'NONE', ( #159492 ), #152560, .T. ) ;
#101482=CARTESIAN_POINT ( 'NONE',  ( 4.887034483293543730, -1.997634423138573867, -0.7120497732875651353 ) ) ;
#101485=CARTESIAN_POINT ( 'NONE',  ( 6.678986255646885972, -0.09454399199107686724, -1.969188304806670287 ) ) ;
#101487=CARTESIAN_POINT ( 'NONE',  ( 1.371341259694250247, -1.728764894987804057, -1.031425992479652720 ) ) ;
#101490=CARTESIAN_POINT ( 'NONE',  ( 0.6853559850922884555, 1.733544695350475395, 1.215283626663875793 ) ) ;
#101492=CARTESIAN_POINT ( 'NONE',  ( 2.893098739488662030, 0.2508700648995808025, 2.055025655848155886 ) ) ;
#101496=CARTESIAN_POINT ( 'NONE',  ( 4.664062431145298504, -1.365975323770602268, 1.582769587995744853 ) ) ;
#101498=CARTESIAN_POINT ( 'NONE',  ( 3.153144192703428939, -1.491587519860730238, -1.052284964708279258 ) ) ;
#101499=CARTESIAN_POINT ( 'NONE',  ( 2.912559398657811549, -0.5280806737378342941, -1.732764662445994919 ) ) ;
#101504=CARTESIAN_POINT ( 'NONE',  ( 5.087059579022827904, -0.2656672225294122169, -2.190654145894948890 ) ) ;
#101507=CARTESIAN_POINT ( 'NONE',  ( 3.773993364719562926, 1.897484654492180400, -0.2369724479281897500 ) ) ;
#101516=CARTESIAN_POINT ( 'NONE',  ( 3.532352470753961082, 1.824241569866682289, 0.4128566369710484629 ) ) ;
#101518=CARTESIAN_POINT ( 'NONE',  ( -0.2409995289980038091, 6.947781193150415646, -2.595509233728268583 ) ) ;
#101522=CARTESIAN_POINT ( 'NONE',  ( 6.411931881972196610E-05, -0.8997486769052507327, 1.687471195204979457 ) ) ;
#101524=CARTESIAN_POINT ( 'NONE',  ( 0.3034763168169403169, -1.518637222489120919, -1.253724199518479354 ) ) ;
#101525=CARTESIAN_POINT ( 'NONE',  ( 1.001577623981730891, -1.966640429010723112, 0.4445266750975271353 ) ) ;
#101530=CARTESIAN_POINT ( 'NONE',  ( 1.500213180713722450, -0.7911926984936793472, -2.043816727864488314 ) ) ;
#101538=ORIENTED_EDGE ( 'NONE', *, *, #42750, .F. ) ;
#101539=CARTESIAN_POINT ( 'NONE',  ( 3.667381569930192597, 1.025862638139760419, 1.528780434079744843 ) ) ;
#101540=CARTESIAN_POINT ( 'NONE',  ( 0.5572895418005788803, -1.725428541193659182, 1.036833936551822655 ) ) ;
#101541=CARTESIAN_POINT ( 'NONE',  ( 3.111036021816812713, 0.8295677418227834776, -2.143598788741421401 ) ) ;
#101543=CARTESIAN_POINT ( 'NONE',  ( 0.7954780101973528694, -1.310620071111982421, -1.321417528198569613 ) ) ;
#101546=CARTESIAN_POINT ( 'NONE',  ( 4.394721148579957770, -1.856311205515799312, -0.4593126252911489127 ) ) ;
#101551=CARTESIAN_POINT ( 'NONE',  ( 3.755486520148888729, 2.074727465276064997, -0.2578676962887976321 ) ) ;
#101552=CARTESIAN_POINT ( 'NONE',  ( 1.938157646728836614, 1.849873822469105145, 0.2772664081076986475 ) ) ;
#101555=CARTESIAN_POINT ( 'NONE',  ( 2.770765728838171960, 1.651868531079144553, -0.5482889651245922424 ) ) ;
#101559=CARTESIAN_POINT ( 'NONE',  ( 4.125434265850294047, -1.649698657028845883, 0.5036723037128154612 ) ) ;
#101561=CARTESIAN_POINT ( 'NONE',  ( 6.129534211984397629, -2.079372889712034489, 0.7396383780838566846 ) ) ;
#101564=CARTESIAN_POINT ( 'NONE',  ( 3.801787986034934619, -1.640574847700679628, -1.422045332411596474 ) ) ;
#101565=CARTESIAN_POINT ( 'NONE',  ( 2.121465551170404140, -1.771062468586531047, 0.4427346646293239818 ) ) ;
#101566=CARTESIAN_POINT ( 'NONE',  ( 0.4440980561614648603, -0.9299495107331550159, 1.727370323332158897 ) ) ;
#101567=CARTESIAN_POINT ( 'NONE',  ( 5.682842148387160286, 1.729519065878544426, -1.221158300678204300 ) ) ;
#101569=CARTESIAN_POINT ( 'NONE',  ( 6.128533286225700039, 0.2205342988230532264, 2.281768524910554596 ) ) ;
#101572=CARTESIAN_POINT ( 'NONE',  ( 1.735180256192244919, 1.979698633766859395, 0.7602586827493148514 ) ) ;
#101576=CARTESIAN_POINT ( 'NONE',  ( 6.883263157960367806, 6.035304072343574688, 2.648703854151325032 ) ) ;
#101578=CARTESIAN_POINT ( 'NONE',  ( 1.225557454335997054, 1.961257301181002388, 1.042886780478131215 ) ) ;
#101580=CARTESIAN_POINT ( 'NONE',  ( 6.117814597332064785, 0.2004318333163370436, 2.006446488866588496 ) ) ;
#101582=CARTESIAN_POINT ( 'NONE',  ( 3.924720150778399752, -1.388762634255924500, 1.525101558930273660 ) ) ;
#101588=CARTESIAN_POINT ( 'NONE',  ( 0.8321122680391360715, 2.060015930055682620, 0.3555243805062404117 ) ) ;
#101589=CARTESIAN_POINT ( 'NONE',  ( 4.746720300533005421, 1.994071680685698400, -0.2986252114312442640 ) ) ;
#101590=CARTESIAN_POINT ( 'NONE',  ( 4.774869596704574448, 1.716175909155163382, -0.6674964387535023969 ) ) ;
#101592=CARTESIAN_POINT ( 'NONE',  ( 0.5512174377280190107, 0.5480947683692177774, -1.635447244754190788 ) ) ;
#101593=CARTESIAN_POINT ( 'NONE',  ( 0.2687680251878405424, -0.2516378192510167477, -2.000730910237565663 ) ) ;
#101594=CARTESIAN_POINT ( 'NONE',  ( 1.301886090224623205, 1.538925899722990431, -1.707713671238730635 ) ) ;
#101596=CARTESIAN_POINT ( 'NONE',  ( 1.441102657128832121, 0.4411821743415585417, 2.218815533503415871 ) ) ;
#101597=CARTESIAN_POINT ( 'NONE',  ( 2.877667905955140437, 1.999614821268459020, -0.6613089454029356107 ) ) ;
#101601=CARTESIAN_POINT ( 'NONE',  ( 5.812500000000003553, 1.451031289061346818, 1.451031289060879637 ) ) ;
#101607=CARTESIAN_POINT ( 'NONE',  ( 5.326523995474015116, -0.9991460305027520805, -1.984133879135864920 ) ) ;
#101608=CARTESIAN_POINT ( 'NONE',  ( 3.943468035136340255, 0.7389761752502190806, -2.063229655756371628 ) ) ;
#101611=CARTESIAN_POINT ( 'NONE',  ( 4.932062528313536198, 1.127988425013145779, 1.604980062286972542 ) ) ;
#101612=CIRCLE ( 'NONE', #73948, 0.04999999999999883010 ) ;
#101614=CARTESIAN_POINT ( 'NONE',  ( 6.890000000000005898, 7.052460701731090076, 2.598152593539102551 ) ) ;
#101616=CARTESIAN_POINT ( 'NONE',  ( 4.781546299372162245, 0.2051969522943071500, -2.110614603223801122 ) ) ;
#101620=CARTESIAN_POINT ( 'NONE',  ( 6.174726448494309849, -2.051094451480539149, -0.6828207641706719455 ) ) ;
#101623=CARTESIAN_POINT ( 'NONE',  ( 5.337399561049260832, 0.7408347518493042516, -1.685818907712175019 ) ) ;
#101625=CARTESIAN_POINT ( 'NONE',  ( 1.276469996339978819, 1.608456030955440541, -0.6653204537699786147 ) ) ;
#101630=CARTESIAN_POINT ( 'NONE',  ( 5.541917325712655717, 0.8799508658935292216, -1.974686638939105343 ) ) ;
#101634=CARTESIAN_POINT ( 'NONE',  ( 5.032170685167933755, 1.114402916724830161, -1.852182961850391774 ) ) ;
#101636=CARTESIAN_POINT ( 'NONE',  ( 4.833256578820930294, -1.803536663746601709, 0.7962986557112069486 ) ) ;
#101637=CARTESIAN_POINT ( 'NONE',  ( 4.305767739847966347, -1.508829150093475180, 0.8539562774845139703 ) ) ;
#101639=CARTESIAN_POINT ( 'NONE',  ( 1.382659466718983543, -0.3261178763579902218, -2.167053615394160637 ) ) ;
#101640=CARTESIAN_POINT ( 'NONE',  ( 2.679136956247138546, -2.208066087050132520, -0.6703273527271095267 ) ) ;
#101641=CARTESIAN_POINT ( 'NONE',  ( 4.762995170230669650, -1.839058295199582638, -0.9300793793675359300 ) ) ;
#101642=CARTESIAN_POINT ( 'NONE',  ( 0.1814471035007196309, -0.9164790359779145801, 1.712077929913154328 ) ) ;
#101647=CARTESIAN_POINT ( 'NONE',  ( 1.442029965644067158, -1.730867108953790590, -1.034163949609874233 ) ) ;
#101649=CARTESIAN_POINT ( 'NONE',  ( 3.592985822966657583, -0.4282699184722462693, -2.164648485658649868 ) ) ;
#101651=CARTESIAN_POINT ( 'NONE',  ( 1.322862136463611504, -1.679459703857703268, -0.8019484745323454122 ) ) ;
#101652=CARTESIAN_POINT ( 'NONE',  ( -0.02880301295722555166, 0.6711181056864559125, -2.353869138803561079 ) ) ;
#101656=CARTESIAN_POINT ( 'NONE',  ( 6.925078400183566352, 7.051505795288234957, 2.842497989238515821 ) ) ;
#101657=CARTESIAN_POINT ( 'NONE',  ( 6.105383947169263692, -1.826632712061267094, 0.2301338403083788009 ) ) ;
#101659=CARTESIAN_POINT ( 'NONE',  ( 3.028252848896676674, 1.146099369071330143, -1.712595011064410366 ) ) ;
#101662=CARTESIAN_POINT ( 'NONE',  ( 1.805337931753002501, 1.756199045189226204, -0.9973023101699033388 ) ) ;
#101665=CARTESIAN_POINT ( 'NONE',  ( 2.061468863205512925, 0.3533766173234990093, -2.030202010101101795 ) ) ;
#101669=CARTESIAN_POINT ( 'NONE',  ( -0.1411974294641968053, 0.7397609206469482057, -1.984549174418163808 ) ) ;
#101670=CARTESIAN_POINT ( 'NONE',  ( 5.795608111622330583, 1.668732747960173235, 1.444295198399044855 ) ) ;
#101672=CARTESIAN_POINT ( 'NONE',  ( 1.089409339093825979, 1.906878951332368954, -1.017924135055588541 ) ) ;
#101674=CARTESIAN_POINT ( 'NONE',  ( 1.516814941429758701, 0.2024661778830244008, 2.006371303556075958 ) ) ;
#101679=CARTESIAN_POINT ( 'NONE',  ( 2.236979667955760309, -1.672073921526989748, 0.8388852543278202401 ) ) ;
#101680=CARTESIAN_POINT ( 'NONE',  ( 3.204314817619222211, 1.275555974797081049, -1.561881975048397209 ) ) ;
#101684=CARTESIAN_POINT ( 'NONE',  ( 5.479168138989118475, -0.05037515785718051087, -2.105640702651077945 ) ) ;
#101688=CARTESIAN_POINT ( 'NONE',  ( 6.539320575229276677, 6.035451701470580410, 2.698157228745074576 ) ) ;
#101689=CARTESIAN_POINT ( 'NONE',  ( 5.449475261934634496, -1.824267568868439771, 0.8672911397697125047 ) ) ;
#101691=CARTESIAN_POINT ( 'NONE',  ( 0.5849265108320426121, 1.972682758258193392, 0.6021488627185996867 ) ) ;
#101700=CARTESIAN_POINT ( 'NONE',  ( 3.649033395009869452, -0.4203537998966280220, -2.129940419224036763 ) ) ;
#101702=CARTESIAN_POINT ( 'NONE',  ( 1.944624168438695566, -1.479605912621816621, -1.095697124569312564 ) ) ;
#101704=CARTESIAN_POINT ( 'NONE',  ( 3.913774547416096095, -1.127657808996849198, -1.879056921112078893 ) ) ;
#101705=CARTESIAN_POINT ( 'NONE',  ( 6.983263157960330147, 7.051826758666251749, 2.751962080009969114 ) ) ;
#101706=CARTESIAN_POINT ( 'NONE',  ( 5.331070463540595661, 0.1608317336210095816, 2.256856606938316023 ) ) ;
#101714=CARTESIAN_POINT ( 'NONE',  ( 6.643818817254954823, 0.6745290893846628277, -1.636350436104140327 ) ) ;
#101715=CARTESIAN_POINT ( 'NONE',  ( 3.299479658734363330, 1.818928663852859451, -0.8628815382619985375 ) ) ;
#101717=CARTESIAN_POINT ( 'NONE',  ( 1.782391780347460486, -1.127077160282144552, 1.778786634185139270 ) ) ;
#101718=CARTESIAN_POINT ( 'NONE',  ( 1.370553398973891390, -0.2825970708170088552, -1.894525755544463008 ) ) ;
#101721=CARTESIAN_POINT ( 'NONE',  ( 1.785543415971390102, -1.855581397249297382, 0.6606886831301524987 ) ) ;
#101722=CARTESIAN_POINT ( 'NONE',  ( 0.5845639792326964290, -0.2246964894469481722, -1.857040431621145959 ) ) ;
#101723=CARTESIAN_POINT ( 'NONE',  ( 1.539427311113782837, 1.813978416018032558, -0.7477436361984082236 ) ) ;
#101724=CARTESIAN_POINT ( 'NONE',  ( 0.4570967503451648373, -1.639016809899789040, 0.9851245988263114262 ) ) ;
#101728=CARTESIAN_POINT ( 'NONE',  ( 6.051601594667257444, 0.5412791183288803154, -1.790613848972313349 ) ) ;
#101730=CARTESIAN_POINT ( 'NONE',  ( 6.983263157960403866, -0.005959781318053494932, 2.045923054782183392 ) ) ;
#101731=CARTESIAN_POINT ( 'NONE',  ( 6.086797785588474063, 1.993605056338519699, 0.5577928598018768724 ) ) ;
#101743=CARTESIAN_POINT ( 'NONE',  ( 5.002378505967388200, 1.956489882415031190, 0.1462272935644214900 ) ) ;
#101746=CARTESIAN_POINT ( 'NONE',  ( 3.620470095612156047, 0.4925664443866035191, -1.954873191151076162 ) ) ;
#101747=CARTESIAN_POINT ( 'NONE',  ( 2.975699994382564828, -0.7717752754876210375, 1.753554302899827277 ) ) ;
#101749=CARTESIAN_POINT ( 'NONE',  ( 0.3807642395799658575, -0.2741851280289032688, -2.174293136291181483 ) ) ;
#101750=CARTESIAN_POINT ( 'NONE',  ( 0.1333692844072559280, 0.001398348041498076455, -2.053671342968105051 ) ) ;
#101751=CARTESIAN_POINT ( 'NONE',  ( 3.374138713240721454, -1.116850685118627728, 1.500355210514233262 ) ) ;
#101755=CARTESIAN_POINT ( 'NONE',  ( 4.851218673320928154, 0.2063579389092398131, -2.107127644889031703 ) ) ;
#101757=CARTESIAN_POINT ( 'NONE',  ( 5.494608840674215955, 2.039112051642687717, 0.3575134270455831986 ) ) ;
#101758=CARTESIAN_POINT ( 'NONE',  ( 0.8200051061889235271, 1.242435332701301132, -1.681397122352365603 ) ) ;
#101759=CARTESIAN_POINT ( 'NONE',  ( 5.983392046985362533, 1.685759371660649375, -0.7011634845648377912 ) ) ;
#101768=CARTESIAN_POINT ( 'NONE',  ( 0.1701768659465550948, 0.6913354060617262764, 1.674562877054022625 ) ) ;
#101777=CARTESIAN_POINT ( 'NONE',  ( 5.800407700000974387, 1.352143934286989868, -1.496062775417882129 ) ) ;
#101778=CARTESIAN_POINT ( 'NONE',  ( 0.1004478525090373164, -0.9956121213324088393, 1.872212410442177566 ) ) ;
#101782=CARTESIAN_POINT ( 'NONE',  ( -0.1399997263889820043, 5.722209607272843002, -2.594334538518060729 ) ) ;
#101786=CARTESIAN_POINT ( 'NONE',  ( 3.309381622104785148, -1.607321225346239668, -1.137771303188861660 ) ) ;
#101787=CARTESIAN_POINT ( 'NONE',  ( 1.348456458401224412, 1.042098076042829780, -1.846665823592225975 ) ) ;
#101791=CARTESIAN_POINT ( 'NONE',  ( 5.613277516225614328, -2.138688192980051639, 0.4772630486022874652 ) ) ;
#101793=CARTESIAN_POINT ( 'NONE',  ( 3.909137014540211119, 1.651653515444248876, 0.9912706138347370244 ) ) ;
#101795=CARTESIAN_POINT ( 'NONE',  ( -0.02988540731095785247, 0.7668091516429014209, -1.812018377701756888 ) ) ;
#101796=CARTESIAN_POINT ( 'NONE',  ( 0.9794701899953797142, -0.05759512415488829418, -2.206297691287119722 ) ) ;
#101800=CARTESIAN_POINT ( 'NONE',  ( 6.227403457816463650, 0.1483525144864000778, -1.963943935631215165 ) ) ;
#101801=CARTESIAN_POINT ( 'NONE',  ( 0.4505971019186795212, -1.641227270844529018, -1.037965677199135017 ) ) ;
#101802=CARTESIAN_POINT ( 'NONE',  ( 6.503268925837763170, 2.271904311083965844, 0.3474358185819835798 ) ) ;
#101804=CARTESIAN_POINT ( 'NONE',  ( 4.117883143796479573, 1.847306362133010360, -0.2240370018555241372 ) ) ;
#101809=CARTESIAN_POINT ( 'NONE',  ( 6.720655732516647163, 2.082321177337285167, 2.135279995619132620 ) ) ;
#101810=CARTESIAN_POINT ( 'NONE',  ( 0.6971427418834205136, 1.794861059153027627, 1.257291590721874686 ) ) ;
#101815=CARTESIAN_POINT ( 'NONE',  ( 0.4514209555319322331, 0.5758240286459560542, -1.732582669633643047 ) ) ;
#101817=CARTESIAN_POINT ( 'NONE',  ( 2.355775467714062543, 0.08314403793566874090, -1.732266345623443948 ) ) ;
#101822=CARTESIAN_POINT ( 'NONE',  ( 5.180226163740526246, -1.011166736308216629, 1.519887457628710248 ) ) ;
#101823=CARTESIAN_POINT ( 'NONE',  ( 3.871884822249270108, -1.933460040528666379, 0.3310023857948928838 ) ) ;
#101827=CARTESIAN_POINT ( 'NONE',  ( 4.863993733624056404, 0.6645719631460760279, -2.013739200842738608 ) ) ;
#101831=CARTESIAN_POINT ( 'NONE',  ( 3.379797469122407083, -1.996479967689598789, 0.5476083754193948883 ) ) ;
#101832=CARTESIAN_POINT ( 'NONE',  ( 6.827182134110226563, 2.468179810210658243, 2.195371296381436022 ) ) ;
#101835=CARTESIAN_POINT ( 'NONE',  ( 4.793709693897413082, 2.072883653632663137, -0.7987435787581667057 ) ) ;
#101837=CARTESIAN_POINT ( 'NONE',  ( 2.461953032136819264, -2.200924886027255667, -0.6633417334961901890 ) ) ;
#101844=CARTESIAN_POINT ( 'NONE',  ( 4.588094604188536429, 1.105678411722615051, 1.560157546714964871 ) ) ;
#101846=CARTESIAN_POINT ( 'NONE',  ( 3.698037441923990087, -1.722821800119245683, -0.08474311298608917797 ) ) ;
#101847=CARTESIAN_POINT ( 'NONE',  ( 3.626185617424377838, 2.007256095728218614, 0.1928357053486499384 ) ) ;
#101848=CARTESIAN_POINT ( 'NONE',  ( 3.657115705757322477, 1.277955821227232613, 1.910552683106376382 ) ) ;
#101851=CARTESIAN_POINT ( 'NONE',  ( 0.03028722099337673168, -1.361824662662258767, -1.737358624739212543 ) ) ;
#101854=CARTESIAN_POINT ( 'NONE',  ( 4.727684277059563733, -1.088367244632810094, -1.395429379651995649 ) ) ;
#101856=CARTESIAN_POINT ( 'NONE',  ( 0.8852319118969053102, 2.019148884293726631, -1.085135299617467020 ) ) ;
#101857=CARTESIAN_POINT ( 'NONE',  ( 0.4095771458324704573, 1.203761932438538462, -1.257115261623420022 ) ) ;
#101859=CARTESIAN_POINT ( 'NONE',  ( 6.685463922536254877, -0.9407050535897142352, 1.977304495687677521 ) ) ;
#101863=CARTESIAN_POINT ( 'NONE',  ( 0.3444781036854955847, -1.022991162849467228, 1.915094836987745630 ) ) ;
#101864=CARTESIAN_POINT ( 'NONE',  ( 1.323454262349360144, -1.463929862531298198, -1.387097294446784090 ) ) ;
#101866=CARTESIAN_POINT ( 'NONE',  ( 4.934167778409569216, 0.9889366926784399769, -1.653171546959011140 ) ) ;
#101869=CARTESIAN_POINT ( 'NONE',  ( 1.477127009259255219, -1.566406750307091533, 1.575387012651897622 ) ) ;
#101877=CARTESIAN_POINT ( 'NONE',  ( 3.772797691900576567, 1.637269354731695881, -0.5906731273508105673 ) ) ;
#101878=CARTESIAN_POINT ( 'NONE',  ( 2.840232074097197579, -1.010955899468408248, 1.681206195012739046 ) ) ;
#101884=CARTESIAN_POINT ( 'NONE',  ( 6.812952578306354035, -1.517200236233799071, 1.243500037895750143 ) ) ;
#101888=CARTESIAN_POINT ( 'NONE',  ( 1.710245752144876619, -2.245277845785878412, 0.2781651023185549021 ) ) ;
#101891=CARTESIAN_POINT ( 'NONE',  ( 2.653401028632852654, 0.5028369177751991215, -1.801603059227441239 ) ) ;
#101892=CARTESIAN_POINT ( 'NONE',  ( 0.8263334968928169877, 0.7041814825227004082, -1.584920328518927279 ) ) ;
#101893=CARTESIAN_POINT ( 'NONE',  ( 4.915667883426772633, -1.172277214026868464, -1.851500752446763709 ) ) ;
#101894=CARTESIAN_POINT ( 'NONE',  ( 5.139818204295112380, -1.627507941656263002, -1.636155730761083227 ) ) ;
#101895=CARTESIAN_POINT ( 'NONE',  ( 0.8661736431406670267, 1.015005012832224329, 1.793514120848164195 ) ) ;
#101896=CARTESIAN_POINT ( 'NONE',  ( 3.626839189636944738, -1.793926730891879151, 0.7440942006126953778 ) ) ;
#101899=CARTESIAN_POINT ( 'NONE',  ( 6.221928862670094595, -1.039020359566013907, -1.555222851818117924 ) ) ;
#101901=CARTESIAN_POINT ( 'NONE',  ( 0.1452960159114678740, -0.1365383601019970750, -1.704228001402931625 ) ) ;
#101904=CARTESIAN_POINT ( 'NONE',  ( 4.606092368833686557, -0.09613688574180989654, 2.014232646917232916 ) ) ;
#101908=CARTESIAN_POINT ( 'NONE',  ( 1.822601884235462766, 1.703052241681313861, 0.6583118566880485911 ) ) ;
#101917=CARTESIAN_POINT ( 'NONE',  ( 5.725262222419306823, 1.782257655895511661, 0.9500345275383536015 ) ) ;
#101918=CARTESIAN_POINT ( 'NONE',  ( 6.604121268705382519, -0.9518609934017449037, 2.004712419625443776 ) ) ;
#101922=CARTESIAN_POINT ( 'NONE',  ( 5.506733764336206427, 1.562011470896901288, -1.344504574768749627 ) ) ;
#101923=CARTESIAN_POINT ( 'NONE',  ( 4.904922738988922504, -1.081064280317966420, -1.701948707654332704 ) ) ;
#101931=CARTESIAN_POINT ( 'NONE',  ( 5.184922634274871989, -1.076153828860962225, -1.704676470440001701 ) ) ;
#101932=CARTESIAN_POINT ( 'NONE',  ( 3.292734131499192252, 1.452021927685825275, 1.131891246899892289 ) ) ;
#101934=CARTESIAN_POINT ( 'NONE',  ( 2.614278096488438674, -2.282406316997650286, 0.3399710349294912115 ) ) ;
#101937=CARTESIAN_POINT ( 'NONE',  ( 4.622454487542248636, 1.333869025858843704, -1.700861402727947391 ) ) ;
#101939=CARTESIAN_POINT ( 'NONE',  ( 0.3099700162084629285, 1.338387961458173070, -1.407469107711552425 ) ) ;
#101944=CARTESIAN_POINT ( 'NONE',  ( 3.186256133050053840, -1.842714570631575510, -0.3211874441736498054 ) ) ;
#101945=CARTESIAN_POINT ( 'NONE',  ( 6.315303677655929704, -0.2418685481465185916, 1.956520841371222952 ) ) ;
#101948=CARTESIAN_POINT ( 'NONE',  ( 1.998912159191484905, -0.5904864226158462737, -2.126349760018491963 ) ) ;
#101953=CARTESIAN_POINT ( 'NONE',  ( 0.5617156953909893113, 1.950523934018918659, -0.2849811346736507156 ) ) ;
#101954=CARTESIAN_POINT ( 'NONE',  ( 6.270204019816865149, 1.180490267363063062, 1.982795515311958079 ) ) ;
#101955=CARTESIAN_POINT ( 'NONE',  ( 0.9593383959572501229, 1.601786533887459507, 1.132500672181527168 ) ) ;
#101956=CARTESIAN_POINT ( 'NONE',  ( 3.995030872118944032, 0.2978362323166737213, 2.040820773513659425 ) ) ;
#101965=CARTESIAN_POINT ( 'NONE',  ( 6.109878594781020134, 0.6360665949224998394, -2.075910194261113784 ) ) ;
#101967=CARTESIAN_POINT ( 'NONE',  ( 5.987831981441136264, -1.833028718050220940, -0.1737628300680846560 ) ) ;
#101970=CARTESIAN_POINT ( 'NONE',  ( 1.792056902697708454, -1.861051795492570049, -0.1884349046137670514 ) ) ;
#101975=CARTESIAN_POINT ( 'NONE',  ( 0.5922591856823838929, -1.062013159134197693, 1.590055880637729402 ) ) ;
#101976=CARTESIAN_POINT ( 'NONE',  ( 2.693947877954734338, -1.764960265255947736, -0.1323486908471616652 ) ) ;
#101977=CARTESIAN_POINT ( 'NONE',  ( 0.9965660710522583621, -1.865815080690262917, -0.4182784585613218420 ) ) ;
#101979=CARTESIAN_POINT ( 'NONE',  ( 4.587445725801254426, -0.5070264450876013074, 1.847228357985892577 ) ) ;
#101981=CARTESIAN_POINT ( 'NONE',  ( 5.512145389550558328, 1.967385609537531277, -0.09471018678799088264 ) ) ;
#101982=CARTESIAN_POINT ( 'NONE',  ( 1.406653384705614629, -2.110883996484512970, -0.2024971186788473154 ) ) ;
#101984=CARTESIAN_POINT ( 'NONE',  ( 3.397188523315307407, 1.473948685399184333, 1.151750840393983344 ) ) ;
#101985=CARTESIAN_POINT ( 'NONE',  ( 6.445920802586958764, 0.6525945181424031016, -1.596887126696917791 ) ) ;
#101987=CARTESIAN_POINT ( 'NONE',  ( 3.018423772948013006, -1.088090592406821155, -1.919924466345590108 ) ) ;
#101990=CARTESIAN_POINT ( 'NONE',  ( 1.188016131547619647, -1.306928873568227623, -1.595823035580832272 ) ) ;
#101998=CARTESIAN_POINT ( 'NONE',  ( 3.631357695093720750, 0.05367941694835526995, -2.069842578854002468 ) ) ;
#102001=CARTESIAN_POINT ( 'NONE',  ( 1.528841242883504981, 2.082761121880230881, 0.5781018612496248155 ) ) ;
#102003=CARTESIAN_POINT ( 'NONE',  ( 1.154951149459724880, 0.3962062163746901677, 1.980246309512444070 ) ) ;
#102006=CARTESIAN_POINT ( 'NONE',  ( 0.1747926744264660381, 7.629137130509078268, -2.455305974604498953 ) ) ;
#102008=CARTESIAN_POINT ( 'NONE',  ( 6.854846703925609575, -0.8643618726141141240, 1.819651424301058418 ) ) ;
#102009=CARTESIAN_POINT ( 'NONE',  ( 6.051949806467664672, 0.9910487912591151582, 1.639330874965704732 ) ) ;
#102010=CARTESIAN_POINT ( 'NONE',  ( 6.639320575229248789, 2.413637632230402286, 2.584074196137386092 ) ) ;
#102011=CARTESIAN_POINT ( 'NONE',  ( 3.491892070630482348, -2.189115664112693871, -0.1057334378413293807 ) ) ;
#102014=CARTESIAN_POINT ( 'NONE',  ( 3.463059065379544776, -1.560675823418774533, 1.104941681961457256 ) ) ;
#102016=EDGE_CURVE ( 'NONE', #117162, #57811, #41509, .T. ) ;
#102019=CARTESIAN_POINT ( 'NONE',  ( 0.9312678054614745848, -1.591333336790928366, -1.238303555203337458 ) ) ;
#102021=CARTESIAN_POINT ( 'NONE',  ( 0.8027370721926800901, 1.731296644042874755, -1.502618532894074876 ) ) ;
#102023=CARTESIAN_POINT ( 'NONE',  ( 4.453923018928796829, 1.724380149092176850, -0.04373908735122617603 ) ) ;
#102029=CARTESIAN_POINT ( 'NONE',  ( 1.539427311113782837, 1.813978416018032558, -0.7477436361984082236 ) ) ;
#102031=CARTESIAN_POINT ( 'NONE',  ( 0.07556134207191073093, 7.629137130509040077, -2.844199257382596269 ) ) ;
#102035=CARTESIAN_POINT ( 'NONE',  ( 3.861793950654641261, 0.6069239149280086787, -1.706917045096454366 ) ) ;
#102040=CARTESIAN_POINT ( 'NONE',  ( 5.215404452620196807, 1.484227587358154077, 1.038217761341611922 ) ) ;
#102044=CARTESIAN_POINT ( 'NONE',  ( 6.092234697878679661, 0.9164522128973868753, -1.619700000576968391 ) ) ;
#102046=CARTESIAN_POINT ( 'NONE',  ( 4.253473425383147877, 1.857088099111468216, -0.4692844457289280236 ) ) ;
#102055=CARTESIAN_POINT ( 'NONE',  ( 1.305796196612363902, -0.5247483525172501606, 2.096912610238470975 ) ) ;
#102059=CARTESIAN_POINT ( 'NONE',  ( 0.7272432748211544729, -1.735090175422876246, 0.5678700757711930835 ) ) ;
#102061=CARTESIAN_POINT ( 'NONE',  ( 3.996943106591983597, 1.542326501817241180, -0.9764022233923684846 ) ) ;
#102063=CARTESIAN_POINT ( 'NONE',  ( 1.546972149855216472, 0.1906517044060058730, 1.902890584052991940 ) ) ;
#102064=CARTESIAN_POINT ( 'NONE',  ( 2.664455434096600683, -0.7511504341344789060, -1.820894044046962534 ) ) ;
#102065=CARTESIAN_POINT ( 'NONE',  ( 4.212401414637350072, 1.776917926058638963, 0.7840673734914437309 ) ) ;
#102068=CARTESIAN_POINT ( 'NONE',  ( 4.043311264919998038, 0.1072909356813686182, 2.118029240109862155 ) ) ;
#102075=CARTESIAN_POINT ( 'NONE',  ( 3.580510235063854019, -1.759844519496515325, -0.4856381957471164745 ) ) ;
#102080=CARTESIAN_POINT ( 'NONE',  ( 5.014452206985246185, 1.289541220462528504, -1.355370375751355105 ) ) ;
#102082=CARTESIAN_POINT ( 'NONE',  ( 3.193887106011963350, -0.7802878698427909709, 1.761581285093082982 ) ) ;
#102083=CARTESIAN_POINT ( 'NONE',  ( 6.930524233185828997, -1.209519613549964845, 1.545115813350018241 ) ) ;
#102089=CARTESIAN_POINT ( 'NONE',  ( 1.511481539699152776, -1.992283995360244253, 0.7168839309619617906 ) ) ;
#102092=CARTESIAN_POINT ( 'NONE',  ( 6.315297747118990834, -1.772576088781053327, -1.069364167438614732 ) ) ;
#102093=CARTESIAN_POINT ( 'NONE',  ( 0.7844012160764175512, 1.623964078452419857, -0.8677550623670119423 ) ) ;
#102095=CARTESIAN_POINT ( 'NONE',  ( 6.609999999999973674, -0.005249217919313375023, 2.280159464062641916 ) ) ;
#102098=CARTESIAN_POINT ( 'NONE',  ( 1.359778343217881602, 2.257671611795939004, -0.3959128255837316979 ) ) ;
#102099=CARTESIAN_POINT ( 'NONE',  ( 0.06470675514189982991, -1.629034059718449834, -0.8243793580787887043 ) ) ;
#102101=CARTESIAN_POINT ( 'NONE',  ( 6.052673674419667194, -1.666704710846309112, -0.9964068823852706425 ) ) ;
#102104=CARTESIAN_POINT ( 'NONE',  ( 0.3166526355253923009, -0.6820779544549429030, -1.894243553402875202 ) ) ;
#102105=CARTESIAN_POINT ( 'NONE',  ( 6.421112215724263272, -1.799107166270615732, 0.9110519380226205222 ) ) ;
#102109=CARTESIAN_POINT ( 'NONE',  ( 2.625039678221803729, -1.950394636745816701, 0.7532777691767779116 ) ) ;
#102110=CARTESIAN_POINT ( 'NONE',  ( 2.465387952175815744, 1.736178859682969700, -0.3425752158293988159 ) ) ;
#102115=CARTESIAN_POINT ( 'NONE',  ( 4.875077803184670877, 2.140050280577758812, -0.8218066810307764758 ) ) ;
#102116=CARTESIAN_POINT ( 'NONE',  ( 3.292619090915947844, 1.372597323508369715, 1.069791993016102172 ) ) ;
#102119=CARTESIAN_POINT ( 'NONE',  ( 3.708057520534962848, -1.311595775785476148, -1.134043610401070712 ) ) ;
#102120=CARTESIAN_POINT ( 'NONE',  ( 3.350208609569472529, -0.8826205156595956502, 1.983864470818137660 ) ) ;
#102122=CARTESIAN_POINT ( 'NONE',  ( 4.206267736153862735, 1.236801365491456028, -1.592660703826812352 ) ) ;
#102123=CARTESIAN_POINT ( 'NONE',  ( 1.406250000000001332, 1.895863743164055926, -0.7852924748300647018 ) ) ;
#102125=CARTESIAN_POINT ( 'NONE',  ( 1.834862671528534994, 0.1865727292883790633, 1.917327306167202261 ) ) ;
#102127=CARTESIAN_POINT ( 'NONE',  ( 5.660436988733716035, 2.218808146451553220, 0.1093606849192785280 ) ) ;
#102129=CARTESIAN_POINT ( 'NONE',  ( 6.883263157960367806, 0.5819222519044697783, 1.998722019247618276 ) ) ;
#102134=CARTESIAN_POINT ( 'NONE',  ( 0.8212868038825784645, 1.678483586613238154, -1.455034836404971665 ) ) ;
#102135=CARTESIAN_POINT ( 'NONE',  ( 5.652778587040098834, -0.4750822840141955550, -1.903360745478323901 ) ) ;
#102139=CARTESIAN_POINT ( 'NONE',  ( 6.380173838452511959, -1.218392737502610013, 1.906166127322491910 ) ) ;
#102143=CARTESIAN_POINT ( 'NONE',  ( 4.703617135414410733, -1.592502274362836978, -1.310920101374695168 ) ) ;
#102148=CARTESIAN_POINT ( 'NONE',  ( 5.782452155351484713, -1.824793809246130438, -0.4103911052399379367 ) ) ;
#102149=CARTESIAN_POINT ( 'NONE',  ( 4.254371668973718990, 1.680547194560323643, -0.4271837243535313022 ) ) ;
#102150=CARTESIAN_POINT ( 'NONE',  ( 2.911345607792231949, -0.8600081332746039031, -1.513042209403854699 ) ) ;
#102152=CARTESIAN_POINT ( 'NONE',  ( 2.068323803795060645, -1.406806521851681424, 1.809881060044524093 ) ) ;
#102154=CARTESIAN_POINT ( 'NONE',  ( 6.110894567773135222, -0.2550301881006194482, 2.075043241552937179 ) ) ;
#102155=CARTESIAN_POINT ( 'NONE',  ( 0.07576575995338691305, -1.785066692240460551, -0.4505573523648154222 ) ) ;
#102158=CARTESIAN_POINT ( 'NONE',  ( 1.547500230860882287, -1.423960469535384465, 1.427938386157491246 ) ) ;
#102163=CARTESIAN_POINT ( 'NONE',  ( 2.701940546545733568, 1.501232083741442125, 1.497845299259780827 ) ) ;
#102165=CARTESIAN_POINT ( 'NONE',  ( 5.830640656690653678, 1.760721658632548037, 0.4824517239352192344 ) ) ;
#102166=EDGE_LOOP ( 'NONE', ( #22917, #24620 ) ) ;
#102171=CARTESIAN_POINT ( 'NONE',  ( 2.531515522815621200, -0.1936091499190935594, 2.010454966646264552 ) ) ;
#102172=CARTESIAN_POINT ( 'NONE',  ( 6.264705869774118696, -1.564926740429407603, 1.556175991035801287 ) ) ;
#102174=CARTESIAN_POINT ( 'NONE',  ( 3.994834637159989654, 0.2691826048217076384, 1.841218289905453664 ) ) ;
#102184=CARTESIAN_POINT ( 'NONE',  ( 1.616079437515309136, 0.5095893236424541284, -1.657241410798731440 ) ) ;
#102185=CARTESIAN_POINT ( 'NONE',  ( 1.306181984371343585, 1.533458449073618057, 0.8229166363448844335 ) ) ;
#102186=CARTESIAN_POINT ( 'NONE',  ( 6.076872578159392191, -2.189301982996785245, -0.7299270095633101363 ) ) ;
#102189=CARTESIAN_POINT ( 'NONE',  ( 1.915377802959626230, -0.2551614870064948803, 2.044872660591416480 ) ) ;
#102191=CARTESIAN_POINT ( 'NONE',  ( 6.503268925837763170, 2.271904311083965844, 0.3474358185819835798 ) ) ;
#102194=CARTESIAN_POINT ( 'NONE',  ( 0.3210827503922530357, -0.09932373348091848297, 1.969089571372897085 ) ) ;
#102196=CARTESIAN_POINT ( 'NONE',  ( 3.181800181368432678, 1.864768544494728175, -0.4233684943922080834 ) ) ;
#102198=CARTESIAN_POINT ( 'NONE',  ( 5.830760709146560750, 2.125890151018691832, 0.5921790101122563765 ) ) ;
#102204=CARTESIAN_POINT ( 'NONE',  ( 6.516280388114966904, -2.120036885061008292, 0.05137064186952475936 ) ) ;
#102206=CARTESIAN_POINT ( 'NONE',  ( 3.241587113499379669, -2.035928198617407592, 1.086232460313860892 ) ) ;
#102207=CARTESIAN_POINT ( 'NONE',  ( 4.334394203492665909, -1.131343785558375226, 1.602600411086833931 ) ) ;
#102208=CARTESIAN_POINT ( 'NONE',  ( 0.9714493606215730548, -0.2934177832072166758, 1.939591667560663035 ) ) ;
#102212=CARTESIAN_POINT ( 'NONE',  ( 6.421112215724263272, -1.799107166270615732, 0.9110519380226205222 ) ) ;
#102215=CARTESIAN_POINT ( 'NONE',  ( 3.608415011292832819, 2.171239808225163159, 0.005094884836047069293 ) ) ;
#102217=CARTESIAN_POINT ( 'NONE',  ( 1.055114822555893728, 0.4192091730233596381, 2.078585086915801128 ) ) ;
#102222=CARTESIAN_POINT ( 'NONE',  ( 1.827488212121135769, -1.941439008138484246, 0.6915448510415463934 ) ) ;
#102228=CARTESIAN_POINT ( 'NONE',  ( 4.670513044250029999, 0.7352163052343118066, 1.765496816765201649 ) ) ;
#102229=CARTESIAN_POINT ( 'NONE',  ( 6.666858444607468570, -2.065188582200903955, -0.9245386165244884324 ) ) ;
#102231=CARTESIAN_POINT ( 'NONE',  ( 0.8963918696095014571, -1.767652434117328308, -0.3957652751337119024 ) ) ;
#102232=CARTESIAN_POINT ( 'NONE',  ( 0.7783702408986278298, -0.4687143430282306733, -1.857332652546606733 ) ) ;
#102233=CARTESIAN_POINT ( 'NONE',  ( 2.207561477879273593, -1.661462528888792090, -1.235070534849058266 ) ) ;
#102235=CARTESIAN_POINT ( 'NONE',  ( 0.7605432175010603535, -1.429589592961340028, 1.357792370201470256 ) ) ;
#102236=CARTESIAN_POINT ( 'NONE',  ( 5.443948574151852959, 0.7788650187186187956, -1.762213160536057144 ) ) ;
#102237=CARTESIAN_POINT ( 'NONE',  ( 6.709632191794143274, -0.4886956906769434061, 2.160084693451309601 ) ) ;
#102240=CARTESIAN_POINT ( 'NONE',  ( 4.352046829380719295, -0.7922827022245787498, 1.904640004429495326 ) ) ;
#102245=CARTESIAN_POINT ( 'NONE',  ( 5.737368847912779124, -1.905360455185100887, 0.8973202462331535401 ) ) ;
#102247=CARTESIAN_POINT ( 'NONE',  ( 6.812946544903684121, -1.603000239855886466, 1.309962327488790157 ) ) ;
#102249=CARTESIAN_POINT ( 'NONE',  ( 5.220075184997099882, -1.151474455836385857, -1.829185309946822713 ) ) ;
#102250=CARTESIAN_POINT ( 'NONE',  ( 4.037763967290787903, -1.932009543340426072, 0.5885129382087511685 ) ) ;
#102251=CARTESIAN_POINT ( 'NONE',  ( 6.620655732516649294, 2.950034989283246478, 2.626075342966327497 ) ) ;
#102256=CARTESIAN_POINT ( 'NONE',  ( 2.553923023464285347, 1.082840749376843270, 1.700961377887353798 ) ) ;
#102263=CARTESIAN_POINT ( 'NONE',  ( 4.816029892389546596, 1.034148959857810190, -1.730877356967218894 ) ) ;
#102265=CARTESIAN_POINT ( 'NONE',  ( 1.171983892495536805, -1.097183398155553435, 1.330944738974817243 ) ) ;
#102270=CARTESIAN_POINT ( 'NONE',  ( 5.923093557443566581, -0.04637014295935313474, 1.870147476527424635 ) ) ;
#102271=CARTESIAN_POINT ( 'NONE',  ( 6.328391183068679204, -0.9529656412403487709, -1.773404795463069838 ) ) ;
#102275=CARTESIAN_POINT ( 'NONE',  ( 0.9488424731869498086, -1.824129051820524205, -0.8596123018156722750 ) ) ;
#102276=CARTESIAN_POINT ( 'NONE',  ( 1.265540092975623088, 0.5243090560775253151, -1.734071359953066382 ) ) ;
#102278=CARTESIAN_POINT ( 'NONE',  ( 5.823154874416164084, -0.05760400987671504547, 2.161107263091876618 ) ) ;
#102282=CARTESIAN_POINT ( 'NONE',  ( -0.2060670157024322158, -0.8220983527124374746, -1.729069022899624164 ) ) ;
#102293=CARTESIAN_POINT ( 'NONE',  ( 3.801785103514757846, -0.6297183656660889639, 2.067937956787009757 ) ) ;
#102296=CARTESIAN_POINT ( 'NONE',  ( 0.8441712343106638761, -1.349783269286155996, -1.635521010841307410 ) ) ;
#102298=CARTESIAN_POINT ( 'NONE',  ( 2.073447407941295673, 1.887670557785134928, -0.5683696268203948243 ) ) ;
#102299=CARTESIAN_POINT ( 'NONE',  ( 4.992401499097729456, -1.057410677138232780, 1.593263788312593743 ) ) ;
#102302=CARTESIAN_POINT ( 'NONE',  ( 6.250452387334210158, -1.959941389959872549, -0.1944618805250642457 ) ) ;
#102303=CARTESIAN_POINT ( 'NONE',  ( 0.7263842893957738189, 0.1423072432159468159, 1.936797167885440096 ) ) ;
#102309=CARTESIAN_POINT ( 'NONE',  ( 4.582611755193141789, -1.246403352314252810, 1.450376384258989182 ) ) ;
#102311=CARTESIAN_POINT ( 'NONE',  ( 3.229339687698820072, 0.05429069646168545316, 2.206380697113208722 ) ) ;
#102312=CARTESIAN_POINT ( 'NONE',  ( 1.958336283151569157, 2.200835622443702011, -0.1624582802550941507 ) ) ;
#102314=CARTESIAN_POINT ( 'NONE',  ( 0.2055213853429035953, 1.417038256915002181, 1.284265443176696442 ) ) ;
#102318=CARTESIAN_POINT ( 'NONE',  ( 2.980987059868036138, 1.948563265827065960, 0.6999735360200682877 ) ) ;
#102323=CARTESIAN_POINT ( 'NONE',  ( 0.7257156204387126275, -2.052300050329861847, 0.6792298617422781737 ) ) ;
#102324=CARTESIAN_POINT ( 'NONE',  ( 2.929422067023911502, -1.473737196803912797, -1.622193633833472814 ) ) ;
#102331=CARTESIAN_POINT ( 'NONE',  ( 6.012339335674446339, -1.629552802491928354, 0.5935831289462877303 ) ) ;
#102334=CARTESIAN_POINT ( 'NONE',  ( 3.467693386974544545, -0.4085244671708112008, 2.029378838279243258 ) ) ;
#102335=CARTESIAN_POINT ( 'NONE',  ( 4.218443861432810138, 2.076744001477859314, 0.4112613105302816430 ) ) ;
#102338=CARTESIAN_POINT ( 'NONE',  ( 3.397268178914572889, -1.739110600408208196, 0.9241587964883835049 ) ) ;
#102339=CARTESIAN_POINT ( 'NONE',  ( 0.5977379272000953314, 1.286164058678052946, 1.415416067018962165 ) ) ;
#102340=CARTESIAN_POINT ( 'NONE',  ( 5.384854118993849248, 2.023671607873143152, -1.076698936902406922 ) ) ;
#102341=CARTESIAN_POINT ( 'NONE',  ( 2.824607995650964209, 1.719152210223941601, 0.6149139946348626262 ) ) ;
#102346=CARTESIAN_POINT ( 'NONE',  ( 4.060795210881157580, 0.5408870827437872730, 1.939095388008914345 ) ) ;
#102347=CARTESIAN_POINT ( 'NONE',  ( 4.856279117655732058, -1.961245242753749674, -0.05215834203427943683 ) ) ;
#102350=CARTESIAN_POINT ( 'NONE',  ( 0.1753634416057497925, 6.947017063990798214, -2.739087685391654148 ) ) ;
#102351=CARTESIAN_POINT ( 'NONE',  ( 0.8903107040577078468, -0.5117213476562210150, -2.027015703535272717 ) ) ;
#102352=CARTESIAN_POINT ( 'NONE',  ( 5.823074959372767090, -0.03971387110058427483, 1.769581062106811986 ) ) ;
#102354=CARTESIAN_POINT ( 'NONE',  ( 1.939652437182255662, 0.8368340126228106524, -2.025574644071465258 ) ) ;
#102355=CARTESIAN_POINT ( 'NONE',  ( 6.544851825567233661, -1.402524398529688021, -1.030163739638074727 ) ) ;
#102357=CARTESIAN_POINT ( 'NONE',  ( 0.1333692844072767447, 1.351132181276387678, -2.308013766563504987 ) ) ;
#102358=CARTESIAN_POINT ( 'NONE',  ( 0.8555558213108410692, 1.723155885897029282, -0.08016331026279581440 ) ) ;
#102359=CARTESIAN_POINT ( 'NONE',  ( 0.9315567102232256147, 1.134920720140248251, 1.998545780126102844 ) ) ;
#102360=CARTESIAN_POINT ( 'NONE',  ( 0.1698123575781598782, 1.266975945507025081, 1.788028528876134393 ) ) ;
#102361=CARTESIAN_POINT ( 'NONE',  ( 6.485661447747480324, 1.619333758318822536, 0.6201139256068515238 ) ) ;
#102362=CARTESIAN_POINT ( 'NONE',  ( 2.420803835572300500, 1.440536793087299205, -1.671967039616916617 ) ) ;
#102364=CARTESIAN_POINT ( 'NONE',  ( 0.6730172731169652423, 1.498246551899045098, -1.571433807820749706 ) ) ;
#102366=CARTESIAN_POINT ( 'NONE',  ( 1.165409582065090266, 1.953992404094638591, -0.8159742408818432269 ) ) ;
#102367=CARTESIAN_POINT ( 'NONE',  ( 6.827182134110230116, 2.398703475977175703, 2.668604416072619223 ) ) ;
#102368=CARTESIAN_POINT ( 'NONE',  ( 5.930678043039342207, 1.856691256794128053, 0.5132231078649931444 ) ) ;
#102370=CARTESIAN_POINT ( 'NONE',  ( 1.839794590071419211, 0.8728355696882350578, -2.119893007042342958 ) ) ;
#102374=CARTESIAN_POINT ( 'NONE',  ( 3.703960633009816483, 1.609604546992912999, 1.531039788047829253 ) ) ;
#102383=CARTESIAN_POINT ( 'NONE',  ( 2.074842474778653134, -0.8596299393073093542, 1.824119475507138821 ) ) ;
#102385=CARTESIAN_POINT ( 'NONE',  ( 1.024372331059967056, 1.013329571420513053, 1.796381585629814426 ) ) ;
#102390=CARTESIAN_POINT ( 'NONE',  ( 4.171962795014371395, -1.262591954434747921, 1.790989659139609724 ) ) ;
#102391=CARTESIAN_POINT ( 'NONE',  ( 1.582657950916711131, -0.6767122143778031562, 1.899619169727875700 ) ) ;
#102392=CARTESIAN_POINT ( 'NONE',  ( -0.04178991631376138827, -1.644041690304678616, -0.8291446804715857377 ) ) ;
#102393=CARTESIAN_POINT ( 'NONE',  ( 5.812145867431055102, 1.542159960141289199, -1.696276722712148688 ) ) ;
#102394=CARTESIAN_POINT ( 'NONE',  ( 3.486116527793288178, -0.3603757036649730128, -1.805346353211812804 ) ) ;
#102396=CARTESIAN_POINT ( 'NONE',  ( 4.014527796464135712, 1.291161025869846712, -1.290856679043244970 ) ) ;
#102397=CARTESIAN_POINT ( 'NONE',  ( 5.326796142270829648, 0.8146286751641409474, -1.844708973168760924 ) ) ;
#102399=CARTESIAN_POINT ( 'NONE',  ( 4.399490234458226290, 1.814852776126129497, 1.350843829522253792 ) ) ;
#102401=CARTESIAN_POINT ( 'NONE',  ( 6.124072230051534227, -1.166888049220366597, -1.752910934067633875 ) ) ;
#102403=CARTESIAN_POINT ( 'NONE',  ( 4.141125838365485201, -0.1998502692034490602, -2.060677327190631569 ) ) ;
#102409=CARTESIAN_POINT ( 'NONE',  ( 2.367692237863534555, 1.889325326408105576, -0.3758258368516536052 ) ) ;
#102411=CARTESIAN_POINT ( 'NONE',  ( 0.4320049508096295288, 1.131045402950446199, 1.612214446364314213 ) ) ;
#102416=CARTESIAN_POINT ( 'NONE',  ( 1.793536179914383188, -0.1149406603053771958, -2.218580859979270681 ) ) ;
#102417=CARTESIAN_POINT ( 'NONE',  ( 2.960101939890079858, 2.095960298449873971, -0.2048252169620876917 ) ) ;
#102420=CARTESIAN_POINT ( 'NONE',  ( 0.9239872072115723478, 0.9125040393608827571, 1.621899335316509649 ) ) ;
#102425=CARTESIAN_POINT ( 'NONE',  ( 1.723052270212792836, 1.567896913533245229, -1.427966198690698851 ) ) ;
#102428=CARTESIAN_POINT ( 'NONE',  ( 4.492601031306558745, 1.923586649950057792, 0.3847822903023030428 ) ) ;
#102429=CARTESIAN_POINT ( 'NONE',  ( 3.274459119871219848, -1.289031633699176949, 1.735169069618908821 ) ) ;
#102430=CARTESIAN_POINT ( 'NONE',  ( 2.050122339901743196, -1.422379512129726908, 1.169167124061460949 ) ) ;
#102433=CARTESIAN_POINT ( 'NONE',  ( 5.033026810027643627, -1.234204449110408053, -1.227257546430237989 ) ) ;
#102437=CARTESIAN_POINT ( 'NONE',  ( 1.499129196564863209, 1.767075381950654611, -1.244890797856931686 ) ) ;
#102439=CARTESIAN_POINT ( 'NONE',  ( 3.286482353612128815, -1.943773746517188039, 0.5350062169211177165 ) ) ;
#102441=CARTESIAN_POINT ( 'NONE',  ( 0.7608789386071808103, -1.564954856162886765, 1.491513986042219297 ) ) ;
#102442=CARTESIAN_POINT ( 'NONE',  ( 3.836761837097919070, 0.2881357685159210424, 1.950175340126619306 ) ) ;
#102445=CARTESIAN_POINT ( 'NONE',  ( 6.609000000000052388, 1.285212548570794588, 2.017169166534539038 ) ) ;
#102446=CARTESIAN_POINT ( 'NONE',  ( 2.999484396081523396, -1.939716604588328508, 0.09806999327347488971 ) ) ;
#102452=CARTESIAN_POINT ( 'NONE',  ( -0.1110810684432622653, 2.888487728959455936, -2.285870655067727242 ) ) ;
#102458=CARTESIAN_POINT ( 'NONE',  ( 6.739320262688799801, -2.065560010629815313, 1.029036360498974068 ) ) ;
#102460=CARTESIAN_POINT ( 'NONE',  ( 3.854310441289869882, -1.959320932037407426, -0.1006921081871253454 ) ) ;
#102462=CARTESIAN_POINT ( 'NONE',  ( 1.723279953462612202, 1.994870059565261755, 0.2930690452552578429 ) ) ;
#102464=CARTESIAN_POINT ( 'NONE',  ( 3.397769718358482738, -2.085282637925215177, 0.3663039253445389276 ) ) ;
#102466=CARTESIAN_POINT ( 'NONE',  ( 0.1747926744264712562, 2.889263262932476817, -2.344248796821886138 ) ) ;
#102468=CARTESIAN_POINT ( 'NONE',  ( 2.659893383946440260, -1.269561761542839617, 1.333649727802692198 ) ) ;
#102469=VERTEX_POINT ( 'NONE', #142981 ) ;
#102472=CARTESIAN_POINT ( 'NONE',  ( 3.990573222356631256, -1.218298518170106925, 1.735533685479621502 ) ) ;
#102476=CARTESIAN_POINT ( 'NONE',  ( 5.325487547722469905, -1.958136382931666031, 0.6425617224121594750 ) ) ;
#102478=CARTESIAN_POINT ( 'NONE',  ( 2.085277916773973228, -0.7859315772556186852, 1.665205719185464561 ) ) ;
#102485=CARTESIAN_POINT ( 'NONE',  ( 2.121956728516772639, -2.140194184088719531, 0.5379336890513550795 ) ) ;
#102486=CARTESIAN_POINT ( 'NONE',  ( 4.798257751182677389, -2.261729152689537781, -0.06211711723675371333 ) ) ;
#102488=CARTESIAN_POINT ( 'NONE',  ( 4.922017755325088118, -1.802143800875387614, 0.1849416998233286979 ) ) ;
#102489=CARTESIAN_POINT ( 'NONE',  ( 3.942530958389865781, -1.415603592240498365, 1.290913190617749118 ) ) ;
#102491=CARTESIAN_POINT ( 'NONE',  ( 3.836761837097919070, 0.2881357685159210424, 1.950175340126619306 ) ) ;
#102492=CARTESIAN_POINT ( 'NONE',  ( 5.612129163471575310, -0.8422657237196762292, -1.670366365510121742 ) ) ;
#102493=CARTESIAN_POINT ( 'NONE',  ( 5.318752605461887661, -1.348013374683079135, 1.283375817886179826 ) ) ;
#102495=CARTESIAN_POINT ( 'NONE',  ( 0.005092704479254389627, -0.09411098085002241043, 2.014433268766747887 ) ) ;
#102497=CARTESIAN_POINT ( 'NONE',  ( 2.033940956955893498, -1.376631898319637726, -1.593950314443808969 ) ) ;
#102500=CARTESIAN_POINT ( 'NONE',  ( 0.07479286986303290696, 5.725009232006174287, -2.449550298930736059 ) ) ;
#102501=CARTESIAN_POINT ( 'NONE',  ( 3.164422831683691761, 2.120778211551369807, -0.003951117757632071313 ) ) ;
#102503=CARTESIAN_POINT ( 'NONE',  ( 2.056904690034748739, 0.4466968674397324701, 1.969590803855451933 ) ) ;
#102509=CARTESIAN_POINT ( 'NONE',  ( 2.020999711022552159, 2.016103727727487804, 0.7800470891412072394 ) ) ;
#102516=CARTESIAN_POINT ( 'NONE',  ( 0.6443834720083198020, 0.6415979653194536780, 2.095529601600601755 ) ) ;
#102518=CARTESIAN_POINT ( 'NONE',  ( 1.622331739061450007, -1.257988004683800787, -1.880359251820800104 ) ) ;
#102526=CARTESIAN_POINT ( 'NONE',  ( 4.248488654339817927, 0.4632642123635377640, 1.661427155677893674 ) ) ;
#102528=CARTESIAN_POINT ( 'NONE',  ( 1.862210123611393708, -1.255811410660602867, 1.247235970127296811 ) ) ;
#102529=CARTESIAN_POINT ( 'NONE',  ( 2.772137614628172653, 2.003179168937582855, -0.1996775111661793500 ) ) ;
#102531=CARTESIAN_POINT ( 'NONE',  ( 5.245248717291847385, -1.895131572898335115, 1.130396782059706950 ) ) ;
#102533=CARTESIAN_POINT ( 'NONE',  ( 4.008073073761713623, -0.7691326184188684856, 1.867817587601346307 ) ) ;
#102535=CARTESIAN_POINT ( 'NONE',  ( 4.077750037130567939, -0.7691059624741981571, 1.864175985064358665 ) ) ;
#102538=CARTESIAN_POINT ( 'NONE',  ( 2.518242125168220102, 1.223528130051700025, -1.415109699333151561 ) ) ;
#102540=CARTESIAN_POINT ( 'NONE',  ( 2.425908952446104827, -1.891012092455180760, 0.2844710172774585488 ) ) ;
#102544=CARTESIAN_POINT ( 'NONE',  ( 0.4922593472763935329, -1.060406550076501642, 1.591262010887870115 ) ) ;
#102546=CARTESIAN_POINT ( 'NONE',  ( 1.574581288703358339, 1.320057194528483135, -1.451483715152704246 ) ) ;
#102548=DIRECTION ( 'NONE',  ( -1.000000000000000000, 1.014813233446432150E-15, 1.972152263052529514E-31 ) ) ;
#102550=CARTESIAN_POINT ( 'NONE',  ( 3.762070191281779774, 0.7111978290502696254, -1.997938288694045550 ) ) ;
#102555=CARTESIAN_POINT ( 'NONE',  ( 5.343030940550726804, -1.692140053440434277, 1.011138898101251016 ) ) ;
#102557=CARTESIAN_POINT ( 'NONE',  ( 1.283448800676566970, 0.1440664973490720091, -2.008080635846798856 ) ) ;
#102560=CARTESIAN_POINT ( 'NONE',  ( 1.441172756004579947, -1.817888344413360668, -1.085095524780084864 ) ) ;
#102562=CARTESIAN_POINT ( 'NONE',  ( 2.541538742049511246, 1.893869637037654208, -0.8368498079355383146 ) ) ;
#102566=CARTESIAN_POINT ( 'NONE',  ( 4.242189115703227209, 0.5575990197337198362, 2.014825664747122769 ) ) ;
#102568=CARTESIAN_POINT ( 'NONE',  ( 3.223480179809079971, -1.759765543241718966, 0.4855387900214308550 ) ) ;
#102569=CARTESIAN_POINT ( 'NONE',  ( 1.101899038012419174, -0.8149344392366760781, 1.617857622727811862 ) ) ;
#102571=CARTESIAN_POINT ( 'NONE',  ( 6.709632191794143274, -0.4886956906769434061, 2.160084693451309601 ) ) ;
#102574=CARTESIAN_POINT ( 'NONE',  ( 5.174942826180319422, -2.076333920960464763, -0.7478091396579674699 ) ) ;
#102577=CARTESIAN_POINT ( 'NONE',  ( 3.844317892072905973, 1.020479721125296280, -1.617037373464407457 ) ) ;
#102585=CARTESIAN_POINT ( 'NONE',  ( 6.585463931165095985, -0.9389328202267492873, 1.978239266594773671 ) ) ;
#102592=CARTESIAN_POINT ( 'NONE',  ( 4.077312411328878561, 1.762187477035919603, -0.6278270876356045749 ) ) ;
#102600=CARTESIAN_POINT ( 'NONE',  ( 6.578973861349465935, 1.929489650308688464, 0.7507879531711419974 ) ) ;
#102602=CARTESIAN_POINT ( 'NONE',  ( 1.089470510105726708, -0.4871801946146369078, 1.956568126268923846 ) ) ;
#102606=CARTESIAN_POINT ( 'NONE',  ( 1.957222284144799929, 0.3726435881295561692, -2.159377063894574622 ) ) ;
#102607=CARTESIAN_POINT ( 'NONE',  ( 5.918537399722813674, 1.222626809077583587, -1.356019982345892050 ) ) ;
#102614=CARTESIAN_POINT ( 'NONE',  ( 3.421284184235491743, -1.099380227797893905, -1.476844927387373163 ) ) ;
#102615=CARTESIAN_POINT ( 'NONE',  ( 1.067042177248921364, -1.585704042599777264, 1.240073755948613243 ) ) ;
#102616=CARTESIAN_POINT ( 'NONE',  ( 2.126706441246130286, 0.3935840842550219487, -2.264316624754546314 ) ) ;
#102618=CARTESIAN_POINT ( 'NONE',  ( 1.129495572712395646, 1.795378659943444033, -0.4894723102292392047 ) ) ;
#102622=CARTESIAN_POINT ( 'NONE',  ( 4.939673314881130040, -1.814047719456039154, 0.6055163330952323397 ) ) ;
#102626=CARTESIAN_POINT ( 'NONE',  ( 3.403930425450612418, -0.8493818440679711257, -1.910634358282743417 ) ) ;
#102627=CARTESIAN_POINT ( 'NONE',  ( 1.744777856283234785, -1.581906188472384400, 0.9981555316627908070 ) ) ;
#102630=CARTESIAN_POINT ( 'NONE',  ( 2.981702274927648944, -1.715113757222336721, -0.2947475401101228853 ) ) ;
#102633=CARTESIAN_POINT ( 'NONE',  ( 4.248488654339817927, 0.4632642123635377640, 1.661427155677893674 ) ) ;
#102634=CARTESIAN_POINT ( 'NONE',  ( 3.579775959861815515, -1.078688530630707243, 1.907616655872627964 ) ) ;
#102635=CARTESIAN_POINT ( 'NONE',  ( 5.971336403843030105, 0.1662174427981797931, -2.200672837095698497 ) ) ;
#102638=CARTESIAN_POINT ( 'NONE',  ( 3.713894982949633050, 0.5324762967815239723, -2.104625409411722270 ) ) ;
#102639=CARTESIAN_POINT ( 'NONE',  ( 1.840199252755945425, 1.805614550920462635, 0.2691313018618191055 ) ) ;
#102640=CARTESIAN_POINT ( 'NONE',  ( 0.2507196182260813533, -0.4238382354822354259, -1.922440920834954436 ) ) ;
#102641=CARTESIAN_POINT ( 'NONE',  ( 4.716069161646245789, 1.085680477651463915, -1.817652797078447735 ) ) ;
#102644=CARTESIAN_POINT ( 'NONE',  ( 4.406014021519581547, -0.9797006336973247409, -2.072624738501188446 ) ) ;
#102646=CARTESIAN_POINT ( 'NONE',  ( 6.720655732516681802, 2.481091636469245021, 2.111593894264688132 ) ) ;
#102648=CARTESIAN_POINT ( 'NONE',  ( 0.8914570141239013257, -0.05588796005432519753, -2.119924415460701983 ) ) ;
#102652=CARTESIAN_POINT ( 'NONE',  ( 6.883263157960367806, 2.959656548886806071, 2.506466465954690914 ) ) ;
#102655=CARTESIAN_POINT ( 'NONE',  ( 5.238907797441370029, 2.013986022392059816, -0.1017483359899013229 ) ) ;
#102657=CARTESIAN_POINT ( 'NONE',  ( 4.610253265130005218, 2.062215687086375038, -0.04552280787792003375 ) ) ;
#102659=CARTESIAN_POINT ( 'NONE',  ( -0.2409995289980245703, 0.2355275985303668385, -2.034371242098035548 ) ) ;
#102663=CARTESIAN_POINT ( 'NONE',  ( 0.2696249905001372182, 1.205521239366886821, 1.707859383111657747 ) ) ;
#102664=CARTESIAN_POINT ( 'NONE',  ( 4.272111401563948085, 1.799923229630392640, -0.9091438646662284295 ) ) ;
#102665=CARTESIAN_POINT ( 'NONE',  ( 4.388128076750056117, -0.4078595375654435751, -1.795341762384855544 ) ) ;
#102669=CARTESIAN_POINT ( 'NONE',  ( 0.8324923845523107824, 0.1201152365052655241, 1.720655618271366150 ) ) ;
#102672=CARTESIAN_POINT ( 'NONE',  ( 0.7907308791721240349, -2.245476950237018432, -0.2759641350603259657 ) ) ;
#102673=CARTESIAN_POINT ( 'NONE',  ( 2.860102072500060544, 2.095886770163409185, -0.2068341903323153708 ) ) ;
#102677=CARTESIAN_POINT ( 'NONE',  ( 6.468749999177490828, 0.7852924545920478838, -1.895863743164218018 ) ) ;
#102682=CARTESIAN_POINT ( 'NONE',  ( 4.658541260611516854, 2.215511418189203496, 0.1622135575486300108 ) ) ;
#102683=CARTESIAN_POINT ( 'NONE',  ( 2.027518650255655253, -1.432890729411402830, -1.658174735819064827 ) ) ;
#102686=CARTESIAN_POINT ( 'NONE',  ( 5.863715402168388380, -0.4781514528688200483, 1.902565108626976809 ) ) ;
#102691=CARTESIAN_POINT ( 'NONE',  ( 4.113620189327307664, 1.705085180707970771, 1.260635662952174663 ) ) ;
#102697=CARTESIAN_POINT ( 'NONE',  ( 5.372543328820884589, -0.05112055865702340440, -1.840719716649619198 ) ) ;
#102701=CARTESIAN_POINT ( 'NONE',  ( 0.5732861554464663278, -0.9687841611035786782, 1.445654263422226027 ) ) ;
#102703=CARTESIAN_POINT ( 'NONE',  ( -0.1604749557937330817, 7.629137130509052511, -2.703579865625728385 ) ) ;
#102704=CARTESIAN_POINT ( 'NONE',  ( 5.190363053866647647, -2.144918610114197488, -0.2683968819863768451 ) ) ;
#102707=CARTESIAN_POINT ( 'NONE',  ( 4.364260218091946975, 1.016419123106377276, 1.907829002176253175 ) ) ;
#102709=CARTESIAN_POINT ( 'NONE',  ( 5.149669460738499183, 0.6209446730581876794, -1.871051946789156650 ) ) ;
#102710=CARTESIAN_POINT ( 'NONE',  ( 4.446485213073447795, 1.132808404574834782, 1.312715084458302872 ) ) ;
#102712=CARTESIAN_POINT ( 'NONE',  ( 0.6443834720083198020, 0.6415979653194536780, 2.095529601600601755 ) ) ;
#102713=CARTESIAN_POINT ( 'NONE',  ( 2.204549329899041510, -2.307029201398633322, 0.05716382847485364238 ) ) ;
#102714=CARTESIAN_POINT ( 'NONE',  ( 4.464173201700037730, 0.9678196394932538915, 1.819351253882226516 ) ) ;
#102715=CARTESIAN_POINT ( 'NONE',  ( -0.02357939311542662716, -0.1349932991356362910, -1.911059701570053226 ) ) ;
#102722=CARTESIAN_POINT ( 'NONE',  ( 3.048105859194950362, 0.7956334958073747465, -2.058523145315640956 ) ) ;
#102724=CARTESIAN_POINT ( 'NONE',  ( 1.217372920688150506, 0.3700031967454868176, -1.823611282344459239 ) ) ;
#102729=CARTESIAN_POINT ( 'NONE',  ( 6.825078400183588023, 2.959908325773926041, 2.496992193004472504 ) ) ;
#102731=CARTESIAN_POINT ( 'NONE',  ( 5.999929499617846496, -0.6670042279848520383, -1.716255146773135287 ) ) ;
#102733=CARTESIAN_POINT ( 'NONE',  ( 3.625900526125751089, -1.226333045360414653, -1.656161981788171200 ) ) ;
#102735=UNCERTAINTY_MEASURE_WITH_UNIT (LENGTH_MEASURE( 1.000000000000000082E-05 ), #68448, 'distance_accuracy_value', 'NONE');
#102737=CARTESIAN_POINT ( 'NONE',  ( 2.789718171214683462, 1.917044005781431748, -0.6357942740662542169 ) ) ;
#102740=CARTESIAN_POINT ( 'NONE',  ( 2.448182087220668102, 2.060414928722671402, 0.05179878229087316738 ) ) ;
#102745=CARTESIAN_POINT ( 'NONE',  ( 5.531908139154323223, -1.397534428995873546, -1.707979418440738195 ) ) ;
#102746=CARTESIAN_POINT ( 'NONE',  ( 1.282749207608822495, -2.108609127331688260, -0.4749100009155197699 ) ) ;
#102749=CARTESIAN_POINT ( 'NONE',  ( 0.3566581422463632189, -1.900417414521380133, -0.6748426577906708745 ) ) ;
#102750=CARTESIAN_POINT ( 'NONE',  ( 1.986132587416184370, 2.144477605524505393, 0.8272852225373708013 ) ) ;
#102752=CARTESIAN_POINT ( 'NONE',  ( 6.551426578739074635, -1.705833205818767295, 0.8644478841580637285 ) ) ;
#102753=CARTESIAN_POINT ( 'NONE',  ( 6.875078400183575411, 7.629137130509070275, 2.455651831298297338 ) ) ;
#102755=CARTESIAN_POINT ( 'NONE',  ( 2.395189659270926086, 1.444574673180216706, 1.188490415850687265 ) ) ;
#102757=CARTESIAN_POINT ( 'NONE',  ( 3.854704076794239764, -1.883312302057647880, -0.7212934815618715634 ) ) ;
#102761=CARTESIAN_POINT ( 'NONE',  ( 5.654936504234950867, -1.661008888676926309, 1.294703585725354156 ) ) ;
#102766=CARTESIAN_POINT ( 'NONE',  ( 5.308855472784884455, -0.4948685743355190070, -1.958072916474236314 ) ) ;
#102768=CARTESIAN_POINT ( 'NONE',  ( 0.9013244701963195604, -1.770926582075180944, 1.057100273733258433 ) ) ;
#102774=CARTESIAN_POINT ( 'NONE',  ( 3.596278845262687263, 0.9791764565295042466, -1.937929667198809769 ) ) ;
#102777=CARTESIAN_POINT ( 'NONE',  ( 1.979791773625012352, -1.805961398883266344, -0.3578489297004632808 ) ) ;
#102779=CARTESIAN_POINT ( 'NONE',  ( 3.966501855323391723, -2.045284974426237579, -0.7877190255709336508 ) ) ;
#102781=CARTESIAN_POINT ( 'NONE',  ( 5.208033936170274103, -2.252144374781993363, 0.2163938657309023850 ) ) ;
#102788=CARTESIAN_POINT ( 'NONE',  ( 5.167173303313960631, 0.1731176489731758861, -1.761265287352784314 ) ) ;
#102790=CARTESIAN_POINT ( 'NONE',  ( 3.527992865196138972, -1.982922396879973626, 0.3464002264041438073 ) ) ;
#102792=CARTESIAN_POINT ( 'NONE',  ( 1.887856735188620627, 1.451798466554796718, 1.525807353268118227 ) ) ;
#102794=CARTESIAN_POINT ( 'NONE',  ( 2.435944266227826116, 1.209484882827957630, 1.554366883019624668 ) ) ;
#102795=CARTESIAN_POINT ( 'NONE',  ( 0.2154177506630133854, -1.835460468737951878, 0.3602540799089171131 ) ) ;
#102796=CARTESIAN_POINT ( 'NONE',  ( 0.1507198084474276056, -0.4258245693303016610, -1.922078969575198526 ) ) ;
#102797=CARTESIAN_POINT ( 'NONE',  ( 5.625234629914776185, 1.601787910378251967, 0.8462062870350762767 ) ) ;
#102802=CARTESIAN_POINT ( 'NONE',  ( 5.506679003988666388, 1.415762158562785533, -1.222804595763474333 ) ) ;
#102805=CARTESIAN_POINT ( 'NONE',  ( 5.700075226665620498, 0.8442301939139056355, -1.890501578402821847 ) ) ;
#102815=CARTESIAN_POINT ( 'NONE',  ( 5.476992472119650124, 1.812042599547862176, 0.7524171098330989516 ) ) ;
#102817=CARTESIAN_POINT ( 'NONE',  ( 3.462267382487670631, 1.587593928739635896, 1.242537129137813556 ) ) ;
#102818=CARTESIAN_POINT ( 'NONE',  ( 2.272541799296357468, -0.3318032026102230581, -1.886604652318550901 ) ) ;
#102820=CARTESIAN_POINT ( 'NONE',  ( 0.6795420635867071013, 1.475991390215245058, 1.620154534501851096 ) ) ;
#102821=CARTESIAN_POINT ( 'NONE',  ( 0.2331713839410939626, 4.091360563681152307, -2.508188233588979799 ) ) ;
#102822=CARTESIAN_POINT ( 'NONE',  ( 1.862360739135361376, -1.326353699019737098, 1.319252464149045734 ) ) ;
#102824=CARTESIAN_POINT ( 'NONE',  ( 3.638934968716364793, 1.913053428401530809, 0.6273635501436899409 ) ) ;
#102827=CARTESIAN_POINT ( 'NONE',  ( 4.956716356600668227, -1.994036693836033658, -0.7120731657841266049 ) ) ;
#102829=CARTESIAN_POINT ( 'NONE',  ( 5.564915762860970894, 1.570151797963925455, -1.349580972669261580 ) ) ;
#102830=CARTESIAN_POINT ( 'NONE',  ( 1.628582148955775910, 0.2080868244966528613, 2.080379227509927542 ) ) ;
#102832=CARTESIAN_POINT ( 'NONE',  ( 6.282242891264209206, -0.9739734823789309992, 1.543877162560060912 ) ) ;
#102841=CARTESIAN_POINT ( 'NONE',  ( 0.9788403037365877024, -1.637337388150851725, -0.7752084675131820646 ) ) ;
#102848=EDGE_CURVE ( 'NONE', #150774, #21539, #1089, .T. ) ;
#102850=CARTESIAN_POINT ( 'NONE',  ( 6.380482474105581225, -0.5405081658083621399, -1.942537888137134461 ) ) ;
#102851=CARTESIAN_POINT ( 'NONE',  ( 0.5223349339509277822, -2.109880975928311031, 0.2119513895993754005 ) ) ;
#102853=CARTESIAN_POINT ( 'NONE',  ( 0.1405533004714279166, 6.947787103499396544, -2.874819994463383654 ) ) ;
#102857=CARTESIAN_POINT ( 'NONE',  ( 3.116014175596728109, 1.960399024780419275, -0.1881816519722582237 ) ) ;
#102858=CARTESIAN_POINT ( 'NONE',  ( 4.183220377109976518, 1.621195451842275315, 1.198844725951081047 ) ) ;
#102861=CARTESIAN_POINT ( 'NONE',  ( 4.259861650310483583, 1.032037387010206198, 1.933225914978464299 ) ) ;
#102863=CARTESIAN_POINT ( 'NONE',  ( 3.065363963417499615, 0.2843319914107733104, -1.905185398925368423 ) ) ;
#102865=CARTESIAN_POINT ( 'NONE',  ( -0.02968770228137587730, 2.889947918782026726, -2.315223470976325526 ) ) ;
#102866=CARTESIAN_POINT ( 'NONE',  ( 0.1333542156527321720, 1.344858830485482937, -2.298444861300387387 ) ) ;
#102870=CARTESIAN_POINT ( 'NONE',  ( 5.348484190341658007, -1.954120660473107396, -0.2448405522006945334 ) ) ;
#102871=CARTESIAN_POINT ( 'NONE',  ( 0.8724827243445825165, -0.04916951280507049493, -1.941606035699546151 ) ) ;
#102872=CARTESIAN_POINT ( 'NONE',  ( 4.529943747908701468, -1.973814829549960237, 0.3949202218342766080 ) ) ;
#102874=CARTESIAN_POINT ( 'NONE',  ( 5.852921341749488526, -1.041456137194999521, 2.048983711149698461 ) ) ;
#102876=CARTESIAN_POINT ( 'NONE',  ( 4.135495018730405370, 1.753490048523008049, -0.6236645969141580981 ) ) ;
#102882=CARTESIAN_POINT ( 'NONE',  ( 0.3631484714031462668, 0.2087870660046411420, -2.181583536649676525 ) ) ;
#102886=CARTESIAN_POINT ( 'NONE',  ( 0.3108172448005979138, 1.586703044182024458, 0.9029097728878652251 ) ) ;
#102888=CARTESIAN_POINT ( 'NONE',  ( 2.373305363469370377, -0.2979590584733567971, -1.708161578628903055 ) ) ;
#102889=CARTESIAN_POINT ( 'NONE',  ( 6.509000000000039421, 2.968845098214093703, 2.453284407971462411 ) ) ;
#102891=CARTESIAN_POINT ( 'NONE',  ( 5.830640656690653678, 1.760721658632548037, 0.4824517239352192344 ) ) ;
#102892=CARTESIAN_POINT ( 'NONE',  ( 3.450005804356533368, -0.7992637590314204399, 1.791754569076028147 ) ) ;
#102896=CARTESIAN_POINT ( 'NONE',  ( 4.354221869268804390, 0.9056986662851629344, -1.917456963280274040 ) ) ;
#102899=CARTESIAN_POINT ( 'NONE',  ( 2.096617048772158487, 2.047133997803842753, 0.3078910663548983795 ) ) ;
#102900=CARTESIAN_POINT ( 'NONE',  ( 6.827182134110196365, 2.083530588508203607, 2.119847806254702594 ) ) ;
#102902=CARTESIAN_POINT ( 'NONE',  ( 4.459788417035775332, -1.717034742021033455, -1.409269467666877995 ) ) ;
#102904=CARTESIAN_POINT ( 'NONE',  ( 3.112262249421397620, 0.05891664663748399922, 2.298092032709637689 ) ) ;
#102913=CARTESIAN_POINT ( 'NONE',  ( 3.322422747544371280, -0.7792853099402965444, -1.746611395919236642 ) ) ;
#102915=CARTESIAN_POINT ( 'NONE',  ( 4.506709144069167117, 1.332172526941363344, -1.095522069602150372 ) ) ;
#102916=CARTESIAN_POINT ( 'NONE',  ( 3.327361509216096191, -1.530157842762596143, -1.313544516083162028 ) ) ;
#102917=CARTESIAN_POINT ( 'NONE',  ( 3.727375017909192234, 2.287664543646179105, 0.2247039424928508056 ) ) ;
#102919=CARTESIAN_POINT ( 'NONE',  ( 6.721333371289576419, -0.1616129481825591130, 2.070667135302119544 ) ) ;
#102921=CARTESIAN_POINT ( 'NONE',  ( 4.428786516960594000, 0.08554295028175006033, 1.767770697671824820 ) ) ;
#102923=CARTESIAN_POINT ( 'NONE',  ( 0.5160991691709617690, -1.231265438625952724, -1.933346247471772861 ) ) ;
#102924=CARTESIAN_POINT ( 'NONE',  ( -0.01232043299871990460, -0.3711077647031227333, -1.706071622908360119 ) ) ;
#102926=CARTESIAN_POINT ( 'NONE',  ( 5.279302027902110339, 1.469929824498400039, 1.625505876179579534 ) ) ;
#102931=CARTESIAN_POINT ( 'NONE',  ( 0.6784789811392475389, -1.161776791282279397, -1.834017514133066129 ) ) ;
#102932=CARTESIAN_POINT ( 'NONE',  ( 0.7961116948485976730, -0.9110139862544311962, -1.799120828532501326 ) ) ;
#102935=CARTESIAN_POINT ( 'NONE',  ( 4.652910101842601343, -1.546415465631932884, 1.148725279867918170 ) ) ;
#102937=CARTESIAN_POINT ( 'NONE',  ( 0.6686063958157261178, 2.218491797483721051, -0.1167170572400257761 ) ) ;
#102946=CARTESIAN_POINT ( 'NONE',  ( 4.862738897425579410, 0.1637244223539826016, -1.732714468228998994 ) ) ;
#102947=CARTESIAN_POINT ( 'NONE',  ( 2.224987305166142626, -1.792472147789250236, -0.7979012372742313453 ) ) ;
#102952=CARTESIAN_POINT ( 'NONE',  ( 6.795372052238223048, -1.752927774724974297, 0.8811163259476795240 ) ) ;
#102955=CARTESIAN_POINT ( 'NONE',  ( 4.926970384345759513, -1.727065721694167832, 1.040790168839386798 ) ) ;
#102956=CARTESIAN_POINT ( 'NONE',  ( 1.059873865361460332, 0.4390357074517194369, -2.219354932451859330 ) ) ;
#102960=CARTESIAN_POINT ( 'NONE',  ( 1.581098268704693055, 1.730367963306264301, -0.7109649657882493035 ) ) ;
#102961=CARTESIAN_POINT ( 'NONE',  ( 0.07043219980315276740, -0.8200377064033654850, 1.527959277978730768 ) ) ;
#102962=ADVANCED_FACE ( 'NONE', ( #78998 ), #178264, .F. ) ;
#102963=CARTESIAN_POINT ( 'NONE',  ( 4.089532599075940134, -0.8378280566024614018, 2.025282237563410526 ) ) ;
#102964=CARTESIAN_POINT ( 'NONE',  ( 5.860475213782774695, 0.9281710514958280145, 2.112872520220021144 ) ) ;
#102965=CARTESIAN_POINT ( 'NONE',  ( 0.7958619820324459582, -0.7424864502722209325, 1.922671381412993652 ) ) ;
#102966=CARTESIAN_POINT ( 'NONE',  ( 3.661996979482002867, -1.303408580024501218, 1.439711300692345652 ) ) ;
#102968=CARTESIAN_POINT ( 'NONE',  ( 5.905500869136258046, -0.4549164269060863020, 1.814235589242949587 ) ) ;
#102972=CARTESIAN_POINT ( 'NONE',  ( 4.570935502227962743, -0.9480417383296577682, 1.779625852769652905 ) ) ;
#102976=CARTESIAN_POINT ( 'NONE',  ( 2.297230901563730665, 1.410920830412419003, 1.158640757216542028 ) ) ;
#102985=CARTESIAN_POINT ( 'NONE',  ( 5.672522982350666432, 0.8204337683548768023, 1.845723718880077469 ) ) ;
#102986=CARTESIAN_POINT ( 'NONE',  ( -0.07530339154229391541, -0.9103892951793614019, -1.913193754492636067 ) ) ;
#102990=CARTESIAN_POINT ( 'NONE',  ( 5.700091634879108859, -2.061077814751426818, -0.002399610236311285148 ) ) ;
#102991=CARTESIAN_POINT ( 'NONE',  ( 4.852185490356213826, 0.1948433276699329531, -2.006959737079899497 ) ) ;
#103001=CARTESIAN_POINT ( 'NONE',  ( 5.659529772124847646, -0.4871306767523299608, -1.956261131662299535 ) ) ;
#103002=CARTESIAN_POINT ( 'NONE',  ( 3.872867692073681756, 1.733033312621637068, -0.6219614626309655225 ) ) ;
#103004=CARTESIAN_POINT ( 'NONE',  ( 2.561488099217507308, -2.008522245525693695, -1.136227173556729975 ) ) ;
#103006=CARTESIAN_POINT ( 'NONE',  ( 5.360679719606757487, -1.569739296358707570, 1.486333574453831297 ) ) ;
#103008=CARTESIAN_POINT ( 'NONE',  ( -0.1235792489666731608, -0.1369701924231395973, -1.910945132828122395 ) ) ;
#103010=CARTESIAN_POINT ( 'NONE',  ( 3.796502476701520301, -2.125173906124724343, 0.8757568767029444423 ) ) ;
#103013=CARTESIAN_POINT ( 'NONE',  ( 2.430351462470367707, 1.813921419787648315, 0.4566771774890953095 ) ) ;
#103015=CARTESIAN_POINT ( 'NONE',  ( 0.2453084554022276487, -1.520975263078115258, -1.253778558530042053 ) ) ;
#103018=CARTESIAN_POINT ( 'NONE',  ( 1.313402753022639091, 1.947697196196996217, 1.037691534346518729 ) ) ;
#103024=CARTESIAN_POINT ( 'NONE',  ( 6.508667090220362716, 1.461156067397894054, -1.323708773930740268 ) ) ;
#103025=CARTESIAN_POINT ( 'NONE',  ( 0.2359759974720798681, -2.107749471535870445, 0.9397143452993106383 ) ) ;
#103026=CARTESIAN_POINT ( 'NONE',  ( 0.8011316787140990714, -1.684513426579350659, 1.005393624328714264 ) ) ;
#103027=CARTESIAN_POINT ( 'NONE',  ( 4.153227615898272163, 1.745077553047107433, -1.099210343703932669 ) ) ;
#103035=CARTESIAN_POINT ( 'NONE',  ( 6.654729725391004713, -0.5723678854598751586, -2.094333189781839355 ) ) ;
#103037=CARTESIAN_POINT ( 'NONE',  ( 5.091278345985558396, -0.6575378499774006125, 1.720029930423284448 ) ) ;
#103038=EDGE_CURVE ( 'NONE', #41277, #176125, #44203, .T. ) ;
#103046=CARTESIAN_POINT ( 'NONE',  ( 0.9614044138335111622, -1.507904615609249488, -1.175938229252027956 ) ) ;
#103047=CARTESIAN_POINT ( 'NONE',  ( 1.568863545881917343, 0.1344791104000986337, -1.764800092583326929 ) ) ;
#103050=CARTESIAN_POINT ( 'NONE',  ( 6.445953599032193004, -1.316566896158730238, -1.522954124987923930 ) ) ;
#103052=CARTESIAN_POINT ( 'NONE',  ( 4.007376490896687571, -1.831982314510060883, 0.5597367571646000295 ) ) ;
#103054=CARTESIAN_POINT ( 'NONE',  ( 5.336368261742150843, -1.095693791129894956, 1.636418990172120003 ) ) ;
#103055=CARTESIAN_POINT ( 'NONE',  ( 6.152604576718359475, 1.998398145963925954, 0.2921455800133450631 ) ) ;
#103057=CARTESIAN_POINT ( 'NONE',  ( 4.030043484472041193, 1.001115284758803625, -1.580040089582811280 ) ) ;
#103058=CARTESIAN_POINT ( 'NONE',  ( 6.094358798449852621, -1.717309950877196956, -0.1615796057152525667 ) ) ;
#103060=CARTESIAN_POINT ( 'NONE',  ( 3.897267319706390065, 1.864829029706360330, -1.179861312946443697 ) ) ;
#103063=CARTESIAN_POINT ( 'NONE',  ( 1.012259994385706019, 2.060384570222949741, -0.09942193159017187476 ) ) ;
#103071=CARTESIAN_POINT ( 'NONE',  ( 3.262232429473245432, -2.068111870375147987, 0.09887451149894616043 ) ) ;
#103075=CARTESIAN_POINT ( 'NONE',  ( 0.6451828087791033894, 0.1507176824743546029, 2.014122433718650296 ) ) ;
#103077=CARTESIAN_POINT ( 'NONE',  ( 0.1747926744264677867, 0.7439089246787933263, -1.939883394317852616 ) ) ;
#103079=CARTESIAN_POINT ( 'NONE',  ( 6.432970213454214381, 1.034009579150240610, 1.730599625746793935 ) ) ;
#103080=CARTESIAN_POINT ( 'NONE',  ( 6.333208386676280277, -1.543085173044305591, -1.135110930932172746 ) ) ;
#103081=CARTESIAN_POINT ( 'NONE',  ( 3.263397454411249399, 2.137687552337414587, -0.4822058812353549606 ) ) ;
#103083=CARTESIAN_POINT ( 'NONE',  ( 2.127084423382288314, 1.709874882824816478, 0.8565708355050825062 ) ) ;
#103087=CARTESIAN_POINT ( 'NONE',  ( 1.019157904985489305, -1.821734318179563106, 0.8647433871810317196 ) ) ;
#103089=CARTESIAN_POINT ( 'NONE',  ( 6.585463931165095985, -0.9389328202267492873, 1.978239266594773671 ) ) ;
#103091=CARTESIAN_POINT ( 'NONE',  ( 3.381609400508314600, 1.093566088711795281, 1.333772831174476758 ) ) ;
#103096=CARTESIAN_POINT ( 'NONE',  ( 1.750371521623844462, -1.952110535733902585, -0.1955497077021361163 ) ) ;
#103099=CARTESIAN_POINT ( 'NONE',  ( 0.1755611466353655115, 0.2306421705509461850, -2.278008211689793061 ) ) ;
#103104=CARTESIAN_POINT ( 'NONE',  ( 3.932113804724958417, -0.9344168170181254007, -1.551720482391373057 ) ) ;
#103108=CARTESIAN_POINT ( 'NONE',  ( 4.723216582411014386, 1.578617123877921857, 0.8883131493910937371 ) ) ;
#103113=EDGE_CURVE ( 'NONE', #87871, #202176, #32760, .T. ) ;
#103114=CARTESIAN_POINT ( 'NONE',  ( 4.844130899818556379, -0.8777628995196519179, 1.641066814073613767 ) ) ;
#103116=CARTESIAN_POINT ( 'NONE',  ( 2.337376834759529398, 0.5087095155123841916, -1.846764813590465515 ) ) ;
#103124=CARTESIAN_POINT ( 'NONE',  ( 0.7969595931820300239, 1.710167217185576183, 1.202247156440580556 ) ) ;
#103126=CARTESIAN_POINT ( 'NONE',  ( 1.324926479183065497, -0.04897172810776688479, 1.825096452545173609 ) ) ;
#103128=CARTESIAN_POINT ( 'NONE',  ( 2.449991753796490368, 1.825138167369045661, 0.04731899098397300552 ) ) ;
#103131=CARTESIAN_POINT ( 'NONE',  ( 2.320441991784210067, -0.7354482596747033973, -1.765520077574176394 ) ) ;
#103132=CARTESIAN_POINT ( 'NONE',  ( 1.715229078707868782, -1.687648322675440626, -1.015142298990583614 ) ) ;
#103133=CARTESIAN_POINT ( 'NONE',  ( 3.983879235506204264, -1.921370479222897165, -0.2818874784011967671 ) ) ;
#103137=CARTESIAN_POINT ( 'NONE',  ( 4.500305224345508393, -0.9970752094022590217, 1.871535012320741265 ) ) ;
#103144=CARTESIAN_POINT ( 'NONE',  ( 3.439906511156048285, 0.8199118703316324863, -1.631291955839441865 ) ) ;
#103149=CARTESIAN_POINT ( 'NONE',  ( 4.891396039733495016, 1.386484060982313249, 1.255958711209571810 ) ) ;
#103151=CARTESIAN_POINT ( 'NONE',  ( 2.701685709380332145, -0.6039436678997743835, 1.829457556829715115 ) ) ;
#103152=CARTESIAN_POINT ( 'NONE',  ( 6.174655700867183405, 1.320063289540554408, -1.451312704123429498 ) ) ;
#103158=CARTESIAN_POINT ( 'NONE',  ( 1.335737955381975928, 0.6106153762303926369, -2.027287256620951439 ) ) ;
#103161=CARTESIAN_POINT ( 'NONE',  ( 6.631696427350994405, 1.982895789845315671, -0.5951614246157420629 ) ) ;
#103162=CARTESIAN_POINT ( 'NONE',  ( 0.6086344939593493208, -0.2706599535906920040, 1.821105742621460744 ) ) ;
#103164=CARTESIAN_POINT ( 'NONE',  ( 0.2811772945982879968, -2.253408246774822210, 0.4517706223704387458 ) ) ;
#103168=CARTESIAN_POINT ( 'NONE',  ( 1.166458296791187621, -1.450650017800562575, 1.774850106915156100 ) ) ;
#103171=CARTESIAN_POINT ( 'NONE',  ( 6.298774621056003831, 1.615917059943820622, 1.076740554856120413 ) ) ;
#103177=CARTESIAN_POINT ( 'NONE',  ( 6.205323455156911194, 1.660478276859885582, -0.9486371710855368011 ) ) ;
#103178=CARTESIAN_POINT ( 'NONE',  ( 6.280482454654814362, -0.5424645211669875122, -1.942098458069536848 ) ) ;
#103183=CARTESIAN_POINT ( 'NONE',  ( 2.695356974763486679, -0.6552250210129506591, 1.985377264055338209 ) ) ;
#103184=CARTESIAN_POINT ( 'NONE',  ( 1.498528727375374459, 1.449451107477307987, -1.015301706168385998 ) ) ;
#103186=CARTESIAN_POINT ( 'NONE',  ( 4.259948577007838466, 1.078808246893525391, 2.022540810160260882 ) ) ;
#103187=CARTESIAN_POINT ( 'NONE',  ( 3.187183321348503018, -0.7043554338151243321, 1.591608241653941214 ) ) ;
#103190=CARTESIAN_POINT ( 'NONE',  ( 3.198323437492247123, -1.162659817912135019, -1.286436312214979338 ) ) ;
#103191=CARTESIAN_POINT ( 'NONE',  ( 3.649033395009869452, -0.4203537998966280220, -2.129940419224036763 ) ) ;
#103193=CARTESIAN_POINT ( 'NONE',  ( 4.962125165302472496, -1.116212726388360998, 1.679221540125563905 ) ) ;
#103194=CARTESIAN_POINT ( 'NONE',  ( 1.625000000000001554, -2.052068128417951165, 9.007296548519099900E-14 ) ) ;
#103197=CARTESIAN_POINT ( 'NONE',  ( 1.571183270939533694, 0.1444824169965253369, -1.921038573443895059 ) ) ;
#103199=CARTESIAN_POINT ( 'NONE',  ( 4.166425639909420831, 2.220860392705526820, -0.05667459126444325535 ) ) ;
#103201=CARTESIAN_POINT ( 'NONE',  ( -0.1106856583841424602, 0.7110496148716296538, -2.078439740052108853 ) ) ;
#103206=CARTESIAN_POINT ( 'NONE',  ( 0.3467151180503316166, 1.136585144892443777, -1.908366640695156047 ) ) ;
#103207=CARTESIAN_POINT ( 'NONE',  ( 5.512146440779991607, 1.959692598237902761, -0.09458084330612320789 ) ) ;
#103210=CARTESIAN_POINT ( 'NONE',  ( 0.4917760118960182170, 1.601382895956671826, 1.452064325093614716 ) ) ;
#103215=CARTESIAN_POINT ( 'NONE',  ( 2.910651161647914265, 0.6924047515337331538, 1.943132885215630878 ) ) ;
#103219=CARTESIAN_POINT ( 'NONE',  ( 5.061713478001653499, 1.850364105758989020, -0.2730526881008291662 ) ) ;
#103220=CARTESIAN_POINT ( 'NONE',  ( 4.078545790824074757, -0.6587176911285116399, 1.604389539659875297 ) ) ;
#103221=CARTESIAN_POINT ( 'NONE',  ( 3.262975863287612466, 1.697222826579761534, -0.3846178214849705901 ) ) ;
#103223=CARTESIAN_POINT ( 'NONE',  ( 0.2227793574855509162, 2.196107815404338748, 0.6574155683778097892 ) ) ;
#103225=CARTESIAN_POINT ( 'NONE',  ( 6.093324021728765416, -0.7037842761165017391, 1.968882989559454622 ) ) ;
#103226=CARTESIAN_POINT ( 'NONE',  ( -0.02968770228140016343, 0.003472272166151618711, -1.826291111852257343 ) ) ;
#103228=CARTESIAN_POINT ( 'NONE',  ( 1.846327496167538884, 0.3419342931599393398, -1.987046799686801757 ) ) ;
#103229=CARTESIAN_POINT ( 'NONE',  ( 0.1995291103054769866, -0.5802879427523646161, 2.113158525371459096 ) ) ;
#103233=CARTESIAN_POINT ( 'NONE',  ( 2.614065066921432479, -0.6628553294307990562, 2.014303955012682223 ) ) ;
#103235=CARTESIAN_POINT ( 'NONE',  ( 5.039593146249602640, -1.293522693445446015, -1.288650932716684849 ) ) ;
#103243=CARTESIAN_POINT ( 'NONE',  ( 2.390883991616198578, -1.934022345091526818, -0.5824046739145176677 ) ) ;
#103244=CARTESIAN_POINT ( 'NONE',  ( 0.2004011508093841987, -2.105512755765154509, -0.05116925900590372361 ) ) ;
#103246=CARTESIAN_POINT ( 'NONE',  ( 4.592532296707762640, 1.824399381888962779, 0.3660411688805977337 ) ) ;
#103251=CARTESIAN_POINT ( 'NONE',  ( 4.934128534657983067, 0.9357288403324083292, -1.567518238613223813 ) ) ;
#103255=CARTESIAN_POINT ( 'NONE',  ( 2.143477642578191844, -0.07974179160761747653, -1.732128062886995057 ) ) ;
#103256=CARTESIAN_POINT ( 'NONE',  ( 6.404252597826388893, 1.360807738692754176, -1.240355271200761278 ) ) ;
#103257=CARTESIAN_POINT ( 'NONE',  ( 5.057380973065424001, -1.947307563149714316, -1.238062830034118988 ) ) ;
#103260=CARTESIAN_POINT ( 'NONE',  ( 1.089218918643636069, 1.818803954151678726, -0.9688405272365168130 ) ) ;
#103262=CARTESIAN_POINT ( 'NONE',  ( 0.3860920070548681804, -0.1017387759476989784, 2.013677428805898728 ) ) ;
#103266=CARTESIAN_POINT ( 'NONE',  ( 0.4441303031895106890, 1.966005183986684335, 0.1476035654904006011 ) ) ;
#103267=CARTESIAN_POINT ( 'NONE',  ( 3.779479514802902340, 0.2291398179169491789, -1.898525689255560422 ) ) ;
#103269=CARTESIAN_POINT ( 'NONE',  ( 4.635508124736155366, -2.018492079602551392, 0.8926152185086615454 ) ) ;
#103273=CARTESIAN_POINT ( 'NONE',  ( 6.252600707356171128, 2.097339953035493476, 0.3115551810550786227 ) ) ;
#103275=CARTESIAN_POINT ( 'NONE',  ( 3.804037270277782490, -0.6727452520632947186, 2.207335857111696331 ) ) ;
#103276=CARTESIAN_POINT ( 'NONE',  ( 3.578520225191741844, 1.246510459297203610, -1.514941731618473009 ) ) ;
#103278=CARTESIAN_POINT ( 'NONE',  ( 1.024179675629211861, 0.9620134025654383247, 1.709582039726687652 ) ) ;
#103282=CARTESIAN_POINT ( 'NONE',  ( 5.893767612163585135, -2.000732204962274441, 0.2516274335107801519 ) ) ;
#103285=CARTESIAN_POINT ( 'NONE',  ( 3.168971741543443077, 1.575705016696099081, -1.493804678357780524 ) ) ;
#103287=CARTESIAN_POINT ( 'NONE',  ( 0.4398875993102538962, -2.011672884243600024, 0.6710486789910232730 ) ) ;
#103293=CARTESIAN_POINT ( 'NONE',  ( 1.229839986812499175, -1.305282058118014010, -1.594721697489847045 ) ) ;
#103297=DIRECTION ( 'NONE',  ( 2.949029909160572061E-17, 1.000000000000000000, -8.673600428462353400E-15 ) ) ;
#103299=CARTESIAN_POINT ( 'NONE',  ( 4.248624793116656306, 1.876006594227698221, 0.3698101955103145766 ) ) ;
#103302=CARTESIAN_POINT ( 'NONE',  ( 0.2283786121510515688, 1.249231189971045319, -1.312217732533569103 ) ) ;
#103304=CARTESIAN_POINT ( 'NONE',  ( 0.2861690844194793026, -0.6482510287857257136, -1.802810126718904504 ) ) ;
#103306=CARTESIAN_POINT ( 'NONE',  ( 2.102089431743926706, 0.7944251937819692966, -1.912079865474418439 ) ) ;
#103308=CARTESIAN_POINT ( 'NONE',  ( 1.024223545076022424, 1.176019522272594875, -1.582147633265261977 ) ) ;
#103309=CARTESIAN_POINT ( 'NONE',  ( 2.947667120405720986, 0.6567698719579934119, -1.703645827024417914 ) ) ;
#103310=CARTESIAN_POINT ( 'NONE',  ( 6.393228082638676923, 1.922373441260841087, -1.083778638264052852 ) ) ;
#103313=CARTESIAN_POINT ( 'NONE',  ( 4.158677964895734824, -0.6440432224011168882, -1.959637643944433849 ) ) ;
#103318=CARTESIAN_POINT ( 'NONE',  ( 4.893641883129576264, 1.558557130586870398, 1.416501212539149845 ) ) ;
#103320=CARTESIAN_POINT ( 'NONE',  ( 6.162566008723842081, -0.7415158119226210598, -1.933206815039355320 ) ) ;
#103322=CARTESIAN_POINT ( 'NONE',  ( 3.286554482555790191, -2.129011082553730727, -0.3730605165198074280 ) ) ;
#103323=CARTESIAN_POINT ( 'NONE',  ( 3.844402842710480162, 1.078523329768014349, -1.707388236230653611 ) ) ;
#103324=CARTESIAN_POINT ( 'NONE',  ( 6.620655732516679493, 7.051632961313193171, 2.871890384929445261 ) ) ;
#103329=CARTESIAN_POINT ( 'NONE',  ( 2.835173002801576914, -1.651343842416473917, -1.157098616274463865 ) ) ;
#103337=CARTESIAN_POINT ( 'NONE',  ( 4.464470365011488973, -1.956567236562205325, -0.4871837624095613495 ) ) ;
#103339=CARTESIAN_POINT ( 'NONE',  ( 6.475633750228043439, 1.648727237068832396, -0.5065655092456061714 ) ) ;
#103344=CARTESIAN_POINT ( 'NONE',  ( 5.676977070516882051, -0.04517083460114229565, -1.870152005306220611 ) ) ;
#103345=CARTESIAN_POINT ( 'NONE',  ( 0.1354021741525688050, -0.09674683032310191222, 2.010873914455484801 ) ) ;
#103351=CARTESIAN_POINT ( 'NONE',  ( 0.8609541034889022226, -0.05231784723681161264, -2.015913592316537439 ) ) ;
#103352=CARTESIAN_POINT ( 'NONE',  ( 0.9491188979427627181, -1.637284982186116400, 0.7756696494297130595 ) ) ;
#103360=CARTESIAN_POINT ( 'NONE',  ( 5.870691181925934643, -0.2860506952705432204, -1.894010149965511758 ) ) ;
#103367=CARTESIAN_POINT ( 'NONE',  ( 3.625982885822197410, -1.285997354380935098, -1.737435825693342872 ) ) ;
#103370=CARTESIAN_POINT ( 'NONE',  ( 0.7914572142167939361, -0.05789999323873443182, -2.119991495365561640 ) ) ;
#103371=CARTESIAN_POINT ( 'NONE',  ( 5.807590115592688562, -0.4411735188285180187, 1.771332044933016547 ) ) ;
#103373=CARTESIAN_POINT ( 'NONE',  ( 2.319545460040703500, -1.913138470506670075, 0.4751570986292509846 ) ) ;
#103374=CARTESIAN_POINT ( 'NONE',  ( 4.658414424252744546, 1.907665749568526747, 0.1350064596054162680 ) ) ;
#103377=CARTESIAN_POINT ( 'NONE',  ( 5.740667673349629574, -1.921128208576441843, -0.4332487841941043971 ) ) ;
#103378=CARTESIAN_POINT ( 'NONE',  ( 0.2517628464389579102, 0.7423079377118102506, 1.794666626680625932 ) ) ;
#103384=CARTESIAN_POINT ( 'NONE',  ( 4.529883686416775745, -1.874680353417649492, 0.3764776581506729114 ) ) ;
#103386=CARTESIAN_POINT ( 'NONE',  ( 0.3236265600991515834, -0.1057403636935544400, 2.204373366691187108 ) ) ;
#103389=CARTESIAN_POINT ( 'NONE',  ( 5.936195100277483760, -1.120233448768311435, -1.672418650214458014 ) ) ;
#103390=CARTESIAN_POINT ( 'NONE',  ( 0.07680821025391781909, 4.096870002413341538, -2.365840309731046975 ) ) ;
#103393=CARTESIAN_POINT ( 'NONE',  ( 2.945825538390863141, 1.462269270728074222, 1.465923284304726959 ) ) ;
#103396=B_SPLINE_CURVE_WITH_KNOTS ( 'NONE', 3,
 ( #148636, #108996, #192286, #59103, #10342, #110062, #175013, #191223, #49009, #65219, #82549 ),
 .UNSPECIFIED., .F., .F.,
 ( 4, 1, 1, 1, 1, 1, 1, 1, 4 ),
 ( 0.000000000000000000, 0.2255509035172358623, 0.3975895543896152406, 0.5252637114030099807, 0.6177357421269481508, 0.6841390318922365710, 0.7334310489036851566, 0.7741974304450970346, 1.000000000000000000 ),
 .UNSPECIFIED. ) ;
#103398=CARTESIAN_POINT ( 'NONE',  ( 1.006953172832128152, 1.636353683469338183, -1.412668763314451903 ) ) ;
#103403=CARTESIAN_POINT ( 'NONE',  ( 6.825078400183510752, 3.697836898538444217, 2.470016017273040543 ) ) ;
#103405=CARTESIAN_POINT ( 'NONE',  ( 2.624232735793774030, 2.001858099149746550, 0.2420302859193757539 ) ) ;
#103406=CARTESIAN_POINT ( 'NONE',  ( 6.117740286212093537, 0.1793736470585994280, 1.724862758254825712 ) ) ;
#103408=CARTESIAN_POINT ( 'NONE',  ( 3.204029340230400091, 0.7494766052340908757, -1.929994576353490032 ) ) ;
#103409=CARTESIAN_POINT ( 'NONE',  ( 4.640305734921336800, 0.8116497034467985427, 1.955664341570842790 ) ) ;
#103412=CARTESIAN_POINT ( 'NONE',  ( 3.326963294591319009, -1.817917149290064982, -0.7580491890798303212 ) ) ;
#103414=CARTESIAN_POINT ( 'NONE',  ( 0.8789968191965717992, -1.730013457311157188, -0.8152767527440167861 ) ) ;
#103415=CARTESIAN_POINT ( 'NONE',  ( 4.506013928309719141, -0.9778350203078637337, -2.073373472838499598 ) ) ;
#103416=CARTESIAN_POINT ( 'NONE',  ( 3.264084022359412973, 0.8216391472936384055, 1.630427331384459055 ) ) ;
#103420=CARTESIAN_POINT ( 'NONE',  ( 4.218997895827368616, 1.553599190986540091, -1.280318274872578543 ) ) ;
#103421=CARTESIAN_POINT ( 'NONE',  ( 2.729291793292155432, 0.1011638768560127188, -1.959297240552673181 ) ) ;
#103425=CARTESIAN_POINT ( 'NONE',  ( 6.333939708931282553, 2.067699390258682879, 0.3079354192142729763 ) ) ;
#103426=CARTESIAN_POINT ( 'NONE',  ( 5.049538948550310380, 0.5532318831848512808, -1.681206329525422483 ) ) ;
#103428=CARTESIAN_POINT ( 'NONE',  ( 1.218978173989828884, -0.05078841826402366588, 2.191026318449231791 ) ) ;
#103429=CARTESIAN_POINT ( 'NONE',  ( 6.703062861115646420, -0.3699031437116198084, 1.706546720392573491 ) ) ;
#103432=CARTESIAN_POINT ( 'NONE',  ( 0.1331715793776652446, 7.629137130509056952, -2.553547540661147419 ) ) ;
#103433=CARTESIAN_POINT ( 'NONE',  ( 0.6678281019706671096, -0.7765434158916887375, -2.163364592831273470 ) ) ;
#103434=CARTESIAN_POINT ( 'NONE',  ( 0.1170720436180875679, -0.1011795954627830590, 2.189343785608413917 ) ) ;
#103435=CARTESIAN_POINT ( 'NONE',  ( 6.696678128945787734, -1.136521523357211017, -1.309519827187540564 ) ) ;
#103436=CARTESIAN_POINT ( 'NONE',  ( 3.282038605231399231, 1.400092287458438722, 1.705885466304429166 ) ) ;
#103437=CARTESIAN_POINT ( 'NONE',  ( 6.443812750726708671, 1.492410320797844747, 1.577172898185905670 ) ) ;
#103439=CARTESIAN_POINT ( 'NONE',  ( 1.393934723748765814, -2.100642827862955198, 0.2651745403093440090 ) ) ;
#103440=CARTESIAN_POINT ( 'NONE',  ( 4.343750000000002665, 1.895863743164175608, 0.7852924748297558377 ) ) ;
#103441=CARTESIAN_POINT ( 'NONE',  ( 6.620655732516651071, 2.021119449029490589, 2.477762541108457839 ) ) ;
#103442=CARTESIAN_POINT ( 'NONE',  ( 4.946275538936047766, 1.921213873770099445, 0.1421515328255736899 ) ) ;
#103445=CARTESIAN_POINT ( 'NONE',  ( 1.646416196899816997, 0.7239943723881783200, 2.175097950400638691 ) ) ;
#103449=CARTESIAN_POINT ( 'NONE',  ( 3.633611385093922674, -0.1624337102359394436, 2.215399726503309630 ) ) ;
#103455=CARTESIAN_POINT ( 'NONE',  ( 2.092422861153935276, -0.4390285686692517175, 1.967888031366466395 ) ) ;
#103457=CARTESIAN_POINT ( 'NONE',  ( 6.707491137888100141, -1.654371308887558234, -1.231747576844913539 ) ) ;
#103460=CARTESIAN_POINT ( 'NONE',  ( 6.427322163675834865, -1.144589508088897478, -1.311236935029986173 ) ) ;
#103463=CARTESIAN_POINT ( 'NONE',  ( 2.881836681058600913, -0.9132262334808398663, 1.515770159524139515 ) ) ;
#103464=CARTESIAN_POINT ( 'NONE',  ( 1.108046318188542489, -0.04667474159409169127, 2.016033875899234662 ) ) ;
#103465=CARTESIAN_POINT ( 'NONE',  ( 6.614805129994690169, -0.1227637983064084892, 1.711830280531308812 ) ) ;
#103466=CARTESIAN_POINT ( 'NONE',  ( 5.548434679399758984, -1.809038938731177160, 1.407827746306972827 ) ) ;
#103467=CARTESIAN_POINT ( 'NONE',  ( 2.906014618889842360, 1.333239036598636407, -1.269987479889053139 ) ) ;
#103469=CARTESIAN_POINT ( 'NONE',  ( 3.610199614654508338, -0.7391254383575728282, -1.669438027971142047 ) ) ;
#103470=CARTESIAN_POINT ( 'NONE',  ( 5.063125043234593115, -1.117834493326537393, 1.678003986596336761 ) ) ;
#103472=CARTESIAN_POINT ( 'NONE',  ( 3.028476438156304962, 1.258033425225786983, -1.880328901638250505 ) ) ;
#103474=CARTESIAN_POINT ( 'NONE',  ( -0.01685825368398767912, -0.1589125243241385210, -2.071875930555002743 ) ) ;
#103476=CARTESIAN_POINT ( 'NONE',  ( 4.035645461687249913, 1.950487776689105557, -0.6946759356915442885 ) ) ;
#103479=CARTESIAN_POINT ( 'NONE',  ( 6.270199134133584096, 2.114857618286110075, -0.1555134818699495936 ) ) ;
#103482=CARTESIAN_POINT ( 'NONE',  ( 2.086434564137104264, -1.889293373815591481, -0.3759864732829041878 ) ) ;
#103486=CARTESIAN_POINT ( 'NONE',  ( 0.4847283499135228713, 1.883623918205453718, 0.5753430019505183513 ) ) ;
#103491=CARTESIAN_POINT ( 'NONE',  ( 0.1236698368150884464, 1.936885272324913698, 1.087587522935773876 ) ) ;
#103492=CARTESIAN_POINT ( 'NONE',  ( 3.575310672209235374, 0.05349853608750848588, -2.105455972502618955 ) ) ;
#103495=CARTESIAN_POINT ( 'NONE',  ( 0.7657746542184565852, -1.852627923093919771, 0.1767624929009704582 ) ) ;
#103501=CARTESIAN_POINT ( 'NONE',  ( 1.512141599020993432, -0.7094941370262074498, 1.998545949238240027 ) ) ;
#103504=CARTESIAN_POINT ( 'NONE',  ( 4.580490334204036174, 1.208584658811951762, -1.545285769342201965 ) ) ;
#103505=CARTESIAN_POINT ( 'NONE',  ( 1.815512348505427642, -0.2646426633909418347, 2.145385951886819242 ) ) ;
#103506=CARTESIAN_POINT ( 'NONE',  ( 1.821575194732877545, 1.059174331173462935, -1.505913648122420900 ) ) ;
#103510=CARTESIAN_POINT ( 'NONE',  ( 3.275097224137039742, 1.105054647683247460, 1.344453793780414186 ) ) ;
#103514=CARTESIAN_POINT ( 'NONE',  ( 0.4093245661422850734, 1.881582470445356314, 1.064130679222355491 ) ) ;
#103515=CARTESIAN_POINT ( 'NONE',  ( 2.864611068004913275, -0.6351033500862738324, 1.913510180259501592 ) ) ;
#103517=CARTESIAN_POINT ( 'NONE',  ( 0.3214396764580421118, -0.1044536432763705502, 2.159311484102262479 ) ) ;
#103519=CARTESIAN_POINT ( 'NONE',  ( 3.274254179156810274, -1.175395456433829144, 1.582609504276990320 ) ) ;
#103521=CARTESIAN_POINT ( 'NONE',  ( 2.155715342533376155, 0.8324662149039625536, 1.754741561904197056 ) ) ;
#103523=ORIENTED_EDGE ( 'NONE', *, *, #60102, .F. ) ;
#103525=CARTESIAN_POINT ( 'NONE',  ( -0.2106854629475270468, 2.024676876401194203, -2.413177685601196831 ) ) ;
#103531=CARTESIAN_POINT ( 'NONE',  ( 0.2533207856364183552, -1.770817270756098960, 1.316655756711228253 ) ) ;
#103533=CARTESIAN_POINT ( 'NONE',  ( 4.487127722112081329, 0.09209952633786910869, 1.959694304038139379 ) ) ;
#103535=CARTESIAN_POINT ( 'NONE',  ( 1.951796282902381163, -1.844710420878793444, -0.8146254186931353169 ) ) ;
#103537=CARTESIAN_POINT ( 'NONE',  ( 2.483745868283081748, -0.6592627125163934565, 2.012192174959149149 ) ) ;
#103540=CARTESIAN_POINT ( 'NONE',  ( 3.573999110145977820, -1.774750109099573869, -0.4897004633943187191 ) ) ;
#103544=CARTESIAN_POINT ( 'NONE',  ( 4.078469121099765005, 1.002472831208834680, 1.868716877859360137 ) ) ;
#103547=CARTESIAN_POINT ( 'NONE',  ( 6.011025214932095295, 1.815421535059216662, 0.9752673143463059802 ) ) ;
#103550=CARTESIAN_POINT ( 'NONE',  ( 2.050122339901743196, -1.422379512129726908, 1.169167124061460949 ) ) ;
#103556=CARTESIAN_POINT ( 'NONE',  ( 2.262606014870732096, 0.9450075053254001212, 1.994452002680577429 ) ) ;
#103557=CARTESIAN_POINT ( 'NONE',  ( 3.761208288054026738, -1.993080904335465142, -1.070619287061522318 ) ) ;
#103559=CARTESIAN_POINT ( 'NONE',  ( 3.673895663291579350, 1.797233291820631962, -0.2271657407440821064 ) ) ;
#103560=CARTESIAN_POINT ( 'NONE',  ( 4.610495038435900916, 1.835019742331613690, 0.5502660077172877306 ) ) ;
#103562=CARTESIAN_POINT ( 'NONE',  ( 4.100430126988792168, -0.6171887515804741486, -1.872443122656509029 ) ) ;
#103563=CARTESIAN_POINT ( 'NONE',  ( 1.325083149161108365, -0.05013198271685941065, 1.925904219417676089 ) ) ;
#103564=CARTESIAN_POINT ( 'NONE',  ( 5.436355746168001879, 1.843147576875401983, 0.3187000444574567548 ) ) ;
#103566=CARTESIAN_POINT ( 'NONE',  ( 3.246982502279437188, 0.5605648102574630753, 2.238460633888791573 ) ) ;
#103567=CARTESIAN_POINT ( 'NONE',  ( 4.457361271359429722, 1.493968932455931542, 1.109517434556703597 ) ) ;
#103569=CARTESIAN_POINT ( 'NONE',  ( 0.3390778084843976137, -1.706115258973059490, -1.074657883261991076 ) ) ;
#103572=CARTESIAN_POINT ( 'NONE',  ( 1.770285920821415449, 1.083698108115097591, 1.805711900068427411 ) ) ;
#103576=CARTESIAN_POINT ( 'NONE',  ( 2.760144723603759065, 0.7592700852765141839, -1.980205354017528840 ) ) ;
#103578=CARTESIAN_POINT ( 'NONE',  ( 0.6682303662221461549, 2.017294962401328107, -0.1032846847020176678 ) ) ;
#103582=ORIENTED_EDGE ( 'NONE', *, *, #17999, .F. ) ;
#103583=CARTESIAN_POINT ( 'NONE',  ( 2.354944161360218224, -1.672559397656541824, 1.369352967626968898 ) ) ;
#103589=CARTESIAN_POINT ( 'NONE',  ( 5.770720322323381168, -0.3006437417610394736, -1.993894057904864514 ) ) ;
#103591=CARTESIAN_POINT ( 'NONE',  ( 0.1346727191937693857, 0.3808678606769915209, 2.158067550307264604 ) ) ;
#103593=CARTESIAN_POINT ( 'NONE',  ( 0.3919815047150644327, 1.678997099660347603, 1.516718289441946199 ) ) ;
#103599=CARTESIAN_POINT ( 'NONE',  ( 4.037519343584392573, -1.191552764850771995, -1.247402213628981293 ) ) ;
#103601=( BOUNDED_SURFACE ( )  B_SPLINE_SURFACE ( 3, 3, ( 
 ( #96084, #32126, #115560, #14786, #146967, #145911, #178388, #181556, #99266, #179452, #128650 ),
 ( #165314, #162138, #182619, #149064, #80877, #132851, #31075, #116625, #150148, #64622, #97149 ),
 ( #1718, #39579, #4905, #68853, #21161, #87265, #101377, #38517, #120912, #168511, #67775 ),
 ( #153331, #5982, #121985, #151212, #2782, #36368, #152269, #154404, #186885, #187951, #51577 ),
 ( #20111, #55829, #105681, #134973, #104595, #185810, #72053, #117702, #102445, #170641, #23307 ),
 ( #138165, #70982, #52628, #183693, #118756, #204172, #200981, #171710, #86197, #136025, #167452 ),
 ( #137095, #3841, #69914, #202038, #169578, #89418, #22226, #203121, #37442, #155467, #35300 ) ),
 .UNSPECIFIED., .T., .F., .T. ) 
 B_SPLINE_SURFACE_WITH_KNOTS ( ( 4, 3, 4 ),
 ( 4, 1, 1, 1, 1, 1, 1, 1, 4 ),
 ( 0.000000000000000000, 0.5000000000000000000, 1.000000000000000000 ),
 ( 0.000000000000000000, 0.2256085737580844630, 0.3975982043691296264, 0.5251069566405043298, 0.6172860083021659561, 0.6832860984239963464, 0.7321959383537668398, 0.7728624839797392232, 1.000000000000000000 ),
 .UNSPECIFIED. ) 
 GEOMETRIC_REPRESENTATION_ITEM ( )  RATIONAL_B_SPLINE_SURFACE ( (
 ( 1.000000000000000222, 1.000000000000000222, 1.000000000000000444, 0.9999999999999996669, 1.000000000000000444, 0.9999999999999997780, 1.000000000000000222, 1.000000000000000222, 0.9999999999999996669, 1.000000000000000000, 1.000000000000000000),
 ( 0.3333333333333334259, 0.3333333333333334259, 0.3333333333333334259, 0.3333333333333333703, 0.3333333333333334259, 0.3333333333333333148, 0.3333333333333334814, 0.3333333333333334259, 0.3333333333333331483, 0.3333333333333334259, 0.3333333333333333703),
 ( 0.3333333333333334259, 0.3333333333333334259, 0.3333333333333334259, 0.3333333333333333703, 0.3333333333333334259, 0.3333333333333333148, 0.3333333333333334814, 0.3333333333333334259, 0.3333333333333331483, 0.3333333333333334259, 0.3333333333333333703),
 ( 1.000000000000000222, 1.000000000000000222, 1.000000000000000444, 0.9999999999999996669, 1.000000000000000444, 0.9999999999999997780, 1.000000000000000222, 1.000000000000000222, 0.9999999999999996669, 1.000000000000000000, 1.000000000000000000),
 ( 0.3333333333333334259, 0.3333333333333334259, 0.3333333333333334259, 0.3333333333333333703, 0.3333333333333334259, 0.3333333333333333148, 0.3333333333333334814, 0.3333333333333334259, 0.3333333333333331483, 0.3333333333333334259, 0.3333333333333333703),
 ( 0.3333333333333334259, 0.3333333333333334259, 0.3333333333333334259, 0.3333333333333333703, 0.3333333333333334259, 0.3333333333333333148, 0.3333333333333334814, 0.3333333333333334259, 0.3333333333333331483, 0.3333333333333334259, 0.3333333333333333703),
 ( 1.000000000000000222, 1.000000000000000222, 1.000000000000000444, 0.9999999999999996669, 1.000000000000000444, 0.9999999999999997780, 1.000000000000000222, 1.000000000000000222, 0.9999999999999996669, 1.000000000000000000, 1.000000000000000000) ) ) 
 REPRESENTATION_ITEM ( '' )  SURFACE ( )  );
#103602=CARTESIAN_POINT ( 'NONE',  ( 2.073191327021279839, 1.695144128639828551, -0.5084401619379045334 ) ) ;
#103603=CARTESIAN_POINT ( 'NONE',  ( 2.684242053459008570, 1.078846248543659403, 1.699430804756915547 ) ) ;
#103605=CARTESIAN_POINT ( 'NONE',  ( 4.770673279661371780, -1.444480529215144804, 1.668407551275403300 ) ) ;
#103607=CARTESIAN_POINT ( 'NONE',  ( 4.623309962349557267, 1.759429041943610716, 0.9917458525283324722 ) ) ;
#103609=CARTESIAN_POINT ( 'NONE',  ( 4.442108405842562391, -1.305342523080333272, -1.670987904322115636 ) ) ;
#103610=CARTESIAN_POINT ( 'NONE',  ( 4.253529916566947122, 1.955168710539030075, -0.4926619687581067497 ) ) ;
#103611=CARTESIAN_POINT ( 'NONE',  ( 4.324329094900294379, -0.7804802743817635946, -1.635003121989448971 ) ) ;
#103617=CARTESIAN_POINT ( 'NONE',  ( 0.9888773766892228201, 1.651582696977690112, -0.8784067438419728147 ) ) ;
#103619=CARTESIAN_POINT ( 'NONE',  ( 5.865820270629499511, 0.5193939906856791522, -1.735422816724658146 ) ) ;
#103627=CARTESIAN_POINT ( 'NONE',  ( 1.803102349535959714, -1.659081995624330563, 1.046767247423967095 ) ) ;
#103630=CARTESIAN_POINT ( 'NONE',  ( 3.709332143218791789, 1.789599998243587731, -1.137392358348317201 ) ) ;
#103633=CARTESIAN_POINT ( 'NONE',  ( 5.009034487593355678, 1.713717141372484765, 0.9743026824079579207 ) ) ;
#103635=CARTESIAN_POINT ( 'NONE',  ( 1.213140692357208117, 1.643459361250454442, -1.162501220127802437 ) ) ;
#103637=CARTESIAN_POINT ( 'NONE',  ( 0.8611331728165865229, -0.05642918589183294059, -2.116647836221299261 ) ) ;
#103639=CARTESIAN_POINT ( 'NONE',  ( 2.647004975520852454, -0.3514972095969396970, -2.040143077068845123 ) ) ;
#103644=CARTESIAN_POINT ( 'NONE',  ( 5.138659532522440010, -1.793477146331866612, 1.074093663348500760 ) ) ;
#103646=CARTESIAN_POINT ( 'NONE',  ( 3.258640109524315154, -1.383274205585843797, 1.191454006006509303 ) ) ;
#103647=CARTESIAN_POINT ( 'NONE',  ( 2.086290463123147365, -1.113812826415590651, 1.428500571052490953 ) ) ;
#103650=CARTESIAN_POINT ( 'NONE',  ( 6.393228082638676923, 1.922373441260841087, -1.083778638264052852 ) ) ;
#103652=CARTESIAN_POINT ( 'NONE',  ( 4.401547605996741552, 1.770323140634282311, 1.317293360403009927 ) ) ;
#103655=CARTESIAN_POINT ( 'NONE',  ( 3.668532269402470458, 0.6909111621477401766, 1.783275653667259597 ) ) ;
#103660=CARTESIAN_POINT ( 'NONE',  ( 6.461392557816405535, 1.719054114842766268, 1.153505076091146275 ) ) ;
#103662=ADVANCED_FACE ( 'NONE', ( #108129 ), #8052, .T. ) ;
#103663=CARTESIAN_POINT ( 'NONE',  ( 6.444889499930222421, -1.758869480593090673, -1.307235502039267860 ) ) ;
#103669=CARTESIAN_POINT ( 'NONE',  ( 4.147608549738549755, 0.6325110726591240962, -1.760471310998643402 ) ) ;
#103674=CARTESIAN_POINT ( 'NONE',  ( 0.3737962156708526384, -1.932529848913757897, 0.3785758322861746406 ) ) ;
#103676=CARTESIAN_POINT ( 'NONE',  ( 1.458611474731505986, -1.915607644094442064, -0.6298556652749932594 ) ) ;
#103680=CARTESIAN_POINT ( 'NONE',  ( 1.482659311839970684, -0.3241159351022730450, -2.167229700873399612 ) ) ;
#103687=CARTESIAN_POINT ( 'NONE',  ( 4.317794123949899365, 1.129187743159822288, -1.454283868005897151 ) ) ;
#103688=CARTESIAN_POINT ( 'NONE',  ( 0.5045416345675997061, -1.998124945550180609, -0.2444111669489754113 ) ) ;
#103689=CARTESIAN_POINT ( 'NONE',  ( 2.478211020838327894, 2.052291828077044133, 1.034905392717075046 ) ) ;
#103691=CARTESIAN_POINT ( 'NONE',  ( 6.104347744599991188, 1.959368324604572775, 0.09974838594294095639 ) ) ;
#103694=CARTESIAN_POINT ( 'NONE',  ( 4.693567934957057375, 1.782326746607498791, -0.6936623114904352239 ) ) ;
#103698=CARTESIAN_POINT ( 'NONE',  ( 2.296528860280427686, 1.677371239548936854, -1.247825592998616617 ) ) ;
#103699=CARTESIAN_POINT ( 'NONE',  ( 1.955717210371358483, 1.865846021326333926, -0.1348392221205765851 ) ) ;
#103702=CARTESIAN_POINT ( 'NONE',  ( 2.946521060880839205, -1.424341091986385921, -0.9998927444686573907 ) ) ;
#103706=CARTESIAN_POINT ( 'NONE',  ( 3.492533829797561218, -0.3379890457658150105, -1.691244694301207829 ) ) ;
#103707=CARTESIAN_POINT ( 'NONE',  ( 3.966501855323391723, -2.045284974426237579, -0.7877190255709336508 ) ) ;
#103708=CARTESIAN_POINT ( 'NONE',  ( 5.901041445831936016, 1.806360628843254768, -1.267562117129708232 ) ) ;
#103710=CARTESIAN_POINT ( 'NONE',  ( 3.502934933135398055, 0.5226102428602089622, 2.107139934106997181 ) ) ;
#103711=CARTESIAN_POINT ( 'NONE',  ( 2.367563199519676420, 1.790531440309536926, -0.3556685536310541518 ) ) ;
#103713=CARTESIAN_POINT ( 'NONE',  ( 4.997310516409209313, -0.3076690597460414733, 2.094731796426703152 ) ) ;
#103714=EDGE_LOOP ( 'NONE', ( #176698, #109045, #72848, #175746 ) ) ;
#103715=CARTESIAN_POINT ( 'NONE',  ( 5.144168085839278426, 0.6632553684719083575, 2.194301386939989218 ) ) ;
#103717=CARTESIAN_POINT ( 'NONE',  ( 6.720655732516671144, 1.288224904612661925, 1.942155157606942240 ) ) ;
#103719=CARTESIAN_POINT ( 'NONE',  ( 0.3992906662320141464, -0.2637550127744873185, -2.103967267096308991 ) ) ;
#103724=CARTESIAN_POINT ( 'NONE',  ( 6.883263157960376688, 2.059069814638575302, 2.260828084523508252 ) ) ;
#103727=CARTESIAN_POINT ( 'NONE',  ( 4.940077362011475515, -1.704937458037486531, -1.076318853994034930 ) ) ;
#103729=CARTESIAN_POINT ( 'NONE',  ( 4.522371018022923295, 0.9678747400500853360, 1.821345444039919270 ) ) ;
#103731=CARTESIAN_POINT ( 'NONE',  ( -0.2409995289980246258, 7.629137130509076492, -2.600476469121239198 ) ) ;
#103735=CARTESIAN_POINT ( 'NONE',  ( 1.007895156502825573, -0.9414231642565270564, -1.866751856443664037 ) ) ;
#103736=CARTESIAN_POINT ( 'NONE',  ( 4.535779832184696936, -1.617819081767550182, 1.203352566194588746 ) ) ;
#103737=CARTESIAN_POINT ( 'NONE',  ( 2.911469271472226339, -0.9098125248445630975, -1.600700954789348263 ) ) ;
#103740=CARTESIAN_POINT ( 'NONE',  ( 0.3754632410046651048, 0.9867877818048297334, 1.414398233496700907 ) ) ;
#103741=CARTESIAN_POINT ( 'NONE',  ( 0.1747926744264660659, 7.629137130509076492, -2.455305974604492292 ) ) ;
#103742=CARTESIAN_POINT ( 'NONE',  ( 0.8097366424872083357, 1.363176973609769416, -1.850781266144943205 ) ) ;
#103744=CARTESIAN_POINT ( 'NONE',  ( 0.3513179634891601677, -1.816012830335328232, 1.349138783986586931 ) ) ;
#103745=CARTESIAN_POINT ( 'NONE',  ( 3.071027892464781583, -1.946086441943569723, -0.8056474276203289264 ) ) ;
#103749=CARTESIAN_POINT ( 'NONE',  ( 0.000000000000000000, 1.328312333417671853, -2.244820250217825830 ) ) ;
#103755=CARTESIAN_POINT ( 'NONE',  ( 2.426173717206762781, -2.096881089210366422, 0.3156149858808757203 ) ) ;
#103756=CARTESIAN_POINT ( 'NONE',  ( 3.516091144284401171, -0.6417545297995127518, 2.126723297420398673 ) ) ;
#103757=CARTESIAN_POINT ( 'NONE',  ( 2.291216553123593958, 1.694975396412688351, 1.389067552005143646 ) ) ;
#103760=CARTESIAN_POINT ( 'NONE',  ( 5.775826483351648832, -1.914393393812302113, 0.4282712878391075062 ) ) ;
#103762=CARTESIAN_POINT ( 'NONE',  ( 6.610000000000009202, 6.036727194997777879, 2.594899704271665275 ) ) ;
#103765=CARTESIAN_POINT ( 'NONE',  ( 4.588201236890728119, 1.223260742344203900, 1.732012071221388450 ) ) ;
#103769=CARTESIAN_POINT ( 'NONE',  ( 5.787991602622606813, -0.9759734195362681497, 1.928925553883020338 ) ) ;
#103771=CARTESIAN_POINT ( 'NONE',  ( 5.513187957602974976, -1.795010045117376496, 0.4093405989887277663 ) ) ;
#103774=CARTESIAN_POINT ( 'NONE',  ( 1.575334329707895664, -0.9311816076861539893, 1.470162731330543426 ) ) ;
#103779=CARTESIAN_POINT ( 'NONE',  ( 4.786082296487640164, -1.021991182799499409, 1.904868704497929333 ) ) ;
#103782=CARTESIAN_POINT ( 'NONE',  ( 4.786082296487640164, -1.021991182799499409, 1.904868704497929333 ) ) ;
#103783=CARTESIAN_POINT ( 'NONE',  ( 5.290288327143207958, -1.956129722686357431, -0.2442305991610035365 ) ) ;
#103784=CARTESIAN_POINT ( 'NONE',  ( 4.428821037005469030, 0.8169072895964669678, 1.529287752448208471 ) ) ;
#103785=CARTESIAN_POINT ( 'NONE',  ( 0.9959476074029065540, -2.191739723303194332, 0.005169097091584088505 ) ) ;
#103786=CARTESIAN_POINT ( 'NONE',  ( 2.239721530183640841, -2.061013379209011287, 1.037980457044695992 ) ) ;
#103787=CARTESIAN_POINT ( 'NONE',  ( 3.954412886046823949, 0.7382688757093980314, 1.924196998259326996 ) ) ;
#103788=CARTESIAN_POINT ( 'NONE',  ( 0.2869206542332564114, 1.438414604794725049, 1.304842588618974952 ) ) ;
#103795=CARTESIAN_POINT ( 'NONE',  ( 3.716033540554028125, -2.174548934981130444, 0.3748234698989146851 ) ) ;
#103798=CARTESIAN_POINT ( 'NONE',  ( 0.8833916088089890373, -1.769421289247067097, 0.5767519331581376640 ) ) ;
#103799=CARTESIAN_POINT ( 'NONE',  ( -0.1288028175206725467, 2.854926803129751001, -2.761885894952537779 ) ) ;
#103803=CARTESIAN_POINT ( 'NONE',  ( 6.925078400183548588, 3.689301810296021777, 2.558360072861276979 ) ) ;
#103806=CARTESIAN_POINT ( 'NONE',  ( 2.782161975763951300, -1.060548055690222702, 1.766919142140084720 ) ) ;
#103811=CARTESIAN_POINT ( 'NONE',  ( 2.413025777909239000, 1.840395853916647173, 0.9276406582674895374 ) ) ;
#103817=CARTESIAN_POINT ( 'NONE',  ( 5.918643953348324160, 1.484978324971843566, -1.632713241052483832 ) ) ;
#103818=CARTESIAN_POINT ( 'NONE',  ( 6.854744688279930998, -1.755419801747569286, 1.426855864884185809 ) ) ;
#103820=CARTESIAN_POINT ( 'NONE',  ( 0.3039231887648624619, -1.082844287645868375, -1.700959134490941160 ) ) ;
#103824=CARTESIAN_POINT ( 'NONE',  ( 1.902992089709685031, 1.553661375375714471, 1.041555772207984676 ) ) ;
#103825=CARTESIAN_POINT ( 'NONE',  ( 3.977750132953357998, -0.7672935630990398437, 1.865046046545227654 ) ) ;
#103827=CARTESIAN_POINT ( 'NONE',  ( 6.639320575229264776, 1.250520135805782029, 2.217830841512329787 ) ) ;
#103829=CARTESIAN_POINT ( 'NONE',  ( 4.969407589744497145, 0.2071734034183834172, -2.095845648730967792 ) ) ;
#103834=CARTESIAN_POINT ( 'NONE',  ( 4.640881595473839383, 1.934004784890541062, 0.5824627899903914718 ) ) ;
#103836=CARTESIAN_POINT ( 'NONE',  ( 0.2685208109398624088, -0.8776176662104094861, -1.864379643416124166 ) ) ;
#103838=CARTESIAN_POINT ( 'NONE',  ( 5.466167184710096549, 1.060119519021487378, 1.883692621652333532 ) ) ;
#103845=CARTESIAN_POINT ( 'NONE',  ( 3.455704523497793001, 1.709784277118444162, 1.338028058695311273 ) ) ;
#103848=CARTESIAN_POINT ( 'NONE',  ( 2.138008341990283778, 0.4048980806483238326, 1.796005048712509655 ) ) ;
#103850=CARTESIAN_POINT ( 'NONE',  ( 2.947022816757136621, -1.793111998972513277, -1.259777465452505796 ) ) ;
#103851=CARTESIAN_POINT ( 'NONE',  ( 6.883263157960364254, 3.685033293952295175, 2.667793810733168236 ) ) ;
#103852=CARTESIAN_POINT ( 'NONE',  ( 4.346707190358800155, 0.5996197433882300976, 2.181559591530066289 ) ) ;
#103859=CARTESIAN_POINT ( 'NONE',  ( 5.835142003873758476, -1.599326089537930873, 0.7579421051841316315 ) ) ;
#103860=CARTESIAN_POINT ( 'NONE',  ( 3.440093027223433797, -1.200828029685986786, -1.615568007891918789 ) ) ;
#103862=CARTESIAN_POINT ( 'NONE',  ( 1.448413646618036399, 2.103543699351087870, 0.1036336169341102176 ) ) ;
#103865=CARTESIAN_POINT ( 'NONE',  ( 1.943746065852373972, 1.356001085411572049, 1.428673526509681047 ) ) ;
#103869=CARTESIAN_POINT ( 'NONE',  ( 5.906502150075481516, -1.803732336900876421, -0.1683732622318224459 ) ) ;
#103874=CARTESIAN_POINT ( 'NONE',  ( 4.944154083221364182, 1.865701114312174225, 0.1370711555178441010 ) ) ;
#103875=CARTESIAN_POINT ( 'NONE',  ( 5.787960296632533641, -1.308950758395693414, -1.603975846202657429 ) ) ;
#103878=CARTESIAN_POINT ( 'NONE',  ( -0.02338929933905827679, 0.006294950389555676457, -1.710968156697997289 ) ) ;
#103886=CARTESIAN_POINT ( 'NONE',  ( 5.090269282739749102, 1.010147525469132557, -1.681691772506640481 ) ) ;
#103888=CARTESIAN_POINT ( 'NONE',  ( 2.970077202574809228, 1.701686883299750264, 1.080900613174784475 ) ) ;
#103889=CARTESIAN_POINT ( 'NONE',  ( 2.044013137410850778, 0.8228895493161382246, 1.730149048491230301 ) ) ;
#103891=CARTESIAN_POINT ( 'NONE',  ( 0.8904706703079521279, -0.5376514911656914419, -2.124458794526106864 ) ) ;
#103893=CARTESIAN_POINT ( 'NONE',  ( 2.635844295777586943, 0.8854499327175249235, -1.647724587607077851 ) ) ;
#103895=CARTESIAN_POINT ( 'NONE',  ( 4.271743731491533858, 0.4368499997736470797, -1.965098791395853750 ) ) ;
#103896=B_SPLINE_CURVE_WITH_KNOTS ( 'NONE', 3,
 ( #147689, #133597, #134657, #316, #98935, #66387, #116299, #64297, #196430, #81604, #213706, #65330, #99992, #16580, #180184, #150891, #18719, #131477, #130443, #97883, #197480, #1391, #149820, #132535, #182290, #164990, #184426, #48075, #33916, #181232, #68529, #32860, #166058, #17644, #51245, #117371, #183368, #34972, #114186, #101044, #84803, #2453, #200660, #52309, #118439, #36043, #102123, #19791, #146641, #71730, #70659, #90163, #136769, #103194, #169257, #6734, #151951, #20843, #138914, #107527, #156229, #106449, #56585, #7806, #137842, #120589, #86942, #153008, #73899, #4585, #21901, #204934, #54447, #39258, #40343, #139992, #121663, #206013, #202797, #88011, #3521, #186567, #69593, #37116, #38195, #154082, #171389, #5649, #24060, #122744, #188707, #170313, #155152, #57648, #172472, #203864, #123808, #189768, #22980, #135703, #119505, #104267, #201729, #41420, #55509, #187631, #105352, #173558, #89099, #72813, #85873, #53370, #185490, #142129, #94437, #91233, #43551, #61912, #78150, #158357, #145340, #160476, #111797, #211341, #58711, #207079, #79222, #9950, #109672, #141072, #112860, #210274, #190824, #174622, #124860, #159406, #175674, #144280, #93370, #42485, #46747, #194030, #62965, #11005, #74962, #128074, #45680, #27262, #77082, #26198, #177802, #29419, #25131, #76026, #95510, #161557, #143210, #209200, #208142, #60840, #127001, #59772, #125931, #157293, #176728, #8883, #192960, #108594, #191889, #44612, #110728, #92314, #28341, #12083, #13146, #129135, #195111, #202274, #30487, #84282, #100534, #137325, #169800, #133073, #83203, #52851, #53925, #101601, #21389, #4072, #183914, #200148, #99475, #67999, #165534, #118986, #1939, #120062, #116843, #36590, #134141, #203341, #37673, #54994, #166609, #17127, #150369, #182844, #102677, #87498, #35525, #51802, #167669, #19270, #149284, #865, #199071, #50718, #34462 ),
 .UNSPECIFIED., .F., .F.,
 ( 4, 1, 1, 1, 1, 1, 1, 1, 1, 1, 1, 1, 1, 1, 1, 1, 1, 1, 1, 1, 1, 1, 1, 1, 1, 1, 1, 1, 1, 1, 1, 1, 1, 1, 1, 1, 1, 1, 1, 1, 1, 1, 1, 1, 1, 1, 1, 1, 1, 1, 1, 1, 1, 1, 1, 1, 1, 1, 1, 1, 1, 1, 1, 1, 1, 1, 1, 1, 1, 1, 1, 1, 1, 1, 1, 1, 1, 1, 1, 1, 1, 1, 1, 1, 1, 1, 1, 1, 1, 1, 1, 1, 1, 1, 1, 1, 1, 1, 1, 1, 1, 1, 1, 1, 1, 1, 1, 1, 1, 1, 1, 1, 1, 1, 1, 1, 1, 1, 1, 1, 1, 1, 1, 1, 1, 1, 1, 1, 1, 1, 1, 1, 1, 1, 1, 1, 1, 1, 1, 1, 1, 1, 1, 1, 1, 1, 1, 1, 1, 1, 1, 1, 1, 1, 1, 1, 1, 1, 1, 1, 1, 1, 1, 1, 1, 1, 1, 1, 1, 1, 1, 1, 1, 1, 1, 1, 1, 1, 1, 1, 1, 1, 1, 1, 1, 1, 1, 1, 1, 1, 1, 1, 1, 1, 1, 1, 1, 1, 1, 1, 1, 1, 1, 1, 1, 1, 1, 1, 1, 1, 1, 1, 1, 1, 1, 1, 4 ),
 ( 0.000000000000000000, 0.004629629629629626771, 0.009259259259259253541, 0.01388888888888887771, 0.01851851851851850361, 0.02314814814814812952, 0.02777777777777775542, 0.03240740740740737785, 0.03703703703703700723, 0.04166666666666662966, 0.04629629629629625903, 0.05092592592592588147, 0.05555555555555549696, 0.06018518518518511939, 0.06481481481481474183, 0.06944444444444436426, 0.07407407407407398670, 0.07870370370370359525, 0.08333333333333321769, 0.08796296296296284012, 0.09259259259259246255, 0.09722222222222209886, 0.1018518518518517213, 0.1064814814814813299, 0.1111111111111109523, 0.1157407407407405747, 0.1203703703703701972, 0.1249999999999998196, 0.1296296296296294281, 0.1342592592592590506, 0.1388888888888886730, 0.1435185185185182954, 0.1481481481481479179, 0.1527777777777775403, 0.1574074074074071627, 0.1620370370370367852, 0.1666666666666664076, 0.1712962962962960300, 0.1759259259259256525, 0.1805555555555552749, 0.1851851851851848973, 0.1898148148148145198, 0.1944444444444441145, 0.1990740740740737091, 0.2037037037037033038, 0.2083333333333328985, 0.2129629629629625209, 0.2175925925925921156, 0.2222222222222217103, 0.2268518518518513050, 0.2314814814814808996, 0.2361111111111104943, 0.2407407407407401168, 0.2453703703703697114, 0.2499999999999993061, 0.2546296296296289285, 0.2592592592592585232, 0.2638888888888881179, 0.2685185185185177126, 0.2731481481481473073, 0.2777777777777769019, 0.2824074074074064966, 0.2870370370370360913, 0.2916666666666656860, 0.2962962962962952806, 0.3009259259259249308, 0.3055555555555545255, 0.3101851851851841202, 0.3148148148148137149, 0.3194444444444433095, 0.3240740740740729042, 0.3287037037037024989, 0.3333333333333320936, 0.3379629629629616883, 0.3425925925925912829, 0.3472222222222209331, 0.3518518518518505278, 0.3564814814814801225, 0.3611111111111097172, 0.3657407407407393118, 0.3703703703703689065, 0.3749999999999985567, 0.3796296296296282069, 0.3842592592592578571, 0.3888888888888874518, 0.3935185185185171020, 0.3981481481481467521, 0.4027777777777764023, 0.4074074074074060525, 0.4120370370370357027, 0.4166666666666652974, 0.4212962962962949476, 0.4259259259259245978, 0.4305555555555542480, 0.4351851851851838981, 0.4398148148148135483, 0.4444444444444431430, 0.4490740740740727932, 0.4537037037037024434, 0.4583333333333320936, 0.4629629629629617438, 0.4675925925925913940, 0.4722222222222209886, 0.4768518518518506388, 0.4814814814814802890, 0.4861111111111099392, 0.4907407407407395894, 0.4953703703703692396, 0.4999999999999988898, 0.5046296296296285400, 0.5092592592592581902, 0.5138888888888878403, 0.5185185185185173795, 0.5231481481481470297, 0.5277777777777766799, 0.5324074074074063301, 0.5370370370370359803, 0.5416666666666656305, 0.5462962962962952806, 0.5509259259259249308, 0.5555555555555545810, 0.5601851851851842312, 0.5648148148148138814, 0.5694444444444435316, 0.5740740740740730708, 0.5787037037037027210, 0.5833333333333323711, 0.5879629629629620213, 0.5925925925925916715, 0.5972222222222213217, 0.6018518518518509719, 0.6064814814814806221, 0.6111111111111102723, 0.6157407407407399225, 0.6203703703703695727, 0.6249999999999992228, 0.6296296296296287620, 0.6342592592592584122, 0.6388888888888880624, 0.6435185185185177126, 0.6481481481481473628, 0.6527777777777770130, 0.6574074074074066631, 0.6620370370370363133, 0.6666666666666659635, 0.6712962962962956137, 0.6759259259259252639, 0.6805555555555549141, 0.6851851851851845643, 0.6898148148148141034, 0.6944444444444437536, 0.6990740740740734038, 0.7037037037037030540, 0.7083333333333327042, 0.7129629629629623544, 0.7175925925925920046, 0.7222222222222216548, 0.7268518518518513050, 0.7314814814814809552, 0.7361111111111106053, 0.7407407407407402555, 0.7453703703703697947, 0.7499999999999994449, 0.7546296296296290951, 0.7592592592592586342, 0.7638888888888882844, 0.7685185185185179346, 0.7731481481481475848, 0.7777777777777772350, 0.7824074074074068852, 0.7870370370370365354, 0.7916666666666661856, 0.7962962962962958358, 0.8009259259259254859, 0.8055555555555551361, 0.8101851851851847863, 0.8148148148148143255, 0.8194444444444439757, 0.8240740740740736259, 0.8287037037037032761, 0.8333333333333329263, 0.8379629629629625764, 0.8425925925925922266, 0.8472222222222218768, 0.8518518518518515270, 0.8564814814814811772, 0.8611111111111108274, 0.8657407407407404776, 0.8703703703703701278, 0.8749999999999996669, 0.8796296296296293171, 0.8842592592592589673, 0.8888888888888886175, 0.8935185185185182677, 0.8981481481481479179, 0.9027777777777775681, 0.9074074074074072183, 0.9120370370370368684, 0.9166666666666665186, 0.9212962962962961688, 0.9259259259259258190, 0.9305555555555553582, 0.9351851851851850084, 0.9398148148148146586, 0.9444444444444443088, 0.9490740740740739589, 0.9537037037037036091, 0.9583333333333332593, 0.9629629629629629095, 0.9675925925925925597, 0.9722222222222222099, 0.9768518518518518601, 0.9814814814814815103, 0.9861111111111110494, 0.9907407407407406996, 0.9953703703703703498, 1.000000000000000000 ),
 .UNSPECIFIED. ) ;
#103899=CARTESIAN_POINT ( 'NONE',  ( 4.306348207420813701, 1.301105652591315387, -1.670210365991892987 ) ) ;
#103901=CARTESIAN_POINT ( 'NONE',  ( 6.021949436824264978, 2.040384406434097464, -0.3501103912618847014 ) ) ;
#103902=CARTESIAN_POINT ( 'NONE',  ( 1.206708187092224716, 1.845608279032302512, 0.9822807542516975854 ) ) ;
#103903=CARTESIAN_POINT ( 'NONE',  ( 6.720655732516620517, 2.957990990047154600, 2.526349433132681011 ) ) ;
#103904=CARTESIAN_POINT ( 'NONE',  ( 6.686557121163758666, -1.791048715316777562, -0.3524728914669760793 ) ) ;
#103913=CARTESIAN_POINT ( 'NONE',  ( 0.2756360753965527155, 1.792041154956749871, -0.2637626551888968551 ) ) ;
#103922=( GEOMETRIC_REPRESENTATION_CONTEXT ( 3 ) GLOBAL_UNCERTAINTY_ASSIGNED_CONTEXT ( ( #31342 ) ) GLOBAL_UNIT_ASSIGNED_CONTEXT ( ( #63187, #33878, #150854 ) ) REPRESENTATION_CONTEXT ( 'NONE', 'WORKASPACE' ) );
#103923=CARTESIAN_POINT ( 'NONE',  ( 6.591432905763006111, -0.4393008961055907546, 1.975236973087670656 ) ) ;
#103924=CARTESIAN_POINT ( 'NONE',  ( 0.1180496341894651385, -0.5612577129426484790, 2.044807062438446454 ) ) ;
#103929=CARTESIAN_POINT ( 'NONE',  ( 2.957809129533952142, -0.6224678976109696560, 1.868526426519439898 ) ) ;
#103931=CARTESIAN_POINT ( 'NONE',  ( 4.640250013031629095, 0.7743308749140092040, 1.862011755488258480 ) ) ;
#103935=CARTESIAN_POINT ( 'NONE',  ( 4.558633756138521065, -1.956834287480881063, -0.9866608250781592204 ) ) ;
#103937=CARTESIAN_POINT ( 'NONE',  ( 2.854421793556624731, 0.6472853923233500284, 1.814523859438036624 ) ) ;
#103940=CARTESIAN_POINT ( 'NONE',  ( -0.02988540731097348233, 2.061246921799511966, -2.144091820287073791 ) ) ;
#103941=CARTESIAN_POINT ( 'NONE',  ( 0.2412292383832773390, 0.3817025157030576321, 2.173470055567463088 ) ) ;
#103945=CARTESIAN_POINT ( 'NONE',  ( 5.612145322048014862, 1.967363499941950034, -0.09270071294615632451 ) ) ;
#103946=VERTEX_POINT ( 'NONE', #118544 ) ;
#103947=CARTESIAN_POINT ( 'NONE',  ( 0.2396544122938427390, 1.936909983681795344, 0.1419545801408238772 ) ) ;
#103948=CARTESIAN_POINT ( 'NONE',  ( 3.985024600404694972, -1.879186454625543901, -0.7224040237710227519 ) ) ;
#103949=CARTESIAN_POINT ( 'NONE',  ( 5.870575887392723402, -0.5666052741825926553, 2.227357739769205924 ) ) ;
#103950=CARTESIAN_POINT ( 'NONE',  ( 4.821077630544555070, -1.661119493813640657, -0.8391380156763434961 ) ) ;
#103955=CARTESIAN_POINT ( 'NONE',  ( 0.5038066827526345159, -2.180447833630628107, 0.2205874978757973448 ) ) ;
#103960=CARTESIAN_POINT ( 'NONE',  ( 0.02954982209854748257, -1.120125052174587577, -1.442194003765177257 ) ) ;
#103963=CARTESIAN_POINT ( 'NONE',  ( 2.724952806592676691, 1.721339412077933284, 0.2094855716100688936 ) ) ;
#103965=CARTESIAN_POINT ( 'NONE',  ( 6.509000000000034980, 7.629137130509102249, 2.499999999999994227 ) ) ;
#103968=CARTESIAN_POINT ( 'NONE',  ( 0.6728209460903146200, 1.430239379376567976, -1.496996390900617646 ) ) ;
#103969=CARTESIAN_POINT ( 'NONE',  ( 5.602125774977974260, -1.825872481414937853, 0.004271240736861136277 ) ) ;
#103970=CARTESIAN_POINT ( 'NONE',  ( 3.643363735869999509, 1.775428317022755609, -0.8347113108059035502 ) ) ;
#103974=CARTESIAN_POINT ( 'NONE',  ( 3.510498622083501719, -2.118129049236017192, -0.1023006277712720374 ) ) ;
#103977=CARTESIAN_POINT ( 'NONE',  ( 1.551716534671506498, 1.565040117424065347, 1.355267069636761912 ) ) ;
#103978=CARTESIAN_POINT ( 'NONE',  ( 6.827182134110209688, 6.038954451951505042, 2.405852596708078384 ) ) ;
#103980=CARTESIAN_POINT ( 'NONE',  ( 4.951916289638909063, -1.570117426187572107, -1.571520405092931005 ) ) ;
#103982=CARTESIAN_POINT ( 'NONE',  ( 1.547921954348607354, -1.621480451111120047, 1.629585861659810009 ) ) ;
#103989=CARTESIAN_POINT ( 'NONE',  ( 3.023589307540079041, -0.3687504995396119201, 1.876329818327879817 ) ) ;
#103991=CARTESIAN_POINT ( 'NONE',  ( 3.785938739704467260, -0.8500231715772713637, 1.500685565699668933 ) ) ;
#103992=CARTESIAN_POINT ( 'NONE',  ( 2.430875351317234756, -1.673853735218135741, 1.124246214196801485 ) ) ;
#103993=CARTESIAN_POINT ( 'NONE',  ( 3.446149177467156655, -2.027825264502993718, -1.082511230532481106 ) ) ;
#103994=CARTESIAN_POINT ( 'NONE',  ( 3.796368952254399964, -2.259583311708447617, -0.1157369865004975740 ) ) ;
#103995=CARTESIAN_POINT ( 'NONE',  ( 6.340466044077378349, 2.082889313809291654, 0.3107213310214774760 ) ) ;
#103998=CARTESIAN_POINT ( 'NONE',  ( 4.586996685387556560, 1.581260375356493331, -0.7947977318805318214 ) ) ;
#104000=CARTESIAN_POINT ( 'NONE',  ( 0.2876181914312899157, 1.702867465475272901, 1.534690983289775712 ) ) ;
#104001=CARTESIAN_POINT ( 'NONE',  ( 5.630750141678076304, -1.662707896839428434, 0.7909858098210584831 ) ) ;
#104003=CARTESIAN_POINT ( 'NONE',  ( 5.947271710577298975, 0.6394180277670692414, -2.096098967930816848 ) ) ;
#104007=CARTESIAN_POINT ( 'NONE',  ( 6.004363041306050697, 2.067815565686380364, 0.1054426792976848049 ) ) ;
#104008=CARTESIAN_POINT ( 'NONE',  ( 1.007046422456716384, -0.04465021774549028655, 2.016188868504041665 ) ) ;
#104010=CARTESIAN_POINT ( 'NONE',  ( 4.090394749938445429, -1.905694808957728137, -0.2815942358586983607 ) ) ;
#104012=CARTESIAN_POINT ( 'NONE',  ( 0.9673671849170182302, -1.746833394359051495, 1.372194155552537431 ) ) ;
#104019=CARTESIAN_POINT ( 'NONE',  ( 3.825523041098664034, 0.9271419989833797892, -1.472723941875812237 ) ) ;
#104020=CARTESIAN_POINT ( 'NONE',  ( 2.523818479427087702, 1.924573107942130656, -0.3798230296482503210 ) ) ;
#104025=CARTESIAN_POINT ( 'NONE',  ( 6.303176765056641706, -1.658072099422291057, 1.048360225930293321 ) ) ;
#104029=CARTESIAN_POINT ( 'NONE',  ( 5.067592334412735156, 1.357865985192594271, 1.490972259599515848 ) ) ;
#104030=CARTESIAN_POINT ( 'NONE',  ( 0.9719599696450488269, 2.179858136331577434, -0.6057951801161051142 ) ) ;
#104034=CARTESIAN_POINT ( 'NONE',  ( 1.633845377418343237, 0.9265681688636999702, -1.624882239709434018 ) ) ;
#104035=CARTESIAN_POINT ( 'NONE',  ( 0.5450593487147866734, -1.257523079656326148, 1.194353625382915673 ) ) ;
#104037=CARTESIAN_POINT ( 'NONE',  ( 4.107102485094754840, -0.3736803571842538529, 2.159302612355806339 ) ) ;
#104038=CARTESIAN_POINT ( 'NONE',  ( 6.141700272255690152, -1.665644196019906875, -1.597301777034014991 ) ) ;
#104039=CARTESIAN_POINT ( 'NONE',  ( 0.6200826401135750565, -1.101877700393244952, -1.741386573944928795 ) ) ;
#104040=CARTESIAN_POINT ( 'NONE',  ( 2.976435162280165247, -0.1435924003432750840, -1.936700533151126891 ) ) ;
#104045=CARTESIAN_POINT ( 'NONE',  ( 5.151017605526480025, 0.9962996879465220168, 1.753031629501592192 ) ) ;
#104049=CARTESIAN_POINT ( 'NONE',  ( 0.8381832108898427114, 1.798179982845280467, 0.3147962740308178353 ) ) ;
#104055=CARTESIAN_POINT ( 'NONE',  ( 6.455941844152293996, 2.055567607077302128, -0.1488206295068068841 ) ) ;
#104059=CARTESIAN_POINT ( 'NONE',  ( 5.408855464265644564, -0.4929012147626107843, -1.958461550952787844 ) ) ;
#104060=CARTESIAN_POINT ( 'NONE',  ( 6.129551335524713096, -0.2748284885467215943, 2.204153950570774345 ) ) ;
#104064=CARTESIAN_POINT ( 'NONE',  ( 5.647358743468454456, -1.623080139260910437, -1.269863021155111849 ) ) ;
#104065=CARTESIAN_POINT ( 'NONE',  ( 4.096327398540238640, -0.3419367296172080017, 1.987046374476949095 ) ) ;
#104070=ORIENTED_EDGE ( 'NONE', *, *, #193642, .T. ) ;
#104072=CARTESIAN_POINT ( 'NONE',  ( 3.690779688840303496, -1.198677090843719872, -1.620934038430859703 ) ) ;
#104073=CARTESIAN_POINT ( 'NONE',  ( 3.415785861374909249, 1.167101634185686576, -1.423959568491977912 ) ) ;
#104075=CARTESIAN_POINT ( 'NONE',  ( 2.333053021162025953, 2.238922732217122125, 0.5587339331782120722 ) ) ;
#104077=CARTESIAN_POINT ( 'NONE',  ( 4.393933622532245842, -0.8317529007547798114, 1.995363109761492337 ) ) ;
#104079=CARTESIAN_POINT ( 'NONE',  ( 6.585540641348407220, -0.7802508550805786758, 1.666130356082275998 ) ) ;
#104085=CARTESIAN_POINT ( 'NONE',  ( 2.623731232481395725, -1.075365945362505293, -1.530472918023266571 ) ) ;
#104086=CARTESIAN_POINT ( 'NONE',  ( 0.4035112227387879225, -0.5299352985012796280, 1.898712856893035816 ) ) ;
#104089=CARTESIAN_POINT ( 'NONE',  ( 2.209865124170300898, -0.4819264253047173541, 2.153463223375853719 ) ) ;
#104095=CARTESIAN_POINT ( 'NONE',  ( 5.998895389381466714, 1.612053949438954303, -1.134635204971563782 ) ) ;
#104096=CARTESIAN_POINT ( 'NONE',  ( 5.567085169132608868, -2.083932277878234096, -0.9915751667191848862 ) ) ;
#104097=CARTESIAN_POINT ( 'NONE',  ( 0.5023040531197673353, 1.956348610274569744, 0.1481081594910879096 ) ) ;
#104098=CARTESIAN_POINT ( 'NONE',  ( 3.696185820831139779, 0.9318344738791024540, -1.840181792940546179 ) ) ;
#104105=CARTESIAN_POINT ( 'NONE',  ( 0.2862954470153349362, -1.335216113735339105, -1.712835229902017531 ) ) ;
#104107=CARTESIAN_POINT ( 'NONE',  ( 4.810013364240863787, 1.265987717737980134, -1.337210144835267345 ) ) ;
#104109=CARTESIAN_POINT ( 'NONE',  ( 6.075747529084263299, -1.173811750163206158, 1.850510016281024850 ) ) ;
#104110=CARTESIAN_POINT ( 'NONE',  ( 0.7548939078372005618, -1.576849831105286537, -1.005952255950369301 ) ) ;
#104115=CARTESIAN_POINT ( 'NONE',  ( 0.3988866192712777758, -0.2342882197893907670, -1.897819253221716851 ) ) ;
#104117=CARTESIAN_POINT ( 'NONE',  ( 2.096244624822783731, -0.4688358662975153357, -1.706545078221621603 ) ) ;
#104119=CARTESIAN_POINT ( 'NONE',  ( 6.041657904462632622, -1.894779907254999118, 0.6802824325803021877 ) ) ;
#104121=CARTESIAN_POINT ( 'NONE',  ( 4.271028807069753519, 1.709443138559762376, -0.8646770750302870123 ) ) ;
#104124=CARTESIAN_POINT ( 'NONE',  ( 5.248484213797577347, -1.954463446003468885, -0.2428638724455249587 ) ) ;
#104125=CARTESIAN_POINT ( 'NONE',  ( 6.293224362130668936, -0.1031327824093461465, -2.017302584901353946 ) ) ;
#104127=CARTESIAN_POINT ( 'NONE',  ( 2.465516990510143280, 1.834972510290140191, -0.3627323784974947340 ) ) ;
#104128=CARTESIAN_POINT ( 'NONE',  ( 5.918504666124354330, 1.153338095414379261, -1.282764499605532738 ) ) ;
#104130=CARTESIAN_POINT ( 'NONE',  ( 3.317197348578094562, 1.995112415077514356, 0.9436014139095407760 ) ) ;
#104133=CARTESIAN_POINT ( 'NONE',  ( 0.4849267205471480269, 1.973383872003172224, 0.6002626889692606049 ) ) ;
#104140=CARTESIAN_POINT ( 'NONE',  ( 3.508316276398337319, 2.070544812355082254, 0.002818362966339192730 ) ) ;
#104144=CARTESIAN_POINT ( 'NONE',  ( 1.348313414878389294, 0.9933643222376374871, -1.758399455230485575 ) ) ;
#104149=CARTESIAN_POINT ( 'NONE',  ( 0.1745949693968146810, 5.726316517925682525, -2.349368801211670021 ) ) ;
#104151=CARTESIAN_POINT ( 'NONE',  ( 6.608749954595573683, 0.7741944705832277673, -1.861732896133998727 ) ) ;
#104152=CARTESIAN_POINT ( 'NONE',  ( 5.524599559428126305, 0.3805214045222211627, 1.877366190154891701 ) ) ;
#104154=CARTESIAN_POINT ( 'NONE',  ( 4.159861740090546434, 1.033864333764370702, 1.932389678422803181 ) ) ;
#104156=CARTESIAN_POINT ( 'NONE',  ( 2.144650067465687648, 1.855875215511919363, 0.4610605321611755958 ) ) ;
#104160=CARTESIAN_POINT ( 'NONE',  ( 0.9840001696646907270, -2.016598147255070472, 0.002831364411433334727 ) ) ;
#104162=CARTESIAN_POINT ( 'NONE',  ( 5.741772062182810998, 2.188963553168365994, 0.1087695542012837302 ) ) ;
#104164=CARTESIAN_POINT ( 'NONE',  ( 3.047548298876975537, 0.6224300751757807504, -1.608722921838340092 ) ) ;
#104165=ORIENTED_EDGE ( 'NONE', *, *, #141101, .T. ) ;
#104170=CARTESIAN_POINT ( 'NONE',  ( 0.9944974185457016169, 1.932217576897478528, 0.3389098420027157332 ) ) ;
#104171=EDGE_CURVE ( 'NONE', #126115, #146910, #158312, .T. ) ;
#104178=CARTESIAN_POINT ( 'NONE',  ( 3.826654739275455519, 1.278450958818643901, -1.283618901898140985 ) ) ;
#104182=CARTESIAN_POINT ( 'NONE',  ( 5.092358660276916638, -1.001593112396873098, 1.509162939045370466 ) ) ;
#104185=CARTESIAN_POINT ( 'NONE',  ( 5.512096448594467901, 1.858919848428818300, -0.09134777953435403719 ) ) ;
#104187=CARTESIAN_POINT ( 'NONE',  ( 3.093272052591877763, -0.3707496286316728229, 1.879197483129394719 ) ) ;
#104197=CARTESIAN_POINT ( 'NONE',  ( 1.113355907768112774, -2.039295093617380594, 0.4597149659458180104 ) ) ;
#104199=CARTESIAN_POINT ( 'NONE',  ( 0.1998643617870856648, -1.825052844667142349, -0.05062755788937112200 ) ) ;
#104202=CARTESIAN_POINT ( 'NONE',  ( 2.467563089314188662, 1.790814366166630034, -0.3536809140580049471 ) ) ;
#104204=CARTESIAN_POINT ( 'NONE',  ( 2.119528921591812498, 0.3396393280722594388, -1.939881811770089115 ) ) ;
#104205=CARTESIAN_POINT ( 'NONE',  ( 3.632312094575868677, 0.2880498525525148623, 1.920478541846024179 ) ) ;
#104210=CARTESIAN_POINT ( 'NONE',  ( 3.797228045176269440, -0.2112621354826669517, -2.110076569278092062 ) ) ;
#104218=CARTESIAN_POINT ( 'NONE',  ( 3.598116246361187542, -1.823677485248562435, -0.08826725125678223927 ) ) ;
#104219=CARTESIAN_POINT ( 'NONE',  ( 6.104703911763087909, 1.883310800321544409, 0.7212973825745233603 ) ) ;
#104220=CARTESIAN_POINT ( 'NONE',  ( 0.1685321339487330372, -0.8835925182541467526, -1.870455940253319183 ) ) ;
#104223=CARTESIAN_POINT ( 'NONE',  ( 6.925078400183553917, 6.038071034253152725, 2.450556290382682523 ) ) ;
#104224=CARTESIAN_POINT ( 'NONE',  ( 4.293723057671197552, -0.7160966649314598476, 1.728361679364013748 ) ) ;
#104226=CARTESIAN_POINT ( 'NONE',  ( 2.367692237863534555, 1.889325326408105576, -0.3758258368516536052 ) ) ;
#104227=CARTESIAN_POINT ( 'NONE',  ( 6.702011072381410806, 0.7537920952922130269, -1.811353739714548272 ) ) ;
#104233=CARTESIAN_POINT ( 'NONE',  ( 1.581820014152079956, -0.7095999980938502150, 1.994918640774499430 ) ) ;
#104236=CARTESIAN_POINT ( 'NONE',  ( 5.102424979711988051, 2.064335680360945169, 0.1577259720206558580 ) ) ;
#104237=CARTESIAN_POINT ( 'NONE',  ( 0.2394788589213901198, 1.836227513651207177, 0.1364553164684492448 ) ) ;
#104239=CARTESIAN_POINT ( 'NONE',  ( 5.133504205653830255, 0.6649215086056580182, 2.200401518963719383 ) ) ;
#104243=CARTESIAN_POINT ( 'NONE',  ( 1.816774867096879964, 2.139948438195220071, 0.8220829075690959664 ) ) ;
#104246=CARTESIAN_POINT ( 'NONE',  ( 6.017518264666532168, -1.080727962582687773, -1.613252759315900731 ) ) ;
#104250=CARTESIAN_POINT ( 'NONE',  ( 6.533470333208203584, -0.1312131129157616261, 1.882018712217728318 ) ) ;
#104251=CARTESIAN_POINT ( 'NONE',  ( 5.700407750362016301, 1.350738941191354625, -1.497498989668680114 ) ) ;
#104255=CARTESIAN_POINT ( 'NONE',  ( 3.222686667372671732, 0.05170946606813638102, 2.090169120961588245 ) ) ;
#104256=CARTESIAN_POINT ( 'NONE',  ( 1.516075769870619316, 1.192070010050453099, -1.308345436402546191 ) ) ;
#104257=CARTESIAN_POINT ( 'NONE',  ( 6.416638760586134360, -1.319225726833603840, -1.525046029381103452 ) ) ;
#104258=CARTESIAN_POINT ( 'NONE',  ( 3.750172280943805170, 0.8240398376481252729, 2.139190334408520577 ) ) ;
#104259=CARTESIAN_POINT ( 'NONE',  ( 3.872797606970843631, 1.637851192275063816, -0.5887498661538635991 ) ) ;
#104262=CARTESIAN_POINT ( 'NONE',  ( 1.985274739808037481, 1.615814429867837410, 0.6292545280836835397 ) ) ;
#104264=CARTESIAN_POINT ( 'NONE',  ( 3.473242058572806990, 1.961495611989271248, 0.9311941066344242568 ) ) ;
#104266=CARTESIAN_POINT ( 'NONE',  ( 4.557827498477605488, 1.164984774316142113, 1.645760986912048640 ) ) ;
#104267=CARTESIAN_POINT ( 'NONE',  ( 3.125000000000001776, -2.052068128417947168, 1.787079010424618414E-13 ) ) ;
#104270=CARTESIAN_POINT ( 'NONE',  ( 0.8504600536136133204, 0.5560621936452102565, 1.844401357902447414 ) ) ;
#104272=CARTESIAN_POINT ( 'NONE',  ( 4.289451472217206351, -0.001904023060144560469, -2.221583672334653148 ) ) ;
#104274=CARTESIAN_POINT ( 'NONE',  ( 6.883263157960366918, 3.696842586722656865, 2.460469087180997327 ) ) ;
#104280=CARTESIAN_POINT ( 'NONE',  ( 1.190412498926897600, 1.327076764020938882, 1.781161496267854361 ) ) ;
#104281=CARTESIAN_POINT ( 'NONE',  ( 5.318788500806308051, -1.422220495204097546, 1.351624447685224162 ) ) ;
#104284=CARTESIAN_POINT ( 'NONE',  ( 6.626273523942327159, 1.310778252226969975, -1.843845376178480322 ) ) ;
#104286=CARTESIAN_POINT ( 'NONE',  ( 3.684078386338876854, -1.226296459201616340, -1.658441301575198645 ) ) ;
#104290=CARTESIAN_POINT ( 'NONE',  ( 4.833189656263336964, -1.710893631887340227, 0.7565425265826587475 ) ) ;
#104291=CARTESIAN_POINT ( 'NONE',  ( 3.551122959743778562, -1.161752147869070884, 1.287673551650715842 ) ) ;
#104292=CARTESIAN_POINT ( 'NONE',  ( 3.034399582073334489, -1.533639759443014894, 0.8228653360542650397 ) ) ;
#104293=CARTESIAN_POINT ( 'NONE',  ( 0.7500711518760843077, 2.289381476473162369, -0.1197363719210968458 ) ) ;
#104295=CARTESIAN_POINT ( 'NONE',  ( 5.038659576058011957, -1.792549807278142726, 1.075873411605046348 ) ) ;
#104296=CARTESIAN_POINT ( 'NONE',  ( 0.2339851986729903077, 0.3116528534230639247, 1.814411239467295101 ) ) ;
#104299=CARTESIAN_POINT ( 'NONE',  ( 1.934220422044398813, -1.621183349045727473, -1.198859219795316955 ) ) ;
#104304=CARTESIAN_POINT ( 'NONE',  ( 2.578903501431661915, -1.460476376761214556, 1.537597662120089081 ) ) ;
#104307=CARTESIAN_POINT ( 'NONE',  ( 4.793472150574508817, 1.354911484294840429, 1.223852735664505698 ) ) ;
#104312=CARTESIAN_POINT ( 'NONE',  ( 1.845969175824228925, -1.322618866652914393, -1.526557775719493915 ) ) ;
#104313=CARTESIAN_POINT ( 'NONE',  ( 5.631908123138919642, -1.395923778694251105, -1.709176034821748624 ) ) ;
#104316=CARTESIAN_POINT ( 'NONE',  ( 4.258551055683129860, -0.5805891344777401875, -1.768159363456432764 ) ) ;
#104323=CARTESIAN_POINT ( 'NONE',  ( 4.740742070742828496, 0.3150700179065483719, 1.798135100120237251 ) ) ;
#104327=CARTESIAN_POINT ( 'NONE',  ( 0.9304778391672563487, 0.8475688526466665929, 1.512457944649912012 ) ) ;
#104328=CARTESIAN_POINT ( 'NONE',  ( 0.1986093482617317107, -0.4694325260376422948, 1.675759954737522150 ) ) ;
#104329=CARTESIAN_POINT ( 'NONE',  ( 6.006511608602003172, -0.8246739634825739351, -2.155485180906725251 ) ) ;
#104331=CARTESIAN_POINT ( 'NONE',  ( 1.018906392562862528, 1.903027849223213330, 0.7912521351585340978 ) ) ;
#104335=CARTESIAN_POINT ( 'NONE',  ( 6.766976407292540685, -2.298085592349991213, 0.04593636341931536110 ) ) ;
#104339=CARTESIAN_POINT ( 'NONE',  ( 6.262560305340551636, -1.321439916381482060, 1.324322166508178356 ) ) ;
#104340=CARTESIAN_POINT ( 'NONE',  ( 3.867365959033176814, -1.592763314076732106, -1.058159689705892692 ) ) ;
#104342=CARTESIAN_POINT ( 'NONE',  ( 4.828867971087246858, 2.111205472107956282, 0.6427781511747706622 ) ) ;
#104347=CARTESIAN_POINT ( 'NONE',  ( 5.953796468794862129, -1.535729488331440074, -1.462440914314271811 ) ) ;
#104349=CARTESIAN_POINT ( 'NONE',  ( 3.276728144386112263, -1.376063543960687641, 1.852258789692583507 ) ) ;
#104350=CARTESIAN_POINT ( 'NONE',  ( 3.947668504265917644, 1.419370528949075005, 1.354593381527373186 ) ) ;
#104352=CARTESIAN_POINT ( 'NONE',  ( 1.094497266827038962, 1.931770780797737341, 0.3408682529649207926 ) ) ;
#104356=CARTESIAN_POINT ( 'NONE',  ( 5.841029835422532734, -1.731992920607817288, -1.032484497598872064 ) ) ;
#104358=CARTESIAN_POINT ( 'NONE',  ( 0.07576575995338691305, -1.785066692240460329, -0.4505573523648153667 ) ) ;
#104359=CARTESIAN_POINT ( 'NONE',  ( 3.415042003188377251, -1.647272610417279015, 1.414370313860166872 ) ) ;
#104361=CARTESIAN_POINT ( 'NONE',  ( 0.9672155168029163974, -1.668165459610539081, 1.309123814877902969 ) ) ;
#104366=CARTESIAN_POINT ( 'NONE',  ( 0.8782832160191712534, -1.147062573054495216, 1.711818785435960111 ) ) ;
#104369=CARTESIAN_POINT ( 'NONE',  ( 6.827182134110188372, 3.700652156503980716, 2.425390344263624431 ) ) ;
#104373=CARTESIAN_POINT ( 'NONE',  ( 4.547458224165379370, -1.746952781796941911, 0.7782266863690867620 ) ) ;
#104374=CARTESIAN_POINT ( 'NONE',  ( 4.856192259477753126, 0.6790438925599675546, 1.634599669825251178 ) ) ;
#104377=CARTESIAN_POINT ( 'NONE',  ( 0.5624193892179689680, 0.5266301872345402479, 1.733300928327138113 ) ) ;
#104379=CARTESIAN_POINT ( 'NONE',  ( 1.165091096179095675, 1.768693976065521589, -0.7364918582971339278 ) ) ;
#104380=CARTESIAN_POINT ( 'NONE',  ( 2.119664376568120012, 0.3561266789769075292, -2.039353370234835872 ) ) ;
#104382=CARTESIAN_POINT ( 'NONE',  ( 0.7078139640715176428, -1.962176506181498636, 0.1910761354673266577 ) ) ;
#104383=CARTESIAN_POINT ( 'NONE',  ( 3.211362085483655981, -0.3553965070040401852, 1.790585553824732390 ) ) ;
#104384=CARTESIAN_POINT ( 'NONE',  ( 6.721333373144884327, -0.1645177889858795151, 2.170883633896856679 ) ) ;
#104387=CARTESIAN_POINT ( 'NONE',  ( 3.895030958483152173, 0.2998364479755392664, 2.040644712996171339 ) ) ;
#104393=CARTESIAN_POINT ( 'NONE',  ( 6.373496627357888578, -0.2573980274669443458, 2.054251119134167691 ) ) ;
#104395=CARTESIAN_POINT ( 'NONE',  ( 4.024825912876791811, 2.051136489140188424, 0.6822911077620784637 ) ) ;
#104396=CARTESIAN_POINT ( 'NONE',  ( 4.758466132964124462, 2.014421802844321707, 0.1462751549737814905 ) ) ;
#104397=CARTESIAN_POINT ( 'NONE',  ( 6.620655732516651071, 1.241313378043694238, 2.288056600130850882 ) ) ;
#104403=CARTESIAN_POINT ( 'NONE',  ( 2.782435679340321766, -0.5899881929209308540, -1.928257399728677601 ) ) ;
#104408=CARTESIAN_POINT ( 'NONE',  ( 6.135011676971933170, 1.786887936952135769, 0.6819008164158718577 ) ) ;
#104409=CARTESIAN_POINT ( 'NONE',  ( 6.720655732516624070, 2.949086357957014570, 2.625980845328681923 ) ) ;
#104411=CARTESIAN_POINT ( 'NONE',  ( 4.903922820734956112, -1.081083478763317007, -1.701937824264573518 ) ) ;
#104414=CARTESIAN_POINT ( 'NONE',  ( 6.334932600541999470, 0.1746011871221597178, 1.715888227437605718 ) ) ;
#104419=CARTESIAN_POINT ( 'NONE',  ( 5.149604166610965095, 0.5880212298954893280, -1.775756280894603689 ) ) ;
#104420=CARTESIAN_POINT ( 'NONE',  ( 6.099863781956886832, 1.391357071557168146, 1.455236689230124947 ) ) ;
#104422=CARTESIAN_POINT ( 'NONE',  ( 2.536061329345109971, 1.270221119870031057, 1.634730569901183150 ) ) ;
#104426=CARTESIAN_POINT ( 'NONE',  ( 1.054314798682391530, -1.277026470193865171, 1.560515422851154854 ) ) ;
#104427=CARTESIAN_POINT ( 'NONE',  ( 1.089788312850032526, 1.080336570596603929, 1.454002670061284919 ) ) ;
#104433=CARTESIAN_POINT ( 'NONE',  ( 5.677321882007140275, 1.453744714618950606, 1.247594701790984306 ) ) ;
#104441=CARTESIAN_POINT ( 'NONE',  ( 2.448304249002517974, 2.161202317112873139, 0.05382173394478938222 ) ) ;
#104444=CARTESIAN_POINT ( 'NONE',  ( 0.6859744409541921328, 2.042103856186634925, -0.5713114342573709648 ) ) ;
#104446=CARTESIAN_POINT ( 'NONE',  ( 5.895480738319402114, 1.384055093596334274, 1.190509915477963698 ) ) ;
#104448=CARTESIAN_POINT ( 'NONE',  ( 1.774623370849885085, -1.870687226035630646, -0.6220538675408300300 ) ) ;
#104449=CARTESIAN_POINT ( 'NONE',  ( 4.904515063324526025, -1.898637117948184017, -0.2282459111111398431 ) ) ;
#104453=CARTESIAN_POINT ( 'NONE',  ( 5.371531009330141160, -0.2907324665500017891, 1.947856185699713638 ) ) ;
#104454=CARTESIAN_POINT ( 'NONE',  ( -0.02357939311542662716, -0.1349932991356362910, -1.911059701570053226 ) ) ;
#104461=CARTESIAN_POINT ( 'NONE',  ( 5.549440478958017842, -1.726947976793650197, 0.8215754744917986852 ) ) ;
#104462=EDGE_LOOP ( 'NONE', ( #16810, #104165 ) ) ;
#104463=CARTESIAN_POINT ( 'NONE',  ( 1.237671066534186792, -1.994493743981802680, 0.9446329514863486265 ) ) ;
#104466=CARTESIAN_POINT ( 'NONE',  ( -0.005422908085399994089, -1.854866876809873943, -0.4647201794698225252 ) ) ;
#104467=CARTESIAN_POINT ( 'NONE',  ( 0.07680821025393863577, 2.892152076732486421, -2.299782885777381658 ) ) ;
#104470=CARTESIAN_POINT ( 'NONE',  ( 2.682155120989743402, -1.190029146579720587, -1.693995171316540427 ) ) ;
#104474=CARTESIAN_POINT ( 'NONE',  ( 0.9542513359644848592, 2.159166806557303531, -0.1069676271590186134 ) ) ;
#104480=CARTESIAN_POINT ( 'NONE',  ( 6.925078400183548588, 0.0006614011395407459748, 1.855452278108092656 ) ) ;
#104482=CARTESIAN_POINT ( 'NONE',  ( 4.518016650454199201, -1.583040169018738785, 0.7084668738900431473 ) ) ;
#104487=CARTESIAN_POINT ( 'NONE',  ( 3.819242646454374057, -1.823515126939363462, -0.9802443236400715243 ) ) ;
#104488=CARTESIAN_POINT ( 'NONE',  ( 4.886377882447483501, -0.7144107685513987338, -1.993165935382594789 ) ) ;
#104491=CARTESIAN_POINT ( 'NONE',  ( 1.340603599695965764, -1.920222134930357427, -0.4367614745469716730 ) ) ;
#104492=CARTESIAN_POINT ( 'NONE',  ( 0.4395310841842986482, -1.815173276516975243, 0.6020934215927520317 ) ) ;
#104493=CARTESIAN_POINT ( 'NONE',  ( 4.664210274407590617, -1.499448637150493813, 1.733910808658318814 ) ) ;
#104494=CARTESIAN_POINT ( 'NONE',  ( 1.910518402784128433, 1.353611321597010253, -1.225282022559864625 ) ) ;
#104498=CARTESIAN_POINT ( 'NONE',  ( 2.338141740155843085, -1.162522942608142928, -1.643444077351646326 ) ) ;
#104499=CARTESIAN_POINT ( 'NONE',  ( 3.537899350542179189, 1.241011212050652901, 1.519374649786103149 ) ) ;
#104502=CARTESIAN_POINT ( 'NONE',  ( 0.07556134207192893859, 0.6772206542668850471, -2.324809334106460845 ) ) ;
#104503=CARTESIAN_POINT ( 'NONE',  ( 5.912080347638632993, 1.404955882617323848, -1.548356120136730851 ) ) ;
#104504=CARTESIAN_POINT ( 'NONE',  ( 4.434285456697817374, 1.735847377751572385, 0.3442416992474469084 ) ) ;
#104506=CARTESIAN_POINT ( 'NONE',  ( 0.4456111923471539615, 0.6836232613432814409, -2.082162021007263331 ) ) ;
#104507=CARTESIAN_POINT ( 'NONE',  ( 6.369106938980155341, 1.663098657370492672, -0.5127371055620026929 ) ) ;
#104510=CARTESIAN_POINT ( 'NONE',  ( 0.1331715793776600265, 0.003733371859311259821, -1.953671397793784070 ) ) ;
#104511=CARTESIAN_POINT ( 'NONE',  ( 6.469376040731918742, -2.253416215261240918, -0.4533134382209720314 ) ) ;
#104512=CARTESIAN_POINT ( 'NONE',  ( 0.1333692844072801587, 4.087911462428309051, -2.608372271572469092 ) ) ;
#104513=CARTESIAN_POINT ( 'NONE',  ( 6.749374558768074017, -1.701276501228730309, -0.3333242692393871831 ) ) ;
#104514=CARTESIAN_POINT ( 'NONE',  ( 2.051678093609669240, -1.773579625386853875, -1.313098587465796774 ) ) ;
#104515=CARTESIAN_POINT ( 'NONE',  ( 6.391115334191724173, 0.2064332055253786102, 2.161336459811058042 ) ) ;
#104517=CARTESIAN_POINT ( 'NONE',  ( 1.675176079212177260, 1.839371217556123650, -1.048680071690030413 ) ) ;
#104518=CARTESIAN_POINT ( 'NONE',  ( 4.375000000000001776, 2.052068128417944504, -2.491713675105573160E-13 ) ) ;
#104520=CARTESIAN_POINT ( 'NONE',  ( 4.559546607354286074, 0.4225000031176616710, -1.879333123156016860 ) ) ;
#104522=CARTESIAN_POINT ( 'NONE',  ( 1.488225144363482189, -2.281859108288700089, -0.2192131398826550337 ) ) ;
#104526=CARTESIAN_POINT ( 'NONE',  ( 3.985193088136604889, -2.072824570928345711, -0.7989420372410382942 ) ) ;
#104532=CARTESIAN_POINT ( 'NONE',  ( 1.828750219146151323, 0.7691198443132395424, -1.864169014999479623 ) ) ;
#104534=CARTESIAN_POINT ( 'NONE',  ( 0.3915631436273382948, -1.887207296038289961, 0.8326094146433449250 ) ) ;
#104537=CARTESIAN_POINT ( 'NONE',  ( 0.3097736896383457839, 1.270387085892955792, -1.333027339516623888 ) ) ;
#104540=CARTESIAN_POINT ( 'NONE',  ( 1.651228947852514173, 0.5200303365089484764, -1.691588852159523704 ) ) ;
#104541=CARTESIAN_POINT ( 'NONE',  ( 0.1412502902482688505, 0.7743183493036235321, 1.862015731718666078 ) ) ;
#104542=CARTESIAN_POINT ( 'NONE',  ( 6.374529642495492254, -0.09526421964337064563, -1.737987611564382862 ) ) ;
#104543=CARTESIAN_POINT ( 'NONE',  ( 4.265347265089792117, 2.223640956194427254, -0.5566138344911036873 ) ) ;
#104544=CARTESIAN_POINT ( 'NONE',  ( 3.872867692073681756, 1.733033312621637068, -0.6219614626309655225 ) ) ;
#104547=CARTESIAN_POINT ( 'NONE',  ( 4.647361241834577328, -1.411646026218037253, -1.157555111390089264 ) ) ;
#104549=CARTESIAN_POINT ( 'NONE',  ( 5.133435478496918947, 0.5880181904946503169, 1.928752423557971829 ) ) ;
#104551=CARTESIAN_POINT ( 'NONE',  ( 3.046068780686244981, 0.8155736813739141722, -2.110571434806473690 ) ) ;
#104553=CARTESIAN_POINT ( 'NONE',  ( 6.141652715049399802, -1.522797514780509065, -1.454946885519771582 ) ) ;
#104555=CARTESIAN_POINT ( 'NONE',  ( 3.912603064140641074, 0.7423916865902054907, 1.932869565047180549 ) ) ;
#104558=CARTESIAN_POINT ( 'NONE',  ( 5.602226918196428151, -0.9533447246646039597, 1.894147766696724799 ) ) ;
#104561=CARTESIAN_POINT ( 'NONE',  ( 2.543477943364984117, -1.427709268621931260, -1.293647605089723429 ) ) ;
#104563=CARTESIAN_POINT ( 'NONE',  ( 0.4671662993806492414, 1.711898730999446228, 0.9738141270322558940 ) ) ;
#104568=CARTESIAN_POINT ( 'NONE',  ( 0.1939906290522614152, 2.069702213058471241, -0.8072921158600793179 ) ) ;
#104569=CARTESIAN_POINT ( 'NONE',  ( 3.381953601626528361, 1.334784698733671560, 1.628938261321200232 ) ) ;
#104572=CARTESIAN_POINT ( 'NONE',  ( 0.4142149233586078227, 0.7067589711089922178, 1.721844540100337717 ) ) ;
#104578=CARTESIAN_POINT ( 'NONE',  ( 1.037531286769650452, -0.04638328994046451298, 2.120250110247793085 ) ) ;
#104581=CARTESIAN_POINT ( 'NONE',  ( 3.068751266904270025, 1.422870340827029345, -1.350941015047700366 ) ) ;
#104582=CARTESIAN_POINT ( 'NONE',  ( 2.641676655999642076, -1.601130012699041982, -1.452526871000489495 ) ) ;
#104583=CARTESIAN_POINT ( 'NONE',  ( 1.171164436615620863, 1.096940724416964885, 1.478650282607060440 ) ) ;
#104586=CARTESIAN_POINT ( 'NONE',  ( 4.013389373331836651, -0.8969206028703354816, -1.491242602974415243 ) ) ;
#104589=ADVANCED_FACE ( 'NONE', ( #152500 ), #24510, .F. ) ;
#104590=CARTESIAN_POINT ( 'NONE',  ( 1.305796196612364124, -0.5247483525172502716, 2.096912610238470975 ) ) ;
#104591=CARTESIAN_POINT ( 'NONE',  ( 3.110703712691643918, 0.7282687159771012997, -1.880146464672841411 ) ) ;
#104593=CARTESIAN_POINT ( 'NONE',  ( 0.6905621207787122628, -2.145541755201633372, -0.2633910710312590275 ) ) ;
#104594=CARTESIAN_POINT ( 'NONE',  ( 1.920718329235811872, 1.838843090712917405, 0.7113003943867537426 ) ) ;
#104595=CARTESIAN_POINT ( 'NONE',  ( 6.609000000000047947, 3.700659725723095761, 2.414405743007182359 ) ) ;
#104596=CARTESIAN_POINT ( 'NONE',  ( 2.349080241353004528, 0.5156090978439072936, -1.872316843566106614 ) ) ;
#104597=CARTESIAN_POINT ( 'NONE',  ( 6.416268857797894576, -1.911816439625917852, 0.05404522429636184067 ) ) ;
#104605=CARTESIAN_POINT ( 'NONE',  ( 0.4291286860223576527, 2.112415399404877547, 0.6383354507134838540 ) ) ;
#104608=CARTESIAN_POINT ( 'NONE',  ( 4.082823661314609609, 1.861412734803047142, 0.6194944872321901386 ) ) ;
#104610=CARTESIAN_POINT ( 'NONE',  ( 1.582657950916711131, -0.6767122143778031562, 1.899619169727875700 ) ) ;
#104612=CARTESIAN_POINT ( 'NONE',  ( 2.430995767774553062, -1.757534028733166442, 1.180493747047051567 ) ) ;
#104615=CARTESIAN_POINT ( 'NONE',  ( 2.906014618889841916, 1.333239036598636185, -1.269987479889052917 ) ) ;
#104619=CARTESIAN_POINT ( 'NONE',  ( 3.709332143218791789, 1.789599998243587731, -1.137392358348317201 ) ) ;
#104620=CARTESIAN_POINT ( 'NONE',  ( 0.3043191165176573620, 1.600368420507289668, 0.9101283655772866021 ) ) ;
#104623=CARTESIAN_POINT ( 'NONE',  ( 4.323548078123999439, -1.973147536489193499, 0.5946332991794788247 ) ) ;
#104626=CARTESIAN_POINT ( 'NONE',  ( 1.065666191918061445, -1.167978014494171823, 1.423405568861766168 ) ) ;
#104631=CARTESIAN_POINT ( 'NONE',  ( 0.7334016978863610037, 0.1661181961954381059, 2.200687262777756725 ) ) ;
#104632=CARTESIAN_POINT ( 'NONE',  ( 3.708526512723071544, -0.9128432734063509635, -2.070237398927244676 ) ) ;
#104634=CARTESIAN_POINT ( 'NONE',  ( 3.111360644411143017, 1.430921235420354654, 1.110905701166440940 ) ) ;
#104635=CARTESIAN_POINT ( 'NONE',  ( 3.995261062014230813, -0.3217480215693402368, 1.888325751980689082 ) ) ;
#104636=CARTESIAN_POINT ( 'NONE',  ( 5.687960312649480876, -1.310561514506687564, -1.602779375087557412 ) ) ;
#104638=CARTESIAN_POINT ( 'NONE',  ( 3.362146542844654196, 0.8852860682435258477, 1.761578244261922332 ) ) ;
#104639=CARTESIAN_POINT ( 'NONE',  ( 1.553604983729965472, 0.5615451523532221101, -1.842721482554928514 ) ) ;
#104640=CARTESIAN_POINT ( 'NONE',  ( 3.643291952642300213, -1.415932857957047375, -1.222571138756740838 ) ) ;
#104641=CARTESIAN_POINT ( 'NONE',  ( 3.809432652880593739, 1.978559473273227232, 1.187534574604662607 ) ) ;
#104642=CARTESIAN_POINT ( 'NONE',  ( 3.613571450151699782, 0.4543224947703514149, -1.804596983994880333 ) ) ;
#104646=CARTESIAN_POINT ( 'NONE',  ( 1.682391906368089662, -1.125439293035620292, 1.779948400507038953 ) ) ;
#104652=CARTESIAN_POINT ( 'NONE',  ( 0.3342475891858322501, -1.084071894752016041, -1.704023929676929727 ) ) ;
#104657=CARTESIAN_POINT ( 'NONE',  ( 1.159701560084012595, 0.4228694819443152286, -2.119656415666733906 ) ) ;
#104661=CARTESIAN_POINT ( 'NONE',  ( 6.559000000000036579, 7.629137130509070275, 2.600000000000001421 ) ) ;
#104664=CARTESIAN_POINT ( 'NONE',  ( 6.280482454654814362, -0.5424645211669875122, -1.942098458069536848 ) ) ;
#104666=CARTESIAN_POINT ( 'NONE',  ( -0.05867695357848409787, -1.698172713885632401, -1.384993232510664640 ) ) ;
#104668=CARTESIAN_POINT ( 'NONE',  ( 0.07556134207191073093, -0.004209888912004143384, -2.244269416743961187 ) ) ;
#104676=CARTESIAN_POINT ( 'NONE',  ( 2.472937804810691809, 0.08526638500995675773, -1.722893361390212874 ) ) ;
#104678=CARTESIAN_POINT ( 'NONE',  ( 2.125891686596991903, 1.023501848097716493, -1.443529828085978739 ) ) ;
#104679=CARTESIAN_POINT ( 'NONE',  ( 2.561191855132368467, -1.672464352163150147, 1.120165047906955147 ) ) ;
#104680=CARTESIAN_POINT ( 'NONE',  ( 5.807716119225245777, -0.5415507062403871474, 2.139171552897000339 ) ) ;
#104682=CARTESIAN_POINT ( 'NONE',  ( 4.254169105220822367, 0.8597269205913078416, -1.827796444439087287 ) ) ;
#104684=CARTESIAN_POINT ( 'NONE',  ( 4.547591073264711348, -1.938359017324686961, 0.8602097090630378418 ) ) ;
#104685=CARTESIAN_POINT ( 'NONE',  ( 3.655875201264874974, 1.122517324909186431, 1.674876314423722423 ) ) ;
#104686=CARTESIAN_POINT ( 'NONE',  ( 4.711091175174894730, 1.502108783192051877, -1.012348896329213765 ) ) ;
#104690=CARTESIAN_POINT ( 'NONE',  ( 0.9185735243398345240, 1.726912363944958617, 0.7195956246372690046 ) ) ;
#104692=CARTESIAN_POINT ( 'NONE',  ( -0.1759689521645991239, -0.7750936178016191169, -1.636263868569738600 ) ) ;
#104697=CARTESIAN_POINT ( 'NONE',  ( 0.1758378621803426134, 1.891278220088285833, -0.2826890867150752551 ) ) ;
#104702=CARTESIAN_POINT ( 'NONE',  ( 3.990573222356631256, -1.218298518170106925, 1.735533685479621502 ) ) ;
#104703=CARTESIAN_POINT ( 'NONE',  ( -0.02968770228140016343, 0.2527710104786498047, -1.861515397111657144 ) ) ;
#104705=CARTESIAN_POINT ( 'NONE',  ( 5.553970887368382847, 1.969207887765548559, -0.09415503477229987539 ) ) ;
#104708=CARTESIAN_POINT ( 'NONE',  ( 0.6330651387380836770, 1.861715503769780566, 0.7666268175344230773 ) ) ;
#104710=CARTESIAN_POINT ( 'NONE',  ( 0.01740989766754827417, -1.933669582450600499, 0.8627405663345076858 ) ) ;
#104713=CARTESIAN_POINT ( 'NONE',  ( 1.609917502266303480, 0.6029389078928657497, -1.980602105166151095 ) ) ;
#104718=CARTESIAN_POINT ( 'NONE',  ( 4.874988757033254849, 1.950858131582337007, -0.7520741601412093136 ) ) ;
#104720=CARTESIAN_POINT ( 'NONE',  ( 3.539906422930443775, 0.8216601389946125433, -1.630302437610211541 ) ) ;
#104721=CARTESIAN_POINT ( 'NONE',  ( 1.875370188833940244, 0.3090493442242334132, -1.784726349569294213 ) ) ;
#104725=CARTESIAN_POINT ( 'NONE',  ( 4.735508036034060453, -2.019198892066270457, 0.8907332283012432406 ) ) ;
#104728=CARTESIAN_POINT ( 'NONE',  ( 3.018110381800835018, -1.909997030407738938, 0.09613604992317337228 ) ) ;
#104731=CARTESIAN_POINT ( 'NONE',  ( 5.986797818411375260, 1.994257276370488219, 0.5558945855626205024 ) ) ;
#104734=CARTESIAN_POINT ( 'NONE',  ( 6.216381822182693639, 2.044192415450503120, 0.7905562269360306704 ) ) ;
#104737=ORIENTED_EDGE ( 'NONE', *, *, #5273, .F. ) ;
#104739=CARTESIAN_POINT ( 'NONE',  ( 3.128041797164154758, 1.042111378005972311, -1.553157497896196393 ) ) ;
#104741=CARTESIAN_POINT ( 'NONE',  ( 6.509000000000010999, 0.004788705324892603143, 2.000274819378269786 ) ) ;
#104745=CARTESIAN_POINT ( 'NONE',  ( 6.877786287229037399, -2.009644702432196617, 0.4970176993947388322 ) ) ;
#104746=CARTESIAN_POINT ( 'NONE',  ( 0.6675924852559199651, 1.356316336250670496, 1.492241973137248934 ) ) ;
#104750=CARTESIAN_POINT ( 'NONE',  ( 1.324469081069843623, 2.112754910877081560, 0.5817525768514880680 ) ) ;
#104751=CARTESIAN_POINT ( 'NONE',  ( 4.705575438601840688, -0.4840451379145363497, 1.760283039881085809 ) ) ;
#104759=CARTESIAN_POINT ( 'NONE',  ( 3.263068207883256466, 1.795673413606920565, -0.4063787724192802209 ) ) ;
#104760=CARTESIAN_POINT ( 'NONE',  ( 6.117445361114795865, 1.676175193246462802, 1.114809878595341308 ) ) ;
#104761=CARTESIAN_POINT ( 'NONE',  ( 1.722429217803717938, -1.971362081364759655, -1.181495133065799230 ) ) ;
#104763=CARTESIAN_POINT ( 'NONE',  ( 6.895372015613538075, -1.753720159772365284, 0.8792710811909019153 ) ) ;
#104766=CARTESIAN_POINT ( 'NONE',  ( 3.269685606991072468, 0.4601866041431811327, -1.856093204100267124 ) ) ;
#104770=CARTESIAN_POINT ( 'NONE',  ( 2.507466893629331395, -2.067604658949507179, 0.3094350269009105703 ) ) ;
#104771=CARTESIAN_POINT ( 'NONE',  ( 1.604156678829884886, -0.6703249191640224813, -1.746612230856612769 ) ) ;
#104772=CARTESIAN_POINT ( 'NONE',  ( 1.897814322125553010, 0.1948091626960517242, 2.006652841580962132 ) ) ;
#104775=CARTESIAN_POINT ( 'NONE',  ( 2.805909833680774845, 1.258924587927259253, -1.202001966437598268 ) ) ;
#104780=CARTESIAN_POINT ( 'NONE',  ( 4.406709194360526993, 1.330975820509268104, -1.097133727364963729 ) ) ;
#104781=CARTESIAN_POINT ( 'NONE',  ( 3.386445149735781257, -0.4294187885149694517, -2.148908265708626697 ) ) ;
#104782=CARTESIAN_POINT ( 'NONE',  ( 0.1934855802202296304, 1.507424494634423517, 0.8570536861387479943 ) ) ;
#104783=FACE_OUTER_BOUND ( 'NONE', #18363, .T. ) ;
#104785=CARTESIAN_POINT ( 'NONE',  ( 4.170888513267295039, 1.539375584636338390, -1.531221199927160770 ) ) ;
#104786=CARTESIAN_POINT ( 'NONE',  ( 2.015964598666186269, -0.8597642540715648707, -1.610575774528985704 ) ) ;
#104787=CARTESIAN_POINT ( 'NONE',  ( 0.4089400952669055567, -1.579117232646386704, 1.163831224039679979 ) ) ;
#104788=CARTESIAN_POINT ( 'NONE',  ( 4.188735998470741073, 1.634407174013367214, -1.345997343221926545 ) ) ;
#104791=CARTESIAN_POINT ( 'NONE',  ( 4.862941710081361002, 0.2263591102839345448, -2.281146386033555462 ) ) ;
#104795=CARTESIAN_POINT ( 'NONE',  ( 0.1707708301344288138, 0.8156354886642532831, 1.957547177562010354 ) ) ;
#104803=CARTESIAN_POINT ( 'NONE',  ( 4.904922738988922504, -1.081064280317966420, -1.701948707654332704 ) ) ;
#104805=CARTESIAN_POINT ( 'NONE',  ( 3.643474114467046387, 1.866637444603681528, -0.8776443792693452428 ) ) ;
#104807=CARTESIAN_POINT ( 'NONE',  ( -0.2411972340276386517, 4.090764154511560058, -2.455280512047691044 ) ) ;
#104811=CARTESIAN_POINT ( 'NONE',  ( 6.263654578238285531, 1.123272483274835087, 1.881548979392036802 ) ) ;
#104812=CARTESIAN_POINT ( 'NONE',  ( 4.078750125433938223, -0.7691220382576718917, 1.864168106189521890 ) ) ;
#104813=CARTESIAN_POINT ( 'NONE',  ( 3.210337823311388394, 1.665856106666419034, 0.7845605768846477535 ) ) ;
#104815=CARTESIAN_POINT ( 'NONE',  ( 0.5863794435163689478, -0.2038549220112067795, -1.712615276990290480 ) ) ;
#104818=CARTESIAN_POINT ( 'NONE',  ( 0.9854702925387841539, -2.298851036028260353, 0.006955682198207107335 ) ) ;
#104820=CARTESIAN_POINT ( 'NONE',  ( 6.368092757517858082, 1.156555634672886246, 1.944455297613384204 ) ) ;
#104821=CARTESIAN_POINT ( 'NONE',  ( 3.211649026191341072, -0.4105298382788050704, 2.065488094592916823 ) ) ;
#104830=CARTESIAN_POINT ( 'NONE',  ( 4.394933515450586192, -2.155188642370196916, -0.5379869938199193236 ) ) ;
#104831=CARTESIAN_POINT ( 'NONE',  ( 2.836070844659248191, 2.175002134116140518, 0.2674123886829762875 ) ) ;
#104834=CARTESIAN_POINT ( 'NONE',  ( 5.810985101215744741, -1.547553103248515027, 1.205733875218002238 ) ) ;
#104838=CARTESIAN_POINT ( 'NONE',  ( 4.236665939827915395, 1.302216991916404387, -1.673619383358643908 ) ) ;
#104841=CARTESIAN_POINT ( 'NONE',  ( 5.998930166150279852, 1.769978137569449883, -1.240765152474863520 ) ) ;
#104843=CARTESIAN_POINT ( 'NONE',  ( 4.897927690869709139, -0.6253142351902387652, -1.731941863025769246 ) ) ;
#104846=CARTESIAN_POINT ( 'NONE',  ( 0.2216635874392547945, 1.664573546290064598, 0.5083179512348577900 ) ) ;
#104847=CARTESIAN_POINT ( 'NONE',  ( 6.827182134110238110, 6.038038905730811479, 2.505852844092556264 ) ) ;
#104851=CARTESIAN_POINT ( 'NONE',  ( 3.995124980148881288, 1.827535992889782523, -1.154293374375232828 ) ) ;
#104854=CARTESIAN_POINT ( 'NONE',  ( 3.450221060135277629, 2.161883445724331665, 0.001893877739161941697 ) ) ;
#104856=CARTESIAN_POINT ( 'NONE',  ( 4.569576162043214929, 1.912950159424832375, -0.4759120794774750474 ) ) ;
#104857=CARTESIAN_POINT ( 'NONE',  ( 3.584998556975723005, 1.101681934899124915, -1.338793912720330770 ) ) ;
#104858=CARTESIAN_POINT ( 'NONE',  ( 0.6619992422990974568, 1.085049530943157148, 1.904046507712559455 ) ) ;
#104859=CARTESIAN_POINT ( 'NONE',  ( 0.7457024085506950284, -1.977219658456253359, 1.189539768987533330 ) ) ;
#104860=CARTESIAN_POINT ( 'NONE',  ( 4.112614458092584968, 1.460029904434188008, -1.454618372460781295 ) ) ;
#104861=CARTESIAN_POINT ( 'NONE',  ( 5.267111086673036624, 1.870628123453799363, -0.5216035295831971119 ) ) ;
#104867=CARTESIAN_POINT ( 'NONE',  ( 3.751171811254182753, -1.805526059370649028, 1.268566889074909554 ) ) ;
#104870=CARTESIAN_POINT ( 'NONE',  ( 1.059155247252058896, 1.517088508067988117, 1.077460967357747990 ) ) ;
#104871=( BOUNDED_SURFACE ( )  B_SPLINE_SURFACE ( 3, 3, ( 
 ( #51819, #99493, #100550, #133089, #4090, #3024, #168753, #68016, #149302, #151452, #53944, #19288, #165550, #85370, #82156, #33414, #17143, #86441, #50733, #119005, #201229, #120081, #166623, #883, #184983, #116859, #152506, #136272, #37692, #70161, #83220, #214250, #198039, #18215, #66949, #134157, #35543, #183931, #101620, #84299, #150384, #1955, #117937, #191389, #169820, #206580, #55013, #170886, #104841, #190326, #71228, #122237, #89662, #23555, #188196, #140568, #41985, #88590, #58209, #22479, #103769, #107017, #105940, #171964, #40911, #38760, #21407, #155714, #139480, #87517, #157862, #74463, #138406, #108094, #153582, #124368, #25696, #39832, #187131, #7297, #73375, #75527, #173041, #205510, #72300, #57141, #5151, #123308, #91804, #59267, #189272, #174123, #9455, #141638, #8380, #207647, #137343, #154647, #125423, #203361, #121162, #6229, #204425, #24624, #56080, #90731, #156794, #46245, #163188, #159980, #43055, #113432, #45184, #145897, #11582, #126494, #78713, #77654, #111298, #210847, #13711, #158915, #194601, #96069, #12643, #143776, #44111, #209771, #142696, #130748, #146953, #192457, #76585, #79784, #162122, #61411, #109168, #175181, #62473, #128635, #47319, #177302, #127574, #28916, #10511, #26767, #112362, #14772, #92869, #212968, #193542, #31059, #80863, #110232, #211907, #161047, #129700, #208706, #95001, #63544, #64608, #178375, #195682, #29984, #27842, #60333, #93939, #144841, #179439, #176240, #97135, #50489, #81917, #199916, #51563, #200967, #100300, #151197, #84044, #115546, #166366, #3827, #33169, #69900, #98195, #198842, #17957, #196742, #16894, #134959, #164243, #214015, #15831, #34227, #181541, #2768, #150132, #52614, #68839, #114495, #19031, #48382, #180492, #102429, #148004, #117688, #82975, #1705, #116610, #66691, #85111, #67759, #20097, #183680, #182603, #118743, #133910, #184727, #36351, #624, #35285, #101361, #168498, #32110, #167439, #65637, #86185, #152254, #131785, #197789, #49426, #99251, #165299, #149048, #132838, #21147, #171695, #70969, #72038, #104582, #190079, #189014, #8127, #39566, #120899, #123060, #25442, #139213, #137079, #205244, #136011, #87251, #153316, #140308, #170627, #24359, #40657, #91548, #138151, #186872, #106758, #22213, #156536, #107840, #157606, #172786, #4891, #202024, #169565, #88326, #206326, #105668, #7036, #155453, #73113, #53684, #56885, #90469, #204160, #9202, #119815, #74213, #203104, #54749, #38504, #57951, #103505, #154390, #121970, #55815, #5968, #124116, #41731, #187936, #173867, #23294, #89404, #185795, #37428, #143517, #159724, #76336, #27584, #195431, #142443, #126240, #92621, #160795, #113178, #29733, #45995, #109980, #127316, #209513, #179182, #158663, #208450, #193286, #61154, #75274, #44931, #11322, #60083, #93682, #47061, #192202, #43864, #112115, #94748, #178118, #125174, #111039, #177046, #59018, #129449, #95815, #175990, #161873, #191135, #13461, #211651, #77401, #10261, #28662, #12387, #30805, #78466, #144585, #210599, #62228, #207399, #128386, #63288, #96885, #194353, #79537, #145655, #162934, #141389, #42801, #108909, #174932, #26512, #203648, #170101, #202582, #130503, #370, #153871, #81662, #98993, #17698, #137631, #131534, #14515, #87797, #16640, #120372, #197536, #97943, #50234, #49181, #82724, #182345, #54234, #196490, #166113 ),
 ( #70445, #115299, #80608, #146702, #33974, #100049, #21687, #148801, #181289, #66444, #48132, #212717, #83785, #55299, #64357, #187418, #32916, #5440, #121449, #163999, #136561, #132585, #104055, #114245, #165048, #186347, #39049, #149879, #71519, #1445, #213766, #180242, #65387, #198588, #116355, #105134, #37982, #31866, #15574, #147748, #174402, #175459, #74748, #125710, #58495, #89951, #7588, #189554, #107308, #204713, #23843, #141917, #205798, #8667, #91016, #208984, #188489, #57428, #109453, #72595, #40119, #56363, #140851, #156001, #191669, #206863, #27043, #43334, #88881, #207929, #192738, #22764, #76865, #138696, #25980, #123590, #124651, #24910, #41201, #59551, #190608, #60620, #158143, #157078, #93152, #173332, #159189, #10790, #42266, #108379, #92087, #142984, #154934, #9734, #171174, #75809, #126781, #44393, #122526, #106230, #6519, #172256, #73673, #139772, #210055, #146172, #45461, #46525, #79001, #164528, #163471, #197020, #13986, #95289, #97416, #214289, #113718, #111578, #179722, #110514, #61694, #127863, #114773, #145117, #213255, #15051, #65923, #112647, #161338, #81144, #211123, #131030, #82197, #132070, #147229, #193813, #176514, #144060, #62747, #180770, #80069, #195970, #129982, #47604, #28126, #31339, #64884, #178656, #198081, #94220, #48656, #177586, #29200, #12921, #32398, #77939, #128907, #96353, #30267, #194888, #98464, #16114, #162408, #148291, #212187, #63824, #160260, #11861, #117975, #134193, #50774, #1992, #169855, #116902, #166665, #182901, #18255, #149345, #137380, #153619, #133130, #83259, #20394, #102733, #150427, #49708, #181823, #3060, #69130, #53981, #51855, #68056, #183968, #17184, #33455, #52906, #21443, #99532, #5191, #200202, #37727, #87551, #199129, #168789, #167727, #136309, #165592, #84339, #86478, #71266, #201265, #202330, #135252, #34517, #924, #100590, #35579, #101659, #115837, #152542, #19328, #66992, #119039, #185022, #120117, #85406, #4128, #151491, #36648, #70196, #186097, #103806, #59306, #38797, #155753, #123344, #203396, #55049, #90768, #7338, #58246, #173080, #124403, #104878, #205544, #189309, #170921, #9493, #190361, #172004, #108132, #22517, #42023, #157899, #89703, #72339, #73415, #139518, #141674, #156829, #40948, #105981, #57182, #88628, #24661, #91841, #121199, #8416, #25731, #174159, #187168, #75565, #207686, #204463, #23594, #154684, #6268, #138445, #56117, #107054, #206618, #122274, #74502, #140606, #188232, #39872, #18496, #84574, #2224, #68299, #82433, #198306, #185258, #49946, #48890, #169023, #148523, #150662, #116067, #199370, #17415, #167960, #89, #115010, #66154, #149581, #53143, #166903, #134433, #200435, #52082, #181007, #118209, #19566, #51016, #136545, #32627, #151726, #132299, #182057, #33687, #135475, #16353, #67229, #34745, #183140, #133363, #85640, #201497, #99764, #3298, #165831, #184196, #117137, #98704, #100818, #35819, #83499, #1165, #20621, #101895, #69366, #119273, #36882, #102965, #86709, #152778, #4360, #70429, #164763, #25965, #5425, #22747, #140835, #104039, #71504, #21672, #40103, #187401, #157063, #23829, #206848, #74730, #120355, #24894, #9719, #54217, #108363, #170085, #205782, #88865, #106215, #56349, #72579, #91000, #89934, #92070, #189538, #122511, #124636, #204699, #8651, #190593, #6504, #172241, #57411, #87780 ),
 ( #155985, #173315, #153854, #139758, #41186, #7573, #105117, #203631, #171157, #137615, #75795, #158128, #55283, #121432, #58480, #107293, #154920, #202565, #186332, #73658, #123576, #42250, #188472, #138680, #174387, #39033, #37966, #145101, #47586, #125694, #97397, #191653, #163453, #94203, #129962, #113700, #10774, #46505, #45445, #13967, #43318, #176497, #112628, #15033, #78982, #80051, #161318, #126761, #109436, #192721, #28108, #77920, #31321, #178638, #210036, #27027, #211105, #62729, #146154, #111560, #96334, #29181, #60602, #177568, #141903, #44375, #207913, #175442, #144039, #95270, #59534, #93135, #128890, #61676, #30250, #12902, #162390, #159174, #127844, #194871, #76848, #195950, #212170, #160243, #63804, #142967, #179704, #208970, #11843, #110498, #193796, #149326, #52888, #18236, #116883, #49690, #83241, #213235, #100572, #3043, #36629, #34498, #19309, #183950, #119023, #200184, #35560, #197004, #82179, #51837, #185005, #85388, #117955, #48639, #66973, #69112, #148273, #165572, #114757, #133112, #182882, #147210, #151472, #904, #101641, #198061, #164511, #166645, #115818, #199109, #84320, #167707, #180754, #150406, #134176, #50754, #181805, #214272, #33438, #32381, #168771, #102714, #16095, #98447, #135234, #201247, #99515, #81125, #64867, #1973, #68036, #131012, #65905, #17167, #132051, #202312, #4110, #23575, #140586, #156810, #87534, #104860, #53961, #6250, #122254, #86461, #90750, #22497, #123325, #137362, #103787, #56098, #203379, #88609, #188213, #205527, #136291, #171983, #73396, #204444, #55032, #21425, #121180, #120099, #108112, #124384, #169838, #186077, #57162, #139499, #187149, #20376, #152525, #39853, #105959, #24640, #154664, #38778, #72319, #37711, #70179, #89684, #206598, #153601, #190342, #170904, #8397, #58226, #5173, #189288, #138425, #107034, #71246, #155733, #40930, #42004, #7318, #173060, #74481, #161882, #9472, #13469, #63297, #113187, #66453, #81671, #30815, #59285, #180251, #31875, #181299, #80618, #131543, #64366, #95823, #146711, #198597, #79545, #50244, #75545, #179191, #212727, #174139, #25713, #97954, #96894, #147757, #196499, #213775, #141654, #162943, #130512, #157879, #16649, #65397, #211659, #49190, #207666, #197545, #99002, #195440, #43072, #47070, #14524, #148810, #114255, #48142, #145663, #164008, #91822, #15584, #165057, #132595, #115309, #32926, #82734, #379, #125444, #191405, #109185, #178126, #29741, #129457, #54507, #87001, #17707, #102189, #166122, #101109, #2520, #52376, #5715, #20905, #184487, #1454, #119569, #185556, #120651, #19855, #70720, #3586, #35035, #85942, #137907, #167195, #203926, #83794, #118505, #152015, #116364, #182354, #37185, #36104, #153073, #135769, #4650, #149889, #168256, #69661, #100058, #170379, #136833, #150956, #202859, #67519, #186630, #38257, #134719, #199665, #200725, #201792, #88074, #53432, #103260, #84868, #169321, #33982, #104331, #21966, #71792, #154148, #133664, #51311, #117437, #183434, #18782, #68593, #56644, #26259, #27331, #208205, #92375, #171455, #41481, #191947, #122808, #140051, #89160, #107592, #157358, #121728, #125990, #57710, #158412, #172536, #138977, #91300, #24120, #123867, #8947, #10012, #23044, #207149, #108657, #25196, #90223, #188767, #156287, #155213, #143271, #159473, #205000, #6794, #76088, #174685, #7871, #55574 ),
 ( #39322, #11071, #73959, #43613, #175738, #40407, #142190, #173624, #59837, #105417, #206076, #109731, #77150, #58772, #93433, #75027, #106509, #124927, #72871, #189832, #187693, #141139, #190888, #42554, #14264, #28408, #144342, #131303, #210342, #209261, #115053, #94502, #30556, #61981, #145408, #177871, #48935, #47890, #81422, #112929, #194099, #196246, #98747, #212469, #128135, #64113, #60906, #160540, #12146, #213524, #29483, #97695, #114002, #164804, #211408, #45748, #179997, #95574, #15333, #181051, #16396, #31621, #78219, #127065, #111866, #161624, #65147, #178942, #80355, #146454, #130255, #193027, #163753, #147503, #63038, #82475, #44679, #197294, #13217, #79290, #129205, #32667, #176793, #195182, #46815, #96635, #162689, #110791, #20659, #133407, #103006, #149624, #52124, #2266, #148565, #68342, #18538, #1206, #100861, #54258, #67268, #199412, #166945, #84615, #182099, #51057, #119313, #183182, #200478, #134475, #186370, #165872, #34786, #86750, #49989, #17458, #33729, #118253, #117181, #169062, #184234, #152821, #4397, #66199, #185299, #170126, #131, #120395, #116107, #151768, #150704, #35858, #101937, #168002, #36923, #19608, #38005, #135515, #85680, #70468, #3338, #136585, #202605, #69408, #201537, #104077, #53185, #21711, #132343, #198349, #99807, #83543, #58518, #122551, #139795, #7614, #125733, #105158, #188512, #26002, #203673, #171197, #121473, #205823, #72621, #42291, #123615, #92111, #174426, #5463, #124673, #109474, #153894, #207953, #55322, #91040, #40142, #57455, #156025, #172279, #190630, #189578, #191694, #74772, #73697, #9758, #89973, #108402, #75833, #106255, #41226, #157100, #187444, #22787, #206886, #107331, #173355, #24937, #8689, #39072, #88904, #141940, #154957, #87822, #59576, #6543, #140875, #138720, #23866, #56387, #43354, #158167, #175482, #71543, #204738, #137653, #131047, #30289, #28148, #96374, #27070, #192760, #126804, #31357, #61716, #129999, #80087, #197037, #29221, #11884, #146191, #210077, #47622, #213271, #48672, #212206, #44417, #93177, #60642, #127884, #97432, #145139, #112666, #46546, #178674, #159211, #162426, #63842, #95311, #114789, #10812, #195989, #110537, #94243, #160282, #113734, #209005, #45485, #12943, #161360, #111601, #179740, #163487, #77960, #15069, #144081, #211145, #79022, #76887, #62767, #177609, #193835, #128931, #81161, #194908, #14003, #147244, #143007, #64900, #176537, #181836, #133144, #86490, #33471, #17198, #199144, #116917, #214305, #99545, #151504, #942, #18272, #100604, #4141, #198095, #67007, #119051, #82213, #49722, #65936, #84354, #165608, #135265, #2006, #185036, #52920, #98478, #3072, #202341, #32412, #152554, #148306, #183983, #50788, #150444, #34533, #182917, #69144, #68072, #70211, #167742, #166680, #102746, #134208, #201279, #168802, #200217, #51869, #35594, #132085, #115851, #85420, #117990, #101672, #19341, #36661, #83272, #149360, #20407, #136323, #180789, #53993, #164544, #16129, #55061, #56129, #88641, #174176, #173095, #206632, #23608, #104894, #107070, #9510, #123358, #121212, #189323, #120132, #71278, #5205, #124419, #154698, #8429, #24676, #75582, #122288, #170933, #90782, #6281, #140620, #91859, #141691, #156845, #137392, #186109, #153632, #72353, #190378, #89716, #205558, #139533, #57198, #37742, #40963, #74517, #188245, #207705 ),
 ( #58263, #42037, #22532, #105996, #7351, #103818, #108150, #39886, #25747, #138457, #203409, #155767, #204476, #172017, #73430, #157915, #21456, #169865, #87564, #187181, #38808, #60385, #27895, #158968, #147002, #163238, #142751, #92922, #30033, #112412, #160031, #59325, #191444, #12689, #78765, #63594, #61459, #11633, #193589, #26818, #43109, #62522, #179489, #109224, #14820, #77706, #47369, #31111, #208760, #178424, #177353, #145945, #175234, #93990, #96119, #80912, #210895, #211956, #144888, #44162, #10562, #110282, #143826, #209823, #125482, #162174, #127625, #76637, #128684, #194653, #129749, #28967, #13760, #161101, #192510, #95050, #126549, #176291, #45233, #111348, #46297, #79836, #195734, #113482, #97184, #679, #183729, #18009, #35337, #48431, #132887, #34277, #196790, #52665, #101416, #33218, #85165, #114546, #167489, #135008, #16944, #81966, #83023, #66745, #184781, #150186, #100350, #181589, #198890, #130796, #84099, #201021, #168550, #166416, #151249, #19084, #36407, #117738, #2817, #180538, #214059, #68889, #102486, #118794, #20149, #32161, #50536, #86234, #65687, #149098, #98238, #1755, #67812, #99302, #116659, #164293, #133959, #213020, #64655, #199967, #15882, #148053, #131835, #197842, #49475, #115595, #165349, #182657, #51615, #90520, #123109, #53737, #138202, #74261, #4942, #22266, #185848, #204214, #39615, #3881, #8177, #154442, #40702, #54805, #21200, #187990, #120953, #6022, #105719, #189067, #119869, #89455, #205298, #122023, #186924, #153371, #38555, #37480, #25493, #41779, #87302, #103557, #106806, #56936, #104632, #152305, #69952, #171748, #23344, #156583, #72092, #170679, #55866, #169616, #136064, #155507, #57999, #202077, #107892, #88375, #140354, #124163, #71018, #172835, #7089, #24406, #137131, #73162, #206372, #173920, #139268, #190125, #203160, #76379, #141437, #142487, #192246, #27628, #195476, #210644, #159768, #191180, #94792, #160840, #95863, #209557, #46040, #193330, #10305, #61202, #113225, #208494, #179229, #207443, #93728, #127360, #91600, #157651, #12432, #11367, #62270, #111084, #128431, #59062, #77446, #44976, #75320, #145700, #194397, #126287, #178164, #125221, #112161, #13510, #110022, #174975, #176036, #143564, #63336, #42848, #9249, #108955, #43908, #161919, #177090, #28706, #78512, #144629, #26557, #29779, #79582, #211699, #92664, #158708, #129495, #60129, #47109, #31915, #117481, #212768, #49232, #16691, #165100, #115351, #67562, #183472, #15630, #199711, #97993, #148849, #99045, #30855, #82777, #181342, #164051, #197588, #150997, #81717, #147799, #32969, #422, #64404, #213817, #1496, #65435, #66494, #132634, #68636, #48182, #131586, #35079, #146750, #114294, #130548, #198640, #50288, #51357, #116407, #101150, #167236, #162982, #133705, #52419, #96932, #2565, #196539, #34026, #182397, #100100, #166160, #17747, #18824, #83836, #134760, #149927, #84909, #200768, #118545, #14562, #80659, #180292, #91074, #190664, #88938, #56423, #92148, #157135, #8726, #140909, #206922, #6576, #122584, #109508, #188546, #184527, #93212, #72656, #74808, #40176, #123650, #156059, #27105, #26036, #59613, #58551, #172310, #174460, #76918, #42324, #106290, #108440, #36148, #138752, #204770, #191731, #7647, #75866, #158202, #143044, #189612, #23899, #9791, #73732, #207985, #159244, #209039, #141973 ),
 ( #125769, #43387, #154991, #173389, #175515, #90005, #57489, #139828, #24972, #124705, #102229, #10844, #41258, #60675, #205857, #107368, #168300, #22823, #128966, #80123, #97466, #28182, #63879, #179774, #96411, #29256, #127918, #95348, #11922, #214340, #16164, #210111, #160318, #163522, #31391, #12982, #126838, #44453, #146228, #212245, #131083, #194946, #79056, #46582, #94277, #110570, #130033, #32448, #176572, #82249, #145174, #114823, #98517, #61751, #15109, #30327, #213308, #77995, #161398, #81198, #148340, #196024, #64933, #47660, #111636, #144117, #177647, #211179, #62805, #192795, #147276, #112701, #193871, #113771, #197072, #48709, #162461, #180821, #14037, #45520, #164579, #178711, #116953, #153670, #181872, #68108, #101706, #65970, #132119, #69178, #134244, #36696, #85454, #102781, #115887, #200251, #167778, #49761, #120167, #168838, #100638, #152589, #33508, #20442, #202380, #84391, #149395, #150478, #51903, #37778, #3107, #19374, #34567, #118025, #198129, #151539, #165645, #135298, #977, #2038, #166715, #186143, #119090, #4176, #184013, #50826, #52952, #169900, #201312, #67043, #185070, #99581, #17233, #83308, #70245, #18305, #86524, #136360, #21489, #35628, #182952, #54030, #103852, #87599, #133180, #199180, #124454, #104930, #71314, #38847, #106032, #9541, #123394, #90815, #24713, #156879, #137426, #8466, #190413, #7388, #92955, #203445, #108183, #170972, #72393, #6319, #91894, #187218, #23647, #205596, #139569, #89755, #42069, #157950, #204514, #174209, #138493, #189358, #73468, #5238, #57233, #155805, #56162, #172054, #125515, #122326, #188283, #40998, #107109, #22571, #39924, #25782, #173132, #74552, #140653, #43145, #88677, #206666, #75616, #121248, #154736, #58298, #141727, #207735, #59358, #191477, #109258, #175266, #55099, #26851, #180569, #10595, #64683, #126582, #162205, #45262, #62551, #12722, #28999, #47402, #194685, #196821, #145975, #78795, #80940, #161134, #113514, #147032, #177385, #128714, #13792, #60422, #27929, #63628, #46327, #112443, #178456, #30065, #192543, #94023, #213054, #160062, #159002, #130829, #96154, #79866, #211987, #76671, #129782, #195763, #144918, #32191, #142786, #179522, #110316, #11666, #77740, #31141, #44196, #95086, #210925, #97216, #163268, #14850, #48463, #143861, #114577, #209854, #208792, #176323, #61492, #127657, #193621, #111382, #50569, #3917, #165382, #149132, #116691, #34308, #131866, #16975, #68922, #132918, #150218, #18045, #136098, #115625, #198923, #36444, #214090, #181620, #197873, #1790, #83056, #52697, #133994, #102518, #184814, #15915, #135043, #119907, #164325, #69986, #65718, #101448, #182690, #67847, #166455, #100383, #201056, #200000, #202114, #85197, #84132, #20181, #51650, #118828, #86268, #117773, #183764, #167521, #49505, #33249, #2853, #35374, #19118, #151282, #168581, #99333, #713, #152339, #66777, #98267, #53774, #185882, #81998, #148085, #188024, #6059, #91635, #90558, #124198, #155548, #22302, #24445, #141470, #40737, #38591, #106843, #37517, #203195, #137171, #41816, #72130, #140391, #156620, #207477, #39653, #88413, #8210, #138237, #58034, #9285, #59097, #74295, #54841, #103593, #71055, #204251, #107929, #7127, #73200, #55903, #105762, #169650, #56973, #173953, #125257, #205335, #190162, #206410, #75358, #25527, #157687, #153408, #104668 ),
 ( #139306, #21235, #87340, #171787, #4977, #154481, #120992, #123147, #122060, #23382, #189104, #186959, #170716, #172874, #89494, #160876, #93760, #192279, #159799, #76409, #64438, #80694, #60164, #10335, #161953, #29816, #77480, #191217, #108989, #144663, #210677, #195508, #193365, #143599, #111120, #158741, #175008, #194432, #96967, #26594, #146785, #209591, #179266, #163015, #126318, #95900, #94825, #63372, #92695, #11402, #13544, #212800, #128464, #129528, #62305, #176067, #142519, #27665, #61237, #127393, #42880, #79615, #45010, #208528, #46073, #112194, #47145, #12470, #145734, #78545, #110055, #178199, #43939, #177123, #28740, #211734, #113261, #30889, #14597, #68669, #34058, #16723, #1530, #116437, #67593, #114326, #148884, #132668, #48214, #101184, #133738, #115384, #199745, #180322, #51391, #35113, #33002, #81750, #99080, #82808, #18858, #100131, #2600, #131620, #130582, #31944, #457, #50319, #196572, #98028, #117512, #182431, #167273, #149961, #84942, #147832, #166192, #17782, #213850, #164082, #151031, #66525, #15663, #197619, #65469, #49263, #83870, #198674, #183505, #181378, #165132, #46775, #145369, #78177, #111826, #27289, #129162, #31579, #65108, #62993, #47848, #212427, #147463, #14219, #64069, #11031, #110754, #80314, #81379, #113959, #146414, #77109, #95536, #97653, #176752, #194055, #143233, #161585, #211368, #175699, #179956, #177828, #130213, #12107, #192985, #195139, #196206, #15294, #209223, #112889, #44639, #45707, #144305, #163712, #162646, #213484, #13173, #94462, #96596, #131264, #178901, #28367, #30515, #109695, #60865, #127027, #197251, #210299, #93396, #159432, #160502, #29445, #61939, #128097, #79251, #209662, #143669, #210743, #79683, #46143, #178271, #141535, #177192, #176136, #144732, #107991, #92763, #28808, #13608, #61303, #62367, #77546, #42947, #174020, #109056, #158808, #208596, #162019, #94892, #126388, #157753, #127465, #193436, #128529, #27736, #12537, #159871, #191281, #93830, #60228, #10404, #192347, #25589, #41880, #45080, #111189, #160944, #194498, #145796, #112257, #29881, #207543, #78610, #11475, #95965, #91701, #76477, #58103, #124262, #190221, #9351, #75423, #175073, #59163, #26660, #142588, #44005, #125321, #110124, #65537, #97032, #521, #66589, #1594, #115449, #166260, #99146, #130646, #181439, #18922, #48278, #85007, #113329, #213914, #33068, #211802, #63440, #132733, #131683, #182495, #16789, #34123, #47214, #197685, #165196, #195578, #51455, #100194, #32010, #83935, #179336, #17850, #133801, #15730, #80760, #81815, #49330, #183570, #148950, #82872, #180386, #198736, #129590, #50383, #199811, #167336, #116504, #150025, #67655, #35176, #117575, #101253, #30957, #212868, #163086, #14667, #146849, #64503, #196638, #114391, #98093, #164145, #147898, #184627, #136976, #38394, #2662, #6931, #153213, #39460, #53577, #188903, #103398, #105555, #169458, #104474, #121862, #52509, #88216, #204056, #120791, #119711, #152152, #185693, #36244, #24253, #40545, #19993, #102323, #187833, #55708, #37323, #151098, #68735, #170521, #22103, #155348, #186768, #134856, #200862, #154287, #4783, #171590, #5861, #23183, #118642, #70861, #71933, #168396, #205137, #89297, #21045, #73010, #86077, #139109, #56780, #87142, #3722, #203003, #54643, #122946, #138043, #106649, #172676, #69797, #135906, #201924 ) ),
 .UNSPECIFIED., .T., .F., .F. ) 
 B_SPLINE_SURFACE_WITH_KNOTS ( ( 4, 3, 4 ),
 ( 4, 1, 1, 1, 1, 1, 1, 1, 1, 1, 1, 1, 1, 1, 1, 1, 1, 1, 1, 1, 1, 1, 1, 1, 1, 1, 1, 1, 1, 1, 1, 1, 1, 1, 1, 1, 1, 1, 1, 1, 1, 1, 1, 1, 1, 1, 1, 1, 1, 1, 1, 1, 1, 1, 1, 1, 1, 1, 1, 1, 1, 1, 1, 1, 1, 1, 1, 1, 1, 1, 1, 1, 1, 1, 1, 1, 1, 1, 1, 1, 1, 1, 1, 1, 1, 1, 1, 1, 1, 1, 1, 1, 1, 1, 1, 1, 1, 1, 1, 1, 1, 1, 1, 1, 1, 1, 1, 1, 1, 1, 1, 1, 1, 1, 1, 1, 1, 1, 1, 1, 1, 1, 1, 1, 1, 1, 1, 1, 1, 1, 1, 1, 1, 1, 1, 1, 1, 1, 1, 1, 1, 1, 1, 1, 1, 1, 1, 1, 1, 1, 1, 1, 1, 1, 1, 1, 1, 1, 1, 1, 1, 1, 1, 1, 1, 1, 1, 1, 1, 1, 1, 1, 1, 1, 1, 1, 1, 1, 1, 1, 1, 1, 1, 1, 1, 1, 1, 1, 1, 1, 1, 1, 1, 1, 1, 1, 1, 1, 1, 1, 1, 1, 1, 1, 1, 1, 1, 1, 1, 1, 1, 1, 1, 1, 1, 1, 1, 1, 1, 1, 1, 1, 1, 1, 1, 1, 1, 1, 1, 1, 1, 1, 1, 1, 1, 1, 1, 1, 1, 1, 1, 1, 1, 1, 1, 1, 1, 1, 1, 1, 1, 1, 1, 1, 1, 1, 1, 1, 1, 1, 1, 1, 1, 1, 1, 1, 1, 1, 1, 1, 1, 1, 1, 1, 1, 1, 1, 1, 1, 1, 1, 1, 1, 1, 1, 1, 1, 1, 1, 1, 1, 1, 1, 1, 1, 1, 1, 1, 1, 1, 1, 1, 1, 1, 1, 1, 1, 1, 1, 1, 1, 1, 1, 1, 1, 1, 1, 1, 1, 1, 1, 1, 1, 1, 1, 1, 1, 1, 1, 1, 1, 1, 1, 1, 1, 1, 1, 1, 1, 1, 1, 1, 1, 1, 1, 1, 1, 1, 1, 1, 1, 1, 1, 1, 1, 1, 1, 1, 1, 1, 1, 1, 1, 1, 1, 1, 1, 1, 1, 1, 1, 1, 1, 1, 1, 1, 1, 1, 1, 1, 1, 1, 1, 1, 4 ),
 ( 0.000000000000000000, 0.5000000000000000000, 1.000000000000000000 ),
 ( 0.000000000000000000, 0.002599909708945224215, 0.005208776875251038344, 0.007813105021672143990, 0.01041684075506122895, 0.01302033053878596733, 0.01562516449037322508, 0.01822901888718816976, 0.02083333248856494152, 0.02343767784666880849, 0.02604151204071371642, 0.02864616705684025488, 0.03124974664057501156, 0.03385445107693609706, 0.03645811663825353210, 0.03906264587105176544, 0.04166673705245293319, 0.04427082116499847508, 0.04687535697974040683, 0.04947901875943551409, 0.05208372524935509645, 0.05468730636643894666, 0.05729195276349181160, 0.05989578571700067411, 0.06250012971910297310, 0.06510448174046053194, 0.06770830932160050442, 0.07031296016926287529, 0.07291653972921435800, 0.07552124384959360559, 0.07812490789241745281, 0.08072943556986492131, 0.08333352577934262373, 0.08593760861062926804, 0.08854214333088818167, 0.09114580385899402615, 0.09375050919907033931, 0.09635408915385039463, 0.09895873428887830281, 0.1015625661591952889, 0.1041669088510773916, 0.1067712598504420435, 0.1093750861808121810, 0.1119797359579501050, 0.1145833143474069837, 0.1171880172914337714, 0.1197916802446672702, 0.1223962066585842084, 0.1250002958591681090, 0.1276043774339237491, 0.1302089111537957367, 0.1328125705047451810, 0.1354172747579587832, 0.1380208536162275679, 0.1406254975582941213, 0.1432293284131295197, 0.1458336698625422867, 0.1484380199076493767, 0.1510418450546419100, 0.1536464938294531402, 0.1562500711155297428, 0.1588547729514310503, 0.1614584348822658832, 0.1640629601007041471, 0.1666670483599762276, 0.1692711287458052438, 0.1718756615333107141, 0.1744793197742946778, 0.1770840230088624179, 0.1796876008377196188, 0.1822922436549848091, 0.1848960735616705098, 0.1875004138364584350, 0.1901047629951247708, 0.1927085870260826783, 0.1953132348667029061, 0.1979168111164897881, 0.2005215119124719170, 0.2031251728880697216, 0.2057296969790492203, 0.2083337843645647058, 0.2109378636290424602, 0.2135423955521746908, 0.2161460527503557827, 0.2187507550344668650, 0.2213543319009846355, 0.2239589736615800464, 0.2265628026874214052, 0.2291671418554001027, 0.2317714901954165685, 0.2343753131776551424, 0.2369799601521939414, 0.2395835354327550959, 0.2421882352569974250, 0.2447918953444941648, 0.2473964183760076208, 0.2500005049552969649, 0.2526045831659717300, 0.2552091142926994904, 0.2578127705152143956, 0.2604174719170327390, 0.2630210478882585856, 0.2656256886602897938, 0.2682295168725681855, 0.2708338550015275126, 0.2734382025906618163, 0.2760420245914711468, 0.2786466707680146371, 0.2812502451463897990, 0.2838549440670474211, 0.2864586033335557724, 0.2890631253735708728, 0.2916672112141422968, 0.2942712884385379479, 0.2968758188368077477, 0.2994794741507696423, 0.3020841747384366283, 0.3046877498813952978, 0.3072923897329448151, 0.3098962171989202430, 0.3125005543566263810, 0.3151049012626256918, 0.3177087223492732204, 0.3203133677958864278, 0.3229169413390938770, 0.3255216394243000688, 0.3281252979369121969, 0.3307298190533745630, 0.3333339042227165261, 0.3359379805283350118, 0.3385425102660742369, 0.3411461647385755636, 0.3437508645802123675, 0.3463544389619092612, 0.3489590779610384774, 0.3515629047479519320, 0.3541672410021501904, 0.3567715872927431642, 0.3593754075324762653, 0.3619800523172059803, 0.3645836250922447341, 0.3671883224101137877, 0.3697919802359038166, 0.3723965004967392245, 0.3750005850623230885, 0.3776046605166471504, 0.3802091896617659783, 0.3828128433598806946, 0.3854175425235913388, 0.3880211162110140388, 0.3906257544257662473, 0.3932295806008425099, 0.3958339160192597128, 0.3984382617621595180, 0.4010420812222079689, 0.4036467254130849946, 0.4062502974869375283, 0.4088549941055670267, 0.4114586513115932598, 0.4140631707847102772, 0.4166672548139925825, 0.4192713294844879757, 0.4218758581048823730, 0.4244795110956688933, 0.4270842096495421902, 0.4296877827096635682, 0.4322924202080664635, 0.4348962458385162155, 0.4375005804888632555, 0.4401049257517701263, 0.4427087444993486054, 0.4453133881643903114, 0.4479169596040251111, 0.4505216555914985932, 0.4531253122448062887, 0.4557298309980991058, 0.4583339145585244578, 0.4609379885126426157, 0.4635425166761967808, 0.4661461690266998081, 0.4687508670388120247, 0.4713544395385928509, 0.4739590763886608604, 0.4765629015416836811, 0.4791672354916582388, 0.4817715803422617515, 0.4843753984445725025, 0.4869800416517858221, 0.4895836125241597725, 0.4921883079485492862, 0.4947919641161733773, 0.4973964822175238609, 0.5000005653765271507, 0.5026046386817077938, 0.5052091664562964324, 0.5078128182335502894, 0.5104175157719683664, 0.5130210877783591972, 0.5156257240480961457, 0.5182295487908826770, 0.5208338821081714975, 0.5234382266141532902, 0.5260420441383883983, 0.5286466869557716608, 0.5312502573278325979, 0.5338549522572011430, 0.5364586080061681805, 0.5390631255234488162, 0.5416672083484578293, 0.5442712810721315186, 0.5468758085256230084, 0.5494794597966533578, 0.5520841569294364648, 0.5546877285093810839, 0.5572923642667827471, 0.5598961886665174692, 0.5625005214187991376, 0.5651048656478350196, 0.5677086826611791315, 0.5703133251567252815, 0.5729168950954143247, 0.5755215895978186280, 0.5781252449951498340, 0.5807297619962258350, 0.5833338445546641937, 0.5859379167642547737, 0.5885424439645127181, 0.5911460947963396162, 0.5937507915915425372, 0.5963543628119793993, 0.5989589981250363904, 0.6015628222488997867, 0.6041671545038470592, 0.6067714985236103420, 0.6093753150932430529, 0.6119799573349418154, 0.6145835269071964202, 0.6171882210506893784, 0.6197918761634028106, 0.6223963927161352272, 0.6250004750754242222, 0.6276045468383509851, 0.6302090738532378777, 0.6328127243128783830, 0.6354174208385534595, 0.6380209917664191321, 0.6406256267031188445, 0.6432294506182901772, 0.6458337824435727015, 0.6484381263217364744, 0.6510419425148348260, 0.6536465845706755928, 0.6562501538434313275, 0.6588548476960643940, 0.6614585025911776661, 0.6640630187634258830, 0.6666671009909873602, 0.6692711723746683772, 0.6718756992720475996, 0.6744793494265174383, 0.6770840457507175669, 0.6796876164529486175, 0.6822922510812780006, 0.6848960748549377531, 0.6875004063182246217, 0.6901047501224634173, 0.6927085660062048955, 0.6953132079441787239, 0.6979167769843723779, 0.7005214706141982273, 0.7031251253587310623, 0.7057296412183544643, 0.7083337233816132672, 0.7109377944534676086, 0.7135423213012055399, 0.7161459712175226588, 0.7187506674083037339, 0.7213542379518396164, 0.7239588723397878400, 0.7265626960391206035, 0.7291670272080824633, 0.7317713710060759214, 0.7343751866476402324, 0.7369798285357428425, 0.7395833974103146469, 0.7421880908853900616, 0.7447917455463664016, 0.7473962611612280371, 0.7500003433276148934, 0.7526044141550642941, 0.7552089410210337528, 0.7578125907662203176, 0.7604172868916432293, 0.7630208573434285046, 0.7656254915589897347, 0.7682293152511859846, 0.7708336461934980344, 0.7734379900529331220, 0.7760418055195050790, 0.7786464474257392965, 0.7812500162016354777, 0.7838547095900232353, 0.7864583642344741277, 0.7890628796724428184, 0.7916669619093961163, 0.7942710325598689725, 0.7968755595119511037, 0.7994792091530360523, 0.8020839052811703507, 0.8046874757081575735, 0.8072921098193328593, 0.8098959335715922858, 0.8125002643549369408, 0.8151046083435100620, 0.8177084237022821389, 0.8203130656946604482, 0.8229166344388356702, 0.8255213278086077633, 0.8281249825035741363, 0.8307294978325265866, 0.8333335802074958165, 0.8359376507484286289, 0.8385421778545157911, 0.8411458274585372763, 0.8437505236574627254, 0.8463540941266142204, 0.8489587282014147140, 0.8515625520809478877, 0.8541668827730166669, 0.8567712269584367712, 0.8593750422766117669, 0.8619796844231587540, 0.8645832532025788941, 0.8671879466218186394, 0.8697916014343529678, 0.8723961167221769841, 0.8750001993026245151, 0.8776042698014647758, 0.8802087971294628721, 0.8828124467634709260, 0.8854171431012803906, 0.8880207136795719158, 0.8906253477860208712, 0.8932291718600525732, 0.8958335025285494302, 0.8984378469785403443, 0.9010416623233333810, 0.9036463046920883979, 0.9062498735737328781, 0.9088545671105374701, 0.9114582221077071056, 0.9140627374223044832, 0.9166668202757080053, 0.9192708907999164181, 0.9218754184177497812, 0.9244790681488107564, 0.9270837646936044285, 0.9296873354480212903, 0.9322919696541906998, 0.9348957939899811276, 0.9375001247025137596, 0.9401044694846933947, 0.9427082849236875228, 0.9453129275835465695, 0.9479164966330613229, 0.9505211903504858784, 0.9531248456066239161, 0.9557293610412391782, 0.9583334441921064206, 0.9609375147049603605, 0.9635420428945489224, 0.9661456931510739032, 0.9687503890924937799, 0.9713539588735070618, 0.9739585961357111188, 0.9765624261165479769, 0.9791667493207181217, 0.9817710620974646751, 0.9843748983037424738, 0.9869797303524157073, 0.9895832060093603388, 0.9921869237806116848, 0.9947912468131487884, 0.9974000922265050528, 0.9999999999999998890 ),
 .UNSPECIFIED. ) 
 GEOMETRIC_REPRESENTATION_ITEM ( )  RATIONAL_B_SPLINE_SURFACE ( (
 ( 1.000000000000000000, 1.000000000000000000, 1.000000000000000000, 0.9999999999999997780, 1.000000000000000000, 1.000000000000000444, 0.9999999999999996669, 0.9999999999999996669, 1.000000000000000444, 1.000000000000000000, 1.000000000000000000, 1.000000000000000000, 1.000000000000000222, 1.000000000000000222, 0.9999999999999997780, 1.000000000000000000, 1.000000000000000222, 1.000000000000000000, 1.000000000000000222, 0.9999999999999994449, 1.000000000000000222, 0.9999999999999997780, 1.000000000000000444, 1.000000000000000000, 1.000000000000000000, 1.000000000000000222, 0.9999999999999997780, 1.000000000000000222, 1.000000000000000000, 1.000000000000000222, 0.9999999999999997780, 1.000000000000000000, 1.000000000000000000, 0.9999999999999997780, 1.000000000000000000, 1.000000000000000000, 1.000000000000000222, 1.000000000000000000, 0.9999999999999997780, 1.000000000000000222, 0.9999999999999997780, 1.000000000000000000, 0.9999999999999997780, 1.000000000000000444, 0.9999999999999996669, 1.000000000000000222, 1.000000000000000000, 1.000000000000000000, 1.000000000000000444, 0.9999999999999996669, 1.000000000000000222, 1.000000000000000444, 1.000000000000000000, 0.9999999999999997780, 1.000000000000000444, 1.000000000000000222, 1.000000000000000000, 1.000000000000000000, 1.000000000000000222, 1.000000000000000000, 1.000000000000000222, 0.9999999999999997780, 1.000000000000000222, 1.000000000000000000, 1.000000000000000000, 1.000000000000000444, 0.9999999999999996669, 1.000000000000000000, 0.9999999999999997780, 1.000000000000000222, 0.9999999999999996669, 1.000000000000000000, 1.000000000000000222, 0.9999999999999997780, 1.000000000000000444, 0.9999999999999997780, 1.000000000000000000, 0.9999999999999997780, 1.000000000000000222, 0.9999999999999996669, 1.000000000000000000, 1.000000000000000222, 0.9999999999999996669, 1.000000000000000444, 0.9999999999999997780, 1.000000000000000000, 1.000000000000000222, 0.9999999999999996669, 1.000000000000000222, 1.000000000000000000, 0.9999999999999997780, 1.000000000000000222, 0.9999999999999997780, 1.000000000000000000, 1.000000000000000222, 0.9999999999999997780, 1.000000000000000000, 1.000000000000000000, 0.9999999999999997780, 1.000000000000000000, 1.000000000000000222, 0.9999999999999997780, 1.000000000000000000, 1.000000000000000000, 1.000000000000000000, 0.9999999999999997780, 1.000000000000000222, 0.9999999999999997780, 0.9999999999999997780, 1.000000000000000444, 1.000000000000000000, 1.000000000000000000, 0.9999999999999997780, 1.000000000000000222, 1.000000000000000000, 1.000000000000000000, 1.000000000000000000, 1.000000000000000000, 1.000000000000000222, 1.000000000000000222, 0.9999999999999997780, 1.000000000000000000, 0.9999999999999997780, 1.000000000000000444, 0.9999999999999996669, 1.000000000000000666, 1.000000000000000000, 0.9999999999999997780, 1.000000000000000222, 1.000000000000000000, 1.000000000000000000, 1.000000000000000000, 0.9999999999999994449, 1.000000000000000666, 0.9999999999999996669, 1.000000000000000000, 1.000000000000000222, 0.9999999999999997780, 1.000000000000000222, 0.9999999999999997780, 1.000000000000000222, 0.9999999999999996669, 1.000000000000000444, 1.000000000000000000, 1.000000000000000222, 0.9999999999999996669, 1.000000000000000000, 1.000000000000000222, 0.9999999999999997780, 1.000000000000000000, 0.9999999999999997780, 1.000000000000000000, 1.000000000000000000, 1.000000000000000222, 0.9999999999999997780, 1.000000000000000222, 0.9999999999999997780, 1.000000000000000000, 1.000000000000000000, 1.000000000000000222, 0.9999999999999997780, 1.000000000000000444, 1.000000000000000000, 0.9999999999999997780, 1.000000000000000000, 1.000000000000000000, 1.000000000000000222, 0.9999999999999997780, 1.000000000000000222, 1.000000000000000000, 1.000000000000000000, 1.000000000000000000, 1.000000000000000222, 1.000000000000000000, 0.9999999999999997780, 1.000000000000000000, 1.000000000000000000, 1.000000000000000000, 1.000000000000000444, 0.9999999999999996669, 1.000000000000000222, 1.000000000000000000, 1.000000000000000222, 0.9999999999999997780, 1.000000000000000000, 0.9999999999999997780, 1.000000000000000000, 0.9999999999999997780, 1.000000000000000000, 1.000000000000000444, 0.9999999999999994449, 1.000000000000000444, 1.000000000000000000, 1.000000000000000222, 1.000000000000000222, 0.9999999999999997780, 1.000000000000000222, 0.9999999999999997780, 1.000000000000000222, 1.000000000000000222, 1.000000000000000222, 0.9999999999999997780, 1.000000000000000000, 1.000000000000000444, 0.9999999999999996669, 1.000000000000000000, 0.9999999999999997780, 1.000000000000000222, 1.000000000000000222, 1.000000000000000000, 0.9999999999999997780, 1.000000000000000222, 0.9999999999999997780, 1.000000000000000222, 0.9999999999999997780, 0.9999999999999997780, 1.000000000000000000, 1.000000000000000000, 1.000000000000000000, 1.000000000000000000, 1.000000000000000000, 1.000000000000000222, 1.000000000000000000, 1.000000000000000000, 1.000000000000000222, 1.000000000000000000, 0.9999999999999997780, 1.000000000000000000, 1.000000000000000000, 1.000000000000000000, 0.9999999999999997780, 1.000000000000000000, 0.9999999999999997780, 1.000000000000000000, 1.000000000000000222, 0.9999999999999996669, 1.000000000000000444, 1.000000000000000000, 0.9999999999999997780, 1.000000000000000222, 1.000000000000000000, 0.9999999999999997780, 1.000000000000000222, 1.000000000000000000, 1.000000000000000222, 1.000000000000000000, 0.9999999999999997780, 1.000000000000000222, 1.000000000000000000, 1.000000000000000000, 1.000000000000000222, 1.000000000000000000, 1.000000000000000000, 1.000000000000000222, 0.9999999999999997780, 0.9999999999999996669, 1.000000000000000444, 0.9999999999999994449, 1.000000000000000444, 0.9999999999999997780, 1.000000000000000222, 1.000000000000000000, 1.000000000000000000, 1.000000000000000000, 1.000000000000000000, 1.000000000000000444, 0.9999999999999996669, 1.000000000000000444, 1.000000000000000000, 0.9999999999999997780, 1.000000000000000444, 0.9999999999999994449, 1.000000000000000444, 0.9999999999999997780, 0.9999999999999997780, 1.000000000000000222, 1.000000000000000444, 0.9999999999999997780, 1.000000000000000444, 0.9999999999999997780, 1.000000000000000000, 1.000000000000000444, 0.9999999999999997780, 0.9999999999999997780, 1.000000000000000000, 1.000000000000000000, 1.000000000000000000, 0.9999999999999997780, 1.000000000000000444, 1.000000000000000222, 0.9999999999999997780, 1.000000000000000444, 1.000000000000000000, 1.000000000000000222, 1.000000000000000000, 1.000000000000000000, 1.000000000000000222, 0.9999999999999997780, 1.000000000000000222, 1.000000000000000222, 0.9999999999999997780, 1.000000000000000222, 1.000000000000000000, 1.000000000000000000, 1.000000000000000222, 0.9999999999999997780, 1.000000000000000444, 0.9999999999999997780, 0.9999999999999997780, 1.000000000000000222, 0.9999999999999997780, 1.000000000000000000, 1.000000000000000000, 0.9999999999999997780, 1.000000000000000222, 0.9999999999999996669, 1.000000000000000444, 0.9999999999999997780, 1.000000000000000222, 1.000000000000000222, 0.9999999999999997780, 1.000000000000000222, 0.9999999999999997780, 1.000000000000000000, 0.9999999999999997780, 1.000000000000000444, 0.9999999999999996669, 1.000000000000000222, 0.9999999999999996669, 1.000000000000000444, 1.000000000000000000, 0.9999999999999997780, 1.000000000000000222, 0.9999999999999996669, 1.000000000000000222, 1.000000000000000222, 0.9999999999999996669, 1.000000000000000444, 1.000000000000000222, 0.9999999999999997780, 1.000000000000000222, 0.9999999999999997780, 1.000000000000000222, 1.000000000000000000, 1.000000000000000222, 0.9999999999999996669, 1.000000000000000444, 1.000000000000000000, 1.000000000000000000, 1.000000000000000222, 0.9999999999999997780, 0.9999999999999997780, 1.000000000000000444, 1.000000000000000000, 1.000000000000000000, 0.9999999999999996669, 1.000000000000000000, 1.000000000000000222, 1.000000000000000000, 1.000000000000000000, 1.000000000000000222, 0.9999999999999997780, 1.000000000000000000, 0.9999999999999997780, 0.9999999999999997780, 1.000000000000000222, 0.9999999999999997780, 1.000000000000000000, 1.000000000000000000, 0.9999999999999997780, 1.000000000000000222, 1.000000000000000000, 1.000000000000000222, 1.000000000000000000, 1.000000000000000444, 1.000000000000000000, 1.000000000000000000, 0.9999999999999997780, 0.9999999999999997780, 1.000000000000000222, 1.000000000000000000, 1.000000000000000000, 1.000000000000000000, 0.9999999999999997780, 1.000000000000000222, 1.000000000000000000, 1.000000000000000000),
 ( 0.3333333333333333703, 0.3333333333333333703, 0.3333333333333333703, 0.3333333333333333148, 0.3333333333333334259, 0.3333333333333334814, 0.3333333333333332593, 0.3333333333333332593, 0.3333333333333334814, 0.3333333333333333703, 0.3333333333333333703, 0.3333333333333334259, 0.3333333333333334259, 0.3333333333333334259, 0.3333333333333332593, 0.3333333333333334259, 0.3333333333333334259, 0.3333333333333333703, 0.3333333333333334259, 0.3333333333333332038, 0.3333333333333334259, 0.3333333333333333148, 0.3333333333333334259, 0.3333333333333333703, 0.3333333333333333703, 0.3333333333333334259, 0.3333333333333333148, 0.3333333333333334259, 0.3333333333333333703, 0.3333333333333333703, 0.3333333333333333148, 0.3333333333333334259, 0.3333333333333333703, 0.3333333333333333703, 0.3333333333333333148, 0.3333333333333333148, 0.3333333333333334259, 0.3333333333333333148, 0.3333333333333334259, 0.3333333333333333703, 0.3333333333333333703, 0.3333333333333333703, 0.3333333333333332593, 0.3333333333333334814, 0.3333333333333332593, 0.3333333333333333703, 0.3333333333333333703, 0.3333333333333333703, 0.3333333333333335369, 0.3333333333333332593, 0.3333333333333333703, 0.3333333333333335369, 0.3333333333333333703, 0.3333333333333333703, 0.3333333333333335369, 0.3333333333333333703, 0.3333333333333334259, 0.3333333333333334259, 0.3333333333333333703, 0.3333333333333333703, 0.3333333333333333703, 0.3333333333333333703, 0.3333333333333333703, 0.3333333333333333148, 0.3333333333333334259, 0.3333333333333334814, 0.3333333333333333148, 0.3333333333333333703, 0.3333333333333333148, 0.3333333333333334259, 0.3333333333333332593, 0.3333333333333334259, 0.3333333333333333703, 0.3333333333333334259, 0.3333333333333333703, 0.3333333333333333703, 0.3333333333333333703, 0.3333333333333333148, 0.3333333333333334814, 0.3333333333333332038, 0.3333333333333334259, 0.3333333333333334259, 0.3333333333333333148, 0.3333333333333334259, 0.3333333333333333703, 0.3333333333333333148, 0.3333333333333333703, 0.3333333333333333148, 0.3333333333333334814, 0.3333333333333333148, 0.3333333333333333148, 0.3333333333333334259, 0.3333333333333333148, 0.3333333333333333148, 0.3333333333333334814, 0.3333333333333333148, 0.3333333333333334259, 0.3333333333333333703, 0.3333333333333333148, 0.3333333333333333703, 0.3333333333333334259, 0.3333333333333333148, 0.3333333333333334259, 0.3333333333333333148, 0.3333333333333333703, 0.3333333333333333148, 0.3333333333333333703, 0.3333333333333333703, 0.3333333333333333148, 0.3333333333333334259, 0.3333333333333334259, 0.3333333333333333148, 0.3333333333333333703, 0.3333333333333333703, 0.3333333333333334259, 0.3333333333333333703, 0.3333333333333333703, 0.3333333333333334259, 0.3333333333333333703, 0.3333333333333334259, 0.3333333333333333148, 0.3333333333333333703, 0.3333333333333333148, 0.3333333333333335369, 0.3333333333333333148, 0.3333333333333335369, 0.3333333333333333703, 0.3333333333333332593, 0.3333333333333334259, 0.3333333333333334259, 0.3333333333333333148, 0.3333333333333333703, 0.3333333333333333148, 0.3333333333333335369, 0.3333333333333333148, 0.3333333333333333703, 0.3333333333333333703, 0.3333333333333334259, 0.3333333333333334259, 0.3333333333333333703, 0.3333333333333334259, 0.3333333333333332593, 0.3333333333333334814, 0.3333333333333333148, 0.3333333333333333703, 0.3333333333333333148, 0.3333333333333333148, 0.3333333333333334259, 0.3333333333333332593, 0.3333333333333333148, 0.3333333333333333703, 0.3333333333333333148, 0.3333333333333333703, 0.3333333333333334259, 0.3333333333333333703, 0.3333333333333334259, 0.3333333333333333148, 0.3333333333333333703, 0.3333333333333333703, 0.3333333333333333703, 0.3333333333333333148, 0.3333333333333335369, 0.3333333333333333148, 0.3333333333333333703, 0.3333333333333333148, 0.3333333333333334259, 0.3333333333333334259, 0.3333333333333333703, 0.3333333333333334259, 0.3333333333333333703, 0.3333333333333333703, 0.3333333333333334259, 0.3333333333333333703, 0.3333333333333333703, 0.3333333333333333703, 0.3333333333333334259, 0.3333333333333333148, 0.3333333333333333148, 0.3333333333333335369, 0.3333333333333333148, 0.3333333333333334259, 0.3333333333333333148, 0.3333333333333334259, 0.3333333333333333703, 0.3333333333333333148, 0.3333333333333333148, 0.3333333333333333703, 0.3333333333333333148, 0.3333333333333334259, 0.3333333333333334259, 0.3333333333333332038, 0.3333333333333335369, 0.3333333333333333703, 0.3333333333333334259, 0.3333333333333334259, 0.3333333333333333703, 0.3333333333333334259, 0.3333333333333332593, 0.3333333333333334814, 0.3333333333333333703, 0.3333333333333334259, 0.3333333333333333148, 0.3333333333333333148, 0.3333333333333335369, 0.3333333333333332593, 0.3333333333333333703, 0.3333333333333332593, 0.3333333333333335369, 0.3333333333333333703, 0.3333333333333333703, 0.3333333333333333703, 0.3333333333333334259, 0.3333333333333332593, 0.3333333333333334814, 0.3333333333333332593, 0.3333333333333333703, 0.3333333333333333703, 0.3333333333333333703, 0.3333333333333334259, 0.3333333333333333148, 0.3333333333333334259, 0.3333333333333334259, 0.3333333333333333703, 0.3333333333333333148, 0.3333333333333334259, 0.3333333333333333148, 0.3333333333333333703, 0.3333333333333333148, 0.3333333333333333703, 0.3333333333333333703, 0.3333333333333333148, 0.3333333333333333703, 0.3333333333333333703, 0.3333333333333333703, 0.3333333333333334259, 0.3333333333333333703, 0.3333333333333333703, 0.3333333333333334814, 0.3333333333333332593, 0.3333333333333333703, 0.3333333333333334259, 0.3333333333333333148, 0.3333333333333334259, 0.3333333333333333703, 0.3333333333333334814, 0.3333333333333333703, 0.3333333333333333148, 0.3333333333333334259, 0.3333333333333333703, 0.3333333333333333703, 0.3333333333333333703, 0.3333333333333334259, 0.3333333333333333148, 0.3333333333333334259, 0.3333333333333333148, 0.3333333333333333148, 0.3333333333333335369, 0.3333333333333332038, 0.3333333333333335369, 0.3333333333333333148, 0.3333333333333333703, 0.3333333333333334259, 0.3333333333333333703, 0.3333333333333333148, 0.3333333333333333703, 0.3333333333333334259, 0.3333333333333333703, 0.3333333333333334259, 0.3333333333333333148, 0.3333333333333333703, 0.3333333333333334259, 0.3333333333333333148, 0.3333333333333333703, 0.3333333333333333703, 0.3333333333333333148, 0.3333333333333334259, 0.3333333333333334259, 0.3333333333333333703, 0.3333333333333335369, 0.3333333333333333148, 0.3333333333333333703, 0.3333333333333333703, 0.3333333333333333148, 0.3333333333333333703, 0.3333333333333333703, 0.3333333333333333703, 0.3333333333333333148, 0.3333333333333333703, 0.3333333333333334814, 0.3333333333333333703, 0.3333333333333333703, 0.3333333333333335369, 0.3333333333333333703, 0.3333333333333333703, 0.3333333333333334259, 0.3333333333333334259, 0.3333333333333333703, 0.3333333333333333703, 0.3333333333333333703, 0.3333333333333333703, 0.3333333333333333148, 0.3333333333333334259, 0.3333333333333333703, 0.3333333333333333703, 0.3333333333333333703, 0.3333333333333333148, 0.3333333333333334814, 0.3333333333333333148, 0.3333333333333333148, 0.3333333333333334814, 0.3333333333333333148, 0.3333333333333333148, 0.3333333333333334259, 0.3333333333333333148, 0.3333333333333334259, 0.3333333333333333148, 0.3333333333333334259, 0.3333333333333332593, 0.3333333333333335369, 0.3333333333333333148, 0.3333333333333333148, 0.3333333333333334259, 0.3333333333333333703, 0.3333333333333333703, 0.3333333333333333148, 0.3333333333333334259, 0.3333333333333333148, 0.3333333333333334259, 0.3333333333333333148, 0.3333333333333334259, 0.3333333333333334259, 0.3333333333333333703, 0.3333333333333334259, 0.3333333333333333703, 0.3333333333333333703, 0.3333333333333334259, 0.3333333333333333148, 0.3333333333333335369, 0.3333333333333334259, 0.3333333333333333148, 0.3333333333333333703, 0.3333333333333333148, 0.3333333333333334814, 0.3333333333333333703, 0.3333333333333333703, 0.3333333333333332593, 0.3333333333333334814, 0.3333333333333333703, 0.3333333333333333148, 0.3333333333333334259, 0.3333333333333332593, 0.3333333333333334814, 0.3333333333333333703, 0.3333333333333334259, 0.3333333333333333703, 0.3333333333333333148, 0.3333333333333333703, 0.3333333333333334259, 0.3333333333333333703, 0.3333333333333334259, 0.3333333333333333703, 0.3333333333333333703, 0.3333333333333333148, 0.3333333333333333148, 0.3333333333333333703, 0.3333333333333333703, 0.3333333333333333703, 0.3333333333333333703, 0.3333333333333333703, 0.3333333333333333148, 0.3333333333333334814, 0.3333333333333333148, 0.3333333333333334814, 0.3333333333333333703, 0.3333333333333334259, 0.3333333333333334259, 0.3333333333333333703, 0.3333333333333332593, 0.3333333333333333703, 0.3333333333333333703, 0.3333333333333333703, 0.3333333333333333148, 0.3333333333333333703, 0.3333333333333332593, 0.3333333333333334259, 0.3333333333333333703, 0.3333333333333333703),
 ( 0.3333333333333333703, 0.3333333333333333703, 0.3333333333333333703, 0.3333333333333333148, 0.3333333333333334259, 0.3333333333333334814, 0.3333333333333332593, 0.3333333333333332593, 0.3333333333333334814, 0.3333333333333333703, 0.3333333333333333703, 0.3333333333333334259, 0.3333333333333334259, 0.3333333333333334259, 0.3333333333333332593, 0.3333333333333334259, 0.3333333333333334259, 0.3333333333333333703, 0.3333333333333334259, 0.3333333333333332038, 0.3333333333333334259, 0.3333333333333333148, 0.3333333333333334259, 0.3333333333333333703, 0.3333333333333333703, 0.3333333333333334259, 0.3333333333333333148, 0.3333333333333334259, 0.3333333333333333703, 0.3333333333333333703, 0.3333333333333333148, 0.3333333333333334259, 0.3333333333333333703, 0.3333333333333333703, 0.3333333333333333148, 0.3333333333333333148, 0.3333333333333334259, 0.3333333333333333148, 0.3333333333333334259, 0.3333333333333333703, 0.3333333333333333703, 0.3333333333333333703, 0.3333333333333332593, 0.3333333333333334814, 0.3333333333333332593, 0.3333333333333333703, 0.3333333333333333703, 0.3333333333333333703, 0.3333333333333335369, 0.3333333333333332593, 0.3333333333333333703, 0.3333333333333335369, 0.3333333333333333703, 0.3333333333333333703, 0.3333333333333335369, 0.3333333333333333703, 0.3333333333333334259, 0.3333333333333334259, 0.3333333333333333703, 0.3333333333333333703, 0.3333333333333333703, 0.3333333333333333703, 0.3333333333333333703, 0.3333333333333333148, 0.3333333333333334259, 0.3333333333333334814, 0.3333333333333333148, 0.3333333333333333703, 0.3333333333333333148, 0.3333333333333334259, 0.3333333333333332593, 0.3333333333333334259, 0.3333333333333333703, 0.3333333333333334259, 0.3333333333333333703, 0.3333333333333333703, 0.3333333333333333703, 0.3333333333333333148, 0.3333333333333334814, 0.3333333333333332038, 0.3333333333333334259, 0.3333333333333334259, 0.3333333333333333148, 0.3333333333333334259, 0.3333333333333333703, 0.3333333333333333148, 0.3333333333333333703, 0.3333333333333333148, 0.3333333333333334814, 0.3333333333333333148, 0.3333333333333333148, 0.3333333333333334259, 0.3333333333333333148, 0.3333333333333333148, 0.3333333333333334814, 0.3333333333333333148, 0.3333333333333334259, 0.3333333333333333703, 0.3333333333333333148, 0.3333333333333333703, 0.3333333333333334259, 0.3333333333333333148, 0.3333333333333334259, 0.3333333333333333148, 0.3333333333333333703, 0.3333333333333333148, 0.3333333333333333703, 0.3333333333333333703, 0.3333333333333333148, 0.3333333333333334259, 0.3333333333333334259, 0.3333333333333333148, 0.3333333333333333703, 0.3333333333333333703, 0.3333333333333334259, 0.3333333333333333703, 0.3333333333333333703, 0.3333333333333334259, 0.3333333333333333703, 0.3333333333333334259, 0.3333333333333333148, 0.3333333333333333703, 0.3333333333333333148, 0.3333333333333335369, 0.3333333333333333148, 0.3333333333333335369, 0.3333333333333333703, 0.3333333333333332593, 0.3333333333333334259, 0.3333333333333334259, 0.3333333333333333148, 0.3333333333333333703, 0.3333333333333333148, 0.3333333333333335369, 0.3333333333333333148, 0.3333333333333333703, 0.3333333333333333703, 0.3333333333333334259, 0.3333333333333334259, 0.3333333333333333703, 0.3333333333333334259, 0.3333333333333332593, 0.3333333333333334814, 0.3333333333333333148, 0.3333333333333333703, 0.3333333333333333148, 0.3333333333333333148, 0.3333333333333334259, 0.3333333333333332593, 0.3333333333333333148, 0.3333333333333333703, 0.3333333333333333148, 0.3333333333333333703, 0.3333333333333334259, 0.3333333333333333703, 0.3333333333333334259, 0.3333333333333333148, 0.3333333333333333703, 0.3333333333333333703, 0.3333333333333333703, 0.3333333333333333148, 0.3333333333333335369, 0.3333333333333333148, 0.3333333333333333703, 0.3333333333333333148, 0.3333333333333334259, 0.3333333333333334259, 0.3333333333333333703, 0.3333333333333334259, 0.3333333333333333703, 0.3333333333333333703, 0.3333333333333334259, 0.3333333333333333703, 0.3333333333333333703, 0.3333333333333333703, 0.3333333333333334259, 0.3333333333333333148, 0.3333333333333333148, 0.3333333333333335369, 0.3333333333333333148, 0.3333333333333334259, 0.3333333333333333148, 0.3333333333333334259, 0.3333333333333333703, 0.3333333333333333148, 0.3333333333333333148, 0.3333333333333333703, 0.3333333333333333148, 0.3333333333333334259, 0.3333333333333334259, 0.3333333333333332038, 0.3333333333333335369, 0.3333333333333333703, 0.3333333333333334259, 0.3333333333333334259, 0.3333333333333333703, 0.3333333333333334259, 0.3333333333333332593, 0.3333333333333334814, 0.3333333333333333703, 0.3333333333333334259, 0.3333333333333333148, 0.3333333333333333148, 0.3333333333333335369, 0.3333333333333332593, 0.3333333333333333703, 0.3333333333333332593, 0.3333333333333335369, 0.3333333333333333703, 0.3333333333333333703, 0.3333333333333333703, 0.3333333333333334259, 0.3333333333333332593, 0.3333333333333334814, 0.3333333333333332593, 0.3333333333333333703, 0.3333333333333333703, 0.3333333333333333703, 0.3333333333333334259, 0.3333333333333333148, 0.3333333333333334259, 0.3333333333333334259, 0.3333333333333333703, 0.3333333333333333148, 0.3333333333333334259, 0.3333333333333333148, 0.3333333333333333703, 0.3333333333333333148, 0.3333333333333333703, 0.3333333333333333703, 0.3333333333333333148, 0.3333333333333333703, 0.3333333333333333703, 0.3333333333333333703, 0.3333333333333334259, 0.3333333333333333703, 0.3333333333333333703, 0.3333333333333334814, 0.3333333333333332593, 0.3333333333333333703, 0.3333333333333334259, 0.3333333333333333148, 0.3333333333333334259, 0.3333333333333333703, 0.3333333333333334814, 0.3333333333333333703, 0.3333333333333333148, 0.3333333333333334259, 0.3333333333333333703, 0.3333333333333333703, 0.3333333333333333703, 0.3333333333333334259, 0.3333333333333333148, 0.3333333333333334259, 0.3333333333333333148, 0.3333333333333333148, 0.3333333333333335369, 0.3333333333333332038, 0.3333333333333335369, 0.3333333333333333148, 0.3333333333333333703, 0.3333333333333334259, 0.3333333333333333703, 0.3333333333333333148, 0.3333333333333333703, 0.3333333333333334259, 0.3333333333333333703, 0.3333333333333334259, 0.3333333333333333148, 0.3333333333333333703, 0.3333333333333334259, 0.3333333333333333148, 0.3333333333333333703, 0.3333333333333333703, 0.3333333333333333148, 0.3333333333333334259, 0.3333333333333334259, 0.3333333333333333703, 0.3333333333333335369, 0.3333333333333333148, 0.3333333333333333703, 0.3333333333333333703, 0.3333333333333333148, 0.3333333333333333703, 0.3333333333333333703, 0.3333333333333333703, 0.3333333333333333148, 0.3333333333333333703, 0.3333333333333334814, 0.3333333333333333703, 0.3333333333333333703, 0.3333333333333335369, 0.3333333333333333703, 0.3333333333333333703, 0.3333333333333334259, 0.3333333333333334259, 0.3333333333333333703, 0.3333333333333333703, 0.3333333333333333703, 0.3333333333333333703, 0.3333333333333333148, 0.3333333333333334259, 0.3333333333333333703, 0.3333333333333333703, 0.3333333333333333703, 0.3333333333333333148, 0.3333333333333334814, 0.3333333333333333148, 0.3333333333333333148, 0.3333333333333334814, 0.3333333333333333148, 0.3333333333333333148, 0.3333333333333334259, 0.3333333333333333148, 0.3333333333333334259, 0.3333333333333333148, 0.3333333333333334259, 0.3333333333333332593, 0.3333333333333335369, 0.3333333333333333148, 0.3333333333333333148, 0.3333333333333334259, 0.3333333333333333703, 0.3333333333333333703, 0.3333333333333333148, 0.3333333333333334259, 0.3333333333333333148, 0.3333333333333334259, 0.3333333333333333148, 0.3333333333333334259, 0.3333333333333334259, 0.3333333333333333703, 0.3333333333333334259, 0.3333333333333333703, 0.3333333333333333703, 0.3333333333333334259, 0.3333333333333333148, 0.3333333333333335369, 0.3333333333333334259, 0.3333333333333333148, 0.3333333333333333703, 0.3333333333333333148, 0.3333333333333334814, 0.3333333333333333703, 0.3333333333333333703, 0.3333333333333332593, 0.3333333333333334814, 0.3333333333333333703, 0.3333333333333333148, 0.3333333333333334259, 0.3333333333333332593, 0.3333333333333334814, 0.3333333333333333703, 0.3333333333333334259, 0.3333333333333333703, 0.3333333333333333148, 0.3333333333333333703, 0.3333333333333334259, 0.3333333333333333703, 0.3333333333333334259, 0.3333333333333333703, 0.3333333333333333703, 0.3333333333333333148, 0.3333333333333333148, 0.3333333333333333703, 0.3333333333333333703, 0.3333333333333333703, 0.3333333333333333703, 0.3333333333333333703, 0.3333333333333333148, 0.3333333333333334814, 0.3333333333333333148, 0.3333333333333334814, 0.3333333333333333703, 0.3333333333333334259, 0.3333333333333334259, 0.3333333333333333703, 0.3333333333333332593, 0.3333333333333333703, 0.3333333333333333703, 0.3333333333333333703, 0.3333333333333333148, 0.3333333333333333703, 0.3333333333333332593, 0.3333333333333334259, 0.3333333333333333703, 0.3333333333333333703),
 ( 1.000000000000000000, 1.000000000000000000, 1.000000000000000000, 0.9999999999999997780, 1.000000000000000000, 1.000000000000000444, 0.9999999999999996669, 0.9999999999999996669, 1.000000000000000444, 1.000000000000000000, 1.000000000000000000, 1.000000000000000000, 1.000000000000000222, 1.000000000000000222, 0.9999999999999997780, 1.000000000000000000, 1.000000000000000222, 1.000000000000000000, 1.000000000000000222, 0.9999999999999994449, 1.000000000000000222, 0.9999999999999997780, 1.000000000000000444, 1.000000000000000000, 1.000000000000000000, 1.000000000000000222, 0.9999999999999997780, 1.000000000000000222, 1.000000000000000000, 1.000000000000000222, 0.9999999999999997780, 1.000000000000000000, 1.000000000000000000, 0.9999999999999997780, 1.000000000000000000, 1.000000000000000000, 1.000000000000000222, 1.000000000000000000, 0.9999999999999997780, 1.000000000000000222, 0.9999999999999997780, 1.000000000000000000, 0.9999999999999997780, 1.000000000000000444, 0.9999999999999996669, 1.000000000000000222, 1.000000000000000000, 1.000000000000000000, 1.000000000000000444, 0.9999999999999996669, 1.000000000000000222, 1.000000000000000444, 1.000000000000000000, 0.9999999999999997780, 1.000000000000000444, 1.000000000000000222, 1.000000000000000000, 1.000000000000000000, 1.000000000000000222, 1.000000000000000000, 1.000000000000000222, 0.9999999999999997780, 1.000000000000000222, 1.000000000000000000, 1.000000000000000000, 1.000000000000000444, 0.9999999999999996669, 1.000000000000000000, 0.9999999999999997780, 1.000000000000000222, 0.9999999999999996669, 1.000000000000000000, 1.000000000000000222, 0.9999999999999997780, 1.000000000000000444, 0.9999999999999997780, 1.000000000000000000, 0.9999999999999997780, 1.000000000000000222, 0.9999999999999996669, 1.000000000000000000, 1.000000000000000222, 0.9999999999999996669, 1.000000000000000444, 0.9999999999999997780, 1.000000000000000000, 1.000000000000000222, 0.9999999999999996669, 1.000000000000000222, 1.000000000000000000, 0.9999999999999997780, 1.000000000000000222, 0.9999999999999997780, 1.000000000000000000, 1.000000000000000222, 0.9999999999999997780, 1.000000000000000000, 1.000000000000000000, 0.9999999999999997780, 1.000000000000000000, 1.000000000000000222, 0.9999999999999997780, 1.000000000000000000, 1.000000000000000000, 1.000000000000000000, 0.9999999999999997780, 1.000000000000000222, 0.9999999999999997780, 0.9999999999999997780, 1.000000000000000444, 1.000000000000000000, 1.000000000000000000, 0.9999999999999997780, 1.000000000000000222, 1.000000000000000000, 1.000000000000000000, 1.000000000000000000, 1.000000000000000000, 1.000000000000000222, 1.000000000000000222, 0.9999999999999997780, 1.000000000000000000, 0.9999999999999997780, 1.000000000000000444, 0.9999999999999996669, 1.000000000000000666, 1.000000000000000000, 0.9999999999999997780, 1.000000000000000222, 1.000000000000000000, 1.000000000000000000, 1.000000000000000000, 0.9999999999999994449, 1.000000000000000666, 0.9999999999999996669, 1.000000000000000000, 1.000000000000000222, 0.9999999999999997780, 1.000000000000000222, 0.9999999999999997780, 1.000000000000000222, 0.9999999999999996669, 1.000000000000000444, 1.000000000000000000, 1.000000000000000222, 0.9999999999999996669, 1.000000000000000000, 1.000000000000000222, 0.9999999999999997780, 1.000000000000000000, 0.9999999999999997780, 1.000000000000000000, 1.000000000000000000, 1.000000000000000222, 0.9999999999999997780, 1.000000000000000222, 0.9999999999999997780, 1.000000000000000000, 1.000000000000000000, 1.000000000000000222, 0.9999999999999997780, 1.000000000000000444, 1.000000000000000000, 0.9999999999999997780, 1.000000000000000000, 1.000000000000000000, 1.000000000000000222, 0.9999999999999997780, 1.000000000000000222, 1.000000000000000000, 1.000000000000000000, 1.000000000000000000, 1.000000000000000222, 1.000000000000000000, 0.9999999999999997780, 1.000000000000000000, 1.000000000000000000, 1.000000000000000000, 1.000000000000000444, 0.9999999999999996669, 1.000000000000000222, 1.000000000000000000, 1.000000000000000222, 0.9999999999999997780, 1.000000000000000000, 0.9999999999999997780, 1.000000000000000000, 0.9999999999999997780, 1.000000000000000000, 1.000000000000000444, 0.9999999999999994449, 1.000000000000000444, 1.000000000000000000, 1.000000000000000222, 1.000000000000000222, 0.9999999999999997780, 1.000000000000000222, 0.9999999999999997780, 1.000000000000000222, 1.000000000000000222, 1.000000000000000222, 0.9999999999999997780, 1.000000000000000000, 1.000000000000000444, 0.9999999999999996669, 1.000000000000000000, 0.9999999999999997780, 1.000000000000000222, 1.000000000000000222, 1.000000000000000000, 0.9999999999999997780, 1.000000000000000222, 0.9999999999999997780, 1.000000000000000222, 0.9999999999999997780, 0.9999999999999997780, 1.000000000000000000, 1.000000000000000000, 1.000000000000000000, 1.000000000000000000, 1.000000000000000000, 1.000000000000000222, 1.000000000000000000, 1.000000000000000000, 1.000000000000000222, 1.000000000000000000, 0.9999999999999997780, 1.000000000000000000, 1.000000000000000000, 1.000000000000000000, 0.9999999999999997780, 1.000000000000000000, 0.9999999999999997780, 1.000000000000000000, 1.000000000000000222, 0.9999999999999996669, 1.000000000000000444, 1.000000000000000000, 0.9999999999999997780, 1.000000000000000222, 1.000000000000000000, 0.9999999999999997780, 1.000000000000000222, 1.000000000000000000, 1.000000000000000222, 1.000000000000000000, 0.9999999999999997780, 1.000000000000000222, 1.000000000000000000, 1.000000000000000000, 1.000000000000000222, 1.000000000000000000, 1.000000000000000000, 1.000000000000000222, 0.9999999999999997780, 0.9999999999999996669, 1.000000000000000444, 0.9999999999999994449, 1.000000000000000444, 0.9999999999999997780, 1.000000000000000222, 1.000000000000000000, 1.000000000000000000, 1.000000000000000000, 1.000000000000000000, 1.000000000000000444, 0.9999999999999996669, 1.000000000000000444, 1.000000000000000000, 0.9999999999999997780, 1.000000000000000444, 0.9999999999999994449, 1.000000000000000444, 0.9999999999999997780, 0.9999999999999997780, 1.000000000000000222, 1.000000000000000444, 0.9999999999999997780, 1.000000000000000444, 0.9999999999999997780, 1.000000000000000000, 1.000000000000000444, 0.9999999999999997780, 0.9999999999999997780, 1.000000000000000000, 1.000000000000000000, 1.000000000000000000, 0.9999999999999997780, 1.000000000000000444, 1.000000000000000222, 0.9999999999999997780, 1.000000000000000444, 1.000000000000000000, 1.000000000000000222, 1.000000000000000000, 1.000000000000000000, 1.000000000000000222, 0.9999999999999997780, 1.000000000000000222, 1.000000000000000222, 0.9999999999999997780, 1.000000000000000222, 1.000000000000000000, 1.000000000000000000, 1.000000000000000222, 0.9999999999999997780, 1.000000000000000444, 0.9999999999999997780, 0.9999999999999997780, 1.000000000000000222, 0.9999999999999997780, 1.000000000000000000, 1.000000000000000000, 0.9999999999999997780, 1.000000000000000222, 0.9999999999999996669, 1.000000000000000444, 0.9999999999999997780, 1.000000000000000222, 1.000000000000000222, 0.9999999999999997780, 1.000000000000000222, 0.9999999999999997780, 1.000000000000000000, 0.9999999999999997780, 1.000000000000000444, 0.9999999999999996669, 1.000000000000000222, 0.9999999999999996669, 1.000000000000000444, 1.000000000000000000, 0.9999999999999997780, 1.000000000000000222, 0.9999999999999996669, 1.000000000000000222, 1.000000000000000222, 0.9999999999999996669, 1.000000000000000444, 1.000000000000000222, 0.9999999999999997780, 1.000000000000000222, 0.9999999999999997780, 1.000000000000000222, 1.000000000000000000, 1.000000000000000222, 0.9999999999999996669, 1.000000000000000444, 1.000000000000000000, 1.000000000000000000, 1.000000000000000222, 0.9999999999999997780, 0.9999999999999997780, 1.000000000000000444, 1.000000000000000000, 1.000000000000000000, 0.9999999999999996669, 1.000000000000000000, 1.000000000000000222, 1.000000000000000000, 1.000000000000000000, 1.000000000000000222, 0.9999999999999997780, 1.000000000000000000, 0.9999999999999997780, 0.9999999999999997780, 1.000000000000000222, 0.9999999999999997780, 1.000000000000000000, 1.000000000000000000, 0.9999999999999997780, 1.000000000000000222, 1.000000000000000000, 1.000000000000000222, 1.000000000000000000, 1.000000000000000444, 1.000000000000000000, 1.000000000000000000, 0.9999999999999997780, 0.9999999999999997780, 1.000000000000000222, 1.000000000000000000, 1.000000000000000000, 1.000000000000000000, 0.9999999999999997780, 1.000000000000000222, 1.000000000000000000, 1.000000000000000000),
 ( 0.3333333333333333703, 0.3333333333333333703, 0.3333333333333333703, 0.3333333333333333148, 0.3333333333333334259, 0.3333333333333334814, 0.3333333333333332593, 0.3333333333333332593, 0.3333333333333334814, 0.3333333333333333703, 0.3333333333333333703, 0.3333333333333334259, 0.3333333333333334259, 0.3333333333333334259, 0.3333333333333332593, 0.3333333333333334259, 0.3333333333333334259, 0.3333333333333333703, 0.3333333333333334259, 0.3333333333333332038, 0.3333333333333334259, 0.3333333333333333148, 0.3333333333333334259, 0.3333333333333333703, 0.3333333333333333703, 0.3333333333333334259, 0.3333333333333333148, 0.3333333333333334259, 0.3333333333333333703, 0.3333333333333333703, 0.3333333333333333148, 0.3333333333333334259, 0.3333333333333333703, 0.3333333333333333703, 0.3333333333333333148, 0.3333333333333333148, 0.3333333333333334259, 0.3333333333333333148, 0.3333333333333334259, 0.3333333333333333703, 0.3333333333333333703, 0.3333333333333333703, 0.3333333333333332593, 0.3333333333333334814, 0.3333333333333332593, 0.3333333333333333703, 0.3333333333333333703, 0.3333333333333333703, 0.3333333333333335369, 0.3333333333333332593, 0.3333333333333333703, 0.3333333333333335369, 0.3333333333333333703, 0.3333333333333333703, 0.3333333333333335369, 0.3333333333333333703, 0.3333333333333334259, 0.3333333333333334259, 0.3333333333333333703, 0.3333333333333333703, 0.3333333333333333703, 0.3333333333333333703, 0.3333333333333333703, 0.3333333333333333148, 0.3333333333333334259, 0.3333333333333334814, 0.3333333333333333148, 0.3333333333333333703, 0.3333333333333333148, 0.3333333333333334259, 0.3333333333333332593, 0.3333333333333334259, 0.3333333333333333703, 0.3333333333333334259, 0.3333333333333333703, 0.3333333333333333703, 0.3333333333333333703, 0.3333333333333333148, 0.3333333333333334814, 0.3333333333333332038, 0.3333333333333334259, 0.3333333333333334259, 0.3333333333333333148, 0.3333333333333334259, 0.3333333333333333703, 0.3333333333333333148, 0.3333333333333333703, 0.3333333333333333148, 0.3333333333333334814, 0.3333333333333333148, 0.3333333333333333148, 0.3333333333333334259, 0.3333333333333333148, 0.3333333333333333148, 0.3333333333333334814, 0.3333333333333333148, 0.3333333333333334259, 0.3333333333333333703, 0.3333333333333333148, 0.3333333333333333703, 0.3333333333333334259, 0.3333333333333333148, 0.3333333333333334259, 0.3333333333333333148, 0.3333333333333333703, 0.3333333333333333148, 0.3333333333333333703, 0.3333333333333333703, 0.3333333333333333148, 0.3333333333333334259, 0.3333333333333334259, 0.3333333333333333148, 0.3333333333333333703, 0.3333333333333333703, 0.3333333333333334259, 0.3333333333333333703, 0.3333333333333333703, 0.3333333333333334259, 0.3333333333333333703, 0.3333333333333334259, 0.3333333333333333148, 0.3333333333333333703, 0.3333333333333333148, 0.3333333333333335369, 0.3333333333333333148, 0.3333333333333335369, 0.3333333333333333703, 0.3333333333333332593, 0.3333333333333334259, 0.3333333333333334259, 0.3333333333333333148, 0.3333333333333333703, 0.3333333333333333148, 0.3333333333333335369, 0.3333333333333333148, 0.3333333333333333703, 0.3333333333333333703, 0.3333333333333334259, 0.3333333333333334259, 0.3333333333333333703, 0.3333333333333334259, 0.3333333333333332593, 0.3333333333333334814, 0.3333333333333333148, 0.3333333333333333703, 0.3333333333333333148, 0.3333333333333333148, 0.3333333333333334259, 0.3333333333333332593, 0.3333333333333333148, 0.3333333333333333703, 0.3333333333333333148, 0.3333333333333333703, 0.3333333333333334259, 0.3333333333333333703, 0.3333333333333334259, 0.3333333333333333148, 0.3333333333333333703, 0.3333333333333333703, 0.3333333333333333703, 0.3333333333333333148, 0.3333333333333335369, 0.3333333333333333148, 0.3333333333333333703, 0.3333333333333333148, 0.3333333333333334259, 0.3333333333333334259, 0.3333333333333333703, 0.3333333333333334259, 0.3333333333333333703, 0.3333333333333333703, 0.3333333333333334259, 0.3333333333333333703, 0.3333333333333333703, 0.3333333333333333703, 0.3333333333333334259, 0.3333333333333333148, 0.3333333333333333148, 0.3333333333333335369, 0.3333333333333333148, 0.3333333333333334259, 0.3333333333333333148, 0.3333333333333334259, 0.3333333333333333703, 0.3333333333333333148, 0.3333333333333333148, 0.3333333333333333703, 0.3333333333333333148, 0.3333333333333334259, 0.3333333333333334259, 0.3333333333333332038, 0.3333333333333335369, 0.3333333333333333703, 0.3333333333333334259, 0.3333333333333334259, 0.3333333333333333703, 0.3333333333333334259, 0.3333333333333332593, 0.3333333333333334814, 0.3333333333333333703, 0.3333333333333334259, 0.3333333333333333148, 0.3333333333333333148, 0.3333333333333335369, 0.3333333333333332593, 0.3333333333333333703, 0.3333333333333332593, 0.3333333333333335369, 0.3333333333333333703, 0.3333333333333333703, 0.3333333333333333703, 0.3333333333333334259, 0.3333333333333332593, 0.3333333333333334814, 0.3333333333333332593, 0.3333333333333333703, 0.3333333333333333703, 0.3333333333333333703, 0.3333333333333334259, 0.3333333333333333148, 0.3333333333333334259, 0.3333333333333334259, 0.3333333333333333703, 0.3333333333333333148, 0.3333333333333334259, 0.3333333333333333148, 0.3333333333333333703, 0.3333333333333333148, 0.3333333333333333703, 0.3333333333333333703, 0.3333333333333333148, 0.3333333333333333703, 0.3333333333333333703, 0.3333333333333333703, 0.3333333333333334259, 0.3333333333333333703, 0.3333333333333333703, 0.3333333333333334814, 0.3333333333333332593, 0.3333333333333333703, 0.3333333333333334259, 0.3333333333333333148, 0.3333333333333334259, 0.3333333333333333703, 0.3333333333333334814, 0.3333333333333333703, 0.3333333333333333148, 0.3333333333333334259, 0.3333333333333333703, 0.3333333333333333703, 0.3333333333333333703, 0.3333333333333334259, 0.3333333333333333148, 0.3333333333333334259, 0.3333333333333333148, 0.3333333333333333148, 0.3333333333333335369, 0.3333333333333332038, 0.3333333333333335369, 0.3333333333333333148, 0.3333333333333333703, 0.3333333333333334259, 0.3333333333333333703, 0.3333333333333333148, 0.3333333333333333703, 0.3333333333333334259, 0.3333333333333333703, 0.3333333333333334259, 0.3333333333333333148, 0.3333333333333333703, 0.3333333333333334259, 0.3333333333333333148, 0.3333333333333333703, 0.3333333333333333703, 0.3333333333333333148, 0.3333333333333334259, 0.3333333333333334259, 0.3333333333333333703, 0.3333333333333335369, 0.3333333333333333148, 0.3333333333333333703, 0.3333333333333333703, 0.3333333333333333148, 0.3333333333333333703, 0.3333333333333333703, 0.3333333333333333703, 0.3333333333333333148, 0.3333333333333333703, 0.3333333333333334814, 0.3333333333333333703, 0.3333333333333333703, 0.3333333333333335369, 0.3333333333333333703, 0.3333333333333333703, 0.3333333333333334259, 0.3333333333333334259, 0.3333333333333333703, 0.3333333333333333703, 0.3333333333333333703, 0.3333333333333333703, 0.3333333333333333148, 0.3333333333333334259, 0.3333333333333333703, 0.3333333333333333703, 0.3333333333333333703, 0.3333333333333333148, 0.3333333333333334814, 0.3333333333333333148, 0.3333333333333333148, 0.3333333333333334814, 0.3333333333333333148, 0.3333333333333333148, 0.3333333333333334259, 0.3333333333333333148, 0.3333333333333334259, 0.3333333333333333148, 0.3333333333333334259, 0.3333333333333332593, 0.3333333333333335369, 0.3333333333333333148, 0.3333333333333333148, 0.3333333333333334259, 0.3333333333333333703, 0.3333333333333333703, 0.3333333333333333148, 0.3333333333333334259, 0.3333333333333333148, 0.3333333333333334259, 0.3333333333333333148, 0.3333333333333334259, 0.3333333333333334259, 0.3333333333333333703, 0.3333333333333334259, 0.3333333333333333703, 0.3333333333333333703, 0.3333333333333334259, 0.3333333333333333148, 0.3333333333333335369, 0.3333333333333334259, 0.3333333333333333148, 0.3333333333333333703, 0.3333333333333333148, 0.3333333333333334814, 0.3333333333333333703, 0.3333333333333333703, 0.3333333333333332593, 0.3333333333333334814, 0.3333333333333333703, 0.3333333333333333148, 0.3333333333333334259, 0.3333333333333332593, 0.3333333333333334814, 0.3333333333333333703, 0.3333333333333334259, 0.3333333333333333703, 0.3333333333333333148, 0.3333333333333333703, 0.3333333333333334259, 0.3333333333333333703, 0.3333333333333334259, 0.3333333333333333703, 0.3333333333333333703, 0.3333333333333333148, 0.3333333333333333148, 0.3333333333333333703, 0.3333333333333333703, 0.3333333333333333703, 0.3333333333333333703, 0.3333333333333333703, 0.3333333333333333148, 0.3333333333333334814, 0.3333333333333333148, 0.3333333333333334814, 0.3333333333333333703, 0.3333333333333334259, 0.3333333333333334259, 0.3333333333333333703, 0.3333333333333332593, 0.3333333333333333703, 0.3333333333333333703, 0.3333333333333333703, 0.3333333333333333148, 0.3333333333333333703, 0.3333333333333332593, 0.3333333333333334259, 0.3333333333333333703, 0.3333333333333333703),
 ( 0.3333333333333333703, 0.3333333333333333703, 0.3333333333333333703, 0.3333333333333333148, 0.3333333333333334259, 0.3333333333333334814, 0.3333333333333332593, 0.3333333333333332593, 0.3333333333333334814, 0.3333333333333333703, 0.3333333333333333703, 0.3333333333333334259, 0.3333333333333334259, 0.3333333333333334259, 0.3333333333333332593, 0.3333333333333334259, 0.3333333333333334259, 0.3333333333333333703, 0.3333333333333334259, 0.3333333333333332038, 0.3333333333333334259, 0.3333333333333333148, 0.3333333333333334259, 0.3333333333333333703, 0.3333333333333333703, 0.3333333333333334259, 0.3333333333333333148, 0.3333333333333334259, 0.3333333333333333703, 0.3333333333333333703, 0.3333333333333333148, 0.3333333333333334259, 0.3333333333333333703, 0.3333333333333333703, 0.3333333333333333148, 0.3333333333333333148, 0.3333333333333334259, 0.3333333333333333148, 0.3333333333333334259, 0.3333333333333333703, 0.3333333333333333703, 0.3333333333333333703, 0.3333333333333332593, 0.3333333333333334814, 0.3333333333333332593, 0.3333333333333333703, 0.3333333333333333703, 0.3333333333333333703, 0.3333333333333335369, 0.3333333333333332593, 0.3333333333333333703, 0.3333333333333335369, 0.3333333333333333703, 0.3333333333333333703, 0.3333333333333335369, 0.3333333333333333703, 0.3333333333333334259, 0.3333333333333334259, 0.3333333333333333703, 0.3333333333333333703, 0.3333333333333333703, 0.3333333333333333703, 0.3333333333333333703, 0.3333333333333333148, 0.3333333333333334259, 0.3333333333333334814, 0.3333333333333333148, 0.3333333333333333703, 0.3333333333333333148, 0.3333333333333334259, 0.3333333333333332593, 0.3333333333333334259, 0.3333333333333333703, 0.3333333333333334259, 0.3333333333333333703, 0.3333333333333333703, 0.3333333333333333703, 0.3333333333333333148, 0.3333333333333334814, 0.3333333333333332038, 0.3333333333333334259, 0.3333333333333334259, 0.3333333333333333148, 0.3333333333333334259, 0.3333333333333333703, 0.3333333333333333148, 0.3333333333333333703, 0.3333333333333333148, 0.3333333333333334814, 0.3333333333333333148, 0.3333333333333333148, 0.3333333333333334259, 0.3333333333333333148, 0.3333333333333333148, 0.3333333333333334814, 0.3333333333333333148, 0.3333333333333334259, 0.3333333333333333703, 0.3333333333333333148, 0.3333333333333333703, 0.3333333333333334259, 0.3333333333333333148, 0.3333333333333334259, 0.3333333333333333148, 0.3333333333333333703, 0.3333333333333333148, 0.3333333333333333703, 0.3333333333333333703, 0.3333333333333333148, 0.3333333333333334259, 0.3333333333333334259, 0.3333333333333333148, 0.3333333333333333703, 0.3333333333333333703, 0.3333333333333334259, 0.3333333333333333703, 0.3333333333333333703, 0.3333333333333334259, 0.3333333333333333703, 0.3333333333333334259, 0.3333333333333333148, 0.3333333333333333703, 0.3333333333333333148, 0.3333333333333335369, 0.3333333333333333148, 0.3333333333333335369, 0.3333333333333333703, 0.3333333333333332593, 0.3333333333333334259, 0.3333333333333334259, 0.3333333333333333148, 0.3333333333333333703, 0.3333333333333333148, 0.3333333333333335369, 0.3333333333333333148, 0.3333333333333333703, 0.3333333333333333703, 0.3333333333333334259, 0.3333333333333334259, 0.3333333333333333703, 0.3333333333333334259, 0.3333333333333332593, 0.3333333333333334814, 0.3333333333333333148, 0.3333333333333333703, 0.3333333333333333148, 0.3333333333333333148, 0.3333333333333334259, 0.3333333333333332593, 0.3333333333333333148, 0.3333333333333333703, 0.3333333333333333148, 0.3333333333333333703, 0.3333333333333334259, 0.3333333333333333703, 0.3333333333333334259, 0.3333333333333333148, 0.3333333333333333703, 0.3333333333333333703, 0.3333333333333333703, 0.3333333333333333148, 0.3333333333333335369, 0.3333333333333333148, 0.3333333333333333703, 0.3333333333333333148, 0.3333333333333334259, 0.3333333333333334259, 0.3333333333333333703, 0.3333333333333334259, 0.3333333333333333703, 0.3333333333333333703, 0.3333333333333334259, 0.3333333333333333703, 0.3333333333333333703, 0.3333333333333333703, 0.3333333333333334259, 0.3333333333333333148, 0.3333333333333333148, 0.3333333333333335369, 0.3333333333333333148, 0.3333333333333334259, 0.3333333333333333148, 0.3333333333333334259, 0.3333333333333333703, 0.3333333333333333148, 0.3333333333333333148, 0.3333333333333333703, 0.3333333333333333148, 0.3333333333333334259, 0.3333333333333334259, 0.3333333333333332038, 0.3333333333333335369, 0.3333333333333333703, 0.3333333333333334259, 0.3333333333333334259, 0.3333333333333333703, 0.3333333333333334259, 0.3333333333333332593, 0.3333333333333334814, 0.3333333333333333703, 0.3333333333333334259, 0.3333333333333333148, 0.3333333333333333148, 0.3333333333333335369, 0.3333333333333332593, 0.3333333333333333703, 0.3333333333333332593, 0.3333333333333335369, 0.3333333333333333703, 0.3333333333333333703, 0.3333333333333333703, 0.3333333333333334259, 0.3333333333333332593, 0.3333333333333334814, 0.3333333333333332593, 0.3333333333333333703, 0.3333333333333333703, 0.3333333333333333703, 0.3333333333333334259, 0.3333333333333333148, 0.3333333333333334259, 0.3333333333333334259, 0.3333333333333333703, 0.3333333333333333148, 0.3333333333333334259, 0.3333333333333333148, 0.3333333333333333703, 0.3333333333333333148, 0.3333333333333333703, 0.3333333333333333703, 0.3333333333333333148, 0.3333333333333333703, 0.3333333333333333703, 0.3333333333333333703, 0.3333333333333334259, 0.3333333333333333703, 0.3333333333333333703, 0.3333333333333334814, 0.3333333333333332593, 0.3333333333333333703, 0.3333333333333334259, 0.3333333333333333148, 0.3333333333333334259, 0.3333333333333333703, 0.3333333333333334814, 0.3333333333333333703, 0.3333333333333333148, 0.3333333333333334259, 0.3333333333333333703, 0.3333333333333333703, 0.3333333333333333703, 0.3333333333333334259, 0.3333333333333333148, 0.3333333333333334259, 0.3333333333333333148, 0.3333333333333333148, 0.3333333333333335369, 0.3333333333333332038, 0.3333333333333335369, 0.3333333333333333148, 0.3333333333333333703, 0.3333333333333334259, 0.3333333333333333703, 0.3333333333333333148, 0.3333333333333333703, 0.3333333333333334259, 0.3333333333333333703, 0.3333333333333334259, 0.3333333333333333148, 0.3333333333333333703, 0.3333333333333334259, 0.3333333333333333148, 0.3333333333333333703, 0.3333333333333333703, 0.3333333333333333148, 0.3333333333333334259, 0.3333333333333334259, 0.3333333333333333703, 0.3333333333333335369, 0.3333333333333333148, 0.3333333333333333703, 0.3333333333333333703, 0.3333333333333333148, 0.3333333333333333703, 0.3333333333333333703, 0.3333333333333333703, 0.3333333333333333148, 0.3333333333333333703, 0.3333333333333334814, 0.3333333333333333703, 0.3333333333333333703, 0.3333333333333335369, 0.3333333333333333703, 0.3333333333333333703, 0.3333333333333334259, 0.3333333333333334259, 0.3333333333333333703, 0.3333333333333333703, 0.3333333333333333703, 0.3333333333333333703, 0.3333333333333333148, 0.3333333333333334259, 0.3333333333333333703, 0.3333333333333333703, 0.3333333333333333703, 0.3333333333333333148, 0.3333333333333334814, 0.3333333333333333148, 0.3333333333333333148, 0.3333333333333334814, 0.3333333333333333148, 0.3333333333333333148, 0.3333333333333334259, 0.3333333333333333148, 0.3333333333333334259, 0.3333333333333333148, 0.3333333333333334259, 0.3333333333333332593, 0.3333333333333335369, 0.3333333333333333148, 0.3333333333333333148, 0.3333333333333334259, 0.3333333333333333703, 0.3333333333333333703, 0.3333333333333333148, 0.3333333333333334259, 0.3333333333333333148, 0.3333333333333334259, 0.3333333333333333148, 0.3333333333333334259, 0.3333333333333334259, 0.3333333333333333703, 0.3333333333333334259, 0.3333333333333333703, 0.3333333333333333703, 0.3333333333333334259, 0.3333333333333333148, 0.3333333333333335369, 0.3333333333333334259, 0.3333333333333333148, 0.3333333333333333703, 0.3333333333333333148, 0.3333333333333334814, 0.3333333333333333703, 0.3333333333333333703, 0.3333333333333332593, 0.3333333333333334814, 0.3333333333333333703, 0.3333333333333333148, 0.3333333333333334259, 0.3333333333333332593, 0.3333333333333334814, 0.3333333333333333703, 0.3333333333333334259, 0.3333333333333333703, 0.3333333333333333148, 0.3333333333333333703, 0.3333333333333334259, 0.3333333333333333703, 0.3333333333333334259, 0.3333333333333333703, 0.3333333333333333703, 0.3333333333333333148, 0.3333333333333333148, 0.3333333333333333703, 0.3333333333333333703, 0.3333333333333333703, 0.3333333333333333703, 0.3333333333333333703, 0.3333333333333333148, 0.3333333333333334814, 0.3333333333333333148, 0.3333333333333334814, 0.3333333333333333703, 0.3333333333333334259, 0.3333333333333334259, 0.3333333333333333703, 0.3333333333333332593, 0.3333333333333333703, 0.3333333333333333703, 0.3333333333333333703, 0.3333333333333333148, 0.3333333333333333703, 0.3333333333333332593, 0.3333333333333334259, 0.3333333333333333703, 0.3333333333333333703),
 ( 1.000000000000000000, 1.000000000000000000, 1.000000000000000000, 0.9999999999999997780, 1.000000000000000000, 1.000000000000000444, 0.9999999999999996669, 0.9999999999999996669, 1.000000000000000444, 1.000000000000000000, 1.000000000000000000, 1.000000000000000000, 1.000000000000000222, 1.000000000000000222, 0.9999999999999997780, 1.000000000000000000, 1.000000000000000222, 1.000000000000000000, 1.000000000000000222, 0.9999999999999994449, 1.000000000000000222, 0.9999999999999997780, 1.000000000000000444, 1.000000000000000000, 1.000000000000000000, 1.000000000000000222, 0.9999999999999997780, 1.000000000000000222, 1.000000000000000000, 1.000000000000000222, 0.9999999999999997780, 1.000000000000000000, 1.000000000000000000, 0.9999999999999997780, 1.000000000000000000, 1.000000000000000000, 1.000000000000000222, 1.000000000000000000, 0.9999999999999997780, 1.000000000000000222, 0.9999999999999997780, 1.000000000000000000, 0.9999999999999997780, 1.000000000000000444, 0.9999999999999996669, 1.000000000000000222, 1.000000000000000000, 1.000000000000000000, 1.000000000000000444, 0.9999999999999996669, 1.000000000000000222, 1.000000000000000444, 1.000000000000000000, 0.9999999999999997780, 1.000000000000000444, 1.000000000000000222, 1.000000000000000000, 1.000000000000000000, 1.000000000000000222, 1.000000000000000000, 1.000000000000000222, 0.9999999999999997780, 1.000000000000000222, 1.000000000000000000, 1.000000000000000000, 1.000000000000000444, 0.9999999999999996669, 1.000000000000000000, 0.9999999999999997780, 1.000000000000000222, 0.9999999999999996669, 1.000000000000000000, 1.000000000000000222, 0.9999999999999997780, 1.000000000000000444, 0.9999999999999997780, 1.000000000000000000, 0.9999999999999997780, 1.000000000000000222, 0.9999999999999996669, 1.000000000000000000, 1.000000000000000222, 0.9999999999999996669, 1.000000000000000444, 0.9999999999999997780, 1.000000000000000000, 1.000000000000000222, 0.9999999999999996669, 1.000000000000000222, 1.000000000000000000, 0.9999999999999997780, 1.000000000000000222, 0.9999999999999997780, 1.000000000000000000, 1.000000000000000222, 0.9999999999999997780, 1.000000000000000000, 1.000000000000000000, 0.9999999999999997780, 1.000000000000000000, 1.000000000000000222, 0.9999999999999997780, 1.000000000000000000, 1.000000000000000000, 1.000000000000000000, 0.9999999999999997780, 1.000000000000000222, 0.9999999999999997780, 0.9999999999999997780, 1.000000000000000444, 1.000000000000000000, 1.000000000000000000, 0.9999999999999997780, 1.000000000000000222, 1.000000000000000000, 1.000000000000000000, 1.000000000000000000, 1.000000000000000000, 1.000000000000000222, 1.000000000000000222, 0.9999999999999997780, 1.000000000000000000, 0.9999999999999997780, 1.000000000000000444, 0.9999999999999996669, 1.000000000000000666, 1.000000000000000000, 0.9999999999999997780, 1.000000000000000222, 1.000000000000000000, 1.000000000000000000, 1.000000000000000000, 0.9999999999999994449, 1.000000000000000666, 0.9999999999999996669, 1.000000000000000000, 1.000000000000000222, 0.9999999999999997780, 1.000000000000000222, 0.9999999999999997780, 1.000000000000000222, 0.9999999999999996669, 1.000000000000000444, 1.000000000000000000, 1.000000000000000222, 0.9999999999999996669, 1.000000000000000000, 1.000000000000000222, 0.9999999999999997780, 1.000000000000000000, 0.9999999999999997780, 1.000000000000000000, 1.000000000000000000, 1.000000000000000222, 0.9999999999999997780, 1.000000000000000222, 0.9999999999999997780, 1.000000000000000000, 1.000000000000000000, 1.000000000000000222, 0.9999999999999997780, 1.000000000000000444, 1.000000000000000000, 0.9999999999999997780, 1.000000000000000000, 1.000000000000000000, 1.000000000000000222, 0.9999999999999997780, 1.000000000000000222, 1.000000000000000000, 1.000000000000000000, 1.000000000000000000, 1.000000000000000222, 1.000000000000000000, 0.9999999999999997780, 1.000000000000000000, 1.000000000000000000, 1.000000000000000000, 1.000000000000000444, 0.9999999999999996669, 1.000000000000000222, 1.000000000000000000, 1.000000000000000222, 0.9999999999999997780, 1.000000000000000000, 0.9999999999999997780, 1.000000000000000000, 0.9999999999999997780, 1.000000000000000000, 1.000000000000000444, 0.9999999999999994449, 1.000000000000000444, 1.000000000000000000, 1.000000000000000222, 1.000000000000000222, 0.9999999999999997780, 1.000000000000000222, 0.9999999999999997780, 1.000000000000000222, 1.000000000000000222, 1.000000000000000222, 0.9999999999999997780, 1.000000000000000000, 1.000000000000000444, 0.9999999999999996669, 1.000000000000000000, 0.9999999999999997780, 1.000000000000000222, 1.000000000000000222, 1.000000000000000000, 0.9999999999999997780, 1.000000000000000222, 0.9999999999999997780, 1.000000000000000222, 0.9999999999999997780, 0.9999999999999997780, 1.000000000000000000, 1.000000000000000000, 1.000000000000000000, 1.000000000000000000, 1.000000000000000000, 1.000000000000000222, 1.000000000000000000, 1.000000000000000000, 1.000000000000000222, 1.000000000000000000, 0.9999999999999997780, 1.000000000000000000, 1.000000000000000000, 1.000000000000000000, 0.9999999999999997780, 1.000000000000000000, 0.9999999999999997780, 1.000000000000000000, 1.000000000000000222, 0.9999999999999996669, 1.000000000000000444, 1.000000000000000000, 0.9999999999999997780, 1.000000000000000222, 1.000000000000000000, 0.9999999999999997780, 1.000000000000000222, 1.000000000000000000, 1.000000000000000222, 1.000000000000000000, 0.9999999999999997780, 1.000000000000000222, 1.000000000000000000, 1.000000000000000000, 1.000000000000000222, 1.000000000000000000, 1.000000000000000000, 1.000000000000000222, 0.9999999999999997780, 0.9999999999999996669, 1.000000000000000444, 0.9999999999999994449, 1.000000000000000444, 0.9999999999999997780, 1.000000000000000222, 1.000000000000000000, 1.000000000000000000, 1.000000000000000000, 1.000000000000000000, 1.000000000000000444, 0.9999999999999996669, 1.000000000000000444, 1.000000000000000000, 0.9999999999999997780, 1.000000000000000444, 0.9999999999999994449, 1.000000000000000444, 0.9999999999999997780, 0.9999999999999997780, 1.000000000000000222, 1.000000000000000444, 0.9999999999999997780, 1.000000000000000444, 0.9999999999999997780, 1.000000000000000000, 1.000000000000000444, 0.9999999999999997780, 0.9999999999999997780, 1.000000000000000000, 1.000000000000000000, 1.000000000000000000, 0.9999999999999997780, 1.000000000000000444, 1.000000000000000222, 0.9999999999999997780, 1.000000000000000444, 1.000000000000000000, 1.000000000000000222, 1.000000000000000000, 1.000000000000000000, 1.000000000000000222, 0.9999999999999997780, 1.000000000000000222, 1.000000000000000222, 0.9999999999999997780, 1.000000000000000222, 1.000000000000000000, 1.000000000000000000, 1.000000000000000222, 0.9999999999999997780, 1.000000000000000444, 0.9999999999999997780, 0.9999999999999997780, 1.000000000000000222, 0.9999999999999997780, 1.000000000000000000, 1.000000000000000000, 0.9999999999999997780, 1.000000000000000222, 0.9999999999999996669, 1.000000000000000444, 0.9999999999999997780, 1.000000000000000222, 1.000000000000000222, 0.9999999999999997780, 1.000000000000000222, 0.9999999999999997780, 1.000000000000000000, 0.9999999999999997780, 1.000000000000000444, 0.9999999999999996669, 1.000000000000000222, 0.9999999999999996669, 1.000000000000000444, 1.000000000000000000, 0.9999999999999997780, 1.000000000000000222, 0.9999999999999996669, 1.000000000000000222, 1.000000000000000222, 0.9999999999999996669, 1.000000000000000444, 1.000000000000000222, 0.9999999999999997780, 1.000000000000000222, 0.9999999999999997780, 1.000000000000000222, 1.000000000000000000, 1.000000000000000222, 0.9999999999999996669, 1.000000000000000444, 1.000000000000000000, 1.000000000000000000, 1.000000000000000222, 0.9999999999999997780, 0.9999999999999997780, 1.000000000000000444, 1.000000000000000000, 1.000000000000000000, 0.9999999999999996669, 1.000000000000000000, 1.000000000000000222, 1.000000000000000000, 1.000000000000000000, 1.000000000000000222, 0.9999999999999997780, 1.000000000000000000, 0.9999999999999997780, 0.9999999999999997780, 1.000000000000000222, 0.9999999999999997780, 1.000000000000000000, 1.000000000000000000, 0.9999999999999997780, 1.000000000000000222, 1.000000000000000000, 1.000000000000000222, 1.000000000000000000, 1.000000000000000444, 1.000000000000000000, 1.000000000000000000, 0.9999999999999997780, 0.9999999999999997780, 1.000000000000000222, 1.000000000000000000, 1.000000000000000000, 1.000000000000000000, 0.9999999999999997780, 1.000000000000000222, 1.000000000000000000, 1.000000000000000000) ) ) 
 REPRESENTATION_ITEM ( '' )  SURFACE ( )  );
